ISO-10303-21;
HEADER;
/* Generated by software containing ST-Developer
 * from STEP Tools, Inc. (www.steptools.com) 
 */

FILE_DESCRIPTION(
/* description */ (''),
/* implementation_level */ '2;1');

FILE_NAME(
/* name */ 'Lifting_Screw.step',
/* time_stamp */ '2026-10-12T15:47:30-07:00',
/* author */ (''),
/* organization */ (''),
/* preprocessor_version */ 'ST-DEVELOPER v20.2',
/* originating_system */ 'Autodesk Translation Framework v15.15.0.0',
/* authorisation */ '');

FILE_SCHEMA (('AUTOMOTIVE_DESIGN { 1 0 10303 214 3 1 1 }'));
ENDSEC;

DATA;
#10=MECHANICAL_DESIGN_GEOMETRIC_PRESENTATION_REPRESENTATION('',(#84),#88483);
#66=SHAPE_REPRESENTATION_RELATIONSHIP('SRR','None',#88522,#75);
#75=ADVANCED_BREP_SHAPE_REPRESENTATION('',(#119),#88476);
#84=STYLED_ITEM('',(#88574),#119);
#119=MANIFOLD_SOLID_BREP('Body1',#12994);
#171=TOROIDAL_SURFACE('',#13814,19.,1.);
#172=TOROIDAL_SURFACE('',#13823,19.,1.);
#357=FACE_BOUND('',#1869,.T.);
#358=FACE_BOUND('',#1870,.T.);
#359=FACE_BOUND('',#1871,.T.);
#360=FACE_BOUND('',#1872,.T.);
#361=FACE_BOUND('',#1873,.T.);
#362=FACE_BOUND('',#1876,.T.);
#363=FACE_BOUND('',#1877,.T.);
#364=FACE_BOUND('',#1878,.T.);
#365=FACE_BOUND('',#1879,.T.);
#516=PLANE('',#13822);
#517=PLANE('',#13826);
#518=PLANE('',#13827);
#756=B_SPLINE_SURFACE_WITH_KNOTS('',3,3,((#77101,#77102,#77103,#77104,#77105,
#77106,#77107,#77108,#77109,#77110,#77111,#77112,#77113,#77114,#77115,#77116,
#77117,#77118,#77119,#77120,#77121,#77122,#77123,#77124,#77125,#77126,#77127,
#77128,#77129,#77130,#77131,#77132,#77133,#77134,#77135,#77136,#77137,#77138,
#77139,#77140,#77141,#77142,#77143,#77144,#77145,#77146,#77147,#77148,#77149,
#77150,#77151,#77152,#77153,#77154,#77155,#77156,#77157,#77158,#77159,#77160,
#77161,#77162,#77163,#77164,#77165,#77166,#77167,#77168,#77169,#77170,#77171,
#77172,#77173,#77174,#77175,#77176,#77177,#77178,#77179,#77180,#77181,#77182,
#77183,#77184,#77185,#77186,#77187,#77188,#77189,#77190,#77191,#77192,#77193,
#77194,#77195,#77196,#77197,#77198,#77199,#77200,#77201,#77202,#77203,#77204,
#77205,#77206,#77207,#77208,#77209,#77210,#77211,#77212,#77213,#77214,#77215,
#77216,#77217,#77218,#77219,#77220,#77221,#77222,#77223,#77224,#77225,#77226,
#77227,#77228,#77229,#77230,#77231,#77232,#77233,#77234,#77235,#77236,#77237,
#77238,#77239,#77240,#77241,#77242,#77243,#77244,#77245,#77246,#77247,#77248,
#77249,#77250,#77251,#77252,#77253,#77254,#77255,#77256,#77257,#77258,#77259,
#77260,#77261,#77262,#77263,#77264,#77265,#77266,#77267,#77268,#77269,#77270,
#77271,#77272,#77273,#77274,#77275,#77276,#77277,#77278,#77279,#77280,#77281,
#77282,#77283,#77284,#77285,#77286,#77287,#77288,#77289,#77290,#77291,#77292,
#77293,#77294,#77295,#77296,#77297,#77298,#77299,#77300,#77301,#77302,#77303,
#77304,#77305,#77306,#77307,#77308,#77309,#77310,#77311,#77312,#77313,#77314,
#77315,#77316,#77317,#77318,#77319,#77320,#77321,#77322,#77323,#77324,#77325,
#77326,#77327,#77328,#77329,#77330,#77331,#77332,#77333,#77334,#77335,#77336,
#77337,#77338,#77339,#77340,#77341,#77342,#77343,#77344,#77345,#77346,#77347,
#77348,#77349,#77350,#77351,#77352,#77353,#77354,#77355,#77356,#77357,#77358,
#77359,#77360,#77361,#77362,#77363,#77364,#77365,#77366,#77367,#77368,#77369,
#77370,#77371,#77372,#77373,#77374,#77375,#77376,#77377,#77378,#77379,#77380,
#77381,#77382,#77383,#77384,#77385,#77386,#77387,#77388,#77389,#77390,#77391,
#77392,#77393,#77394,#77395,#77396,#77397,#77398,#77399,#77400,#77401,#77402,
#77403,#77404,#77405,#77406,#77407,#77408,#77409,#77410,#77411,#77412,#77413,
#77414,#77415,#77416,#77417,#77418,#77419,#77420,#77421,#77422,#77423,#77424,
#77425,#77426,#77427,#77428,#77429,#77430,#77431,#77432,#77433,#77434,#77435,
#77436,#77437,#77438,#77439,#77440,#77441,#77442,#77443,#77444,#77445,#77446,
#77447,#77448,#77449,#77450,#77451,#77452,#77453,#77454,#77455,#77456,#77457,
#77458,#77459,#77460,#77461,#77462,#77463,#77464,#77465,#77466,#77467,#77468,
#77469,#77470,#77471,#77472,#77473,#77474,#77475,#77476,#77477,#77478,#77479,
#77480,#77481,#77482,#77483,#77484,#77485,#77486,#77487,#77488,#77489,#77490,
#77491,#77492,#77493,#77494,#77495,#77496,#77497,#77498,#77499,#77500,#77501,
#77502,#77503,#77504,#77505,#77506,#77507,#77508,#77509,#77510,#77511,#77512,
#77513,#77514,#77515,#77516,#77517,#77518,#77519,#77520,#77521,#77522,#77523,
#77524,#77525,#77526,#77527,#77528,#77529,#77530,#77531,#77532,#77533,#77534,
#77535,#77536,#77537,#77538,#77539,#77540,#77541,#77542,#77543,#77544,#77545,
#77546,#77547,#77548,#77549,#77550,#77551,#77552,#77553,#77554,#77555,#77556,
#77557,#77558,#77559,#77560,#77561,#77562,#77563,#77564,#77565,#77566,#77567,
#77568,#77569,#77570,#77571,#77572,#77573,#77574,#77575,#77576,#77577,#77578,
#77579,#77580,#77581,#77582,#77583,#77584,#77585,#77586,#77587,#77588,#77589,
#77590,#77591,#77592,#77593,#77594,#77595,#77596,#77597,#77598,#77599,#77600,
#77601,#77602,#77603,#77604,#77605,#77606,#77607,#77608,#77609,#77610,#77611,
#77612,#77613,#77614,#77615,#77616,#77617,#77618,#77619,#77620,#77621,#77622,
#77623,#77624,#77625,#77626,#77627,#77628,#77629,#77630,#77631,#77632,#77633,
#77634,#77635,#77636,#77637,#77638,#77639,#77640,#77641,#77642,#77643,#77644,
#77645,#77646),(#77647,#77648,#77649,#77650,#77651,#77652,#77653,#77654,
#77655,#77656,#77657,#77658,#77659,#77660,#77661,#77662,#77663,#77664,#77665,
#77666,#77667,#77668,#77669,#77670,#77671,#77672,#77673,#77674,#77675,#77676,
#77677,#77678,#77679,#77680,#77681,#77682,#77683,#77684,#77685,#77686,#77687,
#77688,#77689,#77690,#77691,#77692,#77693,#77694,#77695,#77696,#77697,#77698,
#77699,#77700,#77701,#77702,#77703,#77704,#77705,#77706,#77707,#77708,#77709,
#77710,#77711,#77712,#77713,#77714,#77715,#77716,#77717,#77718,#77719,#77720,
#77721,#77722,#77723,#77724,#77725,#77726,#77727,#77728,#77729,#77730,#77731,
#77732,#77733,#77734,#77735,#77736,#77737,#77738,#77739,#77740,#77741,#77742,
#77743,#77744,#77745,#77746,#77747,#77748,#77749,#77750,#77751,#77752,#77753,
#77754,#77755,#77756,#77757,#77758,#77759,#77760,#77761,#77762,#77763,#77764,
#77765,#77766,#77767,#77768,#77769,#77770,#77771,#77772,#77773,#77774,#77775,
#77776,#77777,#77778,#77779,#77780,#77781,#77782,#77783,#77784,#77785,#77786,
#77787,#77788,#77789,#77790,#77791,#77792,#77793,#77794,#77795,#77796,#77797,
#77798,#77799,#77800,#77801,#77802,#77803,#77804,#77805,#77806,#77807,#77808,
#77809,#77810,#77811,#77812,#77813,#77814,#77815,#77816,#77817,#77818,#77819,
#77820,#77821,#77822,#77823,#77824,#77825,#77826,#77827,#77828,#77829,#77830,
#77831,#77832,#77833,#77834,#77835,#77836,#77837,#77838,#77839,#77840,#77841,
#77842,#77843,#77844,#77845,#77846,#77847,#77848,#77849,#77850,#77851,#77852,
#77853,#77854,#77855,#77856,#77857,#77858,#77859,#77860,#77861,#77862,#77863,
#77864,#77865,#77866,#77867,#77868,#77869,#77870,#77871,#77872,#77873,#77874,
#77875,#77876,#77877,#77878,#77879,#77880,#77881,#77882,#77883,#77884,#77885,
#77886,#77887,#77888,#77889,#77890,#77891,#77892,#77893,#77894,#77895,#77896,
#77897,#77898,#77899,#77900,#77901,#77902,#77903,#77904,#77905,#77906,#77907,
#77908,#77909,#77910,#77911,#77912,#77913,#77914,#77915,#77916,#77917,#77918,
#77919,#77920,#77921,#77922,#77923,#77924,#77925,#77926,#77927,#77928,#77929,
#77930,#77931,#77932,#77933,#77934,#77935,#77936,#77937,#77938,#77939,#77940,
#77941,#77942,#77943,#77944,#77945,#77946,#77947,#77948,#77949,#77950,#77951,
#77952,#77953,#77954,#77955,#77956,#77957,#77958,#77959,#77960,#77961,#77962,
#77963,#77964,#77965,#77966,#77967,#77968,#77969,#77970,#77971,#77972,#77973,
#77974,#77975,#77976,#77977,#77978,#77979,#77980,#77981,#77982,#77983,#77984,
#77985,#77986,#77987,#77988,#77989,#77990,#77991,#77992,#77993,#77994,#77995,
#77996,#77997,#77998,#77999,#78000,#78001,#78002,#78003,#78004,#78005,#78006,
#78007,#78008,#78009,#78010,#78011,#78012,#78013,#78014,#78015,#78016,#78017,
#78018,#78019,#78020,#78021,#78022,#78023,#78024,#78025,#78026,#78027,#78028,
#78029,#78030,#78031,#78032,#78033,#78034,#78035,#78036,#78037,#78038,#78039,
#78040,#78041,#78042,#78043,#78044,#78045,#78046,#78047,#78048,#78049,#78050,
#78051,#78052,#78053,#78054,#78055,#78056,#78057,#78058,#78059,#78060,#78061,
#78062,#78063,#78064,#78065,#78066,#78067,#78068,#78069,#78070,#78071,#78072,
#78073,#78074,#78075,#78076,#78077,#78078,#78079,#78080,#78081,#78082,#78083,
#78084,#78085,#78086,#78087,#78088,#78089,#78090,#78091,#78092,#78093,#78094,
#78095,#78096,#78097,#78098,#78099,#78100,#78101,#78102,#78103,#78104,#78105,
#78106,#78107,#78108,#78109,#78110,#78111,#78112,#78113,#78114,#78115,#78116,
#78117,#78118,#78119,#78120,#78121,#78122,#78123,#78124,#78125,#78126,#78127,
#78128,#78129,#78130,#78131,#78132,#78133,#78134,#78135,#78136,#78137,#78138,
#78139,#78140,#78141,#78142,#78143,#78144,#78145,#78146,#78147,#78148,#78149,
#78150,#78151,#78152,#78153,#78154,#78155,#78156,#78157,#78158,#78159,#78160,
#78161,#78162,#78163,#78164,#78165,#78166,#78167,#78168,#78169,#78170,#78171,
#78172,#78173,#78174,#78175,#78176,#78177,#78178,#78179,#78180,#78181,#78182,
#78183,#78184,#78185,#78186,#78187,#78188,#78189,#78190,#78191,#78192),
(#78193,#78194,#78195,#78196,#78197,#78198,#78199,#78200,#78201,#78202,
#78203,#78204,#78205,#78206,#78207,#78208,#78209,#78210,#78211,#78212,#78213,
#78214,#78215,#78216,#78217,#78218,#78219,#78220,#78221,#78222,#78223,#78224,
#78225,#78226,#78227,#78228,#78229,#78230,#78231,#78232,#78233,#78234,#78235,
#78236,#78237,#78238,#78239,#78240,#78241,#78242,#78243,#78244,#78245,#78246,
#78247,#78248,#78249,#78250,#78251,#78252,#78253,#78254,#78255,#78256,#78257,
#78258,#78259,#78260,#78261,#78262,#78263,#78264,#78265,#78266,#78267,#78268,
#78269,#78270,#78271,#78272,#78273,#78274,#78275,#78276,#78277,#78278,#78279,
#78280,#78281,#78282,#78283,#78284,#78285,#78286,#78287,#78288,#78289,#78290,
#78291,#78292,#78293,#78294,#78295,#78296,#78297,#78298,#78299,#78300,#78301,
#78302,#78303,#78304,#78305,#78306,#78307,#78308,#78309,#78310,#78311,#78312,
#78313,#78314,#78315,#78316,#78317,#78318,#78319,#78320,#78321,#78322,#78323,
#78324,#78325,#78326,#78327,#78328,#78329,#78330,#78331,#78332,#78333,#78334,
#78335,#78336,#78337,#78338,#78339,#78340,#78341,#78342,#78343,#78344,#78345,
#78346,#78347,#78348,#78349,#78350,#78351,#78352,#78353,#78354,#78355,#78356,
#78357,#78358,#78359,#78360,#78361,#78362,#78363,#78364,#78365,#78366,#78367,
#78368,#78369,#78370,#78371,#78372,#78373,#78374,#78375,#78376,#78377,#78378,
#78379,#78380,#78381,#78382,#78383,#78384,#78385,#78386,#78387,#78388,#78389,
#78390,#78391,#78392,#78393,#78394,#78395,#78396,#78397,#78398,#78399,#78400,
#78401,#78402,#78403,#78404,#78405,#78406,#78407,#78408,#78409,#78410,#78411,
#78412,#78413,#78414,#78415,#78416,#78417,#78418,#78419,#78420,#78421,#78422,
#78423,#78424,#78425,#78426,#78427,#78428,#78429,#78430,#78431,#78432,#78433,
#78434,#78435,#78436,#78437,#78438,#78439,#78440,#78441,#78442,#78443,#78444,
#78445,#78446,#78447,#78448,#78449,#78450,#78451,#78452,#78453,#78454,#78455,
#78456,#78457,#78458,#78459,#78460,#78461,#78462,#78463,#78464,#78465,#78466,
#78467,#78468,#78469,#78470,#78471,#78472,#78473,#78474,#78475,#78476,#78477,
#78478,#78479,#78480,#78481,#78482,#78483,#78484,#78485,#78486,#78487,#78488,
#78489,#78490,#78491,#78492,#78493,#78494,#78495,#78496,#78497,#78498,#78499,
#78500,#78501,#78502,#78503,#78504,#78505,#78506,#78507,#78508,#78509,#78510,
#78511,#78512,#78513,#78514,#78515,#78516,#78517,#78518,#78519,#78520,#78521,
#78522,#78523,#78524,#78525,#78526,#78527,#78528,#78529,#78530,#78531,#78532,
#78533,#78534,#78535,#78536,#78537,#78538,#78539,#78540,#78541,#78542,#78543,
#78544,#78545,#78546,#78547,#78548,#78549,#78550,#78551,#78552,#78553,#78554,
#78555,#78556,#78557,#78558,#78559,#78560,#78561,#78562,#78563,#78564,#78565,
#78566,#78567,#78568,#78569,#78570,#78571,#78572,#78573,#78574,#78575,#78576,
#78577,#78578,#78579,#78580,#78581,#78582,#78583,#78584,#78585,#78586,#78587,
#78588,#78589,#78590,#78591,#78592,#78593,#78594,#78595,#78596,#78597,#78598,
#78599,#78600,#78601,#78602,#78603,#78604,#78605,#78606,#78607,#78608,#78609,
#78610,#78611,#78612,#78613,#78614,#78615,#78616,#78617,#78618,#78619,#78620,
#78621,#78622,#78623,#78624,#78625,#78626,#78627,#78628,#78629,#78630,#78631,
#78632,#78633,#78634,#78635,#78636,#78637,#78638,#78639,#78640,#78641,#78642,
#78643,#78644,#78645,#78646,#78647,#78648,#78649,#78650,#78651,#78652,#78653,
#78654,#78655,#78656,#78657,#78658,#78659,#78660,#78661,#78662,#78663,#78664,
#78665,#78666,#78667,#78668,#78669,#78670,#78671,#78672,#78673,#78674,#78675,
#78676,#78677,#78678,#78679,#78680,#78681,#78682,#78683,#78684,#78685,#78686,
#78687,#78688,#78689,#78690,#78691,#78692,#78693,#78694,#78695,#78696,#78697,
#78698,#78699,#78700,#78701,#78702,#78703,#78704,#78705,#78706,#78707,#78708,
#78709,#78710,#78711,#78712,#78713,#78714,#78715,#78716,#78717,#78718,#78719,
#78720,#78721,#78722,#78723,#78724,#78725,#78726,#78727,#78728,#78729,#78730,
#78731,#78732,#78733,#78734,#78735,#78736,#78737,#78738),(#78739,#78740,
#78741,#78742,#78743,#78744,#78745,#78746,#78747,#78748,#78749,#78750,#78751,
#78752,#78753,#78754,#78755,#78756,#78757,#78758,#78759,#78760,#78761,#78762,
#78763,#78764,#78765,#78766,#78767,#78768,#78769,#78770,#78771,#78772,#78773,
#78774,#78775,#78776,#78777,#78778,#78779,#78780,#78781,#78782,#78783,#78784,
#78785,#78786,#78787,#78788,#78789,#78790,#78791,#78792,#78793,#78794,#78795,
#78796,#78797,#78798,#78799,#78800,#78801,#78802,#78803,#78804,#78805,#78806,
#78807,#78808,#78809,#78810,#78811,#78812,#78813,#78814,#78815,#78816,#78817,
#78818,#78819,#78820,#78821,#78822,#78823,#78824,#78825,#78826,#78827,#78828,
#78829,#78830,#78831,#78832,#78833,#78834,#78835,#78836,#78837,#78838,#78839,
#78840,#78841,#78842,#78843,#78844,#78845,#78846,#78847,#78848,#78849,#78850,
#78851,#78852,#78853,#78854,#78855,#78856,#78857,#78858,#78859,#78860,#78861,
#78862,#78863,#78864,#78865,#78866,#78867,#78868,#78869,#78870,#78871,#78872,
#78873,#78874,#78875,#78876,#78877,#78878,#78879,#78880,#78881,#78882,#78883,
#78884,#78885,#78886,#78887,#78888,#78889,#78890,#78891,#78892,#78893,#78894,
#78895,#78896,#78897,#78898,#78899,#78900,#78901,#78902,#78903,#78904,#78905,
#78906,#78907,#78908,#78909,#78910,#78911,#78912,#78913,#78914,#78915,#78916,
#78917,#78918,#78919,#78920,#78921,#78922,#78923,#78924,#78925,#78926,#78927,
#78928,#78929,#78930,#78931,#78932,#78933,#78934,#78935,#78936,#78937,#78938,
#78939,#78940,#78941,#78942,#78943,#78944,#78945,#78946,#78947,#78948,#78949,
#78950,#78951,#78952,#78953,#78954,#78955,#78956,#78957,#78958,#78959,#78960,
#78961,#78962,#78963,#78964,#78965,#78966,#78967,#78968,#78969,#78970,#78971,
#78972,#78973,#78974,#78975,#78976,#78977,#78978,#78979,#78980,#78981,#78982,
#78983,#78984,#78985,#78986,#78987,#78988,#78989,#78990,#78991,#78992,#78993,
#78994,#78995,#78996,#78997,#78998,#78999,#79000,#79001,#79002,#79003,#79004,
#79005,#79006,#79007,#79008,#79009,#79010,#79011,#79012,#79013,#79014,#79015,
#79016,#79017,#79018,#79019,#79020,#79021,#79022,#79023,#79024,#79025,#79026,
#79027,#79028,#79029,#79030,#79031,#79032,#79033,#79034,#79035,#79036,#79037,
#79038,#79039,#79040,#79041,#79042,#79043,#79044,#79045,#79046,#79047,#79048,
#79049,#79050,#79051,#79052,#79053,#79054,#79055,#79056,#79057,#79058,#79059,
#79060,#79061,#79062,#79063,#79064,#79065,#79066,#79067,#79068,#79069,#79070,
#79071,#79072,#79073,#79074,#79075,#79076,#79077,#79078,#79079,#79080,#79081,
#79082,#79083,#79084,#79085,#79086,#79087,#79088,#79089,#79090,#79091,#79092,
#79093,#79094,#79095,#79096,#79097,#79098,#79099,#79100,#79101,#79102,#79103,
#79104,#79105,#79106,#79107,#79108,#79109,#79110,#79111,#79112,#79113,#79114,
#79115,#79116,#79117,#79118,#79119,#79120,#79121,#79122,#79123,#79124,#79125,
#79126,#79127,#79128,#79129,#79130,#79131,#79132,#79133,#79134,#79135,#79136,
#79137,#79138,#79139,#79140,#79141,#79142,#79143,#79144,#79145,#79146,#79147,
#79148,#79149,#79150,#79151,#79152,#79153,#79154,#79155,#79156,#79157,#79158,
#79159,#79160,#79161,#79162,#79163,#79164,#79165,#79166,#79167,#79168,#79169,
#79170,#79171,#79172,#79173,#79174,#79175,#79176,#79177,#79178,#79179,#79180,
#79181,#79182,#79183,#79184,#79185,#79186,#79187,#79188,#79189,#79190,#79191,
#79192,#79193,#79194,#79195,#79196,#79197,#79198,#79199,#79200,#79201,#79202,
#79203,#79204,#79205,#79206,#79207,#79208,#79209,#79210,#79211,#79212,#79213,
#79214,#79215,#79216,#79217,#79218,#79219,#79220,#79221,#79222,#79223,#79224,
#79225,#79226,#79227,#79228,#79229,#79230,#79231,#79232,#79233,#79234,#79235,
#79236,#79237,#79238,#79239,#79240,#79241,#79242,#79243,#79244,#79245,#79246,
#79247,#79248,#79249,#79250,#79251,#79252,#79253,#79254,#79255,#79256,#79257,
#79258,#79259,#79260,#79261,#79262,#79263,#79264,#79265,#79266,#79267,#79268,
#79269,#79270,#79271,#79272,#79273,#79274,#79275,#79276,#79277,#79278,#79279,
#79280,#79281,#79282,#79283,#79284)),.UNSPECIFIED.,.F.,.F.,.F.,(4,4),(4,
1,1,1,1,1,1,1,1,1,1,1,1,1,1,1,1,1,1,1,1,1,1,1,1,1,1,1,1,1,1,1,1,1,1,1,1,
1,1,1,1,1,1,1,1,1,1,1,1,1,1,1,1,1,1,1,1,1,1,1,1,1,1,1,1,1,1,1,1,1,1,1,1,
1,1,1,1,1,1,1,1,1,1,1,1,1,1,1,1,1,1,1,1,1,1,1,1,1,1,1,1,1,1,1,1,1,1,1,1,
1,1,1,1,1,1,1,1,1,1,1,1,1,1,1,1,1,1,1,1,1,1,1,1,1,1,1,1,1,1,1,1,1,1,1,1,
1,1,1,1,1,1,1,1,1,1,1,1,1,1,1,1,1,1,1,1,1,1,1,1,1,1,1,1,1,1,1,1,1,1,1,1,
1,1,1,1,1,1,1,1,1,1,1,1,1,1,1,1,1,1,1,1,1,1,1,1,1,1,1,1,1,1,1,1,1,1,1,1,
1,1,1,1,1,1,1,1,1,1,1,1,1,1,1,1,1,1,1,1,1,1,1,1,1,1,1,1,1,1,1,1,1,1,1,1,
1,1,1,1,1,1,1,1,1,1,1,1,1,1,1,1,1,1,1,1,1,1,1,1,1,1,1,1,1,1,1,1,1,1,1,1,
1,1,1,1,1,1,1,1,1,1,1,1,1,1,1,1,1,1,1,1,1,1,1,1,1,1,1,1,1,1,1,1,1,1,1,1,
1,1,1,1,1,1,1,1,1,1,1,1,1,1,1,1,1,1,1,1,1,1,1,1,1,1,1,1,1,1,1,1,1,1,1,1,
1,1,1,1,1,1,1,1,1,1,1,1,1,1,1,1,1,1,1,1,1,1,1,1,1,1,1,1,1,1,1,1,1,1,1,1,
1,1,1,1,1,1,1,1,1,1,1,1,1,1,1,1,1,1,1,1,1,1,1,1,1,1,1,1,1,1,1,1,1,1,1,1,
1,1,1,1,1,1,1,1,1,1,1,1,1,1,1,1,1,1,1,1,1,1,1,1,1,1,1,1,1,1,1,1,1,1,1,1,
1,1,1,1,1,1,1,1,1,1,1,1,1,1,1,1,1,1,1,1,1,1,1,1,1,1,1,1,1,1,1,1,1,1,1,1,
1,1,1,1,1,1,1,1,1,1,1,1,1,1,1,1,1,1,1,1,1,1,1,1,1,1,1,1,1,1,1,1,1,1,1,1,
1,1,4),(-0.000633646794057276,0.135400040464203),(8.30104353460145,8.79990044528941,
9.29867163595186,9.7974428266143,10.2962140172767,11.2937563986016,12.2912987799265,
13.2888411612514,13.7876123519139,14.2863835425763,14.7851547332388,15.2839259239012,
16.2814683052261,16.7802394958886,17.279010686551,18.2765530678759,19.2740954492008,
20.2716378305257,20.7704090211881,21.2691802118506,21.767951402513,22.2667225931755,
23.2642649745004,23.7630361651628,24.2618073558252,25.2593497371501,26.256892118475,
27.2544344997999,27.7532056904624,28.2519768811248,28.7507480717873,29.2495192624497,
30.2470616437746,30.745832834437,31.2446040250995,32.2421464064244,33.2396887877493,
34.2372311690742,34.7360023597366,35.2347735503991,35.7335447410615,36.232315931724,
37.2298583130489,37.7286295037113,38.2274006943737,39.2249430756986,40.2224854570235,
41.2200278383484,41.7187990290109,42.2175702196733,42.7163414103358,43.2151126009982,
44.2126549823231,44.7114261729855,45.210197363648,46.2077397449729,47.2052821262978,
48.2028245076227,48.7015956982851,49.2003668889476,49.69913807961,50.1979092702725,
51.1954516515974,51.6942228422598,52.1929940329222,53.1905364142471,54.188078795572,
55.1856211768969,55.6843923675594,56.1831635582218,56.6819347488843,57.1807059395467,
58.1782483208716,58.677019511534,59.1757907021965,60.1733330835214,61.1708754648463,
62.1684178461712,62.6671890368336,63.1659602274961,63.6647314181585,64.1635026088209,
65.1610449901458,65.6598161808083,66.1585873714707,67.1561297527956,68.1536721341205,
69.1512145154454,69.6499857061079,70.1487568967703,70.6475280874328,71.1462992780952,
72.1438416594201,72.6426128500825,73.141384040745,74.1389264220699,75.1364688033948,
76.1340111847197,76.6327823753821,77.1315535660446,77.630324756707,78.1290959473694,
79.1266383286943,79.6254095193568,80.1241807100192,81.1217230913441,82.119265472669,
83.1168078539939,83.6155790446564,84.1143502353188,84.6131214259813,85.1118926166437,
86.1094349979686,86.608206188631,87.1069773792935,88.1045197606184,89.1020621419433,
90.0996045232682,90.5983757139306,91.097146904593,91.5959180952555,92.0946892859179,
93.0922316672428,93.5910028579053,94.0897740485677,95.0873164298926,96.0848588112175,
97.0824011925424,97.5811723832049,98.0799435738673,98.5787147645297,99.0774859551922,
100.075028336517,100.57379952718,101.072570717842,102.070113099167,103.067655480492,
104.065197861817,104.563969052479,105.062740243142,105.561511433804,106.060282624466,
107.057825005791,107.556596196454,108.055367387116,109.052909768441,110.050452149766,
111.047994531091,111.546765721753,112.045536912416,112.544308103078,113.043079293741,
114.040621675066,114.539392865728,115.03816405639,116.035706437715,117.03324881904,
118.030791200365,118.529562391028,119.02833358169,119.527104772352,120.025875963015,
121.02341834434,121.522189535002,122.020960725665,123.01850310699,124.016045488315,
125.013587869639,125.512359060302,126.011130250964,126.509901441627,127.008672632289,
128.006215013614,128.504986204277,129.003757394939,130.001299776264,130.998842157589,
131.996384538914,132.495155729576,132.993926920239,133.492698110901,133.991469301563,
134.989011682888,135.487782873551,135.986554064213,136.984096445538,137.981638826863,
138.979181208188,139.47795239885,139.976723589513,140.475494780175,140.974265970838,
141.971808352163,142.470579542825,142.969350733487,143.966893114812,144.964435496137,
145.961977877462,146.460749068125,146.959520258787,147.45829144945,147.957062640112,
148.954605021437,149.453376212099,149.952147402762,150.949689784087,151.947232165412,
152.944774546736,153.443545737399,153.942316928061,154.441088118724,154.939859309386,
155.937401690711,156.436172881374,156.934944072036,157.932486453361,158.930028834686,
159.927571216011,160.426342406673,160.925113597336,161.423884787998,161.92265597866,
162.920198359985,163.418969550648,163.91774074131,164.915283122635,165.91282550396,
166.910367885285,167.409139075947,167.90791026661,168.406681457272,168.905452647935,
169.90299502926,170.401766219922,170.900537410584,171.898079791909,172.895622173234,
173.893164554559,174.391935745222,174.890706935884,175.389478126546,175.888249317209,
176.885791698534,177.384562889196,177.883334079859,178.880876461184,179.878418842509,
180.875961223833,181.374732414496,181.873503605158,182.372274795821,182.871045986483,
183.868588367808,184.367359558471,184.866130749133,185.863673130458,186.861215511783,
187.858757893108,188.35752908377,188.856300274433,189.355071465095,189.853842655757,
190.851385037082,191.350156227745,191.848927418407,192.846469799732,193.844012181057,
194.841554562382,195.340325753044,195.839096943707,196.337868134369,196.836639325032,
197.834181706357,198.332952897019,198.831724087681,199.829266469006,200.826808850331,
201.824351231656,202.821893612981,203.819435994306,204.318207184968,204.816978375631,
205.814520756956,206.313291947618,206.812063138281,207.310834328943,207.809605519605,
208.80714790093,209.804690282255,210.80223266358,211.301003854243,211.799775044905,
212.79731742623,213.296088616892,213.794859807555,214.293630998217,214.79240218888,
215.789944570205,216.78748695153,217.785029332854,218.283800523517,218.782571714179,
219.780114095504,220.278885286167,220.777656476829,221.276427667492,221.775198858154,
222.772741239479,223.770283620804,224.767826002129,225.266597192791,225.765368383454,
226.762910764778,227.261681955441,227.760453146103,228.259224336766,228.757995527428,
229.755537908753,230.753080290078,231.750622671403,232.249393862065,232.748165052728,
233.745707434053,234.244478624715,234.743249815378,235.24202100604,235.740792196703,
236.738334578027,237.735876959352,238.733419340677,239.23219053134,239.730961722002,
240.728504103327,241.227275293989,241.726046484652,242.224817675314,242.723588865977,
243.721131247302,244.718673628627,245.716216009951,246.214987200614,246.713758391276,
247.711300772601,248.210071963264,248.708843153926,249.207614344589,249.706385535251,
250.703927916576,251.701470297901,252.699012679226,253.197783869888,253.696555060551,
254.694097441875,255.192868632538,255.6916398232,256.190411013863,256.689182204525,
257.68672458585,258.684266967175,259.6818093485,260.180580539162,260.679351729825,
261.67689411115,262.175665301812,262.674436492475,263.173207683137,263.6719788738,
264.669521255124,265.667063636449,266.664606017774,267.163377208437,267.662148399099,
268.659690780424,269.158461971086,269.657233161749,270.156004352411,270.654775543074,
271.652317924399,272.649860305724,273.647402687048,274.146173877711,274.644945068373,
275.642487449698,276.141258640361,276.640029831023,277.138801021686,277.637572212348,
278.635114593673,279.632656974998,280.630199356323,281.128970546985,281.627741737648,
282.625284118972,283.124055309635,283.622826500297,284.12159769096,284.620368881622,
285.617911262947,286.615453644272,287.612996025597,288.111767216259,288.610538406922,
289.608080788247,290.106851978909,290.605623169572,291.104394360234,291.603165550897,
292.600707932221,293.598250313546,294.595792694871,295.094563885534,295.593335076196,
296.590877457521,297.089648648183,297.588419838846,298.087191029508,298.585962220171,
299.583504601496,300.581046982821,301.578589364145,302.077360554808,302.57613174547,
303.573674126795,304.072445317458,304.57121650812,305.069987698783,305.568758889445,
306.56630127077,307.563843652095,308.56138603342,309.060157224082,309.558928414745,
310.556470796069,311.055241986732,311.554013177394,312.052784368057,312.551555558719,
313.549097940044,314.546640321369,315.544182702694,316.042953893356,316.541725084019,
317.539267465344,318.038038656006,318.536809846669,319.035581037331,319.534352227994,
320.531894609318,321.529436990643,322.526979371968,323.025750562631,323.524521753293,
324.522064134618,325.02083532528,325.519606515943,326.018377706605,326.517148897268,
327.514691278593,328.512233659918,329.509776041242,330.008547231905,330.507318422567,
331.504860803892,332.003631994555,332.502403185217,333.00117437588,333.499945566542,
334.497487947867,335.495030329192,336.492572710517,336.991343901179,337.490115091842,
338.487657473166,338.986428663829,339.485199854491,339.983971045154,340.482742235816,
341.480284617141,342.477826998466,343.475369379791,343.974140570453,344.472911761116,
345.470454142441,345.969225333103,346.467996523766,346.966767714428,347.465538905091,
348.463081286415,349.46062366774,350.458166049065,350.956937239728,351.45570843039,
352.453250811715,352.952022002377,353.45079319304,353.949564383702,354.448335574365,
355.44587795569,356.443420337015,357.440962718339,357.939733909002,358.438505099664,
359.436047480989,359.934818671652,360.433589862314,360.932361052977,361.431132243639,
362.428674624964,363.426217006289,364.423759387614,364.922530578276,365.421301768939,
366.418844150263,366.917615340926,367.416386531588,367.915157722251,368.413928912913,
369.411471294238,370.409013675563,371.406556056888,371.90532724755,372.404098438213,
373.401640819538,373.9004120102,374.399183200863,374.897954391525,375.396725582188,
376.394267963512,377.391810344837,378.389352726162,378.888123916825,379.386895107487,
380.384437488812,380.883208679474,381.381979870137,381.880751060799,382.379522251462,
383.377064632787,384.374607014112,385.372149395436,385.870920586099,386.369691776761,
386.868462967424,387.367297249874),.UNSPECIFIED.);
#757=B_SPLINE_SURFACE_WITH_KNOTS('',3,3,((#79509,#79510,#79511,#79512,#79513,
#79514,#79515,#79516,#79517,#79518,#79519,#79520,#79521,#79522,#79523,#79524,
#79525,#79526,#79527,#79528,#79529,#79530,#79531,#79532,#79533,#79534,#79535,
#79536,#79537,#79538,#79539,#79540,#79541,#79542,#79543,#79544,#79545,#79546,
#79547,#79548,#79549,#79550,#79551,#79552,#79553,#79554,#79555,#79556,#79557,
#79558,#79559,#79560,#79561,#79562,#79563,#79564,#79565,#79566,#79567,#79568,
#79569,#79570,#79571,#79572,#79573,#79574,#79575,#79576,#79577,#79578,#79579,
#79580,#79581,#79582,#79583,#79584,#79585,#79586,#79587,#79588,#79589,#79590,
#79591,#79592,#79593,#79594,#79595,#79596,#79597,#79598,#79599,#79600,#79601,
#79602,#79603,#79604,#79605,#79606,#79607,#79608,#79609,#79610,#79611,#79612,
#79613,#79614,#79615,#79616,#79617,#79618,#79619,#79620,#79621,#79622,#79623,
#79624,#79625,#79626,#79627,#79628,#79629,#79630,#79631,#79632,#79633,#79634,
#79635,#79636,#79637,#79638,#79639,#79640,#79641,#79642,#79643,#79644,#79645,
#79646,#79647,#79648,#79649,#79650,#79651,#79652,#79653,#79654,#79655,#79656,
#79657,#79658,#79659,#79660,#79661,#79662,#79663,#79664,#79665,#79666,#79667,
#79668,#79669,#79670,#79671,#79672,#79673,#79674,#79675,#79676,#79677,#79678,
#79679,#79680,#79681,#79682,#79683,#79684,#79685,#79686,#79687,#79688,#79689,
#79690,#79691,#79692,#79693,#79694,#79695,#79696,#79697,#79698,#79699,#79700,
#79701,#79702,#79703,#79704,#79705,#79706,#79707,#79708,#79709,#79710,#79711,
#79712,#79713,#79714,#79715,#79716,#79717,#79718,#79719,#79720,#79721,#79722,
#79723,#79724,#79725,#79726,#79727,#79728,#79729,#79730,#79731,#79732,#79733,
#79734,#79735,#79736,#79737,#79738,#79739,#79740,#79741,#79742,#79743,#79744,
#79745,#79746,#79747,#79748,#79749,#79750,#79751,#79752,#79753,#79754,#79755,
#79756,#79757,#79758,#79759,#79760,#79761,#79762,#79763,#79764,#79765,#79766,
#79767,#79768,#79769,#79770,#79771,#79772,#79773,#79774,#79775,#79776,#79777,
#79778,#79779,#79780,#79781,#79782,#79783,#79784,#79785,#79786,#79787,#79788,
#79789,#79790,#79791,#79792,#79793,#79794,#79795,#79796,#79797,#79798,#79799,
#79800,#79801,#79802,#79803,#79804,#79805,#79806,#79807,#79808,#79809,#79810,
#79811,#79812,#79813,#79814,#79815,#79816,#79817,#79818,#79819,#79820,#79821,
#79822,#79823,#79824,#79825,#79826,#79827,#79828,#79829,#79830,#79831,#79832,
#79833,#79834,#79835,#79836,#79837,#79838,#79839,#79840,#79841,#79842,#79843,
#79844,#79845,#79846,#79847,#79848,#79849,#79850,#79851,#79852,#79853,#79854,
#79855,#79856,#79857,#79858,#79859,#79860,#79861,#79862,#79863,#79864,#79865,
#79866,#79867,#79868,#79869,#79870,#79871,#79872,#79873,#79874,#79875,#79876,
#79877,#79878,#79879,#79880,#79881,#79882,#79883,#79884,#79885,#79886,#79887,
#79888,#79889,#79890,#79891,#79892,#79893,#79894,#79895,#79896,#79897,#79898,
#79899,#79900,#79901,#79902,#79903,#79904,#79905,#79906,#79907,#79908,#79909,
#79910,#79911,#79912,#79913,#79914,#79915,#79916,#79917,#79918,#79919,#79920,
#79921,#79922,#79923,#79924,#79925,#79926,#79927,#79928,#79929,#79930,#79931,
#79932,#79933,#79934,#79935,#79936,#79937,#79938,#79939,#79940,#79941,#79942,
#79943,#79944,#79945,#79946,#79947,#79948,#79949,#79950,#79951,#79952,#79953,
#79954,#79955,#79956,#79957,#79958,#79959,#79960,#79961,#79962,#79963,#79964,
#79965,#79966,#79967,#79968,#79969,#79970,#79971,#79972,#79973,#79974,#79975,
#79976,#79977,#79978,#79979,#79980,#79981,#79982,#79983,#79984,#79985,#79986,
#79987,#79988,#79989,#79990,#79991,#79992,#79993,#79994,#79995,#79996,#79997,
#79998,#79999,#80000,#80001,#80002,#80003,#80004,#80005,#80006,#80007,#80008,
#80009,#80010,#80011,#80012,#80013,#80014,#80015,#80016,#80017,#80018,#80019,
#80020,#80021,#80022,#80023,#80024,#80025,#80026,#80027,#80028,#80029,#80030,
#80031,#80032,#80033,#80034,#80035,#80036,#80037,#80038,#80039,#80040,#80041,
#80042,#80043,#80044,#80045,#80046,#80047,#80048,#80049,#80050,#80051,#80052,
#80053,#80054),(#80055,#80056,#80057,#80058,#80059,#80060,#80061,#80062,
#80063,#80064,#80065,#80066,#80067,#80068,#80069,#80070,#80071,#80072,#80073,
#80074,#80075,#80076,#80077,#80078,#80079,#80080,#80081,#80082,#80083,#80084,
#80085,#80086,#80087,#80088,#80089,#80090,#80091,#80092,#80093,#80094,#80095,
#80096,#80097,#80098,#80099,#80100,#80101,#80102,#80103,#80104,#80105,#80106,
#80107,#80108,#80109,#80110,#80111,#80112,#80113,#80114,#80115,#80116,#80117,
#80118,#80119,#80120,#80121,#80122,#80123,#80124,#80125,#80126,#80127,#80128,
#80129,#80130,#80131,#80132,#80133,#80134,#80135,#80136,#80137,#80138,#80139,
#80140,#80141,#80142,#80143,#80144,#80145,#80146,#80147,#80148,#80149,#80150,
#80151,#80152,#80153,#80154,#80155,#80156,#80157,#80158,#80159,#80160,#80161,
#80162,#80163,#80164,#80165,#80166,#80167,#80168,#80169,#80170,#80171,#80172,
#80173,#80174,#80175,#80176,#80177,#80178,#80179,#80180,#80181,#80182,#80183,
#80184,#80185,#80186,#80187,#80188,#80189,#80190,#80191,#80192,#80193,#80194,
#80195,#80196,#80197,#80198,#80199,#80200,#80201,#80202,#80203,#80204,#80205,
#80206,#80207,#80208,#80209,#80210,#80211,#80212,#80213,#80214,#80215,#80216,
#80217,#80218,#80219,#80220,#80221,#80222,#80223,#80224,#80225,#80226,#80227,
#80228,#80229,#80230,#80231,#80232,#80233,#80234,#80235,#80236,#80237,#80238,
#80239,#80240,#80241,#80242,#80243,#80244,#80245,#80246,#80247,#80248,#80249,
#80250,#80251,#80252,#80253,#80254,#80255,#80256,#80257,#80258,#80259,#80260,
#80261,#80262,#80263,#80264,#80265,#80266,#80267,#80268,#80269,#80270,#80271,
#80272,#80273,#80274,#80275,#80276,#80277,#80278,#80279,#80280,#80281,#80282,
#80283,#80284,#80285,#80286,#80287,#80288,#80289,#80290,#80291,#80292,#80293,
#80294,#80295,#80296,#80297,#80298,#80299,#80300,#80301,#80302,#80303,#80304,
#80305,#80306,#80307,#80308,#80309,#80310,#80311,#80312,#80313,#80314,#80315,
#80316,#80317,#80318,#80319,#80320,#80321,#80322,#80323,#80324,#80325,#80326,
#80327,#80328,#80329,#80330,#80331,#80332,#80333,#80334,#80335,#80336,#80337,
#80338,#80339,#80340,#80341,#80342,#80343,#80344,#80345,#80346,#80347,#80348,
#80349,#80350,#80351,#80352,#80353,#80354,#80355,#80356,#80357,#80358,#80359,
#80360,#80361,#80362,#80363,#80364,#80365,#80366,#80367,#80368,#80369,#80370,
#80371,#80372,#80373,#80374,#80375,#80376,#80377,#80378,#80379,#80380,#80381,
#80382,#80383,#80384,#80385,#80386,#80387,#80388,#80389,#80390,#80391,#80392,
#80393,#80394,#80395,#80396,#80397,#80398,#80399,#80400,#80401,#80402,#80403,
#80404,#80405,#80406,#80407,#80408,#80409,#80410,#80411,#80412,#80413,#80414,
#80415,#80416,#80417,#80418,#80419,#80420,#80421,#80422,#80423,#80424,#80425,
#80426,#80427,#80428,#80429,#80430,#80431,#80432,#80433,#80434,#80435,#80436,
#80437,#80438,#80439,#80440,#80441,#80442,#80443,#80444,#80445,#80446,#80447,
#80448,#80449,#80450,#80451,#80452,#80453,#80454,#80455,#80456,#80457,#80458,
#80459,#80460,#80461,#80462,#80463,#80464,#80465,#80466,#80467,#80468,#80469,
#80470,#80471,#80472,#80473,#80474,#80475,#80476,#80477,#80478,#80479,#80480,
#80481,#80482,#80483,#80484,#80485,#80486,#80487,#80488,#80489,#80490,#80491,
#80492,#80493,#80494,#80495,#80496,#80497,#80498,#80499,#80500,#80501,#80502,
#80503,#80504,#80505,#80506,#80507,#80508,#80509,#80510,#80511,#80512,#80513,
#80514,#80515,#80516,#80517,#80518,#80519,#80520,#80521,#80522,#80523,#80524,
#80525,#80526,#80527,#80528,#80529,#80530,#80531,#80532,#80533,#80534,#80535,
#80536,#80537,#80538,#80539,#80540,#80541,#80542,#80543,#80544,#80545,#80546,
#80547,#80548,#80549,#80550,#80551,#80552,#80553,#80554,#80555,#80556,#80557,
#80558,#80559,#80560,#80561,#80562,#80563,#80564,#80565,#80566,#80567,#80568,
#80569,#80570,#80571,#80572,#80573,#80574,#80575,#80576,#80577,#80578,#80579,
#80580,#80581,#80582,#80583,#80584,#80585,#80586,#80587,#80588,#80589,#80590,
#80591,#80592,#80593,#80594,#80595,#80596,#80597,#80598,#80599,#80600),
(#80601,#80602,#80603,#80604,#80605,#80606,#80607,#80608,#80609,#80610,
#80611,#80612,#80613,#80614,#80615,#80616,#80617,#80618,#80619,#80620,#80621,
#80622,#80623,#80624,#80625,#80626,#80627,#80628,#80629,#80630,#80631,#80632,
#80633,#80634,#80635,#80636,#80637,#80638,#80639,#80640,#80641,#80642,#80643,
#80644,#80645,#80646,#80647,#80648,#80649,#80650,#80651,#80652,#80653,#80654,
#80655,#80656,#80657,#80658,#80659,#80660,#80661,#80662,#80663,#80664,#80665,
#80666,#80667,#80668,#80669,#80670,#80671,#80672,#80673,#80674,#80675,#80676,
#80677,#80678,#80679,#80680,#80681,#80682,#80683,#80684,#80685,#80686,#80687,
#80688,#80689,#80690,#80691,#80692,#80693,#80694,#80695,#80696,#80697,#80698,
#80699,#80700,#80701,#80702,#80703,#80704,#80705,#80706,#80707,#80708,#80709,
#80710,#80711,#80712,#80713,#80714,#80715,#80716,#80717,#80718,#80719,#80720,
#80721,#80722,#80723,#80724,#80725,#80726,#80727,#80728,#80729,#80730,#80731,
#80732,#80733,#80734,#80735,#80736,#80737,#80738,#80739,#80740,#80741,#80742,
#80743,#80744,#80745,#80746,#80747,#80748,#80749,#80750,#80751,#80752,#80753,
#80754,#80755,#80756,#80757,#80758,#80759,#80760,#80761,#80762,#80763,#80764,
#80765,#80766,#80767,#80768,#80769,#80770,#80771,#80772,#80773,#80774,#80775,
#80776,#80777,#80778,#80779,#80780,#80781,#80782,#80783,#80784,#80785,#80786,
#80787,#80788,#80789,#80790,#80791,#80792,#80793,#80794,#80795,#80796,#80797,
#80798,#80799,#80800,#80801,#80802,#80803,#80804,#80805,#80806,#80807,#80808,
#80809,#80810,#80811,#80812,#80813,#80814,#80815,#80816,#80817,#80818,#80819,
#80820,#80821,#80822,#80823,#80824,#80825,#80826,#80827,#80828,#80829,#80830,
#80831,#80832,#80833,#80834,#80835,#80836,#80837,#80838,#80839,#80840,#80841,
#80842,#80843,#80844,#80845,#80846,#80847,#80848,#80849,#80850,#80851,#80852,
#80853,#80854,#80855,#80856,#80857,#80858,#80859,#80860,#80861,#80862,#80863,
#80864,#80865,#80866,#80867,#80868,#80869,#80870,#80871,#80872,#80873,#80874,
#80875,#80876,#80877,#80878,#80879,#80880,#80881,#80882,#80883,#80884,#80885,
#80886,#80887,#80888,#80889,#80890,#80891,#80892,#80893,#80894,#80895,#80896,
#80897,#80898,#80899,#80900,#80901,#80902,#80903,#80904,#80905,#80906,#80907,
#80908,#80909,#80910,#80911,#80912,#80913,#80914,#80915,#80916,#80917,#80918,
#80919,#80920,#80921,#80922,#80923,#80924,#80925,#80926,#80927,#80928,#80929,
#80930,#80931,#80932,#80933,#80934,#80935,#80936,#80937,#80938,#80939,#80940,
#80941,#80942,#80943,#80944,#80945,#80946,#80947,#80948,#80949,#80950,#80951,
#80952,#80953,#80954,#80955,#80956,#80957,#80958,#80959,#80960,#80961,#80962,
#80963,#80964,#80965,#80966,#80967,#80968,#80969,#80970,#80971,#80972,#80973,
#80974,#80975,#80976,#80977,#80978,#80979,#80980,#80981,#80982,#80983,#80984,
#80985,#80986,#80987,#80988,#80989,#80990,#80991,#80992,#80993,#80994,#80995,
#80996,#80997,#80998,#80999,#81000,#81001,#81002,#81003,#81004,#81005,#81006,
#81007,#81008,#81009,#81010,#81011,#81012,#81013,#81014,#81015,#81016,#81017,
#81018,#81019,#81020,#81021,#81022,#81023,#81024,#81025,#81026,#81027,#81028,
#81029,#81030,#81031,#81032,#81033,#81034,#81035,#81036,#81037,#81038,#81039,
#81040,#81041,#81042,#81043,#81044,#81045,#81046,#81047,#81048,#81049,#81050,
#81051,#81052,#81053,#81054,#81055,#81056,#81057,#81058,#81059,#81060,#81061,
#81062,#81063,#81064,#81065,#81066,#81067,#81068,#81069,#81070,#81071,#81072,
#81073,#81074,#81075,#81076,#81077,#81078,#81079,#81080,#81081,#81082,#81083,
#81084,#81085,#81086,#81087,#81088,#81089,#81090,#81091,#81092,#81093,#81094,
#81095,#81096,#81097,#81098,#81099,#81100,#81101,#81102,#81103,#81104,#81105,
#81106,#81107,#81108,#81109,#81110,#81111,#81112,#81113,#81114,#81115,#81116,
#81117,#81118,#81119,#81120,#81121,#81122,#81123,#81124,#81125,#81126,#81127,
#81128,#81129,#81130,#81131,#81132,#81133,#81134,#81135,#81136,#81137,#81138,
#81139,#81140,#81141,#81142,#81143,#81144,#81145,#81146),(#81147,#81148,
#81149,#81150,#81151,#81152,#81153,#81154,#81155,#81156,#81157,#81158,#81159,
#81160,#81161,#81162,#81163,#81164,#81165,#81166,#81167,#81168,#81169,#81170,
#81171,#81172,#81173,#81174,#81175,#81176,#81177,#81178,#81179,#81180,#81181,
#81182,#81183,#81184,#81185,#81186,#81187,#81188,#81189,#81190,#81191,#81192,
#81193,#81194,#81195,#81196,#81197,#81198,#81199,#81200,#81201,#81202,#81203,
#81204,#81205,#81206,#81207,#81208,#81209,#81210,#81211,#81212,#81213,#81214,
#81215,#81216,#81217,#81218,#81219,#81220,#81221,#81222,#81223,#81224,#81225,
#81226,#81227,#81228,#81229,#81230,#81231,#81232,#81233,#81234,#81235,#81236,
#81237,#81238,#81239,#81240,#81241,#81242,#81243,#81244,#81245,#81246,#81247,
#81248,#81249,#81250,#81251,#81252,#81253,#81254,#81255,#81256,#81257,#81258,
#81259,#81260,#81261,#81262,#81263,#81264,#81265,#81266,#81267,#81268,#81269,
#81270,#81271,#81272,#81273,#81274,#81275,#81276,#81277,#81278,#81279,#81280,
#81281,#81282,#81283,#81284,#81285,#81286,#81287,#81288,#81289,#81290,#81291,
#81292,#81293,#81294,#81295,#81296,#81297,#81298,#81299,#81300,#81301,#81302,
#81303,#81304,#81305,#81306,#81307,#81308,#81309,#81310,#81311,#81312,#81313,
#81314,#81315,#81316,#81317,#81318,#81319,#81320,#81321,#81322,#81323,#81324,
#81325,#81326,#81327,#81328,#81329,#81330,#81331,#81332,#81333,#81334,#81335,
#81336,#81337,#81338,#81339,#81340,#81341,#81342,#81343,#81344,#81345,#81346,
#81347,#81348,#81349,#81350,#81351,#81352,#81353,#81354,#81355,#81356,#81357,
#81358,#81359,#81360,#81361,#81362,#81363,#81364,#81365,#81366,#81367,#81368,
#81369,#81370,#81371,#81372,#81373,#81374,#81375,#81376,#81377,#81378,#81379,
#81380,#81381,#81382,#81383,#81384,#81385,#81386,#81387,#81388,#81389,#81390,
#81391,#81392,#81393,#81394,#81395,#81396,#81397,#81398,#81399,#81400,#81401,
#81402,#81403,#81404,#81405,#81406,#81407,#81408,#81409,#81410,#81411,#81412,
#81413,#81414,#81415,#81416,#81417,#81418,#81419,#81420,#81421,#81422,#81423,
#81424,#81425,#81426,#81427,#81428,#81429,#81430,#81431,#81432,#81433,#81434,
#81435,#81436,#81437,#81438,#81439,#81440,#81441,#81442,#81443,#81444,#81445,
#81446,#81447,#81448,#81449,#81450,#81451,#81452,#81453,#81454,#81455,#81456,
#81457,#81458,#81459,#81460,#81461,#81462,#81463,#81464,#81465,#81466,#81467,
#81468,#81469,#81470,#81471,#81472,#81473,#81474,#81475,#81476,#81477,#81478,
#81479,#81480,#81481,#81482,#81483,#81484,#81485,#81486,#81487,#81488,#81489,
#81490,#81491,#81492,#81493,#81494,#81495,#81496,#81497,#81498,#81499,#81500,
#81501,#81502,#81503,#81504,#81505,#81506,#81507,#81508,#81509,#81510,#81511,
#81512,#81513,#81514,#81515,#81516,#81517,#81518,#81519,#81520,#81521,#81522,
#81523,#81524,#81525,#81526,#81527,#81528,#81529,#81530,#81531,#81532,#81533,
#81534,#81535,#81536,#81537,#81538,#81539,#81540,#81541,#81542,#81543,#81544,
#81545,#81546,#81547,#81548,#81549,#81550,#81551,#81552,#81553,#81554,#81555,
#81556,#81557,#81558,#81559,#81560,#81561,#81562,#81563,#81564,#81565,#81566,
#81567,#81568,#81569,#81570,#81571,#81572,#81573,#81574,#81575,#81576,#81577,
#81578,#81579,#81580,#81581,#81582,#81583,#81584,#81585,#81586,#81587,#81588,
#81589,#81590,#81591,#81592,#81593,#81594,#81595,#81596,#81597,#81598,#81599,
#81600,#81601,#81602,#81603,#81604,#81605,#81606,#81607,#81608,#81609,#81610,
#81611,#81612,#81613,#81614,#81615,#81616,#81617,#81618,#81619,#81620,#81621,
#81622,#81623,#81624,#81625,#81626,#81627,#81628,#81629,#81630,#81631,#81632,
#81633,#81634,#81635,#81636,#81637,#81638,#81639,#81640,#81641,#81642,#81643,
#81644,#81645,#81646,#81647,#81648,#81649,#81650,#81651,#81652,#81653,#81654,
#81655,#81656,#81657,#81658,#81659,#81660,#81661,#81662,#81663,#81664,#81665,
#81666,#81667,#81668,#81669,#81670,#81671,#81672,#81673,#81674,#81675,#81676,
#81677,#81678,#81679,#81680,#81681,#81682,#81683,#81684,#81685,#81686,#81687,
#81688,#81689,#81690,#81691,#81692)),.UNSPECIFIED.,.F.,.F.,.F.,(4,4),(4,
1,1,1,1,1,1,1,1,1,1,1,1,1,1,1,1,1,1,1,1,1,1,1,1,1,1,1,1,1,1,1,1,1,1,1,1,
1,1,1,1,1,1,1,1,1,1,1,1,1,1,1,1,1,1,1,1,1,1,1,1,1,1,1,1,1,1,1,1,1,1,1,1,
1,1,1,1,1,1,1,1,1,1,1,1,1,1,1,1,1,1,1,1,1,1,1,1,1,1,1,1,1,1,1,1,1,1,1,1,
1,1,1,1,1,1,1,1,1,1,1,1,1,1,1,1,1,1,1,1,1,1,1,1,1,1,1,1,1,1,1,1,1,1,1,1,
1,1,1,1,1,1,1,1,1,1,1,1,1,1,1,1,1,1,1,1,1,1,1,1,1,1,1,1,1,1,1,1,1,1,1,1,
1,1,1,1,1,1,1,1,1,1,1,1,1,1,1,1,1,1,1,1,1,1,1,1,1,1,1,1,1,1,1,1,1,1,1,1,
1,1,1,1,1,1,1,1,1,1,1,1,1,1,1,1,1,1,1,1,1,1,1,1,1,1,1,1,1,1,1,1,1,1,1,1,
1,1,1,1,1,1,1,1,1,1,1,1,1,1,1,1,1,1,1,1,1,1,1,1,1,1,1,1,1,1,1,1,1,1,1,1,
1,1,1,1,1,1,1,1,1,1,1,1,1,1,1,1,1,1,1,1,1,1,1,1,1,1,1,1,1,1,1,1,1,1,1,1,
1,1,1,1,1,1,1,1,1,1,1,1,1,1,1,1,1,1,1,1,1,1,1,1,1,1,1,1,1,1,1,1,1,1,1,1,
1,1,1,1,1,1,1,1,1,1,1,1,1,1,1,1,1,1,1,1,1,1,1,1,1,1,1,1,1,1,1,1,1,1,1,1,
1,1,1,1,1,1,1,1,1,1,1,1,1,1,1,1,1,1,1,1,1,1,1,1,1,1,1,1,1,1,1,1,1,1,1,1,
1,1,1,1,1,1,1,1,1,1,1,1,1,1,1,1,1,1,1,1,1,1,1,1,1,1,1,1,1,1,1,1,1,1,1,1,
1,1,1,1,1,1,1,1,1,1,1,1,1,1,1,1,1,1,1,1,1,1,1,1,1,1,1,1,1,1,1,1,1,1,1,1,
1,1,1,1,1,1,1,1,1,1,1,1,1,1,1,1,1,1,1,1,1,1,1,1,1,1,1,1,1,1,1,1,1,1,1,1,
1,1,4),(-0.000757559510207718,0.132914936587996),(11.614729191302,12.1138040384816,
12.612575229144,13.1113464198064,13.6101176104689,14.6076599917938,15.6052023731187,
16.6027447544436,17.101515945106,17.6002871357685,18.0990583264309,18.5978295170934,
19.5953718984182,20.0941430890807,20.5929142797431,21.590456661068,22.5879990423929,
23.5855414237178,24.0843126143803,24.5830838050427,25.0818549957052,25.5806261863676,
26.5781685676925,27.0769397583549,27.5757109490174,28.5732533303423,29.5707957116672,
30.5683380929921,31.0671092836545,31.565880474317,32.0646516649794,32.5634228556418,
33.5609652369667,34.0597364276292,34.5585076182916,35.5560499996165,36.5535923809414,
37.5511347622663,38.0499059529288,38.5486771435912,39.0474483342537,39.5462195249161,
40.543761906241,41.0425330969034,41.5413042875659,42.5388466688908,43.5363890502157,
44.5339314315406,45.032702622203,45.5314738128654,46.0302450035279,46.5290161941903,
47.5265585755152,48.0253297661777,48.5241009568401,49.521643338165,50.5191857194899,
51.5167281008148,52.0154992914772,52.5142704821397,53.0130416728021,53.5118128634646,
54.5093552447895,55.0081264354519,55.5068976261144,56.5044400074393,57.5019823887642,
58.4995247700891,58.9982959607515,59.4970671514139,59.9958383420764,60.4946095327388,
61.4921519140637,61.9909231047262,62.4896942953886,63.4872366767135,64.4847790580384,
65.4823214393633,65.9810926300257,66.4798638206882,66.9786350113506,67.4774062020131,
68.474948583338,68.9737197740004,69.4724909646629,70.4700333459878,71.4675757273126,
72.4651181086375,72.9638892993,73.4626604899624,73.9614316806249,74.4602028712873,
75.4577452526122,75.9565164432747,76.4552876339371,77.452830015262,78.4503723965869,
79.4479147779118,79.9466859685742,80.4454571592367,80.9442283498991,81.4429995405616,
82.4405419218865,82.9393131125489,83.4380843032114,84.4356266845362,85.4331690658612,
86.430711447186,86.9294826378485,87.4282538285109,87.9270250191734,88.4257962098358,
89.4233385911607,89.9221097818232,90.4208809724856,91.4184233538105,92.4159657351354,
93.4135081164603,93.9122793071227,94.4110504977852,94.9098216884476,95.4085928791101,
96.406135260435,96.9049064510974,97.4036776417599,98.4012200230847,99.3987624044096,
100.396304785735,100.895075976397,101.393847167059,101.892618357722,102.391389548384,
103.388931929709,103.887703120372,104.386474311034,105.384016692359,106.381559073684,
107.379101455009,107.877872645671,108.376643836334,108.875415026996,109.374186217659,
110.371728598983,110.870499789646,111.369270980308,112.366813361633,113.364355742958,
114.361898124283,114.860669314945,115.359440505608,115.85821169627,116.356982886933,
117.354525268258,117.85329645892,118.352067649583,119.349610030907,120.347152412232,
121.344694793557,121.84346598422,122.342237174882,122.841008365545,123.339779556207,
124.337321937532,124.836093128194,125.334864318857,126.332406700182,127.329949081507,
128.327491462832,128.826262653494,129.325033844156,129.823805034819,130.322576225481,
131.320118606806,131.818889797469,132.317660988131,133.315203369456,134.312745750781,
135.310288132106,135.809059322768,136.307830513431,136.806601704093,137.305372894756,
138.30291527608,138.801686466743,139.300457657405,140.29800003873,141.295542420055,
142.29308480138,142.791855992042,143.290627182705,143.789398373367,144.28816956403,
145.285711945355,145.784483136017,146.28325432668,147.280796708004,148.278339089329,
149.275881470654,149.774652661317,150.273423851979,150.772195042642,151.270966233304,
152.268508614629,152.767279805291,153.266050995954,154.263593377279,155.261135758604,
156.258678139929,156.757449330591,157.256220521253,157.754991711916,158.253762902578,
159.251305283903,159.750076474566,160.248847665228,161.246390046553,162.243932427878,
163.241474809203,163.740245999865,164.239017190528,164.73778838119,165.236559571853,
166.234101953177,166.73287314384,167.231644334502,168.229186715827,169.226729097152,
170.224271478477,170.723042669139,171.221813859802,171.720585050464,172.219356241127,
173.216898622452,173.715669813114,174.214441003777,175.211983385101,176.209525766426,
177.207068147751,177.705839338414,178.204610529076,178.703381719739,179.202152910401,
180.199695291726,180.698466482388,181.197237673051,182.194780054376,183.192322435701,
184.189864817025,184.688636007688,185.18740719835,185.686178389013,186.184949579675,
187.182491961,187.681263151663,188.180034342325,189.17757672365,190.175119104975,
191.1726614863,191.671432676962,192.170203867625,192.668975058287,193.16774624895,
194.165288630274,194.664059820937,195.162831011599,196.160373392924,197.157915774249,
198.155458155574,198.654229346236,199.153000536899,199.651771727561,200.150542918224,
201.148085299549,201.646856490211,202.145627680874,203.143170062198,204.140712443523,
205.138254824848,206.135797206173,207.133339587498,207.63211077816,208.130881968823,
209.128424350148,209.62719554081,210.125966731473,210.624737922135,211.123509112798,
212.121051494122,213.118593875447,214.116136256772,214.614907447435,215.113678638097,
216.111221019422,216.609992210084,217.108763400747,217.607534591409,218.106305782072,
219.103848163397,220.101390544722,221.098932926047,221.597704116709,222.096475307371,
223.094017688696,223.592788879359,224.091560070021,224.590331260684,225.089102451346,
226.086644832671,227.084187213996,228.081729595321,228.580500785983,229.079271976646,
230.076814357971,230.575585548633,231.074356739295,231.573127929958,232.07189912062,
233.069441501945,234.06698388327,235.064526264595,235.563297455257,236.06206864592,
237.059611027245,237.558382217907,238.05715340857,238.555924599232,239.054695789895,
240.052238171219,241.049780552544,242.047322933869,242.546094124532,243.044865315194,
244.042407696519,244.541178887181,245.039950077844,245.538721268506,246.037492459169,
247.035034840494,248.032577221819,249.030119603143,249.528890793806,250.027661984468,
251.025204365793,251.523975556456,252.022746747118,252.521517937781,253.020289128443,
254.017831509768,255.015373891093,256.012916272418,256.51168746308,257.010458653743,
258.008001035068,258.50677222573,259.005543416392,259.504314607055,260.003085797717,
261.000628179042,261.998170560367,262.995712941692,263.494484132354,263.993255323017,
264.990797704342,265.489568895004,265.988340085667,266.487111276329,266.985882466992,
267.983424848316,268.980967229641,269.978509610966,270.477280801629,270.976051992291,
271.973594373616,272.472365564278,272.971136754941,273.469907945603,273.968679136266,
274.966221517591,275.963763898916,276.96130628024,277.460077470903,277.958848661565,
278.95639104289,279.455162233553,279.953933424215,280.452704614878,280.95147580554,
281.949018186865,282.94656056819,283.944102949515,284.442874140177,284.94164533084,
285.939187712165,286.437958902827,286.936730093489,287.435501284152,287.934272474814,
288.931814856139,289.929357237464,290.926899618789,291.425670809451,291.924442000114,
292.921984381439,293.420755572101,293.919526762764,294.418297953426,294.917069144089,
295.914611525413,296.912153906738,297.909696288063,298.408467478726,298.907238669388,
299.904781050713,300.403552241375,300.902323432038,301.4010946227,301.899865813363,
302.897408194688,303.894950576013,304.892492957337,305.391264148,305.890035338662,
306.887577719987,307.38634891065,307.885120101312,308.383891291975,308.882662482637,
309.880204863962,310.877747245287,311.875289626612,312.374060817274,312.872832007937,
313.870374389261,314.369145579924,314.867916770586,315.366687961249,315.865459151911,
316.863001533236,317.860543914561,318.858086295886,319.356857486548,319.855628677211,
320.853171058536,321.351942249198,321.850713439861,322.349484630523,322.848255821186,
323.84579820251,324.843340583835,325.84088296516,326.339654155823,326.838425346485,
327.83596772781,328.334738918472,328.833510109135,329.332281299797,329.83105249046,
330.828594871785,331.82613725311,332.823679634434,333.322450825097,333.821222015759,
334.818764397084,335.317535587747,335.816306778409,336.315077969072,336.813849159734,
337.811391541059,338.808933922384,339.806476303709,340.305247494371,340.804018685034,
341.801561066358,342.300332257021,342.799103447683,343.297874638346,343.796645829008,
344.794188210333,345.791730591658,346.789272972983,347.288044163645,347.786815354308,
348.784357735633,349.283128926295,349.781900116958,350.28067130762,350.779442498283,
351.776984879607,352.774527260932,353.772069642257,354.27084083292,354.769612023582,
355.767154404907,356.265925595569,356.764696786232,357.263467976894,357.762239167557,
358.759781548882,359.757323930207,360.754866311531,361.253637502194,361.752408692856,
362.749951074181,363.248722264844,363.747493455506,364.246264646169,364.745035836831,
365.742578218156,366.740120599481,367.737662980806,368.236434171468,368.735205362131,
369.732747743455,370.231518934118,370.73029012478,371.229061315443,371.727832506105,
372.72537488743,373.722917268755,374.72045965008,375.219230840742,375.718002031405,
376.71554441273,377.214315603392,377.713086794055,378.211857984717,378.710629175379,
379.708171556704,380.705713938029,381.703256319354,382.202027510017,382.700798700679,
383.698341082004,384.197112272666,384.695883463329,385.194654653991,385.693425844654,
386.690968225979,387.688510607304,388.686052988628,389.184824179291,389.683595369953,
390.182366560616,390.681747047565),.UNSPECIFIED.);
#1122=FACE_OUTER_BOUND('',#1798,.T.);
#1123=FACE_OUTER_BOUND('',#1799,.T.);
#1124=FACE_OUTER_BOUND('',#1800,.T.);
#1125=FACE_OUTER_BOUND('',#1801,.T.);
#1126=FACE_OUTER_BOUND('',#1802,.T.);
#1127=FACE_OUTER_BOUND('',#1803,.T.);
#1128=FACE_OUTER_BOUND('',#1804,.T.);
#1129=FACE_OUTER_BOUND('',#1805,.T.);
#1130=FACE_OUTER_BOUND('',#1806,.T.);
#1131=FACE_OUTER_BOUND('',#1807,.T.);
#1132=FACE_OUTER_BOUND('',#1808,.T.);
#1133=FACE_OUTER_BOUND('',#1809,.T.);
#1134=FACE_OUTER_BOUND('',#1810,.T.);
#1135=FACE_OUTER_BOUND('',#1811,.T.);
#1136=FACE_OUTER_BOUND('',#1812,.T.);
#1137=FACE_OUTER_BOUND('',#1813,.T.);
#1138=FACE_OUTER_BOUND('',#1814,.T.);
#1139=FACE_OUTER_BOUND('',#1815,.T.);
#1140=FACE_OUTER_BOUND('',#1816,.T.);
#1141=FACE_OUTER_BOUND('',#1817,.T.);
#1142=FACE_OUTER_BOUND('',#1818,.T.);
#1143=FACE_OUTER_BOUND('',#1819,.T.);
#1144=FACE_OUTER_BOUND('',#1820,.T.);
#1145=FACE_OUTER_BOUND('',#1821,.T.);
#1146=FACE_OUTER_BOUND('',#1822,.T.);
#1147=FACE_OUTER_BOUND('',#1823,.T.);
#1148=FACE_OUTER_BOUND('',#1824,.T.);
#1149=FACE_OUTER_BOUND('',#1825,.T.);
#1150=FACE_OUTER_BOUND('',#1826,.T.);
#1151=FACE_OUTER_BOUND('',#1827,.T.);
#1152=FACE_OUTER_BOUND('',#1828,.T.);
#1153=FACE_OUTER_BOUND('',#1829,.T.);
#1154=FACE_OUTER_BOUND('',#1830,.T.);
#1155=FACE_OUTER_BOUND('',#1831,.T.);
#1156=FACE_OUTER_BOUND('',#1832,.T.);
#1157=FACE_OUTER_BOUND('',#1833,.T.);
#1158=FACE_OUTER_BOUND('',#1834,.T.);
#1159=FACE_OUTER_BOUND('',#1835,.T.);
#1160=FACE_OUTER_BOUND('',#1836,.T.);
#1161=FACE_OUTER_BOUND('',#1837,.T.);
#1162=FACE_OUTER_BOUND('',#1838,.T.);
#1163=FACE_OUTER_BOUND('',#1839,.T.);
#1164=FACE_OUTER_BOUND('',#1840,.T.);
#1165=FACE_OUTER_BOUND('',#1841,.T.);
#1166=FACE_OUTER_BOUND('',#1842,.T.);
#1167=FACE_OUTER_BOUND('',#1843,.T.);
#1168=FACE_OUTER_BOUND('',#1844,.T.);
#1169=FACE_OUTER_BOUND('',#1845,.T.);
#1170=FACE_OUTER_BOUND('',#1846,.T.);
#1171=FACE_OUTER_BOUND('',#1847,.T.);
#1172=FACE_OUTER_BOUND('',#1848,.T.);
#1173=FACE_OUTER_BOUND('',#1849,.T.);
#1174=FACE_OUTER_BOUND('',#1850,.T.);
#1175=FACE_OUTER_BOUND('',#1851,.T.);
#1176=FACE_OUTER_BOUND('',#1852,.T.);
#1177=FACE_OUTER_BOUND('',#1853,.T.);
#1178=FACE_OUTER_BOUND('',#1854,.T.);
#1179=FACE_OUTER_BOUND('',#1855,.T.);
#1180=FACE_OUTER_BOUND('',#1856,.T.);
#1181=FACE_OUTER_BOUND('',#1857,.T.);
#1182=FACE_OUTER_BOUND('',#1858,.T.);
#1183=FACE_OUTER_BOUND('',#1859,.T.);
#1184=FACE_OUTER_BOUND('',#1860,.T.);
#1185=FACE_OUTER_BOUND('',#1861,.T.);
#1186=FACE_OUTER_BOUND('',#1862,.T.);
#1187=FACE_OUTER_BOUND('',#1863,.T.);
#1188=FACE_OUTER_BOUND('',#1864,.T.);
#1189=FACE_OUTER_BOUND('',#1865,.T.);
#1190=FACE_OUTER_BOUND('',#1866,.T.);
#1191=FACE_OUTER_BOUND('',#1867,.T.);
#1192=FACE_OUTER_BOUND('',#1868,.T.);
#1193=FACE_OUTER_BOUND('',#1874,.T.);
#1194=FACE_OUTER_BOUND('',#1875,.T.);
#1195=FACE_OUTER_BOUND('',#1880,.T.);
#1798=EDGE_LOOP('',(#10092,#10093,#10094,#10095));
#1799=EDGE_LOOP('',(#10096,#10097,#10098,#10099,#10100,#10101));
#1800=EDGE_LOOP('',(#10102,#10103,#10104,#10105,#10106,#10107));
#1801=EDGE_LOOP('',(#10108,#10109,#10110,#10111,#10112,#10113));
#1802=EDGE_LOOP('',(#10114,#10115,#10116,#10117,#10118,#10119));
#1803=EDGE_LOOP('',(#10120,#10121,#10122,#10123,#10124,#10125));
#1804=EDGE_LOOP('',(#10126,#10127,#10128,#10129,#10130,#10131));
#1805=EDGE_LOOP('',(#10132,#10133,#10134,#10135,#10136,#10137));
#1806=EDGE_LOOP('',(#10138,#10139,#10140,#10141,#10142,#10143));
#1807=EDGE_LOOP('',(#10144,#10145,#10146,#10147,#10148,#10149));
#1808=EDGE_LOOP('',(#10150,#10151,#10152,#10153,#10154,#10155));
#1809=EDGE_LOOP('',(#10156,#10157,#10158,#10159,#10160,#10161));
#1810=EDGE_LOOP('',(#10162,#10163,#10164,#10165,#10166,#10167));
#1811=EDGE_LOOP('',(#10168,#10169,#10170,#10171,#10172,#10173));
#1812=EDGE_LOOP('',(#10174,#10175,#10176,#10177,#10178,#10179));
#1813=EDGE_LOOP('',(#10180,#10181,#10182,#10183,#10184,#10185));
#1814=EDGE_LOOP('',(#10186,#10187,#10188,#10189,#10190,#10191));
#1815=EDGE_LOOP('',(#10192,#10193,#10194,#10195,#10196,#10197));
#1816=EDGE_LOOP('',(#10198,#10199,#10200,#10201,#10202,#10203));
#1817=EDGE_LOOP('',(#10204,#10205,#10206,#10207,#10208,#10209));
#1818=EDGE_LOOP('',(#10210,#10211,#10212,#10213,#10214,#10215));
#1819=EDGE_LOOP('',(#10216,#10217,#10218,#10219,#10220,#10221));
#1820=EDGE_LOOP('',(#10222,#10223,#10224,#10225,#10226,#10227));
#1821=EDGE_LOOP('',(#10228,#10229,#10230,#10231,#10232,#10233));
#1822=EDGE_LOOP('',(#10234,#10235,#10236,#10237,#10238,#10239));
#1823=EDGE_LOOP('',(#10240,#10241,#10242,#10243,#10244,#10245));
#1824=EDGE_LOOP('',(#10246,#10247,#10248,#10249,#10250,#10251));
#1825=EDGE_LOOP('',(#10252,#10253,#10254,#10255,#10256,#10257));
#1826=EDGE_LOOP('',(#10258,#10259,#10260,#10261,#10262,#10263));
#1827=EDGE_LOOP('',(#10264,#10265,#10266,#10267,#10268,#10269));
#1828=EDGE_LOOP('',(#10270,#10271,#10272,#10273,#10274,#10275));
#1829=EDGE_LOOP('',(#10276,#10277,#10278,#10279,#10280,#10281));
#1830=EDGE_LOOP('',(#10282,#10283,#10284,#10285,#10286,#10287));
#1831=EDGE_LOOP('',(#10288,#10289,#10290,#10291,#10292,#10293));
#1832=EDGE_LOOP('',(#10294,#10295,#10296,#10297,#10298,#10299));
#1833=EDGE_LOOP('',(#10300,#10301,#10302,#10303,#10304,#10305));
#1834=EDGE_LOOP('',(#10306,#10307,#10308,#10309,#10310,#10311));
#1835=EDGE_LOOP('',(#10312,#10313,#10314,#10315,#10316,#10317));
#1836=EDGE_LOOP('',(#10318,#10319,#10320,#10321,#10322,#10323));
#1837=EDGE_LOOP('',(#10324,#10325,#10326,#10327,#10328,#10329));
#1838=EDGE_LOOP('',(#10330,#10331,#10332,#10333,#10334,#10335));
#1839=EDGE_LOOP('',(#10336,#10337,#10338,#10339,#10340,#10341));
#1840=EDGE_LOOP('',(#10342,#10343,#10344,#10345,#10346,#10347));
#1841=EDGE_LOOP('',(#10348,#10349,#10350,#10351,#10352,#10353));
#1842=EDGE_LOOP('',(#10354,#10355,#10356,#10357,#10358,#10359));
#1843=EDGE_LOOP('',(#10360,#10361,#10362,#10363,#10364,#10365));
#1844=EDGE_LOOP('',(#10366,#10367,#10368,#10369,#10370,#10371));
#1845=EDGE_LOOP('',(#10372,#10373,#10374,#10375,#10376,#10377));
#1846=EDGE_LOOP('',(#10378,#10379,#10380,#10381,#10382,#10383));
#1847=EDGE_LOOP('',(#10384,#10385,#10386,#10387,#10388,#10389));
#1848=EDGE_LOOP('',(#10390,#10391,#10392,#10393,#10394,#10395));
#1849=EDGE_LOOP('',(#10396,#10397,#10398,#10399,#10400,#10401));
#1850=EDGE_LOOP('',(#10402,#10403,#10404,#10405,#10406,#10407));
#1851=EDGE_LOOP('',(#10408,#10409,#10410,#10411,#10412,#10413));
#1852=EDGE_LOOP('',(#10414,#10415,#10416,#10417,#10418,#10419));
#1853=EDGE_LOOP('',(#10420,#10421,#10422,#10423,#10424,#10425));
#1854=EDGE_LOOP('',(#10426,#10427,#10428,#10429,#10430,#10431));
#1855=EDGE_LOOP('',(#10432,#10433,#10434,#10435,#10436,#10437));
#1856=EDGE_LOOP('',(#10438,#10439,#10440,#10441,#10442,#10443));
#1857=EDGE_LOOP('',(#10444,#10445,#10446,#10447,#10448,#10449));
#1858=EDGE_LOOP('',(#10450,#10451,#10452,#10453,#10454,#10455,#10456,#10457,
#10458,#10459,#10460,#10461,#10462,#10463,#10464,#10465,#10466,#10467,#10468,
#10469,#10470,#10471,#10472,#10473,#10474,#10475,#10476,#10477,#10478,#10479,
#10480,#10481,#10482,#10483,#10484,#10485,#10486,#10487,#10488,#10489,#10490,
#10491,#10492,#10493,#10494,#10495,#10496,#10497,#10498,#10499,#10500,#10501,
#10502,#10503,#10504,#10505,#10506,#10507,#10508,#10509,#10510,#10511,#10512,
#10513,#10514,#10515,#10516,#10517,#10518,#10519,#10520,#10521,#10522,#10523,
#10524,#10525,#10526,#10527,#10528,#10529,#10530,#10531,#10532,#10533,#10534,
#10535,#10536,#10537,#10538,#10539,#10540,#10541,#10542,#10543,#10544,#10545,
#10546,#10547,#10548,#10549,#10550,#10551,#10552,#10553));
#1859=EDGE_LOOP('',(#10554,#10555,#10556,#10557,#10558,#10559));
#1860=EDGE_LOOP('',(#10560,#10561,#10562,#10563,#10564,#10565,#10566,#10567,
#10568,#10569,#10570,#10571,#10572,#10573,#10574,#10575,#10576,#10577,#10578,
#10579,#10580,#10581,#10582,#10583,#10584,#10585,#10586,#10587,#10588,#10589,
#10590,#10591,#10592,#10593,#10594,#10595,#10596,#10597,#10598,#10599,#10600,
#10601,#10602,#10603,#10604,#10605,#10606,#10607,#10608,#10609,#10610,#10611,
#10612,#10613,#10614,#10615,#10616,#10617,#10618,#10619,#10620,#10621,#10622,
#10623,#10624,#10625,#10626,#10627,#10628,#10629,#10630,#10631,#10632,#10633,
#10634,#10635,#10636,#10637,#10638,#10639,#10640,#10641,#10642,#10643,#10644,
#10645,#10646,#10647,#10648,#10649,#10650,#10651,#10652,#10653,#10654,#10655,
#10656,#10657,#10658,#10659,#10660,#10661,#10662,#10663,#10664,#10665,#10666,
#10667,#10668,#10669,#10670,#10671,#10672,#10673,#10674,#10675,#10676,#10677,
#10678,#10679,#10680,#10681,#10682,#10683,#10684,#10685,#10686,#10687,#10688,
#10689,#10690,#10691,#10692,#10693,#10694,#10695,#10696,#10697,#10698,#10699,
#10700,#10701,#10702,#10703,#10704,#10705,#10706,#10707,#10708,#10709,#10710,
#10711,#10712,#10713,#10714,#10715,#10716,#10717,#10718,#10719,#10720,#10721,
#10722,#10723));
#1861=EDGE_LOOP('',(#10724,#10725,#10726,#10727,#10728,#10729,#10730,#10731,
#10732,#10733,#10734,#10735,#10736,#10737,#10738,#10739,#10740,#10741,#10742,
#10743,#10744,#10745,#10746,#10747,#10748,#10749,#10750,#10751,#10752,#10753,
#10754,#10755,#10756,#10757,#10758,#10759,#10760,#10761,#10762,#10763,#10764,
#10765,#10766,#10767,#10768,#10769,#10770,#10771,#10772,#10773,#10774,#10775,
#10776,#10777,#10778,#10779,#10780,#10781,#10782,#10783,#10784,#10785,#10786,
#10787,#10788,#10789,#10790,#10791,#10792,#10793,#10794,#10795,#10796,#10797,
#10798,#10799,#10800,#10801,#10802,#10803,#10804,#10805,#10806,#10807,#10808,
#10809,#10810,#10811,#10812,#10813,#10814,#10815,#10816,#10817,#10818,#10819,
#10820,#10821,#10822,#10823,#10824,#10825,#10826,#10827,#10828,#10829,#10830,
#10831,#10832,#10833,#10834,#10835,#10836,#10837,#10838,#10839,#10840,#10841,
#10842,#10843,#10844,#10845,#10846,#10847,#10848,#10849,#10850,#10851,#10852,
#10853,#10854,#10855,#10856,#10857,#10858,#10859,#10860,#10861,#10862,#10863,
#10864,#10865,#10866,#10867,#10868,#10869,#10870,#10871,#10872,#10873,#10874,
#10875,#10876,#10877,#10878,#10879,#10880,#10881,#10882,#10883,#10884,#10885,
#10886,#10887,#10888,#10889,#10890,#10891,#10892,#10893,#10894,#10895,#10896,
#10897,#10898,#10899,#10900,#10901,#10902,#10903,#10904,#10905,#10906,#10907));
#1862=EDGE_LOOP('',(#10908,#10909,#10910,#10911));
#1863=EDGE_LOOP('',(#10912,#10913,#10914,#10915));
#1864=EDGE_LOOP('',(#10916,#10917,#10918,#10919));
#1865=EDGE_LOOP('',(#10920,#10921,#10922,#10923));
#1866=EDGE_LOOP('',(#10924,#10925,#10926,#10927,#10928));
#1867=EDGE_LOOP('',(#10929,#10930,#10931,#10932,#10933,#10934));
#1868=EDGE_LOOP('',(#10935));
#1869=EDGE_LOOP('',(#10936,#10937,#10938,#10939));
#1870=EDGE_LOOP('',(#10940));
#1871=EDGE_LOOP('',(#10941));
#1872=EDGE_LOOP('',(#10942));
#1873=EDGE_LOOP('',(#10943));
#1874=EDGE_LOOP('',(#10944,#10945,#10946,#10947,#10948));
#1875=EDGE_LOOP('',(#10949));
#1876=EDGE_LOOP('',(#10950));
#1877=EDGE_LOOP('',(#10951));
#1878=EDGE_LOOP('',(#10952));
#1879=EDGE_LOOP('',(#10953));
#1880=EDGE_LOOP('',(#10954,#10955,#10956,#10957));
#2598=CIRCLE('',#13737,6.767);
#2599=CIRCLE('',#13798,7.911);
#2600=CIRCLE('',#13799,7.911);
#2601=CIRCLE('',#13801,6.767);
#2602=CIRCLE('',#13803,2.);
#2603=CIRCLE('',#13804,2.);
#2604=CIRCLE('',#13806,2.);
#2605=CIRCLE('',#13807,2.);
#2606=CIRCLE('',#13809,2.);
#2607=CIRCLE('',#13810,2.);
#2608=CIRCLE('',#13812,2.);
#2609=CIRCLE('',#13813,2.);
#2610=CIRCLE('',#13815,20.);
#2611=CIRCLE('',#13816,1.);
#2612=CIRCLE('',#13817,19.);
#2613=CIRCLE('',#13818,20.);
#2614=CIRCLE('',#13820,20.);
#2615=CIRCLE('',#13821,20.);
#2616=CIRCLE('',#13824,19.);
#2617=CIRCLE('',#13825,1.);
#3212=B_SPLINE_CURVE_WITH_KNOTS('',3,(#33021,#33022,#33023,#33024,#33025,
#33026,#33027,#33028,#33029,#33030,#33031,#33032,#33033,#33034,#33035,#33036,
#33037,#33038,#33039,#33040,#33041,#33042,#33043,#33044,#33045,#33046,#33047,
#33048,#33049,#33050,#33051,#33052,#33053,#33054,#33055,#33056,#33057,#33058,
#33059,#33060,#33061,#33062,#33063,#33064,#33065,#33066,#33067,#33068,#33069,
#33070,#33071,#33072,#33073,#33074,#33075,#33076,#33077,#33078,#33079,#33080,
#33081,#33082,#33083,#33084,#33085,#33086,#33087,#33088,#33089,#33090,#33091,
#33092,#33093,#33094,#33095,#33096,#33097,#33098,#33099,#33100,#33101,#33102,
#33103,#33104,#33105,#33106,#33107,#33108,#33109,#33110,#33111,#33112,#33113,
#33114,#33115,#33116,#33117,#33118,#33119,#33120,#33121,#33122,#33123,#33124,
#33125,#33126,#33127,#33128,#33129,#33130,#33131,#33132,#33133,#33134,#33135,
#33136,#33137,#33138,#33139,#33140,#33141,#33142,#33143,#33144,#33145,#33146,
#33147,#33148,#33149,#33150,#33151,#33152,#33153),.UNSPECIFIED.,.F.,.F.,
(4,3,3,3,3,3,3,3,3,3,3,3,3,3,3,3,3,3,3,3,3,3,3,3,3,3,3,3,3,3,3,3,3,3,3,
3,3,3,3,3,3,3,3,3,4),(10.3763813528868,10.4542262130358,10.5320112120275,
10.6097514308222,10.6874619179396,10.7651722203897,10.8428857355022,10.9206160760242,
10.998376861546,11.0762274093604,11.1541256248539,11.2321411003828,11.2937563986016,
11.3696586020076,11.4454654112385,11.5211937028804,11.5968602679744,11.672481832139,
11.7498339506124,11.8254308832918,11.9010358142025,11.9766638237259,12.0553225627761,
12.1310851816833,12.206905521287,12.2828337446297,12.2912987799265,12.3696393822356,
12.4478854133682,12.5260516605635,12.6041528549847,12.6822036816841,12.7602218764032,
12.8382231786224,12.9162208344635,12.99422808542,13.0722915935675,13.1503841976854,
13.2285627052136,13.2888411612514,13.3690518606113,13.449169842401,13.5292322801668,
13.6092374927533,13.661551274788),.UNSPECIFIED.);
#3213=B_SPLINE_CURVE_WITH_KNOTS('',3,(#33156,#33157,#33158,#33159,#33160,
#33161,#33162,#33163,#33164,#33165,#33166,#33167,#33168,#33169,#33170,#33171,
#33172,#33173,#33174,#33175,#33176,#33177,#33178,#33179,#33180,#33181,#33182,
#33183,#33184,#33185,#33186,#33187,#33188,#33189,#33190,#33191,#33192,#33193,
#33194,#33195,#33196,#33197,#33198,#33199,#33200,#33201,#33202,#33203,#33204,
#33205,#33206,#33207,#33208,#33209,#33210,#33211,#33212,#33213,#33214,#33215,
#33216,#33217,#33218,#33219,#33220,#33221,#33222,#33223,#33224,#33225,#33226,
#33227,#33228,#33229,#33230,#33231,#33232,#33233,#33234,#33235,#33236,#33237),
 .UNSPECIFIED.,.F.,.F.,(4,3,3,3,3,3,3,3,3,3,3,3,3,3,3,3,3,3,3,3,3,3,3,3,
3,3,3,4),(11.6150328478191,11.6997920262197,11.784576819193,11.8693764519753,
11.9541615193291,12.0389064356849,12.1138040384816,12.1908442532085,12.2678596835335,
12.3448646842034,12.4218948675792,12.4989390429297,12.576038969133,12.612575229144,
12.7000747491645,12.7875920845772,12.875043992548,12.9624105838022,13.0495747511006,
13.1113464198064,13.1892669318928,13.2671805000566,13.3451005231923,13.4230676270369,
13.5010616179069,13.5791262428044,13.6101176104689,13.6616030987896),
 .UNSPECIFIED.);
#3214=B_SPLINE_CURVE_WITH_KNOTS('',3,(#33243,#33244,#33245,#33246,#33247,
#33248,#33249,#33250,#33251,#33252,#33253,#33254,#33255,#33256,#33257,#33258,
#33259,#33260,#33261,#33262,#33263,#33264,#33265,#33266,#33267,#33268,#33269,
#33270,#33271,#33272,#33273,#33274,#33275,#33276,#33277,#33278,#33279,#33280,
#33281,#33282,#33283,#33284,#33285,#33286,#33287,#33288,#33289,#33290,#33291,
#33292,#33293,#33294,#33295,#33296,#33297,#33298,#33299,#33300,#33301,#33302,
#33303,#33304,#33305,#33306,#33307,#33308,#33309,#33310,#33311,#33312,#33313,
#33314,#33315,#33316,#33317,#33318,#33319,#33320,#33321,#33322,#33323,#33324,
#33325,#33326,#33327,#33328,#33329,#33330,#33331,#33332,#33333,#33334,#33335,
#33336,#33337,#33338,#33339,#33340,#33341,#33342,#33343,#33344,#33345,#33346,
#33347,#33348,#33349,#33350,#33351,#33352,#33353,#33354,#33355,#33356,#33357,
#33358,#33359,#33360,#33361,#33362,#33363,#33364,#33365,#33366,#33367,#33368,
#33369,#33370,#33371,#33372,#33373,#33374,#33375,#33376,#33377,#33378,#33379,
#33380,#33381,#33382,#33383,#33384,#33385,#33386,#33387,#33388,#33389,#33390,
#33391,#33392,#33393,#33394,#33395,#33396,#33397,#33398,#33399),
 .UNSPECIFIED.,.F.,.F.,(4,3,3,3,3,3,3,3,3,3,3,3,3,3,3,3,3,3,3,3,3,3,3,3,
3,3,3,3,3,3,3,3,3,3,3,3,3,3,3,3,3,3,3,3,3,3,3,3,3,3,3,3,4),(15.7079632679497,
15.7904254740499,15.8728873318523,15.9553488482074,16.0378100299651,16.1202708839753,
16.2027314170874,16.2851916361505,16.3676515480136,16.4501111595253,16.532570477534,
16.615029508888,16.6974882604348,16.7799467390223,16.8624049514979,16.9448629047087,
17.0273206055016,17.1097780607235,17.1922352772208,17.2782479725068,17.3615727710651,
17.444039376657,17.5265051380402,17.6089700826299,17.6914342378382,17.7738976310748,
17.8563602897465,17.9388222412576,18.02128351301,18.1037441324032,18.1862041268344,
18.2686635236985,18.3511223503886,18.4335806342956,18.5160384028087,18.5984956833151,
18.6826297985062,18.7650957968661,18.8475601734724,18.9300230379678,19.0124844999741,
19.0949446690934,19.1774036549095,19.2598615669898,19.3454590619128,19.4279237989587,
19.510385571345,19.5928448175101,19.6753019757488,19.7577644948314,19.8402221662423,
19.9226809574354,19.9446415263734),.UNSPECIFIED.);
#3215=B_SPLINE_CURVE_WITH_KNOTS('',3,(#33400,#33401,#33402,#33403,#33404,
#33405,#33406,#33407,#33408,#33409,#33410,#33411,#33412,#33413,#33414,#33415,
#33416,#33417,#33418,#33419,#33420,#33421,#33422,#33423,#33424,#33425,#33426,
#33427,#33428,#33429,#33430,#33431,#33432,#33433,#33434,#33435,#33436,#33437,
#33438,#33439,#33440,#33441,#33442,#33443,#33444,#33445,#33446,#33447,#33448,
#33449,#33450,#33451,#33452,#33453,#33454,#33455,#33456,#33457,#33458,#33459,
#33460,#33461,#33462,#33463,#33464,#33465,#33466,#33467,#33468,#33469,#33470,
#33471,#33472,#33473,#33474,#33475,#33476,#33477,#33478,#33479,#33480,#33481),
 .UNSPECIFIED.,.F.,.F.,(4,3,3,3,3,3,3,3,3,3,3,3,3,3,3,3,3,3,3,3,3,3,3,3,
3,3,3,4),(13.661551274788,13.741495797514,13.7876123519139,13.8684595437818,
13.9493475468375,14.0336065457722,14.1146338308566,14.1957114478603,14.2768739065073,
14.2863835425763,14.3718154735951,14.4571706791758,14.5423736904682,14.6274672692567,
14.7123617066816,14.7851547332388,14.8616903646453,14.938220499497,15.0147597510167,
15.0913547207395,15.1679808823156,15.2446904324708,15.2839259239012,15.3707393590102,
15.457380599417,15.5438881964551,15.6301266039185,15.7079632679497),
 .UNSPECIFIED.);
#3216=B_SPLINE_CURVE_WITH_KNOTS('',3,(#33483,#33484,#33485,#33486,#33487,
#33488,#33489,#33490,#33491,#33492,#33493,#33494,#33495,#33496,#33497,#33498,
#33499,#33500,#33501,#33502,#33503,#33504,#33505,#33506,#33507,#33508,#33509,
#33510,#33511,#33512,#33513,#33514,#33515,#33516,#33517,#33518,#33519,#33520,
#33521,#33522,#33523,#33524,#33525,#33526,#33527,#33528,#33529,#33530,#33531,
#33532,#33533,#33534,#33535,#33536,#33537,#33538,#33539,#33540,#33541,#33542,
#33543,#33544,#33545,#33546,#33547,#33548,#33549,#33550,#33551,#33552,#33553,
#33554,#33555,#33556,#33557,#33558,#33559,#33560,#33561,#33562,#33563,#33564),
 .UNSPECIFIED.,.F.,.F.,(4,3,3,3,3,3,3,3,3,3,3,3,3,3,3,3,3,3,3,3,3,3,3,3,
3,3,3,4),(13.6616030987896,13.7400509247693,13.8184450987703,13.8967997953241,
13.9751291593552,14.05419551341,14.132535823946,14.2108945399217,14.2892844834101,
14.368878360506,14.4474090346784,14.5275345132361,14.6076599917938,14.6835621951998,
14.7593690044307,14.8350972960725,14.9107638611665,14.9863854253312,15.0637375438047,
15.139334476484,15.2149394073948,15.2905674169182,15.3692261559683,15.4449887748756,
15.5208091144791,15.5967373378218,15.6052023731187,15.7079632679496),
 .UNSPECIFIED.);
#3217=B_SPLINE_CURVE_WITH_KNOTS('',3,(#33565,#33566,#33567,#33568,#33569,
#33570,#33571,#33572,#33573,#33574,#33575,#33576,#33577,#33578,#33579,#33580,
#33581,#33582,#33583,#33584,#33585,#33586,#33587,#33588,#33589,#33590,#33591,
#33592,#33593,#33594,#33595,#33596,#33597,#33598,#33599,#33600,#33601,#33602,
#33603,#33604,#33605,#33606,#33607,#33608,#33609,#33610,#33611,#33612,#33613,
#33614,#33615,#33616,#33617,#33618,#33619,#33620,#33621,#33622,#33623,#33624,
#33625,#33626,#33627,#33628,#33629,#33630,#33631,#33632,#33633,#33634,#33635,
#33636,#33637,#33638,#33639,#33640,#33641,#33642,#33643,#33644,#33645,#33646,
#33647,#33648,#33649,#33650,#33651,#33652,#33653,#33654,#33655,#33656,#33657,
#33658,#33659,#33660,#33661,#33662,#33663,#33664,#33665,#33666,#33667,#33668,
#33669,#33670,#33671,#33672,#33673,#33674,#33675,#33676,#33677,#33678,#33679,
#33680,#33681,#33682,#33683,#33684,#33685,#33686,#33687,#33688,#33689,#33690,
#33691,#33692,#33693,#33694,#33695,#33696,#33697,#33698,#33699,#33700,#33701,
#33702,#33703,#33704,#33705,#33706,#33707,#33708,#33709,#33710,#33711,#33712,
#33713,#33714,#33715,#33716,#33717,#33718,#33719,#33720,#33721,#33722,#33723,
#33724,#33725,#33726,#33727,#33728,#33729,#33730,#33731,#33732,#33733,#33734,
#33735,#33736),.UNSPECIFIED.,.F.,.F.,(4,3,3,3,3,3,3,3,3,3,3,3,3,3,3,3,3,
3,3,3,3,3,3,3,3,3,3,3,3,3,3,3,3,3,3,3,3,3,3,3,3,3,3,3,3,3,3,3,3,3,3,3,3,
3,3,3,3,4),(15.7079632680317,15.7849462163073,15.8618387115719,15.9386569259526,
16.0154169733244,16.0921360340367,16.1688338913552,16.2455250521911,16.3222240170258,
16.3989783335857,16.475762449498,16.5526324844258,16.6027447544436,16.6829440681553,
16.7630727326106,16.8431403640705,16.9231458883287,17.0031134951737,17.0830489458154,
17.101515945106,17.1823631369738,17.2632511400294,17.3475101389642,17.4285374240485,
17.509615041052,17.5907774996986,17.6002871357685,17.6857190667875,17.7710742723682,
17.8562772836606,17.9413708624499,18.026265299875,18.0990583264309,18.1755939578373,
18.252124092689,18.3286633442088,18.4052583139318,18.4818844755075,18.5585940256627,
18.5978295170934,18.6773734409489,18.7568570513369,18.8362926202057,18.9156923820079,
18.9950685426141,19.0744458783739,19.15382588468,19.2332196505527,19.3126382726157,
19.3921281193603,19.4716563839099,19.5512731075891,19.5953718984182,19.6730799420205,
19.7506743995356,19.8282033634491,19.9056683807068,19.9450135134811),
 .UNSPECIFIED.);
#3218=B_SPLINE_CURVE_WITH_KNOTS('',3,(#33742,#33743,#33744,#33745,#33746,
#33747,#33748,#33749,#33750,#33751,#33752,#33753,#33754,#33755,#33756,#33757,
#33758,#33759,#33760,#33761,#33762,#33763,#33764,#33765,#33766,#33767,#33768,
#33769,#33770,#33771,#33772,#33773,#33774,#33775,#33776,#33777,#33778,#33779,
#33780,#33781,#33782,#33783,#33784,#33785,#33786,#33787,#33788,#33789,#33790,
#33791,#33792,#33793,#33794,#33795,#33796,#33797,#33798,#33799,#33800,#33801,
#33802,#33803,#33804,#33805,#33806,#33807,#33808,#33809,#33810,#33811,#33812,
#33813,#33814,#33815,#33816,#33817,#33818,#33819,#33820,#33821,#33822,#33823,
#33824,#33825,#33826,#33827,#33828,#33829,#33830,#33831,#33832,#33833,#33834,
#33835,#33836,#33837,#33838,#33839,#33840,#33841,#33842,#33843,#33844,#33845,
#33846,#33847,#33848,#33849,#33850,#33851,#33852,#33853,#33854,#33855,#33856,
#33857,#33858,#33859,#33860,#33861,#33862,#33863,#33864,#33865,#33866,#33867,
#33868,#33869,#33870,#33871,#33872,#33873,#33874,#33875,#33876,#33877,#33878,
#33879,#33880,#33881,#33882,#33883,#33884,#33885,#33886,#33887,#33888,#33889,
#33890,#33891,#33892,#33893,#33894,#33895,#33896,#33897,#33898,#33899,#33900,
#33901,#33902,#33903,#33904,#33905,#33906,#33907,#33908,#33909,#33910),
 .UNSPECIFIED.,.F.,.F.,(4,3,3,3,3,3,3,3,3,3,3,3,3,3,3,3,3,3,3,3,3,3,3,3,
3,3,3,3,3,3,3,3,3,3,3,3,3,3,3,3,3,3,3,3,3,3,3,3,3,3,3,3,3,3,3,3,4),(21.9911485751293,
22.073370029129,22.155701741496,22.2382025518265,22.2667225931755,22.3462744183194,
22.425766113522,22.5052099311933,22.5846180863565,22.6640027655525,22.7433887585426,
22.8227774964882,22.9021800515031,22.9816075033574,23.0611061827488,23.1406432843994,
23.2202687745103,23.2642649745004,23.3419325004101,23.4195140009868,23.4970233972062,
23.5744643131551,23.6518655530078,23.7292409089966,23.7630361651628,23.8465275840083,
23.9301752008269,24.0140603945263,24.0980591432093,24.1822433689923,24.2618073558252,
24.3393164898074,24.416743766626,24.4941048029902,24.5714151681249,24.6486903944456,
24.7259588996925,24.8032266354315,24.8805076379063,24.9578159481874,25.0352120613664,
25.1126538238102,25.1902150126104,25.2593497371501,25.3354175880398,25.4113904191998,
25.4872850100609,25.5631180600763,25.6389062073172,25.7146753715244,25.7904368441565,
25.8662056235072,25.9419967122486,26.0178685005078,26.0937833120982,26.1698103065359,
26.2271380078629),.UNSPECIFIED.);
#3219=B_SPLINE_CURVE_WITH_KNOTS('',3,(#33911,#33912,#33913,#33914,#33915,
#33916,#33917,#33918,#33919,#33920,#33921,#33922,#33923,#33924,#33925,#33926,
#33927,#33928,#33929,#33930,#33931,#33932,#33933,#33934,#33935,#33936,#33937,
#33938,#33939,#33940,#33941,#33942,#33943,#33944,#33945,#33946,#33947,#33948,
#33949,#33950,#33951,#33952,#33953,#33954,#33955,#33956,#33957,#33958,#33959,
#33960,#33961,#33962,#33963,#33964,#33965,#33966,#33967,#33968,#33969,#33970,
#33971,#33972,#33973,#33974,#33975,#33976,#33977,#33978,#33979,#33980,#33981,
#33982,#33983,#33984,#33985,#33986),.UNSPECIFIED.,.F.,.F.,(4,3,3,3,3,3,
3,3,3,3,3,3,3,3,3,3,3,3,3,3,3,3,3,3,3,4),(19.9446415263734,20.0271031301035,
20.1095640679554,20.1920243673274,20.2744840556157,20.356943160214,20.4394017085145,
20.521859727907,20.6043172457797,20.690994203864,20.7734609894051,20.855926102473,
20.938389652721,21.0208517497802,21.1033125032619,21.1857720227579,21.268230417843,
21.3506877980765,21.4331541837626,21.5156173852708,21.5980778411205,21.680535989675,
21.7630015934287,21.8454614718166,21.9279255830689,21.9911485751293),
 .UNSPECIFIED.);
#3220=B_SPLINE_CURVE_WITH_KNOTS('',3,(#33988,#33989,#33990,#33991,#33992,
#33993,#33994,#33995,#33996,#33997,#33998,#33999,#34000,#34001,#34002,#34003,
#34004,#34005,#34006,#34007,#34008,#34009,#34010,#34011,#34012,#34013,#34014,
#34015,#34016,#34017,#34018,#34019,#34020,#34021,#34022,#34023,#34024,#34025,
#34026,#34027,#34028,#34029,#34030,#34031,#34032,#34033,#34034,#34035,#34036,
#34037,#34038,#34039,#34040,#34041,#34042,#34043,#34044,#34045,#34046,#34047,
#34048,#34049,#34050,#34051,#34052,#34053,#34054,#34055,#34056,#34057,#34058,
#34059,#34060,#34061,#34062,#34063,#34064,#34065,#34066),.UNSPECIFIED.,
 .F.,.F.,(4,3,3,3,3,3,3,3,3,3,3,3,3,3,3,3,3,3,3,3,3,3,3,3,3,3,4),(19.9450135134811,
20.022424916161,20.0941430890807,20.1776176136089,20.2612475490833,20.3451141481709,
20.429093879934,20.5132587154843,20.5929142797431,20.6704251919161,20.7478542711913,
20.8252171322539,20.9025293423276,20.9798064318453,21.0570768215095,21.1343464544012,
21.2116293650211,21.2889395927012,21.3663376273369,21.4437813163736,21.5213444218647,
21.590456661068,21.6752450130628,21.7596553082193,21.843836383805,21.927646354891,
21.9911485750275),.UNSPECIFIED.);
#3221=B_SPLINE_CURVE_WITH_KNOTS('',3,(#34067,#34068,#34069,#34070,#34071,
#34072,#34073,#34074,#34075,#34076,#34077,#34078,#34079,#34080,#34081,#34082,
#34083,#34084,#34085,#34086,#34087,#34088,#34089,#34090,#34091,#34092,#34093,
#34094,#34095,#34096,#34097,#34098,#34099,#34100,#34101,#34102,#34103,#34104,
#34105,#34106,#34107,#34108,#34109,#34110,#34111,#34112,#34113,#34114,#34115,
#34116,#34117,#34118,#34119,#34120,#34121,#34122,#34123,#34124,#34125,#34126,
#34127,#34128,#34129,#34130,#34131,#34132,#34133,#34134,#34135,#34136,#34137,
#34138,#34139,#34140,#34141,#34142,#34143,#34144,#34145,#34146,#34147,#34148,
#34149,#34150,#34151,#34152,#34153,#34154,#34155,#34156,#34157,#34158,#34159,
#34160,#34161,#34162,#34163,#34164,#34165,#34166,#34167,#34168,#34169,#34170,
#34171,#34172,#34173,#34174,#34175,#34176,#34177,#34178,#34179,#34180,#34181,
#34182,#34183,#34184,#34185,#34186,#34187,#34188,#34189,#34190,#34191,#34192,
#34193,#34194,#34195,#34196,#34197,#34198,#34199,#34200,#34201,#34202,#34203,
#34204,#34205,#34206,#34207,#34208,#34209,#34210,#34211,#34212,#34213,#34214,
#34215,#34216,#34217,#34218,#34219,#34220,#34221,#34222,#34223,#34224,#34225,
#34226,#34227,#34228,#34229,#34230,#34231,#34232),.UNSPECIFIED.,.F.,.F.,
(4,3,3,3,3,3,3,3,3,3,3,3,3,3,3,3,3,3,3,3,3,3,3,3,3,3,3,3,3,3,3,3,3,3,3,
3,3,3,3,3,3,3,3,3,3,3,3,3,3,3,3,3,3,3,3,4),(21.9911485751292,22.0677279286661,
22.1443208546211,22.2209417323296,22.2976049553143,22.3743782822554,22.4512108540594,
22.5281806705101,22.5879990423929,22.6665430117807,22.7449944002324,22.8233677018931,
22.9016773555741,22.9799377545146,23.0581663790971,23.1363785062284,23.2145871226706,
23.292805210708,23.3710782257912,23.4493797856809,23.5277645894362,23.5855414237178,
23.6651913214119,23.7447710878953,23.8242916009709,23.9037553722185,23.9831850756206,
24.0625903140226,24.0843126143803,24.165544261595,24.2468245668753,24.3308893764171,
24.4123210884906,24.4977024467667,24.5830838050427,24.668316709238,24.7534716491106,
24.8384765617015,24.9233748283101,25.0080813472925,25.0818549957052,25.1584140398398,
25.2349676874553,25.3115305349992,25.3881491510158,25.4647990040214,25.541532203083,
25.5806261863676,25.6614896806779,25.7409766543074,25.820418302191,25.8998257438916,
25.9817528431312,26.0611329043551,26.1443335226025,26.2275341408499),
 .UNSPECIFIED.);
#3222=B_SPLINE_CURVE_WITH_KNOTS('',3,(#34238,#34239,#34240,#34241,#34242,
#34243,#34244,#34245,#34246,#34247,#34248,#34249,#34250,#34251,#34252,#34253,
#34254,#34255,#34256,#34257,#34258,#34259,#34260,#34261,#34262,#34263,#34264,
#34265,#34266,#34267,#34268,#34269,#34270,#34271,#34272,#34273,#34274,#34275,
#34276,#34277,#34278,#34279,#34280,#34281,#34282,#34283,#34284,#34285,#34286,
#34287,#34288,#34289,#34290,#34291,#34292,#34293,#34294,#34295,#34296,#34297,
#34298,#34299,#34300,#34301,#34302,#34303,#34304,#34305,#34306,#34307,#34308,
#34309,#34310,#34311,#34312,#34313,#34314,#34315,#34316,#34317,#34318,#34319,
#34320,#34321,#34322,#34323,#34324,#34325,#34326,#34327,#34328,#34329,#34330,
#34331,#34332,#34333,#34334,#34335,#34336,#34337,#34338,#34339,#34340,#34341,
#34342,#34343,#34344,#34345,#34346,#34347,#34348,#34349,#34350,#34351,#34352,
#34353,#34354,#34355,#34356,#34357,#34358,#34359,#34360,#34361,#34362,#34363,
#34364,#34365,#34366,#34367,#34368,#34369,#34370,#34371,#34372,#34373,#34374,
#34375,#34376,#34377,#34378,#34379,#34380,#34381,#34382,#34383,#34384,#34385,
#34386,#34387,#34388,#34389,#34390,#34391,#34392,#34393,#34394,#34395,#34396,
#34397,#34398,#34399,#34400,#34401,#34402,#34403,#34404,#34405,#34406),
 .UNSPECIFIED.,.F.,.F.,(4,3,3,3,3,3,3,3,3,3,3,3,3,3,3,3,3,3,3,3,3,3,3,3,
3,3,3,3,3,3,3,3,3,3,3,3,3,3,3,3,3,3,3,3,3,3,3,3,3,3,3,3,3,3,3,3,4),(28.2743338824462,
28.3590289334677,28.44363761919,28.5280966928244,28.6124520888738,28.6966366011039,
28.7507480717873,28.8273070368857,28.9038606041814,28.9804233701809,29.0570419030758,
29.1336916720016,29.2104247859257,29.2495192624497,29.3290711268508,29.4085628622027,
29.4880067208172,29.5674149176193,29.6467996390536,29.7261856749325,29.805574456112,
29.884977054621,29.9644045501444,30.0439032731761,30.1234404184638,30.2030659518213,
30.2470616437746,30.3247291240364,30.4023105791433,30.4798199301175,30.5572608012783,
30.6346619966133,30.7120373086158,30.745832834437,30.8293242800933,30.9129719248353,
30.9968571476967,31.0808559260971,31.1650401820043,31.2446040250995,31.3221131579345,
31.3995404336048,31.4769014688208,31.5542118328085,31.6314870579847,31.7087555620954,
31.7860232967032,31.8633042980531,31.9406126072162,32.0180087192952,32.0954504806473,
32.1730116683798,32.2421464064244,32.3182081524628,32.394186612896,32.4700773700093,
32.5118535701146),.UNSPECIFIED.);
#3223=B_SPLINE_CURVE_WITH_KNOTS('',3,(#34407,#34408,#34409,#34410,#34411,
#34412,#34413,#34414,#34415,#34416,#34417,#34418,#34419,#34420,#34421,#34422,
#34423,#34424,#34425,#34426,#34427,#34428,#34429,#34430,#34431,#34432,#34433,
#34434,#34435,#34436,#34437,#34438,#34439,#34440,#34441,#34442,#34443,#34444,
#34445,#34446,#34447,#34448,#34449,#34450,#34451,#34452,#34453,#34454,#34455,
#34456,#34457,#34458,#34459,#34460,#34461,#34462,#34463,#34464,#34465,#34466,
#34467,#34468,#34469,#34470,#34471,#34472,#34473,#34474,#34475,#34476,#34477,
#34478,#34479,#34480,#34481,#34482,#34483,#34484,#34485,#34486,#34487,#34488,
#34489,#34490,#34491),.UNSPECIFIED.,.F.,.F.,(4,3,3,3,3,3,3,3,3,3,3,3,3,
3,3,3,3,3,3,3,3,3,3,3,3,3,3,3,4),(26.2271380078629,26.256892118475,26.3354367342183,
26.4138887751831,26.49226273455,26.570573050167,26.6488341143124,26.7270634063487,
26.8052762018615,26.8834854867574,26.961704242466,27.039977920359,27.11828014091,
27.1966655962879,27.2544344997999,27.3340835202497,27.4136624120983,27.4931820549764,
27.5726449666423,27.6520738176217,27.7314782172495,27.7532056904624,27.8344377442233,
27.9157184632528,27.9997830677208,28.081215203302,28.1665960422134,28.2519768811248,
28.2743338823089),.UNSPECIFIED.);
#3224=B_SPLINE_CURVE_WITH_KNOTS('',3,(#34493,#34494,#34495,#34496,#34497,
#34498,#34499,#34500,#34501,#34502,#34503,#34504,#34505,#34506,#34507,#34508,
#34509,#34510,#34511,#34512,#34513,#34514,#34515,#34516,#34517,#34518,#34519,
#34520,#34521,#34522,#34523,#34524,#34525,#34526,#34527,#34528,#34529,#34530,
#34531,#34532,#34533,#34534,#34535,#34536,#34537,#34538,#34539,#34540,#34541,
#34542,#34543,#34544,#34545,#34546,#34547,#34548,#34549,#34550,#34551,#34552,
#34553,#34554,#34555,#34556,#34557,#34558,#34559,#34560,#34561,#34562,#34563,
#34564,#34565,#34566,#34567,#34568,#34569,#34570,#34571,#34572,#34573,#34574,
#34575,#34576,#34577),.UNSPECIFIED.,.F.,.F.,(4,3,3,3,3,3,3,3,3,3,3,3,3,
3,3,3,3,3,3,3,3,3,3,3,3,3,3,3,4),(26.2275341408499,26.3069660971924,26.3864696852463,
26.4660131649361,26.5456425040867,26.5781685676925,26.6558360936021,26.7334175941789,
26.8109269903979,26.8883679063466,26.965769146199,27.0431445021878,27.0769397583549,
27.1604311771999,27.2440787940188,27.3279639877182,27.4119627364012,27.4961469621842,
27.5757109490174,27.6518730153432,27.7296806237139,27.8056774912106,27.8816299400362,
27.9575529772358,28.0367482035041,28.1126749107235,28.1886139449045,28.2645985897077,
28.2743338823088),.UNSPECIFIED.);
#3225=B_SPLINE_CURVE_WITH_KNOTS('',3,(#34578,#34579,#34580,#34581,#34582,
#34583,#34584,#34585,#34586,#34587,#34588,#34589,#34590,#34591,#34592,#34593,
#34594,#34595,#34596,#34597,#34598,#34599,#34600,#34601,#34602,#34603,#34604,
#34605,#34606,#34607,#34608,#34609,#34610,#34611,#34612,#34613,#34614,#34615,
#34616,#34617,#34618,#34619,#34620,#34621,#34622,#34623,#34624,#34625,#34626,
#34627,#34628,#34629,#34630,#34631,#34632,#34633,#34634,#34635,#34636,#34637,
#34638,#34639,#34640,#34641,#34642,#34643,#34644,#34645,#34646,#34647,#34648,
#34649,#34650,#34651,#34652,#34653,#34654,#34655,#34656,#34657,#34658,#34659,
#34660,#34661,#34662,#34663,#34664,#34665,#34666,#34667,#34668,#34669,#34670,
#34671,#34672,#34673,#34674,#34675,#34676,#34677,#34678,#34679,#34680,#34681,
#34682,#34683,#34684,#34685,#34686,#34687,#34688,#34689,#34690,#34691,#34692,
#34693,#34694,#34695,#34696,#34697,#34698,#34699,#34700,#34701,#34702,#34703,
#34704,#34705,#34706,#34707,#34708,#34709,#34710,#34711,#34712,#34713,#34714,
#34715,#34716,#34717,#34718,#34719,#34720,#34721,#34722,#34723,#34724,#34725,
#34726,#34727,#34728,#34729,#34730,#34731,#34732,#34733,#34734,#34735,#34736,
#34737,#34738,#34739,#34740),.UNSPECIFIED.,.F.,.F.,(4,3,3,3,3,3,3,3,3,3,
3,3,3,3,3,3,3,3,3,3,3,3,3,3,3,3,3,3,3,3,3,3,3,3,3,3,3,3,3,3,3,3,3,3,3,3,
3,3,3,3,3,3,3,3,4),(28.2743338823871,28.3727453836561,28.4733999042417,
28.5732533303423,28.6493194915406,28.7252909943352,28.8011846159107,28.8770170539935,
28.9528049453892,29.0300537911739,29.1058175916703,29.1815894995911,29.2573845189297,
29.3357373171141,29.4116658576972,29.4912307846822,29.5707957116672,29.6493403274105,
29.7277923683753,29.8061663277422,29.8844766433592,29.9627377075046,30.0409669995409,
30.1191797950537,30.1973890799497,30.2756078356583,30.3538815135514,30.4321837341024,
30.5105691894803,30.5683380929921,30.647987113442,30.7275660052906,30.8070856481688,
30.8865485598348,30.9659774108142,31.0453818104423,31.0671092836545,31.1483413374153,
31.2296220564447,31.3136866609127,31.3951187964939,31.4804996354054,31.565880474317,
31.6511133966384,31.7362683567024,31.8212732922646,31.9061715832064,31.9908781284146,
32.0646516649794,32.1412084177776,32.2177589008488,32.2943456149223,32.3709501090727,
32.4476276168002,32.5105299619478),.UNSPECIFIED.);
#3226=B_SPLINE_CURVE_WITH_KNOTS('',3,(#34746,#34747,#34748,#34749,#34750,
#34751,#34752,#34753,#34754,#34755,#34756,#34757,#34758,#34759,#34760,#34761,
#34762,#34763,#34764,#34765,#34766,#34767,#34768,#34769,#34770,#34771,#34772,
#34773,#34774,#34775,#34776,#34777,#34778,#34779,#34780,#34781,#34782,#34783,
#34784,#34785,#34786,#34787,#34788,#34789,#34790,#34791,#34792,#34793,#34794,
#34795,#34796,#34797,#34798,#34799,#34800,#34801,#34802,#34803,#34804,#34805,
#34806,#34807,#34808,#34809,#34810,#34811,#34812,#34813,#34814,#34815,#34816,
#34817,#34818,#34819,#34820,#34821,#34822,#34823,#34824,#34825,#34826,#34827,
#34828,#34829,#34830,#34831,#34832,#34833,#34834,#34835,#34836,#34837,#34838,
#34839,#34840,#34841,#34842,#34843,#34844,#34845,#34846,#34847,#34848,#34849,
#34850,#34851,#34852,#34853,#34854,#34855,#34856,#34857,#34858,#34859,#34860,
#34861,#34862,#34863,#34864,#34865,#34866,#34867,#34868,#34869,#34870,#34871,
#34872,#34873,#34874,#34875,#34876,#34877,#34878,#34879,#34880,#34881,#34882,
#34883,#34884,#34885,#34886,#34887,#34888,#34889,#34890,#34891,#34892,#34893,
#34894,#34895,#34896,#34897,#34898,#34899,#34900,#34901,#34902,#34903,#34904,
#34905,#34906,#34907,#34908,#34909,#34910,#34911,#34912,#34913,#34914),
 .UNSPECIFIED.,.F.,.F.,(4,3,3,3,3,3,3,3,3,3,3,3,3,3,3,3,3,3,3,3,3,3,3,3,
3,3,3,3,3,3,3,3,3,3,3,3,3,3,3,3,3,3,3,3,3,3,3,3,3,3,3,3,3,3,3,3,4),(34.5575191896132,
34.6328860307859,34.7082479790274,34.7360023597366,34.8172344128309,34.8985151311743,
34.9825797359805,35.0640118708417,35.1493927106204,35.2347735503991,35.3200064738651,
35.4051614350876,35.4901663718067,35.5750646638952,35.6597712102173,35.7335447410615,
35.8101037057496,35.8866572726299,35.9632200382092,36.0398385706779,36.1164883391738,
36.1932214526645,36.232315931724,36.3118677962225,36.3913595316738,36.4708033903896,
36.5502115872951,36.6295963088339,36.7089823448189,36.7883711261052,36.8677737247216,
36.9472012203527,37.0266999434922,37.1062370888878,37.1858626223519,37.2298583130489,
37.3075257932727,37.3851072483418,37.4626165992783,37.5400574704023,37.6174586657012,
37.6948339776677,37.7286295037113,37.8121209493714,37.8957685941178,37.979653816982,
38.0636525953846,38.1478368512936,38.2274006943737,38.3049039354871,38.3823292364177,
38.4596907462697,38.5370025744167,38.6142794004192,38.6915361823884,38.7687949577837,
38.7940869402089),.UNSPECIFIED.);
#3227=B_SPLINE_CURVE_WITH_KNOTS('',3,(#34915,#34916,#34917,#34918,#34919,
#34920,#34921,#34922,#34923,#34924,#34925,#34926,#34927,#34928,#34929,#34930,
#34931,#34932,#34933,#34934,#34935,#34936,#34937,#34938,#34939,#34940,#34941,
#34942,#34943,#34944,#34945,#34946,#34947,#34948,#34949,#34950,#34951,#34952,
#34953,#34954,#34955,#34956,#34957,#34958,#34959,#34960,#34961,#34962,#34963,
#34964,#34965,#34966,#34967,#34968,#34969,#34970,#34971,#34972,#34973,#34974,
#34975,#34976,#34977,#34978,#34979,#34980,#34981,#34982,#34983,#34984,#34985,
#34986,#34987,#34988,#34989,#34990,#34991,#34992,#34993,#34994,#34995,#34996),
 .UNSPECIFIED.,.F.,.F.,(4,3,3,3,3,3,3,3,3,3,3,3,3,3,3,3,3,3,3,3,3,3,3,3,
3,3,3,4),(32.5118535701146,32.5876594146424,32.6634298563173,32.739195017798,
32.8149612557743,32.890743570437,32.9665569730653,33.0424617773558,33.1184172654376,
33.1944901160972,33.2396887877493,33.3182334046871,33.3966854468569,33.4750594074386,
33.5533697242772,33.6316307896502,33.7098600829166,33.7880728796606,33.8662821657869,
33.944500922725,34.0227746018369,34.1010768236021,34.1794622801768,34.2372311690742,
34.3214988374453,34.4056595487601,34.48964296411,34.5575191894885),
 .UNSPECIFIED.);
#3228=B_SPLINE_CURVE_WITH_KNOTS('',3,(#34998,#34999,#35000,#35001,#35002,
#35003,#35004,#35005,#35006,#35007,#35008,#35009,#35010,#35011,#35012,#35013,
#35014,#35015,#35016,#35017,#35018,#35019,#35020,#35021,#35022,#35023,#35024,
#35025,#35026,#35027,#35028,#35029,#35030,#35031,#35032,#35033,#35034,#35035,
#35036,#35037,#35038,#35039,#35040,#35041,#35042,#35043,#35044,#35045,#35046,
#35047,#35048,#35049,#35050,#35051,#35052,#35053,#35054,#35055,#35056,#35057,
#35058,#35059,#35060,#35061,#35062,#35063,#35064,#35065,#35066,#35067,#35068,
#35069,#35070,#35071,#35072,#35073,#35074,#35075,#35076,#35077,#35078,#35079),
 .UNSPECIFIED.,.F.,.F.,(4,3,3,3,3,3,3,3,3,3,3,3,3,3,3,3,3,3,3,3,3,3,3,3,
3,3,3,4),(32.5105299619478,32.5634228556418,32.6429747200431,32.7224664553949,
32.8019103140094,32.8813185108116,32.9607032322457,33.0400892681246,33.1194780493041,
33.198880647813,33.2783081433365,33.3578068663682,33.4373440116561,33.5169695450135,
33.5609652369667,33.6386327172285,33.7162141723355,33.7937235233092,33.87116439447,
33.9485655898052,34.0259409018075,34.0597364276292,34.1431858165314,34.2267901676328,
34.3106306453124,34.3945842540227,34.478722903774,34.5575191894884),
 .UNSPECIFIED.);
#3229=B_SPLINE_CURVE_WITH_KNOTS('',3,(#35080,#35081,#35082,#35083,#35084,
#35085,#35086,#35087,#35088,#35089,#35090,#35091,#35092,#35093,#35094,#35095,
#35096,#35097,#35098,#35099,#35100,#35101,#35102,#35103,#35104,#35105,#35106,
#35107,#35108,#35109,#35110,#35111,#35112,#35113,#35114,#35115,#35116,#35117,
#35118,#35119,#35120,#35121,#35122,#35123,#35124,#35125,#35126,#35127,#35128,
#35129,#35130,#35131,#35132,#35133,#35134,#35135,#35136,#35137,#35138,#35139,
#35140,#35141,#35142,#35143,#35144,#35145,#35146,#35147,#35148,#35149,#35150,
#35151,#35152,#35153,#35154,#35155,#35156,#35157,#35158,#35159,#35160,#35161,
#35162,#35163,#35164,#35165,#35166,#35167,#35168,#35169,#35170,#35171,#35172,
#35173,#35174,#35175,#35176,#35177,#35178,#35179,#35180,#35181,#35182,#35183,
#35184,#35185,#35186,#35187,#35188,#35189,#35190,#35191,#35192,#35193,#35194,
#35195,#35196,#35197,#35198,#35199,#35200,#35201,#35202,#35203,#35204,#35205,
#35206,#35207,#35208,#35209,#35210,#35211,#35212,#35213,#35214,#35215,#35216,
#35217,#35218,#35219,#35220,#35221,#35222,#35223,#35224,#35225,#35226,#35227,
#35228,#35229,#35230,#35231,#35232,#35233,#35234,#35235,#35236,#35237,#35238,
#35239,#35240,#35241,#35242,#35243,#35244,#35245,#35246,#35247,#35248),
 .UNSPECIFIED.,.F.,.F.,(4,3,3,3,3,3,3,3,3,3,3,3,3,3,3,3,3,3,3,3,3,3,3,3,
3,3,3,3,3,3,3,3,3,3,3,3,3,3,3,3,3,3,3,3,3,3,3,3,3,3,3,3,3,3,3,3,4),(34.5575191895771,
34.5585076182916,34.6360167511266,34.7134440267969,34.7908050620128,34.8681154260008,
34.9453906511771,35.0226591552877,35.0999268898953,35.1772078912449,35.2545162004082,
35.3319123124872,35.4093540738392,35.4869152615718,35.5560499996165,35.6321161590785,
35.7080876601177,35.7839812799196,35.859813716212,35.9356016058013,36.0128504526938,
36.0886142513502,36.1643861574193,36.2401811748956,36.318533976407,36.394462515114,
36.4740274480277,36.5535923809414,36.6321369978792,36.7105890400494,36.7889630006304,
36.8672733174692,36.9455343828414,37.0237636761078,37.1019764728517,37.1801857589785,
37.2584045159164,37.3366781950282,37.4149804167936,37.4933658733684,37.5511347622663,
37.6307837825282,37.7103626741949,37.7898823168981,37.8693452283991,37.9487740792201,
38.0281784786989,38.0499059529288,38.1311380060231,38.2124187243663,38.2964833291725,
38.3779154640338,38.4632963038125,38.5486771435912,38.6339107049348,38.7190353182339,
38.7947691242316),.UNSPECIFIED.);
#3230=B_SPLINE_CURVE_WITH_KNOTS('',3,(#35254,#35255,#35256,#35257,#35258,
#35259,#35260,#35261,#35262,#35263,#35264,#35265,#35266,#35267,#35268,#35269,
#35270,#35271,#35272,#35273,#35274,#35275,#35276,#35277,#35278,#35279,#35280,
#35281,#35282,#35283,#35284,#35285,#35286,#35287,#35288,#35289,#35290,#35291,
#35292,#35293,#35294,#35295,#35296,#35297,#35298,#35299,#35300,#35301,#35302,
#35303,#35304,#35305,#35306,#35307,#35308,#35309,#35310,#35311,#35312,#35313,
#35314,#35315,#35316,#35317,#35318,#35319,#35320,#35321,#35322,#35323,#35324,
#35325,#35326,#35327,#35328,#35329,#35330,#35331,#35332,#35333,#35334,#35335,
#35336,#35337,#35338,#35339,#35340,#35341,#35342,#35343,#35344,#35345,#35346,
#35347,#35348,#35349,#35350,#35351,#35352,#35353,#35354,#35355,#35356,#35357,
#35358,#35359,#35360,#35361,#35362,#35363,#35364,#35365,#35366,#35367,#35368,
#35369,#35370,#35371,#35372,#35373,#35374,#35375,#35376,#35377,#35378,#35379,
#35380,#35381,#35382,#35383,#35384,#35385,#35386,#35387,#35388,#35389,#35390,
#35391,#35392,#35393,#35394,#35395,#35396,#35397,#35398,#35399,#35400,#35401,
#35402,#35403,#35404,#35405,#35406,#35407,#35408,#35409,#35410,#35411,#35412,
#35413,#35414,#35415,#35416,#35417,#35418,#35419,#35420,#35421,#35422),
 .UNSPECIFIED.,.F.,.F.,(4,3,3,3,3,3,3,3,3,3,3,3,3,3,3,3,3,3,3,3,3,3,3,3,
3,3,3,3,3,3,3,3,3,3,3,3,3,3,3,3,3,3,3,3,3,3,3,3,3,3,3,3,3,3,3,3,4),(40.8407044967615,
40.9255123901943,41.0106105815536,41.0958516116635,41.1812825465948,41.2200278383484,
41.2996768586144,41.3792557502852,41.4587753929926,41.5382383044977,41.6176671553226,
41.6970715548056,41.7187990290109,41.8000310821006,41.8813118004394,41.9653764052479,
42.0468085401041,42.1321893798887,42.2175702196733,42.3028031431432,42.3879581043698,
42.4729630410927,42.5578613331851,42.642567879511,42.7163414103358,42.7929003750229,
42.8694539419022,42.9460167074805,43.0226352399482,43.0992850084429,43.1760181219326,
43.2151126009982,43.2946644654967,43.3741562009481,43.453600059664,43.5330082565694,
43.6123929781081,43.6917790140932,43.7711677953796,43.8505703939962,43.9299978896276,
44.0094966127673,44.089033758163,44.1686592916273,44.2126549823231,44.290322462547,
44.3679039176165,44.4454132685533,44.5228541396774,44.6002553349763,44.677630646943,
44.7114261729855,44.794877737273,44.8785677116355,44.9623812548976,45.0463706197337,
45.0770119293198),.UNSPECIFIED.);
#3231=B_SPLINE_CURVE_WITH_KNOTS('',3,(#35423,#35424,#35425,#35426,#35427,
#35428,#35429,#35430,#35431,#35432,#35433,#35434,#35435,#35436,#35437,#35438,
#35439,#35440,#35441,#35442,#35443,#35444,#35445,#35446,#35447,#35448,#35449,
#35450,#35451,#35452,#35453,#35454,#35455,#35456,#35457,#35458,#35459,#35460,
#35461,#35462,#35463,#35464,#35465,#35466,#35467,#35468,#35469,#35470,#35471,
#35472,#35473,#35474,#35475,#35476,#35477,#35478,#35479,#35480,#35481,#35482,
#35483,#35484,#35485,#35486,#35487,#35488,#35489,#35490,#35491,#35492,#35493,
#35494,#35495,#35496,#35497,#35498,#35499,#35500,#35501,#35502,#35503,#35504),
 .UNSPECIFIED.,.F.,.F.,(4,3,3,3,3,3,3,3,3,3,3,3,3,3,3,3,3,3,3,3,3,3,3,3,
3,3,3,4),(38.7940869402089,38.8713753251789,38.9486956114322,39.0261052493249,
39.1035646699761,39.181136360427,39.2249430756986,39.3010092351557,39.37698073619,
39.452874355987,39.5287067922744,39.6044946818586,39.6817435287542,39.7575073274052,
39.8332792334691,39.9090742509398,39.9874270524607,40.0633555911627,40.1429205240931,
40.2224854570235,40.3030798010984,40.3835697204861,40.4639643347003,40.5442727002749,
40.6244792960957,40.7046249184425,40.7847034810469,40.8407044966681),
 .UNSPECIFIED.);
#3232=B_SPLINE_CURVE_WITH_KNOTS('',3,(#35506,#35507,#35508,#35509,#35510,
#35511,#35512,#35513,#35514,#35515,#35516,#35517,#35518,#35519,#35520,#35521,
#35522,#35523,#35524,#35525,#35526,#35527,#35528,#35529,#35530,#35531,#35532,
#35533,#35534,#35535,#35536,#35537,#35538,#35539,#35540,#35541,#35542,#35543,
#35544,#35545,#35546,#35547,#35548,#35549,#35550,#35551,#35552,#35553,#35554,
#35555,#35556,#35557,#35558,#35559,#35560,#35561,#35562,#35563,#35564,#35565,
#35566,#35567,#35568,#35569,#35570,#35571,#35572,#35573,#35574,#35575,#35576,
#35577,#35578,#35579,#35580,#35581,#35582,#35583,#35584,#35585,#35586,#35587),
 .UNSPECIFIED.,.F.,.F.,(4,3,3,3,3,3,3,3,3,3,3,3,3,3,3,3,3,3,3,3,3,3,3,3,
3,3,3,4),(38.7947691242316,38.8796796646918,38.9643964891114,39.0474483342537,
39.1240072989418,39.2005608658222,39.2771236314016,39.3537421638703,39.4303919323663,
39.5071250458572,39.5462195249161,39.6257713894145,39.7052631248656,39.7847069835815,
39.8641151804875,39.9434999020257,40.0228859380105,40.1022747192966,40.1816773179129,
40.2611048135436,40.340603536683,40.4201406820783,40.4997662155423,40.543761906241,
40.6281287683698,40.7123180186424,40.7962321950299,40.840704496668),
 .UNSPECIFIED.);
#3233=B_SPLINE_CURVE_WITH_KNOTS('',3,(#35588,#35589,#35590,#35591,#35592,
#35593,#35594,#35595,#35596,#35597,#35598,#35599,#35600,#35601,#35602,#35603,
#35604,#35605,#35606,#35607,#35608,#35609,#35610,#35611,#35612,#35613,#35614,
#35615,#35616,#35617,#35618,#35619,#35620,#35621,#35622,#35623,#35624,#35625,
#35626,#35627,#35628,#35629,#35630,#35631,#35632,#35633,#35634,#35635,#35636,
#35637,#35638,#35639,#35640,#35641,#35642,#35643,#35644,#35645,#35646,#35647,
#35648,#35649,#35650,#35651,#35652,#35653,#35654,#35655,#35656,#35657,#35658,
#35659,#35660,#35661,#35662,#35663,#35664,#35665,#35666,#35667,#35668,#35669,
#35670,#35671,#35672,#35673,#35674,#35675,#35676,#35677,#35678,#35679,#35680,
#35681,#35682,#35683,#35684,#35685,#35686,#35687,#35688,#35689,#35690,#35691,
#35692,#35693,#35694,#35695,#35696,#35697,#35698,#35699,#35700,#35701,#35702,
#35703,#35704,#35705,#35706,#35707,#35708,#35709,#35710,#35711,#35712,#35713,
#35714,#35715,#35716,#35717,#35718,#35719,#35720,#35721,#35722,#35723,#35724,
#35725,#35726,#35727,#35728,#35729,#35730,#35731,#35732,#35733,#35734,#35735,
#35736,#35737,#35738,#35739,#35740,#35741,#35742,#35743,#35744),
 .UNSPECIFIED.,.F.,.F.,(4,3,3,3,3,3,3,3,3,3,3,3,3,3,3,3,3,3,3,3,3,3,3,3,
3,3,3,3,3,3,3,3,3,3,3,3,3,3,3,3,3,3,3,3,3,3,3,3,3,3,3,3,4),(40.840704496668,
40.9231667027682,41.0056285605707,41.0880900769258,41.1705512586836,41.2530121126939,
41.335472645806,41.4179328648691,41.5003927767322,41.582852388244,41.6653117062528,
41.7477707376065,41.8302294891534,41.9126879677409,41.9951461802166,42.0776041334274,
42.1600618342204,42.2425192894422,42.3249765059394,42.4109892012254,42.4943139997837,
42.5767806053756,42.6592463667588,42.7417113113485,42.8241754665568,42.9066388597934,
42.9891015184651,43.0715634699762,43.1540247417286,43.2364853611217,43.3189453555528,
43.4014047524171,43.4838635791072,43.5663218630143,43.6487796315274,43.7312369120337,
43.8153710272248,43.8978370255847,43.980301402191,44.0627642666864,44.1452257286927,
44.227685897812,44.3101448836281,44.3926027957084,44.4782002906313,44.5606650276772,
44.6431268000635,44.7255860462286,44.8080432044673,44.8905057235499,44.9729633949608,
45.0554221861539,45.0773827550916),.UNSPECIFIED.);
#3234=B_SPLINE_CURVE_WITH_KNOTS('',3,(#35750,#35751,#35752,#35753,#35754,
#35755,#35756,#35757,#35758,#35759,#35760,#35761,#35762,#35763,#35764,#35765,
#35766,#35767,#35768,#35769,#35770,#35771,#35772,#35773,#35774,#35775,#35776,
#35777,#35778,#35779,#35780,#35781,#35782,#35783,#35784,#35785,#35786,#35787,
#35788,#35789,#35790,#35791,#35792,#35793,#35794,#35795,#35796,#35797,#35798,
#35799,#35800,#35801,#35802,#35803,#35804,#35805,#35806,#35807,#35808,#35809,
#35810,#35811,#35812,#35813,#35814,#35815,#35816,#35817,#35818,#35819,#35820,
#35821,#35822,#35823,#35824,#35825,#35826,#35827,#35828,#35829,#35830,#35831,
#35832,#35833,#35834,#35835,#35836,#35837,#35838,#35839,#35840,#35841,#35842,
#35843,#35844,#35845,#35846,#35847,#35848,#35849,#35850,#35851,#35852,#35853,
#35854,#35855,#35856,#35857,#35858,#35859,#35860,#35861,#35862,#35863,#35864,
#35865,#35866,#35867,#35868,#35869,#35870,#35871,#35872,#35873,#35874,#35875,
#35876,#35877,#35878,#35879,#35880,#35881,#35882,#35883,#35884,#35885,#35886,
#35887,#35888,#35889,#35890,#35891,#35892,#35893,#35894,#35895,#35896,#35897,
#35898,#35899,#35900,#35901,#35902,#35903,#35904,#35905,#35906,#35907,#35908,
#35909,#35910,#35911,#35912,#35913,#35914,#35915,#35916,#35917,#35918),
 .UNSPECIFIED.,.F.,.F.,(4,3,3,3,3,3,3,3,3,3,3,3,3,3,3,3,3,3,3,3,3,3,3,3,
3,3,3,3,3,3,3,3,3,3,3,3,3,3,3,3,3,3,3,3,3,3,3,3,3,3,3,3,3,3,3,3,4),(47.1238898038477,
47.2052821262978,47.2838267432363,47.362278785407,47.4406527459888,47.5189630628279,
47.5972241282008,47.6754534214679,47.7536662182125,47.83187550434,47.9100942612782,
47.9883679403908,48.0666701621569,48.1450556187325,48.2028245076227,48.2824735278888,
48.3620524195598,48.4415720622669,48.5210349737721,48.6004638245972,48.6798682240802,
48.7015956982851,48.7828277513748,48.8641084697135,48.948173074522,49.0296052093781,
49.1149860491628,49.2003668889476,49.2855998124176,49.3707547736442,49.4557597103671,
49.5406580024596,49.6253645487856,49.69913807961,49.7756970442971,49.8522506111764,
49.9288133767549,50.0054319092225,50.0820816777174,50.158814791207,50.1979092702725,
50.2774611347711,50.3569528702224,50.4363967289383,50.5158049258438,50.5951896473825,
50.6745756833676,50.7539644646541,50.8333670632707,50.9127945589021,50.9922932820418,
51.0718304274376,51.1514559609018,51.1954516515974,51.2731390205547,51.3507270166998,
51.361293208361),.UNSPECIFIED.);
#3235=B_SPLINE_CURVE_WITH_KNOTS('',3,(#35919,#35920,#35921,#35922,#35923,
#35924,#35925,#35926,#35927,#35928,#35929,#35930,#35931,#35932,#35933,#35934,
#35935,#35936,#35937,#35938,#35939,#35940,#35941,#35942,#35943,#35944,#35945,
#35946,#35947,#35948,#35949,#35950,#35951,#35952,#35953,#35954,#35955,#35956,
#35957,#35958,#35959,#35960,#35961,#35962,#35963,#35964,#35965,#35966,#35967,
#35968,#35969,#35970,#35971,#35972,#35973,#35974,#35975,#35976,#35977,#35978,
#35979,#35980,#35981,#35982,#35983,#35984,#35985,#35986,#35987,#35988,#35989,
#35990,#35991,#35992,#35993,#35994,#35995,#35996,#35997,#35998,#35999,#36000,
#36001,#36002,#36003),.UNSPECIFIED.,.F.,.F.,(4,3,3,3,3,3,3,3,3,3,3,3,3,
3,3,3,3,3,3,3,3,3,3,3,3,3,3,3,4),(45.0770119293198,45.1612179706454,45.210197363648,
45.2877064964886,45.3651337721647,45.4424948073866,45.5198051713802,45.5970803965626,
45.6743489006794,45.7516166352935,45.8288976366497,45.9062059458194,45.983602057905,
46.0610438192636,46.1386050070028,46.2077397449729,46.2830265149734,46.3582198260812,
46.4333368553301,46.5083946723668,46.5853315637925,46.6603308845112,46.7353258134164,
46.810331656291,46.8887211931614,46.9638331599026,47.0389929820916,47.1142482591672,
47.1238898037727),.UNSPECIFIED.);
#3236=B_SPLINE_CURVE_WITH_KNOTS('',3,(#36005,#36006,#36007,#36008,#36009,
#36010,#36011,#36012,#36013,#36014,#36015,#36016,#36017,#36018,#36019,#36020,
#36021,#36022,#36023,#36024,#36025,#36026,#36027,#36028,#36029,#36030,#36031,
#36032,#36033,#36034,#36035,#36036,#36037,#36038,#36039,#36040,#36041,#36042,
#36043,#36044,#36045,#36046,#36047,#36048,#36049,#36050,#36051,#36052,#36053,
#36054,#36055,#36056,#36057,#36058,#36059,#36060,#36061,#36062,#36063,#36064,
#36065,#36066,#36067,#36068,#36069,#36070,#36071,#36072,#36073,#36074,#36075,
#36076,#36077,#36078,#36079,#36080),.UNSPECIFIED.,.F.,.F.,(4,3,3,3,3,3,
3,3,3,3,3,3,3,3,3,3,3,3,3,3,3,3,3,3,3,4),(45.0773827550916,45.1598443588218,
45.2423052966737,45.3247655960457,45.4072252843339,45.4896843889323,45.5721429372327,
45.6546009566253,45.737058474498,45.8237354325824,45.9062022181234,45.9886673311914,
46.0711308814393,46.1535929784986,46.2360537319802,46.3185132514762,46.4009716465613,
46.4834290267949,46.565895412481,46.6483586139892,46.7308190698388,46.8132772183935,
46.8957428221471,46.978202700535,47.0606668117873,47.1238898038476),
 .UNSPECIFIED.);
#3237=B_SPLINE_CURVE_WITH_KNOTS('',3,(#36081,#36082,#36083,#36084,#36085,
#36086,#36087,#36088,#36089,#36090,#36091,#36092,#36093,#36094,#36095,#36096,
#36097,#36098,#36099,#36100,#36101,#36102,#36103,#36104,#36105,#36106,#36107,
#36108,#36109,#36110,#36111,#36112,#36113,#36114,#36115,#36116,#36117,#36118,
#36119,#36120,#36121,#36122,#36123,#36124,#36125,#36126,#36127,#36128,#36129,
#36130,#36131,#36132,#36133,#36134,#36135,#36136,#36137,#36138,#36139,#36140,
#36141,#36142,#36143,#36144,#36145,#36146,#36147,#36148,#36149,#36150,#36151,
#36152,#36153,#36154,#36155,#36156,#36157,#36158,#36159,#36160,#36161,#36162,
#36163,#36164,#36165,#36166,#36167,#36168,#36169,#36170,#36171,#36172,#36173,
#36174,#36175,#36176,#36177,#36178,#36179,#36180,#36181,#36182,#36183,#36184,
#36185,#36186,#36187,#36188,#36189,#36190,#36191,#36192,#36193,#36194,#36195,
#36196,#36197,#36198,#36199,#36200,#36201,#36202,#36203,#36204,#36205,#36206,
#36207,#36208,#36209,#36210,#36211,#36212,#36213,#36214,#36215,#36216,#36217,
#36218,#36219,#36220,#36221,#36222,#36223,#36224,#36225,#36226,#36227,#36228,
#36229,#36230,#36231,#36232,#36233,#36234,#36235,#36236,#36237,#36238,#36239,
#36240,#36241,#36242,#36243,#36244,#36245,#36246),.UNSPECIFIED.,.F.,.F.,
(4,3,3,3,3,3,3,3,3,3,3,3,3,3,3,3,3,3,3,3,3,3,3,3,3,3,3,3,3,3,3,3,3,3,3,
3,3,3,3,3,3,3,3,3,3,3,3,3,3,3,3,3,3,3,3,4),(47.1238898038476,47.2119796337542,
47.3005695584914,47.3893824075732,47.4784338092133,47.5265585755152,47.6042260557391,
47.6818075108085,47.7593168617452,47.8367577328693,47.9141589281681,47.9915342401346,
48.0253297661777,48.1088212118376,48.1924688565826,48.2763540794465,48.360352857849,
48.4445371137578,48.5241009568401,48.6016100896807,48.6790373653567,48.7563984005786,
48.8337087645722,48.9109839897546,48.9882524938714,49.0655202284855,49.1428012298417,
49.2201095390114,49.297505651097,49.3749474124556,49.4525086001948,49.521643338165,
49.5977094976221,49.6736809986562,49.7495746184532,49.8254070547404,49.9011949443246,
49.9784437912203,50.0542075898714,50.1299794959355,50.2057745134066,50.2841273149274,
50.3600558536292,50.4396207865596,50.5191857194899,50.5977395480502,50.6761992297749,
50.7545792646299,50.8328816291235,50.9111392843912,50.9893652504517,51.0675725263625,
51.1457915170971,51.2240148888098,51.3022833526319,51.3603137507763),
 .UNSPECIFIED.);
#3238=B_SPLINE_CURVE_WITH_KNOTS('',3,(#36252,#36253,#36254,#36255,#36256,
#36257,#36258,#36259,#36260,#36261,#36262,#36263,#36264,#36265,#36266,#36267,
#36268,#36269,#36270,#36271,#36272,#36273,#36274,#36275,#36276,#36277,#36278,
#36279,#36280,#36281,#36282,#36283,#36284,#36285,#36286,#36287,#36288,#36289,
#36290,#36291,#36292,#36293,#36294,#36295,#36296,#36297,#36298,#36299,#36300,
#36301,#36302,#36303,#36304,#36305,#36306,#36307,#36308,#36309,#36310,#36311,
#36312,#36313,#36314,#36315,#36316,#36317,#36318,#36319,#36320,#36321,#36322,
#36323,#36324,#36325,#36326,#36327,#36328,#36329,#36330,#36331,#36332,#36333,
#36334,#36335,#36336,#36337,#36338,#36339,#36340,#36341,#36342,#36343,#36344,
#36345,#36346,#36347,#36348,#36349,#36350,#36351,#36352,#36353,#36354,#36355,
#36356,#36357,#36358,#36359,#36360,#36361,#36362,#36363,#36364,#36365,#36366,
#36367,#36368,#36369,#36370,#36371,#36372,#36373,#36374,#36375,#36376,#36377,
#36378,#36379,#36380,#36381,#36382,#36383,#36384,#36385,#36386,#36387,#36388,
#36389,#36390,#36391,#36392,#36393,#36394,#36395,#36396,#36397,#36398,#36399,
#36400,#36401,#36402,#36403,#36404,#36405,#36406,#36407,#36408,#36409,#36410,
#36411,#36412,#36413,#36414,#36415,#36416,#36417,#36418,#36419,#36420),
 .UNSPECIFIED.,.F.,.F.,(4,3,3,3,3,3,3,3,3,3,3,3,3,3,3,3,3,3,3,3,3,3,3,3,
3,3,3,3,3,3,3,3,3,3,3,3,3,3,3,3,3,3,3,3,3,3,3,3,3,3,3,3,3,3,3,3,4),(53.4070751111297,
53.4818397072623,53.5565472546284,53.6312148585454,53.7058712697682,53.7805253462596,
53.8551924996201,53.929888159705,54.0046702141495,54.0795014793999,54.154443083463,
54.188078795572,54.2666234125106,54.3450754546814,54.4234494152635,54.5017597321029,
54.5800207974759,54.658250090743,54.7364628874877,54.8146721736151,54.8928909305534,
54.971164609666,55.0494668314322,55.1278522880078,55.1856211768969,55.2652701971631,
55.3448490888341,55.4243687315413,55.5038316430465,55.5832604938716,55.6626648933549,
55.6843923675594,55.7656244206493,55.8469051389876,55.9309697437962,56.0124018786526,
56.0977827184372,56.1831635582218,56.2683964816917,56.3535514429179,56.4385563796407,
56.523454671733,56.6081612180588,56.6819347488843,56.7584937135713,56.8350472804504,
56.9116100460281,56.9882285784958,57.0648783469907,57.1416114604804,57.1807059395467,
57.2602600160998,57.3397553727982,57.4191965518241,57.4986043528576,57.5779943149647,
57.6435975513154),.UNSPECIFIED.);
#3239=B_SPLINE_CURVE_WITH_KNOTS('',3,(#36421,#36422,#36423,#36424,#36425,
#36426,#36427,#36428,#36429,#36430,#36431,#36432,#36433,#36434,#36435,#36436,
#36437,#36438,#36439,#36440,#36441,#36442,#36443,#36444,#36445,#36446,#36447,
#36448,#36449,#36450,#36451,#36452,#36453,#36454,#36455,#36456,#36457,#36458,
#36459,#36460,#36461,#36462,#36463,#36464,#36465,#36466,#36467,#36468,#36469,
#36470,#36471,#36472,#36473,#36474,#36475,#36476,#36477,#36478,#36479,#36480,
#36481,#36482,#36483,#36484,#36485,#36486,#36487,#36488,#36489,#36490,#36491,
#36492,#36493,#36494,#36495,#36496,#36497,#36498,#36499,#36500,#36501,#36502),
 .UNSPECIFIED.,.F.,.F.,(4,3,3,3,3,3,3,3,3,3,3,3,3,3,3,3,3,3,3,3,3,3,3,3,
3,3,3,4),(51.361293208361,51.4387937872539,51.5162285057782,51.5936252425489,
51.6709973963902,51.6942228422598,51.7777142879196,51.8613619326647,51.9452471555287,
52.029245933931,52.1134301898398,52.1929940329222,52.2705031657628,52.3479304414389,
52.4252914766608,52.5026018406546,52.579877065837,52.6571455699538,52.7344133045679,
52.8116943059241,52.8890026150938,52.9663987271794,53.043840488538,53.1214016762773,
53.1905364142471,53.2988057626372,53.4011481782412,53.4070751110273),
 .UNSPECIFIED.);
#3240=B_SPLINE_CURVE_WITH_KNOTS('',3,(#36504,#36505,#36506,#36507,#36508,
#36509,#36510,#36511,#36512,#36513,#36514,#36515,#36516,#36517,#36518,#36519,
#36520,#36521,#36522,#36523,#36524,#36525,#36526,#36527,#36528,#36529,#36530,
#36531,#36532,#36533,#36534,#36535,#36536,#36537,#36538,#36539,#36540,#36541,
#36542,#36543,#36544,#36545,#36546,#36547,#36548,#36549,#36550,#36551,#36552,
#36553,#36554,#36555,#36556,#36557,#36558,#36559,#36560,#36561,#36562,#36563,
#36564,#36565,#36566,#36567,#36568,#36569,#36570,#36571,#36572,#36573,#36574,
#36575,#36576,#36577,#36578,#36579,#36580,#36581,#36582,#36583,#36584,#36585),
 .UNSPECIFIED.,.F.,.F.,(4,3,3,3,3,3,3,3,3,3,3,3,3,3,3,3,3,3,3,3,3,3,3,3,
3,3,3,4),(51.3603137507763,51.4386948092913,51.5167281008148,51.5963771210809,
51.6759560127519,51.7554756554591,51.8349385669643,51.914367417789,51.9937718172721,
52.0154992914772,52.0967313445668,52.1780120629056,52.2620766677142,52.3435088025703,
52.428889642355,52.5142704821397,52.5995034056097,52.6846583668364,52.7696633035593,
52.8545615956517,52.9392681419776,53.0130416728021,53.0874804553072,53.1619075737966,
53.2363594869538,53.3108262427439,53.3853476244306,53.4064882895547),
 .UNSPECIFIED.);
#3241=B_SPLINE_CURVE_WITH_KNOTS('',3,(#36586,#36587,#36588,#36589,#36590,
#36591,#36592,#36593,#36594,#36595,#36596,#36597,#36598,#36599,#36600,#36601,
#36602,#36603,#36604,#36605,#36606,#36607,#36608,#36609,#36610,#36611,#36612,
#36613,#36614,#36615,#36616,#36617,#36618,#36619,#36620,#36621,#36622,#36623,
#36624,#36625,#36626,#36627,#36628,#36629,#36630,#36631,#36632,#36633,#36634,
#36635,#36636,#36637,#36638,#36639,#36640,#36641,#36642,#36643,#36644,#36645,
#36646,#36647,#36648,#36649,#36650,#36651,#36652,#36653,#36654,#36655,#36656,
#36657,#36658,#36659,#36660,#36661,#36662,#36663,#36664,#36665,#36666,#36667,
#36668,#36669,#36670,#36671,#36672,#36673,#36674,#36675,#36676,#36677,#36678,
#36679,#36680,#36681,#36682,#36683,#36684,#36685,#36686,#36687,#36688,#36689,
#36690,#36691,#36692,#36693,#36694,#36695,#36696,#36697,#36698,#36699,#36700,
#36701,#36702,#36703,#36704,#36705,#36706,#36707,#36708,#36709,#36710,#36711,
#36712,#36713,#36714,#36715,#36716,#36717,#36718,#36719,#36720,#36721,#36722,
#36723,#36724,#36725,#36726,#36727,#36728,#36729,#36730,#36731,#36732,#36733,
#36734,#36735,#36736,#36737,#36738,#36739,#36740,#36741,#36742),
 .UNSPECIFIED.,.F.,.F.,(4,3,3,3,3,3,3,3,3,3,3,3,3,3,3,3,3,3,3,3,3,3,3,3,
3,3,3,3,3,3,3,3,3,3,3,3,3,3,3,3,3,3,3,3,3,3,3,3,3,3,3,3,4),(53.4070751110272,
53.4895373171274,53.5719991749299,53.6544606912851,53.7369218730428,53.819382727053,
53.9018432601651,53.9843034792282,54.0667633910913,54.1492230026029,54.2316823206116,
54.3141413519655,54.3966001035122,54.4790585820998,54.5615167945754,54.6439747477863,
54.7264324485793,54.8088899038012,54.8913471202984,54.9773598155844,55.0606846141428,
55.1431512197346,55.2256169811179,55.3080819257075,55.3905460809158,55.4730094741524,
55.5554721328241,55.6379340843352,55.7203953560876,55.8028559754807,55.8853159699119,
55.9677753667761,56.0502341934662,56.1326924773733,56.2151502458864,56.2976075263927,
56.3817416415839,56.4642076399438,56.54667201655,56.6291348810454,56.7115963430517,
56.794056512171,56.8765154979871,56.9589734100674,57.0445709049904,57.1270356420362,
57.2094974144226,57.2919566605877,57.3744138188264,57.456876337909,57.5393340093198,
57.6217928005129,57.6437533694508),.UNSPECIFIED.);
#3242=B_SPLINE_CURVE_WITH_KNOTS('',3,(#36748,#36749,#36750,#36751,#36752,
#36753,#36754,#36755,#36756,#36757,#36758,#36759,#36760,#36761,#36762,#36763,
#36764,#36765,#36766,#36767,#36768,#36769,#36770,#36771,#36772,#36773,#36774,
#36775,#36776,#36777,#36778,#36779,#36780,#36781,#36782,#36783,#36784,#36785,
#36786,#36787,#36788,#36789,#36790,#36791,#36792,#36793,#36794,#36795,#36796,
#36797,#36798,#36799,#36800,#36801,#36802,#36803,#36804,#36805,#36806,#36807,
#36808,#36809,#36810,#36811,#36812,#36813,#36814,#36815,#36816,#36817,#36818,
#36819,#36820,#36821,#36822,#36823,#36824,#36825,#36826,#36827,#36828,#36829,
#36830,#36831,#36832,#36833,#36834,#36835,#36836,#36837,#36838,#36839,#36840,
#36841,#36842,#36843,#36844,#36845,#36846,#36847,#36848,#36849,#36850,#36851,
#36852,#36853,#36854,#36855,#36856,#36857,#36858,#36859,#36860,#36861,#36862,
#36863,#36864,#36865,#36866,#36867,#36868,#36869,#36870,#36871,#36872,#36873,
#36874,#36875,#36876,#36877,#36878,#36879,#36880,#36881,#36882,#36883,#36884,
#36885,#36886,#36887,#36888,#36889,#36890,#36891,#36892,#36893,#36894,#36895,
#36896,#36897,#36898,#36899,#36900,#36901,#36902,#36903,#36904,#36905,#36906,
#36907,#36908,#36909,#36910,#36911,#36912,#36913),.UNSPECIFIED.,.F.,.F.,
(4,3,3,3,3,3,3,3,3,3,3,3,3,3,3,3,3,3,3,3,3,3,3,3,3,3,3,3,3,3,3,3,3,3,3,
3,3,3,3,3,3,3,3,3,3,3,3,3,3,3,3,3,3,3,3,4),(59.6902604183505,59.773786672866,
59.857514913502,59.9415451416528,60.0257275351874,60.1101466313872,60.1733330835214,
60.2493992429785,60.3253707440126,60.4012643638095,60.4770968000968,60.5528846896809,
60.6301335365766,60.7058973352277,60.7816692412918,60.8574642587629,60.9358170602838,
61.0117455989856,61.0913105319159,61.1708754648463,61.2494200817848,61.3278721239556,
61.4062460845375,61.4845564013767,61.5628174667496,61.6410467600166,61.7192595567613,
61.7974688428887,61.8756875998268,61.9539612789394,62.0322635007056,62.1106489572812,
62.1684178461712,62.2480668664373,62.3276457581083,62.4071654008154,62.4866283123206,
62.5660571631454,62.6454615626284,62.6671890368336,62.7484210899233,62.829701808262,
62.9137664130706,62.9951985479267,63.0805793877114,63.1659602274961,63.2511931509661,
63.3363481121926,63.4213530489155,63.5062513410079,63.5909578873339,63.6647314181585,
63.7412915888735,63.8178421365915,63.8944126561589,63.9265539370322),
 .UNSPECIFIED.);
#3243=B_SPLINE_CURVE_WITH_KNOTS('',3,(#36914,#36915,#36916,#36917,#36918,
#36919,#36920,#36921,#36922,#36923,#36924,#36925,#36926,#36927,#36928,#36929,
#36930,#36931,#36932,#36933,#36934,#36935,#36936,#36937,#36938,#36939,#36940,
#36941,#36942,#36943,#36944,#36945,#36946,#36947,#36948,#36949,#36950,#36951,
#36952,#36953,#36954,#36955,#36956,#36957,#36958,#36959,#36960,#36961,#36962,
#36963,#36964,#36965,#36966,#36967,#36968,#36969,#36970,#36971,#36972,#36973,
#36974,#36975,#36976,#36977,#36978,#36979,#36980,#36981,#36982,#36983,#36984,
#36985,#36986,#36987,#36988,#36989,#36990,#36991,#36992,#36993,#36994,#36995),
 .UNSPECIFIED.,.F.,.F.,(4,3,3,3,3,3,3,3,3,3,3,3,3,3,3,3,3,3,3,3,3,3,3,3,
3,3,3,4),(57.6435975513154,57.7229850624315,57.8023844693303,57.8818068498589,
57.9612999462789,58.0408296972273,58.1204509651146,58.1782483208716,58.2559158010956,
58.3334972561652,58.4110066071021,58.4884474782263,58.5658486735253,58.6432239854919,
58.677019511534,58.7605109571932,58.8441586019384,58.9280438248024,59.0120426032054,
59.0962268591141,59.1757907021965,59.2548924531588,59.3338943814981,59.4128084842863,
59.4916257902556,59.5703864116441,59.6490922606897,59.6902604182069),
 .UNSPECIFIED.);
#3244=B_SPLINE_CURVE_WITH_KNOTS('',3,(#36997,#36998,#36999,#37000,#37001,
#37002,#37003,#37004,#37005,#37006,#37007,#37008,#37009,#37010,#37011,#37012,
#37013,#37014,#37015,#37016,#37017,#37018,#37019,#37020,#37021,#37022,#37023,
#37024,#37025,#37026,#37027,#37028,#37029,#37030,#37031,#37032,#37033,#37034,
#37035,#37036,#37037,#37038,#37039,#37040,#37041,#37042,#37043,#37044,#37045,
#37046,#37047,#37048,#37049,#37050,#37051,#37052,#37053,#37054,#37055,#37056,
#37057,#37058,#37059,#37060,#37061,#37062,#37063,#37064,#37065,#37066,#37067,
#37068,#37069,#37070,#37071,#37072),.UNSPECIFIED.,.F.,.F.,(4,3,3,3,3,3,
3,3,3,3,3,3,3,3,3,3,3,3,3,3,3,3,3,3,3,4),(57.6437533694508,57.7262149731809,
57.8086759110328,57.8911362104048,57.973595898693,58.0560550032914,58.1385135515919,
58.2209715709845,58.3034290888572,58.3901060469355,58.4725728324766,58.5550379455445,
58.6375014957924,58.7199635928517,58.8024243463332,58.8848838658292,58.9673422609144,
59.0497996411478,59.1322660268339,59.2147292283421,59.2971896841918,59.3796478327465,
59.4621134365,59.5445733148879,59.6270374261401,59.690260418109),
 .UNSPECIFIED.);
#3245=B_SPLINE_CURVE_WITH_KNOTS('',3,(#37073,#37074,#37075,#37076,#37077,
#37078,#37079,#37080,#37081,#37082,#37083,#37084,#37085,#37086,#37087,#37088,
#37089,#37090,#37091,#37092,#37093,#37094,#37095,#37096,#37097,#37098,#37099,
#37100,#37101,#37102,#37103,#37104,#37105,#37106,#37107,#37108,#37109,#37110,
#37111,#37112,#37113,#37114,#37115,#37116,#37117,#37118,#37119,#37120,#37121,
#37122,#37123,#37124,#37125,#37126,#37127,#37128,#37129,#37130,#37131,#37132,
#37133,#37134,#37135,#37136,#37137,#37138,#37139,#37140,#37141,#37142,#37143,
#37144,#37145,#37146,#37147,#37148,#37149,#37150,#37151,#37152,#37153,#37154,
#37155,#37156,#37157,#37158,#37159,#37160,#37161,#37162,#37163,#37164,#37165,
#37166,#37167,#37168,#37169,#37170,#37171,#37172,#37173,#37174,#37175,#37176,
#37177,#37178,#37179,#37180,#37181,#37182,#37183,#37184,#37185,#37186,#37187,
#37188,#37189,#37190,#37191,#37192,#37193,#37194,#37195,#37196,#37197,#37198,
#37199,#37200,#37201,#37202,#37203,#37204,#37205,#37206,#37207,#37208,#37209,
#37210,#37211,#37212,#37213,#37214,#37215,#37216,#37217,#37218,#37219,#37220,
#37221,#37222,#37223,#37224,#37225,#37226,#37227,#37228,#37229),
 .UNSPECIFIED.,.F.,.F.,(4,3,3,3,3,3,3,3,3,3,3,3,3,3,3,3,3,3,3,3,3,3,3,3,
3,3,3,3,3,3,3,3,3,3,3,3,3,3,3,3,3,3,3,3,3,3,3,3,3,3,3,3,4),(59.6902604182067,
59.7727226243069,59.8551844821094,59.9376459984645,60.0201071802223,60.1025680342325,
60.1850285673446,60.2674887864077,60.3499486982708,60.4324083097826,60.5148676277913,
60.5973266591451,60.679785410692,60.7622438892796,60.8447021017553,60.9271600549663,
61.0096177557593,61.0920752109812,61.1745324274788,61.2605451227648,61.3438699213231,
61.426336526915,61.5088022882982,61.5912672328878,61.6737313880962,61.7561947813327,
61.8386574400044,61.9211193915156,62.0035806632679,62.0860412826611,62.1685012770921,
62.2509606739563,62.3334195006465,62.4158777845535,62.4983355530665,62.5807928335728,
62.6649269487639,62.7473929471238,62.8298573237301,62.9123201882255,62.9947816502318,
63.077241819351,63.1597008051672,63.2421587172475,63.3277562121703,63.4102209492162,
63.4926827216026,63.5751419677676,63.6575991260063,63.7400616450889,63.8225193164998,
63.9049781076929,63.9269386766303),.UNSPECIFIED.);
#3246=B_SPLINE_CURVE_WITH_KNOTS('',3,(#37235,#37236,#37237,#37238,#37239,
#37240,#37241,#37242,#37243,#37244,#37245,#37246,#37247,#37248,#37249,#37250,
#37251,#37252,#37253,#37254,#37255,#37256,#37257,#37258,#37259,#37260,#37261,
#37262,#37263,#37264,#37265,#37266,#37267,#37268,#37269,#37270,#37271,#37272,
#37273,#37274,#37275,#37276,#37277,#37278,#37279,#37280,#37281,#37282,#37283,
#37284,#37285,#37286,#37287,#37288,#37289,#37290,#37291,#37292,#37293,#37294,
#37295,#37296,#37297,#37298,#37299,#37300,#37301,#37302,#37303,#37304,#37305,
#37306,#37307,#37308,#37309,#37310,#37311,#37312,#37313,#37314,#37315,#37316,
#37317,#37318,#37319,#37320,#37321,#37322,#37323,#37324,#37325,#37326,#37327,
#37328,#37329,#37330,#37331,#37332,#37333,#37334,#37335,#37336,#37337,#37338,
#37339,#37340,#37341,#37342,#37343,#37344,#37345,#37346,#37347,#37348,#37349,
#37350,#37351,#37352,#37353,#37354,#37355,#37356,#37357,#37358,#37359,#37360,
#37361,#37362,#37363,#37364,#37365,#37366,#37367,#37368,#37369,#37370,#37371,
#37372,#37373,#37374,#37375,#37376,#37377,#37378,#37379,#37380,#37381,#37382,
#37383,#37384,#37385,#37386,#37387,#37388,#37389,#37390,#37391,#37392,#37393,
#37394,#37395,#37396,#37397,#37398,#37399,#37400),.UNSPECIFIED.,.F.,.F.,
(4,3,3,3,3,3,3,3,3,3,3,3,3,3,3,3,3,3,3,3,3,3,3,3,3,3,3,3,3,3,3,3,3,3,3,
3,3,3,3,3,3,3,3,3,3,3,3,3,3,3,3,3,3,3,3,4),(65.9734457253864,66.0829124996505,
66.1585873714707,66.2360965043113,66.3135237799874,66.3908848152093,66.4681951792031,
66.5454704043854,66.6227389085023,66.7000066431164,66.7772876444726,66.8545959536425,
66.9319920657281,67.0094338270867,67.086995014826,67.1561297527956,67.2321959122527,
67.3081674132868,67.3840610330838,67.459893469371,67.5356813589552,67.6129302058509,
67.688694004502,67.7644659105661,67.8402609280372,67.918613729558,67.9945422682598,
68.0741072011901,68.1536721341205,68.232216751059,68.3106687932298,68.3890427538117,
68.4673530706508,68.5456141360238,68.6238434292908,68.7020562260355,68.7802655121629,
68.8584842691011,68.9367579482137,69.0150601699799,69.0934456265554,69.1512145154454,
69.2308635357115,69.3104424273825,69.3899620700895,69.4694249815946,69.5488538324195,
69.6282582319025,69.6499857061079,69.7312177591976,69.8124984775364,69.8965630823449,
69.9779952172011,70.0633760569857,70.1487568967703,70.2102685302427),
 .UNSPECIFIED.);
#3247=B_SPLINE_CURVE_WITH_KNOTS('',3,(#37401,#37402,#37403,#37404,#37405,
#37406,#37407,#37408,#37409,#37410,#37411,#37412,#37413,#37414,#37415,#37416,
#37417,#37418,#37419,#37420,#37421,#37422,#37423,#37424,#37425,#37426,#37427,
#37428,#37429,#37430,#37431,#37432,#37433,#37434,#37435,#37436,#37437,#37438,
#37439,#37440,#37441,#37442,#37443,#37444,#37445,#37446,#37447,#37448,#37449,
#37450,#37451,#37452,#37453,#37454,#37455,#37456,#37457,#37458,#37459,#37460,
#37461,#37462,#37463,#37464,#37465,#37466,#37467,#37468,#37469,#37470,#37471,
#37472,#37473,#37474,#37475,#37476,#37477,#37478,#37479,#37480,#37481,#37482),
 .UNSPECIFIED.,.F.,.F.,(4,3,3,3,3,3,3,3,3,3,3,3,3,3,3,3,3,3,3,3,3,3,3,3,
3,3,3,4),(63.9265539370322,64.00318398046,64.0833432946404,64.1635026088209,
64.2430544733194,64.3225462087708,64.4019900674868,64.4813982643922,64.560782985931,
64.6401690219161,64.7195578032026,64.7989604018192,64.8783878974505,64.9578866205902,
65.037423765986,65.1170492994503,65.1610449901458,65.2387124703698,65.3162939254393,
65.3938032763762,65.4712441475004,65.5486453427992,65.6260206547658,65.6598161808083,
65.7382235669259,65.8164648295238,65.8949552774012,65.9734457252786),
 .UNSPECIFIED.);
#3248=B_SPLINE_CURVE_WITH_KNOTS('',3,(#37484,#37485,#37486,#37487,#37488,
#37489,#37490,#37491,#37492,#37493,#37494,#37495,#37496,#37497,#37498,#37499,
#37500,#37501,#37502,#37503,#37504,#37505,#37506,#37507,#37508,#37509,#37510,
#37511,#37512,#37513,#37514,#37515,#37516,#37517,#37518,#37519,#37520,#37521,
#37522,#37523,#37524,#37525,#37526,#37527,#37528,#37529,#37530,#37531,#37532,
#37533,#37534,#37535,#37536,#37537,#37538,#37539,#37540,#37541,#37542,#37543,
#37544,#37545,#37546,#37547,#37548,#37549,#37550,#37551,#37552,#37553,#37554,
#37555,#37556,#37557,#37558,#37559),.UNSPECIFIED.,.F.,.F.,(4,3,3,3,3,3,
3,3,3,3,3,3,3,3,3,3,3,3,3,3,3,3,3,3,3,4),(63.9269386766303,64.0094002803605,
64.0918612182123,64.1743215175843,64.2567812058726,64.3392403104709,64.4216988587714,
64.5041568781639,64.5866143960367,64.673291354121,64.7557581396621,64.83822325273,
64.920686802978,65.0031489000373,65.0856096535188,65.1680691730148,65.2505275681,
65.3329849483335,65.4154513340197,65.4979145355279,65.5803749913775,65.6628331399324,
65.745298743686,65.8277586220738,65.9102227333261,65.9734457253863),
 .UNSPECIFIED.);
#3249=B_SPLINE_CURVE_WITH_KNOTS('',3,(#37560,#37561,#37562,#37563,#37564,
#37565,#37566,#37567,#37568,#37569,#37570,#37571,#37572,#37573,#37574,#37575,
#37576,#37577,#37578,#37579,#37580,#37581,#37582,#37583,#37584,#37585,#37586,
#37587,#37588,#37589,#37590,#37591,#37592,#37593,#37594,#37595,#37596,#37597,
#37598,#37599,#37600,#37601,#37602,#37603,#37604,#37605,#37606,#37607,#37608,
#37609,#37610,#37611,#37612,#37613,#37614,#37615,#37616,#37617,#37618,#37619,
#37620,#37621,#37622,#37623,#37624,#37625,#37626,#37627,#37628,#37629,#37630,
#37631,#37632,#37633,#37634,#37635,#37636,#37637,#37638,#37639,#37640,#37641,
#37642,#37643,#37644,#37645,#37646,#37647,#37648,#37649,#37650,#37651,#37652,
#37653,#37654,#37655,#37656,#37657,#37658,#37659,#37660,#37661,#37662,#37663,
#37664,#37665,#37666,#37667,#37668,#37669,#37670,#37671,#37672,#37673,#37674,
#37675,#37676,#37677,#37678,#37679,#37680,#37681,#37682,#37683,#37684,#37685,
#37686,#37687,#37688,#37689,#37690,#37691,#37692,#37693,#37694,#37695,#37696,
#37697,#37698,#37699,#37700,#37701,#37702,#37703,#37704,#37705,#37706,#37707,
#37708,#37709,#37710,#37711,#37712,#37713,#37714,#37715,#37716,#37717,#37718,
#37719,#37720,#37721,#37722,#37723,#37724,#37725,#37726,#37727,#37728),
 .UNSPECIFIED.,.F.,.F.,(4,3,3,3,3,3,3,3,3,3,3,3,3,3,3,3,3,3,3,3,3,3,3,3,
3,3,3,3,3,3,3,3,3,3,3,3,3,3,3,3,3,3,3,3,3,3,3,3,3,3,3,3,3,3,3,3,4),(65.9734457253863,
65.9810926300257,66.0623246831153,66.1436054014539,66.2276700062625,66.3091021411186,
66.3944829809034,66.4798638206882,66.5650967441582,66.6502517053848,66.7352566421077,
66.8201549341999,66.9048614805259,66.9786350113506,67.0551939760377,67.1317475429172,
67.2083103084957,67.2849288409634,67.3615786094582,67.4383117229479,67.4774062020131,
67.5569580665117,67.636449801963,67.7158936606789,67.7953018575844,67.8746865791232,
67.9540726151082,68.0334613963946,68.1128639950112,68.1922914906426,68.2717902137823,
68.3513273591781,68.4309528926424,68.474948583338,68.5526160635619,68.6301975186313,
68.7077068695681,68.7851477406922,68.8625489359912,68.9399242479578,68.9737197740004,
69.0572112196602,69.1408588644053,69.2247440872693,69.3087428656718,69.3929271215806,
69.4724909646629,69.550013477377,69.6274512587079,69.7048066037302,69.7821149488811,
69.859390366979,69.9366469095249,70.0139157169229,70.0911907175262,70.168510631772,
70.2097424676708),.UNSPECIFIED.);
#3250=B_SPLINE_CURVE_WITH_KNOTS('',3,(#37734,#37735,#37736,#37737,#37738,
#37739,#37740,#37741,#37742,#37743,#37744,#37745,#37746,#37747,#37748,#37749,
#37750,#37751,#37752,#37753,#37754,#37755,#37756,#37757,#37758,#37759,#37760,
#37761,#37762,#37763,#37764,#37765,#37766,#37767,#37768,#37769,#37770,#37771,
#37772,#37773,#37774,#37775,#37776,#37777,#37778,#37779,#37780,#37781,#37782,
#37783,#37784,#37785,#37786,#37787,#37788,#37789,#37790,#37791,#37792,#37793,
#37794,#37795,#37796,#37797,#37798,#37799,#37800,#37801,#37802,#37803,#37804,
#37805,#37806,#37807,#37808,#37809,#37810,#37811,#37812,#37813,#37814,#37815,
#37816,#37817,#37818,#37819,#37820,#37821,#37822,#37823,#37824,#37825,#37826,
#37827,#37828,#37829,#37830,#37831,#37832,#37833,#37834,#37835,#37836,#37837,
#37838,#37839,#37840,#37841,#37842,#37843,#37844,#37845,#37846,#37847,#37848,
#37849,#37850,#37851,#37852,#37853,#37854,#37855,#37856,#37857,#37858,#37859,
#37860,#37861,#37862,#37863,#37864,#37865,#37866,#37867,#37868,#37869,#37870,
#37871,#37872,#37873,#37874,#37875,#37876,#37877,#37878,#37879,#37880,#37881,
#37882,#37883,#37884,#37885,#37886,#37887,#37888,#37889,#37890,#37891,#37892,
#37893,#37894,#37895,#37896,#37897,#37898,#37899,#37900,#37901,#37902),
 .UNSPECIFIED.,.F.,.F.,(4,3,3,3,3,3,3,3,3,3,3,3,3,3,3,3,3,3,3,3,3,3,3,3,
3,3,3,3,3,3,3,3,3,3,3,3,3,3,3,3,3,3,3,3,3,3,3,3,3,3,3,3,3,3,3,3,4),(72.2566310327126,
72.3313121276164,72.4091373082329,72.4837084895956,72.5582532064747,72.632791315131,
72.6426128500825,72.726104295742,72.8097519404872,72.8936371633511,72.9776359417537,
73.0618201976625,73.141384040745,73.2188931735855,73.2963204492617,73.3736814844835,
73.4509918484771,73.5282670736598,73.6055355777766,73.6828033123908,73.760084313747,
73.8373926229171,73.9147887350027,73.9922304963612,74.0697916841005,74.1389264220699,
74.214992581527,74.2909640825609,74.3668577023579,74.4426901386452,74.5184780282295,
74.5957268751251,74.6714906737762,74.7472625798402,74.8230575973111,74.9014103988321,
74.977338937534,75.0569038704644,75.1364688033948,75.2150134203333,75.2934654625038,
75.3718394230859,75.4501497399251,75.5284108052985,75.6066400985656,75.6848528953103,
75.7630621814379,75.8412809383761,75.9195546174888,75.997856839255,76.0762422958305,
76.1340111847197,76.2136727228051,76.2932430320982,76.3727592970901,76.4522228690431,
76.4934152645304),.UNSPECIFIED.);
#3251=B_SPLINE_CURVE_WITH_KNOTS('',3,(#37903,#37904,#37905,#37906,#37907,
#37908,#37909,#37910,#37911,#37912,#37913,#37914,#37915,#37916,#37917,#37918,
#37919,#37920,#37921,#37922,#37923,#37924,#37925,#37926,#37927,#37928,#37929,
#37930,#37931,#37932,#37933,#37934,#37935,#37936,#37937,#37938,#37939,#37940,
#37941,#37942,#37943,#37944,#37945,#37946,#37947,#37948,#37949,#37950,#37951,
#37952,#37953,#37954,#37955,#37956,#37957,#37958,#37959,#37960,#37961,#37962,
#37963,#37964,#37965,#37966,#37967,#37968,#37969,#37970,#37971,#37972,#37973,
#37974,#37975,#37976,#37977,#37978,#37979,#37980,#37981,#37982,#37983,#37984,
#37985,#37986,#37987),.UNSPECIFIED.,.F.,.F.,(4,3,3,3,3,3,3,3,3,3,3,3,3,
3,3,3,3,3,3,3,3,3,3,3,3,3,3,3,4),(70.2102685302427,70.2954469856682,70.3834672611094,
70.4683925970241,70.5532024315297,70.6378374491525,70.6475280874328,70.7240870521199,
70.8006406189992,70.8772033845776,70.9538219170453,71.0304716855401,71.1072047990298,
71.1462992780952,71.2258511425937,71.305342878045,71.3847867367609,71.4641949336664,
71.5435796552054,71.6229656911904,71.7023544724769,71.7817570710934,71.8611845667248,
71.9406832898644,72.0202204352601,72.0998459687243,72.1438416594201,72.2468670271058,
72.256631032566),.UNSPECIFIED.);
#3252=B_SPLINE_CURVE_WITH_KNOTS('',3,(#37989,#37990,#37991,#37992,#37993,
#37994,#37995,#37996,#37997,#37998,#37999,#38000,#38001,#38002,#38003,#38004,
#38005,#38006,#38007,#38008,#38009,#38010,#38011,#38012,#38013,#38014,#38015,
#38016,#38017,#38018,#38019,#38020,#38021,#38022,#38023,#38024,#38025,#38026,
#38027,#38028,#38029,#38030,#38031,#38032,#38033,#38034,#38035,#38036,#38037,
#38038,#38039,#38040,#38041,#38042,#38043,#38044,#38045,#38046,#38047,#38048,
#38049,#38050,#38051,#38052,#38053,#38054,#38055,#38056,#38057,#38058,#38059,
#38060,#38061,#38062,#38063,#38064,#38065,#38066,#38067,#38068,#38069,#38070),
 .UNSPECIFIED.,.F.,.F.,(4,3,3,3,3,3,3,3,3,3,3,3,3,3,3,3,3,3,3,3,3,3,3,3,
3,3,3,4),(70.2097424676708,70.2871613343337,70.3646325929258,70.4422117669932,
70.4700333459878,70.5460995054449,70.6220710064789,70.6979646262759,70.7737970625631,
70.8495849521472,70.9268337990429,71.002597597694,71.0783695037581,71.1541645212292,
71.2325173227501,71.3084458614519,71.3880107943822,71.4675757273126,71.5456282131303,
71.6235863221168,71.7027169109229,71.7805192981694,71.8582788079244,71.9360090598409,
72.0161645530222,72.0938914798003,72.1752612561831,72.2566310325659),
 .UNSPECIFIED.);
#3253=B_SPLINE_CURVE_WITH_KNOTS('',3,(#38071,#38072,#38073,#38074,#38075,
#38076,#38077,#38078,#38079,#38080,#38081,#38082,#38083,#38084,#38085,#38086,
#38087,#38088,#38089,#38090,#38091,#38092,#38093,#38094,#38095,#38096,#38097,
#38098,#38099,#38100,#38101,#38102,#38103,#38104,#38105,#38106,#38107,#38108,
#38109,#38110,#38111,#38112,#38113,#38114,#38115,#38116,#38117,#38118,#38119,
#38120,#38121,#38122,#38123,#38124,#38125,#38126,#38127,#38128,#38129,#38130,
#38131,#38132,#38133,#38134,#38135,#38136,#38137,#38138,#38139,#38140,#38141,
#38142,#38143,#38144,#38145,#38146,#38147,#38148,#38149,#38150,#38151,#38152,
#38153,#38154,#38155,#38156,#38157,#38158,#38159,#38160,#38161,#38162,#38163,
#38164,#38165,#38166,#38167,#38168,#38169,#38170,#38171,#38172,#38173,#38174,
#38175,#38176,#38177,#38178,#38179,#38180,#38181,#38182,#38183,#38184,#38185,
#38186,#38187,#38188,#38189,#38190,#38191,#38192,#38193,#38194,#38195,#38196,
#38197,#38198,#38199,#38200,#38201,#38202,#38203,#38204,#38205,#38206,#38207,
#38208,#38209,#38210,#38211,#38212,#38213,#38214,#38215,#38216,#38217,#38218,
#38219,#38220,#38221,#38222,#38223,#38224,#38225,#38226,#38227,#38228,#38229,
#38230,#38231,#38232,#38233,#38234,#38235,#38236),.UNSPECIFIED.,.F.,.F.,
(4,3,3,3,3,3,3,3,3,3,3,3,3,3,3,3,3,3,3,3,3,3,3,3,3,3,3,3,3,3,3,3,3,3,3,
3,3,3,3,3,3,3,3,3,3,3,3,3,3,3,3,3,3,3,3,4),(72.2566310326885,72.360874570663,
72.4651181086375,72.5447671289035,72.6243460205744,72.7038656632815,72.7833285747867,
72.8627574256116,72.9421618250946,72.9638892993,73.0451213523897,73.1264020707285,
73.2104666755369,73.2918988103931,73.3772796501777,73.4626604899624,73.5478934134323,
73.6330483746588,73.7180533113817,73.802951603474,73.8876581497999,73.9614316806249,
74.037990645312,74.1145442121913,74.1911069777697,74.2677255102374,74.3443752787323,
74.421108392222,74.4602028712873,74.5397547357858,74.6192464712371,74.6986903299531,
74.7780985268585,74.8574832483973,74.9368692843824,75.0162580656689,75.0956606642855,
75.1750881599169,75.2545868830565,75.3341240284524,75.4137495619166,75.4577452526122,
75.5354127328361,75.6129941879055,75.6905035388423,75.7679444099664,75.8453456052653,
75.922720917232,75.9565164432747,76.0400078889345,76.1236555336797,76.2075407565437,
76.2915395349461,76.3757237908549,76.4552876339371,76.493677445244),
 .UNSPECIFIED.);
#3254=B_SPLINE_CURVE_WITH_KNOTS('',3,(#38242,#38243,#38244,#38245,#38246,
#38247,#38248,#38249,#38250,#38251,#38252,#38253,#38254,#38255,#38256,#38257,
#38258,#38259,#38260,#38261,#38262,#38263,#38264,#38265,#38266,#38267,#38268,
#38269,#38270,#38271,#38272,#38273,#38274,#38275,#38276,#38277,#38278,#38279,
#38280,#38281,#38282,#38283,#38284,#38285,#38286,#38287,#38288,#38289,#38290,
#38291,#38292,#38293,#38294,#38295,#38296,#38297,#38298,#38299,#38300,#38301,
#38302,#38303,#38304,#38305,#38306,#38307,#38308,#38309,#38310,#38311,#38312,
#38313,#38314,#38315,#38316,#38317,#38318,#38319,#38320,#38321,#38322,#38323,
#38324,#38325,#38326,#38327,#38328,#38329,#38330,#38331,#38332,#38333,#38334,
#38335,#38336,#38337,#38338,#38339,#38340,#38341,#38342,#38343,#38344,#38345,
#38346,#38347,#38348,#38349,#38350,#38351,#38352,#38353,#38354,#38355,#38356,
#38357,#38358,#38359,#38360,#38361,#38362,#38363,#38364,#38365,#38366,#38367,
#38368,#38369,#38370,#38371,#38372,#38373,#38374,#38375,#38376,#38377,#38378,
#38379,#38380,#38381,#38382,#38383,#38384,#38385,#38386,#38387,#38388,#38389,
#38390,#38391,#38392,#38393,#38394,#38395,#38396,#38397,#38398),
 .UNSPECIFIED.,.F.,.F.,(4,3,3,3,3,3,3,3,3,3,3,3,3,3,3,3,3,3,3,3,3,3,3,3,
3,3,3,3,3,3,3,3,3,3,3,3,3,3,3,3,3,3,3,3,3,3,3,3,3,3,3,3,4),(78.5398163397456,
78.6222785458458,78.7047404036483,78.7872019200034,78.8696631017612,78.9521239557714,
79.0345844888835,79.1170447079467,79.1995046198099,79.2819642313217,79.3644235493305,
79.4468825806843,79.5293413322312,79.6117998108189,79.6942580232945,79.7767159765052,
79.8591736772983,79.9416311325201,80.0240883490175,80.1101010443035,80.1934258428618,
80.2758924484537,80.3583582098369,80.4408231544265,80.5232873096349,80.6057507028715,
80.6882133615431,80.7706753130542,80.8531365848066,80.9355972041998,81.0180571986309,
81.1005165954951,81.1829754221853,81.2654337060924,81.3478914746055,81.4303487551118,
81.5144828703029,81.5969488686628,81.679413245269,81.7618761097644,81.8443375717707,
81.92679774089,82.0092567267061,82.0917146387864,82.1773121337093,82.2597768707552,
82.3422386431415,82.4246978893066,82.5071550475453,82.5896175666279,82.6720752380387,
82.7545340292318,82.7764945981692),.UNSPECIFIED.);
#3255=B_SPLINE_CURVE_WITH_KNOTS('',3,(#38399,#38400,#38401,#38402,#38403,
#38404,#38405,#38406,#38407,#38408,#38409,#38410,#38411,#38412,#38413,#38414,
#38415,#38416,#38417,#38418,#38419,#38420,#38421,#38422,#38423,#38424,#38425,
#38426,#38427,#38428,#38429,#38430,#38431,#38432,#38433,#38434,#38435,#38436,
#38437,#38438,#38439,#38440,#38441,#38442,#38443,#38444,#38445,#38446,#38447,
#38448,#38449,#38450,#38451,#38452,#38453,#38454,#38455,#38456,#38457,#38458,
#38459,#38460,#38461,#38462,#38463,#38464,#38465,#38466,#38467,#38468,#38469,
#38470,#38471,#38472,#38473,#38474,#38475,#38476,#38477),.UNSPECIFIED.,
 .F.,.F.,(4,3,3,3,3,3,3,3,3,3,3,3,3,3,3,3,3,3,3,3,3,3,3,3,3,3,4),(76.4934152645304,
76.5728312760312,76.6327823753821,76.7140144284718,76.7952951468106,76.8793597516191,
76.9607918864751,77.0461727262598,77.1315535660446,77.2167864895144,77.3019414507413,
77.3869463874641,77.471844679557,77.5565512258828,77.630324756707,77.7068837213938,
77.7834372882729,77.8600000538509,77.9366185863188,78.0132683548138,78.0900014683037,
78.1290959473694,78.2166417543684,78.304004464484,78.3912175495642,78.4781314906048,
78.5398163397456),.UNSPECIFIED.);
#3256=B_SPLINE_CURVE_WITH_KNOTS('',3,(#38479,#38480,#38481,#38482,#38483,
#38484,#38485,#38486,#38487,#38488,#38489,#38490,#38491,#38492,#38493,#38494,
#38495,#38496,#38497,#38498,#38499,#38500,#38501,#38502,#38503,#38504,#38505,
#38506,#38507,#38508,#38509,#38510,#38511,#38512,#38513,#38514,#38515,#38516,
#38517,#38518,#38519,#38520,#38521,#38522,#38523,#38524,#38525,#38526,#38527,
#38528,#38529,#38530,#38531,#38532,#38533,#38534,#38535,#38536,#38537,#38538,
#38539,#38540,#38541,#38542,#38543,#38544,#38545,#38546,#38547,#38548,#38549,
#38550,#38551,#38552,#38553,#38554,#38555,#38556,#38557,#38558,#38559,#38560),
 .UNSPECIFIED.,.F.,.F.,(4,3,3,3,3,3,3,3,3,3,3,3,3,3,3,3,3,3,3,3,3,3,3,3,
3,3,3,4),(76.493677445244,76.5711440912438,76.6485366193094,76.7258706212713,
76.8031616468261,76.8843701928806,76.9616365371571,77.038909777402,77.1162039515329,
77.1935331065581,77.2709525658535,77.3484245796304,77.4260042417807,77.452830015262,
77.5288961747191,77.6048676757532,77.6807612955502,77.7565937318376,77.8323816214217,
77.9096304683173,77.9853942669685,78.0611661730325,78.1369611905036,78.2153139920244,
78.2912425307263,78.3708074636566,78.4503723965869,78.5398163397455),
 .UNSPECIFIED.);
#3257=B_SPLINE_CURVE_WITH_KNOTS('',3,(#38561,#38562,#38563,#38564,#38565,
#38566,#38567,#38568,#38569,#38570,#38571,#38572,#38573,#38574,#38575,#38576,
#38577,#38578,#38579,#38580,#38581,#38582,#38583,#38584,#38585,#38586,#38587,
#38588,#38589,#38590,#38591,#38592,#38593,#38594,#38595,#38596,#38597,#38598,
#38599,#38600,#38601,#38602,#38603,#38604,#38605,#38606,#38607,#38608,#38609,
#38610,#38611,#38612,#38613,#38614,#38615,#38616,#38617,#38618,#38619,#38620,
#38621,#38622,#38623,#38624,#38625,#38626,#38627,#38628,#38629,#38630,#38631,
#38632,#38633,#38634,#38635,#38636,#38637,#38638,#38639,#38640,#38641,#38642,
#38643,#38644,#38645,#38646,#38647,#38648,#38649,#38650,#38651,#38652,#38653,
#38654,#38655,#38656,#38657,#38658,#38659,#38660,#38661,#38662,#38663,#38664,
#38665,#38666,#38667,#38668,#38669,#38670,#38671,#38672,#38673,#38674,#38675,
#38676,#38677,#38678,#38679,#38680,#38681,#38682,#38683,#38684,#38685,#38686,
#38687,#38688,#38689,#38690,#38691,#38692,#38693,#38694,#38695,#38696,#38697,
#38698,#38699,#38700,#38701,#38702,#38703,#38704,#38705,#38706,#38707,#38708,
#38709,#38710,#38711,#38712,#38713,#38714,#38715,#38716,#38717,#38718,#38719,
#38720,#38721,#38722,#38723,#38724,#38725,#38726,#38727,#38728,#38729),
 .UNSPECIFIED.,.F.,.F.,(4,3,3,3,3,3,3,3,3,3,3,3,3,3,3,3,3,3,3,3,3,3,3,3,
3,3,3,3,3,3,3,3,3,3,3,3,3,3,3,3,3,3,3,3,3,3,3,3,3,3,3,3,3,3,3,3,4),(78.539816339892,
78.617154154896,78.6944012009266,78.7715733540667,78.8486864351297,78.9257566485886,
79.002804254068,79.0798434968287,79.1568886147571,79.2339870215937,79.3111130641337,
79.3883252186171,79.4479147779118,79.5275637981778,79.607142689849,79.6866623325567,
79.766125244062,79.8455540948865,79.9249584943695,79.9466859685742,80.0279180216639,
80.1091987400025,80.1932633448111,80.2746954796673,80.360076319452,80.4454571592367,
80.5306900827067,80.6158450439336,80.7008499806565,80.7857482727492,80.8704548190752,
80.9442283498991,81.0207873145861,81.0973408814656,81.1739036470445,81.2505221795123,
81.3271719480072,81.4039050614971,81.4429995405616,81.52255140506,81.6020431405114,
81.6814869992272,81.7608951961323,81.8402799176709,81.919665953656,81.9990547349426,
82.0784573335592,82.1578848291906,82.2373835523303,82.3169206977262,82.3965462311905,
82.4405419218865,82.5182286726415,82.5958021443857,82.6733101098667,82.7507541166275,
82.7769101946331),.UNSPECIFIED.);
#3258=B_SPLINE_CURVE_WITH_KNOTS('',3,(#38735,#38736,#38737,#38738,#38739,
#38740,#38741,#38742,#38743,#38744,#38745,#38746,#38747,#38748,#38749,#38750,
#38751,#38752,#38753,#38754,#38755,#38756,#38757,#38758,#38759,#38760,#38761,
#38762,#38763,#38764,#38765,#38766,#38767,#38768,#38769,#38770,#38771,#38772,
#38773,#38774,#38775,#38776,#38777,#38778,#38779,#38780,#38781,#38782,#38783,
#38784,#38785,#38786,#38787,#38788,#38789,#38790,#38791,#38792,#38793,#38794,
#38795,#38796,#38797,#38798,#38799,#38800,#38801,#38802,#38803,#38804,#38805,
#38806,#38807,#38808,#38809,#38810,#38811,#38812,#38813,#38814,#38815,#38816,
#38817,#38818,#38819,#38820,#38821,#38822,#38823,#38824,#38825,#38826,#38827,
#38828,#38829,#38830,#38831,#38832,#38833,#38834,#38835,#38836,#38837,#38838,
#38839,#38840,#38841,#38842,#38843,#38844,#38845,#38846,#38847,#38848,#38849,
#38850,#38851,#38852,#38853,#38854,#38855,#38856,#38857,#38858,#38859,#38860,
#38861,#38862,#38863,#38864,#38865,#38866,#38867,#38868,#38869,#38870,#38871,
#38872,#38873,#38874,#38875,#38876,#38877,#38878,#38879,#38880,#38881,#38882,
#38883,#38884,#38885,#38886,#38887,#38888,#38889,#38890,#38891,#38892,#38893,
#38894,#38895,#38896,#38897,#38898,#38899,#38900,#38901,#38902,#38903),
 .UNSPECIFIED.,.F.,.F.,(4,3,3,3,3,3,3,3,3,3,3,3,3,3,3,3,3,3,3,3,3,3,3,3,
3,3,3,3,3,3,3,3,3,3,3,3,3,3,3,3,3,3,3,3,3,3,3,3,3,3,3,3,3,3,3,3,4),(84.8230016469252,
84.9046620215766,84.986419473943,85.0683393510559,85.1118926166437,85.1914444811422,
85.2709362165935,85.3503800753096,85.4297882722149,85.5091729937536,85.5885590297386,
85.6679478110251,85.7473504096418,85.8267779052732,85.9062766284129,85.9858137738086,
86.0654393072728,86.1094349979686,86.1871024781925,86.2646839332619,86.3421932841988,
86.4196341553229,86.4970353506218,86.5744106625885,86.608206188631,86.6916976342907,
86.7753452790357,86.8592305018997,86.9432292803021,87.0274135362109,87.1069773792935,
87.1844865121341,87.2619137878101,87.339274823032,87.4165851870257,87.4938604122081,
87.571128916325,87.648396650939,87.7256776522952,87.802985961465,87.8803820735506,
87.9578238349092,88.0353850226484,88.1045197606184,88.1805883831446,88.2565618233008,
88.3324568615356,88.4082901980865,88.4840784716002,88.559846870807,88.6356073499835,
88.7113749072108,88.7871645446807,88.8630316358468,88.9389416534897,89.014956447619,
89.0589179048957),.UNSPECIFIED.);
#3259=B_SPLINE_CURVE_WITH_KNOTS('',3,(#38904,#38905,#38906,#38907,#38908,
#38909,#38910,#38911,#38912,#38913,#38914,#38915,#38916,#38917,#38918,#38919,
#38920,#38921,#38922,#38923,#38924,#38925,#38926,#38927,#38928,#38929,#38930,
#38931,#38932,#38933,#38934,#38935,#38936,#38937,#38938,#38939,#38940,#38941,
#38942,#38943,#38944,#38945,#38946,#38947,#38948,#38949,#38950,#38951,#38952,
#38953,#38954,#38955,#38956,#38957,#38958,#38959,#38960,#38961,#38962,#38963,
#38964,#38965,#38966,#38967,#38968,#38969,#38970,#38971,#38972,#38973,#38974,
#38975,#38976,#38977,#38978,#38979),.UNSPECIFIED.,.F.,.F.,(4,3,3,3,3,3,
3,3,3,3,3,3,3,3,3,3,3,3,3,3,3,3,3,3,3,4),(82.7764945981692,82.8589562018994,
82.9414171397513,83.0238774391233,83.1063371274115,83.1887962320099,83.2712547803103,
83.3537127997029,83.4361703175757,83.52284727566,83.6053140612011,83.687779174269,
83.770242724517,83.8527048215763,83.935165575058,84.0176250945539,84.1000834896391,
84.1825408698725,84.2650072555586,84.3474704570668,84.4299309129164,84.5123890614711,
84.5948546652248,84.6773145436127,84.759778654865,84.8230016469252),
 .UNSPECIFIED.);
#3260=B_SPLINE_CURVE_WITH_KNOTS('',3,(#38981,#38982,#38983,#38984,#38985,
#38986,#38987,#38988,#38989,#38990,#38991,#38992,#38993,#38994,#38995,#38996,
#38997,#38998,#38999,#39000,#39001,#39002,#39003,#39004,#39005,#39006,#39007,
#39008,#39009,#39010,#39011,#39012,#39013,#39014,#39015,#39016,#39017,#39018,
#39019,#39020,#39021,#39022,#39023,#39024,#39025,#39026,#39027,#39028,#39029,
#39030,#39031,#39032,#39033,#39034,#39035,#39036,#39037,#39038,#39039,#39040,
#39041,#39042,#39043,#39044,#39045,#39046,#39047,#39048,#39049,#39050,#39051,
#39052,#39053,#39054,#39055,#39056,#39057,#39058,#39059),.UNSPECIFIED.,
 .F.,.F.,(4,3,3,3,3,3,3,3,3,3,3,3,3,3,3,3,3,3,3,3,3,3,3,3,3,3,4),(82.7769101946331,
82.858111653591,82.9393131125489,83.0228045582085,83.1064522029543,83.1903374258182,
83.2743362042209,83.3585204601296,83.4380843032114,83.515593436052,83.593020711728,
83.6703817469499,83.7476921109432,83.8249673361251,83.902235840242,83.979503574856,
84.0567845762123,84.1340928853825,84.2114889974682,84.2889307588269,84.3664919465661,
84.4356266845362,84.5212431429555,84.6064436584641,84.6913848685092,84.7759142460088,
84.8230016468185),.UNSPECIFIED.);
#3261=B_SPLINE_CURVE_WITH_KNOTS('',3,(#39060,#39061,#39062,#39063,#39064,
#39065,#39066,#39067,#39068,#39069,#39070,#39071,#39072,#39073,#39074,#39075,
#39076,#39077,#39078,#39079,#39080,#39081,#39082,#39083,#39084,#39085,#39086,
#39087,#39088,#39089,#39090,#39091,#39092,#39093,#39094,#39095,#39096,#39097,
#39098,#39099,#39100,#39101,#39102,#39103,#39104,#39105,#39106,#39107,#39108,
#39109,#39110,#39111,#39112,#39113,#39114,#39115,#39116,#39117,#39118,#39119,
#39120,#39121,#39122,#39123,#39124,#39125,#39126,#39127,#39128,#39129,#39130,
#39131,#39132,#39133,#39134,#39135,#39136,#39137,#39138,#39139,#39140,#39141,
#39142,#39143,#39144,#39145,#39146,#39147,#39148,#39149,#39150,#39151,#39152,
#39153,#39154,#39155,#39156,#39157,#39158,#39159,#39160,#39161,#39162,#39163,
#39164,#39165,#39166,#39167,#39168,#39169,#39170,#39171,#39172,#39173,#39174,
#39175,#39176,#39177,#39178,#39179,#39180,#39181,#39182,#39183,#39184,#39185,
#39186,#39187,#39188,#39189,#39190,#39191,#39192,#39193,#39194,#39195,#39196,
#39197,#39198,#39199,#39200,#39201,#39202,#39203,#39204,#39205,#39206,#39207,
#39208,#39209,#39210,#39211,#39212,#39213,#39214,#39215,#39216,#39217,#39218,
#39219,#39220,#39221,#39222,#39223,#39224,#39225),.UNSPECIFIED.,.F.,.F.,
(4,3,3,3,3,3,3,3,3,3,3,3,3,3,3,3,3,3,3,3,3,3,3,3,3,3,3,3,3,3,3,3,3,3,3,
3,3,3,3,3,3,3,3,3,3,3,3,3,3,3,3,3,3,3,3,4),(84.8230016469251,84.8993440070806,
84.9756935320769,85.0520647933022,85.1284723735079,85.2049850548415,85.2815520053968,
85.3582581219713,85.4331690658612,85.5117136827997,85.5901657249703,85.6685396855523,
85.7468500023917,85.8251110677647,85.9033403610317,85.9815531577765,86.0597624439038,
86.137981200842,86.2162548799545,86.2945571017208,86.3729425582962,86.430711447186,
86.5103604674521,86.5899393591232,86.6694590018299,86.7489219133351,86.8283507641594,
86.9077551636423,86.9294826378485,87.0107146909381,87.0919954092767,87.1760600140853,
87.2574921489416,87.3428729887263,87.4282538285109,87.5134867519808,87.5986417132072,
87.6836466499301,87.7685449420231,87.853251488349,87.9270250191734,88.0035839838605,
88.0801375507398,88.1567003163181,88.2333188487859,88.3099686172805,88.3867017307701,
88.4257962098358,88.5053412725672,88.584829525727,88.6642721208719,88.743680178324,
88.8230722497529,88.9024514737574,88.9818487872157,89.0593915850525),
 .UNSPECIFIED.);
#3262=B_SPLINE_CURVE_WITH_KNOTS('',3,(#39231,#39232,#39233,#39234,#39235,
#39236,#39237,#39238,#39239,#39240,#39241,#39242,#39243,#39244,#39245,#39246,
#39247,#39248,#39249,#39250,#39251,#39252,#39253,#39254,#39255,#39256,#39257,
#39258,#39259,#39260,#39261,#39262,#39263,#39264,#39265,#39266,#39267,#39268,
#39269,#39270,#39271,#39272,#39273,#39274,#39275,#39276,#39277,#39278,#39279,
#39280,#39281,#39282,#39283,#39284,#39285,#39286,#39287,#39288,#39289,#39290,
#39291,#39292,#39293,#39294,#39295,#39296,#39297,#39298,#39299,#39300,#39301,
#39302,#39303,#39304,#39305,#39306,#39307,#39308,#39309,#39310,#39311,#39312,
#39313,#39314,#39315,#39316,#39317,#39318,#39319,#39320,#39321,#39322,#39323,
#39324,#39325,#39326,#39327,#39328,#39329,#39330,#39331,#39332,#39333,#39334,
#39335,#39336,#39337,#39338,#39339,#39340,#39341,#39342,#39343,#39344,#39345,
#39346,#39347,#39348,#39349,#39350,#39351,#39352,#39353,#39354,#39355,#39356,
#39357,#39358,#39359,#39360,#39361,#39362,#39363,#39364,#39365,#39366,#39367,
#39368,#39369,#39370,#39371,#39372,#39373,#39374,#39375,#39376,#39377,#39378,
#39379,#39380,#39381,#39382,#39383,#39384,#39385,#39386,#39387,#39388,#39389,
#39390,#39391,#39392,#39393,#39394,#39395,#39396,#39397,#39398,#39399),
 .UNSPECIFIED.,.F.,.F.,(4,3,3,3,3,3,3,3,3,3,3,3,3,3,3,3,3,3,3,3,3,3,3,3,
3,3,3,3,3,3,3,3,3,3,3,3,3,3,3,3,3,3,3,3,3,3,3,3,3,3,3,3,3,3,3,3,4),(91.1061869541048,
91.1911951043501,91.2761214668079,91.360897646181,91.4455683287238,91.5300560524809,
91.5959180952555,91.6724770599426,91.7490306268218,91.8255933924003,91.9022119248679,
91.9788616933629,92.0555948068526,92.0946892859179,92.1742411504165,92.2537328858677,
92.3331767445836,92.4125849414891,92.4919696630279,92.5713556990129,92.6507444802995,
92.7301470789161,92.8095745745474,92.889073297687,92.9686104430828,93.048235976547,
93.0922316672428,93.1698991474668,93.2474806025362,93.324989953473,93.4024308245972,
93.479832019896,93.5572073318627,93.5910028579053,93.6744943035652,93.7581419483103,
93.8420271711743,93.9260259495767,94.0102102054854,94.0897740485677,94.1672831814083,
94.2447104570843,94.3220714923062,94.3993818562999,94.4766570814823,94.5539255855992,
94.6311933202132,94.7084743215694,94.7857826307392,94.8631787428249,94.9406205041834,
95.0181816919226,95.0873164298926,95.1633810280806,95.2393622405657,95.3152561915304,
95.343736224813),.UNSPECIFIED.);
#3263=B_SPLINE_CURVE_WITH_KNOTS('',3,(#39400,#39401,#39402,#39403,#39404,
#39405,#39406,#39407,#39408,#39409,#39410,#39411,#39412,#39413,#39414,#39415,
#39416,#39417,#39418,#39419,#39420,#39421,#39422,#39423,#39424,#39425,#39426,
#39427,#39428,#39429,#39430,#39431,#39432,#39433,#39434,#39435,#39436,#39437,
#39438,#39439,#39440,#39441,#39442,#39443,#39444,#39445,#39446,#39447,#39448,
#39449,#39450,#39451,#39452,#39453,#39454,#39455,#39456,#39457,#39458,#39459,
#39460,#39461,#39462,#39463,#39464,#39465,#39466,#39467,#39468,#39469,#39470,
#39471,#39472,#39473,#39474,#39475,#39476,#39477,#39478,#39479,#39480,#39481,
#39482,#39483,#39484),.UNSPECIFIED.,.F.,.F.,(4,3,3,3,3,3,3,3,3,3,3,3,3,
3,3,3,3,3,3,3,3,3,3,3,3,3,3,3,4),(89.0589179048957,89.1020621419433,89.1806067588819,
89.2590588010526,89.3374327616345,89.4157430784736,89.4940041438465,89.5722334371135,
89.6504462338582,89.7286555199856,89.8068742769238,89.8851479560364,89.9634501778026,
90.0418356343781,90.0996045232682,90.1792535435342,90.2588324352052,90.3383520779123,
90.4178149894175,90.4972438402421,90.576648239725,90.5983757139306,90.6796077670204,
90.7608884853588,90.8449530901674,90.9263852250236,91.0117660648083,91.097146904593,
91.1061869541048),.UNSPECIFIED.);
#3264=B_SPLINE_CURVE_WITH_KNOTS('',3,(#39486,#39487,#39488,#39489,#39490,
#39491,#39492,#39493,#39494,#39495,#39496,#39497,#39498,#39499,#39500,#39501,
#39502,#39503,#39504,#39505,#39506,#39507,#39508,#39509,#39510,#39511,#39512,
#39513,#39514,#39515,#39516,#39517,#39518,#39519,#39520,#39521,#39522,#39523,
#39524,#39525,#39526,#39527,#39528,#39529,#39530,#39531,#39532,#39533,#39534,
#39535,#39536,#39537,#39538,#39539,#39540,#39541,#39542,#39543,#39544,#39545,
#39546,#39547,#39548,#39549,#39550,#39551,#39552,#39553,#39554,#39555,#39556,
#39557,#39558,#39559,#39560,#39561,#39562,#39563,#39564,#39565,#39566,#39567),
 .UNSPECIFIED.,.F.,.F.,(4,3,3,3,3,3,3,3,3,3,3,3,3,3,3,3,3,3,3,3,3,3,3,3,
3,3,3,4),(89.0593915850525,89.1388183698175,89.2183163145536,89.2978524425878,
89.3774773761306,89.4233385911607,89.5010060713846,89.5785875264542,89.6560968773908,
89.733537748515,89.8109389438138,89.8883142557805,89.9221097818232,90.0056012274829,
90.089248872227,90.1731340950911,90.2571328734935,90.3413171294022,90.4208809724856,
90.4971492482531,90.5733121606026,90.6494144829602,90.7254712026133,90.8014972719894,
90.8776696925182,90.9536943508863,91.0299406524955,91.1061869541047),
 .UNSPECIFIED.);
#3265=B_SPLINE_CURVE_WITH_KNOTS('',3,(#39568,#39569,#39570,#39571,#39572,
#39573,#39574,#39575,#39576,#39577,#39578,#39579,#39580,#39581,#39582,#39583,
#39584,#39585,#39586,#39587,#39588,#39589,#39590,#39591,#39592,#39593,#39594,
#39595,#39596,#39597,#39598,#39599,#39600,#39601,#39602,#39603,#39604,#39605,
#39606,#39607,#39608,#39609,#39610,#39611,#39612,#39613,#39614,#39615,#39616,
#39617,#39618,#39619,#39620,#39621,#39622,#39623,#39624,#39625,#39626,#39627,
#39628,#39629,#39630,#39631,#39632,#39633,#39634,#39635,#39636,#39637,#39638,
#39639,#39640,#39641,#39642,#39643,#39644,#39645,#39646,#39647,#39648,#39649,
#39650,#39651,#39652,#39653,#39654,#39655,#39656,#39657,#39658,#39659,#39660,
#39661,#39662,#39663,#39664,#39665,#39666,#39667,#39668,#39669,#39670,#39671,
#39672,#39673,#39674,#39675,#39676,#39677,#39678,#39679,#39680,#39681,#39682,
#39683,#39684,#39685,#39686,#39687,#39688,#39689,#39690,#39691,#39692,#39693,
#39694,#39695,#39696,#39697,#39698,#39699,#39700,#39701,#39702,#39703,#39704,
#39705,#39706,#39707,#39708,#39709,#39710,#39711,#39712,#39713,#39714,#39715,
#39716,#39717,#39718,#39719,#39720,#39721,#39722,#39723,#39724,#39725,#39726,
#39727,#39728,#39729,#39730,#39731,#39732,#39733),.UNSPECIFIED.,.F.,.F.,
(4,3,3,3,3,3,3,3,3,3,3,3,3,3,3,3,3,3,3,3,3,3,3,3,3,3,3,3,3,3,3,3,3,3,3,
3,3,3,3,3,3,3,3,3,3,3,3,3,3,3,3,3,3,3,3,4),(91.1061869541992,91.202852706791,
91.300745271717,91.3998480253286,91.4184233538105,91.4944895132676,91.5704610143016,
91.6463546340986,91.7221870703858,91.7979749599698,91.8752238068655,91.9509876055167,
92.0267595115807,92.102554529052,92.1809073305728,92.2568358692746,92.336400802205,
92.4159657351354,92.4945103520739,92.5729623942447,92.6513363548266,92.7296466716657,
92.8079077370387,92.8861370303058,92.9643498270504,93.0425591131778,93.1207778701159,
93.1990515492285,93.2773537709948,93.3557392275703,93.4135081164603,93.4931571367264,
93.5727360283973,93.6522556711044,93.7317185826096,93.8111474334344,93.8905518329174,
93.9122793071227,93.9935113602123,94.0747920785511,94.1588566833596,94.2402888182157,
94.3256696580005,94.4110504977852,94.4962834212552,94.5814383824818,94.6664433192047,
94.7513416112971,94.8360481576231,94.9098216884476,94.9863779586668,95.0629277392939,
95.139511303211,95.2161125564466,95.2927809813326,95.3423637038624),
 .UNSPECIFIED.);
#3266=B_SPLINE_CURVE_WITH_KNOTS('',3,(#39739,#39740,#39741,#39742,#39743,
#39744,#39745,#39746,#39747,#39748,#39749,#39750,#39751,#39752,#39753,#39754,
#39755,#39756,#39757,#39758,#39759,#39760,#39761,#39762,#39763,#39764,#39765,
#39766,#39767,#39768,#39769,#39770,#39771,#39772,#39773,#39774,#39775,#39776,
#39777,#39778,#39779,#39780,#39781,#39782,#39783,#39784,#39785,#39786,#39787,
#39788,#39789,#39790,#39791,#39792,#39793,#39794,#39795,#39796,#39797,#39798,
#39799,#39800,#39801,#39802,#39803,#39804,#39805,#39806,#39807,#39808,#39809,
#39810,#39811,#39812,#39813,#39814,#39815,#39816,#39817,#39818,#39819,#39820,
#39821,#39822,#39823,#39824,#39825,#39826,#39827,#39828,#39829,#39830,#39831,
#39832,#39833,#39834,#39835,#39836,#39837,#39838,#39839,#39840,#39841,#39842,
#39843,#39844,#39845,#39846,#39847,#39848,#39849,#39850,#39851,#39852,#39853,
#39854,#39855,#39856,#39857,#39858,#39859,#39860,#39861,#39862,#39863,#39864,
#39865,#39866,#39867,#39868,#39869,#39870,#39871,#39872,#39873,#39874,#39875,
#39876,#39877,#39878,#39879,#39880,#39881,#39882,#39883,#39884,#39885,#39886,
#39887,#39888,#39889,#39890,#39891,#39892,#39893,#39894,#39895,#39896,#39897,
#39898,#39899,#39900,#39901,#39902,#39903,#39904,#39905,#39906,#39907),
 .UNSPECIFIED.,.F.,.F.,(4,3,3,3,3,3,3,3,3,3,3,3,3,3,3,3,3,3,3,3,3,3,3,3,
3,3,3,3,3,3,3,3,3,3,3,3,3,3,3,3,3,3,3,3,3,3,3,3,3,3,3,3,3,3,3,3,4),(97.3893722613792,
97.4647384476076,97.5400988535631,97.5811723832049,97.6624044362947,97.7436851546336,
97.827749759442,97.9091818942983,97.9945627340828,98.0799435738673,98.1651764973373,
98.2503314585637,98.3353363952866,98.4202346873789,98.5049412337048,98.5787147645297,
98.6552737292166,98.7318272960958,98.8083900616736,98.8850085941413,98.9616583626361,
99.0383914761257,99.0774859551922,99.1570378196909,99.2365295551422,99.315973413858,
99.3953816107634,99.4747663323018,99.5541523682869,99.6335411495736,99.7129437481902,
99.7923712438222,99.8718699669619,99.9514071123577,100.031032645822,100.075028336517,
100.152695816741,100.23027727181,100.307786622747,100.385227493871,100.46262868917,
100.540004001137,100.57379952718,100.65729097284,100.740938617584,100.824823840448,
100.908822618851,100.993006874759,101.072570717842,101.150075052448,101.227501237278,
101.304863422243,101.385140997451,101.462416258506,101.539671877,101.616927213878,
101.625973723073),.UNSPECIFIED.);
#3267=B_SPLINE_CURVE_WITH_KNOTS('',3,(#39908,#39909,#39910,#39911,#39912,
#39913,#39914,#39915,#39916,#39917,#39918,#39919,#39920,#39921,#39922,#39923,
#39924,#39925,#39926,#39927,#39928,#39929,#39930,#39931,#39932,#39933,#39934,
#39935,#39936,#39937,#39938,#39939,#39940,#39941,#39942,#39943,#39944,#39945,
#39946,#39947,#39948,#39949,#39950,#39951,#39952,#39953,#39954,#39955,#39956,
#39957,#39958,#39959,#39960,#39961,#39962,#39963,#39964,#39965,#39966,#39967,
#39968,#39969,#39970,#39971,#39972,#39973,#39974,#39975,#39976,#39977,#39978,
#39979,#39980,#39981,#39982,#39983,#39984,#39985,#39986,#39987,#39988,#39989),
 .UNSPECIFIED.,.F.,.F.,(4,3,3,3,3,3,3,3,3,3,3,3,3,3,3,3,3,3,3,3,3,3,3,3,
3,3,3,4),(95.343736224813,95.4195499814771,95.4953254278548,95.5710919447158,
95.6468569104745,95.7226353245225,95.7984421953838,95.8743395178615,95.9502851548077,
96.0263520783713,96.0848588112175,96.163403428156,96.2418554703267,96.3202294309087,
96.3985397477477,96.4768008131207,96.5550301063878,96.6332429031325,96.7114521892599,
96.7896709461978,96.8679446253104,96.9462468470766,97.0246323036522,97.0824011925424,
97.1672384844942,97.2519609493412,97.3364921077939,97.3893722612844),
 .UNSPECIFIED.);
#3268=B_SPLINE_CURVE_WITH_KNOTS('',3,(#39991,#39992,#39993,#39994,#39995,
#39996,#39997,#39998,#39999,#40000,#40001,#40002,#40003,#40004,#40005,#40006,
#40007,#40008,#40009,#40010,#40011,#40012,#40013,#40014,#40015,#40016,#40017,
#40018,#40019,#40020,#40021,#40022,#40023,#40024,#40025,#40026,#40027,#40028,
#40029,#40030,#40031,#40032,#40033,#40034,#40035,#40036,#40037,#40038,#40039,
#40040,#40041,#40042,#40043,#40044,#40045,#40046,#40047,#40048,#40049,#40050,
#40051,#40052,#40053,#40054,#40055,#40056,#40057,#40058,#40059,#40060,#40061,
#40062,#40063,#40064,#40065,#40066,#40067,#40068,#40069,#40070,#40071,#40072),
 .UNSPECIFIED.,.F.,.F.,(4,3,3,3,3,3,3,3,3,3,3,3,3,3,3,3,3,3,3,3,3,3,3,3,
3,3,3,4),(95.3423637038624,95.4085928791101,95.4881447436086,95.56763647906,
95.6470803377759,95.7264885346813,95.80587325622,95.885259292205,95.9646480734914,
96.0440506721081,96.1234781677394,96.2029768908791,96.2825140362749,96.3621395697392,
96.406135260435,96.483802740659,96.5613841957283,96.6388935466651,96.7163344177893,
96.793735613088,96.8711109250547,96.9049064510974,96.9878070421606,97.0708472264203,
97.1541051534459,97.2374707156566,97.3210147106648,97.3893722612843),
 .UNSPECIFIED.);
#3269=B_SPLINE_CURVE_WITH_KNOTS('',3,(#40073,#40074,#40075,#40076,#40077,
#40078,#40079,#40080,#40081,#40082,#40083,#40084,#40085,#40086,#40087,#40088,
#40089,#40090,#40091,#40092,#40093,#40094,#40095,#40096,#40097,#40098,#40099,
#40100,#40101,#40102,#40103,#40104,#40105,#40106,#40107,#40108,#40109,#40110,
#40111,#40112,#40113,#40114,#40115,#40116,#40117,#40118,#40119,#40120,#40121,
#40122,#40123,#40124,#40125,#40126,#40127,#40128,#40129,#40130,#40131,#40132,
#40133,#40134,#40135,#40136,#40137,#40138,#40139,#40140,#40141,#40142,#40143,
#40144,#40145,#40146,#40147,#40148,#40149,#40150,#40151,#40152,#40153,#40154,
#40155,#40156,#40157,#40158,#40159,#40160,#40161,#40162,#40163,#40164,#40165,
#40166,#40167,#40168,#40169,#40170,#40171,#40172,#40173,#40174,#40175,#40176,
#40177,#40178,#40179,#40180,#40181,#40182,#40183,#40184,#40185,#40186,#40187,
#40188,#40189,#40190,#40191,#40192,#40193,#40194,#40195,#40196,#40197,#40198,
#40199,#40200,#40201,#40202,#40203,#40204,#40205,#40206,#40207,#40208,#40209,
#40210,#40211,#40212,#40213,#40214,#40215,#40216,#40217,#40218,#40219,#40220,
#40221,#40222,#40223,#40224,#40225,#40226,#40227,#40228,#40229,#40230,#40231,
#40232,#40233,#40234,#40235,#40236,#40237,#40238,#40239,#40240,#40241),
 .UNSPECIFIED.,.F.,.F.,(4,3,3,3,3,3,3,3,3,3,3,3,3,3,3,3,3,3,3,3,3,3,3,3,
3,3,3,3,3,3,3,3,3,3,3,3,3,3,3,3,3,3,3,3,3,3,3,3,3,3,3,3,3,3,3,3,4),(97.3893722613959,
97.4036776417599,97.4811867746005,97.5586140502765,97.6359750854984,97.713285449492,
97.7905606746746,97.8678291787915,97.9450969134055,98.0223779147616,98.0996862239315,
98.1770823360171,98.2545240973756,98.3320852851148,98.4012200230847,98.4772861825419,
98.5532576835759,98.6291513033729,98.7049837396601,98.7807716292446,98.8580204761402,
98.9337842747913,99.0095561808557,99.085351198327,99.1637039998477,99.2396325385496,
99.3191974714796,99.3987624044096,99.4773070213482,99.5557590635188,99.6341330241006,
99.7124433409397,99.7907044063129,99.86893369958,99.9471464963246,100.025355782452,
100.10357453939,100.181848218503,100.260150440269,100.338535896844,100.396304785735,
100.475953806001,100.555532697672,100.635052340379,100.714515251884,100.793944102709,
100.873348502192,100.895075976397,100.976308029487,101.057588747826,101.141653352634,
101.22308548749,101.308466327275,101.393847167059,101.479083303059,101.564215036154,
101.626603951495),.UNSPECIFIED.);
#3270=B_SPLINE_CURVE_WITH_KNOTS('',3,(#40247,#40248,#40249,#40250,#40251,
#40252,#40253,#40254,#40255,#40256,#40257,#40258,#40259,#40260,#40261,#40262,
#40263,#40264,#40265,#40266,#40267,#40268,#40269,#40270,#40271,#40272,#40273,
#40274,#40275,#40276,#40277,#40278,#40279,#40280,#40281,#40282,#40283,#40284,
#40285,#40286,#40287,#40288,#40289,#40290,#40291,#40292,#40293,#40294,#40295,
#40296,#40297,#40298,#40299,#40300,#40301,#40302,#40303,#40304,#40305,#40306,
#40307,#40308,#40309,#40310,#40311,#40312,#40313,#40314,#40315,#40316,#40317,
#40318,#40319,#40320,#40321,#40322,#40323,#40324,#40325,#40326,#40327,#40328,
#40329,#40330,#40331,#40332,#40333,#40334,#40335,#40336,#40337,#40338,#40339,
#40340,#40341,#40342,#40343,#40344,#40345,#40346,#40347,#40348,#40349,#40350,
#40351,#40352,#40353,#40354,#40355,#40356,#40357,#40358,#40359,#40360,#40361,
#40362,#40363,#40364,#40365,#40366,#40367,#40368,#40369,#40370,#40371,#40372,
#40373,#40374,#40375,#40376,#40377,#40378,#40379,#40380,#40381,#40382,#40383,
#40384,#40385,#40386,#40387,#40388,#40389,#40390,#40391,#40392,#40393,#40394,
#40395,#40396,#40397,#40398,#40399,#40400,#40401,#40402,#40403,#40404,#40405,
#40406,#40407,#40408,#40409,#40410,#40411,#40412,#40413,#40414,#40415),
 .UNSPECIFIED.,.F.,.F.,(4,3,3,3,3,3,3,3,3,3,3,3,3,3,3,3,3,3,3,3,3,3,3,3,
3,3,3,3,3,3,3,3,3,3,3,3,3,3,3,3,3,3,3,3,3,3,3,3,3,3,3,3,3,3,3,3,4),(103.672557568545,
103.756707913208,103.841117967449,103.925654775611,104.01037559108,104.065197861817,
104.144846882083,104.224425773754,104.303945416462,104.383408327967,104.462837178792,
104.542241578275,104.563969052479,104.645201105569,104.726481823907,104.810546428716,
104.891978563572,104.977359403357,105.062740243142,105.147973166612,105.233128127839,
105.318133064562,105.403031356655,105.487737902981,105.561511433804,105.638070398491,
105.71462396537,105.791186730948,105.867805263416,105.94445503191,106.0211881454,
106.060282624466,106.139834488965,106.219326224416,106.298770083132,106.378178280037,
106.457563001576,106.536949037561,106.616337818847,106.695740417464,106.775167913095,
106.854666636235,106.934203781631,107.013829315095,107.057825005791,107.135492486015,
107.213073941084,107.290583292022,107.368024163146,107.445425358445,107.522800670411,
107.556596196454,107.640043784118,107.723726110521,107.807532534318,107.891508514147,
107.908824909855),.UNSPECIFIED.);
#3271=B_SPLINE_CURVE_WITH_KNOTS('',3,(#40416,#40417,#40418,#40419,#40420,
#40421,#40422,#40423,#40424,#40425,#40426,#40427,#40428,#40429,#40430,#40431,
#40432,#40433,#40434,#40435,#40436,#40437,#40438,#40439,#40440,#40441,#40442,
#40443,#40444,#40445,#40446,#40447,#40448,#40449,#40450,#40451,#40452,#40453,
#40454,#40455,#40456,#40457,#40458,#40459,#40460,#40461,#40462,#40463,#40464,
#40465,#40466,#40467,#40468,#40469,#40470,#40471,#40472,#40473,#40474,#40475,
#40476,#40477,#40478,#40479,#40480,#40481,#40482,#40483,#40484,#40485,#40486,
#40487,#40488,#40489,#40490,#40491,#40492,#40493,#40494,#40495,#40496,#40497),
 .UNSPECIFIED.,.F.,.F.,(4,3,3,3,3,3,3,3,3,3,3,3,3,3,3,3,3,3,3,3,3,3,3,3,
3,3,3,4),(101.625973723073,101.703258039259,101.780571841722,101.857974200672,
101.935424169097,102.012990130556,102.070113099167,102.146179258624,102.222150759659,
102.298044379455,102.373876815743,102.449664705327,102.526913552223,102.602677350874,
102.678449256938,102.75424427441,102.83259707593,102.908525614632,102.988090547562,
103.067655480492,103.148594355004,103.229425492566,103.31015705143,103.390797126932,
103.471326024254,103.551787785923,103.632171854257,103.672557568464),
 .UNSPECIFIED.);
#3272=B_SPLINE_CURVE_WITH_KNOTS('',3,(#40499,#40500,#40501,#40502,#40503,
#40504,#40505,#40506,#40507,#40508,#40509,#40510,#40511,#40512,#40513,#40514,
#40515,#40516,#40517,#40518,#40519,#40520,#40521,#40522,#40523,#40524,#40525,
#40526,#40527,#40528,#40529,#40530,#40531,#40532,#40533,#40534,#40535,#40536,
#40537,#40538,#40539,#40540,#40541,#40542,#40543,#40544,#40545,#40546,#40547,
#40548,#40549,#40550,#40551,#40552,#40553,#40554,#40555,#40556,#40557,#40558,
#40559,#40560,#40561,#40562,#40563,#40564,#40565,#40566,#40567,#40568,#40569,
#40570,#40571,#40572,#40573,#40574,#40575,#40576,#40577,#40578,#40579,#40580,
#40581,#40582,#40583),.UNSPECIFIED.,.F.,.F.,(4,3,3,3,3,3,3,3,3,3,3,3,3,
3,3,3,3,3,3,3,3,3,3,3,3,3,3,3,4),(101.626603951495,101.711531805551,101.796344425241,
101.880981628715,101.892618357722,101.969177322409,102.045730889288,102.122293654866,
102.198912187334,102.275561955829,102.352295069318,102.391389548384,102.470941412883,
102.550433148334,102.62987700705,102.709285203955,102.788669925493,102.868055961478,
102.947444742764,103.02684734138,103.106274837012,103.185773560151,103.265310705547,
103.344936239011,103.388931929709,103.474046022759,103.558963574929,103.643580610126,
103.672557568464),.UNSPECIFIED.);
#3273=B_SPLINE_CURVE_WITH_KNOTS('',3,(#40584,#40585,#40586,#40587,#40588,
#40589,#40590,#40591,#40592,#40593,#40594,#40595,#40596,#40597,#40598,#40599,
#40600,#40601,#40602,#40603,#40604,#40605,#40606,#40607,#40608,#40609,#40610,
#40611,#40612,#40613,#40614,#40615,#40616,#40617,#40618,#40619,#40620,#40621,
#40622,#40623,#40624,#40625,#40626,#40627,#40628,#40629,#40630,#40631,#40632,
#40633,#40634,#40635,#40636,#40637,#40638,#40639,#40640,#40641,#40642,#40643,
#40644,#40645,#40646,#40647,#40648,#40649,#40650,#40651,#40652,#40653,#40654,
#40655,#40656,#40657,#40658,#40659,#40660,#40661,#40662,#40663,#40664,#40665,
#40666,#40667,#40668,#40669,#40670,#40671,#40672,#40673,#40674,#40675,#40676,
#40677,#40678,#40679,#40680,#40681,#40682,#40683,#40684,#40685,#40686,#40687,
#40688,#40689,#40690,#40691,#40692,#40693,#40694,#40695,#40696,#40697,#40698,
#40699,#40700,#40701,#40702,#40703,#40704,#40705,#40706,#40707,#40708,#40709,
#40710,#40711,#40712,#40713,#40714,#40715,#40716,#40717,#40718,#40719,#40720,
#40721,#40722,#40723,#40724,#40725,#40726,#40727,#40728,#40729,#40730,#40731,
#40732,#40733,#40734,#40735,#40736,#40737,#40738,#40739,#40740),
 .UNSPECIFIED.,.F.,.F.,(4,3,3,3,3,3,3,3,3,3,3,3,3,3,3,3,3,3,3,3,3,3,3,3,
3,3,3,3,3,3,3,3,3,3,3,3,3,3,3,3,3,3,3,3,3,3,3,3,3,3,3,3,4),(103.672557568464,
103.755019774564,103.837481632367,103.919943148722,104.00240433048,104.08486518449,
104.167325717602,104.249785936665,104.332245848528,104.41470546004,104.497164778049,
104.579623809402,104.662082560949,104.744541039537,104.826999252012,104.909457205223,
104.991914906016,105.074372361238,105.156829577736,105.242842273022,105.32616707158,
105.408633677172,105.491099438555,105.573564383145,105.656028538353,105.73849193159,
105.820954590261,105.903416541772,105.985877813525,106.068338432918,106.150798427349,
106.233257824213,106.315716650903,106.39817493481,106.480632703323,106.56308998383,
106.647224099021,106.729690097381,106.812154473987,106.894617338482,106.977078800489,
107.059538969608,107.141997955424,107.224455867504,107.310053362427,107.392518099473,
107.474979871859,107.557439118025,107.639896276263,107.722358795346,107.804816466757,
107.88727525795,107.909235826887),.UNSPECIFIED.);
#3274=B_SPLINE_CURVE_WITH_KNOTS('',3,(#40746,#40747,#40748,#40749,#40750,
#40751,#40752,#40753,#40754,#40755,#40756,#40757,#40758,#40759,#40760,#40761,
#40762,#40763,#40764,#40765,#40766,#40767,#40768,#40769,#40770,#40771,#40772,
#40773,#40774,#40775,#40776,#40777,#40778,#40779,#40780,#40781,#40782,#40783,
#40784,#40785,#40786,#40787,#40788,#40789,#40790,#40791,#40792,#40793,#40794,
#40795,#40796,#40797,#40798,#40799,#40800,#40801,#40802,#40803,#40804,#40805,
#40806,#40807,#40808,#40809,#40810,#40811,#40812,#40813,#40814,#40815,#40816,
#40817,#40818,#40819,#40820,#40821,#40822,#40823,#40824,#40825,#40826,#40827,
#40828,#40829,#40830,#40831,#40832,#40833,#40834,#40835,#40836,#40837,#40838,
#40839,#40840,#40841,#40842,#40843,#40844,#40845,#40846,#40847,#40848,#40849,
#40850,#40851,#40852,#40853,#40854,#40855,#40856,#40857,#40858,#40859,#40860,
#40861,#40862,#40863,#40864,#40865,#40866,#40867,#40868,#40869,#40870,#40871,
#40872,#40873,#40874,#40875,#40876,#40877,#40878,#40879,#40880,#40881,#40882,
#40883,#40884,#40885,#40886,#40887,#40888,#40889,#40890,#40891,#40892,#40893,
#40894,#40895,#40896,#40897,#40898,#40899,#40900,#40901,#40902,#40903,#40904,
#40905,#40906,#40907,#40908,#40909,#40910,#40911),.UNSPECIFIED.,.F.,.F.,
(4,3,3,3,3,3,3,3,3,3,3,3,3,3,3,3,3,3,3,3,3,3,3,3,3,3,3,3,3,3,3,3,3,3,3,
3,3,3,3,3,3,3,3,3,3,3,3,3,3,3,3,3,3,3,3,4),(109.955742875644,110.050452149766,
110.128996766704,110.207448808875,110.285822769457,110.364133086296,110.442394151669,
110.520623444936,110.598836241681,110.677045527808,110.755264284746,110.833537963859,
110.911840185625,110.9902256422,111.047994531091,111.127643551357,111.207222443028,
111.286742085736,111.366204997241,111.445633848066,111.525038247549,111.546765721753,
111.627997774842,111.709278493181,111.79334309799,111.874775232845,111.960156072631,
112.045536912416,112.130769835886,112.215924797113,112.300929733837,112.385828025929,
112.470534572256,112.544308103078,112.620867067765,112.697420634644,112.773983400223,
112.85060193269,112.927251701185,113.003984814675,113.043079293741,113.12263115824,
113.202122893691,113.281566752407,113.360974949312,113.440359670851,113.519745706836,
113.599134488123,113.67853708674,113.757964582371,113.837463305511,113.917000450907,
113.996625984371,114.040621675066,114.118278370784,114.193145417554),
 .UNSPECIFIED.);
#3275=B_SPLINE_CURVE_WITH_KNOTS('',3,(#40912,#40913,#40914,#40915,#40916,
#40917,#40918,#40919,#40920,#40921,#40922,#40923,#40924,#40925,#40926,#40927,
#40928,#40929,#40930,#40931,#40932,#40933,#40934,#40935,#40936,#40937,#40938,
#40939,#40940,#40941,#40942,#40943,#40944,#40945,#40946,#40947,#40948,#40949,
#40950,#40951,#40952,#40953,#40954,#40955,#40956,#40957,#40958,#40959,#40960,
#40961,#40962,#40963,#40964,#40965,#40966,#40967,#40968,#40969,#40970,#40971,
#40972,#40973,#40974,#40975,#40976,#40977,#40978,#40979,#40980,#40981,#40982,
#40983,#40984,#40985,#40986,#40987,#40988,#40989,#40990,#40991,#40992,#40993),
 .UNSPECIFIED.,.F.,.F.,(4,3,3,3,3,3,3,3,3,3,3,3,3,3,3,3,3,3,3,3,3,3,3,3,
3,3,3,4),(107.908824909855,107.9930213909,108.055367387116,108.132876519957,
108.210303795633,108.287664830855,108.364975194848,108.442250420031,108.519518924148,
108.596786658762,108.674067660118,108.751375969287,108.828772081373,108.906213842731,
108.98377503047,109.052909768441,109.128120422795,109.203237706626,109.278278831806,
109.353260899253,109.428571146293,109.503494903372,109.578414098686,109.653344062158,
109.72894376551,109.803975886335,109.879859380951,109.955742875567),
 .UNSPECIFIED.);
#3276=B_SPLINE_CURVE_WITH_KNOTS('',3,(#40995,#40996,#40997,#40998,#40999,
#41000,#41001,#41002,#41003,#41004,#41005,#41006,#41007,#41008,#41009,#41010,
#41011,#41012,#41013,#41014,#41015,#41016,#41017,#41018,#41019,#41020,#41021,
#41022,#41023,#41024,#41025,#41026,#41027,#41028,#41029,#41030,#41031,#41032,
#41033,#41034,#41035,#41036,#41037,#41038,#41039,#41040,#41041,#41042,#41043,
#41044,#41045,#41046,#41047,#41048,#41049,#41050,#41051,#41052,#41053,#41054,
#41055,#41056,#41057,#41058,#41059,#41060,#41061,#41062,#41063,#41064,#41065,
#41066,#41067,#41068,#41069,#41070),.UNSPECIFIED.,.F.,.F.,(4,3,3,3,3,3,
3,3,3,3,3,3,3,3,3,3,3,3,3,3,3,3,3,3,3,4),(107.909235826887,107.991697430617,
108.074158368469,108.156618667841,108.239078356129,108.321537460728,108.403996009028,
108.486454028421,108.568911546294,108.655588504378,108.738055289919,108.820520402987,
108.902983953235,108.985446050294,109.067906803776,109.150366323272,109.232824718357,
109.315282098591,109.397748484277,109.480211685785,109.562672141635,109.645130290189,
109.727595893943,109.810055772331,109.892519883583,109.955742875643),
 .UNSPECIFIED.);
#3277=B_SPLINE_CURVE_WITH_KNOTS('',3,(#41071,#41072,#41073,#41074,#41075,
#41076,#41077,#41078,#41079,#41080,#41081,#41082,#41083,#41084,#41085,#41086,
#41087,#41088,#41089,#41090,#41091,#41092,#41093,#41094,#41095,#41096,#41097,
#41098,#41099,#41100,#41101,#41102,#41103,#41104,#41105,#41106,#41107,#41108,
#41109,#41110,#41111,#41112,#41113,#41114,#41115,#41116,#41117,#41118,#41119,
#41120,#41121,#41122,#41123,#41124,#41125,#41126,#41127,#41128,#41129,#41130,
#41131,#41132,#41133,#41134,#41135,#41136,#41137,#41138,#41139,#41140,#41141,
#41142,#41143,#41144,#41145,#41146,#41147,#41148,#41149,#41150,#41151,#41152,
#41153,#41154,#41155,#41156,#41157,#41158,#41159,#41160,#41161,#41162,#41163,
#41164,#41165,#41166,#41167,#41168,#41169,#41170,#41171,#41172,#41173,#41174,
#41175,#41176,#41177,#41178,#41179,#41180,#41181,#41182,#41183,#41184,#41185,
#41186,#41187,#41188,#41189,#41190,#41191,#41192,#41193,#41194,#41195,#41196,
#41197,#41198,#41199,#41200,#41201,#41202,#41203,#41204,#41205,#41206,#41207,
#41208,#41209,#41210,#41211,#41212,#41213,#41214,#41215,#41216,#41217,#41218,
#41219,#41220,#41221,#41222,#41223,#41224,#41225,#41226,#41227,#41228,#41229,
#41230,#41231,#41232,#41233,#41234,#41235,#41236),.UNSPECIFIED.,.F.,.F.,
(4,3,3,3,3,3,3,3,3,3,3,3,3,3,3,3,3,3,3,3,3,3,3,3,3,3,3,3,3,3,3,3,3,3,3,
3,3,3,3,3,3,3,3,3,3,3,3,3,3,3,3,3,3,3,3,4),(109.955742875643,110.04305544946,
110.130814483544,110.21877247887,110.306963574977,110.371728598983,110.449396079207,
110.526977534276,110.604486885213,110.681927756337,110.759328951636,110.836704263602,
110.870499789646,110.953991235306,111.037638880051,111.121524102915,111.205522881317,
111.289707137226,111.369270980308,111.446780113149,111.524207388825,111.601568424046,
111.67887878804,111.756154013223,111.833422517339,111.910690251953,111.987971253309,
112.065279562479,112.142675674565,112.220117435923,112.297678623663,112.366813361633,
112.44287952109,112.518851022124,112.594744641921,112.670577078209,112.746364967793,
112.823613814688,112.89937761334,112.975149519404,113.050944536875,113.129297338396,
113.205225877097,113.284790810028,113.364355742958,113.442910397955,113.52137077222,
113.599751366313,113.678053989655,113.756311716738,113.834537567872,113.912744542277,
113.990961418735,114.069182613729,114.14744453706,114.192166287218),
 .UNSPECIFIED.);
#3278=B_SPLINE_CURVE_WITH_KNOTS('',3,(#41242,#41243,#41244,#41245,#41246,
#41247,#41248,#41249,#41250,#41251,#41252,#41253,#41254,#41255,#41256,#41257,
#41258,#41259,#41260,#41261,#41262,#41263,#41264,#41265,#41266,#41267,#41268,
#41269,#41270,#41271,#41272,#41273,#41274,#41275,#41276,#41277,#41278,#41279,
#41280,#41281,#41282,#41283,#41284,#41285,#41286,#41287,#41288,#41289,#41290,
#41291,#41292,#41293,#41294,#41295,#41296,#41297,#41298,#41299,#41300,#41301,
#41302,#41303,#41304,#41305,#41306,#41307,#41308,#41309,#41310,#41311,#41312,
#41313,#41314,#41315,#41316,#41317,#41318,#41319,#41320,#41321,#41322,#41323,
#41324,#41325,#41326,#41327,#41328,#41329,#41330,#41331,#41332,#41333,#41334,
#41335,#41336,#41337,#41338,#41339,#41340,#41341,#41342,#41343,#41344,#41345,
#41346,#41347,#41348,#41349,#41350,#41351,#41352,#41353,#41354,#41355,#41356,
#41357,#41358,#41359,#41360,#41361,#41362,#41363,#41364,#41365,#41366,#41367,
#41368,#41369,#41370,#41371,#41372,#41373,#41374,#41375,#41376,#41377,#41378,
#41379,#41380,#41381,#41382,#41383,#41384,#41385,#41386,#41387,#41388,#41389,
#41390,#41391,#41392,#41393,#41394,#41395,#41396,#41397,#41398,#41399,#41400,
#41401,#41402,#41403,#41404,#41405,#41406,#41407,#41408,#41409,#41410),
 .UNSPECIFIED.,.F.,.F.,(4,3,3,3,3,3,3,3,3,3,3,3,3,3,3,3,3,3,3,3,3,3,3,3,
3,3,3,3,3,3,3,3,3,3,3,3,3,3,3,3,3,3,3,3,3,3,3,3,3,3,3,3,3,3,3,3,4),(116.238928182898,
116.313671447667,116.38835424761,116.462993716109,116.537617697695,116.61223630112,
116.68686494645,116.761519068711,116.836258196363,116.911043816793,116.985943411631,
117.03324881904,117.111793435979,117.190245478149,117.268619438731,117.34692975557,
117.425190820944,117.503420114211,117.581632910955,117.659842197083,117.738060954021,
117.816334633134,117.8946368549,117.973022311475,118.030791200365,118.110440220631,
118.190019112302,118.269538755009,118.349001666515,118.42843051734,118.507834916823,
118.529562391028,118.610794444118,118.692075162456,118.776139767265,118.857571902121,
118.942952741906,119.02833358169,119.11356650516,119.198721466387,119.283726403109,
119.368624695201,119.453331241527,119.527104772352,119.603663737039,119.680217303918,
119.756780069497,119.833398601965,119.91004837046,119.98678148395,120.025875963015,
120.105430902719,120.184926973534,120.26436824715,120.343776124697,120.42316427217,
120.475463669947),.UNSPECIFIED.);
#3279=B_SPLINE_CURVE_WITH_KNOTS('',3,(#41411,#41412,#41413,#41414,#41415,
#41416,#41417,#41418,#41419,#41420,#41421,#41422,#41423,#41424,#41425,#41426,
#41427,#41428,#41429,#41430,#41431,#41432,#41433,#41434,#41435,#41436,#41437,
#41438,#41439,#41440,#41441,#41442,#41443,#41444,#41445,#41446,#41447,#41448,
#41449,#41450,#41451,#41452,#41453,#41454,#41455,#41456,#41457,#41458,#41459,
#41460,#41461,#41462,#41463,#41464,#41465,#41466,#41467,#41468,#41469,#41470,
#41471,#41472,#41473,#41474,#41475,#41476,#41477,#41478,#41479,#41480,#41481,
#41482,#41483,#41484,#41485,#41486,#41487,#41488,#41489),.UNSPECIFIED.,
 .F.,.F.,(4,3,3,3,3,3,3,3,3,3,3,3,3,3,3,3,3,3,3,3,3,3,3,3,3,3,4),(114.193145417554,
114.270657066993,114.348099558365,114.425501938043,114.502878108584,114.539392865728,
114.622884311388,114.706531956133,114.790417178996,114.874415957399,114.958600213307,
115.03816405639,115.115673189231,115.193100464907,115.270461500129,115.347771864122,
115.425047089304,115.502315593421,115.579583328035,115.656864329392,115.734172638561,
115.811568750647,115.889010512005,115.966571699745,116.035706437715,116.142943422663,
116.238928182823),.UNSPECIFIED.);
#3280=B_SPLINE_CURVE_WITH_KNOTS('',3,(#41491,#41492,#41493,#41494,#41495,
#41496,#41497,#41498,#41499,#41500,#41501,#41502,#41503,#41504,#41505,#41506,
#41507,#41508,#41509,#41510,#41511,#41512,#41513,#41514,#41515,#41516,#41517,
#41518,#41519,#41520,#41521,#41522,#41523,#41524,#41525,#41526,#41527,#41528,
#41529,#41530,#41531,#41532,#41533,#41534,#41535,#41536,#41537,#41538,#41539,
#41540,#41541,#41542,#41543,#41544,#41545,#41546,#41547,#41548,#41549,#41550,
#41551,#41552,#41553,#41554,#41555,#41556,#41557,#41558,#41559,#41560,#41561,
#41562,#41563,#41564,#41565,#41566,#41567,#41568,#41569,#41570,#41571,#41572),
 .UNSPECIFIED.,.F.,.F.,(4,3,3,3,3,3,3,3,3,3,3,3,3,3,3,3,3,3,3,3,3,3,3,3,
3,3,3,4),(114.192166287218,114.27049007846,114.348888723008,114.361898124283,
114.441547144549,114.52112603622,114.600645678928,114.680108590433,114.759537441258,
114.838941840741,114.860669314945,114.941901368034,115.023182086373,115.107246691182,
115.188678826038,115.274059665823,115.359440505608,115.444673429078,115.529828390305,
115.614833327029,115.699731619121,115.784438165448,115.85821169627,115.932457125966,
116.008925505731,116.08318163116,116.160756138093,116.238330645025),
 .UNSPECIFIED.);
#3281=B_SPLINE_CURVE_WITH_KNOTS('',3,(#41573,#41574,#41575,#41576,#41577,
#41578,#41579,#41580,#41581,#41582,#41583,#41584,#41585,#41586,#41587,#41588,
#41589,#41590,#41591,#41592,#41593,#41594,#41595,#41596,#41597,#41598,#41599,
#41600,#41601,#41602,#41603,#41604,#41605,#41606,#41607,#41608,#41609,#41610,
#41611,#41612,#41613,#41614,#41615,#41616,#41617,#41618,#41619,#41620,#41621,
#41622,#41623,#41624,#41625,#41626,#41627,#41628,#41629,#41630,#41631,#41632,
#41633,#41634,#41635,#41636,#41637,#41638,#41639,#41640,#41641,#41642,#41643,
#41644,#41645,#41646,#41647,#41648,#41649,#41650,#41651,#41652,#41653,#41654,
#41655,#41656,#41657,#41658,#41659,#41660,#41661,#41662,#41663,#41664,#41665,
#41666,#41667,#41668,#41669,#41670,#41671,#41672,#41673,#41674,#41675,#41676,
#41677,#41678,#41679,#41680,#41681,#41682,#41683,#41684,#41685,#41686,#41687,
#41688,#41689,#41690,#41691,#41692,#41693,#41694,#41695,#41696,#41697,#41698,
#41699,#41700,#41701,#41702,#41703,#41704,#41705,#41706,#41707,#41708,#41709,
#41710,#41711,#41712,#41713,#41714,#41715,#41716,#41717,#41718,#41719,#41720,
#41721,#41722,#41723,#41724,#41725,#41726,#41727,#41728,#41729),
 .UNSPECIFIED.,.F.,.F.,(4,3,3,3,3,3,3,3,3,3,3,3,3,3,3,3,3,3,3,3,3,3,3,3,
3,3,3,3,3,3,3,3,3,3,3,3,3,3,3,3,3,3,3,3,3,3,3,3,3,3,3,3,4),(116.238928182823,
116.321390388923,116.403852246726,116.486313763081,116.568774944839,116.651235798849,
116.733696331961,116.816156551024,116.898616462887,116.981076074399,117.063535392408,
117.145994423762,117.228453175308,117.310911653896,117.393369866372,117.475827819582,
117.558285520376,117.640742975597,117.723200192095,117.809212887381,117.892537685939,
117.975004291531,118.057470052914,118.139934997504,118.222399152712,118.304862545949,
118.38732520462,118.469787156132,118.552248427884,118.634709047277,118.717169041708,
118.799628438572,118.882087265263,118.96454554917,119.047003317683,119.129460598189,
119.21359471338,119.29606071174,119.378525088346,119.460987952842,119.543449414848,
119.625909583967,119.708368569783,119.790826481864,119.876423976787,119.958888713832,
120.041350486219,120.123809732384,120.206266890623,120.288729409705,120.371187081116,
120.453645872309,120.475606441247),.UNSPECIFIED.);
#3282=B_SPLINE_CURVE_WITH_KNOTS('',3,(#41735,#41736,#41737,#41738,#41739,
#41740,#41741,#41742,#41743,#41744,#41745,#41746,#41747,#41748,#41749,#41750,
#41751,#41752,#41753,#41754,#41755,#41756,#41757,#41758,#41759,#41760,#41761,
#41762,#41763,#41764,#41765,#41766,#41767,#41768,#41769,#41770,#41771,#41772,
#41773,#41774,#41775,#41776,#41777,#41778,#41779,#41780,#41781,#41782,#41783,
#41784,#41785,#41786,#41787,#41788,#41789,#41790,#41791,#41792,#41793,#41794,
#41795,#41796,#41797,#41798,#41799,#41800,#41801,#41802,#41803,#41804,#41805,
#41806,#41807,#41808,#41809,#41810,#41811,#41812,#41813,#41814,#41815,#41816,
#41817,#41818,#41819,#41820,#41821,#41822,#41823,#41824,#41825,#41826,#41827,
#41828,#41829,#41830,#41831,#41832,#41833,#41834,#41835,#41836,#41837,#41838,
#41839,#41840,#41841,#41842,#41843,#41844,#41845,#41846,#41847,#41848,#41849,
#41850,#41851,#41852,#41853,#41854,#41855,#41856,#41857,#41858,#41859,#41860,
#41861,#41862,#41863,#41864,#41865,#41866,#41867,#41868,#41869,#41870,#41871,
#41872,#41873,#41874,#41875,#41876,#41877,#41878,#41879,#41880,#41881,#41882,
#41883,#41884,#41885,#41886,#41887,#41888,#41889,#41890,#41891,#41892,#41893,
#41894,#41895,#41896,#41897,#41898,#41899,#41900),.UNSPECIFIED.,.F.,.F.,
(4,3,3,3,3,3,3,3,3,3,3,3,3,3,3,3,3,3,3,3,3,3,3,3,3,3,3,3,3,3,3,3,3,3,3,
3,3,3,3,3,3,3,3,3,3,3,3,3,3,3,3,3,3,3,3,4),(122.522113490113,122.605069596484,
122.68820086178,122.77160718408,122.855150126164,122.938923640885,123.01850310699,
123.094569266447,123.170540767481,123.246434387278,123.322266823565,123.398054713149,
123.475303560045,123.551067358696,123.62683926476,123.702634282231,123.780987083752,
123.856915622454,123.936480555384,124.016045488315,124.094590105254,124.173042147424,
124.251416108006,124.329726424845,124.407987490218,124.486216783485,124.56442958023,
124.642638866358,124.720857623296,124.799131302408,124.877433524174,124.95581898075,
125.013587869639,125.093236889905,125.172815781575,125.252335424282,125.331798335787,
125.411227186612,125.490631586094,125.512359060302,125.593591113392,125.674871831731,
125.75893643654,125.840368571396,125.92574941118,126.011130250964,126.096363174434,
126.18151813566,126.266523072382,126.351421364474,126.4361279108,126.509901441627,
126.586460327823,126.663009501421,126.739575236472,126.758437754617),
 .UNSPECIFIED.);
#3283=B_SPLINE_CURVE_WITH_KNOTS('',3,(#41901,#41902,#41903,#41904,#41905,
#41906,#41907,#41908,#41909,#41910,#41911,#41912,#41913,#41914,#41915,#41916,
#41917,#41918,#41919,#41920,#41921,#41922,#41923,#41924,#41925,#41926,#41927,
#41928,#41929,#41930,#41931,#41932,#41933,#41934,#41935,#41936,#41937,#41938,
#41939,#41940,#41941,#41942,#41943,#41944,#41945,#41946,#41947,#41948,#41949,
#41950,#41951,#41952,#41953,#41954,#41955,#41956,#41957,#41958,#41959,#41960,
#41961,#41962,#41963,#41964,#41965,#41966,#41967,#41968,#41969,#41970,#41971,
#41972,#41973,#41974,#41975,#41976,#41977,#41978,#41979,#41980,#41981,#41982),
 .UNSPECIFIED.,.F.,.F.,(4,3,3,3,3,3,3,3,3,3,3,3,3,3,3,3,3,3,3,3,3,3,3,3,
3,3,3,4),(120.475463669947,120.554850270742,120.634246911642,120.713664668923,
120.793152621789,120.872675522437,120.952293050511,121.02341834434,121.101085824564,
121.178667279634,121.25617663057,121.333617501694,121.411018696993,121.48839400896,
121.522189535002,121.605680980661,121.689328625406,121.77321384827,121.857212626673,
121.941396882581,122.020960725665,122.100426388793,122.17978824849,122.259057631398,
122.338222246484,122.417325067641,122.496364377615,122.522113490003),
 .UNSPECIFIED.);
#3284=B_SPLINE_CURVE_WITH_KNOTS('',3,(#41984,#41985,#41986,#41987,#41988,
#41989,#41990,#41991,#41992,#41993,#41994,#41995,#41996,#41997,#41998,#41999,
#42000,#42001,#42002,#42003,#42004,#42005,#42006,#42007,#42008,#42009,#42010,
#42011,#42012,#42013,#42014,#42015,#42016,#42017,#42018,#42019,#42020,#42021,
#42022,#42023,#42024,#42025,#42026,#42027,#42028,#42029,#42030,#42031,#42032,
#42033,#42034,#42035,#42036,#42037,#42038,#42039,#42040,#42041,#42042,#42043,
#42044,#42045,#42046,#42047,#42048,#42049,#42050,#42051,#42052,#42053,#42054,
#42055,#42056,#42057,#42058,#42059),.UNSPECIFIED.,.F.,.F.,(4,3,3,3,3,3,
3,3,3,3,3,3,3,3,3,3,3,3,3,3,3,3,3,3,3,4),(120.475606441247,120.558068044977,
120.640528982829,120.722989282201,120.805448970489,120.887908075087,120.970366623388,
121.052824642781,121.135282160653,121.221959118733,121.304425904274,121.386891017342,
121.46935456759,121.551816664649,121.634277418131,121.716736937627,121.799195332712,
121.881652712945,121.964119098632,122.04658230014,122.12904275599,122.211500904544,
122.293966508298,122.376426386686,122.458890497938,122.522113489927),
 .UNSPECIFIED.);
#3285=B_SPLINE_CURVE_WITH_KNOTS('',3,(#42060,#42061,#42062,#42063,#42064,
#42065,#42066,#42067,#42068,#42069,#42070,#42071,#42072,#42073,#42074,#42075,
#42076,#42077,#42078,#42079,#42080,#42081,#42082,#42083,#42084,#42085,#42086,
#42087,#42088,#42089,#42090,#42091,#42092,#42093,#42094,#42095,#42096,#42097,
#42098,#42099,#42100,#42101,#42102,#42103,#42104,#42105,#42106,#42107,#42108,
#42109,#42110,#42111,#42112,#42113,#42114,#42115,#42116,#42117,#42118,#42119,
#42120,#42121,#42122,#42123,#42124,#42125,#42126,#42127,#42128,#42129,#42130,
#42131,#42132,#42133,#42134,#42135,#42136,#42137,#42138,#42139,#42140,#42141,
#42142,#42143,#42144,#42145,#42146,#42147,#42148,#42149,#42150,#42151,#42152,
#42153,#42154,#42155,#42156,#42157,#42158,#42159,#42160,#42161,#42162,#42163,
#42164,#42165,#42166,#42167,#42168,#42169,#42170,#42171,#42172,#42173,#42174,
#42175,#42176,#42177,#42178,#42179,#42180,#42181,#42182,#42183,#42184,#42185,
#42186,#42187,#42188,#42189,#42190,#42191,#42192,#42193,#42194,#42195,#42196,
#42197,#42198,#42199,#42200,#42201,#42202,#42203,#42204,#42205,#42206,#42207,
#42208,#42209,#42210,#42211,#42212,#42213,#42214,#42215,#42216),
 .UNSPECIFIED.,.F.,.F.,(4,3,3,3,3,3,3,3,3,3,3,3,3,3,3,3,3,3,3,3,3,3,3,3,
3,3,3,3,3,3,3,3,3,3,3,3,3,3,3,3,3,3,3,3,3,3,3,3,3,3,3,3,4),(122.522113490003,
122.604575696103,122.687037553906,122.769499070261,122.851960252018,122.934421106029,
123.016881639141,123.099341858204,123.181801770067,123.264261381579,123.346720699588,
123.429179730941,123.511638482488,123.594096961076,123.676555173551,123.759013126762,
123.841470827555,123.923928282777,124.006385499274,124.09239819456,124.175722993119,
124.258189598711,124.340655360094,124.423120304683,124.505584459892,124.588047853128,
124.6705105118,124.752972463311,124.835433735064,124.917894354457,125.000354348888,
125.082813745752,125.165272572442,125.247730856349,125.330188624862,125.412645905368,
125.49678002056,125.579246018919,125.661710395526,125.744173260021,125.826634722027,
125.909094891147,125.991553876963,126.074011789043,126.159609283966,126.242074021012,
126.324535793398,126.406995039563,126.489452197802,126.571914716884,126.654372388295,
126.736831179488,126.758791748426),.UNSPECIFIED.);
#3286=B_SPLINE_CURVE_WITH_KNOTS('',3,(#42222,#42223,#42224,#42225,#42226,
#42227,#42228,#42229,#42230,#42231,#42232,#42233,#42234,#42235,#42236,#42237,
#42238,#42239,#42240,#42241,#42242,#42243,#42244,#42245,#42246,#42247,#42248,
#42249,#42250,#42251,#42252,#42253,#42254,#42255,#42256,#42257,#42258,#42259,
#42260,#42261,#42262,#42263,#42264,#42265,#42266,#42267,#42268,#42269,#42270,
#42271,#42272,#42273,#42274,#42275,#42276,#42277,#42278,#42279,#42280,#42281,
#42282,#42283,#42284,#42285,#42286,#42287,#42288,#42289,#42290,#42291,#42292,
#42293,#42294,#42295,#42296,#42297,#42298,#42299,#42300,#42301,#42302,#42303,
#42304,#42305,#42306,#42307,#42308,#42309,#42310,#42311,#42312,#42313,#42314,
#42315,#42316,#42317,#42318,#42319,#42320,#42321,#42322,#42323,#42324,#42325,
#42326,#42327,#42328,#42329,#42330,#42331,#42332,#42333,#42334,#42335,#42336,
#42337,#42338,#42339,#42340,#42341,#42342,#42343,#42344,#42345,#42346,#42347,
#42348,#42349,#42350,#42351,#42352,#42353,#42354,#42355,#42356,#42357,#42358,
#42359,#42360,#42361,#42362,#42363,#42364,#42365,#42366,#42367,#42368,#42369,
#42370,#42371,#42372,#42373,#42374,#42375,#42376,#42377,#42378,#42379,#42380,
#42381,#42382,#42383,#42384,#42385,#42386,#42387),.UNSPECIFIED.,.F.,.F.,
(4,3,3,3,3,3,3,3,3,3,3,3,3,3,3,3,3,3,3,3,3,3,3,3,3,3,3,3,3,3,3,3,3,3,3,
3,3,3,3,3,3,3,3,3,3,3,3,3,3,3,3,3,3,3,3,4),(128.805298797182,128.911988861494,
129.003757394939,129.08126652778,129.158693803456,129.236054838678,129.313365202671,
129.390640427854,129.46790893197,129.545176666585,129.622457667941,129.699765977111,
129.777162089196,129.854603850555,129.932165038294,130.001299776264,130.077365935721,
130.153337436755,130.229231056552,130.30506349284,130.380851382424,130.458100229319,
130.533864027971,130.609635934035,130.685430951506,130.763783753026,130.839712291728,
130.919277224659,130.998842157589,131.077386774527,131.155838816698,131.23421277728,
131.312523094119,131.390784159492,131.469013452759,131.547226249504,131.625435535631,
131.703654292569,131.781927971682,131.860230193448,131.938615650023,131.996384538914,
132.07603355918,132.155612450851,132.235132093558,132.314595005064,132.394023855889,
132.473428255372,132.495155729576,132.576387782666,132.657668501004,132.741733105813,
132.823165240669,132.908546080454,132.993926920239,133.04207837227),
 .UNSPECIFIED.);
#3287=B_SPLINE_CURVE_WITH_KNOTS('',3,(#42388,#42389,#42390,#42391,#42392,
#42393,#42394,#42395,#42396,#42397,#42398,#42399,#42400,#42401,#42402,#42403,
#42404,#42405,#42406,#42407,#42408,#42409,#42410,#42411,#42412,#42413,#42414,
#42415,#42416,#42417,#42418,#42419,#42420,#42421,#42422,#42423,#42424,#42425,
#42426,#42427,#42428,#42429,#42430,#42431,#42432,#42433,#42434,#42435,#42436,
#42437,#42438,#42439,#42440,#42441,#42442,#42443,#42444,#42445,#42446,#42447,
#42448,#42449,#42450,#42451,#42452,#42453,#42454,#42455,#42456,#42457,#42458,
#42459,#42460,#42461,#42462,#42463,#42464,#42465,#42466,#42467,#42468,#42469,
#42470,#42471,#42472),.UNSPECIFIED.,.F.,.F.,(4,3,3,3,3,3,3,3,3,3,3,3,3,
3,3,3,3,3,3,3,3,3,3,3,3,3,3,3,4),(126.758437754617,126.835062761065,126.911722231118,
126.988461459613,127.008672632289,127.088224496788,127.167716232239,127.247160090955,
127.32656828786,127.405953009399,127.485339045384,127.564727826671,127.644130425287,
127.723557920918,127.803056644058,127.882593789454,127.962219322918,128.006215013614,
128.083882493838,128.161463948907,128.238973299844,128.316414170968,128.393815366268,
128.471190678234,128.504986204277,128.582949343818,128.660954630138,128.739069201868,
128.805298797085),.UNSPECIFIED.);
#3288=B_SPLINE_CURVE_WITH_KNOTS('',3,(#42474,#42475,#42476,#42477,#42478,
#42479,#42480,#42481,#42482,#42483,#42484,#42485,#42486,#42487,#42488,#42489,
#42490,#42491,#42492,#42493,#42494,#42495,#42496,#42497,#42498,#42499,#42500,
#42501,#42502,#42503,#42504,#42505,#42506,#42507,#42508,#42509,#42510,#42511,
#42512,#42513,#42514,#42515,#42516,#42517,#42518,#42519,#42520,#42521,#42522,
#42523,#42524,#42525,#42526,#42527,#42528,#42529,#42530,#42531,#42532,#42533,
#42534,#42535,#42536,#42537,#42538,#42539,#42540,#42541,#42542,#42543,#42544,
#42545,#42546,#42547,#42548,#42549),.UNSPECIFIED.,.F.,.F.,(4,3,3,3,3,3,
3,3,3,3,3,3,3,3,3,3,3,3,3,3,3,3,3,3,3,4),(126.758791748426,126.841253352156,
126.923714290008,127.00617458938,127.088634277668,127.171093382267,127.253551930567,
127.33600994996,127.418467467832,127.505144425917,127.587611211458,127.670076324526,
127.752539874774,127.835001971833,127.917462725315,127.999922244811,128.082380639896,
128.164838020129,128.247304405816,128.329767607324,128.412228063174,128.494686211728,
128.577151815482,128.65961169387,128.742075805122,128.805298797182),
 .UNSPECIFIED.);
#3289=B_SPLINE_CURVE_WITH_KNOTS('',3,(#42550,#42551,#42552,#42553,#42554,
#42555,#42556,#42557,#42558,#42559,#42560,#42561,#42562,#42563,#42564,#42565,
#42566,#42567,#42568,#42569,#42570,#42571,#42572,#42573,#42574,#42575,#42576,
#42577,#42578,#42579,#42580,#42581,#42582,#42583,#42584,#42585,#42586,#42587,
#42588,#42589,#42590,#42591,#42592,#42593,#42594,#42595,#42596,#42597,#42598,
#42599,#42600,#42601,#42602,#42603,#42604,#42605,#42606,#42607,#42608,#42609,
#42610,#42611,#42612,#42613,#42614,#42615,#42616,#42617,#42618,#42619,#42620,
#42621,#42622,#42623,#42624,#42625,#42626,#42627,#42628,#42629,#42630,#42631,
#42632,#42633,#42634,#42635,#42636,#42637,#42638,#42639,#42640,#42641,#42642,
#42643,#42644,#42645,#42646,#42647,#42648,#42649,#42650,#42651,#42652,#42653,
#42654,#42655,#42656,#42657,#42658,#42659,#42660,#42661,#42662,#42663,#42664,
#42665,#42666,#42667,#42668,#42669,#42670,#42671,#42672,#42673,#42674,#42675,
#42676,#42677,#42678,#42679,#42680,#42681,#42682,#42683,#42684,#42685,#42686,
#42687,#42688,#42689,#42690,#42691,#42692,#42693,#42694,#42695,#42696,#42697,
#42698,#42699,#42700,#42701,#42702,#42703,#42704,#42705,#42706,#42707,#42708,
#42709,#42710,#42711,#42712,#42713,#42714,#42715,#42716,#42717,#42718),
 .UNSPECIFIED.,.F.,.F.,(4,3,3,3,3,3,3,3,3,3,3,3,3,3,3,3,3,3,3,3,3,3,3,3,
3,3,3,3,3,3,3,3,3,3,3,3,3,3,3,3,3,3,3,3,3,3,3,3,3,3,3,3,3,3,3,3,4),(128.805298797182,
128.826262653494,128.907494706584,128.988775424924,129.072840029732,129.154272164589,
129.239653004372,129.325033844156,129.410266767626,129.495421728852,129.580426665574,
129.665324957666,129.750031503992,129.823805034819,129.900363999506,129.976917566385,
130.053480331964,130.130098864432,130.206748632926,130.283481746416,130.322576225481,
130.40212808998,130.481619825431,130.561063684147,130.640471881052,130.719856602591,
130.799242638576,130.878631419863,130.958034018479,131.037461514111,131.11696023725,
131.196497382646,131.27612291611,131.320118606806,131.39778608703,131.475367542099,
131.552876893036,131.630317764161,131.707718959459,131.785094271426,131.818889797469,
131.902381243129,131.986028887874,132.069914110738,132.15391288914,132.238097145049,
132.317660988131,132.39518425885,132.475986430167,132.553339738529,132.630646450832,
132.70792063914,132.78517635439,132.862442965893,132.939716235435,133.017029806076,
133.041601629382),.UNSPECIFIED.);
#3290=B_SPLINE_CURVE_WITH_KNOTS('',3,(#42724,#42725,#42726,#42727,#42728,
#42729,#42730,#42731,#42732,#42733,#42734,#42735,#42736,#42737,#42738,#42739,
#42740,#42741,#42742,#42743,#42744,#42745,#42746,#42747,#42748,#42749,#42750,
#42751,#42752,#42753,#42754,#42755,#42756,#42757,#42758,#42759,#42760,#42761,
#42762,#42763,#42764,#42765,#42766,#42767,#42768,#42769,#42770,#42771,#42772,
#42773,#42774,#42775,#42776,#42777,#42778,#42779,#42780,#42781,#42782,#42783,
#42784,#42785,#42786,#42787,#42788,#42789,#42790,#42791,#42792,#42793,#42794,
#42795,#42796,#42797,#42798,#42799,#42800,#42801,#42802,#42803,#42804,#42805,
#42806,#42807,#42808,#42809,#42810,#42811,#42812,#42813,#42814,#42815,#42816,
#42817,#42818,#42819,#42820,#42821,#42822,#42823,#42824,#42825,#42826,#42827,
#42828,#42829,#42830,#42831,#42832,#42833,#42834,#42835,#42836,#42837,#42838,
#42839,#42840,#42841,#42842,#42843,#42844,#42845,#42846,#42847,#42848,#42849,
#42850,#42851,#42852,#42853,#42854,#42855,#42856,#42857,#42858,#42859,#42860,
#42861,#42862,#42863,#42864,#42865,#42866,#42867,#42868,#42869,#42870,#42871,
#42872,#42873,#42874,#42875,#42876,#42877,#42878,#42879,#42880,#42881,#42882,
#42883,#42884,#42885,#42886,#42887,#42888,#42889,#42890,#42891,#42892),
 .UNSPECIFIED.,.F.,.F.,(4,3,3,3,3,3,3,3,3,3,3,3,3,3,3,3,3,3,3,3,3,3,3,3,
3,3,3,3,3,3,3,3,3,3,3,3,3,3,3,3,3,3,3,3,3,3,3,3,3,3,3,3,3,3,3,3,4),(135.088484104504,
135.163442230927,135.238336606457,135.313179200081,135.387991964862,135.462795806253,
135.487782873551,135.571274319211,135.654921963956,135.73880718682,135.822805965222,
135.906990221131,135.986554064213,136.064063197054,136.14149047273,136.218851507951,
136.296161871945,136.373437097127,136.450705601244,136.527973335858,136.605254337215,
136.682562646384,136.75995875847,136.837400519828,136.914961707568,136.984096445538,
137.060162604995,137.136134106029,137.212027725826,137.287860162113,137.363648051697,
137.440896898593,137.516660697244,137.592432603309,137.66822762078,137.746580422301,
137.822508961003,137.902073893933,137.981638826863,138.060183443802,138.138635485972,
138.217009446554,138.295319763393,138.373580828766,138.451810122033,138.530022918778,
138.608232204905,138.686450961843,138.764724640956,138.843026862722,138.921412319298,
138.979181208188,139.058844071035,139.138415807856,139.217933488224,139.297398307652,
139.325292139011),.UNSPECIFIED.);
#3291=B_SPLINE_CURVE_WITH_KNOTS('',3,(#42893,#42894,#42895,#42896,#42897,
#42898,#42899,#42900,#42901,#42902,#42903,#42904,#42905,#42906,#42907,#42908,
#42909,#42910,#42911,#42912,#42913,#42914,#42915,#42916,#42917,#42918,#42919,
#42920,#42921,#42922,#42923,#42924,#42925,#42926,#42927,#42928,#42929,#42930,
#42931,#42932,#42933,#42934,#42935,#42936,#42937,#42938,#42939,#42940,#42941,
#42942,#42943,#42944,#42945,#42946,#42947,#42948,#42949,#42950,#42951,#42952,
#42953,#42954,#42955,#42956,#42957,#42958,#42959,#42960,#42961,#42962,#42963,
#42964,#42965,#42966,#42967,#42968,#42969,#42970,#42971,#42972,#42973,#42974),
 .UNSPECIFIED.,.F.,.F.,(4,3,3,3,3,3,3,3,3,3,3,3,3,3,3,3,3,3,3,3,3,3,3,3,
3,3,3,4),(133.04207837227,133.127269451156,133.212372531528,133.297318640989,
133.382151476148,133.466804667066,133.492698110901,133.569257075588,133.645810642467,
133.722373408045,133.798991940513,133.875641709007,133.952374822497,133.991469301563,
134.071021166062,134.150512901513,134.229956760229,134.309364957134,134.388749678673,
134.468135714658,134.547524495944,134.626927094561,134.706354590192,134.785853313332,
134.865390458728,134.945015992192,134.989011682888,135.088484104362),
 .UNSPECIFIED.);
#3292=B_SPLINE_CURVE_WITH_KNOTS('',3,(#42976,#42977,#42978,#42979,#42980,
#42981,#42982,#42983,#42984,#42985,#42986,#42987,#42988,#42989,#42990,#42991,
#42992,#42993,#42994,#42995,#42996,#42997,#42998,#42999,#43000,#43001,#43002,
#43003,#43004,#43005,#43006,#43007,#43008,#43009,#43010,#43011,#43012,#43013,
#43014,#43015,#43016,#43017,#43018,#43019,#43020,#43021,#43022,#43023,#43024,
#43025,#43026,#43027,#43028,#43029,#43030,#43031,#43032,#43033,#43034,#43035,
#43036,#43037,#43038,#43039,#43040,#43041,#43042,#43043,#43044,#43045,#43046,
#43047,#43048,#43049,#43050,#43051,#43052,#43053,#43054,#43055,#43056,#43057),
 .UNSPECIFIED.,.F.,.F.,(4,3,3,3,3,3,3,3,3,3,3,3,3,3,3,3,3,3,3,3,3,3,3,3,
3,3,3,4),(133.041601629382,133.119012760366,133.196474106686,133.274046992174,
133.315203369456,133.391269528913,133.467241029947,133.543134649744,133.618967086032,
133.694754975616,133.772003822511,133.847767621162,133.923539527227,133.999334544698,
134.077687346218,134.15361588492,134.233180817851,134.312745750781,134.39089412348,
134.46894753747,134.546901574216,134.62479799234,134.702650332631,134.7804721082,
134.858290455892,134.936103782312,135.013953840078,135.088484104362),
 .UNSPECIFIED.);
#3293=B_SPLINE_CURVE_WITH_KNOTS('',3,(#43058,#43059,#43060,#43061,#43062,
#43063,#43064,#43065,#43066,#43067,#43068,#43069,#43070,#43071,#43072,#43073,
#43074,#43075,#43076,#43077,#43078,#43079,#43080,#43081,#43082,#43083,#43084,
#43085,#43086,#43087,#43088,#43089,#43090,#43091,#43092,#43093,#43094,#43095,
#43096,#43097,#43098,#43099,#43100,#43101,#43102,#43103,#43104,#43105,#43106,
#43107,#43108,#43109,#43110,#43111,#43112,#43113,#43114,#43115,#43116,#43117,
#43118,#43119,#43120,#43121,#43122,#43123,#43124,#43125,#43126,#43127,#43128,
#43129,#43130,#43131,#43132,#43133,#43134,#43135,#43136,#43137,#43138,#43139,
#43140,#43141,#43142,#43143,#43144,#43145,#43146,#43147,#43148,#43149,#43150,
#43151,#43152,#43153,#43154,#43155,#43156,#43157,#43158,#43159,#43160,#43161,
#43162,#43163,#43164,#43165,#43166,#43167,#43168,#43169,#43170,#43171,#43172,
#43173,#43174,#43175,#43176,#43177,#43178,#43179,#43180,#43181,#43182,#43183,
#43184,#43185,#43186,#43187,#43188,#43189,#43190,#43191,#43192,#43193,#43194,
#43195,#43196,#43197,#43198,#43199,#43200,#43201,#43202,#43203,#43204,#43205,
#43206,#43207,#43208,#43209,#43210,#43211,#43212,#43213,#43214,#43215,#43216,
#43217,#43218,#43219,#43220,#43221,#43222,#43223,#43224,#43225,#43226),
 .UNSPECIFIED.,.F.,.F.,(4,3,3,3,3,3,3,3,3,3,3,3,3,3,3,3,3,3,3,3,3,3,3,3,
3,3,3,3,3,3,3,3,3,3,3,3,3,3,3,3,3,3,3,3,3,3,3,3,3,3,3,3,3,3,3,3,4),(135.088484104437,
135.187057197254,135.286852023069,135.310288132106,135.389937152372,135.469516044044,
135.549035686751,135.628498598256,135.707927449082,135.787331848565,135.809059322768,
135.890291375857,135.971572094196,136.055636699005,136.137068833861,136.222449673646,
136.307830513431,136.393063436902,136.478218398129,136.563223334852,136.648121626945,
136.732828173272,136.806601704093,136.88316066878,136.959714235659,137.036277001237,
137.112895533704,137.189545302199,137.266278415688,137.305372894756,137.384924759255,
137.464416494706,137.543860353422,137.623268550328,137.702653271866,137.782039307852,
137.861428089138,137.940830687755,138.020258183386,138.099756906526,138.179294051922,
138.258919585386,138.30291527608,138.380582756304,138.458164211373,138.53567356231,
138.613114433433,138.690515628732,138.767890940699,138.801686466743,138.885177912403,
138.968825557148,139.052710780013,139.136709558415,139.220893814324,139.300457657405,
139.325474057287),.UNSPECIFIED.);
#3294=B_SPLINE_CURVE_WITH_KNOTS('',3,(#43232,#43233,#43234,#43235,#43236,
#43237,#43238,#43239,#43240,#43241,#43242,#43243,#43244,#43245,#43246,#43247,
#43248,#43249,#43250,#43251,#43252,#43253,#43254,#43255,#43256,#43257,#43258,
#43259,#43260,#43261,#43262,#43263,#43264,#43265,#43266,#43267,#43268,#43269,
#43270,#43271,#43272,#43273,#43274,#43275,#43276,#43277,#43278,#43279,#43280,
#43281,#43282,#43283,#43284,#43285,#43286,#43287,#43288,#43289,#43290,#43291,
#43292,#43293,#43294,#43295,#43296,#43297,#43298,#43299,#43300,#43301,#43302,
#43303,#43304,#43305,#43306,#43307,#43308,#43309,#43310,#43311,#43312,#43313,
#43314,#43315,#43316,#43317,#43318,#43319,#43320,#43321,#43322,#43323,#43324,
#43325,#43326,#43327,#43328,#43329,#43330,#43331,#43332,#43333,#43334,#43335,
#43336,#43337,#43338,#43339,#43340,#43341,#43342,#43343,#43344,#43345,#43346,
#43347,#43348,#43349,#43350,#43351,#43352,#43353,#43354,#43355,#43356,#43357,
#43358,#43359,#43360,#43361,#43362,#43363,#43364,#43365,#43366,#43367,#43368,
#43369,#43370,#43371,#43372,#43373,#43374,#43375,#43376,#43377,#43378,#43379,
#43380,#43381,#43382,#43383,#43384,#43385,#43386,#43387,#43388),
 .UNSPECIFIED.,.F.,.F.,(4,3,3,3,3,3,3,3,3,3,3,3,3,3,3,3,3,3,3,3,3,3,3,3,
3,3,3,3,3,3,3,3,3,3,3,3,3,3,3,3,3,3,3,3,3,3,3,3,3,3,3,3,4),(141.371669411542,
141.454131617642,141.536593475445,141.6190549918,141.701516173558,141.783977027568,
141.86643756068,141.948897779743,142.031357691606,142.113817303118,142.196276621127,
142.27873565248,142.361194404027,142.443652882615,142.52611109509,142.608569048301,
142.691026749094,142.773484204316,142.855941420814,142.9419541161,143.025278914658,
143.10774552025,143.190211281633,143.272676226223,143.355140381431,143.437603774668,
143.520066433339,143.602528384851,143.684989656603,143.767450275996,143.849910270427,
143.932369667291,144.014828493982,144.097286777889,144.179744546402,144.262201826908,
144.346335942099,144.428801940459,144.511266317065,144.593729181561,144.676190643567,
144.758650812686,144.841109798502,144.923567710583,145.009165205505,145.091629942551,
145.174091714938,145.256550961103,145.339008119341,145.421470638424,145.503928309835,
145.586387101028,145.608347669965),.UNSPECIFIED.);
#3295=B_SPLINE_CURVE_WITH_KNOTS('',3,(#43389,#43390,#43391,#43392,#43393,
#43394,#43395,#43396,#43397,#43398,#43399,#43400,#43401,#43402,#43403,#43404,
#43405,#43406,#43407,#43408,#43409,#43410,#43411,#43412,#43413,#43414,#43415,
#43416,#43417,#43418,#43419,#43420,#43421,#43422,#43423,#43424,#43425,#43426,
#43427,#43428,#43429,#43430,#43431,#43432,#43433,#43434,#43435,#43436,#43437,
#43438,#43439,#43440,#43441,#43442,#43443,#43444,#43445,#43446,#43447,#43448,
#43449,#43450,#43451,#43452,#43453,#43454,#43455,#43456,#43457,#43458,#43459,
#43460,#43461,#43462,#43463,#43464,#43465,#43466,#43467),.UNSPECIFIED.,
 .F.,.F.,(4,3,3,3,3,3,3,3,3,3,3,3,3,3,3,3,3,3,3,3,3,3,3,3,3,3,4),(139.325292139011,
139.404712893845,139.47795239885,139.559184451939,139.640465170277,139.724529775086,
139.805961909942,139.891342749727,139.976723589513,140.061956512983,140.14711147421,
140.232116410933,140.317014703026,140.401721249352,140.475494780175,140.552053744862,
140.628607311741,140.70517007732,140.781788609787,140.858438378282,140.935171491771,
140.974265970838,141.062620839722,141.150779269528,141.238767802836,141.326421620508,
141.371669411542),.UNSPECIFIED.);
#3296=B_SPLINE_CURVE_WITH_KNOTS('',3,(#43469,#43470,#43471,#43472,#43473,
#43474,#43475,#43476,#43477,#43478,#43479,#43480,#43481,#43482,#43483,#43484,
#43485,#43486,#43487,#43488,#43489,#43490,#43491,#43492,#43493,#43494,#43495,
#43496,#43497,#43498,#43499,#43500,#43501,#43502,#43503,#43504,#43505,#43506,
#43507,#43508,#43509,#43510,#43511,#43512,#43513,#43514,#43515,#43516,#43517,
#43518,#43519,#43520,#43521,#43522,#43523,#43524,#43525,#43526,#43527,#43528,
#43529,#43530,#43531,#43532,#43533,#43534,#43535,#43536,#43537,#43538,#43539,
#43540,#43541,#43542,#43543,#43544,#43545,#43546,#43547,#43548,#43549,#43550),
 .UNSPECIFIED.,.F.,.F.,(4,3,3,3,3,3,3,3,3,3,3,3,3,3,3,3,3,3,3,3,3,3,3,3,
3,3,3,4),(139.325474057287,139.402955071056,139.480359271889,139.557702259976,
139.634999591525,139.71226678928,139.789533511538,139.866803992031,139.944092267711,
140.021412382873,140.098821829852,140.176281003969,140.253852542081,140.29800003873,
140.374066198187,140.450037699221,140.525931319018,140.601763755305,140.67755164489,
140.754800491785,140.830564290437,140.9063361965,140.982131213972,141.060484015493,
141.136412554194,141.215977487125,141.295542420055,141.371669411541),
 .UNSPECIFIED.);
#3297=B_SPLINE_CURVE_WITH_KNOTS('',3,(#43551,#43552,#43553,#43554,#43555,
#43556,#43557,#43558,#43559,#43560,#43561,#43562,#43563,#43564,#43565,#43566,
#43567,#43568,#43569,#43570,#43571,#43572,#43573,#43574,#43575,#43576,#43577,
#43578,#43579,#43580,#43581,#43582,#43583,#43584,#43585,#43586,#43587,#43588,
#43589,#43590,#43591,#43592,#43593,#43594,#43595,#43596,#43597,#43598,#43599,
#43600,#43601,#43602,#43603,#43604,#43605,#43606,#43607,#43608,#43609,#43610,
#43611,#43612,#43613,#43614,#43615,#43616,#43617,#43618,#43619,#43620,#43621,
#43622,#43623,#43624,#43625,#43626,#43627,#43628,#43629,#43630,#43631,#43632,
#43633,#43634,#43635,#43636,#43637,#43638,#43639,#43640,#43641,#43642,#43643,
#43644,#43645,#43646,#43647,#43648,#43649,#43650,#43651,#43652,#43653,#43654,
#43655,#43656,#43657,#43658,#43659,#43660,#43661,#43662,#43663,#43664,#43665,
#43666,#43667,#43668,#43669,#43670,#43671,#43672,#43673,#43674,#43675,#43676,
#43677,#43678,#43679,#43680,#43681,#43682,#43683,#43684,#43685,#43686,#43687,
#43688,#43689,#43690,#43691,#43692,#43693,#43694,#43695,#43696,#43697,#43698,
#43699,#43700,#43701,#43702,#43703,#43704,#43705,#43706,#43707,#43708,#43709,
#43710,#43711,#43712,#43713,#43714,#43715,#43716,#43717,#43718,#43719),
 .UNSPECIFIED.,.F.,.F.,(4,3,3,3,3,3,3,3,3,3,3,3,3,3,3,3,3,3,3,3,3,3,3,3,
3,3,3,3,3,3,3,3,3,3,3,3,3,3,3,3,3,3,3,3,3,3,3,3,3,3,3,3,3,3,3,3,4),(141.371669411676,
141.449146283997,141.52653116975,141.603839824246,141.681087947451,141.758291013893,
141.835469916872,141.912638791059,141.989811762845,142.06703702738,142.144288126524,
142.221627655501,142.29308480138,142.372733821646,142.452312713318,142.531832356025,
142.61129526753,142.690724118355,142.770128517839,142.791855992042,142.873088045131,
142.95436876347,143.038433368278,143.119865503134,143.20524634292,143.290627182705,
143.375860106175,143.461015067402,143.546020004126,143.630918296218,143.715624842544,
143.789398373367,143.865957338054,143.942510904934,144.019073670512,144.09569220298,
144.172341971474,144.249075084964,144.28816956403,144.367721428528,144.44721316398,
144.526657022696,144.606065219601,144.68544994114,144.764835977125,144.844224758411,
144.923627357028,145.003054852659,145.082553575799,145.162090721195,145.241716254659,
145.285711945355,145.366485127798,145.444057801989,145.521565384887,145.599009972342,
145.608804675126),.UNSPECIFIED.);
#3298=B_SPLINE_CURVE_WITH_KNOTS('',3,(#43725,#43726,#43727,#43728,#43729,
#43730,#43731,#43732,#43733,#43734,#43735,#43736,#43737,#43738,#43739,#43740,
#43741,#43742,#43743,#43744,#43745,#43746,#43747,#43748,#43749,#43750,#43751,
#43752,#43753,#43754,#43755,#43756,#43757,#43758,#43759,#43760,#43761,#43762,
#43763,#43764,#43765,#43766,#43767,#43768,#43769,#43770,#43771,#43772,#43773,
#43774,#43775,#43776,#43777,#43778,#43779,#43780,#43781,#43782,#43783,#43784,
#43785,#43786,#43787,#43788,#43789,#43790,#43791,#43792,#43793,#43794,#43795,
#43796,#43797,#43798,#43799,#43800,#43801,#43802,#43803,#43804,#43805,#43806,
#43807,#43808,#43809,#43810,#43811,#43812,#43813,#43814,#43815,#43816,#43817,
#43818,#43819,#43820,#43821,#43822,#43823,#43824,#43825,#43826,#43827,#43828,
#43829,#43830,#43831,#43832,#43833,#43834,#43835,#43836,#43837,#43838,#43839,
#43840,#43841,#43842,#43843,#43844,#43845,#43846,#43847,#43848,#43849,#43850,
#43851,#43852,#43853,#43854,#43855,#43856,#43857,#43858,#43859,#43860,#43861,
#43862,#43863,#43864,#43865,#43866,#43867,#43868,#43869,#43870,#43871,#43872,
#43873,#43874,#43875,#43876,#43877,#43878,#43879,#43880,#43881,#43882,#43883,
#43884,#43885,#43886,#43887,#43888,#43889,#43890,#43891,#43892,#43893),
 .UNSPECIFIED.,.F.,.F.,(4,3,3,3,3,3,3,3,3,3,3,3,3,3,3,3,3,3,3,3,3,3,3,3,
3,3,3,3,3,3,3,3,3,3,3,3,3,3,3,3,3,3,3,3,3,3,3,3,3,3,3,3,3,3,3,3,4),(147.654854718721,
147.735992160244,147.81721488668,147.898594140889,147.957062640112,148.036614504611,
148.116106240062,148.195550098778,148.274958295683,148.354343017221,148.433729053206,
148.513117834493,148.592520433109,148.671947928741,148.75144665188,148.830983797276,
148.91060933074,148.954605021437,149.032272501661,149.10985395673,149.187363307667,
149.264804178791,149.34220537409,149.419580686057,149.453376212099,149.536867657759,
149.620515302504,149.704400525368,149.78839930377,149.872583559679,149.952147402762,
150.029656535603,150.107083811279,150.184444846501,150.261755210495,150.339030435677,
150.416298939794,150.493566674408,150.570847675764,150.648155984934,150.72555209702,
150.802993858379,150.880555046118,150.949689784087,151.025759187579,151.101733246166,
151.177628741318,151.253462374057,151.333117788431,151.40888467808,151.484644184838,
151.560411306516,151.636201045329,151.712065430347,151.787973334086,151.863978077359,
151.890705689046),.UNSPECIFIED.);
#3299=B_SPLINE_CURVE_WITH_KNOTS('',3,(#43894,#43895,#43896,#43897,#43898,
#43899,#43900,#43901,#43902,#43903,#43904,#43905,#43906,#43907,#43908,#43909,
#43910,#43911,#43912,#43913,#43914,#43915,#43916,#43917,#43918,#43919,#43920,
#43921,#43922,#43923,#43924,#43925,#43926,#43927,#43928,#43929,#43930,#43931,
#43932,#43933,#43934,#43935,#43936,#43937,#43938,#43939,#43940,#43941,#43942,
#43943,#43944,#43945,#43946,#43947,#43948,#43949,#43950,#43951,#43952,#43953,
#43954,#43955,#43956,#43957,#43958,#43959,#43960,#43961,#43962,#43963,#43964,
#43965,#43966,#43967,#43968,#43969),.UNSPECIFIED.,.F.,.F.,(4,3,3,3,3,3,
3,3,3,3,3,3,3,3,3,3,3,3,3,3,3,3,3,3,3,4),(145.608347669965,145.690809273695,
145.773270211547,145.855730510919,145.938190199207,146.020649303806,146.103107852106,
146.185565871499,146.268023389372,146.354700347456,146.437167132997,146.519632246065,
146.602095796313,146.684557893372,146.767018646854,146.84947816635,146.931936561435,
147.014393941668,147.096860327354,147.179323528863,147.261783984712,147.344242133267,
147.426707737021,147.509167615408,147.591631726661,147.654854718721),
 .UNSPECIFIED.);
#3300=B_SPLINE_CURVE_WITH_KNOTS('',3,(#43971,#43972,#43973,#43974,#43975,
#43976,#43977,#43978,#43979,#43980,#43981,#43982,#43983,#43984,#43985,#43986,
#43987,#43988,#43989,#43990,#43991,#43992,#43993,#43994,#43995,#43996,#43997,
#43998,#43999,#44000,#44001,#44002,#44003,#44004,#44005,#44006,#44007,#44008,
#44009,#44010,#44011,#44012,#44013,#44014,#44015,#44016,#44017,#44018,#44019,
#44020,#44021,#44022,#44023,#44024,#44025,#44026,#44027,#44028,#44029,#44030,
#44031,#44032,#44033,#44034,#44035,#44036,#44037,#44038,#44039,#44040,#44041,
#44042,#44043,#44044,#44045,#44046,#44047,#44048,#44049,#44050,#44051,#44052),
 .UNSPECIFIED.,.F.,.F.,(4,3,3,3,3,3,3,3,3,3,3,3,3,3,3,3,3,3,3,3,3,3,3,3,
3,3,3,4),(145.608804675126,145.68620046657,145.763571967009,145.784483136017,
145.867974581677,145.951622226421,146.035507449285,146.119506227687,146.203690483596,
146.28325432668,146.360763459521,146.438190735197,146.515551770419,146.592862134412,
146.670137359595,146.747405863712,146.824673598326,146.901954599682,146.979262908852,
147.056659020938,147.134100782296,147.211661970036,147.280796708004,147.367304586155,
147.453352142583,147.539103971683,147.624397890549,147.654854718612),
 .UNSPECIFIED.);
#3301=B_SPLINE_CURVE_WITH_KNOTS('',3,(#44053,#44054,#44055,#44056,#44057,
#44058,#44059,#44060,#44061,#44062,#44063,#44064,#44065,#44066,#44067,#44068,
#44069,#44070,#44071,#44072,#44073,#44074,#44075,#44076,#44077,#44078,#44079,
#44080,#44081,#44082,#44083,#44084,#44085,#44086,#44087,#44088,#44089,#44090,
#44091,#44092,#44093,#44094,#44095,#44096,#44097,#44098,#44099,#44100,#44101,
#44102,#44103,#44104,#44105,#44106,#44107,#44108,#44109,#44110,#44111,#44112,
#44113,#44114,#44115,#44116,#44117,#44118,#44119,#44120,#44121,#44122,#44123,
#44124,#44125,#44126,#44127,#44128,#44129,#44130,#44131,#44132,#44133,#44134,
#44135,#44136,#44137,#44138,#44139,#44140,#44141,#44142,#44143,#44144,#44145,
#44146,#44147,#44148,#44149,#44150,#44151,#44152,#44153,#44154,#44155,#44156,
#44157,#44158,#44159,#44160,#44161,#44162,#44163,#44164,#44165,#44166,#44167,
#44168,#44169,#44170,#44171,#44172,#44173,#44174,#44175,#44176,#44177,#44178,
#44179,#44180,#44181,#44182,#44183,#44184,#44185,#44186,#44187,#44188,#44189,
#44190,#44191,#44192,#44193,#44194,#44195,#44196,#44197,#44198,#44199,#44200,
#44201,#44202,#44203,#44204,#44205,#44206,#44207,#44208,#44209,#44210,#44211,
#44212,#44213,#44214,#44215,#44216,#44217,#44218,#44219,#44220,#44221),
 .UNSPECIFIED.,.F.,.F.,(4,3,3,3,3,3,3,3,3,3,3,3,3,3,3,3,3,3,3,3,3,3,3,3,
3,3,3,3,3,3,3,3,3,3,3,3,3,3,3,3,3,3,3,3,3,3,3,3,3,3,3,3,3,3,3,3,4),(147.654854718721,
147.732790265047,147.808916093018,147.885058211055,147.961231357942,148.040508290788,
148.116834096366,148.193223597051,148.269728528119,148.278339089329,148.356883706268,
148.435335748438,148.51370970902,148.59202002586,148.670281091232,148.7485103845,
148.826723181244,148.904932467372,148.98315122431,149.061424903423,149.139727125189,
149.218112581765,149.275881470654,149.35553049092,149.435109382591,149.514629025297,
149.594091936802,149.673520787627,149.75292518711,149.774652661317,149.855884714407,
149.937165432746,150.021230037554,150.102662172411,150.188043012195,150.273423851979,
150.358656775449,150.443811736675,150.528816673398,150.61371496549,150.698421511816,
150.772195042642,150.848754007329,150.925307574209,151.001870339787,151.078488872255,
151.155138640751,151.23187175424,151.270966233304,151.350511861412,151.430000531118,
151.5094433945,151.588851572278,151.668242509683,151.747620582116,151.827013456949,
151.891250266881),.UNSPECIFIED.);
#3302=B_SPLINE_CURVE_WITH_KNOTS('',3,(#44227,#44228,#44229,#44230,#44231,
#44232,#44233,#44234,#44235,#44236,#44237,#44238,#44239,#44240,#44241,#44242,
#44243,#44244,#44245,#44246,#44247,#44248,#44249,#44250,#44251,#44252,#44253,
#44254,#44255,#44256,#44257,#44258,#44259,#44260,#44261,#44262,#44263,#44264,
#44265,#44266,#44267,#44268,#44269,#44270,#44271,#44272,#44273,#44274,#44275,
#44276,#44277,#44278,#44279,#44280,#44281,#44282,#44283,#44284,#44285,#44286,
#44287,#44288,#44289,#44290,#44291,#44292,#44293,#44294,#44295,#44296,#44297,
#44298,#44299,#44300,#44301,#44302,#44303,#44304,#44305,#44306,#44307,#44308,
#44309,#44310,#44311,#44312,#44313,#44314,#44315,#44316,#44317,#44318,#44319,
#44320,#44321,#44322,#44323,#44324,#44325,#44326,#44327,#44328,#44329,#44330,
#44331,#44332,#44333,#44334,#44335,#44336,#44337,#44338,#44339,#44340,#44341,
#44342,#44343,#44344,#44345,#44346,#44347,#44348,#44349,#44350,#44351,#44352,
#44353,#44354,#44355,#44356,#44357,#44358,#44359,#44360,#44361,#44362,#44363,
#44364,#44365,#44366,#44367,#44368,#44369,#44370,#44371,#44372,#44373,#44374,
#44375,#44376,#44377,#44378,#44379,#44380,#44381,#44382,#44383,#44384,#44385,
#44386,#44387,#44388,#44389,#44390,#44391,#44392,#44393,#44394,#44395,#44396,
#44397,#44398),.UNSPECIFIED.,.F.,.F.,(4,3,3,3,3,3,3,3,3,3,3,3,3,3,3,3,3,
3,3,3,3,3,3,3,3,3,3,3,3,3,3,3,3,3,3,3,3,3,3,3,3,3,3,3,3,3,3,3,3,3,3,3,3,
3,3,3,3,4),(153.938040025901,153.942316928061,154.027549851531,154.112704812757,
154.197709749479,154.282608041571,154.367314587896,154.441088118724,154.517647083411,
154.594200650291,154.670763415869,154.747381948337,154.824031716832,154.900764830322,
154.939859309386,155.019411173885,155.098902909336,155.178346768052,155.257754964957,
155.337139686496,155.416525722481,155.495914503768,155.575317102384,155.654744598016,
155.734243321155,155.813780466551,155.893406000015,155.937401690711,156.015069170935,
156.092650626004,156.170159976941,156.247600848065,156.325002043364,156.402377355331,
156.436172881374,156.519664327034,156.603311971779,156.687197194643,156.771195973045,
156.855380228954,156.934944072036,157.012453204877,157.089880480553,157.167241515774,
157.244551879768,157.32182710495,157.399095609067,157.476363343681,157.553644345037,
157.630952654207,157.708348766293,157.785790527651,157.863351715391,157.932486453361,
158.008554031517,158.084538123659,158.160435777525,158.175614821639),
 .UNSPECIFIED.);
#3303=B_SPLINE_CURVE_WITH_KNOTS('',3,(#44399,#44400,#44401,#44402,#44403,
#44404,#44405,#44406,#44407,#44408,#44409,#44410,#44411,#44412,#44413,#44414,
#44415,#44416,#44417,#44418,#44419,#44420,#44421,#44422,#44423,#44424,#44425,
#44426,#44427,#44428,#44429,#44430,#44431,#44432,#44433,#44434,#44435,#44436,
#44437,#44438,#44439,#44440,#44441,#44442,#44443,#44444,#44445,#44446,#44447,
#44448,#44449,#44450,#44451,#44452,#44453,#44454,#44455,#44456,#44457,#44458,
#44459,#44460,#44461,#44462,#44463,#44464,#44465,#44466,#44467,#44468,#44469,
#44470,#44471,#44472,#44473,#44474,#44475,#44476,#44477,#44478,#44479,#44480),
 .UNSPECIFIED.,.F.,.F.,(4,3,3,3,3,3,3,3,3,3,3,3,3,3,3,3,3,3,3,3,3,3,3,3,
3,3,3,4),(151.890705689046,151.947232165412,152.025776782351,152.104228824521,
152.182602785103,152.260913101942,152.339174167315,152.417403460582,152.495616257327,
152.573825543454,152.652044300392,152.730317979505,152.808620201271,152.887005657847,
152.944774546736,153.024423567002,153.104002458673,153.18352210138,153.262985012885,
153.342413863709,153.421818263192,153.443545737399,153.524692192321,153.605886223705,
153.688924674217,153.770267683524,153.854153854638,153.938040025753),
 .UNSPECIFIED.);
#3304=B_SPLINE_CURVE_WITH_KNOTS('',3,(#44482,#44483,#44484,#44485,#44486,
#44487,#44488,#44489,#44490,#44491,#44492,#44493,#44494,#44495,#44496,#44497,
#44498,#44499,#44500,#44501,#44502,#44503,#44504,#44505,#44506,#44507,#44508,
#44509,#44510,#44511,#44512,#44513,#44514,#44515,#44516,#44517,#44518,#44519,
#44520,#44521,#44522,#44523,#44524,#44525,#44526,#44527,#44528,#44529,#44530,
#44531,#44532,#44533,#44534,#44535,#44536,#44537,#44538,#44539,#44540,#44541,
#44542,#44543,#44544,#44545,#44546,#44547,#44548,#44549,#44550,#44551,#44552,
#44553,#44554,#44555,#44556,#44557,#44558,#44559,#44560,#44561,#44562,#44563),
 .UNSPECIFIED.,.F.,.F.,(4,3,3,3,3,3,3,3,3,3,3,3,3,3,3,3,3,3,3,3,3,3,3,3,
3,3,3,4),(151.891250266881,151.970672148343,152.050164692382,152.129693712078,
152.20931457057,152.268508614629,152.346176094853,152.423757549922,152.50126690086,
152.578707771984,152.656108967283,152.73348427925,152.767279805291,152.850771250951,
152.934418895696,153.01830411856,153.102302896962,153.186487152871,153.266050995954,
153.342440609636,153.418723562481,153.494945030612,153.571119933994,153.647263158056,
153.723404093323,153.799541433539,153.875718072013,153.938040025901),
 .UNSPECIFIED.);
#3305=B_SPLINE_CURVE_WITH_KNOTS('',3,(#44564,#44565,#44566,#44567,#44568,
#44569,#44570,#44571,#44572,#44573,#44574,#44575,#44576,#44577,#44578,#44579,
#44580,#44581,#44582,#44583,#44584,#44585,#44586,#44587,#44588,#44589,#44590,
#44591,#44592,#44593,#44594,#44595,#44596,#44597,#44598,#44599,#44600,#44601,
#44602,#44603,#44604,#44605,#44606,#44607,#44608,#44609,#44610,#44611,#44612,
#44613,#44614,#44615,#44616,#44617,#44618,#44619,#44620,#44621,#44622,#44623,
#44624,#44625,#44626,#44627,#44628,#44629,#44630,#44631,#44632,#44633,#44634,
#44635,#44636,#44637,#44638,#44639,#44640,#44641,#44642,#44643,#44644,#44645,
#44646,#44647,#44648,#44649,#44650,#44651,#44652,#44653,#44654,#44655,#44656,
#44657,#44658,#44659,#44660,#44661,#44662,#44663,#44664,#44665,#44666,#44667,
#44668,#44669,#44670,#44671,#44672,#44673,#44674,#44675,#44676,#44677,#44678,
#44679,#44680,#44681,#44682,#44683,#44684,#44685,#44686,#44687,#44688,#44689,
#44690,#44691,#44692,#44693,#44694,#44695,#44696,#44697,#44698,#44699,#44700,
#44701,#44702,#44703,#44704,#44705,#44706,#44707,#44708,#44709,#44710,#44711,
#44712,#44713,#44714,#44715,#44716,#44717,#44718,#44719,#44720,#44721,#44722,
#44723,#44724,#44725,#44726,#44727,#44728,#44729),.UNSPECIFIED.,.F.,.F.,
(4,3,3,3,3,3,3,3,3,3,3,3,3,3,3,3,3,3,3,3,3,3,3,3,3,3,3,3,3,3,3,3,3,3,3,
3,3,3,3,3,3,3,3,3,3,3,3,3,3,3,3,3,3,3,3,4),(153.93804002601,154.033124962491,
154.129221750043,154.22638602197,154.263593377279,154.339659536736,154.41563103777,
154.491524657567,154.567357093854,154.643144983438,154.720393830334,154.796157628985,
154.871929535049,154.94772455252,155.026077354041,155.102005892743,155.181570825674,
155.261135758604,155.339680375543,155.418132417713,155.496506378295,155.574816695134,
155.653077760507,155.731307053774,155.809519850519,155.887729136647,155.965947893585,
156.044221572697,156.122523794464,156.200909251039,156.258678139929,156.338327160195,
156.417906051866,156.497425694573,156.576888606078,156.656317456902,156.735721856385,
156.757449330591,156.838681383681,156.91996210202,157.004026706828,157.085458841684,
157.170839681469,157.256220521253,157.341453444723,157.426608405949,157.511613342672,
157.596511634764,157.68121818109,157.754991711916,157.831547530587,157.908096639881,
157.984677176914,158.061275312524,158.137935144021,158.174202348312),
 .UNSPECIFIED.);
#3306=B_SPLINE_CURVE_WITH_KNOTS('',3,(#44735,#44736,#44737,#44738,#44739,
#44740,#44741,#44742,#44743,#44744,#44745,#44746,#44747,#44748,#44749,#44750,
#44751,#44752,#44753,#44754,#44755,#44756,#44757,#44758,#44759,#44760,#44761,
#44762,#44763,#44764,#44765,#44766,#44767,#44768,#44769,#44770,#44771,#44772,
#44773,#44774,#44775,#44776,#44777,#44778,#44779,#44780,#44781,#44782,#44783,
#44784,#44785,#44786,#44787,#44788,#44789,#44790,#44791,#44792,#44793,#44794,
#44795,#44796,#44797,#44798,#44799,#44800,#44801,#44802,#44803,#44804,#44805,
#44806,#44807,#44808,#44809,#44810,#44811,#44812,#44813,#44814,#44815,#44816,
#44817,#44818,#44819,#44820,#44821,#44822,#44823,#44824,#44825,#44826,#44827,
#44828,#44829,#44830,#44831,#44832,#44833,#44834,#44835,#44836,#44837,#44838,
#44839,#44840,#44841,#44842,#44843,#44844,#44845,#44846,#44847,#44848,#44849,
#44850,#44851,#44852,#44853,#44854,#44855,#44856,#44857,#44858,#44859,#44860,
#44861,#44862,#44863,#44864,#44865,#44866,#44867,#44868,#44869,#44870,#44871,
#44872,#44873,#44874,#44875,#44876,#44877,#44878,#44879,#44880,#44881,#44882,
#44883,#44884,#44885,#44886,#44887,#44888,#44889,#44890,#44891,#44892,#44893,
#44894,#44895,#44896,#44897,#44898,#44899,#44900),.UNSPECIFIED.,.F.,.F.,
(4,3,3,3,3,3,3,3,3,3,3,3,3,3,3,3,3,3,3,3,3,3,3,3,3,3,3,3,3,3,3,3,3,3,3,
3,3,3,3,3,3,3,3,3,3,3,3,3,3,3,3,3,3,3,3,4),(160.22122533321,160.296604869896,
160.371977837822,160.426342406673,160.507574459763,160.588855178101,160.67291978291,
160.754351917766,160.839732757551,160.925113597336,161.010346520806,161.095501482032,
161.180506418755,161.265404710847,161.350111257173,161.423884787998,161.500443752685,
161.576997319564,161.653560085142,161.730178617609,161.806828386104,161.883561499593,
161.92265597866,162.002207843159,162.08169957861,162.161143437326,162.240551634232,
162.319936355771,162.399322391757,162.478711173043,162.55811377166,162.637541267291,
162.717039990431,162.796577135827,162.876202669291,162.920198359985,162.997865840209,
163.075447295279,163.152956646216,163.23039751734,163.307798712638,163.385174024605,
163.418969550648,163.502460996308,163.586108641053,163.669993863916,163.753992642319,
163.838176898228,163.91774074131,163.995246197943,164.072673295197,164.150036183801,
164.227344815413,164.304620636586,164.381889295796,164.457861495641),
 .UNSPECIFIED.);
#3307=B_SPLINE_CURVE_WITH_KNOTS('',3,(#44901,#44902,#44903,#44904,#44905,
#44906,#44907,#44908,#44909,#44910,#44911,#44912,#44913,#44914,#44915,#44916,
#44917,#44918,#44919,#44920,#44921,#44922,#44923,#44924,#44925,#44926,#44927,
#44928,#44929,#44930,#44931,#44932,#44933,#44934,#44935,#44936,#44937,#44938,
#44939,#44940,#44941,#44942,#44943,#44944,#44945,#44946,#44947,#44948,#44949,
#44950,#44951,#44952,#44953,#44954,#44955,#44956,#44957,#44958,#44959,#44960,
#44961,#44962,#44963,#44964,#44965,#44966,#44967,#44968,#44969,#44970,#44971,
#44972,#44973,#44974,#44975,#44976,#44977,#44978,#44979,#44980,#44981,#44982),
 .UNSPECIFIED.,.F.,.F.,(4,3,3,3,3,3,3,3,3,3,3,3,3,3,3,3,3,3,3,3,3,3,3,3,
3,3,3,4),(158.175614821639,158.251437002153,158.327217963255,158.402986296286,
158.478750450059,158.554525423503,158.630326222735,158.706216476536,158.782152675983,
158.858214181058,158.930028834686,159.008573451625,159.087025493795,159.165399454377,
159.243709771216,159.321970836589,159.400200129856,159.478412926601,159.556622212728,
159.634840969667,159.713114648779,159.791416870546,159.869802327121,159.927571216011,
160.013020842873,160.098346443543,160.183465540732,160.22122533308),
 .UNSPECIFIED.);
#3308=B_SPLINE_CURVE_WITH_KNOTS('',3,(#44984,#44985,#44986,#44987,#44988,
#44989,#44990,#44991,#44992,#44993,#44994,#44995,#44996,#44997,#44998,#44999,
#45000,#45001,#45002,#45003,#45004,#45005,#45006,#45007,#45008,#45009,#45010,
#45011,#45012,#45013,#45014,#45015,#45016,#45017,#45018,#45019,#45020,#45021,
#45022,#45023,#45024,#45025,#45026,#45027,#45028,#45029,#45030,#45031,#45032,
#45033,#45034,#45035,#45036,#45037,#45038,#45039,#45040,#45041,#45042,#45043,
#45044,#45045,#45046,#45047,#45048,#45049,#45050,#45051,#45052,#45053,#45054,
#45055,#45056,#45057,#45058,#45059,#45060,#45061,#45062,#45063,#45064,#45065),
 .UNSPECIFIED.,.F.,.F.,(4,3,3,3,3,3,3,3,3,3,3,3,3,3,3,3,3,3,3,3,3,3,3,3,
3,3,3,4),(158.174202348312,158.253762902578,158.333314767077,158.412806502528,
158.492250361244,158.571658558149,158.651043279688,158.730429315673,158.80981809696,
158.889220695576,158.968648191208,159.048146914347,159.127684059743,159.207309593207,
159.251305283903,159.328972764127,159.406554219196,159.484063570133,159.561504441257,
159.638905636556,159.716280948523,159.750076474566,159.832460025215,159.914969935679,
159.997681173828,160.080494964793,160.163479563051,160.22122533308),
 .UNSPECIFIED.);
#3309=B_SPLINE_CURVE_WITH_KNOTS('',3,(#45066,#45067,#45068,#45069,#45070,
#45071,#45072,#45073,#45074,#45075,#45076,#45077,#45078,#45079,#45080,#45081,
#45082,#45083,#45084,#45085,#45086,#45087,#45088,#45089,#45090,#45091,#45092,
#45093,#45094,#45095,#45096,#45097,#45098,#45099,#45100,#45101,#45102,#45103,
#45104,#45105,#45106,#45107,#45108,#45109,#45110,#45111,#45112,#45113,#45114,
#45115,#45116,#45117,#45118,#45119,#45120,#45121,#45122,#45123,#45124,#45125,
#45126,#45127,#45128,#45129,#45130,#45131,#45132,#45133,#45134,#45135,#45136,
#45137,#45138,#45139,#45140,#45141,#45142,#45143,#45144,#45145,#45146,#45147,
#45148,#45149,#45150,#45151,#45152,#45153,#45154,#45155,#45156,#45157,#45158,
#45159,#45160,#45161,#45162,#45163,#45164,#45165,#45166,#45167,#45168,#45169,
#45170,#45171,#45172,#45173,#45174,#45175,#45176,#45177,#45178,#45179,#45180,
#45181,#45182,#45183,#45184,#45185,#45186,#45187,#45188,#45189,#45190,#45191,
#45192,#45193,#45194,#45195,#45196,#45197,#45198,#45199,#45200,#45201,#45202,
#45203,#45204,#45205,#45206,#45207,#45208,#45209,#45210,#45211,#45212,#45213,
#45214,#45215,#45216,#45217,#45218,#45219,#45220,#45221,#45222,#45223,#45224,
#45225,#45226,#45227,#45228,#45229,#45230,#45231,#45232,#45233,#45234),
 .UNSPECIFIED.,.F.,.F.,(4,3,3,3,3,3,3,3,3,3,3,3,3,3,3,3,3,3,3,3,3,3,3,3,
3,3,3,3,3,3,3,3,3,3,3,3,3,3,3,3,3,3,3,3,3,3,3,3,3,3,3,3,3,3,3,3,4),(160.221225333172,
160.248847665228,160.326356798069,160.403784073745,160.481145108966,160.55845547296,
160.635730698142,160.712999202259,160.790266936873,160.86754793823,160.944856247399,
161.022252359485,161.099694120844,161.177255308583,161.246390046553,161.32245620601,
161.398427707044,161.474321326841,161.550153763129,161.625941652713,161.703190499609,
161.77895429826,161.854726204324,161.930521221795,162.008874023316,162.084802562018,
162.164367494948,162.243932427878,162.322477044816,162.400929086987,162.479303047569,
162.557613364408,162.635874429781,162.714103723048,162.792316519793,162.87052580592,
162.948744562858,163.02701824197,163.105320463736,163.183705920312,163.241474809203,
163.321123829469,163.40070272114,163.480222363847,163.559685275352,163.639114126177,
163.71851852566,163.740245999865,163.821478052954,163.902758771292,163.986823376101,
164.068255510957,164.153636350743,164.239017190528,164.324255888769,164.409394694648,
164.4584365467),.UNSPECIFIED.);
#3310=B_SPLINE_CURVE_WITH_KNOTS('',3,(#45240,#45241,#45242,#45243,#45244,
#45245,#45246,#45247,#45248,#45249,#45250,#45251,#45252,#45253,#45254,#45255,
#45256,#45257,#45258,#45259,#45260,#45261,#45262,#45263,#45264,#45265,#45266,
#45267,#45268,#45269,#45270,#45271,#45272,#45273,#45274,#45275,#45276,#45277,
#45278,#45279,#45280,#45281,#45282,#45283,#45284,#45285,#45286,#45287,#45288,
#45289,#45290,#45291,#45292,#45293,#45294,#45295,#45296,#45297,#45298,#45299,
#45300,#45301,#45302,#45303,#45304,#45305,#45306,#45307,#45308,#45309,#45310,
#45311,#45312,#45313,#45314,#45315,#45316,#45317,#45318,#45319,#45320,#45321,
#45322,#45323,#45324,#45325,#45326,#45327,#45328,#45329,#45330,#45331,#45332,
#45333,#45334,#45335,#45336,#45337,#45338,#45339,#45340,#45341,#45342,#45343,
#45344,#45345,#45346,#45347,#45348,#45349,#45350,#45351,#45352,#45353,#45354,
#45355,#45356,#45357,#45358,#45359,#45360,#45361,#45362,#45363,#45364,#45365,
#45366,#45367,#45368,#45369,#45370,#45371,#45372,#45373,#45374,#45375,#45376,
#45377,#45378,#45379,#45380,#45381,#45382,#45383,#45384,#45385,#45386,#45387,
#45388,#45389,#45390,#45391,#45392,#45393,#45394,#45395,#45396,#45397,#45398,
#45399,#45400,#45401,#45402,#45403,#45404,#45405),.UNSPECIFIED.,.F.,.F.,
(4,3,3,3,3,3,3,3,3,3,3,3,3,3,3,3,3,3,3,3,3,3,3,3,3,3,3,3,3,3,3,3,3,3,3,
3,3,3,3,3,3,3,3,3,3,3,3,3,3,3,3,3,3,3,3,4),(166.504410640395,166.587946906,
166.671715849388,166.755597078121,166.839656736721,166.910367885285,166.990016905551,
167.069595797223,167.14911543993,167.228578351436,167.308007202261,167.387411601744,
167.409139075947,167.490371129036,167.571651847375,167.655716452183,167.737148587039,
167.822529426825,167.90791026661,167.99314319008,168.078298151307,168.16330308803,
168.248201380123,168.33290792645,168.406681457272,168.483240421959,168.559793988838,
168.636356754416,168.712975286884,168.789625055379,168.866358168868,168.905452647935,
168.985004512434,169.064496247885,169.143940106601,169.223348303507,169.302733025045,
169.38211906103,169.461507842317,169.540910440934,169.620337936565,169.699836659705,
169.779373805101,169.858999338565,169.90299502926,169.980662509484,170.058243964553,
170.13575331549,170.213194186614,170.290595381913,170.367970693879,170.401766219922,
170.486484918568,170.570161549865,170.655401282185,170.740641014505),
 .UNSPECIFIED.);
#3311=B_SPLINE_CURVE_WITH_KNOTS('',3,(#45406,#45407,#45408,#45409,#45410,
#45411,#45412,#45413,#45414,#45415,#45416,#45417,#45418,#45419,#45420,#45421,
#45422,#45423,#45424,#45425,#45426,#45427,#45428,#45429,#45430,#45431,#45432,
#45433,#45434,#45435,#45436,#45437,#45438,#45439,#45440,#45441,#45442,#45443,
#45444,#45445,#45446,#45447,#45448,#45449,#45450,#45451,#45452,#45453,#45454,
#45455,#45456,#45457,#45458,#45459,#45460,#45461,#45462,#45463,#45464,#45465,
#45466,#45467,#45468,#45469,#45470,#45471,#45472,#45473,#45474,#45475,#45476,
#45477,#45478,#45479,#45480,#45481,#45482,#45483,#45484,#45485,#45486,#45487),
 .UNSPECIFIED.,.F.,.F.,(4,3,3,3,3,3,3,3,3,3,3,3,3,3,3,3,3,3,3,3,3,3,3,3,
3,3,3,4),(164.457861495641,164.535142158086,164.612449892308,164.689845345729,
164.767286236049,164.844846929011,164.915283122635,164.991349282092,165.067320783126,
165.143214402924,165.219046839211,165.294834728795,165.372083575691,165.447847374342,
165.523619280406,165.599414297878,165.677767099398,165.7536956381,165.83326057103,
165.91282550396,165.994134477169,166.075331973723,166.15642500465,166.237420520553,
166.318294474902,166.399094121635,166.479805234646,166.50441064026),
 .UNSPECIFIED.);
#3312=B_SPLINE_CURVE_WITH_KNOTS('',3,(#45489,#45490,#45491,#45492,#45493,
#45494,#45495,#45496,#45497,#45498,#45499,#45500,#45501,#45502,#45503,#45504,
#45505,#45506,#45507,#45508,#45509,#45510,#45511,#45512,#45513,#45514,#45515,
#45516,#45517,#45518,#45519,#45520,#45521,#45522,#45523,#45524,#45525,#45526,
#45527,#45528,#45529,#45530,#45531,#45532,#45533,#45534,#45535,#45536,#45537,
#45538,#45539,#45540,#45541,#45542,#45543,#45544,#45545,#45546,#45547,#45548,
#45549,#45550,#45551,#45552,#45553,#45554,#45555,#45556,#45557,#45558,#45559,
#45560,#45561,#45562,#45563,#45564,#45565,#45566,#45567,#45568,#45569,#45570,
#45571,#45572,#45573),.UNSPECIFIED.,.F.,.F.,(4,3,3,3,3,3,3,3,3,3,3,3,3,
3,3,3,3,3,3,3,3,3,3,3,3,3,3,3,4),(164.4584365467,164.543381424743,164.62821289491,
164.712864999446,164.73778838119,164.814347345877,164.890900912755,164.967463678333,
165.0440822108,165.120731979295,165.197465092784,165.236559571853,165.316111436352,
165.395603171803,165.475047030519,165.554455227425,165.633839948965,165.71322598495,
165.792614766236,165.872017364853,165.951444860484,166.030943583623,166.110480729019,
166.190106262483,166.234101953177,166.320020536337,166.405719948851,166.491090206055,
166.50441064026),.UNSPECIFIED.);
#3313=B_SPLINE_CURVE_WITH_KNOTS('',3,(#45574,#45575,#45576,#45577,#45578,
#45579,#45580,#45581,#45582,#45583,#45584,#45585,#45586,#45587,#45588,#45589,
#45590,#45591,#45592,#45593,#45594,#45595,#45596,#45597,#45598,#45599,#45600,
#45601,#45602,#45603,#45604,#45605,#45606,#45607,#45608,#45609,#45610,#45611,
#45612,#45613,#45614,#45615,#45616,#45617,#45618,#45619,#45620,#45621,#45622,
#45623,#45624,#45625,#45626,#45627,#45628,#45629,#45630,#45631,#45632,#45633,
#45634,#45635,#45636,#45637,#45638,#45639,#45640,#45641,#45642,#45643,#45644,
#45645,#45646,#45647,#45648,#45649,#45650,#45651,#45652,#45653,#45654,#45655,
#45656,#45657,#45658,#45659,#45660,#45661,#45662,#45663,#45664,#45665,#45666,
#45667,#45668,#45669,#45670,#45671,#45672,#45673,#45674,#45675,#45676,#45677,
#45678,#45679,#45680,#45681,#45682,#45683,#45684,#45685,#45686,#45687,#45688,
#45689,#45690,#45691,#45692,#45693,#45694,#45695,#45696,#45697,#45698,#45699,
#45700,#45701,#45702,#45703,#45704,#45705,#45706,#45707,#45708,#45709,#45710,
#45711,#45712,#45713,#45714,#45715,#45716,#45717,#45718,#45719,#45720,#45721,
#45722,#45723,#45724,#45725,#45726,#45727,#45728,#45729,#45730),
 .UNSPECIFIED.,.F.,.F.,(4,3,3,3,3,3,3,3,3,3,3,3,3,3,3,3,3,3,3,3,3,3,3,3,
3,3,3,3,3,3,3,3,3,3,3,3,3,3,3,3,3,3,3,3,3,3,3,3,3,3,3,3,4),(166.50441064026,
166.58687284636,166.669334704163,166.751796220518,166.834257402276,166.916718256286,
166.999178789398,167.081639008461,167.164098920324,167.246558531836,167.329017849845,
167.411476881198,167.493935632745,167.576394111333,167.658852323808,167.741310277019,
167.823767977812,167.906225433034,167.988682649532,168.074695344818,168.158020143376,
168.240486748968,168.322952510351,168.405417454941,168.487881610149,168.570345003385,
168.652807662057,168.735269613568,168.817730885321,168.900191504714,168.982651499145,
169.065110896009,169.147569722699,169.230028006606,169.312485775119,169.394943055626,
169.479077170817,169.561543169177,169.644007545783,169.726470410278,169.808931872285,
169.891392041404,169.97385102722,170.0563089393,170.141906434223,170.224371171269,
170.306832943655,170.38929218982,170.471749348059,170.554211867142,170.636669538553,
170.719128329746,170.741088898683),.UNSPECIFIED.);
#3314=B_SPLINE_CURVE_WITH_KNOTS('',3,(#45736,#45737,#45738,#45739,#45740,
#45741,#45742,#45743,#45744,#45745,#45746,#45747,#45748,#45749,#45750,#45751,
#45752,#45753,#45754,#45755,#45756,#45757,#45758,#45759,#45760,#45761,#45762,
#45763,#45764,#45765,#45766,#45767,#45768,#45769,#45770,#45771,#45772,#45773,
#45774,#45775,#45776,#45777,#45778,#45779,#45780,#45781,#45782,#45783,#45784,
#45785,#45786,#45787,#45788,#45789,#45790,#45791,#45792,#45793,#45794,#45795,
#45796,#45797,#45798,#45799,#45800,#45801,#45802,#45803,#45804,#45805,#45806,
#45807,#45808,#45809,#45810,#45811,#45812,#45813,#45814,#45815,#45816,#45817,
#45818,#45819,#45820,#45821,#45822,#45823,#45824,#45825,#45826,#45827,#45828,
#45829,#45830,#45831,#45832,#45833,#45834,#45835,#45836,#45837,#45838,#45839,
#45840,#45841,#45842,#45843,#45844,#45845,#45846,#45847,#45848,#45849,#45850,
#45851,#45852,#45853,#45854,#45855,#45856,#45857,#45858,#45859,#45860,#45861,
#45862,#45863,#45864,#45865,#45866,#45867,#45868,#45869,#45870,#45871,#45872,
#45873,#45874,#45875,#45876,#45877,#45878,#45879,#45880,#45881,#45882,#45883,
#45884,#45885,#45886,#45887,#45888,#45889,#45890,#45891,#45892,#45893,#45894,
#45895,#45896,#45897,#45898,#45899,#45900,#45901),.UNSPECIFIED.,.F.,.F.,
(4,3,3,3,3,3,3,3,3,3,3,3,3,3,3,3,3,3,3,3,3,3,3,3,3,3,3,3,3,3,3,3,3,3,3,
3,3,3,3,3,3,3,3,3,3,3,3,3,3,3,3,3,3,3,3,4),(172.787595947439,172.895622173234,
172.974166790173,173.052618832344,173.130992792926,173.209303109765,173.287564175138,
173.365793468405,173.44400626515,173.522215551277,173.600434308216,173.678707987328,
173.757010209094,173.83539566567,173.893164554559,173.972813574825,174.052392466497,
174.131912109204,174.21137502071,174.290803871535,174.370208271018,174.391935745222,
174.473167798311,174.554448516648,174.638513121457,174.719945256312,174.805326096098,
174.890706935884,174.975939859356,175.061094820585,175.14609975731,175.230998049405,
175.315704595733,175.389478126546,175.466037091231,175.542590658109,175.619153423685,
175.695771956151,175.772421724644,175.849154838132,175.888249317209,175.967801181708,
176.04729291716,176.126736775876,176.206144972782,176.285529694321,176.364915730306,
176.444304511593,176.52370711021,176.603134605842,176.682633328982,176.762170474378,
176.841796007843,176.885791698534,176.963453310415,177.024993203619),
 .UNSPECIFIED.);
#3315=B_SPLINE_CURVE_WITH_KNOTS('',3,(#45902,#45903,#45904,#45905,#45906,
#45907,#45908,#45909,#45910,#45911,#45912,#45913,#45914,#45915,#45916,#45917,
#45918,#45919,#45920,#45921,#45922,#45923,#45924,#45925,#45926,#45927,#45928,
#45929,#45930,#45931,#45932,#45933,#45934,#45935,#45936,#45937,#45938,#45939,
#45940,#45941,#45942,#45943,#45944,#45945,#45946,#45947,#45948,#45949,#45950,
#45951,#45952,#45953,#45954,#45955,#45956,#45957,#45958,#45959,#45960,#45961,
#45962,#45963,#45964,#45965,#45966,#45967,#45968,#45969,#45970,#45971,#45972,
#45973,#45974,#45975,#45976,#45977,#45978,#45979,#45980,#45981,#45982,#45983),
 .UNSPECIFIED.,.F.,.F.,(4,3,3,3,3,3,3,3,3,3,3,3,3,3,3,3,3,3,3,3,3,3,3,3,
3,3,3,4),(170.740641014505,170.824827998365,170.900537410584,170.978046543425,
171.055473819101,171.132834854323,171.210145218316,171.287420443499,171.364688947616,
171.44195668223,171.519237683587,171.596545992756,171.673942104842,171.7513838662,
171.828945053939,171.898079791909,171.973228297357,172.048283482188,172.123262586557,
172.198182736578,172.273064321956,172.347925999265,172.422783121255,172.49765103696,
172.572584895655,172.647552314513,172.72262266121,172.787595947362),
 .UNSPECIFIED.);
#3316=B_SPLINE_CURVE_WITH_KNOTS('',3,(#45985,#45986,#45987,#45988,#45989,
#45990,#45991,#45992,#45993,#45994,#45995,#45996,#45997,#45998,#45999,#46000,
#46001,#46002,#46003,#46004,#46005,#46006,#46007,#46008,#46009,#46010,#46011,
#46012,#46013,#46014,#46015,#46016,#46017,#46018,#46019,#46020,#46021,#46022,
#46023,#46024,#46025,#46026,#46027,#46028,#46029,#46030,#46031,#46032,#46033,
#46034,#46035,#46036,#46037,#46038,#46039,#46040,#46041,#46042,#46043,#46044,
#46045,#46046,#46047,#46048,#46049,#46050,#46051,#46052,#46053,#46054,#46055,
#46056,#46057,#46058,#46059,#46060),.UNSPECIFIED.,.F.,.F.,(4,3,3,3,3,3,
3,3,3,3,3,3,3,3,3,3,3,3,3,3,3,3,3,3,3,4),(170.741088898683,170.823550502413,
170.906011440265,170.988471739637,171.070931427926,171.153390532524,171.235849080824,
171.318307100217,171.40076461809,171.487441576174,171.569908361715,171.652373474783,
171.734837025031,171.81729912209,171.899759875572,171.982219395068,172.064677790153,
172.147135170387,172.229601556073,172.312064757581,172.394525213431,172.476983361985,
172.559448965739,172.641908844127,172.724372955379,172.787595947439),
 .UNSPECIFIED.);
#3317=B_SPLINE_CURVE_WITH_KNOTS('',3,(#46061,#46062,#46063,#46064,#46065,
#46066,#46067,#46068,#46069,#46070,#46071,#46072,#46073,#46074,#46075,#46076,
#46077,#46078,#46079,#46080,#46081,#46082,#46083,#46084,#46085,#46086,#46087,
#46088,#46089,#46090,#46091,#46092,#46093,#46094,#46095,#46096,#46097,#46098,
#46099,#46100,#46101,#46102,#46103,#46104,#46105,#46106,#46107,#46108,#46109,
#46110,#46111,#46112,#46113,#46114,#46115,#46116,#46117,#46118,#46119,#46120,
#46121,#46122,#46123,#46124,#46125,#46126,#46127,#46128,#46129,#46130,#46131,
#46132,#46133,#46134,#46135,#46136,#46137,#46138,#46139,#46140,#46141,#46142,
#46143,#46144,#46145,#46146,#46147,#46148,#46149,#46150,#46151,#46152,#46153,
#46154,#46155,#46156,#46157,#46158,#46159,#46160,#46161,#46162,#46163,#46164,
#46165,#46166,#46167,#46168,#46169,#46170,#46171,#46172,#46173,#46174,#46175,
#46176,#46177,#46178,#46179,#46180,#46181,#46182,#46183,#46184,#46185,#46186,
#46187,#46188,#46189,#46190,#46191,#46192,#46193,#46194,#46195,#46196,#46197,
#46198,#46199,#46200,#46201,#46202,#46203,#46204,#46205,#46206,#46207,#46208,
#46209,#46210,#46211,#46212,#46213,#46214,#46215,#46216,#46217,#46218,#46219,
#46220,#46221,#46222,#46223,#46224,#46225,#46226),.UNSPECIFIED.,.F.,.F.,
(4,3,3,3,3,3,3,3,3,3,3,3,3,3,3,3,3,3,3,3,3,3,3,3,3,3,3,3,3,3,3,3,3,3,3,
3,3,3,3,3,3,3,3,3,3,3,3,3,3,3,3,3,3,3,3,4),(172.787595947439,172.874185025021,
172.961173772969,173.048340074132,173.135733550733,173.216898622452,173.294566102676,
173.372147557746,173.449656908683,173.527097779807,173.604498975107,173.681874287074,
173.715669813114,173.799161258773,173.882808903518,173.966694126382,174.050692904784,
174.134877160692,174.214441003777,174.291950136618,174.369377412294,174.446738447516,
174.524048811509,174.601324036692,174.678592540809,174.755860275423,174.833141276779,
174.910449585949,174.987845698034,175.065287459393,175.142848647132,175.211983385101,
175.288049544558,175.364021045592,175.439914665389,175.515747101676,175.59153499126,
175.668783838156,175.744547636807,175.820319542871,175.896114560342,175.974467361863,
176.050395900565,176.129960833495,176.209525766426,176.288081254305,176.366542327576,
176.448727218835,176.52702763694,176.605283604676,176.683508141454,176.761714245822,
176.839929050713,176.91814867986,176.996404746631,177.024021457654),
 .UNSPECIFIED.);
#3318=B_SPLINE_CURVE_WITH_KNOTS('',3,(#46232,#46233,#46234,#46235,#46236,
#46237,#46238,#46239,#46240,#46241,#46242,#46243,#46244,#46245,#46246,#46247,
#46248,#46249,#46250,#46251,#46252,#46253,#46254,#46255,#46256,#46257,#46258,
#46259,#46260,#46261,#46262,#46263,#46264,#46265,#46266,#46267,#46268,#46269,
#46270,#46271,#46272,#46273,#46274,#46275,#46276,#46277,#46278,#46279,#46280,
#46281,#46282,#46283,#46284,#46285,#46286,#46287,#46288,#46289,#46290,#46291,
#46292,#46293,#46294,#46295,#46296,#46297,#46298,#46299,#46300,#46301,#46302,
#46303,#46304,#46305,#46306,#46307,#46308,#46309,#46310,#46311,#46312,#46313,
#46314,#46315,#46316,#46317,#46318,#46319,#46320,#46321,#46322,#46323,#46324,
#46325,#46326,#46327,#46328,#46329,#46330,#46331,#46332,#46333,#46334,#46335,
#46336,#46337,#46338,#46339,#46340,#46341,#46342,#46343,#46344,#46345,#46346,
#46347,#46348,#46349,#46350,#46351,#46352,#46353,#46354,#46355,#46356,#46357,
#46358,#46359,#46360,#46361,#46362,#46363,#46364,#46365,#46366,#46367,#46368,
#46369,#46370,#46371,#46372,#46373,#46374,#46375,#46376,#46377,#46378,#46379,
#46380,#46381,#46382,#46383,#46384,#46385,#46386,#46387,#46388,#46389,#46390,
#46391,#46392,#46393,#46394,#46395,#46396,#46397,#46398,#46399,#46400),
 .UNSPECIFIED.,.F.,.F.,(4,3,3,3,3,3,3,3,3,3,3,3,3,3,3,3,3,3,3,3,3,3,3,3,
3,3,3,3,3,3,3,3,3,3,3,3,3,3,3,3,3,3,3,3,3,3,3,3,3,3,3,3,3,3,3,3,4),(179.070781254718,
179.145516621503,179.220188243222,179.294813277258,179.369418651496,179.444015720104,
179.518619908358,179.593246653133,179.667957077619,179.7427113662,179.817583406695,
179.878418842509,179.956963459425,180.035415501573,180.113789462133,180.192099778949,
180.2703608443,180.348590137545,180.426802934267,180.505012220373,180.583230977289,
180.66150465638,180.739806878126,180.818192334681,180.875961223833,180.955610244282,
181.035189136134,181.114708779021,181.194171690702,181.273600541701,181.353004941354,
181.374732414496,181.455964467135,181.537245185018,181.621309790053,181.702741924448,
181.788122764803,181.873503605158,181.958736529484,182.043891491562,182.128896429114,
182.213794722016,182.298501269109,182.372274795821,182.44883376006,182.525387326491,
182.601950091619,182.678568623636,182.75521839168,182.83195150472,182.871045986483,
182.95060181219,183.030098619949,183.109540080683,183.188948127209,183.268334831295,
183.307329714257),.UNSPECIFIED.);
#3319=B_SPLINE_CURVE_WITH_KNOTS('',3,(#46401,#46402,#46403,#46404,#46405,
#46406,#46407,#46408,#46409,#46410,#46411,#46412,#46413,#46414,#46415,#46416,
#46417,#46418,#46419,#46420,#46421,#46422,#46423,#46424,#46425,#46426,#46427,
#46428,#46429,#46430,#46431,#46432,#46433,#46434,#46435,#46436,#46437,#46438,
#46439,#46440,#46441,#46442,#46443,#46444,#46445,#46446,#46447,#46448,#46449,
#46450,#46451,#46452,#46453,#46454,#46455,#46456,#46457,#46458,#46459,#46460,
#46461,#46462,#46463,#46464,#46465,#46466,#46467,#46468,#46469,#46470,#46471,
#46472,#46473,#46474,#46475,#46476,#46477,#46478,#46479),.UNSPECIFIED.,
 .F.,.F.,(4,3,3,3,3,3,3,3,3,3,3,3,3,3,3,3,3,3,3,3,3,3,3,3,3,3,4),(177.024993203619,
177.102516334983,177.179966967019,177.257375356394,177.334755995492,177.384562889196,
177.468054334845,177.551701979579,177.635587202431,177.719585980822,177.803770236719,
177.883334079859,177.960843212706,178.038270488389,178.115631523618,178.192941887618,
178.270217112807,178.347485616931,178.424753351552,178.502034352915,178.579342662092,
178.656738774184,178.734180535549,178.811741723295,178.880876461184,178.991529382284,
179.070781254619),.UNSPECIFIED.);
#3320=B_SPLINE_CURVE_WITH_KNOTS('',3,(#46481,#46482,#46483,#46484,#46485,
#46486,#46487,#46488,#46489,#46490,#46491,#46492,#46493,#46494,#46495,#46496,
#46497,#46498,#46499,#46500,#46501,#46502,#46503,#46504,#46505,#46506,#46507,
#46508,#46509,#46510,#46511,#46512,#46513,#46514,#46515,#46516,#46517,#46518,
#46519,#46520,#46521,#46522,#46523,#46524,#46525,#46526,#46527,#46528,#46529,
#46530,#46531,#46532,#46533,#46534,#46535,#46536,#46537,#46538,#46539,#46540,
#46541,#46542,#46543,#46544,#46545,#46546,#46547,#46548,#46549,#46550,#46551,
#46552,#46553,#46554,#46555,#46556,#46557,#46558,#46559,#46560,#46561,#46562),
 .UNSPECIFIED.,.F.,.F.,(4,3,3,3,3,3,3,3,3,3,3,3,3,3,3,3,3,3,3,3,3,3,3,3,
3,3,3,4),(177.024021457654,177.102338427649,177.180732646031,177.207068147751,
177.286717168017,177.366296059689,177.445815702396,177.525278613901,177.604707464726,
177.684111864209,177.705839338414,177.787071391503,177.868352109841,177.95241671465,
178.033848849505,178.119229689291,178.204610529076,178.289843452548,178.374998413777,
178.460003350502,178.544901642596,178.629608188924,178.703381719739,178.777449137334,
178.851524089071,178.925599451328,178.999727625761,179.070177698457),
 .UNSPECIFIED.);
#3321=B_SPLINE_CURVE_WITH_KNOTS('',3,(#46563,#46564,#46565,#46566,#46567,
#46568,#46569,#46570,#46571,#46572,#46573,#46574,#46575,#46576,#46577,#46578,
#46579,#46580,#46581,#46582,#46583,#46584,#46585,#46586,#46587,#46588,#46589,
#46590,#46591,#46592,#46593,#46594,#46595,#46596,#46597,#46598,#46599,#46600,
#46601,#46602,#46603,#46604,#46605,#46606,#46607,#46608,#46609,#46610,#46611,
#46612,#46613,#46614,#46615,#46616,#46617,#46618,#46619,#46620,#46621,#46622,
#46623,#46624,#46625,#46626,#46627,#46628,#46629,#46630,#46631,#46632,#46633,
#46634,#46635,#46636,#46637,#46638,#46639,#46640,#46641,#46642,#46643,#46644,
#46645,#46646,#46647,#46648,#46649,#46650,#46651,#46652,#46653,#46654,#46655,
#46656,#46657,#46658,#46659,#46660,#46661,#46662,#46663,#46664,#46665,#46666,
#46667,#46668,#46669,#46670,#46671,#46672,#46673,#46674,#46675,#46676,#46677,
#46678,#46679,#46680,#46681,#46682,#46683,#46684,#46685,#46686,#46687,#46688,
#46689,#46690,#46691,#46692,#46693,#46694,#46695,#46696,#46697,#46698,#46699,
#46700,#46701,#46702,#46703,#46704,#46705,#46706,#46707,#46708,#46709,#46710,
#46711,#46712,#46713,#46714,#46715,#46716,#46717,#46718,#46719),
 .UNSPECIFIED.,.F.,.F.,(4,3,3,3,3,3,3,3,3,3,3,3,3,3,3,3,3,3,3,3,3,3,3,3,
3,3,3,3,3,3,3,3,3,3,3,3,3,3,3,3,3,3,3,3,3,3,3,3,3,3,3,3,4),(179.070781254619,
179.153243460719,179.235705318522,179.318166834877,179.400628016635,179.483088870645,
179.565549403757,179.64800962282,179.730469534683,179.812929146195,179.895388464203,
179.977847495557,180.060306247104,180.142764725692,180.225222938167,180.307680891378,
180.390138592171,180.472596047393,180.55505326389,180.641065959176,180.724390757735,
180.806857363326,180.88932312471,180.971788069299,181.054252224508,181.136715617744,
181.219178276416,181.301640227927,181.384101499679,181.466562119072,181.549022113504,
181.631481510368,181.713940337058,181.796398620965,181.878856389478,181.961313669984,
182.045447785175,182.127913783535,182.210378160142,182.292841024637,182.375302486643,
182.457762655763,182.540221641579,182.622679553659,182.708277048582,182.790741785628,
182.873203558014,182.955662804179,183.038119962418,183.1205824815,183.203040152911,
183.285498944104,183.307459513042),.UNSPECIFIED.);
#3322=B_SPLINE_CURVE_WITH_KNOTS('',3,(#46725,#46726,#46727,#46728,#46729,
#46730,#46731,#46732,#46733,#46734,#46735,#46736,#46737,#46738,#46739,#46740,
#46741,#46742,#46743,#46744,#46745,#46746,#46747,#46748,#46749,#46750,#46751,
#46752,#46753,#46754,#46755,#46756,#46757,#46758,#46759,#46760,#46761,#46762,
#46763,#46764,#46765,#46766,#46767,#46768,#46769,#46770,#46771,#46772,#46773,
#46774,#46775,#46776,#46777,#46778,#46779,#46780,#46781,#46782,#46783,#46784,
#46785,#46786,#46787,#46788,#46789,#46790,#46791,#46792,#46793,#46794,#46795,
#46796,#46797,#46798,#46799,#46800,#46801,#46802,#46803,#46804,#46805,#46806,
#46807,#46808,#46809,#46810,#46811,#46812,#46813,#46814,#46815,#46816,#46817,
#46818,#46819,#46820,#46821,#46822,#46823,#46824,#46825,#46826,#46827,#46828,
#46829,#46830,#46831,#46832,#46833,#46834,#46835,#46836,#46837,#46838,#46839,
#46840,#46841,#46842,#46843,#46844,#46845,#46846,#46847,#46848,#46849,#46850,
#46851,#46852,#46853,#46854,#46855,#46856,#46857,#46858,#46859,#46860,#46861,
#46862,#46863,#46864,#46865,#46866,#46867,#46868,#46869,#46870,#46871,#46872,
#46873,#46874,#46875,#46876,#46877,#46878,#46879,#46880,#46881,#46882,#46883,
#46884,#46885,#46886,#46887,#46888,#46889,#46890),.UNSPECIFIED.,.F.,.F.,
(4,3,3,3,3,3,3,3,3,3,3,3,3,3,3,3,3,3,3,3,3,3,3,3,3,3,3,3,3,3,3,3,3,3,3,
3,3,3,3,3,3,3,3,3,3,3,3,3,3,3,3,3,3,3,3,4),(185.353966561872,185.436388795968,
185.518962685979,185.605140297099,185.688092821579,185.771168370801,185.854416769343,
185.863673130458,185.939739291683,186.015710794493,186.091604416073,186.16743685415,
186.24322474553,186.320473591312,186.396237391765,186.472009299633,186.547804318909,
186.626157117128,186.702085657623,186.781650584703,186.861215511783,186.939760116234,
187.018212145929,187.096586094066,187.174896398507,187.253157451547,187.331386732632,
187.409599517296,187.487808791459,187.566027536567,187.644301204122,187.722603414474,
187.800988859965,187.858757893108,187.938406980073,188.017985937837,188.097505645893,
188.17696862134,188.256397535211,188.3358019962,188.35752908377,188.438761019251,
188.520041618791,188.604106282702,188.685538298093,188.770919286263,188.856300274433,
188.941533289162,189.026688340278,189.111693363037,189.196591738378,189.281298362221,
189.355071465095,189.431629262761,189.510976499295,189.590323735828),
 .UNSPECIFIED.);
#3323=B_SPLINE_CURVE_WITH_KNOTS('',3,(#46891,#46892,#46893,#46894,#46895,
#46896,#46897,#46898,#46899,#46900,#46901,#46902,#46903,#46904,#46905,#46906,
#46907,#46908,#46909,#46910,#46911,#46912,#46913,#46914,#46915,#46916,#46917,
#46918,#46919,#46920,#46921,#46922,#46923,#46924,#46925,#46926,#46927,#46928,
#46929,#46930,#46931,#46932,#46933,#46934,#46935,#46936,#46937,#46938,#46939,
#46940,#46941,#46942,#46943,#46944,#46945,#46946,#46947,#46948,#46949,#46950,
#46951,#46952,#46953,#46954,#46955,#46956,#46957,#46958,#46959,#46960,#46961,
#46962,#46963,#46964,#46965,#46966,#46967,#46968,#46969),.UNSPECIFIED.,
 .F.,.F.,(4,3,3,3,3,3,3,3,3,3,3,3,3,3,3,3,3,3,3,3,3,3,3,3,3,3,4),(183.307329714257,
183.386715715262,183.466109900837,183.545523345885,183.626289601365,183.705806557614,
183.787197462711,183.868588367808,183.946255851014,184.023837309042,184.101346662911,
184.178787536922,184.256188735078,184.333564049854,184.367359558471,184.450850997495,
184.534498635367,184.618383851108,184.702382622282,184.786566870907,184.866130749133,
184.945985690768,185.025732308557,185.107790871867,185.187323979618,185.270645270708,
185.353966561798),.UNSPECIFIED.);
#3324=B_SPLINE_CURVE_WITH_KNOTS('',3,(#46971,#46972,#46973,#46974,#46975,
#46976,#46977,#46978,#46979,#46980,#46981,#46982,#46983,#46984,#46985,#46986,
#46987,#46988,#46989,#46990,#46991,#46992,#46993,#46994,#46995,#46996,#46997,
#46998,#46999,#47000,#47001,#47002,#47003,#47004,#47005,#47006,#47007,#47008,
#47009,#47010,#47011,#47012,#47013,#47014,#47015,#47016,#47017,#47018,#47019,
#47020,#47021,#47022,#47023,#47024,#47025,#47026,#47027,#47028,#47029,#47030,
#47031,#47032,#47033,#47034,#47035,#47036,#47037,#47038,#47039,#47040,#47041,
#47042,#47043,#47044,#47045,#47046),.UNSPECIFIED.,.F.,.F.,(4,3,3,3,3,3,
3,3,3,3,3,3,3,3,3,3,3,3,3,3,3,3,3,3,3,4),(183.307459513042,183.389921116772,
183.472382054624,183.554842353996,183.637302042285,183.719761146883,183.802219695183,
183.884677714576,183.967135232449,184.053812190533,184.136278976074,184.218744089142,
184.30120763939,184.383669736449,184.466130489931,184.548590009427,184.631048404512,
184.713505784746,184.795972170432,184.87843537194,184.96089582779,185.043353976344,
185.125819580098,185.208279458486,185.290743569738,185.353966561798),
 .UNSPECIFIED.);
#3325=B_SPLINE_CURVE_WITH_KNOTS('',3,(#47047,#47048,#47049,#47050,#47051,
#47052,#47053,#47054,#47055,#47056,#47057,#47058,#47059,#47060,#47061,#47062,
#47063,#47064,#47065,#47066,#47067,#47068,#47069,#47070,#47071,#47072,#47073,
#47074,#47075,#47076,#47077,#47078,#47079,#47080,#47081,#47082,#47083,#47084,
#47085,#47086,#47087,#47088,#47089,#47090,#47091,#47092,#47093,#47094,#47095,
#47096,#47097,#47098,#47099,#47100,#47101,#47102,#47103,#47104,#47105,#47106,
#47107,#47108,#47109,#47110,#47111,#47112,#47113,#47114,#47115,#47116,#47117,
#47118,#47119,#47120,#47121,#47122,#47123,#47124,#47125,#47126,#47127,#47128,
#47129,#47130,#47131,#47132,#47133,#47134,#47135,#47136,#47137,#47138,#47139,
#47140,#47141,#47142,#47143,#47144,#47145,#47146,#47147,#47148,#47149,#47150,
#47151,#47152,#47153,#47154,#47155,#47156,#47157,#47158,#47159,#47160,#47161,
#47162,#47163,#47164,#47165,#47166,#47167,#47168,#47169,#47170,#47171,#47172,
#47173,#47174,#47175,#47176,#47177,#47178,#47179,#47180,#47181,#47182,#47183,
#47184,#47185,#47186,#47187,#47188,#47189,#47190,#47191,#47192,#47193,#47194,
#47195,#47196,#47197,#47198,#47199,#47200,#47201,#47202,#47203),
 .UNSPECIFIED.,.F.,.F.,(4,3,3,3,3,3,3,3,3,3,3,3,3,3,3,3,3,3,3,3,3,3,3,3,
3,3,3,3,3,3,3,3,3,3,3,3,3,3,3,3,3,3,3,3,3,3,3,3,3,3,3,3,4),(185.353966561918,
185.436428768018,185.518890625821,185.601352142176,185.683813323934,185.766274177944,
185.848734711056,185.931194930119,186.013654841982,186.096114453494,186.178573771503,
186.261032802857,186.343491554403,186.425950032991,186.508408245466,186.590866198677,
186.67332389947,186.755781354692,186.838238571189,186.924251266472,187.007576065026,
187.090042670618,187.172508432001,187.254973376591,187.337437531799,187.419900925036,
187.502363583708,187.584825535219,187.667286806971,187.749747426364,187.832207420795,
187.91466681766,187.99712564435,188.079583928257,188.16204169677,188.244498977276,
188.32863309246,188.41109909082,188.493563467426,188.576026331922,188.658487793928,
188.740947963047,188.823406948864,188.905864860944,188.991462355854,189.0739270929,
189.156388865286,189.238848111451,189.32130526969,189.403767788772,189.486225460183,
189.568684251376,189.590644820222),.UNSPECIFIED.);
#3326=B_SPLINE_CURVE_WITH_KNOTS('',3,(#47209,#47210,#47211,#47212,#47213,
#47214,#47215,#47216,#47217,#47218,#47219,#47220,#47221,#47222,#47223,#47224,
#47225,#47226,#47227,#47228,#47229,#47230,#47231,#47232,#47233,#47234,#47235,
#47236,#47237,#47238,#47239,#47240,#47241,#47242,#47243,#47244,#47245,#47246,
#47247,#47248,#47249,#47250,#47251,#47252,#47253,#47254,#47255,#47256,#47257,
#47258,#47259,#47260,#47261,#47262,#47263,#47264,#47265,#47266,#47267,#47268,
#47269,#47270,#47271,#47272,#47273,#47274,#47275,#47276,#47277,#47278,#47279,
#47280,#47281,#47282,#47283,#47284,#47285,#47286,#47287,#47288,#47289,#47290,
#47291,#47292,#47293,#47294,#47295,#47296,#47297,#47298,#47299,#47300,#47301,
#47302,#47303,#47304,#47305,#47306,#47307,#47308,#47309,#47310,#47311,#47312,
#47313,#47314,#47315,#47316,#47317,#47318,#47319,#47320,#47321,#47322,#47323,
#47324,#47325,#47326,#47327,#47328,#47329,#47330,#47331,#47332,#47333,#47334,
#47335,#47336,#47337,#47338,#47339,#47340,#47341,#47342,#47343,#47344,#47345,
#47346,#47347,#47348,#47349,#47350,#47351,#47352,#47353,#47354,#47355,#47356,
#47357,#47358,#47359,#47360,#47361,#47362,#47363,#47364,#47365,#47366,#47367,
#47368,#47369,#47370,#47371,#47372,#47373,#47374),.UNSPECIFIED.,.F.,.F.,
(4,3,3,3,3,3,3,3,3,3,3,3,3,3,3,3,3,3,3,3,3,3,3,3,3,3,3,3,3,3,3,3,3,3,3,
3,3,3,3,3,3,3,3,3,3,3,3,3,3,3,3,3,3,3,3,4),(191.637151868978,191.743039643692,
191.848927418407,191.92643671887,192.003864162199,192.081225364945,192.158535896175,
192.235811288146,192.31307995782,192.390347857223,192.467629022458,192.544937494451,
192.622333766832,192.699775687347,192.777337030803,192.846469799732,192.922537679677,
192.998510902649,193.074406244851,193.15024040308,193.226030013248,193.303277784224,
193.379043294017,193.454816906719,193.53061362553,193.608963264412,193.68489347934,
193.764452830198,193.844012181057,193.922552739501,194.001000738238,194.079370676038,
194.15767699636,194.235934097122,194.31415949021,194.392368429138,194.470573904931,
194.548788904164,194.627058928218,194.705357549035,194.783739523544,194.841554562382,
194.921213750279,195.000802647214,195.080332112034,195.159804529953,195.239242691842,
195.318656084451,195.340325753044,195.421563458961,195.502850079269,195.586911795378,
195.668350324312,195.75372363401,195.839096943707,195.873887289425),
 .UNSPECIFIED.);
#3327=B_SPLINE_CURVE_WITH_KNOTS('',3,(#47375,#47376,#47377,#47378,#47379,
#47380,#47381,#47382,#47383,#47384,#47385,#47386,#47387,#47388,#47389,#47390,
#47391,#47392,#47393,#47394,#47395,#47396,#47397,#47398,#47399,#47400,#47401,
#47402,#47403,#47404,#47405,#47406,#47407,#47408,#47409,#47410,#47411,#47412,
#47413,#47414,#47415,#47416,#47417,#47418,#47419,#47420,#47421,#47422,#47423,
#47424,#47425,#47426,#47427,#47428,#47429,#47430,#47431,#47432,#47433,#47434,
#47435,#47436,#47437,#47438,#47439,#47440,#47441,#47442,#47443,#47444,#47445,
#47446,#47447,#47448,#47449,#47450,#47451,#47452,#47453,#47454,#47455,#47456,
#47457,#47458,#47459),.UNSPECIFIED.,.F.,.F.,(4,3,3,3,3,3,3,3,3,3,3,3,3,
3,3,3,3,3,3,3,3,3,3,3,3,3,3,3,4),(189.590323735828,189.666944177838,189.743596810827,
189.820331710161,189.853842655757,189.933394206177,190.012885625034,190.092329165352,
190.171737042769,190.251121444441,190.330507161835,190.409895625754,190.489297908858,
190.568725091464,190.648223507518,190.727760349111,190.807385586633,190.851385037082,
190.929053808582,191.006636543012,191.084147160091,191.161589274167,191.238991698868,
191.316368216488,191.350156227745,191.427900202662,191.5056845015,191.583569631828,
191.637151868893),.UNSPECIFIED.);
#3328=B_SPLINE_CURVE_WITH_KNOTS('',3,(#47461,#47462,#47463,#47464,#47465,
#47466,#47467,#47468,#47469,#47470,#47471,#47472,#47473,#47474,#47475,#47476,
#47477,#47478,#47479,#47480,#47481,#47482,#47483,#47484,#47485,#47486,#47487,
#47488,#47489,#47490,#47491,#47492,#47493,#47494,#47495,#47496,#47497,#47498,
#47499,#47500,#47501,#47502,#47503,#47504,#47505,#47506,#47507,#47508,#47509,
#47510,#47511,#47512,#47513,#47514,#47515,#47516,#47517,#47518,#47519,#47520,
#47521,#47522,#47523,#47524,#47525,#47526,#47527,#47528,#47529,#47530,#47531,
#47532,#47533,#47534,#47535,#47536),.UNSPECIFIED.,.F.,.F.,(4,3,3,3,3,3,
3,3,3,3,3,3,3,3,3,3,3,3,3,3,3,3,3,3,3,4),(189.590644820222,189.673106423952,
189.755567361804,189.838027661176,189.920487349464,190.002946454063,190.085405002363,
190.167863021756,190.250320539629,190.336997497713,190.419464283254,190.501929396322,
190.58439294657,190.666855043629,190.749315797111,190.831775316607,190.914233711692,
190.996691091925,191.079157477611,191.161620679119,191.244081134969,191.326539283524,
191.409004887277,191.491464765665,191.573928876918,191.637151868978),
 .UNSPECIFIED.);
#3329=B_SPLINE_CURVE_WITH_KNOTS('',3,(#47537,#47538,#47539,#47540,#47541,
#47542,#47543,#47544,#47545,#47546,#47547,#47548,#47549,#47550,#47551,#47552,
#47553,#47554,#47555,#47556,#47557,#47558,#47559,#47560,#47561,#47562,#47563,
#47564,#47565,#47566,#47567,#47568,#47569,#47570,#47571,#47572,#47573,#47574,
#47575,#47576,#47577,#47578,#47579,#47580,#47581,#47582,#47583,#47584,#47585,
#47586,#47587,#47588,#47589,#47590,#47591,#47592,#47593,#47594,#47595,#47596,
#47597,#47598,#47599,#47600,#47601,#47602,#47603,#47604,#47605,#47606,#47607,
#47608,#47609,#47610,#47611,#47612,#47613,#47614,#47615,#47616,#47617,#47618,
#47619,#47620,#47621,#47622,#47623,#47624,#47625,#47626,#47627,#47628,#47629,
#47630,#47631,#47632,#47633,#47634,#47635,#47636,#47637,#47638,#47639,#47640,
#47641,#47642,#47643,#47644,#47645,#47646,#47647,#47648,#47649,#47650,#47651,
#47652,#47653,#47654,#47655,#47656,#47657,#47658,#47659,#47660,#47661,#47662,
#47663,#47664,#47665,#47666,#47667,#47668,#47669,#47670,#47671,#47672,#47673,
#47674,#47675,#47676,#47677,#47678,#47679,#47680,#47681,#47682,#47683,#47684,
#47685,#47686,#47687,#47688,#47689,#47690,#47691,#47692,#47693,#47694,#47695,
#47696,#47697,#47698,#47699,#47700,#47701,#47702,#47703,#47704,#47705),
 .UNSPECIFIED.,.F.,.F.,(4,3,3,3,3,3,3,3,3,3,3,3,3,3,3,3,3,3,3,3,3,3,3,3,
3,3,3,3,3,3,3,3,3,3,3,3,3,3,3,3,3,3,3,3,3,3,3,3,3,3,3,3,3,3,3,3,4),(191.637151868978,
191.671432676962,191.752664612443,191.833945211983,191.918009875893,191.999441891284,
192.084822879455,192.170203867625,192.255436882354,192.340591933471,192.425596956231,
192.510495331572,192.595201955416,192.668975058287,192.745534097889,192.822087740658,
192.898650583046,192.975269193464,193.051919040613,193.128652233458,193.16774624895,
193.24729779937,193.326789218227,193.406232758545,193.485640635962,193.565025037634,
193.644410755028,193.723799218947,193.803201502051,193.882628684658,193.962127100712,
194.041663942304,194.121289179826,194.165288630274,194.242957401773,194.320540136204,
194.398050753283,194.475492867358,194.55289529206,194.630271809679,194.664059820937,
194.747548890742,194.831194081817,194.915076772407,194.999072986065,195.083254667227,
195.162831011599,195.240355214955,195.319493794587,195.396848759866,195.47415661739,
195.551431439975,195.631939542984,195.709204239896,195.786475770957,195.863783539233,
195.873463852012),.UNSPECIFIED.);
#3330=B_SPLINE_CURVE_WITH_KNOTS('',3,(#47711,#47712,#47713,#47714,#47715,
#47716,#47717,#47718,#47719,#47720,#47721,#47722,#47723,#47724,#47725,#47726,
#47727,#47728,#47729,#47730,#47731,#47732,#47733,#47734,#47735,#47736,#47737,
#47738,#47739,#47740,#47741,#47742,#47743,#47744,#47745,#47746,#47747,#47748,
#47749,#47750,#47751,#47752,#47753,#47754,#47755,#47756,#47757,#47758,#47759,
#47760,#47761,#47762,#47763,#47764,#47765,#47766,#47767,#47768,#47769,#47770,
#47771,#47772,#47773,#47774,#47775,#47776,#47777,#47778,#47779,#47780,#47781,
#47782,#47783,#47784,#47785,#47786,#47787,#47788,#47789,#47790,#47791,#47792,
#47793,#47794,#47795,#47796,#47797,#47798,#47799,#47800,#47801,#47802,#47803,
#47804,#47805,#47806,#47807,#47808,#47809,#47810,#47811,#47812,#47813,#47814,
#47815,#47816,#47817,#47818,#47819,#47820,#47821,#47822,#47823,#47824,#47825,
#47826,#47827,#47828,#47829,#47830,#47831,#47832,#47833,#47834,#47835,#47836,
#47837,#47838,#47839,#47840,#47841,#47842,#47843,#47844,#47845,#47846,#47847,
#47848,#47849,#47850,#47851,#47852,#47853,#47854,#47855,#47856,#47857,#47858,
#47859,#47860,#47861,#47862,#47863,#47864,#47865,#47866,#47867,#47868,#47869,
#47870,#47871,#47872,#47873,#47874,#47875,#47876,#47877,#47878,#47879),
 .UNSPECIFIED.,.F.,.F.,(4,3,3,3,3,3,3,3,3,3,3,3,3,3,3,3,3,3,3,3,3,3,3,3,
3,3,3,3,3,3,3,3,3,3,3,3,3,3,3,3,3,3,3,3,3,3,3,3,3,3,3,3,3,3,3,3,4),(197.920337176296,
197.995786692891,198.071166512278,198.146485647516,198.221769556338,198.297038071666,
198.332952897019,198.416105006492,198.499405917416,198.582938677015,198.666583255601,
198.750416364689,198.831724087681,198.908963344172,198.986118992796,199.063206910824,
199.140242925539,199.217242825609,199.294235412097,199.371226878564,199.448231489223,
199.525263513282,199.602384967768,199.679552527019,199.75684291302,199.829266469006,
199.906142422896,199.982923501785,200.059625966089,200.136266013088,200.212859790473,
200.289603422955,200.366165741792,200.442732814096,200.519319204004,200.596191615586,
200.672896533004,200.749852691668,200.826808850331,200.904657929378,200.982422320009,
201.060117311562,201.137758144491,201.215360020605,201.292948237709,201.370531383653,
201.448123190583,201.52573739284,201.603430020003,201.681163571845,201.759005861736,
201.824351231656,201.901201730848,201.977941849885,202.054618325147,202.131235123842,
202.157407101182),.UNSPECIFIED.);
#3331=B_SPLINE_CURVE_WITH_KNOTS('',3,(#47880,#47881,#47882,#47883,#47884,
#47885,#47886,#47887,#47888,#47889,#47890,#47891,#47892,#47893,#47894,#47895,
#47896,#47897,#47898,#47899,#47900,#47901,#47902,#47903,#47904,#47905,#47906,
#47907,#47908,#47909,#47910,#47911,#47912,#47913,#47914,#47915,#47916,#47917,
#47918,#47919,#47920,#47921,#47922,#47923,#47924,#47925,#47926,#47927,#47928,
#47929,#47930,#47931,#47932,#47933,#47934,#47935,#47936,#47937,#47938,#47939,
#47940,#47941,#47942,#47943,#47944,#47945,#47946,#47947,#47948,#47949,#47950,
#47951,#47952,#47953,#47954,#47955,#47956,#47957,#47958,#47959,#47960,#47961),
 .UNSPECIFIED.,.F.,.F.,(4,3,3,3,3,3,3,3,3,3,3,3,3,3,3,3,3,3,3,3,3,3,3,3,
3,3,3,4),(195.873887289425,195.958993449409,196.044014597101,196.128882576401,
196.213641033484,196.298220101784,196.337868134369,196.414558774872,196.491244931537,
196.56794110509,196.644693851934,196.721478386049,196.79834647228,196.836639325032,
196.916055518261,196.995410541899,197.074716947158,197.153987247531,197.233233927819,
197.312482484322,197.391734311925,197.471000747633,197.550293136381,197.629659279841,
197.709065232079,197.788562924981,197.834181706357,197.920337176158),
 .UNSPECIFIED.);
#3332=B_SPLINE_CURVE_WITH_KNOTS('',3,(#47963,#47964,#47965,#47966,#47967,
#47968,#47969,#47970,#47971,#47972,#47973,#47974,#47975,#47976,#47977,#47978,
#47979,#47980,#47981,#47982,#47983,#47984,#47985,#47986,#47987,#47988,#47989,
#47990,#47991,#47992,#47993,#47994,#47995,#47996,#47997,#47998,#47999,#48000,
#48001,#48002,#48003,#48004,#48005,#48006,#48007,#48008,#48009,#48010,#48011,
#48012,#48013,#48014,#48015,#48016,#48017,#48018,#48019,#48020,#48021,#48022,
#48023,#48024,#48025,#48026,#48027,#48028,#48029,#48030,#48031,#48032,#48033,
#48034,#48035,#48036,#48037,#48038,#48039,#48040,#48041,#48042,#48043,#48044),
 .UNSPECIFIED.,.F.,.F.,(4,3,3,3,3,3,3,3,3,3,3,3,3,3,3,3,3,3,3,3,3,3,3,3,
3,3,3,4),(195.873463852012,195.950867781641,196.028319749536,196.105886963599,
196.160373392924,196.236441272869,196.312414495841,196.388309838043,196.464143996272,
196.53993360644,196.617181377416,196.692946887209,196.768720499911,196.844517218722,
196.922866857604,196.998797072532,197.07835642339,197.157915774249,197.23617105997,
197.314330723584,197.39238967049,197.470390009991,197.548345159058,197.626268506195,
197.704184682042,197.78209465691,197.860034597259,197.920337176157),
 .UNSPECIFIED.);
#3333=B_SPLINE_CURVE_WITH_KNOTS('',3,(#48045,#48046,#48047,#48048,#48049,
#48050,#48051,#48052,#48053,#48054,#48055,#48056,#48057,#48058,#48059,#48060,
#48061,#48062,#48063,#48064,#48065,#48066,#48067,#48068,#48069,#48070,#48071,
#48072,#48073,#48074,#48075,#48076,#48077,#48078,#48079,#48080,#48081,#48082,
#48083,#48084,#48085,#48086,#48087,#48088,#48089,#48090,#48091,#48092,#48093,
#48094,#48095,#48096,#48097,#48098,#48099,#48100,#48101,#48102,#48103,#48104,
#48105,#48106,#48107,#48108,#48109,#48110,#48111,#48112,#48113,#48114,#48115,
#48116,#48117,#48118,#48119,#48120,#48121,#48122,#48123,#48124,#48125,#48126,
#48127,#48128,#48129,#48130,#48131,#48132,#48133,#48134,#48135,#48136,#48137,
#48138,#48139,#48140,#48141,#48142,#48143,#48144,#48145,#48146,#48147,#48148,
#48149,#48150,#48151,#48152,#48153,#48154,#48155,#48156,#48157,#48158,#48159,
#48160,#48161,#48162,#48163,#48164,#48165,#48166,#48167,#48168,#48169,#48170,
#48171,#48172,#48173,#48174,#48175,#48176,#48177,#48178,#48179,#48180,#48181,
#48182,#48183,#48184,#48185,#48186,#48187,#48188,#48189,#48190,#48191,#48192,
#48193,#48194,#48195,#48196,#48197,#48198,#48199,#48200,#48201,#48202,#48203,
#48204,#48205,#48206,#48207,#48208,#48209,#48210,#48211,#48212,#48213),
 .UNSPECIFIED.,.F.,.F.,(4,3,3,3,3,3,3,3,3,3,3,3,3,3,3,3,3,3,3,3,3,3,3,3,
3,3,3,3,3,3,3,3,3,3,3,3,3,3,3,3,3,3,3,3,3,3,3,3,3,3,3,3,3,3,3,3,4),(197.920337176245,
198.017095852488,198.114911702306,198.155458155574,198.235117343471,198.314706240407,
198.394235705227,198.473708123146,198.553146285035,198.632559677644,198.654229346236,
198.735467052153,198.816753672461,198.90081538857,198.982253917504,199.067627227201,
199.153000536899,199.238136566563,199.323194478014,199.408104032074,199.49290859628,
199.57752545438,199.651771727561,199.728462368064,199.805148524729,199.881844698282,
199.958597445127,200.035381979242,200.112250065472,200.150542918224,200.229959111453,
200.309314135091,200.38862054035,200.467890840722,200.547137521011,200.626386077513,
200.705637905117,200.784904340824,200.864196729572,200.943562873032,201.02296882527,
201.102466518172,201.148085299549,201.226055183723,201.303935307852,201.381739272854,
201.459467884952,201.537152794248,201.614805015986,201.646856490211,201.730008599684,
201.813309510607,201.896842270206,201.980486848792,202.064319957879,202.145627680874,
202.157254934226),.UNSPECIFIED.);
#3334=B_SPLINE_CURVE_WITH_KNOTS('',3,(#48219,#48220,#48221,#48222,#48223,
#48224,#48225,#48226,#48227,#48228,#48229,#48230,#48231,#48232,#48233,#48234,
#48235,#48236,#48237,#48238,#48239,#48240,#48241,#48242,#48243,#48244,#48245,
#48246,#48247,#48248,#48249,#48250,#48251,#48252,#48253,#48254,#48255,#48256,
#48257,#48258,#48259,#48260,#48261,#48262,#48263,#48264,#48265,#48266,#48267,
#48268,#48269,#48270,#48271,#48272,#48273,#48274,#48275,#48276,#48277,#48278,
#48279,#48280,#48281,#48282,#48283,#48284,#48285,#48286,#48287,#48288,#48289,
#48290,#48291,#48292,#48293,#48294,#48295,#48296,#48297,#48298,#48299,#48300,
#48301,#48302,#48303,#48304,#48305,#48306,#48307,#48308,#48309,#48310,#48311,
#48312,#48313,#48314,#48315,#48316,#48317,#48318,#48319,#48320,#48321,#48322,
#48323,#48324,#48325,#48326,#48327,#48328,#48329,#48330,#48331,#48332,#48333,
#48334,#48335,#48336,#48337,#48338,#48339,#48340,#48341,#48342,#48343,#48344,
#48345,#48346,#48347,#48348,#48349,#48350,#48351,#48352,#48353,#48354,#48355,
#48356,#48357,#48358,#48359,#48360,#48361,#48362,#48363,#48364,#48365,#48366,
#48367,#48368,#48369,#48370,#48371,#48372,#48373,#48374,#48375,#48376,#48377,
#48378,#48379,#48380,#48381,#48382,#48383,#48384,#48385,#48386,#48387),
 .UNSPECIFIED.,.F.,.F.,(4,3,3,3,3,3,3,3,3,3,3,3,3,3,3,3,3,3,3,3,3,3,3,3,
3,3,3,3,3,3,3,3,3,3,3,3,3,3,3,3,3,3,3,3,3,3,3,3,3,3,3,3,3,3,3,3,4),(204.203522483337,
204.279096250864,204.318207184968,204.395864860296,204.473546509871,204.551265588754,
204.629078219832,204.706944446481,204.784921232184,204.816978375631,204.896476211081,
204.975898867201,205.055258947777,205.134569008754,205.213841567289,205.293095130547,
205.372339038655,205.451584627026,205.530843230627,205.610155979876,205.689497401063,
205.768913514027,205.814520756956,205.891386076715,205.968184122965,206.044929482336,
206.121637400688,206.198323397914,206.275012318157,206.313291947618,206.397871525398,
206.48259324056,206.567510644375,206.652513000439,206.737635319519,206.812063138281,
206.893626765733,206.975115123468,207.059044924837,207.140378225501,207.225606277222,
207.310834328943,207.390254575581,207.469693513538,207.549161881788,207.628703563694,
207.708287119169,207.787954456856,207.809605519605,207.888377344815,207.966692049295,
208.044957511354,208.12318676496,208.202335104042,208.280540557168,208.360160339228,
208.439780121288),.UNSPECIFIED.);
#3335=B_SPLINE_CURVE_WITH_KNOTS('',3,(#48388,#48389,#48390,#48391,#48392,
#48393,#48394,#48395,#48396,#48397,#48398,#48399,#48400,#48401,#48402,#48403,
#48404,#48405,#48406,#48407,#48408,#48409,#48410,#48411,#48412,#48413,#48414,
#48415,#48416,#48417,#48418,#48419,#48420,#48421,#48422,#48423,#48424,#48425,
#48426,#48427,#48428,#48429,#48430,#48431,#48432,#48433,#48434,#48435,#48436,
#48437,#48438,#48439,#48440,#48441,#48442,#48443,#48444,#48445,#48446,#48447,
#48448,#48449,#48450,#48451,#48452,#48453,#48454,#48455,#48456,#48457,#48458,
#48459,#48460,#48461,#48462,#48463,#48464,#48465,#48466,#48467,#48468,#48469),
 .UNSPECIFIED.,.F.,.F.,(4,3,3,3,3,3,3,3,3,3,3,3,3,3,3,3,3,3,3,3,3,3,3,3,
3,3,3,4),(202.157407101182,202.233976138733,202.310541728034,202.38710926321,
202.463693308331,202.54030843525,202.617014883942,202.693771249812,202.77064566072,
202.821893612981,202.899194427024,202.976401365088,203.053530343199,203.130597219573,
203.207617806501,203.284615533229,203.361602667683,203.438593474282,203.515602216988,
203.592685532518,203.669806798868,203.747037420885,203.819435994306,203.908020543679,
203.996275196705,204.084282235795,204.1718575171,204.203522483235),
 .UNSPECIFIED.);
#3336=B_SPLINE_CURVE_WITH_KNOTS('',3,(#48471,#48472,#48473,#48474,#48475,
#48476,#48477,#48478,#48479,#48480,#48481,#48482,#48483,#48484,#48485,#48486,
#48487,#48488,#48489,#48490,#48491,#48492,#48493,#48494,#48495,#48496,#48497,
#48498,#48499,#48500,#48501,#48502,#48503,#48504,#48505,#48506,#48507,#48508,
#48509,#48510,#48511,#48512,#48513,#48514,#48515,#48516,#48517,#48518,#48519,
#48520,#48521,#48522,#48523,#48524,#48525,#48526,#48527,#48528,#48529,#48530,
#48531,#48532,#48533,#48534,#48535,#48536,#48537,#48538,#48539,#48540,#48541,
#48542,#48543,#48544,#48545,#48546,#48547,#48548,#48549,#48550,#48551,#48552),
 .UNSPECIFIED.,.F.,.F.,(4,3,3,3,3,3,3,3,3,3,3,3,3,3,3,3,3,3,3,3,3,3,3,3,
3,3,3,4),(202.157254934226,202.234480594198,202.311625038834,202.388704137127,
202.46573370984,202.542729540775,202.619721047223,202.696713579503,202.773721402066,
202.850758785572,202.927886350971,203.005061952553,203.082356969342,203.143170062198,
203.220046016088,203.296827094977,203.373529559281,203.45016960628,203.526763383665,
203.603507016147,203.680069334984,203.756636407288,203.833222797196,203.910095208777,
203.986800126196,204.063756284859,204.140712443523,204.203522483337),
 .UNSPECIFIED.);
#3337=B_SPLINE_CURVE_WITH_KNOTS('',3,(#48553,#48554,#48555,#48556,#48557,
#48558,#48559,#48560,#48561,#48562,#48563,#48564,#48565,#48566,#48567,#48568,
#48569,#48570,#48571,#48572,#48573,#48574,#48575,#48576,#48577,#48578,#48579,
#48580,#48581,#48582,#48583,#48584,#48585,#48586,#48587,#48588,#48589,#48590,
#48591,#48592,#48593,#48594,#48595,#48596,#48597,#48598,#48599,#48600,#48601,
#48602,#48603,#48604,#48605,#48606,#48607,#48608,#48609,#48610,#48611,#48612,
#48613,#48614,#48615,#48616,#48617,#48618,#48619,#48620,#48621,#48622,#48623,
#48624,#48625,#48626,#48627,#48628,#48629,#48630,#48631,#48632,#48633,#48634,
#48635,#48636,#48637,#48638,#48639,#48640,#48641,#48642,#48643,#48644,#48645,
#48646,#48647,#48648,#48649,#48650,#48651,#48652,#48653,#48654,#48655,#48656,
#48657,#48658,#48659,#48660,#48661,#48662,#48663,#48664,#48665,#48666,#48667,
#48668,#48669,#48670,#48671,#48672,#48673,#48674,#48675,#48676,#48677,#48678,
#48679,#48680,#48681,#48682,#48683,#48684,#48685,#48686,#48687,#48688,#48689,
#48690,#48691,#48692,#48693,#48694,#48695,#48696,#48697,#48698,#48699,#48700,
#48701,#48702,#48703,#48704,#48705,#48706,#48707,#48708,#48709,#48710,#48711,
#48712,#48713,#48714,#48715,#48716,#48717,#48718),.UNSPECIFIED.,.F.,.F.,
(4,3,3,3,3,3,3,3,3,3,3,3,3,3,3,3,3,3,3,3,3,3,3,3,3,3,3,3,3,3,3,3,3,3,3,
3,3,3,3,3,3,3,3,3,3,3,3,3,3,3,3,3,3,3,3,4),(204.203522483439,204.280638712373,
204.357672734015,204.434640552169,204.511558120638,204.589895208664,204.66677088276,
204.74364729744,204.820538833263,204.899967831159,204.976969817163,205.057612321005,
205.138254824848,205.215086266976,205.291830223095,205.368502923075,205.445120540013,
205.521699203249,205.598461453615,205.675026695918,205.751603505063,205.828206449279,
205.905104138502,205.981842244115,206.058819725144,206.135797206173,206.213098020216,
206.29030495828,206.367433936391,206.444500812766,206.521521399694,206.598519126422,
206.675506260877,206.752497067476,206.829505810182,206.906589125712,206.983710392062,
207.060941014079,207.133339587498,207.217202174031,207.300936274521,207.384466767405,
207.467870922295,207.55106929973,207.63211077816,207.709768453488,207.787450103063,
207.865169181945,207.942981813023,208.020848039672,208.098824825375,208.130881968823,
208.210370620897,208.289793196534,208.369146266771,208.440541694968),
 .UNSPECIFIED.);
#3338=B_SPLINE_CURVE_WITH_KNOTS('',3,(#48724,#48725,#48726,#48727,#48728,
#48729,#48730,#48731,#48732,#48733,#48734,#48735,#48736,#48737,#48738,#48739,
#48740,#48741,#48742,#48743,#48744,#48745,#48746,#48747,#48748,#48749,#48750,
#48751,#48752,#48753,#48754,#48755,#48756,#48757,#48758,#48759,#48760,#48761,
#48762,#48763,#48764,#48765,#48766,#48767,#48768,#48769,#48770,#48771,#48772,
#48773,#48774,#48775,#48776,#48777,#48778,#48779,#48780,#48781,#48782,#48783,
#48784,#48785,#48786,#48787,#48788,#48789,#48790,#48791,#48792,#48793,#48794,
#48795,#48796,#48797,#48798,#48799,#48800,#48801,#48802,#48803,#48804,#48805,
#48806,#48807,#48808,#48809,#48810,#48811,#48812,#48813,#48814,#48815,#48816,
#48817,#48818,#48819,#48820,#48821,#48822,#48823,#48824,#48825,#48826,#48827,
#48828,#48829,#48830,#48831,#48832,#48833,#48834,#48835,#48836,#48837,#48838,
#48839,#48840,#48841,#48842,#48843,#48844,#48845,#48846,#48847,#48848,#48849,
#48850,#48851,#48852,#48853,#48854,#48855,#48856,#48857,#48858,#48859,#48860,
#48861,#48862,#48863,#48864,#48865,#48866,#48867,#48868,#48869,#48870,#48871,
#48872,#48873,#48874,#48875,#48876,#48877,#48878,#48879,#48880,#48881,#48882,
#48883,#48884,#48885,#48886,#48887,#48888,#48889),.UNSPECIFIED.,.F.,.F.,
(4,3,3,3,3,3,3,3,3,3,3,3,3,3,3,3,3,3,3,3,3,3,3,3,3,3,3,3,3,3,3,3,3,3,3,
3,3,3,3,3,3,3,3,3,3,3,3,3,3,3,3,3,3,3,3,4),(210.486707790649,210.574035997978,
210.661686182205,210.749760506045,210.80223266358,210.886442245555,210.97052570924,
211.054404114442,211.138153424452,211.221688690448,211.301003854243,211.378384829864,
211.455784219723,211.533215809293,211.610734371807,211.688302600197,211.765977187034,
211.799775044905,211.879399937905,211.958952092152,212.038443808265,212.117887340283,
212.19729490458,212.276685021492,212.356066253251,212.43544967092,212.514846345597,
212.594296643381,212.673775344177,212.753327168943,212.79731742623,212.874048083749,
212.950711760688,213.027323139814,213.103897983228,213.180451388659,213.257008861462,
213.296088616892,213.380757685452,213.465572218932,213.550585623803,213.635685128274,
213.720904607872,213.794859807555,213.876416669066,213.957898399095,214.041831548876,
214.123158669838,214.208394834028,214.293630998217,214.373037155101,214.45246100326,
214.531942537781,214.611455786587,214.691042107325,214.723212227427),
 .UNSPECIFIED.);
#3339=B_SPLINE_CURVE_WITH_KNOTS('',3,(#48890,#48891,#48892,#48893,#48894,
#48895,#48896,#48897,#48898,#48899,#48900,#48901,#48902,#48903,#48904,#48905,
#48906,#48907,#48908,#48909,#48910,#48911,#48912,#48913,#48914,#48915,#48916,
#48917,#48918,#48919,#48920,#48921,#48922,#48923,#48924,#48925,#48926,#48927,
#48928,#48929,#48930,#48931,#48932,#48933,#48934,#48935,#48936,#48937,#48938,
#48939,#48940,#48941,#48942,#48943,#48944,#48945,#48946,#48947,#48948,#48949,
#48950,#48951,#48952,#48953,#48954,#48955,#48956,#48957,#48958,#48959,#48960,
#48961,#48962,#48963,#48964,#48965,#48966,#48967,#48968,#48969,#48970,#48971),
 .UNSPECIFIED.,.F.,.F.,(4,3,3,3,3,3,3,3,3,3,3,3,3,3,3,3,3,3,3,3,3,3,3,3,
3,3,3,4),(208.439780121288,208.518059139744,208.596430820126,208.674852659219,
208.753389883147,208.80714790093,208.883220824591,208.959198260761,209.035096990122,
209.110933712966,209.186725067822,209.263970719626,209.339735933323,209.415508486867,
209.491303382834,209.56965010769,209.645576602262,209.725133442259,209.804690282255,
209.883057417126,209.961290668218,210.039444773925,210.117533004171,210.195568587955,
210.273564240263,210.35153553291,210.429506710964,210.486707790517),
 .UNSPECIFIED.);
#3340=B_SPLINE_CURVE_WITH_KNOTS('',3,(#48973,#48974,#48975,#48976,#48977,
#48978,#48979,#48980,#48981,#48982,#48983,#48984,#48985,#48986,#48987,#48988,
#48989,#48990,#48991,#48992,#48993,#48994,#48995,#48996,#48997,#48998,#48999,
#49000,#49001,#49002,#49003,#49004,#49005,#49006,#49007,#49008,#49009,#49010,
#49011,#49012,#49013,#49014,#49015,#49016,#49017,#49018,#49019,#49020,#49021,
#49022,#49023,#49024,#49025,#49026,#49027,#49028,#49029,#49030,#49031,#49032,
#49033,#49034,#49035,#49036,#49037,#49038,#49039,#49040,#49041,#49042,#49043,
#49044,#49045,#49046,#49047,#49048,#49049,#49050,#49051,#49052,#49053,#49054),
 .UNSPECIFIED.,.F.,.F.,(4,3,3,3,3,3,3,3,3,3,3,3,3,3,3,3,3,3,3,3,3,3,3,3,
3,3,3,4),(208.440541694968,208.519817442129,208.599072594872,208.678316958421,
208.757561868633,208.836818660193,208.916129113754,208.995467201196,209.074881457727,
209.128424350148,209.205289669907,209.282087716157,209.358833075529,209.43554099388,
209.512226991107,209.58891591135,209.62719554081,209.711775118591,209.796496833754,
209.881414237569,209.966416593633,210.051538912713,210.125966731473,210.209270925977,
210.292449952588,210.375545570823,210.458524059154,210.486707790517),
 .UNSPECIFIED.);
#3341=B_SPLINE_CURVE_WITH_KNOTS('',3,(#49055,#49056,#49057,#49058,#49059,
#49060,#49061,#49062,#49063,#49064,#49065,#49066,#49067,#49068,#49069,#49070,
#49071,#49072,#49073,#49074,#49075,#49076,#49077,#49078,#49079,#49080,#49081,
#49082,#49083,#49084,#49085,#49086,#49087,#49088,#49089,#49090,#49091,#49092,
#49093,#49094,#49095,#49096,#49097,#49098,#49099,#49100,#49101,#49102,#49103,
#49104,#49105,#49106,#49107,#49108,#49109,#49110,#49111,#49112,#49113,#49114,
#49115,#49116,#49117,#49118,#49119,#49120,#49121,#49122,#49123,#49124,#49125,
#49126,#49127,#49128,#49129,#49130,#49131,#49132,#49133,#49134,#49135,#49136,
#49137,#49138,#49139,#49140,#49141,#49142,#49143,#49144,#49145,#49146,#49147,
#49148,#49149,#49150,#49151,#49152,#49153,#49154,#49155,#49156,#49157,#49158,
#49159,#49160,#49161,#49162,#49163,#49164,#49165,#49166,#49167,#49168,#49169,
#49170,#49171,#49172,#49173,#49174,#49175,#49176,#49177,#49178,#49179,#49180,
#49181,#49182,#49183,#49184,#49185,#49186,#49187,#49188,#49189,#49190,#49191,
#49192,#49193,#49194,#49195,#49196,#49197,#49198,#49199,#49200,#49201,#49202,
#49203,#49204,#49205,#49206,#49207,#49208,#49209,#49210,#49211),
 .UNSPECIFIED.,.F.,.F.,(4,3,3,3,3,3,3,3,3,3,3,3,3,3,3,3,3,3,3,3,3,3,3,3,
3,3,3,3,3,3,3,3,3,3,3,3,3,3,3,3,3,3,3,3,3,3,3,3,3,3,3,3,4),(210.486707790517,
210.569169996617,210.65163185442,210.734093370775,210.816554552533,210.899015406543,
210.981475939655,211.063936158718,211.146396070581,211.228855682093,211.311315000102,
211.393774031456,211.476232783002,211.55869126159,211.641149474066,211.723607427277,
211.806065128069,211.888522583291,211.970979799789,212.056992495075,212.140317293633,
212.222783899225,212.305249660608,212.387714605198,212.470178760406,212.552642153643,
212.635104812314,212.717566763826,212.800028035578,212.882488654971,212.964948649402,
213.047408046266,213.129866872957,213.212325156864,213.294782925377,213.377240205883,
213.461374321074,213.543840319434,213.62630469604,213.708767560536,213.791229022542,
213.873689191661,213.956148177477,214.038606089558,214.12420358448,214.206668321526,
214.289130093913,214.371589340078,214.454046498316,214.536509017399,214.61896668881,
214.701425480003,214.72338604894),.UNSPECIFIED.);
#3342=B_SPLINE_CURVE_WITH_KNOTS('',3,(#49217,#49218,#49219,#49220,#49221,
#49222,#49223,#49224,#49225,#49226,#49227,#49228,#49229,#49230,#49231,#49232,
#49233,#49234,#49235,#49236,#49237,#49238,#49239,#49240,#49241,#49242,#49243,
#49244,#49245,#49246,#49247,#49248,#49249,#49250,#49251,#49252,#49253,#49254,
#49255,#49256,#49257,#49258,#49259,#49260,#49261,#49262,#49263,#49264,#49265,
#49266,#49267,#49268,#49269,#49270,#49271,#49272,#49273,#49274,#49275,#49276,
#49277,#49278,#49279,#49280,#49281,#49282,#49283,#49284,#49285,#49286,#49287,
#49288,#49289,#49290,#49291,#49292,#49293,#49294,#49295,#49296,#49297,#49298,
#49299,#49300,#49301,#49302,#49303,#49304,#49305,#49306,#49307,#49308,#49309,
#49310,#49311,#49312,#49313,#49314,#49315,#49316,#49317,#49318,#49319,#49320,
#49321,#49322,#49323,#49324,#49325,#49326,#49327,#49328,#49329,#49330,#49331,
#49332,#49333,#49334,#49335,#49336,#49337,#49338,#49339,#49340,#49341,#49342,
#49343,#49344,#49345,#49346,#49347,#49348,#49349,#49350,#49351,#49352,#49353,
#49354,#49355,#49356,#49357,#49358,#49359,#49360,#49361,#49362,#49363,#49364,
#49365,#49366,#49367,#49368,#49369,#49370,#49371,#49372,#49373,#49374,#49375,
#49376,#49377,#49378,#49379,#49380,#49381,#49382,#49383,#49384,#49385),
 .UNSPECIFIED.,.F.,.F.,(4,3,3,3,3,3,3,3,3,3,3,3,3,3,3,3,3,3,3,3,3,3,3,3,
3,3,3,3,3,3,3,3,3,3,3,3,3,3,3,3,3,3,3,3,3,3,3,3,3,3,3,3,3,3,3,3,4),(216.769893097696,
216.78748695153,216.865057174543,216.942535317151,217.01993703317,217.097277921584,
217.174573537611,217.251846979369,217.329110216827,217.40637728642,217.483662224083,
217.561020228582,217.638415761792,217.715917430692,217.785029332854,217.869241477041,
217.953327497511,218.037208412379,218.120960191465,218.204497832145,218.283800523517,
218.361180292665,218.438578456566,218.516008802034,218.593526098427,218.671093047367,
218.748766341805,218.782571714179,218.862196901683,218.941749356195,219.021241377614,
219.100685219253,219.180093096772,219.25948353051,219.338865080873,219.418248818292,
219.497645813234,219.577096429974,219.656575449028,219.7361275883,219.780114095504,
219.85684467338,219.933508271297,220.010119572076,220.086694338341,220.163247667286,
220.239805064844,220.278885286167,220.363554278549,220.448368731396,220.533382050469,
220.618481466828,220.703700856217,220.777656476829,220.859217231912,220.940684707488,
221.007081309262),.UNSPECIFIED.);
#3343=B_SPLINE_CURVE_WITH_KNOTS('',3,(#49386,#49387,#49388,#49389,#49390,
#49391,#49392,#49393,#49394,#49395,#49396,#49397,#49398,#49399,#49400,#49401,
#49402,#49403,#49404,#49405,#49406,#49407,#49408,#49409,#49410,#49411,#49412,
#49413,#49414,#49415,#49416,#49417,#49418,#49419,#49420,#49421,#49422,#49423,
#49424,#49425,#49426,#49427,#49428,#49429,#49430,#49431,#49432,#49433,#49434,
#49435,#49436,#49437,#49438,#49439,#49440,#49441,#49442,#49443,#49444,#49445,
#49446,#49447,#49448,#49449,#49450,#49451,#49452,#49453,#49454,#49455,#49456,
#49457,#49458,#49459,#49460,#49461,#49462,#49463,#49464,#49465,#49466,#49467),
 .UNSPECIFIED.,.F.,.F.,(4,3,3,3,3,3,3,3,3,3,3,3,3,3,3,3,3,3,3,3,3,3,3,3,
3,3,3,4),(214.723212227427,214.79240218888,214.870790556853,214.949112810023,
215.027383347989,215.10561653284,215.183826698642,215.262044821928,215.340270874921,
215.418517844138,215.496798725914,215.575172141155,215.65359512691,215.732134673559,
215.789944570205,215.865782243268,215.941524820589,216.017189214147,216.092792248486,
216.16835068143,216.243891735941,216.319425700808,216.394967679098,216.470532780008,
216.546183611105,216.621878216807,216.697695297951,216.769893097579),
 .UNSPECIFIED.);
#3344=B_SPLINE_CURVE_WITH_KNOTS('',3,(#49469,#49470,#49471,#49472,#49473,
#49474,#49475,#49476,#49477,#49478,#49479,#49480,#49481,#49482,#49483,#49484,
#49485,#49486,#49487,#49488,#49489,#49490,#49491,#49492,#49493,#49494,#49495,
#49496,#49497,#49498,#49499,#49500,#49501,#49502,#49503,#49504,#49505,#49506,
#49507,#49508,#49509,#49510,#49511,#49512,#49513,#49514,#49515,#49516,#49517,
#49518,#49519,#49520,#49521,#49522,#49523,#49524,#49525,#49526,#49527,#49528,
#49529,#49530,#49531,#49532,#49533,#49534,#49535,#49536,#49537,#49538,#49539,
#49540,#49541,#49542,#49543,#49544),.UNSPECIFIED.,.F.,.F.,(4,3,3,3,3,3,
3,3,3,3,3,3,3,3,3,3,3,3,3,3,3,3,3,3,3,4),(214.72338604894,214.805847652671,
214.888308590522,214.970768889894,215.053228578183,215.135687682781,215.218146231082,
215.300604250474,215.383061768347,215.469738726431,215.552205511972,215.63467062504,
215.717134175288,215.799596272347,215.882057025829,215.964516545325,216.04697494041,
216.129432320643,216.21189870633,216.294361907838,216.376822363687,216.459280512242,
216.541746115996,216.624205994384,216.706670105636,216.769893097696),
 .UNSPECIFIED.);
#3345=B_SPLINE_CURVE_WITH_KNOTS('',3,(#49545,#49546,#49547,#49548,#49549,
#49550,#49551,#49552,#49553,#49554,#49555,#49556,#49557,#49558,#49559,#49560,
#49561,#49562,#49563,#49564,#49565,#49566,#49567,#49568,#49569,#49570,#49571,
#49572,#49573,#49574,#49575,#49576,#49577,#49578,#49579,#49580,#49581,#49582,
#49583,#49584,#49585,#49586,#49587,#49588,#49589,#49590,#49591,#49592,#49593,
#49594,#49595,#49596,#49597,#49598,#49599,#49600,#49601,#49602,#49603,#49604,
#49605,#49606,#49607,#49608,#49609,#49610,#49611,#49612,#49613,#49614,#49615,
#49616,#49617,#49618,#49619,#49620,#49621,#49622,#49623,#49624,#49625,#49626,
#49627,#49628,#49629,#49630,#49631,#49632,#49633,#49634,#49635,#49636,#49637,
#49638,#49639,#49640,#49641,#49642,#49643,#49644,#49645,#49646,#49647,#49648,
#49649,#49650,#49651,#49652,#49653,#49654,#49655,#49656,#49657,#49658,#49659,
#49660,#49661,#49662,#49663,#49664,#49665,#49666,#49667,#49668,#49669,#49670,
#49671,#49672,#49673,#49674,#49675,#49676,#49677,#49678,#49679,#49680,#49681,
#49682,#49683,#49684,#49685,#49686,#49687,#49688,#49689,#49690,#49691,#49692,
#49693,#49694,#49695,#49696,#49697,#49698,#49699,#49700,#49701,#49702,#49703,
#49704,#49705,#49706,#49707,#49708,#49709,#49710),.UNSPECIFIED.,.F.,.F.,
(4,3,3,3,3,3,3,3,3,3,3,3,3,3,3,3,3,3,3,3,3,3,3,3,3,3,3,3,3,3,3,3,3,3,3,
3,3,3,3,3,3,3,3,3,3,3,3,3,3,3,3,3,3,3,3,4),(216.769893097696,216.857542834203,
216.94535140566,217.033334882977,217.108763400747,217.190320262258,217.271801992287,
217.355735142068,217.43706226303,217.52229842722,217.607534591409,217.686945851679,
217.766375539313,217.8458344145,217.925366303503,218.004939896209,218.0845970871,
218.106305782072,218.184694150045,218.263016403215,218.341286941181,218.419520126032,
218.497730291834,218.57594841512,218.654174468113,218.73242143733,218.810702319106,
218.889075734348,218.967498720102,219.046038266751,219.103848163397,219.179919442805,
219.255895221033,219.331792279812,219.407627320417,219.483416982312,219.560663677613,
219.636427177676,219.712198010845,219.787991180482,219.866341021542,219.942265786842,
220.021828165782,220.101390544722,220.178966041541,220.256448430164,220.333853368607,
220.41119645919,220.488491688953,220.565761219485,220.643019095461,220.720279352326,
220.797585916934,220.874916814307,220.952325353479,221.006028990015),
 .UNSPECIFIED.);
#3346=B_SPLINE_CURVE_WITH_KNOTS('',3,(#49716,#49717,#49718,#49719,#49720,
#49721,#49722,#49723,#49724,#49725,#49726,#49727,#49728,#49729,#49730,#49731,
#49732,#49733,#49734,#49735,#49736,#49737,#49738,#49739,#49740,#49741,#49742,
#49743,#49744,#49745,#49746,#49747,#49748,#49749,#49750,#49751,#49752,#49753,
#49754,#49755,#49756,#49757,#49758,#49759,#49760,#49761,#49762,#49763,#49764,
#49765,#49766,#49767,#49768,#49769,#49770,#49771,#49772,#49773,#49774,#49775,
#49776,#49777,#49778,#49779,#49780,#49781,#49782,#49783,#49784,#49785,#49786,
#49787,#49788,#49789,#49790,#49791,#49792,#49793,#49794,#49795,#49796,#49797,
#49798,#49799,#49800,#49801,#49802,#49803,#49804,#49805,#49806,#49807,#49808,
#49809,#49810,#49811,#49812,#49813,#49814,#49815,#49816,#49817,#49818,#49819,
#49820,#49821,#49822,#49823,#49824,#49825,#49826,#49827,#49828,#49829,#49830,
#49831,#49832,#49833,#49834,#49835,#49836,#49837,#49838,#49839,#49840,#49841,
#49842,#49843,#49844,#49845,#49846,#49847,#49848,#49849,#49850,#49851,#49852,
#49853,#49854,#49855,#49856,#49857,#49858,#49859,#49860,#49861,#49862,#49863,
#49864,#49865,#49866,#49867,#49868,#49869,#49870,#49871,#49872),
 .UNSPECIFIED.,.F.,.F.,(4,3,3,3,3,3,3,3,3,3,3,3,3,3,3,3,3,3,3,3,3,3,3,3,
3,3,3,3,3,3,3,3,3,3,3,3,3,3,3,3,3,3,3,3,3,3,3,3,3,3,3,3,4),(223.053078404876,
223.135540610976,223.218002468779,223.300463985134,223.382925166892,223.465386020902,
223.547846554014,223.630306773077,223.71276668494,223.795226296452,223.877685614461,
223.960144645815,224.042603397362,224.125061875949,224.207520088425,224.289978041636,
224.372435742429,224.45489319765,224.537350414148,224.623363109434,224.706687907992,
224.789154513584,224.871620274967,224.954085219557,225.036549374765,225.119012768002,
225.201475426674,225.283937378185,225.366398649937,225.44885926933,225.531319263761,
225.613778660626,225.696237487316,225.778695771223,225.861153539736,225.943610820242,
226.027744935433,226.110210933793,226.192675310399,226.275138174895,226.357599636901,
226.44005980602,226.522518791836,226.604976703917,226.690574198839,226.773038935885,
226.855500708272,226.937959954437,227.020417112675,227.102879631758,227.185337303169,
227.267796094362,227.289756663299),.UNSPECIFIED.);
#3347=B_SPLINE_CURVE_WITH_KNOTS('',3,(#49873,#49874,#49875,#49876,#49877,
#49878,#49879,#49880,#49881,#49882,#49883,#49884,#49885,#49886,#49887,#49888,
#49889,#49890,#49891,#49892,#49893,#49894,#49895,#49896,#49897,#49898,#49899,
#49900,#49901,#49902,#49903,#49904,#49905,#49906,#49907,#49908,#49909,#49910,
#49911,#49912,#49913,#49914,#49915,#49916,#49917,#49918,#49919,#49920,#49921,
#49922,#49923,#49924,#49925,#49926,#49927,#49928,#49929,#49930,#49931,#49932,
#49933,#49934,#49935,#49936,#49937,#49938,#49939,#49940,#49941,#49942,#49943,
#49944,#49945,#49946,#49947,#49948,#49949,#49950,#49951,#49952,#49953,#49954),
 .UNSPECIFIED.,.F.,.F.,(4,3,3,3,3,3,3,3,3,3,3,3,3,3,3,3,3,3,3,3,3,3,3,3,
3,3,3,4),(221.007081309262,221.08842070214,221.169705935063,221.250929267071,
221.276427667492,221.355838866142,221.435268490865,221.514727301993,221.594259125629,
221.67383265224,221.753489776388,221.775198858154,221.853587237142,221.931909501563,
222.010180051,222.088413247522,222.166623425177,222.244841560538,222.323067625735,
222.40131460727,222.479595501462,222.557968929194,222.636391927495,222.714931486662,
222.772741239479,222.865773615059,222.959426009967,223.053078404876),
 .UNSPECIFIED.);
#3348=B_SPLINE_CURVE_WITH_KNOTS('',3,(#49956,#49957,#49958,#49959,#49960,
#49961,#49962,#49963,#49964,#49965,#49966,#49967,#49968,#49969,#49970,#49971,
#49972,#49973,#49974,#49975,#49976,#49977,#49978,#49979,#49980,#49981,#49982,
#49983,#49984,#49985,#49986,#49987,#49988,#49989,#49990,#49991,#49992,#49993,
#49994,#49995,#49996,#49997,#49998,#49999,#50000,#50001,#50002,#50003,#50004,
#50005,#50006,#50007,#50008,#50009,#50010,#50011,#50012,#50013,#50014,#50015,
#50016,#50017,#50018,#50019,#50020,#50021,#50022,#50023,#50024,#50025,#50026,
#50027,#50028,#50029,#50030,#50031,#50032,#50033,#50034,#50035,#50036,#50037),
 .UNSPECIFIED.,.F.,.F.,(4,3,3,3,3,3,3,3,3,3,3,3,3,3,3,3,3,3,3,3,3,3,3,3,
3,3,3,4),(221.006028990015,221.08355116665,221.098932926047,221.183145070235,
221.267231090704,221.351112005572,221.434863784658,221.518401425339,221.597704116709,
221.675083885857,221.752482049758,221.829912395226,221.907429691619,221.984996640559,
222.062669934996,222.096475307371,222.175596135735,222.254642773363,222.333628560977,
222.412566793728,222.492630745122,222.57152068099,222.650405615386,222.729297551187,
222.81024276461,222.889213089609,222.971145747242,223.053078404876),
 .UNSPECIFIED.);
#3349=B_SPLINE_CURVE_WITH_KNOTS('',3,(#50038,#50039,#50040,#50041,#50042,
#50043,#50044,#50045,#50046,#50047,#50048,#50049,#50050,#50051,#50052,#50053,
#50054,#50055,#50056,#50057,#50058,#50059,#50060,#50061,#50062,#50063,#50064,
#50065,#50066,#50067,#50068,#50069,#50070,#50071,#50072,#50073,#50074,#50075,
#50076,#50077,#50078,#50079,#50080,#50081,#50082,#50083,#50084,#50085,#50086,
#50087,#50088,#50089,#50090,#50091,#50092,#50093,#50094,#50095,#50096,#50097,
#50098,#50099,#50100,#50101,#50102,#50103,#50104,#50105,#50106,#50107,#50108,
#50109,#50110,#50111,#50112,#50113,#50114,#50115,#50116,#50117,#50118,#50119,
#50120,#50121,#50122,#50123,#50124,#50125,#50126,#50127,#50128,#50129,#50130,
#50131,#50132,#50133,#50134,#50135,#50136,#50137,#50138,#50139,#50140,#50141,
#50142,#50143,#50144,#50145,#50146,#50147,#50148,#50149,#50150,#50151,#50152,
#50153,#50154,#50155,#50156,#50157,#50158,#50159,#50160,#50161,#50162,#50163,
#50164,#50165,#50166,#50167,#50168,#50169,#50170,#50171,#50172,#50173,#50174,
#50175,#50176,#50177,#50178,#50179,#50180,#50181,#50182,#50183,#50184,#50185,
#50186,#50187,#50188,#50189,#50190,#50191,#50192,#50193,#50194),
 .UNSPECIFIED.,.F.,.F.,(4,3,3,3,3,3,3,3,3,3,3,3,3,3,3,3,3,3,3,3,3,3,3,3,
3,3,3,3,3,3,3,3,3,3,3,3,3,3,3,3,3,3,3,3,3,3,3,3,3,3,3,3,4),(223.053078404876,
223.135540610976,223.218002468779,223.300463985134,223.382925166892,223.465386020902,
223.547846554014,223.630306773077,223.71276668494,223.795226296452,223.877685614461,
223.960144645814,224.042603397361,224.125061875949,224.207520088424,224.289978041635,
224.372435742428,224.45489319765,224.537350414148,224.623363109434,224.706687907992,
224.789154513584,224.871620274967,224.954085219557,225.036549374765,225.119012768002,
225.201475426673,225.283937378184,225.366398649937,225.44885926933,225.531319263761,
225.613778660625,225.696237487315,225.778695771222,225.861153539735,225.943610820242,
226.027744935433,226.110210933793,226.192675310399,226.275138174894,226.357599636901,
226.44005980602,226.522518791836,226.604976703916,226.690574198839,226.773038935885,
226.855500708271,226.937959954437,227.020417112675,227.102879631758,227.185337303169,
227.267796094362,227.289756663299),.UNSPECIFIED.);
#3350=B_SPLINE_CURVE_WITH_KNOTS('',3,(#50200,#50201,#50202,#50203,#50204,
#50205,#50206,#50207,#50208,#50209,#50210,#50211,#50212,#50213,#50214,#50215,
#50216,#50217,#50218,#50219,#50220,#50221,#50222,#50223,#50224,#50225,#50226,
#50227,#50228,#50229,#50230,#50231,#50232,#50233,#50234,#50235,#50236,#50237,
#50238,#50239,#50240,#50241,#50242,#50243,#50244,#50245,#50246,#50247,#50248,
#50249,#50250,#50251,#50252,#50253,#50254,#50255,#50256,#50257,#50258,#50259,
#50260,#50261,#50262,#50263,#50264,#50265,#50266,#50267,#50268,#50269,#50270,
#50271,#50272,#50273,#50274,#50275,#50276,#50277,#50278,#50279,#50280,#50281,
#50282,#50283,#50284,#50285,#50286,#50287,#50288,#50289,#50290,#50291,#50292,
#50293,#50294,#50295,#50296,#50297,#50298,#50299,#50300,#50301,#50302,#50303,
#50304,#50305,#50306,#50307,#50308,#50309,#50310,#50311,#50312,#50313,#50314,
#50315,#50316,#50317,#50318,#50319,#50320,#50321,#50322,#50323,#50324,#50325,
#50326,#50327,#50328,#50329,#50330,#50331,#50332,#50333,#50334,#50335,#50336,
#50337,#50338,#50339,#50340,#50341,#50342,#50343,#50344,#50345,#50346,#50347,
#50348,#50349,#50350,#50351,#50352,#50353,#50354,#50355,#50356,#50357,#50358,
#50359,#50360,#50361,#50362,#50363,#50364,#50365),.UNSPECIFIED.,.F.,.F.,
(4,3,3,3,3,3,3,3,3,3,3,3,3,3,3,3,3,3,3,3,3,3,3,3,3,3,3,3,3,3,3,3,3,3,3,
3,3,3,3,3,3,3,3,3,3,3,3,3,3,3,3,3,3,3,3,4),(229.336263712055,229.42420714738,
229.512813714511,229.60173220212,229.691037881645,229.755537908753,229.831609186389,
229.907584962836,229.983482019828,230.059317058641,230.135106718738,230.212353415156,
230.288116913416,230.363887744783,230.439680912617,230.518030756982,230.593955520493,
230.673517905285,230.753080290078,230.830650511021,230.908128651541,230.985530365454,
231.062871251749,231.140166865644,231.217440305258,231.294703540565,231.371970608002,
231.449255543505,231.526613545852,231.604009076909,231.681510743676,231.750622671403,
231.834834822864,231.918920850574,232.00280177252,232.086553558554,232.170091205891,
232.249393862065,232.326773628396,232.404171789439,232.481602132012,232.559119425465,
232.636686371439,232.714359662886,232.748165052728,232.827797669572,232.907356129713,
232.990558092998,233.069996494092,233.149402444597,233.228787037255,233.30816134938,
233.387551861245,233.46695070344,233.546387278613,233.572971835991),
 .UNSPECIFIED.);
#3351=B_SPLINE_CURVE_WITH_KNOTS('',3,(#50366,#50367,#50368,#50369,#50370,
#50371,#50372,#50373,#50374,#50375,#50376,#50377,#50378,#50379,#50380,#50381,
#50382,#50383,#50384,#50385,#50386,#50387,#50388,#50389,#50390,#50391,#50392,
#50393,#50394,#50395,#50396,#50397,#50398,#50399,#50400,#50401,#50402,#50403,
#50404,#50405,#50406,#50407,#50408,#50409,#50410,#50411,#50412,#50413,#50414,
#50415,#50416,#50417,#50418,#50419,#50420,#50421,#50422,#50423,#50424,#50425,
#50426,#50427,#50428,#50429,#50430,#50431,#50432,#50433,#50434,#50435,#50436,
#50437,#50438,#50439,#50440,#50441),.UNSPECIFIED.,.F.,.F.,(4,3,3,3,3,3,
3,3,3,3,3,3,3,3,3,3,3,3,3,3,3,3,3,3,3,4),(227.289756663299,227.37221826703,
227.454679204882,227.537139504254,227.619599192542,227.70205829714,227.784516845441,
227.866974864833,227.949432382706,228.03610934079,228.118576126331,228.201041239399,
228.283504789647,228.365966886706,228.448427640188,228.530887159684,228.613345554769,
228.695802935002,228.778269320689,228.860732522197,228.943192978047,229.025651126601,
229.108116730355,229.190576608743,229.273040719995,229.336263712055),
 .UNSPECIFIED.);
#3352=B_SPLINE_CURVE_WITH_KNOTS('',3,(#50443,#50444,#50445,#50446,#50447,
#50448,#50449,#50450,#50451,#50452,#50453,#50454,#50455,#50456,#50457,#50458,
#50459,#50460,#50461,#50462,#50463,#50464,#50465,#50466,#50467,#50468,#50469,
#50470,#50471,#50472,#50473,#50474,#50475,#50476,#50477,#50478,#50479,#50480,
#50481,#50482,#50483,#50484,#50485,#50486,#50487,#50488,#50489,#50490,#50491,
#50492,#50493,#50494,#50495,#50496,#50497,#50498,#50499,#50500,#50501,#50502,
#50503,#50504,#50505,#50506,#50507,#50508,#50509,#50510,#50511,#50512,#50513,
#50514,#50515,#50516,#50517,#50518),.UNSPECIFIED.,.F.,.F.,(4,3,3,3,3,3,
3,3,3,3,3,3,3,3,3,3,3,3,3,3,3,3,3,3,3,4),(227.289756663299,227.37221826703,
227.454679204882,227.537139504254,227.619599192542,227.70205829714,227.784516845441,
227.866974864833,227.949432382706,228.036109340785,228.118576126326,228.201041239394,
228.283504789642,228.365966886701,228.448427640183,228.530887159679,228.613345554764,
228.695802934997,228.778269320684,228.860732522192,228.943192978041,229.025651126596,
229.10811673035,229.190576608738,229.27304071999,229.33626371197),
 .UNSPECIFIED.);
#3353=B_SPLINE_CURVE_WITH_KNOTS('',3,(#50519,#50520,#50521,#50522,#50523,
#50524,#50525,#50526,#50527,#50528,#50529,#50530,#50531,#50532,#50533,#50534,
#50535,#50536,#50537,#50538,#50539,#50540,#50541,#50542,#50543,#50544,#50545,
#50546,#50547,#50548,#50549,#50550,#50551,#50552,#50553,#50554,#50555,#50556,
#50557,#50558,#50559,#50560,#50561,#50562,#50563,#50564,#50565,#50566,#50567,
#50568,#50569,#50570,#50571,#50572,#50573,#50574,#50575,#50576,#50577,#50578,
#50579,#50580,#50581,#50582,#50583,#50584,#50585,#50586,#50587,#50588,#50589,
#50590,#50591,#50592,#50593,#50594,#50595,#50596,#50597,#50598,#50599,#50600,
#50601,#50602,#50603,#50604,#50605,#50606,#50607,#50608,#50609,#50610,#50611,
#50612,#50613,#50614,#50615,#50616,#50617,#50618,#50619,#50620,#50621,#50622,
#50623,#50624,#50625,#50626,#50627,#50628,#50629,#50630,#50631,#50632,#50633,
#50634,#50635,#50636,#50637,#50638,#50639,#50640,#50641,#50642,#50643,#50644,
#50645,#50646,#50647,#50648,#50649,#50650,#50651,#50652,#50653,#50654,#50655,
#50656,#50657,#50658,#50659,#50660,#50661,#50662,#50663,#50664,#50665,#50666,
#50667,#50668,#50669,#50670,#50671,#50672,#50673,#50674,#50675),
 .UNSPECIFIED.,.F.,.F.,(4,3,3,3,3,3,3,3,3,3,3,3,3,3,3,3,3,3,3,3,3,3,3,3,
3,3,3,3,3,3,3,3,3,3,3,3,3,3,3,3,3,3,3,3,3,3,3,3,3,3,3,3,4),(229.336263712055,
229.418725918155,229.501187775958,229.583649292313,229.666110474071,229.748571328081,
229.831031861193,229.913492080256,229.995951992119,230.078411603631,230.16087092164,
230.243329952993,230.32578870454,230.408247183128,230.490705395604,230.573163348814,
230.655621049607,230.738078504829,230.820535721327,230.906548416613,230.989873215171,
231.072339820763,231.154805582146,231.237270526736,231.319734681944,231.402198075181,
231.484660733853,231.567122685364,231.649583957116,231.732044576509,231.81450457094,
231.896963967805,231.979422794495,232.061881078402,232.144338846915,232.226796127421,
232.310930242612,232.393396240972,232.475860617579,232.558323482074,232.64078494408,
232.7232451132,232.805704099016,232.888162011096,232.973759506019,233.056224243065,
233.138686015451,233.221145261616,233.303602419855,233.386064938937,233.468522610348,
233.550981401542,233.572941970479),.UNSPECIFIED.);
#3354=B_SPLINE_CURVE_WITH_KNOTS('',3,(#50681,#50682,#50683,#50684,#50685,
#50686,#50687,#50688,#50689,#50690,#50691,#50692,#50693,#50694,#50695,#50696,
#50697,#50698,#50699,#50700,#50701,#50702,#50703,#50704,#50705,#50706,#50707,
#50708,#50709,#50710,#50711,#50712,#50713,#50714,#50715,#50716,#50717,#50718,
#50719,#50720,#50721,#50722,#50723,#50724,#50725,#50726,#50727,#50728,#50729,
#50730,#50731,#50732,#50733,#50734,#50735,#50736,#50737,#50738,#50739,#50740,
#50741,#50742,#50743,#50744,#50745,#50746,#50747,#50748,#50749,#50750,#50751,
#50752,#50753,#50754,#50755,#50756,#50757,#50758,#50759,#50760,#50761,#50762,
#50763,#50764,#50765,#50766,#50767,#50768,#50769,#50770,#50771,#50772,#50773,
#50774,#50775,#50776,#50777,#50778,#50779,#50780,#50781,#50782,#50783,#50784,
#50785,#50786,#50787,#50788,#50789,#50790,#50791,#50792,#50793,#50794,#50795,
#50796,#50797,#50798,#50799,#50800,#50801,#50802,#50803,#50804,#50805,#50806,
#50807,#50808,#50809,#50810,#50811,#50812,#50813,#50814,#50815,#50816,#50817,
#50818,#50819,#50820,#50821,#50822,#50823,#50824,#50825,#50826,#50827,#50828,
#50829,#50830,#50831,#50832,#50833,#50834,#50835,#50836,#50837,#50838,#50839,
#50840,#50841,#50842,#50843,#50844,#50845,#50846,#50847,#50848,#50849),
 .UNSPECIFIED.,.F.,.F.,(4,3,3,3,3,3,3,3,3,3,3,3,3,3,3,3,3,3,3,3,3,3,3,3,
3,3,3,3,3,3,3,3,3,3,3,3,3,3,3,3,3,3,3,3,3,3,3,3,3,3,3,3,3,3,3,3,4),(235.619449019235,
235.719318537606,235.740792196703,235.819180575711,235.897502840153,235.975773389612,
236.054006586156,236.132216763833,236.210434899216,236.288660964436,236.366907945993,
236.445188840208,236.523562267962,236.601985266286,236.680524825476,236.738334578027,
236.814405855663,236.89038163211,236.966278689102,237.042113727915,237.117903388012,
237.195150084429,237.27091358269,237.346684414057,237.42247758189,237.500827426256,
237.576752189766,237.656314574559,237.735876959352,237.813447180295,237.890925320815,
237.968327034729,238.045667921024,238.122963534918,238.200236974532,238.277500209839,
238.354767277276,238.43205221278,238.509410215127,238.586805746184,238.664307412951,
238.733419340677,238.817631492138,238.901717519848,238.985598441794,239.069350227828,
239.152887875165,239.23219053134,239.309570297671,239.386968458714,239.464398801287,
239.54191609474,239.619483040714,239.697156332161,239.730961722002,239.81058672982,
239.856215740081),.UNSPECIFIED.);
#3355=B_SPLINE_CURVE_WITH_KNOTS('',3,(#50850,#50851,#50852,#50853,#50854,
#50855,#50856,#50857,#50858,#50859,#50860,#50861,#50862,#50863,#50864,#50865,
#50866,#50867,#50868,#50869,#50870,#50871,#50872,#50873,#50874,#50875,#50876,
#50877,#50878,#50879,#50880,#50881,#50882,#50883,#50884,#50885,#50886,#50887,
#50888,#50889,#50890,#50891,#50892,#50893,#50894,#50895,#50896,#50897,#50898,
#50899,#50900,#50901,#50902,#50903,#50904,#50905,#50906,#50907,#50908,#50909,
#50910,#50911,#50912,#50913,#50914,#50915,#50916,#50917,#50918,#50919,#50920,
#50921,#50922,#50923,#50924,#50925,#50926,#50927,#50928,#50929,#50930,#50931),
 .UNSPECIFIED.,.F.,.F.,(4,3,3,3,3,3,3,3,3,3,3,3,3,3,3,3,3,3,3,3,3,3,3,3,
3,3,3,4),(233.572971835991,233.652464355483,233.732024717962,233.745707434053,
233.822438012378,233.899101610745,233.975712911973,234.052287678688,234.128841008082,
234.205398406087,234.244478624715,234.329147616333,234.413962068381,234.498975386618,
234.584074802128,234.66929419066,234.743249815378,234.824806795004,234.906288643971,
234.990221734488,235.071548974518,235.156784990279,235.24202100604,235.318774721805,
235.395557004039,235.472352167508,235.549215192412,235.619449019133),
 .UNSPECIFIED.);
#3356=B_SPLINE_CURVE_WITH_KNOTS('',3,(#50933,#50934,#50935,#50936,#50937,
#50938,#50939,#50940,#50941,#50942,#50943,#50944,#50945,#50946,#50947,#50948,
#50949,#50950,#50951,#50952,#50953,#50954,#50955,#50956,#50957,#50958,#50959,
#50960,#50961,#50962,#50963,#50964,#50965,#50966,#50967,#50968,#50969,#50970,
#50971,#50972,#50973,#50974,#50975,#50976,#50977,#50978,#50979,#50980,#50981,
#50982,#50983,#50984,#50985,#50986,#50987,#50988,#50989,#50990,#50991,#50992,
#50993,#50994,#50995,#50996,#50997,#50998,#50999,#51000,#51001,#51002,#51003,
#51004,#51005,#51006,#51007,#51008),.UNSPECIFIED.,.F.,.F.,(4,3,3,3,3,3,
3,3,3,3,3,3,3,3,3,3,3,3,3,3,3,3,3,3,3,4),(233.572941970479,233.655403574209,
233.737864512061,233.820324811433,233.902784499722,233.98524360432,234.06770215262,
234.150160172013,234.232617689886,234.31929464797,234.401761433511,234.484226546579,
234.566690096827,234.649152193886,234.731612947368,234.814072466864,234.896530861949,
234.978988242183,235.061454627869,235.143917829377,235.226378285227,235.308836433781,
235.391302037535,235.473761915923,235.556226027175,235.619449019235),
 .UNSPECIFIED.);
#3357=B_SPLINE_CURVE_WITH_KNOTS('',3,(#51009,#51010,#51011,#51012,#51013,
#51014,#51015,#51016,#51017,#51018,#51019,#51020,#51021,#51022,#51023,#51024,
#51025,#51026,#51027,#51028,#51029,#51030,#51031,#51032,#51033,#51034,#51035,
#51036,#51037,#51038,#51039,#51040,#51041,#51042,#51043,#51044,#51045,#51046,
#51047,#51048,#51049,#51050,#51051,#51052,#51053,#51054,#51055,#51056,#51057,
#51058,#51059,#51060,#51061,#51062,#51063,#51064,#51065,#51066,#51067,#51068,
#51069,#51070,#51071,#51072,#51073,#51074,#51075,#51076,#51077,#51078,#51079,
#51080,#51081,#51082,#51083,#51084,#51085,#51086,#51087,#51088,#51089,#51090,
#51091,#51092,#51093,#51094,#51095,#51096,#51097,#51098,#51099,#51100,#51101,
#51102,#51103,#51104,#51105,#51106,#51107,#51108,#51109,#51110,#51111,#51112,
#51113,#51114,#51115,#51116,#51117,#51118,#51119,#51120,#51121,#51122,#51123,
#51124,#51125,#51126,#51127,#51128,#51129,#51130,#51131,#51132,#51133,#51134,
#51135,#51136,#51137,#51138,#51139,#51140,#51141,#51142,#51143,#51144,#51145,
#51146,#51147,#51148,#51149,#51150,#51151,#51152,#51153,#51154,#51155,#51156,
#51157,#51158,#51159,#51160,#51161,#51162,#51163,#51164,#51165,#51166,#51167,
#51168,#51169,#51170,#51171,#51172,#51173,#51174,#51175,#51176,#51177),
 .UNSPECIFIED.,.F.,.F.,(4,3,3,3,3,3,3,3,3,3,3,3,3,3,3,3,3,3,3,3,3,3,3,3,
3,3,3,3,3,3,3,3,3,3,3,3,3,3,3,3,3,3,3,3,3,3,3,3,3,3,3,3,3,3,3,3,4),(235.619449019235,
235.697995435465,235.776589771173,235.855293804889,235.934057908597,236.012948288771,
236.06206864592,236.141693833781,236.221246288657,236.300738310445,236.38018215246,
236.459590030358,236.53898046448,236.618362015229,236.697745753035,236.777142748366,
236.856593365491,236.93607238493,237.015624524582,237.059611027245,237.13634160557,
237.213005203937,237.289616505166,237.36619127188,237.442744601275,237.51930199928,
237.558382217907,237.643051209525,237.727865661573,237.81287897981,237.897978395319,
237.983197783851,238.05715340857,238.138710388197,238.220192237163,238.30412532768,
238.385452567711,238.470688583471,238.555924599232,238.63533579771,238.714765422258,
238.794224233208,238.873756056663,238.953329583092,239.032986707056,239.054695789895,
239.133091487211,239.211419106365,239.291963083862,239.370196668063,239.448409834818,
239.526615572052,239.608904410625,239.687159228354,239.765440135615,239.843782795569,
239.855770926344),.UNSPECIFIED.);
#3358=B_SPLINE_CURVE_WITH_KNOTS('',3,(#51183,#51184,#51185,#51186,#51187,
#51188,#51189,#51190,#51191,#51192,#51193,#51194,#51195,#51196,#51197,#51198,
#51199,#51200,#51201,#51202,#51203,#51204,#51205,#51206,#51207,#51208,#51209,
#51210,#51211,#51212,#51213,#51214,#51215,#51216,#51217,#51218,#51219,#51220,
#51221,#51222,#51223,#51224,#51225,#51226,#51227,#51228,#51229,#51230,#51231,
#51232,#51233,#51234,#51235,#51236,#51237,#51238,#51239,#51240,#51241,#51242,
#51243,#51244,#51245,#51246,#51247,#51248,#51249,#51250,#51251,#51252,#51253,
#51254,#51255,#51256,#51257,#51258,#51259,#51260,#51261,#51262,#51263,#51264,
#51265,#51266,#51267,#51268,#51269,#51270,#51271,#51272,#51273,#51274,#51275,
#51276,#51277,#51278,#51279,#51280,#51281,#51282,#51283,#51284,#51285,#51286,
#51287,#51288,#51289,#51290,#51291,#51292,#51293,#51294,#51295,#51296,#51297,
#51298,#51299,#51300,#51301,#51302,#51303,#51304,#51305,#51306,#51307,#51308,
#51309,#51310,#51311,#51312,#51313,#51314,#51315,#51316,#51317,#51318,#51319,
#51320,#51321,#51322,#51323,#51324,#51325,#51326,#51327,#51328,#51329,#51330,
#51331,#51332,#51333,#51334,#51335,#51336,#51337,#51338,#51339,#51340,#51341,
#51342,#51343,#51344,#51345,#51346,#51347,#51348),.UNSPECIFIED.,.F.,.F.,
(4,3,3,3,3,3,3,3,3,3,3,3,3,3,3,3,3,3,3,3,3,3,3,3,3,3,3,3,3,3,3,3,3,3,3,
3,3,3,3,3,3,3,3,3,3,3,3,3,3,3,3,3,3,3,3,4),(241.902634326415,241.98318016364,
242.062446252954,242.143631964134,242.224817675314,242.304228873793,242.383658498341,
242.463117309291,242.542649132746,242.622222659175,242.70187978314,242.723588865977,
242.801977244985,242.880299509428,242.958570058886,243.03680325543,243.115013433108,
243.193231568491,243.27145763371,243.349704615268,243.427985509483,243.506358937238,
243.584781935561,243.663321494752,243.721131247302,243.797202524938,243.873178301385,
243.949075358377,244.024910397189,244.100700057287,244.177946753704,244.253710251965,
244.329481083332,244.405274251165,244.48362409553,244.559548859041,244.639111243834,
244.718673628627,244.79624384957,244.87372199009,244.951123704003,245.028464590298,
245.105760204192,245.183033643806,245.260296879113,245.33756394655,245.414848882054,
245.4922068844,245.569602415457,245.647104082225,245.716216009951,245.800441773244,
245.885279409835,245.969191086817,246.054491703213,246.139792319609),
 .UNSPECIFIED.);
#3359=B_SPLINE_CURVE_WITH_KNOTS('',3,(#51349,#51350,#51351,#51352,#51353,
#51354,#51355,#51356,#51357,#51358,#51359,#51360,#51361,#51362,#51363,#51364,
#51365,#51366,#51367,#51368,#51369,#51370,#51371,#51372,#51373,#51374,#51375,
#51376,#51377,#51378,#51379,#51380,#51381,#51382,#51383,#51384,#51385,#51386,
#51387,#51388,#51389,#51390,#51391,#51392,#51393,#51394,#51395,#51396,#51397,
#51398,#51399,#51400,#51401,#51402,#51403,#51404,#51405,#51406,#51407,#51408,
#51409,#51410,#51411,#51412,#51413,#51414,#51415,#51416,#51417,#51418,#51419,
#51420,#51421,#51422,#51423,#51424,#51425,#51426,#51427),.UNSPECIFIED.,
 .F.,.F.,(4,3,3,3,3,3,3,3,3,3,3,3,3,3,3,3,3,3,3,3,3,3,3,3,3,3,4),(239.856215740081,
239.935732037462,240.015194933753,240.094616659583,240.17401425183,240.25339823729,
240.332779688537,240.412169675154,240.491611274401,240.57107694136,240.650622166768,
240.728504103327,240.805234681652,240.881898280019,240.958509581247,241.035084347962,
241.111637677356,241.188195075361,241.227275293989,241.311944285607,241.396758737655,
241.481772055892,241.566871471401,241.652090859933,241.726046484652,241.815739306581,
241.902634326327),.UNSPECIFIED.);
#3360=B_SPLINE_CURVE_WITH_KNOTS('',3,(#51429,#51430,#51431,#51432,#51433,
#51434,#51435,#51436,#51437,#51438,#51439,#51440,#51441,#51442,#51443,#51444,
#51445,#51446,#51447,#51448,#51449,#51450,#51451,#51452,#51453,#51454,#51455,
#51456,#51457,#51458,#51459,#51460,#51461,#51462,#51463,#51464,#51465,#51466,
#51467,#51468,#51469,#51470,#51471,#51472,#51473,#51474,#51475,#51476,#51477,
#51478,#51479,#51480,#51481,#51482,#51483,#51484,#51485,#51486,#51487,#51488,
#51489,#51490,#51491,#51492,#51493,#51494,#51495,#51496,#51497,#51498,#51499,
#51500,#51501,#51502,#51503,#51504,#51505,#51506,#51507,#51508,#51509,#51510),
 .UNSPECIFIED.,.F.,.F.,(4,3,3,3,3,3,3,3,3,3,3,3,3,3,3,3,3,3,3,3,3,3,3,3,
3,3,3,4),(239.855770926344,239.934207194177,240.012754847305,240.052238171219,
240.128309448855,240.204285225302,240.280182282294,240.356017321107,240.431806981204,
240.509053677621,240.584817175882,240.660588007249,240.736381175082,240.814731019448,
240.890655782958,240.970218167751,241.049780552544,241.126660567282,241.203448426267,
241.280160407913,241.357969647713,241.434577319922,241.511162590235,241.587740052588,
241.666463621019,241.743095422845,241.822864874578,241.902634326311),
 .UNSPECIFIED.);
#3361=B_SPLINE_CURVE_WITH_KNOTS('',3,(#51511,#51512,#51513,#51514,#51515,
#51516,#51517,#51518,#51519,#51520,#51521,#51522,#51523,#51524,#51525,#51526,
#51527,#51528,#51529,#51530,#51531,#51532,#51533,#51534,#51535,#51536,#51537,
#51538,#51539,#51540,#51541,#51542,#51543,#51544,#51545,#51546,#51547,#51548,
#51549,#51550,#51551,#51552,#51553,#51554,#51555,#51556,#51557,#51558,#51559,
#51560,#51561,#51562,#51563,#51564,#51565,#51566,#51567,#51568,#51569,#51570,
#51571,#51572,#51573,#51574,#51575,#51576,#51577,#51578,#51579,#51580,#51581,
#51582,#51583,#51584,#51585,#51586,#51587,#51588,#51589,#51590,#51591,#51592,
#51593,#51594,#51595,#51596,#51597,#51598,#51599,#51600,#51601,#51602,#51603,
#51604,#51605,#51606,#51607,#51608,#51609,#51610,#51611,#51612,#51613,#51614,
#51615,#51616,#51617,#51618,#51619,#51620,#51621,#51622,#51623,#51624,#51625,
#51626,#51627,#51628,#51629,#51630,#51631,#51632,#51633,#51634,#51635,#51636,
#51637,#51638,#51639,#51640,#51641,#51642,#51643,#51644,#51645,#51646,#51647,
#51648,#51649,#51650,#51651,#51652,#51653,#51654,#51655,#51656,#51657,#51658,
#51659,#51660,#51661,#51662,#51663,#51664,#51665,#51666,#51667,#51668,#51669,
#51670,#51671,#51672,#51673,#51674,#51675,#51676,#51677,#51678,#51679),
 .UNSPECIFIED.,.F.,.F.,(4,3,3,3,3,3,3,3,3,3,3,3,3,3,3,3,3,3,3,3,3,3,3,3,
3,3,3,3,3,3,3,3,3,3,3,3,3,3,3,3,3,3,3,3,3,3,3,3,3,3,3,3,3,3,3,3,4),(241.902634326414,
242.015184170787,242.047322933869,242.131535085329,242.215621113039,242.299502034985,
242.383253821019,242.466791468355,242.546094124532,242.623473890863,242.700872051906,
242.778302394478,242.855819687931,242.933386633905,243.011059925353,243.044865315194,
243.124490503055,243.204042957931,243.283534979719,243.362978821734,243.442386699632,
243.521777133754,243.601158684503,243.680542422309,243.759939417639,243.839390034765,
243.918869054203,243.998421193856,244.042407696519,244.119138274844,244.195801873211,
244.272413174439,244.348987941154,244.425541270549,244.502098668554,244.541178887181,
244.625847878799,244.710662330847,244.795675649084,244.880775064593,244.965994453125,
245.039950077844,245.12150705747,245.202988906437,245.286921996954,245.368249236984,
245.453485252745,245.538721268506,245.618132466985,245.697562091533,245.777020902483,
245.856552725938,245.936126252367,246.015783376331,246.037492459169,246.115887536402,
246.139534544986),.UNSPECIFIED.);
#3362=B_SPLINE_CURVE_WITH_KNOTS('',3,(#51685,#51686,#51687,#51688,#51689,
#51690,#51691,#51692,#51693,#51694,#51695,#51696,#51697,#51698,#51699,#51700,
#51701,#51702,#51703,#51704,#51705,#51706,#51707,#51708,#51709,#51710,#51711,
#51712,#51713,#51714,#51715,#51716,#51717,#51718,#51719,#51720,#51721,#51722,
#51723,#51724,#51725,#51726,#51727,#51728,#51729,#51730,#51731,#51732,#51733,
#51734,#51735,#51736,#51737,#51738,#51739,#51740,#51741,#51742,#51743,#51744,
#51745,#51746,#51747,#51748,#51749,#51750,#51751,#51752,#51753,#51754,#51755,
#51756,#51757,#51758,#51759,#51760,#51761,#51762,#51763,#51764,#51765,#51766,
#51767,#51768,#51769,#51770,#51771,#51772,#51773,#51774,#51775,#51776,#51777,
#51778,#51779,#51780,#51781,#51782,#51783,#51784,#51785,#51786,#51787,#51788,
#51789,#51790,#51791,#51792,#51793,#51794,#51795,#51796,#51797,#51798,#51799,
#51800,#51801,#51802,#51803,#51804,#51805,#51806,#51807,#51808,#51809,#51810,
#51811,#51812,#51813,#51814,#51815,#51816,#51817,#51818,#51819,#51820,#51821,
#51822,#51823,#51824,#51825,#51826,#51827,#51828,#51829,#51830,#51831,#51832,
#51833,#51834,#51835,#51836,#51837,#51838,#51839,#51840,#51841,#51842,#51843,
#51844,#51845,#51846,#51847,#51848,#51849,#51850,#51851,#51852,#51853),
 .UNSPECIFIED.,.F.,.F.,(4,3,3,3,3,3,3,3,3,3,3,3,3,3,3,3,3,3,3,3,3,3,3,3,
3,3,3,3,3,3,3,3,3,3,3,3,3,3,3,3,3,3,3,3,3,3,3,3,3,3,3,3,3,3,3,3,4),(248.185819633594,
248.210071963264,248.294740954883,248.379555406932,248.46456872517,248.54966814068,
248.634887529213,248.708843153926,248.790400133552,248.871881982518,248.955815073036,
249.037142313065,249.122378328827,249.207614344589,249.287025543068,249.366455167616,
249.445913978566,249.525445802022,249.605019328451,249.684676452415,249.706385535251,
249.784773914259,249.863096178701,249.94136672816,250.019599924704,250.097810102381,
250.176028237764,250.254254302983,250.332501284541,250.410782178755,250.48915560651,
250.567578604833,250.646118164024,250.703927916576,250.779999194212,250.855974970659,
250.931872027651,251.007707066464,251.083496726561,251.160743422979,251.23650692124,
251.312277752606,251.38807092044,251.466420764805,251.542345528316,251.621907913108,
251.701470297901,251.779057283285,251.859412540702,251.936804083104,252.014139407901,
252.091432606192,252.168697742376,252.245959341539,252.323219410462,252.40050714282,
252.421899342621),.UNSPECIFIED.);
#3363=B_SPLINE_CURVE_WITH_KNOTS('',3,(#51854,#51855,#51856,#51857,#51858,
#51859,#51860,#51861,#51862,#51863,#51864,#51865,#51866,#51867,#51868,#51869,
#51870,#51871,#51872,#51873,#51874,#51875,#51876,#51877,#51878,#51879,#51880,
#51881,#51882,#51883,#51884,#51885,#51886,#51887,#51888,#51889,#51890,#51891,
#51892,#51893,#51894,#51895,#51896,#51897,#51898,#51899,#51900,#51901,#51902,
#51903,#51904,#51905,#51906,#51907,#51908,#51909,#51910,#51911,#51912,#51913,
#51914,#51915,#51916,#51917,#51918,#51919,#51920,#51921,#51922,#51923,#51924,
#51925,#51926,#51927,#51928,#51929,#51930,#51931,#51932,#51933,#51934,#51935,
#51936,#51937,#51938),.UNSPECIFIED.,.F.,.F.,(4,3,3,3,3,3,3,3,3,3,3,3,3,
3,3,3,3,3,3,3,3,3,3,3,3,3,3,3,4),(246.139792319609,246.214987200614,246.292366966945,
246.369765127988,246.447195470561,246.524712764014,246.602279709988,246.679953001435,
246.713758391276,246.793383579137,246.872936034014,246.952428055801,247.031871897816,
247.111279775714,247.190670209836,247.270051760585,247.349435498391,247.428832493721,
247.508283110847,247.587762130286,247.667314269938,247.711300772601,247.788353016447,
247.865335961784,247.945456879711,248.022341303414,248.099202416832,248.176058884343,
248.185819633493),.UNSPECIFIED.);
#3364=B_SPLINE_CURVE_WITH_KNOTS('',3,(#51940,#51941,#51942,#51943,#51944,
#51945,#51946,#51947,#51948,#51949,#51950,#51951,#51952,#51953,#51954,#51955,
#51956,#51957,#51958,#51959,#51960,#51961,#51962,#51963,#51964,#51965,#51966,
#51967,#51968,#51969,#51970,#51971,#51972,#51973,#51974,#51975,#51976,#51977,
#51978,#51979,#51980,#51981,#51982,#51983,#51984,#51985,#51986,#51987,#51988,
#51989,#51990,#51991,#51992,#51993,#51994,#51995,#51996,#51997,#51998,#51999,
#52000,#52001,#52002,#52003,#52004,#52005,#52006,#52007,#52008,#52009,#52010,
#52011,#52012,#52013,#52014,#52015,#52016,#52017,#52018),.UNSPECIFIED.,
 .F.,.F.,(4,3,3,3,3,3,3,3,3,3,3,3,3,3,3,3,3,3,3,3,3,3,3,3,3,3,4),(246.139534544986,
246.217839679845,246.296097439495,246.374322176552,246.452528218451,246.53074737945,
246.608978389857,246.687234238348,246.765527925682,246.84391506779,246.922355332936,
247.000905501758,247.035034840494,247.11110611813,247.187081894577,247.262978951569,
247.338813990382,247.414603650479,247.491850346897,247.567613845157,247.643384676524,
247.719177844357,247.797527688723,247.873452452233,247.953014837026,248.032577221819,
248.185819633594),.UNSPECIFIED.);
#3365=B_SPLINE_CURVE_WITH_KNOTS('',3,(#52019,#52020,#52021,#52022,#52023,
#52024,#52025,#52026,#52027,#52028,#52029,#52030,#52031,#52032,#52033,#52034,
#52035,#52036,#52037,#52038,#52039,#52040,#52041,#52042,#52043,#52044,#52045,
#52046,#52047,#52048,#52049,#52050,#52051,#52052,#52053,#52054,#52055,#52056,
#52057,#52058,#52059,#52060,#52061,#52062,#52063,#52064,#52065,#52066,#52067,
#52068,#52069,#52070,#52071,#52072,#52073,#52074,#52075,#52076,#52077,#52078,
#52079,#52080,#52081,#52082,#52083,#52084,#52085,#52086,#52087,#52088,#52089,
#52090,#52091,#52092,#52093,#52094,#52095,#52096,#52097,#52098,#52099,#52100,
#52101,#52102,#52103,#52104,#52105,#52106,#52107,#52108,#52109,#52110,#52111,
#52112,#52113,#52114,#52115,#52116,#52117,#52118,#52119,#52120,#52121,#52122,
#52123,#52124,#52125,#52126,#52127,#52128,#52129,#52130,#52131,#52132,#52133,
#52134,#52135,#52136,#52137,#52138,#52139,#52140,#52141,#52142,#52143,#52144,
#52145,#52146,#52147,#52148,#52149,#52150,#52151,#52152,#52153,#52154,#52155,
#52156,#52157,#52158,#52159,#52160,#52161,#52162,#52163,#52164,#52165,#52166,
#52167,#52168,#52169,#52170,#52171,#52172,#52173,#52174,#52175,#52176,#52177,
#52178,#52179,#52180,#52181,#52182,#52183,#52184),.UNSPECIFIED.,.F.,.F.,
(4,3,3,3,3,3,3,3,3,3,3,3,3,3,3,3,3,3,3,3,3,3,3,3,3,3,3,3,3,3,3,3,3,3,3,
3,3,3,3,3,3,3,3,3,3,3,3,3,3,3,3,3,3,3,3,4),(248.185819633673,248.261727296346,
248.337557347104,248.413326582018,248.490425709659,248.566130909788,248.641829363112,
248.717536151477,248.795682014394,248.87148595455,248.950802778847,249.030119603143,
249.114331754604,249.198417782314,249.28229870426,249.366050490294,249.449588137631,
249.528890793806,249.606270560137,249.68366872118,249.761099063753,249.838616357206,
249.91618330318,249.993856594627,250.027661984468,250.107287172329,250.186839627206,
250.266331648994,250.345775491009,250.425183368907,250.50457380303,250.583955353779,
250.663339091584,250.742736086915,250.82218670404,250.901665723479,250.981217863132,
251.025204365793,251.101934944118,251.178598542485,251.255209843713,251.331784610428,
251.408337939822,251.484895337827,251.523975556456,251.608644548074,251.693459000123,
251.778472318361,251.863571733871,251.948791122404,252.022746747118,252.104313318822,
252.185777478726,252.267178306333,252.348500730148,252.422903338315),
 .UNSPECIFIED.);
#3366=B_SPLINE_CURVE_WITH_KNOTS('',3,(#52190,#52191,#52192,#52193,#52194,
#52195,#52196,#52197,#52198,#52199,#52200,#52201,#52202,#52203,#52204,#52205,
#52206,#52207,#52208,#52209,#52210,#52211,#52212,#52213,#52214,#52215,#52216,
#52217,#52218,#52219,#52220,#52221,#52222,#52223,#52224,#52225,#52226,#52227,
#52228,#52229,#52230,#52231,#52232,#52233,#52234,#52235,#52236,#52237,#52238,
#52239,#52240,#52241,#52242,#52243,#52244,#52245,#52246,#52247,#52248,#52249,
#52250,#52251,#52252,#52253,#52254,#52255,#52256,#52257,#52258,#52259,#52260,
#52261,#52262,#52263,#52264,#52265,#52266,#52267,#52268,#52269,#52270,#52271,
#52272,#52273,#52274,#52275,#52276,#52277,#52278,#52279,#52280,#52281,#52282,
#52283,#52284,#52285,#52286,#52287,#52288,#52289,#52290,#52291,#52292,#52293,
#52294,#52295,#52296,#52297,#52298,#52299,#52300,#52301,#52302,#52303,#52304,
#52305,#52306,#52307,#52308,#52309,#52310,#52311,#52312,#52313,#52314,#52315,
#52316,#52317,#52318,#52319,#52320,#52321,#52322,#52323,#52324,#52325,#52326,
#52327,#52328,#52329,#52330,#52331,#52332,#52333,#52334,#52335,#52336,#52337,
#52338,#52339,#52340,#52341,#52342,#52343,#52344,#52345,#52346),
 .UNSPECIFIED.,.F.,.F.,(4,3,3,3,3,3,3,3,3,3,3,3,3,3,3,3,3,3,3,3,3,3,3,3,
3,3,3,3,3,3,3,3,3,3,3,3,3,3,3,3,3,3,3,3,3,3,3,3,3,3,3,3,4),(254.469004947998,
254.551467154099,254.633929011901,254.716390528256,254.798851710014,254.881312564024,
254.963773097136,255.046233316199,255.128693228062,255.211152839574,255.293612157583,
255.376071188936,255.458529940483,255.540988419071,255.623446631547,255.705904584757,
255.788362285551,255.870819740773,255.95327695727,256.03928965233,256.12261445067,
256.205081056261,256.287546817645,256.370011762234,256.452475917442,256.534939310679,
256.617401969351,256.699863920862,256.782325192614,256.864785812007,256.947245806438,
257.029705203302,257.112164029992,257.194622313899,257.277080082412,257.359537362919,
257.443671477686,257.526137476046,257.608601852652,257.691064717147,257.773526179154,
257.855986348273,257.938445334089,258.020903246169,258.106500740298,258.188965477343,
258.271427249729,258.353886495894,258.436343654133,258.518806173215,258.601263844626,
258.683722635818,258.705683199198),.UNSPECIFIED.);
#3367=B_SPLINE_CURVE_WITH_KNOTS('',3,(#52347,#52348,#52349,#52350,#52351,
#52352,#52353,#52354,#52355,#52356,#52357,#52358,#52359,#52360,#52361,#52362,
#52363,#52364,#52365,#52366,#52367,#52368,#52369,#52370,#52371,#52372,#52373,
#52374,#52375,#52376,#52377,#52378,#52379,#52380,#52381,#52382,#52383,#52384,
#52385,#52386,#52387,#52388,#52389,#52390,#52391,#52392,#52393,#52394,#52395,
#52396,#52397,#52398,#52399,#52400,#52401,#52402,#52403,#52404,#52405,#52406,
#52407,#52408,#52409,#52410,#52411,#52412,#52413,#52414,#52415,#52416,#52417,
#52418,#52419,#52420,#52421,#52422,#52423,#52424,#52425,#52426,#52427,#52428),
 .UNSPECIFIED.,.F.,.F.,(4,3,3,3,3,3,3,3,3,3,3,3,3,3,3,3,3,3,3,3,3,3,3,3,
3,3,3,4),(252.421899342621,252.49926775373,252.576677654447,252.654187664594,
252.699012679226,252.783224830687,252.867310858397,252.951191780343,253.034943566377,
253.118481213714,253.197783869888,253.275163636219,253.352561797262,253.429992139835,
253.507509433288,253.585076379262,253.662749670709,253.696555060551,253.775214607533,
253.853797534827,253.932306748353,254.010773496424,254.089210548492,254.167630654032,
254.246065414596,254.324505545484,254.402994321971,254.468741656967),
 .UNSPECIFIED.);
#3368=B_SPLINE_CURVE_WITH_KNOTS('',3,(#52430,#52431,#52432,#52433,#52434,
#52435,#52436,#52437,#52438,#52439,#52440,#52441,#52442,#52443,#52444,#52445,
#52446,#52447,#52448,#52449,#52450,#52451,#52452,#52453,#52454,#52455,#52456,
#52457,#52458,#52459,#52460,#52461,#52462,#52463,#52464,#52465,#52466,#52467,
#52468,#52469,#52470,#52471,#52472,#52473,#52474,#52475,#52476,#52477,#52478,
#52479,#52480,#52481,#52482,#52483,#52484,#52485,#52486,#52487,#52488,#52489,
#52490,#52491,#52492,#52493,#52494,#52495,#52496,#52497,#52498,#52499,#52500,
#52501,#52502,#52503,#52504,#52505,#52506,#52507,#52508,#52509,#52510,#52511,
#52512,#52513,#52514),.UNSPECIFIED.,.F.,.F.,(4,3,3,3,3,3,3,3,3,3,3,3,3,
3,3,3,3,3,3,3,3,3,3,3,3,3,3,3,4),(252.422903338315,252.504122891163,252.521517937781,
252.60092913626,252.680358760809,252.759817571759,252.839349395215,252.918922921644,
252.998580045609,253.020289128443,253.098677507451,253.176999771893,253.255270321351,
253.333503517895,253.411713695572,253.489931830955,253.568157896175,253.646404877732,
253.724685771947,253.803059199701,253.881482198025,253.960021757215,254.017831509768,
254.099160682654,254.18032212957,254.261253618944,254.342049835182,254.422661110171,
254.469004940773),.UNSPECIFIED.);
#3369=B_SPLINE_CURVE_WITH_KNOTS('',3,(#52515,#52516,#52517,#52518,#52519,
#52520,#52521,#52522,#52523,#52524,#52525,#52526,#52527,#52528,#52529,#52530,
#52531,#52532,#52533,#52534,#52535,#52536,#52537,#52538,#52539,#52540,#52541,
#52542,#52543,#52544,#52545,#52546,#52547,#52548,#52549,#52550,#52551,#52552,
#52553,#52554,#52555,#52556,#52557,#52558,#52559,#52560,#52561,#52562,#52563,
#52564,#52565,#52566,#52567,#52568,#52569,#52570,#52571,#52572,#52573,#52574,
#52575,#52576,#52577,#52578,#52579,#52580,#52581,#52582,#52583,#52584,#52585,
#52586,#52587,#52588,#52589,#52590,#52591,#52592,#52593,#52594,#52595,#52596,
#52597,#52598,#52599,#52600,#52601,#52602,#52603,#52604,#52605,#52606,#52607,
#52608,#52609,#52610,#52611,#52612,#52613,#52614,#52615,#52616,#52617,#52618,
#52619,#52620,#52621,#52622,#52623,#52624,#52625,#52626,#52627,#52628,#52629,
#52630,#52631,#52632,#52633,#52634,#52635,#52636,#52637,#52638,#52639,#52640,
#52641,#52642,#52643,#52644,#52645,#52646,#52647,#52648,#52649,#52650,#52651,
#52652,#52653,#52654,#52655,#52656,#52657,#52658,#52659,#52660,#52661,#52662,
#52663,#52664,#52665,#52666,#52667,#52668,#52669,#52670,#52671),
 .UNSPECIFIED.,.F.,.F.,(4,3,3,3,3,3,3,3,3,3,3,3,3,3,3,3,3,3,3,3,3,3,3,3,
3,3,3,3,3,3,3,3,3,3,3,3,3,3,3,3,3,3,3,3,3,3,3,3,3,3,3,3,4),(254.469004940774,
254.551467146874,254.633929004677,254.716390521032,254.79885170279,254.8813125568,
254.963773089912,255.046233308975,255.128693220838,255.21115283235,255.293612150359,
255.376071181713,255.45852993326,255.540988411847,255.623446624323,255.705904577533,
255.788362278326,255.870819733548,255.953276950046,256.039289645332,256.12261444389,
256.205081049482,256.287546810865,256.370011755455,256.452475910663,256.5349393039,
256.617401962571,256.699863914082,256.782325185835,256.864785805228,256.947245799659,
257.029705196523,257.112164023213,257.194622307121,257.277080075634,257.35953735614,
257.443671471331,257.526137469691,257.608601846297,257.691064710793,257.773526172799,
257.855986341918,257.938445327734,258.020903239815,258.106500734737,258.188965471783,
258.27142724417,258.353886490335,258.436343648574,258.518806167656,258.601263839067,
258.68372263026,258.705683199198),.UNSPECIFIED.);
#3370=B_SPLINE_CURVE_WITH_KNOTS('',3,(#52677,#52678,#52679,#52680,#52681,
#52682,#52683,#52684,#52685,#52686,#52687,#52688,#52689,#52690,#52691,#52692,
#52693,#52694,#52695,#52696,#52697,#52698,#52699,#52700,#52701,#52702,#52703,
#52704,#52705,#52706,#52707,#52708,#52709,#52710,#52711,#52712,#52713,#52714,
#52715,#52716,#52717,#52718,#52719,#52720,#52721,#52722,#52723,#52724,#52725,
#52726,#52727,#52728,#52729,#52730,#52731,#52732,#52733,#52734,#52735,#52736,
#52737,#52738,#52739,#52740,#52741,#52742,#52743,#52744,#52745,#52746,#52747,
#52748,#52749,#52750,#52751,#52752,#52753,#52754,#52755,#52756,#52757,#52758,
#52759,#52760,#52761,#52762,#52763,#52764,#52765,#52766,#52767,#52768,#52769,
#52770,#52771,#52772,#52773,#52774,#52775,#52776,#52777,#52778,#52779,#52780,
#52781,#52782,#52783,#52784,#52785,#52786,#52787,#52788,#52789,#52790,#52791,
#52792,#52793,#52794,#52795,#52796,#52797,#52798,#52799,#52800,#52801,#52802,
#52803,#52804,#52805,#52806,#52807,#52808,#52809,#52810,#52811,#52812,#52813,
#52814,#52815,#52816,#52817,#52818,#52819,#52820,#52821,#52822,#52823,#52824,
#52825,#52826,#52827,#52828,#52829,#52830,#52831,#52832,#52833,#52834,#52835,
#52836,#52837,#52838,#52839,#52840,#52841,#52842,#52843,#52844,#52845),
 .UNSPECIFIED.,.F.,.F.,(4,3,3,3,3,3,3,3,3,3,3,3,3,3,3,3,3,3,3,3,3,3,3,3,
3,3,3,3,3,3,3,3,3,3,3,3,3,3,3,3,3,3,3,3,3,3,3,3,3,3,3,3,3,3,3,3,4),(260.752196538802,
260.830967913365,260.909662513798,260.988294308136,261.066877218579,261.145427802033,
261.223961216436,261.302490027466,261.381026795821,261.459615390821,261.538230451882,
261.616925325411,261.67689411115,261.753624689475,261.830288287842,261.906899589071,
261.983474355786,262.06002768518,262.136585083185,262.175665301812,262.26033429343,
262.345148745477,262.430162063714,262.515261479224,262.600480867756,262.674436492475,
262.755993472102,262.837475321068,262.921408411586,263.002735651616,263.087971667376,
263.173207683137,263.252618881615,263.332048506163,263.411507317113,263.491039140568,
263.570612666997,263.650269790961,263.6719788738,263.750367252808,263.82868951725,
263.906960066709,263.985193263253,264.06340344093,264.141621576313,264.219847641533,
264.29809462309,264.376375517305,264.454748945059,264.533171943383,264.611711502573,
264.669521255124,264.74957128564,264.825540665302,264.901440764819,264.977274285402,
264.989721377187),.UNSPECIFIED.);
#3371=B_SPLINE_CURVE_WITH_KNOTS('',3,(#52846,#52847,#52848,#52849,#52850,
#52851,#52852,#52853,#52854,#52855,#52856,#52857,#52858,#52859,#52860,#52861,
#52862,#52863,#52864,#52865,#52866,#52867,#52868,#52869,#52870,#52871,#52872,
#52873,#52874,#52875,#52876,#52877,#52878,#52879,#52880,#52881,#52882,#52883,
#52884,#52885,#52886,#52887,#52888,#52889,#52890,#52891,#52892,#52893,#52894,
#52895,#52896,#52897,#52898,#52899,#52900,#52901,#52902,#52903,#52904,#52905,
#52906,#52907,#52908,#52909,#52910,#52911,#52912,#52913,#52914,#52915,#52916,
#52917,#52918,#52919,#52920,#52921),.UNSPECIFIED.,.F.,.F.,(4,3,3,3,3,3,
3,3,3,3,3,3,3,3,3,3,3,3,3,3,3,3,3,3,3,4),(258.705683199198,258.788144802928,
258.87060574078,258.953066040152,259.03552572844,259.117984833038,259.200443381339,
259.282901400731,259.365358918604,259.452035876688,259.534502662229,259.616967775297,
259.699431325545,259.781893422604,259.864354176086,259.946813695582,260.029272090667,
260.111729470901,260.194195856587,260.276659058095,260.359119513945,260.4415776625,
260.524043266253,260.606503144641,260.688967255893,260.752190247953),
 .UNSPECIFIED.);
#3372=B_SPLINE_CURVE_WITH_KNOTS('',3,(#52923,#52924,#52925,#52926,#52927,
#52928,#52929,#52930,#52931,#52932,#52933,#52934,#52935,#52936,#52937,#52938,
#52939,#52940,#52941,#52942,#52943,#52944,#52945,#52946,#52947,#52948,#52949,
#52950,#52951,#52952,#52953,#52954,#52955,#52956,#52957,#52958,#52959,#52960,
#52961,#52962,#52963,#52964,#52965,#52966,#52967,#52968,#52969,#52970,#52971,
#52972,#52973,#52974,#52975,#52976,#52977,#52978,#52979,#52980,#52981,#52982,
#52983,#52984,#52985,#52986,#52987,#52988,#52989,#52990,#52991,#52992,#52993,
#52994,#52995,#52996,#52997,#52998),.UNSPECIFIED.,.F.,.F.,(4,3,3,3,3,3,
3,3,3,3,3,3,3,3,3,3,3,3,3,3,3,3,3,3,3,4),(258.705683199198,258.788144802928,
258.87060574078,258.953066040152,259.03552572844,259.117984833038,259.200443381339,
259.282901400731,259.365358918604,259.452035876688,259.534502662229,259.616967775297,
259.699431325545,259.781893422605,259.864354176086,259.946813695582,260.029272090667,
260.111729470901,260.194195856587,260.276659058095,260.359119513945,260.441577662499,
260.524043266253,260.606503144641,260.688967255893,260.752190247953),
 .UNSPECIFIED.);
#3373=B_SPLINE_CURVE_WITH_KNOTS('',3,(#52999,#53000,#53001,#53002,#53003,
#53004,#53005,#53006,#53007,#53008,#53009,#53010,#53011,#53012,#53013,#53014,
#53015,#53016,#53017,#53018,#53019,#53020,#53021,#53022,#53023,#53024,#53025,
#53026,#53027,#53028,#53029,#53030,#53031,#53032,#53033,#53034,#53035,#53036,
#53037,#53038,#53039,#53040,#53041,#53042,#53043,#53044,#53045,#53046,#53047,
#53048,#53049,#53050,#53051,#53052,#53053,#53054,#53055,#53056,#53057,#53058,
#53059,#53060,#53061,#53062,#53063,#53064,#53065,#53066,#53067,#53068,#53069,
#53070,#53071,#53072,#53073,#53074,#53075,#53076,#53077,#53078,#53079,#53080,
#53081,#53082,#53083,#53084,#53085,#53086,#53087,#53088,#53089,#53090,#53091,
#53092,#53093,#53094,#53095,#53096,#53097,#53098,#53099,#53100,#53101,#53102,
#53103,#53104,#53105,#53106,#53107,#53108,#53109,#53110,#53111,#53112,#53113,
#53114,#53115,#53116,#53117,#53118,#53119,#53120,#53121,#53122,#53123,#53124,
#53125,#53126,#53127,#53128,#53129,#53130,#53131,#53132,#53133,#53134,#53135,
#53136,#53137,#53138,#53139,#53140,#53141,#53142,#53143,#53144,#53145,#53146,
#53147,#53148,#53149,#53150,#53151,#53152,#53153,#53154,#53155,#53156,#53157,
#53158,#53159,#53160,#53161,#53162,#53163,#53164),.UNSPECIFIED.,.F.,.F.,
(4,3,3,3,3,3,3,3,3,3,3,3,3,3,3,3,3,3,3,3,3,3,3,3,3,3,3,3,3,3,3,3,3,3,3,
3,3,3,3,3,3,3,3,3,3,3,3,3,3,3,3,3,3,3,3,4),(260.752190247953,260.861381773017,
260.975984016104,261.000628179042,261.076699456678,261.152675233125,261.228572290117,
261.30440732893,261.380196989027,261.457443685445,261.533207183705,261.608978015072,
261.684771182906,261.763121027271,261.839045790782,261.918608175574,261.998170560367,
262.07574078131,262.15321892183,262.230620635743,262.307961522038,262.385257135933,
262.462530575547,262.539793810854,262.61706087829,262.694345813794,262.771703816141,
262.849099347198,262.926601013965,262.995712941692,263.079925093153,263.164011120863,
263.247892042809,263.331643828844,263.41518147618,263.494484132354,263.571863898685,
263.649262059728,263.726692402301,263.804209695754,263.881776641728,263.959449933175,
263.993255323017,264.072880574431,264.152433079837,264.231925139183,264.31136900583,
264.390776895467,264.470167265223,264.549548734105,264.628932372527,264.708329250924,
264.787779482255,264.867258113544,264.946809269139,264.989216780594),
 .UNSPECIFIED.);
#3374=B_SPLINE_CURVE_WITH_KNOTS('',3,(#53170,#53171,#53172,#53173,#53174,
#53175,#53176,#53177,#53178,#53179,#53180,#53181,#53182,#53183,#53184,#53185,
#53186,#53187,#53188,#53189,#53190,#53191,#53192,#53193,#53194,#53195,#53196,
#53197,#53198,#53199,#53200,#53201,#53202,#53203,#53204,#53205,#53206,#53207,
#53208,#53209,#53210,#53211,#53212,#53213,#53214,#53215,#53216,#53217,#53218,
#53219,#53220,#53221,#53222,#53223,#53224,#53225,#53226,#53227,#53228,#53229,
#53230,#53231,#53232,#53233,#53234,#53235,#53236,#53237,#53238,#53239,#53240,
#53241,#53242,#53243,#53244,#53245,#53246,#53247,#53248,#53249,#53250,#53251,
#53252,#53253,#53254,#53255,#53256,#53257,#53258,#53259,#53260,#53261,#53262,
#53263,#53264,#53265,#53266,#53267,#53268,#53269,#53270,#53271,#53272,#53273,
#53274,#53275,#53276,#53277,#53278,#53279,#53280,#53281,#53282,#53283,#53284,
#53285,#53286,#53287,#53288,#53289,#53290,#53291,#53292,#53293,#53294,#53295,
#53296,#53297,#53298,#53299,#53300,#53301,#53302,#53303,#53304,#53305,#53306,
#53307,#53308,#53309,#53310,#53311,#53312,#53313,#53314,#53315,#53316,#53317,
#53318,#53319,#53320,#53321,#53322,#53323,#53324,#53325,#53326,#53327,#53328,
#53329,#53330,#53331,#53332,#53333,#53334,#53335,#53336,#53337,#53338),
 .UNSPECIFIED.,.F.,.F.,(4,3,3,3,3,3,3,3,3,3,3,3,3,3,3,3,3,3,3,3,3,3,3,3,
3,3,3,3,3,3,3,3,3,3,3,3,3,3,3,3,3,3,3,3,3,3,3,3,3,3,3,3,3,3,3,3,4),(267.035375555133,
267.111715052275,267.163377208437,267.240756974768,267.318155135812,267.395585478384,
267.473102771837,267.550669717811,267.628343009258,267.662148399099,267.74177358696,
267.821326041836,267.900818063625,267.98026190564,268.059669783537,268.139060217659,
268.218441768408,268.297825506214,268.377222501545,268.45667311867,268.536152138109,
268.615704277761,268.659690780424,268.73642135875,268.813084957116,268.889696258344,
268.966271025059,269.042824354454,269.119381752459,269.158461971086,269.243130962704,
269.327945414752,269.412958732989,269.498058148498,269.58327753703,269.657233161749,
269.738790141376,269.820271990342,269.904205080859,269.985532320889,270.07076833665,
270.156004352411,270.23541555089,270.314845175438,270.394303986388,270.473835809843,
270.553409336272,270.633066460236,270.654775543074,270.733157031107,270.811476038419,
270.889745625621,270.967978821928,271.046197558055,271.124405445832,271.202637380801,
271.271644794101),.UNSPECIFIED.);
#3375=B_SPLINE_CURVE_WITH_KNOTS('',3,(#53339,#53340,#53341,#53342,#53343,
#53344,#53345,#53346,#53347,#53348,#53349,#53350,#53351,#53352,#53353,#53354,
#53355,#53356,#53357,#53358,#53359,#53360,#53361,#53362,#53363,#53364,#53365,
#53366,#53367,#53368,#53369,#53370,#53371,#53372,#53373,#53374,#53375,#53376,
#53377,#53378,#53379,#53380,#53381,#53382,#53383,#53384,#53385,#53386,#53387,
#53388,#53389,#53390,#53391,#53392,#53393,#53394,#53395,#53396,#53397,#53398,
#53399,#53400,#53401,#53402,#53403,#53404,#53405,#53406,#53407,#53408,#53409,
#53410,#53411,#53412,#53413,#53414,#53415,#53416,#53417,#53418,#53419,#53420),
 .UNSPECIFIED.,.F.,.F.,(4,3,3,3,3,3,3,3,3,3,3,3,3,3,3,3,3,3,3,3,3,3,3,3,
3,3,3,4),(264.989721377187,265.065503395217,265.141271860983,265.217035617893,
265.292809664754,265.368609007136,265.444496684426,265.520429859431,265.596486860221,
265.667063636449,265.744633857392,265.822111997912,265.899513711826,265.976854598122,
266.054150212016,266.13142365163,266.208686886937,266.285953954373,266.363238889877,
266.440596892224,266.517992423281,266.595494090048,266.664606017774,266.757298402093,
266.84637076419,266.93517428811,267.023523487286,267.035375555049),
 .UNSPECIFIED.);
#3376=B_SPLINE_CURVE_WITH_KNOTS('',3,(#53422,#53423,#53424,#53425,#53426,
#53427,#53428,#53429,#53430,#53431,#53432,#53433,#53434,#53435,#53436,#53437,
#53438,#53439,#53440,#53441,#53442,#53443,#53444,#53445,#53446,#53447,#53448,
#53449,#53450,#53451,#53452,#53453,#53454,#53455,#53456,#53457,#53458,#53459,
#53460,#53461,#53462,#53463,#53464,#53465,#53466,#53467,#53468,#53469,#53470,
#53471,#53472,#53473,#53474,#53475,#53476,#53477,#53478,#53479,#53480,#53481,
#53482,#53483,#53484,#53485,#53486,#53487,#53488,#53489,#53490,#53491,#53492,
#53493,#53494,#53495,#53496,#53497,#53498,#53499,#53500,#53501,#53502,#53503,
#53504,#53505,#53506),.UNSPECIFIED.,.F.,.F.,(4,3,3,3,3,3,3,3,3,3,3,3,3,
3,3,3,3,3,3,3,3,3,3,3,3,3,3,3,4),(264.989216780594,264.990797704342,265.067528282667,
265.144191881034,265.220803182262,265.297377948977,265.373931278371,265.450488676376,
265.489568895004,265.574237886622,265.65905233867,265.744065656907,265.829165072416,
265.914384460948,265.988340085667,266.069897065294,266.15137891426,266.235312004777,
266.316639244808,266.401875260568,266.487111276329,266.566522474807,266.645952099355,
266.725410910304,266.804942733759,266.884516260188,266.964173384152,266.985882466992,
267.035375555133),.UNSPECIFIED.);
#3377=B_SPLINE_CURVE_WITH_KNOTS('',3,(#53507,#53508,#53509,#53510,#53511,
#53512,#53513,#53514,#53515,#53516,#53517,#53518,#53519,#53520,#53521,#53522,
#53523,#53524,#53525,#53526,#53527,#53528,#53529,#53530,#53531,#53532,#53533,
#53534,#53535,#53536,#53537,#53538,#53539,#53540,#53541,#53542,#53543,#53544,
#53545,#53546,#53547,#53548,#53549,#53550,#53551,#53552,#53553,#53554,#53555,
#53556,#53557,#53558,#53559,#53560,#53561,#53562,#53563,#53564,#53565,#53566,
#53567,#53568,#53569,#53570,#53571,#53572,#53573,#53574,#53575,#53576,#53577,
#53578,#53579,#53580,#53581,#53582,#53583,#53584,#53585,#53586,#53587,#53588,
#53589,#53590,#53591,#53592,#53593,#53594,#53595,#53596,#53597,#53598,#53599,
#53600,#53601,#53602,#53603,#53604,#53605,#53606,#53607,#53608,#53609,#53610,
#53611,#53612,#53613,#53614,#53615,#53616,#53617,#53618,#53619,#53620,#53621,
#53622,#53623,#53624,#53625,#53626,#53627,#53628,#53629,#53630,#53631,#53632,
#53633,#53634,#53635,#53636,#53637,#53638,#53639,#53640,#53641,#53642,#53643,
#53644,#53645,#53646,#53647,#53648,#53649,#53650,#53651,#53652,#53653,#53654,
#53655,#53656,#53657,#53658,#53659,#53660,#53661,#53662,#53663,#53664,#53665,
#53666,#53667,#53668,#53669,#53670,#53671,#53672,#53673,#53674,#53675),
 .UNSPECIFIED.,.F.,.F.,(4,3,3,3,3,3,3,3,3,3,3,3,3,3,3,3,3,3,3,3,3,3,3,3,
3,3,3,3,3,3,3,3,3,3,3,3,3,3,3,3,3,3,3,3,3,3,3,3,3,3,3,3,3,3,3,3,4),(267.035375555213,
267.113312000005,267.191183295891,267.269004458145,267.346790466105,267.426369763881,
267.504146913764,267.581936059632,267.659750746375,267.74066927186,267.818616933769,
267.896620423716,267.974726358261,267.983424848316,268.059496125952,268.135471902399,
268.211368959391,268.287203998204,268.362993658301,268.440240354718,268.516003852979,
268.591774684346,268.66756785218,268.745917696545,268.821842460055,268.901404844848,
268.980967229641,269.058537450584,269.136015591105,269.213417305018,269.290758191313,
269.368053805207,269.445327244821,269.522590480128,269.599857547566,269.677142483069,
269.754500485416,269.831896016473,269.90939768324,269.978509610966,270.062721762427,
270.146807790137,270.230688712083,270.314440498118,270.397978145454,270.477280801629,
270.55466056796,270.632058729003,270.709489071576,270.787006365029,270.864573311003,
270.94224660245,270.976051992291,271.055670219224,271.135224360004,271.214711332198,
271.272349559382),.UNSPECIFIED.);
#3378=B_SPLINE_CURVE_WITH_KNOTS('',3,(#53681,#53682,#53683,#53684,#53685,
#53686,#53687,#53688,#53689,#53690,#53691,#53692,#53693,#53694,#53695,#53696,
#53697,#53698,#53699,#53700,#53701,#53702,#53703,#53704,#53705,#53706,#53707,
#53708,#53709,#53710,#53711,#53712,#53713,#53714,#53715,#53716,#53717,#53718,
#53719,#53720,#53721,#53722,#53723,#53724,#53725,#53726,#53727,#53728,#53729,
#53730,#53731,#53732,#53733,#53734,#53735,#53736,#53737,#53738,#53739,#53740,
#53741,#53742,#53743,#53744,#53745,#53746,#53747,#53748,#53749,#53750,#53751,
#53752,#53753,#53754,#53755,#53756,#53757,#53758,#53759,#53760,#53761,#53762,
#53763,#53764,#53765,#53766,#53767,#53768,#53769,#53770,#53771,#53772,#53773,
#53774,#53775,#53776,#53777,#53778,#53779,#53780,#53781,#53782,#53783,#53784,
#53785,#53786,#53787,#53788,#53789,#53790,#53791,#53792,#53793,#53794,#53795,
#53796,#53797,#53798,#53799,#53800,#53801,#53802,#53803,#53804,#53805,#53806,
#53807,#53808,#53809,#53810,#53811,#53812,#53813,#53814,#53815,#53816,#53817,
#53818,#53819,#53820,#53821,#53822,#53823,#53824,#53825,#53826,#53827,#53828,
#53829,#53830,#53831,#53832,#53833,#53834,#53835,#53836,#53837,#53838,#53839,
#53840,#53841,#53842,#53843,#53844,#53845,#53846),.UNSPECIFIED.,.F.,.F.,
(4,3,3,3,3,3,3,3,3,3,3,3,3,3,3,3,3,3,3,3,3,3,3,3,3,3,3,3,3,3,3,3,3,3,3,
3,3,3,3,3,3,3,3,3,3,3,3,3,3,3,3,3,3,3,3,4),(273.318560862442,273.405000238929,
273.491718545237,273.578829877679,273.647402687048,273.731614838509,273.815700866218,
273.899581788165,273.983333574198,274.066871221535,274.146173877711,274.223553644042,
274.300951805085,274.378382147658,274.45589944111,274.533466387085,274.611139678532,
274.644945068373,274.724570256234,274.804122711111,274.883614732899,274.963058574914,
275.042466452812,275.121856886934,275.201238437683,275.280622175489,275.360019170819,
275.439469787945,275.518948807384,275.598500947036,275.642487449698,275.719218028023,
275.79588162639,275.872492927618,275.949067694333,276.025621023727,276.102178421732,
276.141258640361,276.225927631979,276.310742084028,276.395755402266,276.480854817776,
276.566074206309,276.640029831023,276.721586810649,276.803068659615,276.887001750133,
276.968328990162,277.053565005924,277.138801021686,277.218206203887,277.297628934143,
277.37710710278,277.456616972324,277.536195134398,277.55504144039),
 .UNSPECIFIED.);
#3379=B_SPLINE_CURVE_WITH_KNOTS('',3,(#53847,#53848,#53849,#53850,#53851,
#53852,#53853,#53854,#53855,#53856,#53857,#53858,#53859,#53860,#53861,#53862,
#53863,#53864,#53865,#53866,#53867,#53868,#53869,#53870,#53871,#53872,#53873,
#53874,#53875,#53876,#53877,#53878,#53879,#53880,#53881,#53882,#53883,#53884,
#53885,#53886,#53887,#53888,#53889,#53890,#53891,#53892,#53893,#53894,#53895,
#53896,#53897,#53898,#53899,#53900,#53901,#53902,#53903,#53904,#53905,#53906,
#53907,#53908,#53909,#53910,#53911,#53912,#53913,#53914,#53915,#53916,#53917,
#53918,#53919,#53920,#53921,#53922,#53923,#53924,#53925,#53926,#53927,#53928),
 .UNSPECIFIED.,.F.,.F.,(4,3,3,3,3,3,3,3,3,3,3,3,3,3,3,3,3,3,3,3,3,3,3,3,
3,3,3,4),(271.271644794101,271.34992100394,271.428289355457,271.506705887669,
271.585241659055,271.652317924399,271.728389202035,271.804364978482,271.880262035474,
271.956097074287,272.031886734384,272.109133430802,272.184896929063,272.260667760429,
272.336460928263,272.414810772628,272.490735536139,272.570297920931,272.649860305724,
272.72846319729,272.806929470045,272.885314382992,272.963630897435,273.041891931622,
273.120107163257,273.198295155157,273.276474989067,273.318560862312),
 .UNSPECIFIED.);
#3380=B_SPLINE_CURVE_WITH_KNOTS('',3,(#53930,#53931,#53932,#53933,#53934,
#53935,#53936,#53937,#53938,#53939,#53940,#53941,#53942,#53943,#53944,#53945,
#53946,#53947,#53948,#53949,#53950,#53951,#53952,#53953,#53954,#53955,#53956,
#53957,#53958,#53959,#53960,#53961,#53962,#53963,#53964,#53965,#53966,#53967,
#53968,#53969,#53970,#53971,#53972,#53973,#53974,#53975,#53976,#53977,#53978,
#53979,#53980,#53981,#53982,#53983,#53984,#53985,#53986,#53987,#53988,#53989,
#53990,#53991,#53992,#53993,#53994,#53995,#53996,#53997,#53998,#53999,#54000,
#54001,#54002,#54003,#54004,#54005,#54006,#54007,#54008,#54009,#54010,#54011),
 .UNSPECIFIED.,.F.,.F.,(4,3,3,3,3,3,3,3,3,3,3,3,3,3,3,3,3,3,3,3,3,3,3,3,
3,3,3,4),(271.272349559382,271.351766100178,271.431160912595,271.510543800256,
271.589925834822,271.669318086045,271.748762684496,271.828232893785,271.907780304428,
271.973594373616,272.050324951941,272.126988550308,272.203599851536,272.280174618251,
272.356727947646,272.433285345651,272.472365564278,272.557034555896,272.641849007944,
272.726862326181,272.811961741691,272.897181130223,272.971136754941,273.057992781784,
273.14141558143,273.224751553311,273.307968176738,273.318560862312),
 .UNSPECIFIED.);
#3381=B_SPLINE_CURVE_WITH_KNOTS('',3,(#54012,#54013,#54014,#54015,#54016,
#54017,#54018,#54019,#54020,#54021,#54022,#54023,#54024,#54025,#54026,#54027,
#54028,#54029,#54030,#54031,#54032,#54033,#54034,#54035,#54036,#54037,#54038,
#54039,#54040,#54041,#54042,#54043,#54044,#54045,#54046,#54047,#54048,#54049,
#54050,#54051,#54052,#54053,#54054,#54055,#54056,#54057,#54058,#54059,#54060,
#54061,#54062,#54063,#54064,#54065,#54066,#54067,#54068,#54069,#54070,#54071,
#54072,#54073,#54074,#54075,#54076,#54077,#54078,#54079,#54080,#54081,#54082,
#54083,#54084,#54085,#54086,#54087,#54088,#54089,#54090,#54091,#54092,#54093,
#54094,#54095,#54096,#54097,#54098,#54099,#54100,#54101,#54102,#54103,#54104,
#54105,#54106,#54107,#54108,#54109,#54110,#54111,#54112,#54113,#54114,#54115,
#54116,#54117,#54118,#54119,#54120,#54121,#54122,#54123,#54124,#54125,#54126,
#54127,#54128,#54129,#54130,#54131,#54132,#54133,#54134,#54135,#54136,#54137,
#54138,#54139,#54140,#54141,#54142,#54143,#54144,#54145,#54146,#54147,#54148,
#54149,#54150,#54151,#54152,#54153,#54154,#54155,#54156,#54157,#54158,#54159,
#54160,#54161,#54162,#54163,#54164,#54165,#54166,#54167,#54168),
 .UNSPECIFIED.,.F.,.F.,(4,3,3,3,3,3,3,3,3,3,3,3,3,3,3,3,3,3,3,3,3,3,3,3,
3,3,3,3,3,3,3,3,3,3,3,3,3,3,3,3,3,3,3,3,3,3,3,3,3,3,3,3,4),(273.318560862312,
273.401023068412,273.483484926215,273.56594644257,273.648407624328,273.730868478338,
273.81332901145,273.895789230513,273.978249142376,274.060708753888,274.143168071897,
274.22562710325,274.308085854797,274.390544333385,274.473002545861,274.555460499071,
274.637918199864,274.720375655086,274.802832871584,274.88884556687,274.972170365428,
275.05463697102,275.137102732403,275.219567676993,275.302031832201,275.384495225438,
275.46695788411,275.549419835621,275.631881107373,275.714341726766,275.796801721197,
275.879261118062,275.961719944752,276.044178228659,276.126635997172,276.209093277678,
276.293227392869,276.375693391229,276.458157767836,276.540620632331,276.623082094337,
276.705542263457,276.788001249273,276.870459161353,276.956056656276,277.038521393322,
277.120983165708,277.203442411873,277.285899570112,277.368362089195,277.450819760606,
277.533278551799,277.555239120736),.UNSPECIFIED.);
#3382=B_SPLINE_CURVE_WITH_KNOTS('',3,(#54174,#54175,#54176,#54177,#54178,
#54179,#54180,#54181,#54182,#54183,#54184,#54185,#54186,#54187,#54188,#54189,
#54190,#54191,#54192,#54193,#54194,#54195,#54196,#54197,#54198,#54199,#54200,
#54201,#54202,#54203,#54204,#54205,#54206,#54207,#54208,#54209,#54210,#54211,
#54212,#54213,#54214,#54215,#54216,#54217,#54218,#54219,#54220,#54221,#54222,
#54223,#54224,#54225,#54226,#54227,#54228,#54229,#54230,#54231,#54232,#54233,
#54234,#54235,#54236,#54237,#54238,#54239,#54240,#54241,#54242,#54243,#54244,
#54245,#54246,#54247,#54248,#54249,#54250,#54251,#54252,#54253,#54254,#54255,
#54256,#54257,#54258,#54259,#54260,#54261,#54262,#54263,#54264,#54265,#54266,
#54267,#54268,#54269,#54270,#54271,#54272,#54273,#54274,#54275,#54276,#54277,
#54278,#54279,#54280,#54281,#54282,#54283,#54284,#54285,#54286,#54287,#54288,
#54289,#54290,#54291,#54292,#54293,#54294,#54295,#54296,#54297,#54298,#54299,
#54300,#54301,#54302,#54303,#54304,#54305,#54306,#54307,#54308,#54309,#54310,
#54311,#54312,#54313,#54314,#54315,#54316,#54317,#54318,#54319,#54320,#54321,
#54322,#54323,#54324,#54325,#54326,#54327,#54328,#54329,#54330,#54331,#54332,
#54333,#54334,#54335,#54336,#54337,#54338,#54339,#54340,#54341,#54342),
 .UNSPECIFIED.,.F.,.F.,(4,3,3,3,3,3,3,3,3,3,3,3,3,3,3,3,3,3,3,3,3,3,3,3,
3,3,3,3,3,3,3,3,3,3,3,3,3,3,3,3,3,3,3,3,3,3,3,3,3,3,3,3,3,3,3,3,4),(279.601746169492,
279.632656974998,279.710227195941,279.787705336461,279.865107050374,279.942447936669,
280.019743550563,280.097016990177,280.174280225484,280.251547292921,280.328832228425,
280.406190230771,280.483585761829,280.561087428595,280.630199356323,280.714411507784,
280.798497535494,280.882378457441,280.966130243475,281.049667890812,281.128970546985,
281.206350313315,281.283748474359,281.361178816931,281.438696110384,281.516263056358,
281.593936347805,281.627741737648,281.707366925509,281.786919380386,281.866411402174,
281.945855244189,282.025263122087,282.104653556209,282.184035106958,282.263418844764,
282.342815840095,282.422266457221,282.501745476659,282.581297616312,282.625284118972,
282.702014697297,282.778678295663,282.855289596891,282.931864363606,283.008417693,
283.084975091004,283.124055309635,283.208724301254,283.293538753303,283.378552071541,
283.463651487051,283.548870875584,283.622826500297,283.704389857304,283.785861431739,
283.838928063841),.UNSPECIFIED.);
#3383=B_SPLINE_CURVE_WITH_KNOTS('',3,(#54343,#54344,#54345,#54346,#54347,
#54348,#54349,#54350,#54351,#54352,#54353,#54354,#54355,#54356,#54357,#54358,
#54359,#54360,#54361,#54362,#54363,#54364,#54365,#54366,#54367,#54368,#54369,
#54370,#54371,#54372,#54373,#54374,#54375,#54376,#54377,#54378,#54379,#54380,
#54381,#54382,#54383,#54384,#54385,#54386,#54387,#54388,#54389,#54390,#54391,
#54392,#54393,#54394,#54395,#54396,#54397,#54398,#54399,#54400,#54401,#54402,
#54403,#54404,#54405,#54406,#54407,#54408,#54409,#54410,#54411,#54412,#54413,
#54414,#54415,#54416,#54417,#54418,#54419,#54420,#54421,#54422,#54423,#54424),
 .UNSPECIFIED.,.F.,.F.,(4,3,3,3,3,3,3,3,3,3,3,3,3,3,3,3,3,3,3,3,3,3,3,3,
3,3,3,4),(277.55504144039,277.637572212348,277.715960591356,277.794282855798,
277.872553405257,277.950786601801,278.028996779478,278.107214914861,278.185440980081,
278.263687961638,278.341968855853,278.420342283607,278.498765281931,278.577304841121,
278.635114593673,278.710793424333,278.786377441824,278.861883641082,278.937328924206,
279.01273012275,279.08811438325,279.163492108499,279.23887846607,279.314288630994,
279.389783238998,279.465322399708,279.540978914284,279.601746169399),
 .UNSPECIFIED.);
#3384=B_SPLINE_CURVE_WITH_KNOTS('',3,(#54426,#54427,#54428,#54429,#54430,
#54431,#54432,#54433,#54434,#54435,#54436,#54437,#54438,#54439,#54440,#54441,
#54442,#54443,#54444,#54445,#54446,#54447,#54448,#54449,#54450,#54451,#54452,
#54453,#54454,#54455,#54456,#54457,#54458,#54459,#54460,#54461,#54462,#54463,
#54464,#54465,#54466,#54467,#54468,#54469,#54470,#54471,#54472,#54473,#54474,
#54475,#54476,#54477,#54478,#54479,#54480,#54481,#54482,#54483,#54484,#54485,
#54486,#54487,#54488,#54489,#54490,#54491,#54492,#54493,#54494,#54495,#54496,
#54497,#54498,#54499,#54500,#54501),.UNSPECIFIED.,.F.,.F.,(4,3,3,3,3,3,
3,3,3,3,3,3,3,3,3,3,3,3,3,3,3,3,3,3,3,4),(277.555239120736,277.637700724466,
277.720161662318,277.80262196169,277.885081649979,277.967540754577,278.049999302877,
278.13245732227,278.214914840143,278.301591798227,278.384058583768,278.466523696836,
278.548987247084,278.631449344143,278.713910097625,278.796369617121,278.878828012206,
278.96128539244,279.043751778126,279.126214979634,279.208675435484,279.291133584038,
279.373599187792,279.45605906618,279.538523177432,279.601746169492),
 .UNSPECIFIED.);
#3385=B_SPLINE_CURVE_WITH_KNOTS('',3,(#54502,#54503,#54504,#54505,#54506,
#54507,#54508,#54509,#54510,#54511,#54512,#54513,#54514,#54515,#54516,#54517,
#54518,#54519,#54520,#54521,#54522,#54523,#54524,#54525,#54526,#54527,#54528,
#54529,#54530,#54531,#54532,#54533,#54534,#54535,#54536,#54537,#54538,#54539,
#54540,#54541,#54542,#54543,#54544,#54545,#54546,#54547,#54548,#54549,#54550,
#54551,#54552,#54553,#54554,#54555,#54556,#54557,#54558,#54559,#54560,#54561,
#54562,#54563,#54564,#54565,#54566,#54567,#54568,#54569,#54570,#54571,#54572,
#54573,#54574,#54575,#54576,#54577,#54578,#54579,#54580,#54581,#54582,#54583,
#54584,#54585,#54586,#54587,#54588,#54589,#54590,#54591,#54592,#54593,#54594,
#54595,#54596,#54597,#54598,#54599,#54600,#54601,#54602,#54603,#54604,#54605,
#54606,#54607,#54608,#54609,#54610,#54611,#54612,#54613,#54614,#54615,#54616,
#54617,#54618,#54619,#54620,#54621,#54622,#54623,#54624,#54625,#54626,#54627,
#54628,#54629,#54630,#54631,#54632,#54633,#54634,#54635,#54636,#54637,#54638,
#54639,#54640,#54641,#54642,#54643,#54644,#54645,#54646,#54647,#54648,#54649,
#54650,#54651,#54652,#54653,#54654,#54655,#54656,#54657,#54658,#54659,#54660,
#54661,#54662,#54663,#54664,#54665,#54666,#54667),.UNSPECIFIED.,.F.,.F.,
(4,3,3,3,3,3,3,3,3,3,3,3,3,3,3,3,3,3,3,3,3,3,3,3,3,3,3,3,3,3,3,3,3,3,3,
3,3,3,3,3,3,3,3,3,3,3,3,3,3,3,3,3,3,3,3,4),(279.601746169492,279.689792983173,
279.777223068222,279.865578246219,279.953933424215,280.035490403841,280.116972252807,
280.200905343325,280.282232583354,280.367468599116,280.452704614878,280.532115813357,
280.611545437905,280.691004248855,280.77053607231,280.850109598739,280.929766722704,
280.95147580554,281.029864184548,281.10818644899,281.186456998449,281.264690194993,
281.34290037267,281.421118508053,281.499344573272,281.57759155483,281.655872449044,
281.734245876799,281.812668875122,281.891208434313,281.949018186865,282.025089464501,
282.101065240948,282.17696229794,282.252797336753,282.32858699685,282.405833693268,
282.481597191528,282.557368022895,282.633161190729,282.711511035094,282.787435798605,
282.866998183397,282.94656056819,283.024136849311,283.101619874536,283.179025302498,
283.256368736008,283.333663725309,283.410932806938,283.488190025617,283.565449416688,
283.642752625717,283.720080084015,283.797479430723,283.837852220474),
 .UNSPECIFIED.);
#3386=B_SPLINE_CURVE_WITH_KNOTS('',3,(#54673,#54674,#54675,#54676,#54677,
#54678,#54679,#54680,#54681,#54682,#54683,#54684,#54685,#54686,#54687,#54688,
#54689,#54690,#54691,#54692,#54693,#54694,#54695,#54696,#54697,#54698,#54699,
#54700,#54701,#54702,#54703,#54704,#54705,#54706,#54707,#54708,#54709,#54710,
#54711,#54712,#54713,#54714,#54715,#54716,#54717,#54718,#54719,#54720,#54721,
#54722,#54723,#54724,#54725,#54726,#54727,#54728,#54729,#54730,#54731,#54732,
#54733,#54734,#54735,#54736,#54737,#54738,#54739,#54740,#54741,#54742,#54743,
#54744,#54745,#54746,#54747,#54748,#54749,#54750,#54751,#54752,#54753,#54754,
#54755,#54756,#54757,#54758,#54759,#54760,#54761,#54762,#54763,#54764,#54765,
#54766,#54767,#54768,#54769,#54770,#54771,#54772,#54773,#54774,#54775,#54776,
#54777,#54778,#54779,#54780,#54781,#54782,#54783,#54784,#54785,#54786,#54787,
#54788,#54789,#54790,#54791,#54792,#54793,#54794,#54795,#54796,#54797,#54798,
#54799,#54800,#54801,#54802,#54803,#54804,#54805,#54806,#54807,#54808,#54809,
#54810,#54811,#54812,#54813,#54814,#54815,#54816,#54817,#54818,#54819,#54820,
#54821,#54822,#54823,#54824,#54825,#54826,#54827,#54828,#54829),
 .UNSPECIFIED.,.F.,.F.,(4,3,3,3,3,3,3,3,3,3,3,3,3,3,3,3,3,3,3,3,3,3,3,3,
3,3,3,3,3,3,3,3,3,3,3,3,3,3,3,3,3,3,3,3,3,3,3,3,3,3,3,3,4),(285.884931476671,
285.967393682771,286.049855540574,286.132317056929,286.214778238687,286.297239092697,
286.379699625809,286.462159844872,286.544619756735,286.627079368247,286.709538686256,
286.79199771761,286.874456469157,286.956914947744,287.03937316022,287.121831113431,
287.204288814224,287.286746269445,287.369203485943,287.455216181229,287.538540979787,
287.621007585379,287.703473346762,287.785938291352,287.86840244656,287.950865839797,
288.033328498468,288.115790449979,288.198251721732,288.280712341125,288.363172335556,
288.44563173242,288.52809055911,288.610548843017,288.69300661153,288.775463892037,
288.859598007228,288.942064005588,289.024528382194,289.106991246689,289.189452708696,
289.271912877815,289.354371863631,289.436829775711,289.522427270634,289.60489200768,
289.687353780067,289.769813026232,289.85227018447,289.934732703553,290.017190374964,
290.099649166157,290.121609735095),.UNSPECIFIED.);
#3387=B_SPLINE_CURVE_WITH_KNOTS('',3,(#54830,#54831,#54832,#54833,#54834,
#54835,#54836,#54837,#54838,#54839,#54840,#54841,#54842,#54843,#54844,#54845,
#54846,#54847,#54848,#54849,#54850,#54851,#54852,#54853,#54854,#54855,#54856,
#54857,#54858,#54859,#54860,#54861,#54862,#54863,#54864,#54865,#54866,#54867,
#54868,#54869,#54870,#54871,#54872,#54873,#54874,#54875,#54876,#54877,#54878,
#54879,#54880,#54881,#54882,#54883,#54884,#54885,#54886,#54887,#54888,#54889,
#54890,#54891,#54892,#54893,#54894,#54895,#54896,#54897,#54898,#54899,#54900,
#54901,#54902,#54903,#54904,#54905,#54906,#54907,#54908,#54909,#54910,#54911),
 .UNSPECIFIED.,.F.,.F.,(4,3,3,3,3,3,3,3,3,3,3,3,3,3,3,3,3,3,3,3,3,3,3,3,
3,3,3,4),(283.838928063841,283.920276857637,284.001570576253,284.082800319923,
284.12159769096,284.201008889439,284.280438513987,284.359897324937,284.439429148393,
284.519002674822,284.598659798787,284.620368881622,284.69875726063,284.777079525072,
284.85535007453,284.933583271075,285.011793448752,285.090011584135,285.168237649354,
285.246484630912,285.324765525126,285.403138952881,285.481561951204,285.560101510394,
285.617911262947,285.712522593592,285.805716091708,285.884931476671),
 .UNSPECIFIED.);
#3388=B_SPLINE_CURVE_WITH_KNOTS('',3,(#54913,#54914,#54915,#54916,#54917,
#54918,#54919,#54920,#54921,#54922,#54923,#54924,#54925,#54926,#54927,#54928,
#54929,#54930,#54931,#54932,#54933,#54934,#54935,#54936,#54937,#54938,#54939,
#54940,#54941,#54942,#54943,#54944,#54945,#54946,#54947,#54948,#54949,#54950,
#54951,#54952,#54953,#54954,#54955,#54956,#54957,#54958,#54959,#54960,#54961,
#54962,#54963,#54964,#54965,#54966,#54967,#54968,#54969,#54970,#54971,#54972,
#54973,#54974,#54975,#54976,#54977,#54978,#54979,#54980,#54981,#54982,#54983,
#54984,#54985,#54986,#54987,#54988,#54989,#54990,#54991,#54992,#54993,#54994),
 .UNSPECIFIED.,.F.,.F.,(4,3,3,3,3,3,3,3,3,3,3,3,3,3,3,3,3,3,3,3,3,3,3,3,
3,3,3,4),(283.837852220474,283.915368600167,283.944102949515,284.028315100976,
284.112401128686,284.196282050633,284.280033836667,284.363571484004,284.442874140177,
284.520253906507,284.597652067551,284.675082410124,284.752599703576,284.83016664955,
284.907839940997,284.94164533084,285.020635129152,285.099550436348,285.178404835331,
285.257211863794,285.335988443429,285.414748496302,285.493504247453,285.572267917277,
285.651085075272,285.729927923759,285.808855343169,285.884931476671),
 .UNSPECIFIED.);
#3389=B_SPLINE_CURVE_WITH_KNOTS('',3,(#54995,#54996,#54997,#54998,#54999,
#55000,#55001,#55002,#55003,#55004,#55005,#55006,#55007,#55008,#55009,#55010,
#55011,#55012,#55013,#55014,#55015,#55016,#55017,#55018,#55019,#55020,#55021,
#55022,#55023,#55024,#55025,#55026,#55027,#55028,#55029,#55030,#55031,#55032,
#55033,#55034,#55035,#55036,#55037,#55038,#55039,#55040,#55041,#55042,#55043,
#55044,#55045,#55046,#55047,#55048,#55049,#55050,#55051,#55052,#55053,#55054,
#55055,#55056,#55057,#55058,#55059,#55060,#55061,#55062,#55063,#55064,#55065,
#55066,#55067,#55068,#55069,#55070,#55071,#55072,#55073,#55074,#55075,#55076,
#55077,#55078,#55079,#55080,#55081,#55082,#55083,#55084,#55085,#55086,#55087,
#55088,#55089,#55090,#55091,#55092,#55093,#55094,#55095,#55096,#55097,#55098,
#55099,#55100,#55101,#55102,#55103,#55104,#55105,#55106,#55107,#55108,#55109,
#55110,#55111,#55112,#55113,#55114,#55115,#55116,#55117,#55118,#55119,#55120,
#55121,#55122,#55123,#55124,#55125,#55126,#55127,#55128,#55129,#55130,#55131,
#55132,#55133,#55134,#55135,#55136,#55137,#55138,#55139,#55140,#55141,#55142,
#55143,#55144,#55145,#55146,#55147,#55148,#55149,#55150,#55151),
 .UNSPECIFIED.,.F.,.F.,(4,3,3,3,3,3,3,3,3,3,3,3,3,3,3,3,3,3,3,3,3,3,3,3,
3,3,3,3,3,3,3,3,3,3,3,3,3,3,3,3,3,3,3,3,3,3,3,3,3,3,3,3,4),(285.884931476671,
285.967393682771,286.049855540574,286.132317056929,286.214778238687,286.297239092697,
286.379699625809,286.462159844872,286.544619756735,286.627079368247,286.709538686256,
286.791997717609,286.874456469156,286.956914947744,287.039373160219,287.12183111343,
287.204288814223,287.286746269445,287.369203485942,287.455216181228,287.538540979787,
287.621007585379,287.703473346762,287.785938291352,287.86840244656,287.950865839796,
288.033328498468,288.115790449979,288.198251721732,288.280712341125,288.363172335556,
288.44563173242,288.52809055911,288.610548843017,288.69300661153,288.775463892036,
288.859598007228,288.942064005588,289.024528382194,289.106991246689,289.189452708696,
289.271912877815,289.354371863631,289.436829775711,289.522427270634,289.60489200768,
289.687353780067,289.769813026232,289.85227018447,289.934732703553,290.017190374964,
290.099649166157,290.121609735095),.UNSPECIFIED.);
#3390=B_SPLINE_CURVE_WITH_KNOTS('',3,(#55157,#55158,#55159,#55160,#55161,
#55162,#55163,#55164,#55165,#55166,#55167,#55168,#55169,#55170,#55171,#55172,
#55173,#55174,#55175,#55176,#55177,#55178,#55179,#55180,#55181,#55182,#55183,
#55184,#55185,#55186,#55187,#55188,#55189,#55190,#55191,#55192,#55193,#55194,
#55195,#55196,#55197,#55198,#55199,#55200,#55201,#55202,#55203,#55204,#55205,
#55206,#55207,#55208,#55209,#55210,#55211,#55212,#55213,#55214,#55215,#55216,
#55217,#55218,#55219,#55220,#55221,#55222,#55223,#55224,#55225,#55226,#55227,
#55228,#55229,#55230,#55231,#55232,#55233,#55234,#55235,#55236,#55237,#55238,
#55239,#55240,#55241,#55242,#55243,#55244,#55245,#55246,#55247,#55248,#55249,
#55250,#55251,#55252,#55253,#55254,#55255,#55256,#55257,#55258,#55259,#55260,
#55261,#55262,#55263,#55264,#55265,#55266,#55267,#55268,#55269,#55270,#55271,
#55272,#55273,#55274,#55275,#55276,#55277,#55278,#55279,#55280,#55281,#55282,
#55283,#55284,#55285,#55286,#55287,#55288,#55289,#55290,#55291,#55292,#55293,
#55294,#55295,#55296,#55297,#55298,#55299,#55300,#55301,#55302,#55303,#55304,
#55305,#55306,#55307,#55308,#55309,#55310,#55311,#55312,#55313,#55314,#55315,
#55316,#55317,#55318,#55319,#55320,#55321,#55322),.UNSPECIFIED.,.F.,.F.,
(4,3,3,3,3,3,3,3,3,3,3,3,3,3,3,3,3,3,3,3,3,3,3,3,3,3,3,3,3,3,3,3,3,3,3,
3,3,3,3,3,3,3,3,3,3,3,3,3,3,3,3,3,3,3,3,4),(292.168116783851,292.255250415141,
292.342972619817,292.430969857911,292.51933491208,292.600707932221,292.676779209857,
292.752754986304,292.828652043296,292.904487082109,292.980276742206,293.057523438624,
293.133286936884,293.209057768251,293.284850936085,293.36320078045,293.439125543961,
293.518687928753,293.598250313546,293.675820534489,293.753298675009,293.830700388923,
293.908041275218,293.985336889112,294.062610328726,294.139873564033,294.21714063147,
294.294425566974,294.371783569321,294.449179100378,294.526680767145,294.595792694871,
294.680004846332,294.764090874042,294.847971795988,294.931723582022,295.015261229359,
295.094563885534,295.171943651865,295.249341812908,295.326772155481,295.404289448934,
295.481856394908,295.559529686355,295.593335076196,295.672968306783,295.752527270792,
295.834063474569,295.9135027365,295.992909167164,296.072293859906,296.15542462018,
296.234813253758,296.314210466724,296.393641864363,296.404816901002),
 .UNSPECIFIED.);
#3391=B_SPLINE_CURVE_WITH_KNOTS('',3,(#55323,#55324,#55325,#55326,#55327,
#55328,#55329,#55330,#55331,#55332,#55333,#55334,#55335,#55336,#55337,#55338,
#55339,#55340,#55341,#55342,#55343,#55344,#55345,#55346,#55347,#55348,#55349,
#55350,#55351,#55352,#55353,#55354,#55355,#55356,#55357,#55358,#55359,#55360,
#55361,#55362,#55363,#55364,#55365,#55366,#55367,#55368,#55369,#55370,#55371,
#55372,#55373,#55374,#55375,#55376,#55377,#55378,#55379,#55380,#55381,#55382,
#55383,#55384,#55385,#55386,#55387,#55388,#55389,#55390,#55391,#55392,#55393,
#55394,#55395,#55396,#55397,#55398),.UNSPECIFIED.,.F.,.F.,(4,3,3,3,3,3,
3,3,3,3,3,3,3,3,3,3,3,3,3,3,3,3,3,3,3,4),(290.121609735095,290.204071338826,
290.286532276678,290.36899257605,290.451452264338,290.533911368936,290.616369917237,
290.698827936629,290.781285454502,290.867962412586,290.950429198127,291.032894311195,
291.115357861443,291.197819958503,291.280280711984,291.36274023148,291.445198626565,
291.527656006799,291.610122392485,291.692585593993,291.775046049843,291.857504198398,
291.939969802151,292.022429680539,292.104893791791,292.168116783851),
 .UNSPECIFIED.);
#3392=B_SPLINE_CURVE_WITH_KNOTS('',3,(#55400,#55401,#55402,#55403,#55404,
#55405,#55406,#55407,#55408,#55409,#55410,#55411,#55412,#55413,#55414,#55415,
#55416,#55417,#55418,#55419,#55420,#55421,#55422,#55423,#55424,#55425,#55426,
#55427,#55428,#55429,#55430,#55431,#55432,#55433,#55434,#55435,#55436,#55437,
#55438,#55439,#55440,#55441,#55442,#55443,#55444,#55445,#55446,#55447,#55448,
#55449,#55450,#55451,#55452,#55453,#55454,#55455,#55456,#55457,#55458,#55459,
#55460,#55461,#55462,#55463,#55464,#55465,#55466,#55467,#55468,#55469,#55470,
#55471,#55472,#55473,#55474,#55475),.UNSPECIFIED.,.F.,.F.,(4,3,3,3,3,3,
3,3,3,3,3,3,3,3,3,3,3,3,3,3,3,3,3,3,3,4),(290.121609735095,290.204071338826,
290.286532276677,290.368992576049,290.451452264338,290.533911368936,290.616369917236,
290.698827936629,290.781285454502,290.867962412577,290.950429198118,291.032894311186,
291.115357861434,291.197819958493,291.280280711975,291.362740231471,291.445198626556,
291.52765600679,291.610122392476,291.692585593984,291.775046049833,291.857504198388,
291.939969802142,292.02242968053,292.104893791782,292.16811678371),
 .UNSPECIFIED.);
#3393=B_SPLINE_CURVE_WITH_KNOTS('',3,(#55476,#55477,#55478,#55479,#55480,
#55481,#55482,#55483,#55484,#55485,#55486,#55487,#55488,#55489,#55490,#55491,
#55492,#55493,#55494,#55495,#55496,#55497,#55498,#55499,#55500,#55501,#55502,
#55503,#55504,#55505,#55506,#55507,#55508,#55509,#55510,#55511,#55512,#55513,
#55514,#55515,#55516,#55517,#55518,#55519,#55520,#55521,#55522,#55523,#55524,
#55525,#55526,#55527,#55528,#55529,#55530,#55531,#55532,#55533,#55534,#55535,
#55536,#55537,#55538,#55539,#55540,#55541,#55542,#55543,#55544,#55545,#55546,
#55547,#55548,#55549,#55550,#55551,#55552,#55553,#55554,#55555,#55556,#55557,
#55558,#55559,#55560,#55561,#55562,#55563,#55564,#55565,#55566,#55567,#55568,
#55569,#55570,#55571,#55572,#55573,#55574,#55575,#55576,#55577,#55578,#55579,
#55580,#55581,#55582,#55583,#55584,#55585,#55586,#55587,#55588,#55589,#55590,
#55591,#55592,#55593,#55594,#55595,#55596,#55597,#55598,#55599,#55600,#55601,
#55602,#55603,#55604,#55605,#55606,#55607,#55608,#55609,#55610,#55611,#55612,
#55613,#55614,#55615,#55616,#55617,#55618,#55619,#55620,#55621,#55622,#55623,
#55624,#55625,#55626,#55627,#55628,#55629,#55630,#55631,#55632),
 .UNSPECIFIED.,.F.,.F.,(4,3,3,3,3,3,3,3,3,3,3,3,3,3,3,3,3,3,3,3,3,3,3,3,
3,3,3,3,3,3,3,3,3,3,3,3,3,3,3,3,3,3,3,3,3,3,3,3,3,3,3,3,4),(292.168116783851,
292.250578989951,292.333040847754,292.415502364109,292.497963545867,292.580424399877,
292.662884932989,292.745345152052,292.827805063915,292.910264675427,292.992723993436,
293.07518302479,293.157641776337,293.240100254924,293.3225584674,293.405016420611,
293.487474121404,293.569931576626,293.652388793123,293.738401488409,293.821726286967,
293.904192892559,293.986658653942,294.069123598532,294.151587753741,294.234051146977,
294.316513805649,294.39897575716,294.481437028912,294.563897648306,294.646357642737,
294.728817039601,294.811275866291,294.893734150198,294.976191918711,295.058649199218,
295.142783314409,295.225249312769,295.307713689375,295.39017655387,295.472638015877,
295.555098184996,295.637557170812,295.720015082892,295.805612577815,295.888077314861,
295.970539087247,296.052998333412,296.135455491651,296.217918010734,296.300375682145,
296.382834473338,296.404795042275),.UNSPECIFIED.);
#3394=B_SPLINE_CURVE_WITH_KNOTS('',3,(#55638,#55639,#55640,#55641,#55642,
#55643,#55644,#55645,#55646,#55647,#55648,#55649,#55650,#55651,#55652,#55653,
#55654,#55655,#55656,#55657,#55658,#55659,#55660,#55661,#55662,#55663,#55664,
#55665,#55666,#55667,#55668,#55669,#55670,#55671,#55672,#55673,#55674,#55675,
#55676,#55677,#55678,#55679,#55680,#55681,#55682,#55683,#55684,#55685,#55686,
#55687,#55688,#55689,#55690,#55691,#55692,#55693,#55694,#55695,#55696,#55697,
#55698,#55699,#55700,#55701,#55702,#55703,#55704,#55705,#55706,#55707,#55708,
#55709,#55710,#55711,#55712,#55713,#55714,#55715,#55716,#55717,#55718,#55719,
#55720,#55721,#55722,#55723,#55724,#55725,#55726,#55727,#55728,#55729,#55730,
#55731,#55732,#55733,#55734,#55735,#55736,#55737,#55738,#55739,#55740,#55741,
#55742,#55743,#55744,#55745,#55746,#55747,#55748,#55749,#55750,#55751,#55752,
#55753,#55754,#55755,#55756,#55757,#55758,#55759,#55760,#55761,#55762,#55763,
#55764,#55765,#55766,#55767,#55768,#55769,#55770,#55771,#55772,#55773,#55774,
#55775,#55776,#55777,#55778,#55779,#55780,#55781,#55782,#55783,#55784,#55785,
#55786,#55787,#55788,#55789,#55790,#55791,#55792,#55793,#55794,#55795,#55796,
#55797,#55798,#55799,#55800,#55801,#55802,#55803,#55804,#55805,#55806),
 .UNSPECIFIED.,.F.,.F.,(4,3,3,3,3,3,3,3,3,3,3,3,3,3,3,3,3,3,3,3,3,3,3,3,
3,3,3,3,3,3,3,3,3,3,3,3,3,3,3,3,3,3,3,3,3,3,3,3,3,3,3,3,3,3,3,3,4),(298.451302091031,
298.549288570198,298.585962220171,298.664350599179,298.742672863622,298.82094341308,
298.899176609624,298.977386787301,299.055604922684,299.133830987904,299.212077969461,
299.290358863676,299.368732291431,299.447155289754,299.525694848945,299.583504601496,
299.659575879132,299.735551655579,299.811448712571,299.887283751384,299.963073411481,
300.040320107898,300.116083606159,300.191854437526,300.267647605359,300.345997449725,
300.421922213235,300.501484598028,300.581046982821,300.658617203764,300.736095344284,
300.813497058198,300.890837944493,300.968133558387,301.045406998001,301.122670233308,
301.199937300745,301.277222236249,301.354580238595,301.431975769652,301.509477436419,
301.578589364145,301.662801515606,301.746887543315,301.830768465262,301.914520251295,
301.998057898632,302.077360554808,302.154740321139,302.232138482182,302.309568824755,
302.387086118208,302.464653064182,302.54232635563,302.57613174547,302.655761215605,
302.688034846856),.UNSPECIFIED.);
#3395=B_SPLINE_CURVE_WITH_KNOTS('',3,(#55807,#55808,#55809,#55810,#55811,
#55812,#55813,#55814,#55815,#55816,#55817,#55818,#55819,#55820,#55821,#55822,
#55823,#55824,#55825,#55826,#55827,#55828,#55829,#55830,#55831,#55832,#55833,
#55834,#55835,#55836,#55837,#55838,#55839,#55840,#55841,#55842,#55843,#55844,
#55845,#55846,#55847,#55848,#55849,#55850,#55851,#55852,#55853,#55854,#55855,
#55856,#55857,#55858,#55859,#55860,#55861,#55862,#55863,#55864,#55865,#55866,
#55867,#55868,#55869,#55870,#55871,#55872,#55873,#55874,#55875,#55876,#55877,
#55878,#55879,#55880,#55881,#55882,#55883,#55884,#55885,#55886,#55887,#55888),
 .UNSPECIFIED.,.F.,.F.,(4,3,3,3,3,3,3,3,3,3,3,3,3,3,3,3,3,3,3,3,3,3,3,3,
3,3,3,4),(296.404816901002,296.484303298207,296.563859804948,296.590877457521,
296.667608035846,296.744271634213,296.820882935442,296.897457702157,296.974011031551,
297.050568429556,297.089648648183,297.174317639801,297.259132091849,297.344145410086,
297.429244825595,297.514464214127,297.588419838846,297.669976818473,297.751458667439,
297.835391757956,297.916718997986,298.001955013747,298.087191029508,298.163747110249,
298.240328867758,298.316923015151,298.393579483727,298.451302090923),
 .UNSPECIFIED.);
#3396=B_SPLINE_CURVE_WITH_KNOTS('',3,(#55890,#55891,#55892,#55893,#55894,
#55895,#55896,#55897,#55898,#55899,#55900,#55901,#55902,#55903,#55904,#55905,
#55906,#55907,#55908,#55909,#55910,#55911,#55912,#55913,#55914,#55915,#55916,
#55917,#55918,#55919,#55920,#55921,#55922,#55923,#55924,#55925,#55926,#55927,
#55928,#55929,#55930,#55931,#55932,#55933,#55934,#55935,#55936,#55937,#55938,
#55939,#55940,#55941,#55942,#55943,#55944,#55945,#55946,#55947,#55948,#55949,
#55950,#55951,#55952,#55953,#55954,#55955,#55956,#55957,#55958,#55959,#55960,
#55961,#55962,#55963,#55964,#55965),.UNSPECIFIED.,.F.,.F.,(4,3,3,3,3,3,
3,3,3,3,3,3,3,3,3,3,3,3,3,3,3,3,3,3,3,4),(296.404795042275,296.487256646006,
296.569717583857,296.652177883229,296.734637571518,296.817096676116,296.899555224416,
296.982013243809,297.064470761682,297.151147719766,297.233614505307,297.316079618375,
297.398543168623,297.481005265682,297.563466019164,297.64592553866,297.728383933745,
297.810841313978,297.893307699665,297.975770901173,298.058231357022,298.140689505577,
298.223155109331,298.305614987719,298.388079098971,298.451302091031),
 .UNSPECIFIED.);
#3397=B_SPLINE_CURVE_WITH_KNOTS('',3,(#55966,#55967,#55968,#55969,#55970,
#55971,#55972,#55973,#55974,#55975,#55976,#55977,#55978,#55979,#55980,#55981,
#55982,#55983,#55984,#55985,#55986,#55987,#55988,#55989,#55990,#55991,#55992,
#55993,#55994,#55995,#55996,#55997,#55998,#55999,#56000,#56001,#56002,#56003,
#56004,#56005,#56006,#56007,#56008,#56009,#56010,#56011,#56012,#56013,#56014,
#56015,#56016,#56017,#56018,#56019,#56020,#56021,#56022,#56023,#56024,#56025,
#56026,#56027,#56028,#56029,#56030,#56031,#56032,#56033,#56034,#56035,#56036,
#56037,#56038,#56039,#56040,#56041,#56042,#56043,#56044,#56045,#56046,#56047,
#56048,#56049,#56050,#56051,#56052,#56053,#56054,#56055,#56056,#56057,#56058,
#56059,#56060,#56061,#56062,#56063,#56064,#56065,#56066,#56067,#56068,#56069,
#56070,#56071,#56072,#56073,#56074,#56075,#56076,#56077,#56078,#56079,#56080,
#56081,#56082,#56083,#56084,#56085,#56086,#56087,#56088,#56089,#56090,#56091,
#56092,#56093,#56094,#56095,#56096,#56097,#56098,#56099,#56100,#56101,#56102,
#56103,#56104,#56105,#56106,#56107,#56108,#56109,#56110,#56111,#56112,#56113,
#56114,#56115,#56116,#56117,#56118,#56119,#56120,#56121,#56122,#56123,#56124,
#56125,#56126,#56127,#56128,#56129,#56130,#56131),.UNSPECIFIED.,.F.,.F.,
(4,3,3,3,3,3,3,3,3,3,3,3,3,3,3,3,3,3,3,3,3,3,3,3,3,3,3,3,3,3,3,3,3,3,3,
3,3,3,3,3,3,3,3,3,3,3,3,3,3,3,3,3,3,3,3,4),(298.451328562689,298.529563567541,
298.607838564957,298.686215847642,298.764647222749,298.843204822482,298.907238669388,
298.986863857249,299.066416312125,299.145908333914,299.225352175928,299.304760053826,
299.384150487948,299.463532038697,299.542915776503,299.622312771833,299.701763388958,
299.781242408397,299.860794548049,299.904781050713,299.981511629038,300.058175227405,
300.134786528633,300.211361295348,300.287914624742,300.364472022747,300.403552241375,
300.488221232992,300.57303568504,300.658049003277,300.743148418786,300.828367807318,
300.902323432038,300.983880411665,301.065362260631,301.149295351148,301.230622591178,
301.315858606939,301.4010946227,301.480505821178,301.559935445727,301.639394256677,
301.718926080132,301.79849960656,301.878156730524,301.899865813363,301.978262059829,
302.056590094759,302.135466386161,302.213700289115,302.291913310575,302.370118438689,
302.44948893551,302.527739594342,302.607670010156,302.687600425971),
 .UNSPECIFIED.);
#3398=B_SPLINE_CURVE_WITH_KNOTS('',3,(#56137,#56138,#56139,#56140,#56141,
#56142,#56143,#56144,#56145,#56146,#56147,#56148,#56149,#56150,#56151,#56152,
#56153,#56154,#56155,#56156,#56157,#56158,#56159,#56160,#56161,#56162,#56163,
#56164,#56165,#56166,#56167,#56168,#56169,#56170,#56171,#56172,#56173,#56174,
#56175,#56176,#56177,#56178,#56179,#56180,#56181,#56182,#56183,#56184,#56185,
#56186,#56187,#56188,#56189,#56190,#56191,#56192,#56193,#56194,#56195,#56196,
#56197,#56198,#56199,#56200,#56201,#56202,#56203,#56204,#56205,#56206,#56207,
#56208,#56209,#56210,#56211,#56212,#56213,#56214,#56215,#56216,#56217,#56218,
#56219,#56220,#56221,#56222,#56223,#56224,#56225,#56226,#56227,#56228,#56229,
#56230,#56231,#56232,#56233,#56234,#56235,#56236,#56237,#56238,#56239,#56240,
#56241,#56242,#56243,#56244,#56245,#56246,#56247,#56248,#56249,#56250,#56251,
#56252,#56253,#56254,#56255,#56256,#56257,#56258,#56259,#56260,#56261,#56262,
#56263,#56264,#56265,#56266,#56267,#56268,#56269,#56270,#56271,#56272,#56273,
#56274,#56275,#56276,#56277,#56278,#56279,#56280,#56281,#56282,#56283,#56284,
#56285,#56286,#56287,#56288,#56289,#56290,#56291,#56292,#56293,#56294,#56295,
#56296,#56297,#56298,#56299,#56300,#56301,#56302,#56303,#56304,#56305),
 .UNSPECIFIED.,.F.,.F.,(4,3,3,3,3,3,3,3,3,3,3,3,3,3,3,3,3,3,3,3,3,3,3,3,
3,3,3,3,3,3,3,3,3,3,3,3,3,3,3,3,3,3,3,3,3,3,3,3,3,3,3,3,3,3,3,3,4),(304.73448739821,
304.813891893521,304.893222832093,304.972510106595,305.051759714261,305.069987698783,
305.149398897262,305.22882852181,305.30828733276,305.387819156215,305.467392682644,
305.547049806609,305.568758889445,305.647147268453,305.725469532895,305.803740082354,
305.881973278898,305.960183456575,306.038401591958,306.116627657178,306.194874638735,
306.27315553295,306.351528960704,306.429951959028,306.508491518218,306.56630127077,
306.642372548406,306.718348324853,306.794245381845,306.870080420658,306.945870080755,
307.023116777173,307.098880275434,307.1746511068,307.250444274634,307.328794118999,
307.40471888251,307.484281267302,307.563843652095,307.641413873038,307.718892013558,
307.796293727472,307.873634613767,307.950930227661,308.028203667275,308.105466902582,
308.182733970019,308.260018905523,308.337376907869,308.414772438926,308.492274105693,
308.56138603342,308.645614213841,308.729653534376,308.813572069845,308.897291973851,
308.97167806506),.UNSPECIFIED.);
#3399=B_SPLINE_CURVE_WITH_KNOTS('',3,(#56306,#56307,#56308,#56309,#56310,
#56311,#56312,#56313,#56314,#56315,#56316,#56317,#56318,#56319,#56320,#56321,
#56322,#56323,#56324,#56325,#56326,#56327,#56328,#56329,#56330,#56331,#56332,
#56333,#56334,#56335,#56336,#56337,#56338,#56339,#56340,#56341,#56342,#56343,
#56344,#56345,#56346,#56347,#56348,#56349,#56350,#56351,#56352,#56353,#56354,
#56355,#56356,#56357,#56358,#56359,#56360,#56361,#56362,#56363,#56364,#56365,
#56366,#56367,#56368,#56369,#56370,#56371,#56372,#56373,#56374,#56375,#56376,
#56377,#56378,#56379,#56380,#56381,#56382,#56383,#56384),.UNSPECIFIED.,
 .F.,.F.,(4,3,3,3,3,3,3,3,3,3,3,3,3,3,3,3,3,3,3,3,3,3,3,3,3,3,4),(302.688034846856,
302.767561307616,302.847032310861,302.926460093556,303.007361847711,303.086747157603,
303.166128284763,303.245516298769,303.327555755776,303.407018106382,303.490346116589,
303.573674126795,303.65040470512,303.727068303487,303.803679604715,303.88025437143,
303.956807700825,304.03336509883,304.072445317458,304.157114309076,304.241928761125,
304.326942079363,304.412041494873,304.497260883406,304.57121650812,304.661692225701,
304.734487398087),.UNSPECIFIED.);
#3400=B_SPLINE_CURVE_WITH_KNOTS('',3,(#56386,#56387,#56388,#56389,#56390,
#56391,#56392,#56393,#56394,#56395,#56396,#56397,#56398,#56399,#56400,#56401,
#56402,#56403,#56404,#56405,#56406,#56407,#56408,#56409,#56410,#56411,#56412,
#56413,#56414,#56415,#56416,#56417,#56418,#56419,#56420,#56421,#56422,#56423,
#56424,#56425,#56426,#56427,#56428,#56429,#56430,#56431,#56432,#56433,#56434,
#56435,#56436,#56437,#56438,#56439,#56440,#56441,#56442,#56443,#56444,#56445,
#56446,#56447,#56448,#56449,#56450,#56451,#56452,#56453,#56454,#56455,#56456,
#56457,#56458,#56459,#56460,#56461,#56462,#56463,#56464,#56465,#56466,#56467),
 .UNSPECIFIED.,.F.,.F.,(4,3,3,3,3,3,3,3,3,3,3,3,3,3,3,3,3,3,3,3,3,3,3,3,
3,3,3,4),(302.687600425971,302.766026959837,302.844568635012,302.897408194688,
302.973479472324,303.049455248771,303.125352305763,303.201187344575,303.276977004672,
303.35422370109,303.429987199351,303.505758030717,303.581551198551,303.659901042916,
303.735825806427,303.81538819122,303.894950576013,303.971854137115,304.048665300184,
304.125400326618,304.202067988151,304.278698060654,304.355305138939,304.431903801529,
304.508536833966,304.585185693517,304.661908603409,304.73448739821),
 .UNSPECIFIED.);
#3401=B_SPLINE_CURVE_WITH_KNOTS('',3,(#56468,#56469,#56470,#56471,#56472,
#56473,#56474,#56475,#56476,#56477,#56478,#56479,#56480,#56481,#56482,#56483,
#56484,#56485,#56486,#56487,#56488,#56489,#56490,#56491,#56492,#56493,#56494,
#56495,#56496,#56497,#56498,#56499,#56500,#56501,#56502,#56503,#56504,#56505,
#56506,#56507,#56508,#56509,#56510,#56511,#56512,#56513,#56514,#56515,#56516,
#56517,#56518,#56519,#56520,#56521,#56522,#56523,#56524,#56525,#56526,#56527,
#56528,#56529,#56530,#56531,#56532,#56533,#56534,#56535,#56536,#56537,#56538,
#56539,#56540,#56541,#56542,#56543,#56544,#56545,#56546,#56547,#56548,#56549,
#56550,#56551,#56552,#56553,#56554,#56555,#56556,#56557,#56558,#56559,#56560,
#56561,#56562,#56563,#56564,#56565,#56566,#56567,#56568,#56569,#56570,#56571,
#56572,#56573,#56574,#56575,#56576,#56577,#56578,#56579,#56580,#56581,#56582,
#56583,#56584,#56585,#56586,#56587,#56588,#56589,#56590,#56591,#56592,#56593,
#56594,#56595,#56596,#56597,#56598,#56599,#56600,#56601,#56602,#56603,#56604,
#56605,#56606,#56607,#56608,#56609,#56610,#56611,#56612,#56613,#56614,#56615,
#56616,#56617,#56618,#56619,#56620,#56621,#56622,#56623,#56624,#56625,#56626,
#56627,#56628,#56629,#56630,#56631,#56632,#56633,#56634,#56635,#56636),
 .UNSPECIFIED.,.F.,.F.,(4,3,3,3,3,3,3,3,3,3,3,3,3,3,3,3,3,3,3,3,3,3,3,3,
3,3,3,3,3,3,3,3,3,3,3,3,3,3,3,3,3,3,3,3,3,3,3,3,3,3,3,3,3,3,3,3,4),(304.734487398285,
304.843285397621,304.892492957337,304.976705108798,305.060791136507,305.144672058453,
305.228423844487,305.311961491823,305.391264148,305.468643914331,305.546042075374,
305.623472417947,305.7009897114,305.778556657374,305.856229948821,305.890035338662,
305.969660526523,306.0492129814,306.128705003188,306.208148845203,306.287556723101,
306.366947157223,306.446328707972,306.525712445778,306.605109441108,306.684560058234,
306.764039077673,306.843591217325,306.887577719987,306.964308298312,307.040971896679,
307.117583197907,307.194157964622,307.270711294016,307.347268692021,307.38634891065,
307.471017902268,307.555832354317,307.640845672555,307.725945088065,307.811164476598,
307.885120101312,307.966677080938,308.048158929904,308.132092020422,308.213419260451,
308.298655276213,308.383891291975,308.463302490454,308.542732115002,308.622190925952,
308.701722749408,308.781296275836,308.860953399801,308.882662482637,308.961062075537,
308.971371590973),.UNSPECIFIED.);
#3402=B_SPLINE_CURVE_WITH_KNOTS('',3,(#56642,#56643,#56644,#56645,#56646,
#56647,#56648,#56649,#56650,#56651,#56652,#56653,#56654,#56655,#56656,#56657,
#56658,#56659,#56660,#56661,#56662,#56663,#56664,#56665,#56666,#56667,#56668,
#56669,#56670,#56671,#56672,#56673,#56674,#56675,#56676,#56677,#56678,#56679,
#56680,#56681,#56682,#56683,#56684,#56685,#56686,#56687,#56688,#56689,#56690,
#56691,#56692,#56693,#56694,#56695,#56696,#56697,#56698,#56699,#56700,#56701,
#56702,#56703,#56704,#56705,#56706,#56707,#56708,#56709,#56710,#56711,#56712,
#56713,#56714,#56715,#56716,#56717,#56718,#56719,#56720,#56721,#56722,#56723,
#56724,#56725,#56726,#56727,#56728,#56729,#56730,#56731,#56732,#56733,#56734,
#56735,#56736,#56737,#56738,#56739,#56740,#56741,#56742,#56743,#56744,#56745,
#56746,#56747,#56748,#56749,#56750,#56751,#56752,#56753,#56754,#56755,#56756,
#56757,#56758,#56759,#56760,#56761,#56762,#56763,#56764,#56765,#56766,#56767,
#56768,#56769,#56770,#56771,#56772,#56773,#56774,#56775,#56776,#56777,#56778,
#56779,#56780,#56781,#56782,#56783,#56784,#56785,#56786,#56787,#56788,#56789,
#56790,#56791,#56792,#56793,#56794,#56795,#56796,#56797,#56798),
 .UNSPECIFIED.,.F.,.F.,(4,3,3,3,3,3,3,3,3,3,3,3,3,3,3,3,3,3,3,3,3,3,3,3,
3,3,3,3,3,3,3,3,3,3,3,3,3,3,3,3,3,3,3,3,3,3,3,3,3,3,3,3,4),(311.01767270539,
311.10013491149,311.182596769293,311.265058285648,311.347519467406,311.429980321416,
311.512440854528,311.594901073591,311.677360985454,311.759820596966,311.842279914975,
311.924738946328,312.007197697875,312.089656176463,312.172114388939,312.254572342149,
312.337030042942,312.419487498164,312.501944714662,312.587957409948,312.671282208506,
312.753748814098,312.836214575481,312.918679520071,313.001143675279,313.083607068516,
313.166069727187,313.248531678698,313.330992950451,313.413453569844,313.495913564275,
313.578372961139,313.660831787829,313.743290071736,313.825747840249,313.908205120756,
313.992339235947,314.074805234307,314.157269610913,314.239732475408,314.322193937415,
314.404654106534,314.48711309235,314.56957100443,314.655168499353,314.737633236399,
314.820095008786,314.902554254951,314.985011413189,315.067473932272,315.149931603683,
315.232390394876,315.254350963814),.UNSPECIFIED.);
#3403=B_SPLINE_CURVE_WITH_KNOTS('',3,(#56799,#56800,#56801,#56802,#56803,
#56804,#56805,#56806,#56807,#56808,#56809,#56810,#56811,#56812,#56813,#56814,
#56815,#56816,#56817,#56818,#56819,#56820,#56821,#56822,#56823,#56824,#56825,
#56826,#56827,#56828,#56829,#56830,#56831,#56832,#56833,#56834,#56835,#56836,
#56837,#56838,#56839,#56840,#56841,#56842,#56843,#56844,#56845,#56846,#56847,
#56848,#56849,#56850,#56851,#56852,#56853,#56854,#56855,#56856,#56857,#56858,
#56859,#56860,#56861,#56862,#56863,#56864,#56865,#56866,#56867,#56868,#56869,
#56870,#56871,#56872,#56873,#56874,#56875,#56876,#56877,#56878,#56879,#56880,
#56881,#56882,#56883),.UNSPECIFIED.,.F.,.F.,(4,3,3,3,3,3,3,3,3,3,3,3,3,
3,3,3,3,3,3,3,3,3,3,3,3,3,3,3,4),(308.97167806506,309.055126155017,309.060157224082,
309.137536990412,309.214935151455,309.292365494027,309.36988278748,309.447449733453,
309.5251230249,309.558928414745,309.638553602606,309.718106057483,309.797598079271,
309.877041921286,309.956449799184,310.035840233306,310.115221784055,310.194605521861,
310.274002517192,310.353453134318,310.432932153757,310.51248429341,310.556470796069,
310.63372559496,310.710909566525,310.788029325159,310.865110869191,310.942176575884,
311.017385294333),.UNSPECIFIED.);
#3404=B_SPLINE_CURVE_WITH_KNOTS('',3,(#56885,#56886,#56887,#56888,#56889,
#56890,#56891,#56892,#56893,#56894,#56895,#56896,#56897,#56898,#56899,#56900,
#56901,#56902,#56903,#56904,#56905,#56906,#56907,#56908,#56909,#56910,#56911,
#56912,#56913,#56914,#56915,#56916,#56917,#56918,#56919,#56920,#56921,#56922,
#56923,#56924,#56925,#56926,#56927,#56928,#56929,#56930,#56931,#56932,#56933,
#56934,#56935,#56936,#56937,#56938,#56939,#56940,#56941,#56942,#56943,#56944,
#56945,#56946,#56947,#56948,#56949,#56950,#56951,#56952,#56953,#56954,#56955,
#56956,#56957,#56958,#56959,#56960,#56961,#56962,#56963),.UNSPECIFIED.,
 .F.,.F.,(4,3,3,3,3,3,3,3,3,3,3,3,3,3,3,3,3,3,3,3,3,3,3,3,3,3,4),(308.971371590973,
309.04968622051,309.127951028894,309.206180373963,309.284388586774,309.362607024147,
309.440835101417,309.51908580595,309.597372135917,309.675751415483,309.754181815283,
309.832725838633,309.880204863962,309.956276141598,310.032251918045,310.108148975037,
310.18398401385,310.259773673947,310.337020370365,310.412783868626,310.488554699992,
310.564347867826,310.642697712191,310.718622475702,310.798184860494,310.877747245287,
311.01767270539),.UNSPECIFIED.);
#3405=B_SPLINE_CURVE_WITH_KNOTS('',3,(#56964,#56965,#56966,#56967,#56968,
#56969,#56970,#56971,#56972,#56973,#56974,#56975,#56976,#56977,#56978,#56979,
#56980,#56981,#56982,#56983,#56984,#56985,#56986,#56987,#56988,#56989,#56990,
#56991,#56992,#56993,#56994,#56995,#56996,#56997,#56998,#56999,#57000,#57001,
#57002,#57003,#57004,#57005,#57006,#57007,#57008,#57009,#57010,#57011,#57012,
#57013,#57014,#57015,#57016,#57017,#57018,#57019,#57020,#57021,#57022,#57023,
#57024,#57025,#57026,#57027,#57028,#57029,#57030,#57031,#57032,#57033,#57034,
#57035,#57036,#57037,#57038,#57039,#57040,#57041,#57042,#57043,#57044,#57045,
#57046,#57047,#57048,#57049,#57050,#57051,#57052,#57053,#57054,#57055,#57056,
#57057,#57058,#57059,#57060,#57061,#57062,#57063,#57064,#57065,#57066,#57067,
#57068,#57069,#57070,#57071,#57072,#57073,#57074,#57075,#57076,#57077,#57078,
#57079,#57080,#57081,#57082,#57083,#57084,#57085,#57086,#57087,#57088,#57089,
#57090,#57091,#57092,#57093,#57094,#57095,#57096,#57097,#57098,#57099,#57100,
#57101,#57102,#57103,#57104,#57105,#57106,#57107,#57108,#57109,#57110,#57111,
#57112,#57113,#57114,#57115,#57116,#57117,#57118,#57119,#57120,#57121,#57122,
#57123,#57124,#57125,#57126,#57127,#57128,#57129,#57130,#57131,#57132),
 .UNSPECIFIED.,.F.,.F.,(4,3,3,3,3,3,3,3,3,3,3,3,3,3,3,3,3,3,3,3,3,3,3,3,
3,3,3,3,3,3,3,3,3,3,3,3,3,3,3,3,3,3,3,3,3,3,3,3,3,3,3,3,3,3,3,3,4),(311.017672705475,
311.093653448508,311.169554239541,311.245391850987,311.32412907294,311.399896824238,
311.475655932485,311.551421451453,311.627208438666,311.703067230971,311.778968690416,
311.854962775979,311.875289626612,311.959501778073,312.043587805783,312.12746872773,
312.211220513764,312.294758161101,312.374060817274,312.451440583604,312.528838744648,
312.606269087221,312.683786380673,312.761353326647,312.839026618094,312.872832007937,
312.952457195798,313.032009650675,313.111501672463,313.190945514478,313.270353392376,
313.349743826498,313.429125377247,313.508509115053,313.587906110384,313.667356727509,
313.746835746948,313.826387886601,313.870374389261,313.947104967586,314.023768565952,
314.10037986718,314.176954633894,314.253507963288,314.330065361293,314.369145579924,
314.453814571542,314.538629023591,314.623642341829,314.70874175734,314.793961145872,
314.867916770586,314.949484703759,315.030950764819,315.112353629913,315.193678956862,
315.254776117011),.UNSPECIFIED.);
#3406=B_SPLINE_CURVE_WITH_KNOTS('',3,(#57138,#57139,#57140,#57141,#57142,
#57143,#57144,#57145,#57146,#57147,#57148,#57149,#57150,#57151,#57152,#57153,
#57154,#57155,#57156,#57157,#57158,#57159,#57160,#57161,#57162,#57163,#57164,
#57165,#57166,#57167,#57168,#57169,#57170,#57171,#57172,#57173,#57174,#57175,
#57176,#57177,#57178,#57179,#57180,#57181,#57182,#57183,#57184,#57185,#57186,
#57187,#57188,#57189,#57190,#57191,#57192,#57193,#57194,#57195,#57196,#57197,
#57198,#57199,#57200,#57201,#57202,#57203,#57204,#57205,#57206,#57207,#57208,
#57209,#57210,#57211,#57212,#57213,#57214,#57215,#57216,#57217,#57218,#57219,
#57220,#57221,#57222,#57223,#57224,#57225,#57226,#57227,#57228,#57229,#57230,
#57231,#57232,#57233,#57234,#57235,#57236,#57237,#57238,#57239,#57240,#57241,
#57242,#57243,#57244,#57245,#57246,#57247,#57248,#57249,#57250,#57251,#57252,
#57253,#57254,#57255,#57256,#57257,#57258,#57259,#57260,#57261,#57262,#57263,
#57264,#57265,#57266,#57267,#57268,#57269,#57270,#57271,#57272,#57273,#57274,
#57275,#57276,#57277,#57278,#57279,#57280,#57281,#57282,#57283,#57284,#57285,
#57286,#57287,#57288,#57289,#57290,#57291,#57292,#57293,#57294,#57295,#57296,
#57297,#57298,#57299,#57300,#57301,#57302,#57303,#57304,#57305,#57306),
 .UNSPECIFIED.,.F.,.F.,(4,3,3,3,3,3,3,3,3,3,3,3,3,3,3,3,3,3,3,3,3,3,3,3,
3,3,3,3,3,3,3,3,3,3,3,3,3,3,3,3,3,3,3,3,3,3,3,3,3,3,3,3,3,3,3,3,4),(317.300858012569,
317.405449909472,317.511692304035,317.539267465344,317.61599804367,317.692661642036,
317.769272943265,317.84584770998,317.922401039375,317.99895843738,318.038038656006,
318.122707647623,318.207522099672,318.292535417908,318.377634833418,318.462854221949,
318.536809846669,318.618366826296,318.699848675262,318.78378176578,318.86510900581,
318.95034502157,319.035581037331,319.114992235809,319.194421860357,319.273880671307,
319.353412494762,319.432986021191,319.512643145155,319.534352227994,319.612740607002,
319.691062871444,319.769333420903,319.847566617447,319.925776795124,320.003994930507,
320.082220995727,320.160467977284,320.238748871499,320.317122299253,320.395545297577,
320.474084856767,320.531894609318,320.607965886954,320.683941663401,320.759838720393,
320.835673759206,320.911463419303,320.98871011572,321.064473613981,321.140244445348,
321.216037613181,321.294387457547,321.370312221057,321.44987460585,321.529436990643,
321.537211865788),.UNSPECIFIED.);
#3407=B_SPLINE_CURVE_WITH_KNOTS('',3,(#57307,#57308,#57309,#57310,#57311,
#57312,#57313,#57314,#57315,#57316,#57317,#57318,#57319,#57320,#57321,#57322,
#57323,#57324,#57325,#57326,#57327,#57328,#57329,#57330,#57331,#57332,#57333,
#57334,#57335,#57336,#57337,#57338,#57339,#57340,#57341,#57342,#57343,#57344,
#57345,#57346,#57347,#57348,#57349,#57350,#57351,#57352,#57353,#57354,#57355,
#57356,#57357,#57358,#57359,#57360,#57361,#57362,#57363,#57364,#57365,#57366,
#57367,#57368,#57369,#57370,#57371,#57372,#57373,#57374,#57375,#57376,#57377,
#57378,#57379,#57380,#57381,#57382),.UNSPECIFIED.,.F.,.F.,(4,3,3,3,3,3,
3,3,3,3,3,3,3,3,3,3,3,3,3,3,3,3,3,3,3,4),(315.254350963814,315.336812567544,
315.419273505396,315.501733804768,315.584193493056,315.666652597654,315.749111145955,
315.831569165347,315.91402668322,316.000703641305,316.083170426846,316.165635539914,
316.248099090161,316.330561187221,316.413021940702,316.495481460198,316.577939855283,
316.660397235517,316.742863621203,316.825326822711,316.907787278561,316.990245427116,
317.072711030869,317.155170909257,317.237635020509,317.300858012569),
 .UNSPECIFIED.);
#3408=B_SPLINE_CURVE_WITH_KNOTS('',3,(#57384,#57385,#57386,#57387,#57388,
#57389,#57390,#57391,#57392,#57393,#57394,#57395,#57396,#57397,#57398,#57399,
#57400,#57401,#57402,#57403,#57404,#57405,#57406,#57407,#57408,#57409,#57410,
#57411,#57412,#57413,#57414,#57415,#57416,#57417,#57418,#57419,#57420,#57421,
#57422,#57423,#57424,#57425,#57426,#57427,#57428,#57429,#57430,#57431,#57432,
#57433,#57434,#57435,#57436,#57437,#57438,#57439,#57440,#57441,#57442,#57443,
#57444,#57445,#57446,#57447,#57448,#57449,#57450,#57451,#57452,#57453,#57454,
#57455,#57456,#57457,#57458,#57459,#57460,#57461,#57462,#57463,#57464,#57465,
#57466,#57467,#57468),.UNSPECIFIED.,.F.,.F.,(4,3,3,3,3,3,3,3,3,3,3,3,3,
3,3,3,3,3,3,3,3,3,3,3,3,3,3,3,4),(315.254776117011,315.336001919561,315.366687961249,
315.446099159728,315.525528784276,315.604987595228,315.684519418683,315.764092945111,
315.843750069076,315.865459151911,315.943847530919,316.022169795362,316.10044034482,
316.178673541364,316.256883719042,316.335101854425,316.413327919644,316.491574901202,
316.569855795417,316.648229223171,316.726652221494,316.805191780685,316.863001533236,
316.944912825012,317.026643855742,317.108125228796,317.189456846659,317.270585182372,
317.300858012569),.UNSPECIFIED.);
#3409=B_SPLINE_CURVE_WITH_KNOTS('',3,(#57469,#57470,#57471,#57472,#57473,
#57474,#57475,#57476,#57477,#57478,#57479,#57480,#57481,#57482,#57483,#57484,
#57485,#57486,#57487,#57488,#57489,#57490,#57491,#57492,#57493,#57494,#57495,
#57496,#57497,#57498,#57499,#57500,#57501,#57502,#57503,#57504,#57505,#57506,
#57507,#57508,#57509,#57510,#57511,#57512,#57513,#57514,#57515,#57516,#57517,
#57518,#57519,#57520,#57521,#57522,#57523,#57524,#57525,#57526,#57527,#57528,
#57529,#57530,#57531,#57532,#57533,#57534,#57535,#57536,#57537,#57538,#57539,
#57540,#57541,#57542,#57543,#57544,#57545,#57546,#57547,#57548,#57549,#57550,
#57551,#57552,#57553,#57554,#57555,#57556,#57557,#57558,#57559,#57560,#57561,
#57562,#57563,#57564,#57565,#57566,#57567,#57568,#57569,#57570,#57571,#57572,
#57573,#57574,#57575,#57576,#57577,#57578,#57579,#57580,#57581,#57582,#57583,
#57584,#57585,#57586,#57587,#57588,#57589,#57590,#57591,#57592,#57593,#57594,
#57595,#57596,#57597,#57598,#57599,#57600,#57601,#57602,#57603,#57604,#57605,
#57606,#57607,#57608,#57609,#57610,#57611,#57612,#57613,#57614,#57615,#57616,
#57617,#57618,#57619,#57620,#57621,#57622,#57623,#57624,#57625),
 .UNSPECIFIED.,.F.,.F.,(4,3,3,3,3,3,3,3,3,3,3,3,3,3,3,3,3,3,3,3,3,3,3,3,
3,3,3,3,3,3,3,3,3,3,3,3,3,3,3,3,3,3,3,3,3,3,3,3,3,3,3,3,4),(317.300858012569,
317.383320218669,317.465782076472,317.548243592827,317.630704774585,317.713165628595,
317.795626161707,317.87808638077,317.960546292633,318.043005904145,318.125465222154,
318.207924253507,318.290383005054,318.372841483642,318.455299696117,318.537757649328,
318.620215350121,318.702672805343,318.785130021841,318.871142717127,318.954467515685,
319.036934121277,319.11939988266,319.20186482725,319.284328982458,319.366792375695,
319.449255034366,319.531716985877,319.61417825763,319.696638877023,319.779098871454,
319.861558268318,319.944017095009,320.026475378916,320.108933147429,320.191390427935,
320.275524543126,320.357990541486,320.440454918092,320.522917782588,320.605379244594,
320.687839413713,320.770298399529,320.85275631161,320.938353806533,321.020818543579,
321.103280315965,321.18573956213,321.268196720369,321.350659239451,321.433116910862,
321.515575702055,321.537536270993),.UNSPECIFIED.);
#3410=B_SPLINE_CURVE_WITH_KNOTS('',3,(#57631,#57632,#57633,#57634,#57635,
#57636,#57637,#57638,#57639,#57640,#57641,#57642,#57643,#57644,#57645,#57646,
#57647,#57648,#57649,#57650,#57651,#57652,#57653,#57654,#57655,#57656,#57657,
#57658,#57659,#57660,#57661,#57662,#57663,#57664,#57665,#57666,#57667,#57668,
#57669,#57670,#57671,#57672,#57673,#57674,#57675,#57676,#57677,#57678,#57679,
#57680,#57681,#57682,#57683,#57684,#57685,#57686,#57687,#57688,#57689,#57690,
#57691,#57692,#57693,#57694,#57695,#57696,#57697,#57698,#57699,#57700,#57701,
#57702,#57703,#57704,#57705,#57706,#57707,#57708,#57709,#57710,#57711,#57712,
#57713,#57714,#57715,#57716,#57717,#57718,#57719,#57720,#57721,#57722,#57723,
#57724,#57725,#57726,#57727,#57728,#57729,#57730,#57731,#57732,#57733,#57734,
#57735,#57736,#57737,#57738,#57739,#57740,#57741,#57742,#57743,#57744,#57745,
#57746,#57747,#57748,#57749,#57750,#57751,#57752,#57753,#57754,#57755,#57756,
#57757,#57758,#57759,#57760,#57761,#57762,#57763,#57764,#57765,#57766,#57767,
#57768,#57769,#57770,#57771,#57772,#57773,#57774,#57775,#57776,#57777,#57778,
#57779,#57780,#57781,#57782,#57783,#57784,#57785,#57786,#57787,#57788,#57789,
#57790,#57791,#57792,#57793,#57794,#57795,#57796),.UNSPECIFIED.,.F.,.F.,
(4,3,3,3,3,3,3,3,3,3,3,3,3,3,3,3,3,3,3,3,3,3,3,3,3,3,3,3,3,3,3,3,3,3,3,
3,3,3,3,3,3,3,3,3,3,3,3,3,3,3,3,3,3,3,3,4),(323.584043319834,323.662939677337,
323.741758955307,323.820514918581,323.899221285436,323.977894112601,324.056548709419,
324.135197457686,324.213852733542,324.292559073698,324.371290225758,324.450103140527,
324.522064134618,324.598794712943,324.67545831131,324.752069612538,324.828644379253,
324.905197708647,324.981755106653,325.02083532528,325.105504316898,325.190318768946,
325.275332087183,325.360431502692,325.445650891224,325.519606515943,325.601163495569,
325.682645344536,325.766578435053,325.847905675083,325.933141690844,326.018377706605,
326.097788905084,326.177218529632,326.256677340582,326.336209164037,326.415782690466,
326.49543981443,326.517148897268,326.595537276276,326.673859540719,326.752130090177,
326.830363286721,326.908573464398,326.986791599782,327.065017665001,327.143264646559,
327.221545540774,327.299918968528,327.378341966852,327.456881526042,327.514691278593,
327.591422594397,327.667397616857,327.744507079332,327.821616541808),
 .UNSPECIFIED.);
#3411=B_SPLINE_CURVE_WITH_KNOTS('',3,(#57797,#57798,#57799,#57800,#57801,
#57802,#57803,#57804,#57805,#57806,#57807,#57808,#57809,#57810,#57811,#57812,
#57813,#57814,#57815,#57816,#57817,#57818,#57819,#57820,#57821,#57822,#57823,
#57824,#57825,#57826,#57827,#57828,#57829,#57830,#57831,#57832,#57833,#57834,
#57835,#57836,#57837,#57838,#57839,#57840,#57841,#57842,#57843,#57844,#57845,
#57846,#57847,#57848,#57849,#57850,#57851,#57852,#57853,#57854,#57855,#57856,
#57857,#57858,#57859,#57860,#57861,#57862,#57863,#57864,#57865,#57866,#57867,
#57868,#57869,#57870,#57871,#57872,#57873,#57874,#57875,#57876,#57877,#57878),
 .UNSPECIFIED.,.F.,.F.,(4,3,3,3,3,3,3,3,3,3,3,3,3,3,3,3,3,3,3,3,3,3,3,3,
3,3,3,4),(321.537211865788,321.614772155658,321.692241935962,321.769636854507,
321.846972505409,321.924264440088,322.001536224865,322.078799211522,322.156067436099,
322.233354934908,322.31071612535,322.388116108845,322.465620272822,322.526979371968,
322.611191523429,322.695277551139,322.779158473085,322.862910259119,322.946447906456,
323.025750562631,323.103130328962,323.180528490006,323.257958832578,323.335476126032,
323.413043072006,323.490716363454,323.524521753293,323.584043319749),
 .UNSPECIFIED.);
#3412=B_SPLINE_CURVE_WITH_KNOTS('',3,(#57880,#57881,#57882,#57883,#57884,
#57885,#57886,#57887,#57888,#57889,#57890,#57891,#57892,#57893,#57894,#57895,
#57896,#57897,#57898,#57899,#57900,#57901,#57902,#57903,#57904,#57905,#57906,
#57907,#57908,#57909,#57910,#57911,#57912,#57913,#57914,#57915,#57916,#57917,
#57918,#57919,#57920,#57921,#57922,#57923,#57924,#57925,#57926,#57927,#57928,
#57929,#57930,#57931,#57932,#57933,#57934,#57935,#57936,#57937,#57938,#57939,
#57940,#57941,#57942,#57943,#57944,#57945,#57946,#57947,#57948,#57949,#57950,
#57951,#57952,#57953,#57954,#57955),.UNSPECIFIED.,.F.,.F.,(4,3,3,3,3,3,
3,3,3,3,3,3,3,3,3,3,3,3,3,3,3,3,3,3,3,4),(321.537536270993,321.619997874724,
321.702458812576,321.784919111948,321.867378800236,321.949837904834,322.032296453135,
322.114754472527,322.1972119904,322.283888948484,322.366355734025,322.448820847093,
322.531284397341,322.613746494401,322.696207247882,322.778666767378,322.861125162463,
322.943582542697,323.026048928383,323.108512129891,323.190972585741,323.273430734296,
323.355896338049,323.438356216437,323.520820327689,323.584043319749),
 .UNSPECIFIED.);
#3413=B_SPLINE_CURVE_WITH_KNOTS('',3,(#57956,#57957,#57958,#57959,#57960,
#57961,#57962,#57963,#57964,#57965,#57966,#57967,#57968,#57969,#57970,#57971,
#57972,#57973,#57974,#57975,#57976,#57977,#57978,#57979,#57980,#57981,#57982,
#57983,#57984,#57985,#57986,#57987,#57988,#57989,#57990,#57991,#57992,#57993,
#57994,#57995,#57996,#57997,#57998,#57999,#58000,#58001,#58002,#58003,#58004,
#58005,#58006,#58007,#58008,#58009,#58010,#58011,#58012,#58013,#58014,#58015,
#58016,#58017,#58018,#58019,#58020,#58021,#58022,#58023,#58024,#58025,#58026,
#58027,#58028,#58029,#58030,#58031,#58032,#58033,#58034,#58035,#58036,#58037,
#58038,#58039,#58040,#58041,#58042,#58043,#58044,#58045,#58046,#58047,#58048,
#58049,#58050,#58051,#58052,#58053,#58054,#58055,#58056,#58057,#58058,#58059,
#58060,#58061,#58062,#58063,#58064,#58065,#58066,#58067,#58068,#58069,#58070,
#58071,#58072,#58073,#58074,#58075,#58076,#58077,#58078,#58079,#58080,#58081,
#58082,#58083,#58084,#58085,#58086,#58087,#58088,#58089,#58090,#58091,#58092,
#58093,#58094,#58095,#58096,#58097,#58098,#58099,#58100,#58101,#58102,#58103,
#58104,#58105,#58106,#58107,#58108,#58109,#58110,#58111,#58112,#58113,#58114,
#58115,#58116,#58117,#58118,#58119,#58120,#58121),.UNSPECIFIED.,.F.,.F.,
(4,3,3,3,3,3,3,3,3,3,3,3,3,3,3,3,3,3,3,3,3,3,3,3,3,3,3,3,3,3,3,3,3,3,3,
3,3,3,3,3,3,3,3,3,3,3,3,3,3,3,3,3,3,3,3,4),(323.584043319749,323.690372261978,
323.800918922704,323.84579820251,323.921869480146,323.997845256593,324.073742313585,
324.149577352398,324.225367012495,324.302613708912,324.378377207173,324.45414803854,
324.529941206373,324.608291050739,324.684215814249,324.763778199042,324.843340583835,
324.920910804778,324.998388945298,325.075790659212,325.153131545507,325.230427159401,
325.307700599015,325.384963834322,325.462230901759,325.539515837263,325.61687383961,
325.694269370667,325.771771037434,325.84088296516,325.925095116621,326.009181144331,
326.093062066277,326.176813852311,326.260351499648,326.339654155823,326.417033922154,
326.494432083197,326.57186242577,326.649379719223,326.726946665197,326.804619956644,
326.838425346485,326.918051138193,326.997604073827,327.077096453802,327.15654053185,
327.239601489672,327.318990669289,327.398371309586,327.477754480676,327.5571512529,
327.63659935889,327.716076312641,327.795620307696,327.821028194423),
 .UNSPECIFIED.);
#3414=B_SPLINE_CURVE_WITH_KNOTS('',3,(#58127,#58128,#58129,#58130,#58131,
#58132,#58133,#58134,#58135,#58136,#58137,#58138,#58139,#58140,#58141,#58142,
#58143,#58144,#58145,#58146,#58147,#58148,#58149,#58150,#58151,#58152,#58153,
#58154,#58155,#58156,#58157,#58158,#58159,#58160,#58161,#58162,#58163,#58164,
#58165,#58166,#58167,#58168,#58169,#58170,#58171,#58172,#58173,#58174,#58175,
#58176,#58177,#58178,#58179,#58180,#58181,#58182,#58183,#58184,#58185,#58186,
#58187,#58188,#58189,#58190,#58191,#58192,#58193,#58194,#58195,#58196,#58197,
#58198,#58199,#58200,#58201,#58202,#58203,#58204,#58205,#58206,#58207,#58208,
#58209,#58210,#58211,#58212,#58213,#58214,#58215,#58216,#58217,#58218,#58219,
#58220,#58221,#58222,#58223,#58224,#58225,#58226,#58227,#58228,#58229,#58230,
#58231,#58232,#58233,#58234,#58235,#58236,#58237,#58238,#58239,#58240,#58241,
#58242,#58243,#58244,#58245,#58246,#58247,#58248,#58249,#58250,#58251,#58252,
#58253,#58254,#58255,#58256,#58257,#58258,#58259,#58260,#58261,#58262,#58263,
#58264,#58265,#58266,#58267,#58268,#58269,#58270,#58271,#58272,#58273,#58274,
#58275,#58276,#58277,#58278,#58279,#58280,#58281,#58282,#58283,#58284,#58285,
#58286,#58287,#58288,#58289,#58290,#58291,#58292,#58293,#58294,#58295),
 .UNSPECIFIED.,.F.,.F.,(4,3,3,3,3,3,3,3,3,3,3,3,3,3,3,3,3,3,3,3,3,3,3,3,
3,3,3,3,3,3,3,3,3,3,3,3,3,3,3,3,3,3,3,3,3,3,3,3,3,3,3,3,3,3,3,3,4),(329.867228626928,
329.943617592086,330.008547231905,330.085926998236,330.163325159279,330.240755501852,
330.318272795305,330.395839741279,330.473513032726,330.507318422567,330.586943610428,
330.666496065305,330.745988087093,330.825431929108,330.904839807006,330.984230241128,
331.063611791877,331.142995529683,331.222392525014,331.301843142139,331.381322161578,
331.46087430123,331.504860803892,331.581591382217,331.658254980583,331.734866281812,
331.811441048527,331.887994377921,331.964551775926,332.003631994555,332.088300986173,
332.173115438222,332.25812875646,332.34322817197,332.428447560503,332.502403185217,
332.583960164843,332.665442013809,332.749375104327,332.830702344356,332.915938360118,
333.00117437588,333.080585574359,333.160015198907,333.239474009857,333.319005833312,
333.398579359741,333.478236483706,333.499945566542,333.57832772668,333.656647218315,
333.734917102583,333.813150409088,333.891367812278,333.969574304964,334.047801090439,
334.103512245329),.UNSPECIFIED.);
#3415=B_SPLINE_CURVE_WITH_KNOTS('',3,(#58296,#58297,#58298,#58299,#58300,
#58301,#58302,#58303,#58304,#58305,#58306,#58307,#58308,#58309,#58310,#58311,
#58312,#58313,#58314,#58315,#58316,#58317,#58318,#58319,#58320,#58321,#58322,
#58323,#58324,#58325,#58326,#58327,#58328,#58329,#58330,#58331,#58332,#58333,
#58334,#58335,#58336,#58337,#58338,#58339,#58340,#58341,#58342,#58343,#58344,
#58345,#58346,#58347,#58348,#58349,#58350,#58351,#58352,#58353,#58354,#58355,
#58356,#58357,#58358,#58359,#58360,#58361,#58362,#58363,#58364,#58365,#58366,
#58367,#58368,#58369,#58370,#58371,#58372,#58373,#58374),.UNSPECIFIED.,
 .F.,.F.,(4,3,3,3,3,3,3,3,3,3,3,3,3,3,3,3,3,3,3,3,3,3,3,3,3,3,4),(327.821616541808,
327.897404677541,327.974258300338,328.050021802456,328.125793182404,328.201587443917,
328.279248997918,328.355175127646,328.433704393782,328.512233659918,328.589803880861,
328.667282021381,328.744683735295,328.82202462159,328.899320235484,328.976593675098,
329.053856910405,329.131123977842,329.208408913346,329.285766915693,329.36316244675,
329.440664113517,329.509776041242,329.599849599845,329.689690847903,329.778994110244,
329.867228626851),.UNSPECIFIED.);
#3416=B_SPLINE_CURVE_WITH_KNOTS('',3,(#58376,#58377,#58378,#58379,#58380,
#58381,#58382,#58383,#58384,#58385,#58386,#58387,#58388,#58389,#58390,#58391,
#58392,#58393,#58394,#58395,#58396,#58397,#58398,#58399,#58400,#58401,#58402,
#58403,#58404,#58405,#58406,#58407,#58408,#58409,#58410,#58411,#58412,#58413,
#58414,#58415,#58416,#58417,#58418,#58419,#58420,#58421,#58422,#58423,#58424,
#58425,#58426,#58427,#58428,#58429,#58430,#58431,#58432,#58433,#58434,#58435,
#58436,#58437,#58438,#58439,#58440,#58441,#58442,#58443,#58444,#58445,#58446,
#58447,#58448,#58449,#58450,#58451,#58452,#58453,#58454,#58455,#58456,#58457,
#58458,#58459,#58460),.UNSPECIFIED.,.F.,.F.,(4,3,3,3,3,3,3,3,3,3,3,3,3,
3,3,3,3,3,3,3,3,3,3,3,3,3,3,3,4),(327.821028194423,327.83596772781,327.912698306135,
327.989361904502,328.06597320573,328.142547972445,328.21910130184,328.295658699845,
328.334738918472,328.419407910089,328.504222362138,328.589235680374,328.674335095884,
328.759554484416,328.833510109135,328.915067088762,328.996548937728,329.080482028246,
329.161809268276,329.247045284036,329.332281299797,329.411692498275,329.491122122823,
329.570580933772,329.650112757227,329.729686283655,329.80934340762,329.83105249046,
329.867228626928),.UNSPECIFIED.);
#3417=B_SPLINE_CURVE_WITH_KNOTS('',3,(#58461,#58462,#58463,#58464,#58465,
#58466,#58467,#58468,#58469,#58470,#58471,#58472,#58473,#58474,#58475,#58476,
#58477,#58478,#58479,#58480,#58481,#58482,#58483,#58484,#58485,#58486,#58487,
#58488,#58489,#58490,#58491,#58492,#58493,#58494,#58495,#58496,#58497,#58498,
#58499,#58500,#58501,#58502,#58503,#58504,#58505,#58506,#58507,#58508,#58509,
#58510,#58511,#58512,#58513,#58514,#58515,#58516,#58517,#58518,#58519,#58520,
#58521,#58522,#58523,#58524,#58525,#58526,#58527,#58528,#58529,#58530,#58531,
#58532,#58533,#58534,#58535,#58536,#58537,#58538,#58539,#58540,#58541,#58542,
#58543,#58544,#58545,#58546,#58547,#58548,#58549,#58550,#58551,#58552,#58553,
#58554,#58555,#58556,#58557,#58558,#58559,#58560,#58561,#58562,#58563,#58564,
#58565,#58566,#58567,#58568,#58569,#58570,#58571,#58572,#58573,#58574,#58575,
#58576,#58577,#58578,#58579,#58580,#58581,#58582,#58583,#58584,#58585,#58586,
#58587,#58588,#58589,#58590,#58591,#58592,#58593,#58594,#58595,#58596,#58597,
#58598,#58599,#58600,#58601,#58602,#58603,#58604,#58605,#58606,#58607,#58608,
#58609,#58610,#58611,#58612,#58613,#58614,#58615,#58616,#58617,#58618,#58619,
#58620,#58621,#58622,#58623,#58624,#58625,#58626,#58627,#58628,#58629),
 .UNSPECIFIED.,.F.,.F.,(4,3,3,3,3,3,3,3,3,3,3,3,3,3,3,3,3,3,3,3,3,3,3,3,
3,3,3,3,3,3,3,3,3,3,3,3,3,3,3,3,3,3,3,3,3,3,3,3,3,3,3,3,3,3,3,3,4),(329.867228627004,
329.94526820949,330.023241864104,330.101164479558,330.179050907982,330.260243903457,
330.338119015045,330.4160050831,330.493915536161,330.571863814,330.649904125189,
330.727998408715,330.806198926277,330.828594871785,330.904666149421,330.980641925868,
331.05653898286,331.132374021673,331.20816368177,331.285410378187,331.361173876448,
331.436944707815,331.512737875648,331.591087720014,331.667012483524,331.746574868317,
331.82613725311,331.903707474053,331.981185614573,332.058587328486,332.135928214781,
332.213223828676,332.29049726829,332.367760503597,332.445027571034,332.522312506538,
332.599670508884,332.677066039942,332.754567706709,332.823679634434,332.907891785895,
332.991977813603,333.07585873555,333.159610521584,333.24314816892,333.322450825097,
333.399830591428,333.477228752471,333.554659095044,333.632176388497,333.709743334471,
333.787416625919,333.821222015759,333.900842101732,333.9803980806,334.059886867007,
334.104199260309),.UNSPECIFIED.);
#3418=B_SPLINE_CURVE_WITH_KNOTS('',3,(#58635,#58636,#58637,#58638,#58639,
#58640,#58641,#58642,#58643,#58644,#58645,#58646,#58647,#58648,#58649,#58650,
#58651,#58652,#58653,#58654,#58655,#58656,#58657,#58658,#58659,#58660,#58661,
#58662,#58663,#58664,#58665,#58666,#58667,#58668,#58669,#58670,#58671,#58672,
#58673,#58674,#58675,#58676,#58677,#58678,#58679,#58680,#58681,#58682,#58683,
#58684,#58685,#58686,#58687,#58688,#58689,#58690,#58691,#58692,#58693,#58694,
#58695,#58696,#58697,#58698,#58699,#58700,#58701,#58702,#58703,#58704,#58705,
#58706,#58707,#58708,#58709,#58710,#58711,#58712,#58713,#58714,#58715,#58716,
#58717,#58718,#58719,#58720,#58721,#58722,#58723,#58724,#58725,#58726,#58727,
#58728,#58729,#58730,#58731,#58732,#58733,#58734,#58735,#58736,#58737,#58738,
#58739,#58740,#58741,#58742,#58743,#58744,#58745,#58746,#58747,#58748,#58749,
#58750,#58751,#58752,#58753,#58754,#58755,#58756,#58757,#58758,#58759,#58760,
#58761,#58762,#58763,#58764,#58765,#58766,#58767,#58768,#58769,#58770,#58771,
#58772,#58773,#58774,#58775,#58776,#58777,#58778,#58779,#58780,#58781,#58782,
#58783,#58784,#58785,#58786,#58787,#58788,#58789,#58790,#58791,#58792,#58793,
#58794,#58795,#58796,#58797),.UNSPECIFIED.,.F.,.F.,(4,3,3,3,3,3,3,3,3,3,
3,3,3,3,3,3,3,3,3,3,3,3,3,3,3,3,3,3,3,3,3,3,3,3,3,3,3,3,3,3,3,3,3,3,3,3,
3,3,3,3,3,3,3,3,4),(336.150413934233,336.236030499722,336.321889399997,
336.408114041914,336.492572710517,336.576784861978,336.660870889689,336.744751811636,
336.82850359767,336.912041245007,336.991343901179,337.068723667509,337.146121828553,
337.223552171125,337.301069464577,337.378636410551,337.456309701998,337.490115091842,
337.569740279703,337.64929273458,337.728784756368,337.808228598383,337.887636476281,
337.967026910403,338.046408461153,338.125792198958,338.205189194289,338.284639811415,
338.364118830854,338.443670970506,338.487657473166,338.564388051491,338.641051649857,
338.717662951085,338.7942377178,338.870791047194,338.947348445198,338.986428663829,
339.071097655448,339.155912107497,339.240925425735,339.326024841245,339.411244229778,
339.485199854491,339.566756834117,339.648238683083,339.7321717736,339.81349901363,
339.898735029392,339.983971045154,340.063375337463,340.144249967054,340.223725417313,
340.30529963657,340.386873855827),.UNSPECIFIED.);
#3419=B_SPLINE_CURVE_WITH_KNOTS('',3,(#58798,#58799,#58800,#58801,#58802,
#58803,#58804,#58805,#58806,#58807,#58808,#58809,#58810,#58811,#58812,#58813,
#58814,#58815,#58816,#58817,#58818,#58819,#58820,#58821,#58822,#58823,#58824,
#58825,#58826,#58827,#58828,#58829,#58830,#58831,#58832,#58833,#58834,#58835,
#58836,#58837,#58838,#58839,#58840,#58841,#58842,#58843,#58844,#58845,#58846,
#58847,#58848,#58849,#58850,#58851,#58852,#58853,#58854,#58855,#58856,#58857,
#58858,#58859,#58860,#58861,#58862,#58863,#58864,#58865,#58866,#58867,#58868,
#58869,#58870,#58871,#58872,#58873,#58874,#58875,#58876,#58877,#58878,#58879),
 .UNSPECIFIED.,.F.,.F.,(4,3,3,3,3,3,3,3,3,3,3,3,3,3,3,3,3,3,3,3,3,3,3,3,
3,3,3,4),(334.103512245329,334.181782034169,334.260708512593,334.339116405703,
334.418302176785,334.497487947867,334.573559225503,334.64953500195,334.725432058942,
334.801267097755,334.877056757853,334.95430345427,335.030066952531,335.105837783897,
335.181630951731,335.259980796096,335.335905559607,335.415467944399,335.495030329192,
335.576953279807,335.65566819483,335.734299732993,335.812860488271,335.891363009308,
335.96981408632,336.048235026965,336.126640203039,336.150413934108),
 .UNSPECIFIED.);
#3420=B_SPLINE_CURVE_WITH_KNOTS('',3,(#58881,#58882,#58883,#58884,#58885,
#58886,#58887,#58888,#58889,#58890,#58891,#58892,#58893,#58894,#58895,#58896,
#58897,#58898,#58899,#58900,#58901,#58902,#58903,#58904,#58905,#58906,#58907,
#58908,#58909,#58910,#58911,#58912,#58913,#58914,#58915,#58916,#58917,#58918,
#58919,#58920,#58921,#58922,#58923,#58924,#58925,#58926,#58927,#58928,#58929,
#58930,#58931,#58932,#58933,#58934,#58935,#58936,#58937,#58938,#58939,#58940,
#58941,#58942,#58943,#58944,#58945,#58946,#58947,#58948,#58949,#58950,#58951,
#58952,#58953,#58954,#58955,#58956,#58957,#58958,#58959),.UNSPECIFIED.,
 .F.,.F.,(4,3,3,3,3,3,3,3,3,3,3,3,3,3,3,3,3,3,3,3,3,3,3,3,3,3,4),(334.104199260309,
334.183621542074,334.263019438394,334.342403552811,334.421784958005,334.501174723552,
334.580616024033,334.660081231601,334.739626247106,334.818764397084,334.895494975409,
334.972158573775,335.048769875004,335.125344641718,335.201897971113,335.278455369118,
335.317535587747,335.402204579365,335.487019031413,335.572032349651,335.657131765161,
335.742351153693,335.816306778409,335.900123568842,335.98385277894,336.067438212658,
336.150413934108),.UNSPECIFIED.);
#3421=B_SPLINE_CURVE_WITH_KNOTS('',3,(#58960,#58961,#58962,#58963,#58964,
#58965,#58966,#58967,#58968,#58969,#58970,#58971,#58972,#58973,#58974,#58975,
#58976,#58977,#58978,#58979,#58980,#58981,#58982,#58983,#58984,#58985,#58986,
#58987,#58988,#58989,#58990,#58991,#58992,#58993,#58994,#58995,#58996,#58997,
#58998,#58999,#59000,#59001,#59002,#59003,#59004,#59005,#59006,#59007,#59008,
#59009,#59010,#59011,#59012,#59013,#59014,#59015,#59016,#59017,#59018,#59019,
#59020,#59021,#59022,#59023,#59024,#59025,#59026,#59027,#59028,#59029,#59030,
#59031,#59032,#59033,#59034,#59035,#59036,#59037,#59038,#59039,#59040,#59041,
#59042,#59043,#59044,#59045,#59046,#59047,#59048,#59049,#59050,#59051,#59052,
#59053,#59054,#59055,#59056,#59057,#59058,#59059,#59060,#59061,#59062,#59063,
#59064,#59065,#59066,#59067,#59068,#59069,#59070,#59071,#59072,#59073,#59074,
#59075,#59076,#59077,#59078,#59079,#59080,#59081,#59082,#59083,#59084,#59085,
#59086,#59087,#59088,#59089,#59090,#59091,#59092,#59093,#59094,#59095,#59096,
#59097,#59098,#59099,#59100,#59101,#59102,#59103,#59104,#59105,#59106,#59107,
#59108,#59109,#59110,#59111,#59112,#59113,#59114,#59115,#59116),
 .UNSPECIFIED.,.F.,.F.,(4,3,3,3,3,3,3,3,3,3,3,3,3,3,3,3,3,3,3,3,3,3,3,3,
3,3,3,3,3,3,3,3,3,3,3,3,3,3,3,3,3,3,3,3,3,3,3,3,3,3,3,3,4),(336.150413934108,
336.232876140208,336.315337998011,336.397799514366,336.480260696124,336.562721550134,
336.645182083246,336.727642302309,336.810102214172,336.892561825684,336.975021143693,
337.057480175047,337.139938926594,337.222397405181,337.304855617657,337.387313570867,
337.46977127166,337.552228726882,337.63468594338,337.720698638666,337.804023437224,
337.886490042816,337.968955804199,338.051420748789,338.133884903997,338.216348297234,
338.298810955905,338.381272907416,338.463734179169,338.546194798562,338.628654792993,
338.711114189857,338.793573016547,338.876031300454,338.958489068967,339.040946349474,
339.125080464665,339.207546463025,339.290010839631,339.372473704127,339.454935166133,
339.537395335252,339.619854321068,339.702312233149,339.787909728071,339.870374465117,
339.952836237504,340.035295483669,340.117752641908,340.20021516099,340.282672832401,
340.365131623594,340.387092192532),.UNSPECIFIED.);
#3422=B_SPLINE_CURVE_WITH_KNOTS('',3,(#59122,#59123,#59124,#59125,#59126,
#59127,#59128,#59129,#59130,#59131,#59132,#59133,#59134,#59135,#59136,#59137,
#59138,#59139,#59140,#59141,#59142,#59143,#59144,#59145,#59146,#59147,#59148,
#59149,#59150,#59151,#59152,#59153,#59154,#59155,#59156,#59157,#59158,#59159,
#59160,#59161,#59162,#59163,#59164,#59165,#59166,#59167,#59168,#59169,#59170,
#59171,#59172,#59173,#59174,#59175,#59176,#59177,#59178,#59179,#59180,#59181,
#59182,#59183,#59184,#59185,#59186,#59187,#59188,#59189,#59190,#59191,#59192,
#59193,#59194,#59195,#59196,#59197,#59198,#59199,#59200,#59201,#59202,#59203,
#59204,#59205,#59206,#59207,#59208,#59209,#59210,#59211,#59212,#59213,#59214,
#59215,#59216,#59217,#59218,#59219,#59220,#59221,#59222,#59223,#59224,#59225,
#59226,#59227,#59228,#59229,#59230,#59231,#59232,#59233,#59234,#59235,#59236,
#59237,#59238,#59239,#59240,#59241,#59242,#59243,#59244,#59245,#59246,#59247,
#59248,#59249,#59250,#59251,#59252,#59253,#59254,#59255,#59256,#59257,#59258,
#59259,#59260,#59261,#59262,#59263,#59264,#59265,#59266,#59267,#59268,#59269,
#59270,#59271,#59272,#59273,#59274,#59275,#59276,#59277,#59278,#59279,#59280,
#59281,#59282,#59283,#59284,#59285,#59286,#59287,#59288,#59289,#59290),
 .UNSPECIFIED.,.F.,.F.,(4,3,3,3,3,3,3,3,3,3,3,3,3,3,3,3,3,3,3,3,3,3,3,3,
3,3,3,3,3,3,3,3,3,3,3,3,3,3,3,3,3,3,3,3,3,3,3,3,3,3,3,3,3,3,3,3,4),(342.433599241288,
342.477826998466,342.555397219409,342.632875359929,342.710277073842,342.787617960137,
342.864913574031,342.942187013645,343.019450248952,343.096717316389,343.174002251893,
343.251360254239,343.328755785296,343.406257452063,343.475369379791,343.559581531252,
343.643667558962,343.727548480909,343.811300266943,343.89483791428,343.974140570453,
344.051520336784,344.128918497827,344.2063488404,344.283866133853,344.361433079827,
344.439106371274,344.472911761116,344.552536948977,344.632089403854,344.711581425642,
344.791025267657,344.870433145555,344.949823579677,345.029205130426,345.108588868232,
345.187985863562,345.267436480688,345.346915500127,345.426467639779,345.470454142441,
345.547184720766,345.623848319133,345.700459620361,345.777034387076,345.85358771647,
345.930145114475,345.969225333103,346.053894324721,346.138708776769,346.223722095006,
346.308821510515,346.394040899047,346.467996523766,346.549562547653,346.631038481119,
346.670772567163),.UNSPECIFIED.);
#3423=B_SPLINE_CURVE_WITH_KNOTS('',3,(#59291,#59292,#59293,#59294,#59295,
#59296,#59297,#59298,#59299,#59300,#59301,#59302,#59303,#59304,#59305,#59306,
#59307,#59308,#59309,#59310,#59311,#59312,#59313,#59314,#59315,#59316,#59317,
#59318,#59319,#59320,#59321,#59322,#59323,#59324,#59325,#59326,#59327,#59328,
#59329,#59330,#59331,#59332,#59333,#59334,#59335,#59336,#59337,#59338,#59339,
#59340,#59341,#59342,#59343,#59344,#59345,#59346,#59347,#59348,#59349,#59350,
#59351,#59352,#59353,#59354,#59355,#59356,#59357,#59358,#59359,#59360,#59361,
#59362,#59363,#59364,#59365,#59366,#59367,#59368,#59369,#59370,#59371,#59372,
#59373,#59374,#59375),.UNSPECIFIED.,.F.,.F.,(4,3,3,3,3,3,3,3,3,3,3,3,3,
3,3,3,3,3,3,3,3,3,3,3,3,3,3,3,4),(340.386873855827,340.466533053165,340.482742235816,
340.561130614824,340.639452879266,340.717723428725,340.795956625269,340.874166802946,
340.952384938329,341.030611003548,341.108857985106,341.187138879321,341.265512307075,
341.343935305399,341.422474864589,341.480284617141,341.555819702447,341.631260231986,
341.706623272285,341.781925791665,341.857184684089,341.93242693873,342.007663131993,
342.082908485691,342.15817823038,342.233530905522,342.308928811165,342.384438784184,
342.433599241167),.UNSPECIFIED.);
#3424=B_SPLINE_CURVE_WITH_KNOTS('',3,(#59377,#59378,#59379,#59380,#59381,
#59382,#59383,#59384,#59385,#59386,#59387,#59388,#59389,#59390,#59391,#59392,
#59393,#59394,#59395,#59396,#59397,#59398,#59399,#59400,#59401,#59402,#59403,
#59404,#59405,#59406,#59407,#59408,#59409,#59410,#59411,#59412,#59413,#59414,
#59415,#59416,#59417,#59418,#59419,#59420,#59421,#59422,#59423,#59424,#59425,
#59426,#59427,#59428,#59429,#59430,#59431,#59432,#59433,#59434,#59435,#59436,
#59437,#59438,#59439,#59440,#59441,#59442,#59443,#59444,#59445,#59446,#59447,
#59448,#59449,#59450,#59451,#59452),.UNSPECIFIED.,.F.,.F.,(4,3,3,3,3,3,
3,3,3,3,3,3,3,3,3,3,3,3,3,3,3,3,3,3,3,4),(340.387092192532,340.469553796262,
340.552014734114,340.634475033486,340.716934721774,340.799393826373,340.881852374673,
340.964310394066,341.046767911938,341.133444870023,341.215911655564,341.298376768632,
341.38084031888,341.463302415939,341.54576316942,341.628222688916,341.710681084001,
341.793138464235,341.875604849921,341.958068051429,342.040528507279,342.122986655834,
342.205452259587,342.287912137975,342.370376249227,342.433599241287),
 .UNSPECIFIED.);
#3425=B_SPLINE_CURVE_WITH_KNOTS('',3,(#59453,#59454,#59455,#59456,#59457,
#59458,#59459,#59460,#59461,#59462,#59463,#59464,#59465,#59466,#59467,#59468,
#59469,#59470,#59471,#59472,#59473,#59474,#59475,#59476,#59477,#59478,#59479,
#59480,#59481,#59482,#59483,#59484,#59485,#59486,#59487,#59488,#59489,#59490,
#59491,#59492,#59493,#59494,#59495,#59496,#59497,#59498,#59499,#59500,#59501,
#59502,#59503,#59504,#59505,#59506,#59507,#59508,#59509,#59510,#59511,#59512,
#59513,#59514,#59515,#59516,#59517,#59518,#59519,#59520,#59521,#59522,#59523,
#59524,#59525,#59526,#59527,#59528,#59529,#59530,#59531,#59532,#59533,#59534,
#59535,#59536,#59537,#59538,#59539,#59540,#59541,#59542,#59543,#59544,#59545,
#59546,#59547,#59548,#59549,#59550,#59551,#59552,#59553,#59554,#59555,#59556,
#59557,#59558,#59559,#59560,#59561,#59562,#59563,#59564,#59565,#59566,#59567,
#59568,#59569,#59570,#59571,#59572,#59573,#59574,#59575,#59576,#59577,#59578,
#59579,#59580,#59581,#59582,#59583,#59584,#59585,#59586,#59587,#59588,#59589,
#59590,#59591,#59592,#59593,#59594,#59595,#59596,#59597,#59598,#59599,#59600,
#59601,#59602,#59603,#59604,#59605,#59606,#59607,#59608,#59609,#59610,#59611,
#59612,#59613,#59614,#59615,#59616,#59617,#59618,#59619,#59620,#59621),
 .UNSPECIFIED.,.F.,.F.,(4,3,3,3,3,3,3,3,3,3,3,3,3,3,3,3,3,3,3,3,3,3,3,3,
3,3,3,3,3,3,3,3,3,3,3,3,3,3,3,3,3,3,3,3,3,3,3,3,3,3,3,3,3,3,3,3,4),(342.433599241287,
342.524975292886,342.612060527846,342.699260153072,342.786567572675,342.799103447683,
342.880660427309,342.962142276275,343.046075366793,343.127402606822,343.212638622584,
343.297874638346,343.377285836825,343.456715461373,343.536174272323,343.615706095778,
343.695279622207,343.774936746172,343.796645829008,343.875034208016,343.953356472458,
344.031627021917,344.109860218461,344.188070396138,344.266288531521,344.34451459674,
344.422761578298,344.501042472512,344.579415900267,344.65783889859,344.73637845778,
344.794188210333,344.870259487969,344.946235264416,345.022132321408,345.097967360221,
345.173757020318,345.251003716736,345.326767214997,345.402538046363,345.478331214197,
345.556681058562,345.632605822073,345.712168206865,345.791730591658,345.869307666084,
345.946791336978,346.024197263591,346.104882624974,346.182175985526,346.259443837389,
346.336700224768,346.413959182672,346.491259938658,346.568585405038,346.645976866206,
346.669680154653),.UNSPECIFIED.);
#3426=B_SPLINE_CURVE_WITH_KNOTS('',3,(#59627,#59628,#59629,#59630,#59631,
#59632,#59633,#59634,#59635,#59636,#59637,#59638,#59639,#59640,#59641,#59642,
#59643,#59644,#59645,#59646,#59647,#59648,#59649,#59650,#59651,#59652,#59653,
#59654,#59655,#59656,#59657,#59658,#59659,#59660,#59661,#59662,#59663,#59664,
#59665,#59666,#59667,#59668,#59669,#59670,#59671,#59672,#59673,#59674,#59675,
#59676,#59677,#59678,#59679,#59680,#59681,#59682,#59683,#59684,#59685,#59686,
#59687,#59688,#59689,#59690,#59691,#59692,#59693,#59694,#59695,#59696,#59697,
#59698,#59699,#59700,#59701,#59702,#59703,#59704,#59705,#59706,#59707,#59708,
#59709,#59710,#59711,#59712,#59713,#59714,#59715,#59716,#59717,#59718,#59719,
#59720,#59721,#59722,#59723,#59724,#59725,#59726,#59727,#59728,#59729,#59730,
#59731,#59732,#59733,#59734,#59735,#59736,#59737,#59738,#59739,#59740,#59741,
#59742,#59743,#59744,#59745,#59746,#59747,#59748,#59749,#59750,#59751,#59752,
#59753,#59754,#59755,#59756,#59757,#59758,#59759,#59760,#59761,#59762,#59763,
#59764,#59765,#59766,#59767,#59768,#59769,#59770,#59771,#59772,#59773,#59774,
#59775,#59776,#59777,#59778,#59779,#59780,#59781,#59782,#59783),
 .UNSPECIFIED.,.F.,.F.,(4,3,3,3,3,3,3,3,3,3,3,3,3,3,3,3,3,3,3,3,3,3,3,3,
3,3,3,3,3,3,3,3,3,3,3,3,3,3,3,3,3,3,3,3,3,3,3,3,3,3,3,3,4),(348.716784548467,
348.799246754567,348.88170861237,348.964170128725,349.046631310483,349.129092164493,
349.211552697605,349.294012916668,349.376472828531,349.458932440043,349.541391758052,
349.623850789406,349.706309540952,349.78876801954,349.871226232016,349.953684185226,
350.036141886019,350.118599341241,350.201056557739,350.287069253025,350.370394051583,
350.452860657175,350.535326418558,350.617791363148,350.700255518356,350.782718911593,
350.865181570264,350.947643521776,351.030104793528,351.112565412921,351.195025407352,
351.277484804216,351.359943630907,351.442401914814,351.524859683327,351.607316963833,
351.691451079024,351.773917077384,351.85638145399,351.938844318486,352.021305780492,
352.103765949611,352.186224935427,352.268682847508,352.354280342431,352.436745079477,
352.519206851863,352.601666098028,352.684123256267,352.766585775349,352.84904344676,
352.931502237953,352.953462806892),.UNSPECIFIED.);
#3427=B_SPLINE_CURVE_WITH_KNOTS('',3,(#59784,#59785,#59786,#59787,#59788,
#59789,#59790,#59791,#59792,#59793,#59794,#59795,#59796,#59797,#59798,#59799,
#59800,#59801,#59802,#59803,#59804,#59805,#59806,#59807,#59808,#59809,#59810,
#59811,#59812,#59813,#59814,#59815,#59816,#59817,#59818,#59819,#59820,#59821,
#59822,#59823,#59824,#59825,#59826,#59827,#59828,#59829,#59830,#59831,#59832,
#59833,#59834,#59835,#59836,#59837,#59838,#59839,#59840,#59841,#59842,#59843,
#59844,#59845,#59846,#59847,#59848,#59849,#59850,#59851,#59852,#59853,#59854,
#59855,#59856,#59857,#59858,#59859,#59860,#59861,#59862,#59863,#59864,#59865),
 .UNSPECIFIED.,.F.,.F.,(4,3,3,3,3,3,3,3,3,3,3,3,3,3,3,3,3,3,3,3,3,3,3,3,
3,3,3,4),(346.670772567163,346.752130912072,346.833433265937,346.914669680485,
346.966767714428,347.046178912906,347.125608537454,347.205067348404,347.284599171859,
347.364172698288,347.443829822252,347.465538905091,347.543927284099,347.622249548542,
347.700520098,347.778753294544,347.856963472221,347.935181607604,348.013407672824,
348.091654654381,348.169935548596,348.248308976351,348.326731974674,348.405271533864,
348.463081286415,348.559444813209,348.654143106288,348.716784548467),
 .UNSPECIFIED.);
#3428=B_SPLINE_CURVE_WITH_KNOTS('',3,(#59867,#59868,#59869,#59870,#59871,
#59872,#59873,#59874,#59875,#59876,#59877,#59878,#59879,#59880,#59881,#59882,
#59883,#59884,#59885,#59886,#59887,#59888,#59889,#59890,#59891,#59892,#59893,
#59894,#59895,#59896,#59897,#59898,#59899,#59900,#59901,#59902,#59903,#59904,
#59905,#59906,#59907,#59908,#59909,#59910,#59911,#59912,#59913,#59914,#59915,
#59916,#59917,#59918,#59919,#59920,#59921,#59922,#59923,#59924,#59925,#59926,
#59927,#59928,#59929,#59930,#59931,#59932,#59933,#59934,#59935,#59936,#59937,
#59938,#59939,#59940,#59941,#59942,#59943,#59944,#59945,#59946,#59947,#59948),
 .UNSPECIFIED.,.F.,.F.,(4,3,3,3,3,3,3,3,3,3,3,3,3,3,3,3,3,3,3,3,3,3,3,3,
3,3,3,4),(346.669680154653,346.747191203291,346.789272972983,346.873485124444,
346.957571152154,347.041452074101,347.125203860135,347.208741507471,347.288044163645,
347.365423929975,347.442822091019,347.520252433591,347.597769727044,347.675336673018,
347.753009964465,347.786815354308,347.865689846335,347.944489604546,348.023228416047,
348.10192002307,348.180581543913,348.259227091072,348.337869072739,348.416519892818,
348.495224142986,348.573955300432,348.652768292807,348.716784548467),
 .UNSPECIFIED.);
#3429=B_SPLINE_CURVE_WITH_KNOTS('',3,(#59949,#59950,#59951,#59952,#59953,
#59954,#59955,#59956,#59957,#59958,#59959,#59960,#59961,#59962,#59963,#59964,
#59965,#59966,#59967,#59968,#59969,#59970,#59971,#59972,#59973,#59974,#59975,
#59976,#59977,#59978,#59979,#59980,#59981,#59982,#59983,#59984,#59985,#59986,
#59987,#59988,#59989,#59990,#59991,#59992,#59993,#59994,#59995,#59996,#59997,
#59998,#59999,#60000,#60001,#60002,#60003,#60004,#60005,#60006,#60007,#60008,
#60009,#60010,#60011,#60012,#60013,#60014,#60015,#60016,#60017,#60018,#60019,
#60020,#60021,#60022,#60023,#60024,#60025,#60026,#60027,#60028,#60029,#60030,
#60031,#60032,#60033,#60034,#60035,#60036,#60037,#60038,#60039,#60040,#60041,
#60042,#60043,#60044,#60045,#60046,#60047,#60048,#60049,#60050,#60051,#60052,
#60053,#60054,#60055,#60056,#60057,#60058,#60059,#60060,#60061,#60062,#60063,
#60064,#60065,#60066,#60067,#60068,#60069,#60070,#60071,#60072,#60073,#60074,
#60075,#60076,#60077,#60078,#60079,#60080,#60081,#60082,#60083,#60084,#60085,
#60086,#60087,#60088,#60089,#60090,#60091,#60092,#60093,#60094,#60095,#60096,
#60097,#60098,#60099,#60100,#60101,#60102,#60103,#60104,#60105),
 .UNSPECIFIED.,.F.,.F.,(4,3,3,3,3,3,3,3,3,3,3,3,3,3,3,3,3,3,3,3,3,3,3,3,
3,3,3,3,3,3,3,3,3,3,3,3,3,3,3,3,3,3,3,3,3,3,3,3,3,3,3,3,4),(348.716784548467,
348.799246754567,348.88170861237,348.964170128725,349.046631310483,349.129092164493,
349.211552697605,349.294012916668,349.376472828531,349.458932440043,349.541391758052,
349.623850789406,349.706309540952,349.78876801954,349.871226232015,349.953684185226,
350.036141886019,350.118599341241,350.201056557739,350.287069253025,350.370394051583,
350.452860657175,350.535326418558,350.617791363148,350.700255518356,350.782718911593,
350.865181570265,350.947643521776,351.030104793528,351.112565412921,351.195025407353,
351.277484804217,351.359943630907,351.442401914814,351.524859683327,351.607316963833,
351.691451079025,351.773917077384,351.856381453991,351.938844318486,352.021305780492,
352.103765949612,352.186224935428,352.268682847508,352.354280342431,352.436745079477,
352.519206851863,352.601666098028,352.684123256267,352.76658577535,352.849043446761,
352.931502237954,352.953462806892),.UNSPECIFIED.);
#3430=B_SPLINE_CURVE_WITH_KNOTS('',3,(#60111,#60112,#60113,#60114,#60115,
#60116,#60117,#60118,#60119,#60120,#60121,#60122,#60123,#60124,#60125,#60126,
#60127,#60128,#60129,#60130,#60131,#60132,#60133,#60134,#60135,#60136,#60137,
#60138,#60139,#60140,#60141,#60142,#60143,#60144,#60145,#60146,#60147,#60148,
#60149,#60150,#60151,#60152,#60153,#60154,#60155,#60156,#60157,#60158,#60159,
#60160,#60161,#60162,#60163,#60164,#60165,#60166,#60167,#60168,#60169,#60170,
#60171,#60172,#60173,#60174,#60175,#60176,#60177,#60178,#60179,#60180,#60181,
#60182,#60183,#60184,#60185,#60186,#60187,#60188,#60189,#60190,#60191,#60192,
#60193,#60194,#60195,#60196,#60197,#60198,#60199,#60200,#60201,#60202,#60203,
#60204,#60205,#60206,#60207,#60208,#60209,#60210,#60211,#60212,#60213,#60214,
#60215,#60216,#60217,#60218,#60219,#60220,#60221,#60222,#60223,#60224,#60225,
#60226,#60227,#60228,#60229,#60230,#60231,#60232,#60233,#60234,#60235,#60236,
#60237,#60238,#60239,#60240,#60241,#60242,#60243,#60244,#60245,#60246,#60247,
#60248,#60249,#60250,#60251,#60252,#60253,#60254,#60255,#60256,#60257,#60258,
#60259,#60260,#60261,#60262,#60263,#60264,#60265,#60266,#60267,#60268,#60269,
#60270,#60271,#60272,#60273),.UNSPECIFIED.,.F.,.F.,(4,3,3,3,3,3,3,3,3,3,
3,3,3,3,3,3,3,3,3,3,3,3,3,3,3,3,3,3,3,3,3,3,3,3,3,3,3,3,3,3,3,3,3,3,3,3,
3,3,3,3,3,3,3,3,4),(354.999969855647,355.086348997711,355.176231237206,
355.26338554274,355.354631749215,355.44587795569,355.521949233326,355.597925009773,
355.673822066765,355.749657105578,355.825446765675,355.902693462092,355.978456960353,
356.05422779172,356.130020959553,356.208370803918,356.284295567429,356.363857952222,
356.443420337015,356.520990557958,356.598468698478,356.675870412391,356.753211298687,
356.830506912581,356.907780352195,356.985043587502,357.062310654939,357.139595590443,
357.216953592789,357.294349123846,357.371850790613,357.440962718339,357.5251748698,
357.609260897509,357.693141819456,357.77689360549,357.860431252827,357.939733909002,
358.017113675332,358.094511836376,358.171942178949,358.249459472402,358.327026418376,
358.404699709823,358.438505099664,358.518138949726,358.597698423346,358.677569110537,
358.75700926755,358.836416212645,358.915801039783,358.996016760055,359.075403334798,
359.156033627834,359.236663920869),.UNSPECIFIED.);
#3431=B_SPLINE_CURVE_WITH_KNOTS('',3,(#60274,#60275,#60276,#60277,#60278,
#60279,#60280,#60281,#60282,#60283,#60284,#60285,#60286,#60287,#60288,#60289,
#60290,#60291,#60292,#60293,#60294,#60295,#60296,#60297,#60298,#60299,#60300,
#60301,#60302,#60303,#60304,#60305,#60306,#60307,#60308,#60309,#60310,#60311,
#60312,#60313,#60314,#60315,#60316,#60317,#60318,#60319,#60320,#60321,#60322,
#60323,#60324,#60325,#60326,#60327,#60328,#60329,#60330,#60331,#60332,#60333,
#60334,#60335,#60336,#60337,#60338,#60339,#60340,#60341,#60342,#60343,#60344,
#60345,#60346,#60347,#60348,#60349),.UNSPECIFIED.,.F.,.F.,(4,3,3,3,3,3,
3,3,3,3,3,3,3,3,3,3,3,3,3,3,3,3,3,3,3,4),(352.953462806892,353.035924410622,
353.118385348474,353.200845647846,353.283305336134,353.365764440732,353.448222989033,
353.530681008425,353.613138526298,353.699815484382,353.782282269923,353.864747382991,
353.947210933239,354.029673030299,354.11213378378,354.194593303276,354.277051698362,
354.359509078595,354.441975464281,354.524438665789,354.606899121639,354.689357270194,
354.771822873948,354.854282752335,354.936746863588,354.999969855647),
 .UNSPECIFIED.);
#3432=B_SPLINE_CURVE_WITH_KNOTS('',3,(#60351,#60352,#60353,#60354,#60355,
#60356,#60357,#60358,#60359,#60360,#60361,#60362,#60363,#60364,#60365,#60366,
#60367,#60368,#60369,#60370,#60371,#60372,#60373,#60374,#60375,#60376,#60377,
#60378,#60379,#60380,#60381,#60382,#60383,#60384,#60385,#60386,#60387,#60388,
#60389,#60390,#60391,#60392,#60393,#60394,#60395,#60396,#60397,#60398,#60399,
#60400,#60401,#60402,#60403,#60404,#60405,#60406,#60407,#60408,#60409,#60410,
#60411,#60412,#60413,#60414,#60415,#60416,#60417,#60418,#60419,#60420,#60421,
#60422,#60423,#60424,#60425,#60426),.UNSPECIFIED.,.F.,.F.,(4,3,3,3,3,3,
3,3,3,3,3,3,3,3,3,3,3,3,3,3,3,3,3,3,3,4),(352.953462806892,353.035924410622,
353.118385348474,353.200845647846,353.283305336134,353.365764440732,353.448222989033,
353.530681008425,353.613138526298,353.699815484375,353.782282269916,353.864747382984,
353.947210933232,354.029673030292,354.112133783773,354.194593303269,354.277051698355,
354.359509078588,354.441975464274,354.524438665782,354.606899121632,354.689357270187,
354.77182287394,354.854282752328,354.93674686358,354.999969855537),
 .UNSPECIFIED.);
#3433=B_SPLINE_CURVE_WITH_KNOTS('',3,(#60427,#60428,#60429,#60430,#60431,
#60432,#60433,#60434,#60435,#60436,#60437,#60438,#60439,#60440,#60441,#60442,
#60443,#60444,#60445,#60446,#60447,#60448,#60449,#60450,#60451,#60452,#60453,
#60454,#60455,#60456,#60457,#60458,#60459,#60460,#60461,#60462,#60463,#60464,
#60465,#60466,#60467,#60468,#60469,#60470,#60471,#60472,#60473,#60474,#60475,
#60476,#60477,#60478,#60479,#60480,#60481,#60482,#60483,#60484,#60485,#60486,
#60487,#60488,#60489,#60490,#60491,#60492,#60493,#60494,#60495,#60496,#60497,
#60498,#60499,#60500,#60501,#60502,#60503,#60504,#60505,#60506,#60507,#60508,
#60509,#60510,#60511,#60512,#60513,#60514,#60515,#60516,#60517,#60518,#60519,
#60520,#60521,#60522,#60523,#60524,#60525,#60526,#60527,#60528,#60529,#60530,
#60531,#60532,#60533,#60534,#60535,#60536,#60537,#60538,#60539,#60540,#60541,
#60542,#60543,#60544,#60545,#60546,#60547,#60548,#60549,#60550,#60551,#60552,
#60553,#60554,#60555,#60556,#60557,#60558,#60559,#60560,#60561,#60562,#60563,
#60564,#60565,#60566,#60567,#60568,#60569,#60570,#60571,#60572,#60573,#60574,
#60575,#60576,#60577,#60578,#60579,#60580,#60581,#60582,#60583),
 .UNSPECIFIED.,.F.,.F.,(4,3,3,3,3,3,3,3,3,3,3,3,3,3,3,3,3,3,3,3,3,3,3,3,
3,3,3,3,3,3,3,3,3,3,3,3,3,3,3,3,3,3,3,3,3,3,3,3,3,3,3,3,4),(354.999969855647,
355.082432061747,355.16489391955,355.247355435905,355.329816617663,355.412277471673,
355.494738004785,355.577198223848,355.659658135711,355.742117747223,355.824577065232,
355.907036096586,355.989494848132,356.07195332672,356.154411539196,356.236869492407,
356.3193271932,356.401784648421,356.484241864919,356.570254560205,356.653579358763,
356.736045964355,356.818511725738,356.900976670328,356.983440825536,357.065904218773,
357.148366877444,357.230828828955,357.313290100708,357.395750720101,357.478210714532,
357.560670111396,357.643128938086,357.725587221993,357.808044990506,357.890502271013,
357.974636386204,358.057102384564,358.13956676117,358.222029625665,358.304491087672,
358.386951256791,358.469410242607,358.551868154687,358.63746564961,358.719930386656,
358.802392159042,358.884851405207,358.967308563446,359.049771082529,359.13222875394,
359.214687545133,359.236648114071),.UNSPECIFIED.);
#3434=B_SPLINE_CURVE_WITH_KNOTS('',3,(#60589,#60590,#60591,#60592,#60593,
#60594,#60595,#60596,#60597,#60598,#60599,#60600,#60601,#60602,#60603,#60604,
#60605,#60606,#60607,#60608,#60609,#60610,#60611,#60612,#60613,#60614,#60615,
#60616,#60617,#60618,#60619,#60620,#60621,#60622,#60623,#60624,#60625,#60626,
#60627,#60628,#60629,#60630,#60631,#60632,#60633,#60634,#60635,#60636,#60637,
#60638,#60639,#60640,#60641,#60642,#60643,#60644,#60645,#60646,#60647,#60648,
#60649,#60650,#60651,#60652,#60653,#60654,#60655,#60656,#60657,#60658,#60659,
#60660,#60661,#60662,#60663,#60664,#60665,#60666,#60667,#60668,#60669,#60670,
#60671,#60672,#60673,#60674,#60675,#60676,#60677,#60678,#60679,#60680,#60681,
#60682,#60683,#60684,#60685,#60686,#60687,#60688,#60689,#60690,#60691,#60692,
#60693,#60694,#60695,#60696,#60697,#60698,#60699,#60700,#60701,#60702,#60703,
#60704,#60705,#60706,#60707,#60708,#60709,#60710,#60711,#60712,#60713,#60714,
#60715,#60716,#60717,#60718,#60719,#60720,#60721,#60722,#60723,#60724,#60725,
#60726,#60727,#60728,#60729,#60730,#60731,#60732,#60733,#60734,#60735,#60736,
#60737,#60738,#60739,#60740,#60741,#60742,#60743,#60744,#60745,#60746,#60747,
#60748,#60749,#60750,#60751,#60752,#60753,#60754,#60755,#60756,#60757),
 .UNSPECIFIED.,.F.,.F.,(4,3,3,3,3,3,3,3,3,3,3,3,3,3,3,3,3,3,3,3,3,3,3,3,
3,3,3,3,3,3,3,3,3,3,3,3,3,3,3,3,3,3,3,3,3,3,3,3,3,3,3,3,3,3,3,3,4),(361.283155162826,
361.37946164755,361.431132243639,361.509520622646,361.587842887088,361.666113436546,
361.744346633089,361.822556810765,361.900774946147,361.979001011366,362.057247992923,
362.135528887137,362.213902314891,362.292325313213,362.370864872403,362.428674624964,
362.504745902605,362.580721679058,362.656618736055,362.732453774873,362.808243434975,
362.885490131389,362.961253629656,363.037024461027,363.112817628866,363.191167473222,
363.267092236737,363.346654621513,363.426217006289,363.503787227225,363.581265367739,
363.658667081645,363.736007967934,363.813303581822,363.890577021429,363.96784025673,
364.045107324161,364.122392259659,364.199750261999,364.277145793051,364.354647459812,
364.423759387614,364.507971539074,364.592057566781,364.675938488726,364.759690274757,
364.843227922091,364.922530578276,364.999910344642,365.077308505722,365.154738848331,
365.232256141821,365.309823087832,365.387496379317,365.421301768939,365.50093607667,
365.519850897371),.UNSPECIFIED.);
#3435=B_SPLINE_CURVE_WITH_KNOTS('',3,(#60758,#60759,#60760,#60761,#60762,
#60763,#60764,#60765,#60766,#60767,#60768,#60769,#60770,#60771,#60772,#60773,
#60774,#60775,#60776,#60777,#60778,#60779,#60780,#60781,#60782,#60783,#60784,
#60785,#60786,#60787,#60788,#60789,#60790,#60791,#60792,#60793,#60794,#60795,
#60796,#60797,#60798,#60799,#60800,#60801,#60802,#60803,#60804,#60805,#60806,
#60807,#60808,#60809,#60810,#60811,#60812,#60813,#60814,#60815,#60816,#60817,
#60818,#60819,#60820,#60821,#60822,#60823,#60824,#60825,#60826,#60827,#60828,
#60829,#60830,#60831,#60832,#60833,#60834,#60835,#60836,#60837,#60838,#60839),
 .UNSPECIFIED.,.F.,.F.,(4,3,3,3,3,3,3,3,3,3,3,3,3,3,3,3,3,3,3,3,3,3,3,3,
3,3,3,4),(359.236663920869,359.316144482474,359.395697507158,359.436047480989,
359.512778059315,359.589441657683,359.666052958912,359.742627725628,359.819181055023,
359.895738453029,359.934818671652,360.019487663267,360.104302115312,360.189315433545,
360.274414849052,360.359634237581,360.433589862314,360.515146841945,360.596628690916,
360.680561781431,360.761889021465,360.847125037221,360.932361052977,361.008735782809,
361.085133475983,361.161543131563,361.238009836076,361.283155162716),
 .UNSPECIFIED.);
#3436=B_SPLINE_CURVE_WITH_KNOTS('',3,(#60841,#60842,#60843,#60844,#60845,
#60846,#60847,#60848,#60849,#60850,#60851,#60852,#60853,#60854,#60855,#60856,
#60857,#60858,#60859,#60860,#60861,#60862,#60863,#60864,#60865,#60866,#60867,
#60868,#60869,#60870,#60871,#60872,#60873,#60874,#60875,#60876,#60877,#60878,
#60879,#60880,#60881,#60882,#60883,#60884,#60885,#60886,#60887,#60888,#60889,
#60890,#60891,#60892,#60893,#60894,#60895,#60896,#60897,#60898,#60899,#60900,
#60901,#60902,#60903,#60904,#60905,#60906,#60907,#60908,#60909,#60910,#60911,
#60912,#60913,#60914,#60915,#60916),.UNSPECIFIED.,.F.,.F.,(4,3,3,3,3,3,
3,3,3,3,3,3,3,3,3,3,3,3,3,3,3,3,3,3,3,4),(359.236648114071,359.319109717801,
359.401570655653,359.484030955025,359.566490643313,359.648949747912,359.731408296212,
359.813866315605,359.896323833477,359.983000791562,360.065467577103,360.147932690171,
360.230396240419,360.312858337478,360.395319090959,360.477778610456,360.560237005541,
360.642694385774,360.72516077146,360.807623972968,360.890084428818,360.972542577373,
361.055008181126,361.137468059514,361.219932170767,361.283155162826),
 .UNSPECIFIED.);
#3437=B_SPLINE_CURVE_WITH_KNOTS('',3,(#60917,#60918,#60919,#60920,#60921,
#60922,#60923,#60924,#60925,#60926,#60927,#60928,#60929,#60930,#60931,#60932,
#60933,#60934,#60935,#60936,#60937,#60938,#60939,#60940,#60941,#60942,#60943,
#60944,#60945,#60946,#60947,#60948,#60949,#60950,#60951,#60952,#60953,#60954,
#60955,#60956,#60957,#60958,#60959,#60960,#60961,#60962,#60963,#60964,#60965,
#60966,#60967,#60968,#60969,#60970,#60971,#60972,#60973,#60974,#60975,#60976,
#60977,#60978,#60979,#60980,#60981,#60982,#60983,#60984,#60985,#60986,#60987,
#60988,#60989,#60990,#60991,#60992,#60993,#60994,#60995,#60996,#60997,#60998,
#60999,#61000,#61001,#61002,#61003,#61004,#61005,#61006,#61007,#61008,#61009,
#61010,#61011,#61012,#61013,#61014,#61015,#61016,#61017,#61018,#61019,#61020,
#61021,#61022,#61023,#61024,#61025,#61026,#61027,#61028,#61029,#61030,#61031,
#61032,#61033,#61034,#61035,#61036,#61037,#61038,#61039,#61040,#61041,#61042,
#61043,#61044,#61045,#61046,#61047,#61048,#61049,#61050,#61051,#61052,#61053,
#61054,#61055,#61056,#61057,#61058,#61059,#61060,#61061,#61062,#61063,#61064,
#61065,#61066,#61067,#61068,#61069,#61070,#61071,#61072,#61073,#61074,#61075,
#61076,#61077,#61078,#61079,#61080,#61081,#61082),.UNSPECIFIED.,.F.,.F.,
(4,3,3,3,3,3,3,3,3,3,3,3,3,3,3,3,3,3,3,3,3,3,3,3,3,3,3,3,3,3,3,3,3,3,3,
3,3,3,3,3,3,3,3,3,3,3,3,3,3,3,3,3,3,3,3,4),(361.283242682583,361.361188581313,
361.439167184356,361.517477561481,361.595600258852,361.674004475854,361.752408692856,
361.832033880717,361.911586335594,361.991078357382,362.070522199397,362.149930077295,
362.229320511417,362.308702062166,362.388085799972,362.467482795302,362.546933412428,
362.626412431866,362.705964571519,362.749951074181,362.826681652507,362.903345250875,
362.979956552104,363.05653131882,363.133084648215,363.209642046221,363.248722264844,
363.333391256458,363.418205708503,363.503219026736,363.588318442243,363.673537830771,
363.747493455506,363.829050435137,363.910532284107,363.994465374623,364.075792614657,
364.161028630413,364.246264646169,364.325675844644,364.405105469188,364.484564280135,
364.564096103586,364.643669630011,364.723326753972,364.745035836831,364.823432638934,
364.901761096159,364.98002915517,365.058263041594,365.136475758451,365.214680293984,
365.292914335254,365.371161677635,365.449472774848,365.519433547733),
 .UNSPECIFIED.);
#3438=B_SPLINE_CURVE_WITH_KNOTS('',3,(#61088,#61089,#61090,#61091,#61092,
#61093,#61094,#61095,#61096,#61097,#61098,#61099,#61100,#61101,#61102,#61103,
#61104,#61105,#61106,#61107,#61108,#61109,#61110,#61111,#61112,#61113,#61114,
#61115,#61116,#61117,#61118,#61119,#61120,#61121,#61122,#61123,#61124,#61125,
#61126,#61127,#61128,#61129,#61130,#61131,#61132,#61133,#61134,#61135,#61136,
#61137,#61138,#61139,#61140,#61141,#61142,#61143,#61144,#61145,#61146,#61147,
#61148,#61149,#61150,#61151,#61152,#61153,#61154,#61155,#61156,#61157,#61158,
#61159,#61160,#61161,#61162,#61163,#61164,#61165,#61166,#61167,#61168,#61169,
#61170,#61171,#61172,#61173,#61174,#61175,#61176,#61177,#61178,#61179,#61180,
#61181,#61182,#61183,#61184,#61185,#61186,#61187,#61188,#61189,#61190,#61191,
#61192,#61193,#61194,#61195,#61196,#61197,#61198,#61199,#61200,#61201,#61202,
#61203,#61204,#61205,#61206,#61207,#61208,#61209,#61210,#61211,#61212,#61213,
#61214,#61215,#61216,#61217,#61218,#61219,#61220,#61221,#61222,#61223,#61224,
#61225,#61226,#61227,#61228,#61229,#61230,#61231,#61232,#61233,#61234,#61235,
#61236,#61237,#61238,#61239,#61240,#61241,#61242,#61243,#61244,#61245,#61246,
#61247,#61248,#61249,#61250,#61251,#61252,#61253,#61254,#61255,#61256),
 .UNSPECIFIED.,.F.,.F.,(4,3,3,3,3,3,3,3,3,3,3,3,3,3,3,3,3,3,3,3,3,3,3,3,
3,3,3,3,3,3,3,3,3,3,3,3,3,3,3,3,3,3,3,3,3,3,3,3,3,3,3,3,3,3,3,3,4),(367.566340470006,
367.645827499919,367.725237982588,367.804602928402,367.883927771408,367.915157722251,
367.994568920876,368.073998545579,368.153457356692,368.232989180319,368.312562706926,
368.392219831076,368.413928912913,368.492317290727,368.570639553964,368.648910102208,
368.72714329753,368.805353473978,368.883571608129,368.961797672114,369.040044652437,
369.118325545418,369.196698971949,369.275121969053,369.353661527042,369.411471294238,
369.487542573751,369.563518352073,369.639415410935,369.715250451613,369.791040113569,
369.868286808818,369.944050308916,370.019821142111,370.095614311762,370.173964152712,
370.249888918004,370.329451296783,370.409013675563,370.48658389756,370.56406203915,
370.641463754147,370.718804641539,370.796100256541,370.873373697278,370.950636933715,
371.02790400229,371.105188938938,371.182546942431,371.259942474638,371.337444142551,
371.406556056888,371.490786628699,371.574831076646,371.658755274643,371.742487247285,
371.80355994147),.UNSPECIFIED.);
#3439=B_SPLINE_CURVE_WITH_KNOTS('',3,(#61257,#61258,#61259,#61260,#61261,
#61262,#61263,#61264,#61265,#61266,#61267,#61268,#61269,#61270,#61271,#61272,
#61273,#61274,#61275,#61276,#61277,#61278,#61279,#61280,#61281,#61282,#61283,
#61284,#61285,#61286,#61287,#61288,#61289,#61290,#61291,#61292,#61293,#61294,
#61295,#61296,#61297,#61298,#61299,#61300,#61301,#61302,#61303,#61304,#61305,
#61306,#61307,#61308,#61309,#61310,#61311,#61312,#61313,#61314,#61315,#61316,
#61317,#61318,#61319,#61320,#61321,#61322,#61323,#61324,#61325,#61326,#61327,
#61328,#61329,#61330,#61331,#61332,#61333,#61334,#61335,#61336,#61337,#61338),
 .UNSPECIFIED.,.F.,.F.,(4,3,3,3,3,3,3,3,3,3,3,3,3,3,3,3,3,3,3,3,3,3,3,3,
3,3,3,4),(365.519850897371,365.599387868167,365.678867323637,365.758301507332,
365.840869337698,365.920256194552,365.999637242409,366.079023550997,366.158426192054,
366.237883672978,366.317372379599,366.396930317931,366.418844150263,366.495574729022,
366.572238327818,366.648849629473,366.725424396608,366.80197772642,366.878535124835,
366.917615340926,367.002284331427,367.087098782331,367.172112099402,367.257211513743,
367.342430901122,367.416386531588,367.507707819992,367.566340469871),
 .UNSPECIFIED.);
#3440=B_SPLINE_CURVE_WITH_KNOTS('',3,(#61340,#61341,#61342,#61343,#61344,
#61345,#61346,#61347,#61348,#61349,#61350,#61351,#61352,#61353,#61354,#61355,
#61356,#61357,#61358,#61359,#61360,#61361,#61362,#61363,#61364,#61365,#61366,
#61367,#61368,#61369,#61370,#61371,#61372,#61373,#61374,#61375,#61376,#61377,
#61378,#61379,#61380,#61381,#61382,#61383,#61384,#61385,#61386,#61387,#61388,
#61389,#61390,#61391,#61392,#61393,#61394,#61395,#61396,#61397,#61398,#61399,
#61400,#61401,#61402,#61403,#61404,#61405,#61406,#61407,#61408,#61409,#61410,
#61411,#61412,#61413,#61414,#61415,#61416,#61417,#61418,#61419,#61420,#61421),
 .UNSPECIFIED.,.F.,.F.,(4,3,3,3,3,3,3,3,3,3,3,3,3,3,3,3,3,3,3,3,3,3,3,3,
3,3,3,4),(365.519433547733,365.597850690332,365.676386814573,365.742578218156,
365.818649495797,365.894625272249,365.970522329247,366.046357368065,366.122147028167,
366.199393724581,366.275157222847,366.350928054219,366.426721222057,366.505071066413,
366.580995829929,366.660558214705,366.740120599481,366.817062464566,366.893911625604,
366.970684315063,367.047388774677,367.124055194297,367.200698142882,367.277332172827,
367.353997548231,367.430678376817,367.507426594913,367.566340470006),
 .UNSPECIFIED.);
#3441=B_SPLINE_CURVE_WITH_KNOTS('',3,(#61422,#61423,#61424,#61425,#61426,
#61427,#61428,#61429,#61430,#61431,#61432,#61433,#61434,#61435,#61436,#61437,
#61438,#61439,#61440,#61441,#61442,#61443,#61444,#61445,#61446,#61447,#61448,
#61449,#61450,#61451,#61452,#61453,#61454,#61455,#61456,#61457,#61458,#61459,
#61460,#61461,#61462,#61463,#61464,#61465,#61466,#61467,#61468,#61469,#61470,
#61471,#61472,#61473,#61474,#61475,#61476,#61477,#61478,#61479,#61480,#61481,
#61482,#61483,#61484,#61485,#61486,#61487,#61488,#61489,#61490,#61491,#61492,
#61493,#61494,#61495,#61496,#61497,#61498,#61499,#61500,#61501,#61502,#61503,
#61504,#61505,#61506,#61507,#61508,#61509,#61510,#61511,#61512,#61513,#61514,
#61515,#61516,#61517,#61518,#61519,#61520,#61521,#61522,#61523,#61524,#61525,
#61526,#61527,#61528,#61529,#61530,#61531,#61532,#61533,#61534,#61535,#61536,
#61537,#61538,#61539,#61540,#61541,#61542,#61543,#61544,#61545,#61546,#61547,
#61548,#61549,#61550,#61551,#61552,#61553,#61554,#61555,#61556,#61557,#61558,
#61559,#61560,#61561,#61562,#61563,#61564,#61565,#61566,#61567,#61568,#61569,
#61570,#61571,#61572,#61573,#61574,#61575,#61576,#61577,#61578,#61579,#61580,
#61581,#61582,#61583,#61584,#61585,#61586,#61587),.UNSPECIFIED.,.F.,.F.,
(4,3,3,3,3,3,3,3,3,3,3,3,3,3,3,3,3,3,3,3,3,3,3,3,3,3,3,3,3,3,3,3,3,3,3,
3,3,3,3,3,3,3,3,3,3,3,3,3,3,3,3,3,3,3,3,4),(367.566340470089,367.671959825277,
367.737662980806,367.821875132266,367.905961159974,367.989842081919,368.073593867951,
368.157131515285,368.236434171468,368.313813937834,368.391212098914,368.468642441523,
368.546159735013,368.623726681024,368.70139997251,368.735205362131,368.814830549885,
368.894383004655,368.973875026336,369.053318868243,369.132726746034,369.21211718005,
369.291498730693,369.370882468393,369.45027946362,369.529730080644,369.609209099982,
369.688761239537,369.732747743455,369.809478322214,369.88614192101,369.962753222665,
370.0393279898,370.115881319612,370.192438718027,370.231518934118,370.316187924619,
370.401002375523,370.486015692594,370.571115106935,370.656334494314,370.73029012478,
370.811847105145,370.893328954842,370.977262044992,371.058589285723,371.143825300583,
371.229061315443,371.308472514068,371.387902138771,371.467360949883,371.546892773511,
371.626466300118,371.706123424268,371.727832506105,371.803205170848),
 .UNSPECIFIED.);
#3442=B_SPLINE_CURVE_WITH_KNOTS('',3,(#61593,#61594,#61595,#61596,#61597,
#61598,#61599,#61600,#61601,#61602,#61603,#61604,#61605,#61606,#61607,#61608,
#61609,#61610,#61611,#61612,#61613,#61614,#61615,#61616,#61617,#61618,#61619,
#61620,#61621,#61622,#61623,#61624,#61625,#61626,#61627,#61628,#61629,#61630,
#61631,#61632,#61633,#61634,#61635,#61636,#61637,#61638,#61639,#61640,#61641,
#61642,#61643,#61644,#61645,#61646,#61647,#61648,#61649,#61650,#61651,#61652,
#61653,#61654,#61655,#61656,#61657,#61658,#61659,#61660,#61661,#61662,#61663,
#61664,#61665,#61666,#61667,#61668,#61669,#61670,#61671,#61672,#61673,#61674,
#61675,#61676,#61677,#61678,#61679,#61680,#61681,#61682,#61683,#61684,#61685,
#61686,#61687,#61688,#61689,#61690,#61691,#61692,#61693,#61694,#61695,#61696,
#61697,#61698,#61699,#61700,#61701,#61702,#61703,#61704,#61705,#61706,#61707,
#61708,#61709,#61710,#61711,#61712,#61713,#61714,#61715,#61716,#61717,#61718,
#61719,#61720,#61721,#61722,#61723,#61724,#61725,#61726,#61727,#61728,#61729,
#61730,#61731,#61732,#61733,#61734,#61735,#61736,#61737,#61738,#61739,#61740,
#61741,#61742,#61743,#61744,#61745,#61746,#61747,#61748,#61749),
 .UNSPECIFIED.,.F.,.F.,(4,3,3,3,3,3,3,3,3,3,3,3,3,3,3,3,3,3,3,3,3,3,3,3,
3,3,3,3,3,3,3,3,3,3,3,3,3,3,3,3,3,3,3,3,3,3,3,3,3,3,3,3,4),(373.849525777185,
373.931987983285,374.014449841088,374.096911357443,374.179372539201,374.261833393211,
374.344293926323,374.426754145386,374.509214057249,374.591673668761,374.67413298677,
374.756592018124,374.839050769671,374.921509248258,375.003967460734,375.086425413945,
375.168883114738,375.25134056996,375.333797786457,375.419810481743,375.503135280301,
375.585601885893,375.668067647276,375.750532591866,375.832996747075,375.915460140311,
375.997922798983,376.080384750494,376.162846022246,376.24530664164,376.327766636071,
376.410226032935,376.492684859625,376.575143143532,376.657600912045,376.740058192551,
376.824192307743,376.906658306102,376.989122682709,377.071585547204,377.15404700921,
377.23650717833,377.318966164146,377.401424076226,377.487021571149,377.569486308195,
377.651948080581,377.734407326746,377.816864484985,377.899327004068,377.981784675479,
378.064243466672,378.08620403561),.UNSPECIFIED.);
#3443=B_SPLINE_CURVE_WITH_KNOTS('',3,(#61750,#61751,#61752,#61753,#61754,
#61755,#61756,#61757,#61758,#61759,#61760,#61761,#61762,#61763,#61764,#61765,
#61766,#61767,#61768,#61769,#61770,#61771,#61772,#61773,#61774,#61775,#61776,
#61777,#61778,#61779,#61780,#61781,#61782,#61783,#61784,#61785,#61786,#61787,
#61788,#61789,#61790,#61791,#61792,#61793,#61794,#61795,#61796,#61797,#61798,
#61799,#61800,#61801,#61802,#61803,#61804,#61805,#61806,#61807,#61808,#61809,
#61810,#61811,#61812,#61813,#61814,#61815,#61816,#61817,#61818,#61819,#61820,
#61821,#61822,#61823,#61824,#61825,#61826,#61827,#61828,#61829,#61830,#61831,
#61832,#61833,#61834),.UNSPECIFIED.,.F.,.F.,(4,3,3,3,3,3,3,3,3,3,3,3,3,
3,3,3,3,3,3,3,3,3,3,3,3,3,3,3,4),(371.80355994147,371.887023856295,371.90532724755,
371.982707058008,372.060105263626,372.137535651175,372.215052990023,372.292619981656,
372.370293318913,372.404098438213,372.48372358287,372.563275994317,372.642767972546,
372.722211770968,372.801619605335,372.881009996262,372.960391504087,373.039775199325,
373.119172152529,373.19862272848,373.278101707279,373.357653807471,373.401640819538,
373.479117409525,373.556521439858,373.633857436576,373.711153486426,373.788427537233,
373.849284737275),.UNSPECIFIED.);
#3444=B_SPLINE_CURVE_WITH_KNOTS('',3,(#61836,#61837,#61838,#61839,#61840,
#61841,#61842,#61843,#61844,#61845,#61846,#61847,#61848,#61849,#61850,#61851,
#61852,#61853,#61854,#61855,#61856,#61857,#61858,#61859,#61860,#61861,#61862,
#61863,#61864,#61865,#61866,#61867,#61868,#61869,#61870,#61871,#61872,#61873,
#61874,#61875,#61876,#61877,#61878,#61879,#61880,#61881,#61882,#61883,#61884,
#61885,#61886,#61887,#61888,#61889,#61890,#61891,#61892,#61893,#61894,#61895,
#61896,#61897,#61898,#61899,#61900,#61901,#61902,#61903,#61904,#61905,#61906,
#61907,#61908,#61909,#61910,#61911,#61912,#61913,#61914),.UNSPECIFIED.,
 .F.,.F.,(4,3,3,3,3,3,3,3,3,3,3,3,3,3,3,3,3,3,3,3,3,3,3,3,3,3,4),(371.803205170848,
371.881529712004,371.959801984707,372.038036352297,372.116247149726,372.194465238155,
372.272690756781,372.35093669188,372.429216039255,372.507587794488,372.586008667588,
372.664546969386,372.72537488743,372.801446166943,372.877421945265,372.953319004127,
373.029154044804,373.10494370676,373.18219040201,373.257953902108,373.333724735302,
373.409517904954,373.487867745904,373.563792511196,373.643354889975,373.722917268755,
373.849525777185),.UNSPECIFIED.);
#3445=B_SPLINE_CURVE_WITH_KNOTS('',3,(#61915,#61916,#61917,#61918,#61919,
#61920,#61921,#61922,#61923,#61924,#61925,#61926,#61927,#61928,#61929,#61930,
#61931,#61932,#61933,#61934,#61935,#61936,#61937,#61938,#61939,#61940,#61941,
#61942,#61943,#61944,#61945,#61946,#61947,#61948,#61949,#61950,#61951,#61952,
#61953,#61954,#61955,#61956,#61957,#61958,#61959,#61960,#61961,#61962,#61963,
#61964,#61965,#61966,#61967,#61968,#61969,#61970,#61971,#61972,#61973,#61974,
#61975,#61976,#61977,#61978,#61979,#61980,#61981,#61982,#61983,#61984,#61985,
#61986,#61987,#61988,#61989,#61990,#61991,#61992,#61993,#61994,#61995,#61996,
#61997,#61998,#61999,#62000,#62001,#62002,#62003,#62004,#62005,#62006,#62007,
#62008,#62009,#62010,#62011,#62012,#62013,#62014,#62015,#62016,#62017,#62018,
#62019,#62020,#62021,#62022,#62023,#62024,#62025,#62026,#62027,#62028,#62029,
#62030,#62031,#62032,#62033,#62034,#62035,#62036,#62037,#62038,#62039,#62040,
#62041,#62042,#62043,#62044,#62045,#62046,#62047,#62048,#62049,#62050,#62051,
#62052,#62053,#62054,#62055,#62056,#62057,#62058,#62059,#62060,#62061,#62062,
#62063,#62064,#62065,#62066,#62067,#62068,#62069,#62070,#62071,#62072,#62073,
#62074,#62075,#62076,#62077,#62078,#62079,#62080,#62081,#62082,#62083),
 .UNSPECIFIED.,.F.,.F.,(4,3,3,3,3,3,3,3,3,3,3,3,3,3,3,3,3,3,3,3,3,3,3,3,
3,3,3,3,3,3,3,3,3,3,3,3,3,3,3,3,3,3,3,3,3,3,3,3,3,3,3,3,3,3,3,3,4),(373.849525777274,
373.925592910461,374.001577904088,374.077497497404,374.153368363852,374.229213553232,
374.30504741323,374.380884962493,374.456741221151,374.53266819445,374.608635285085,
374.684698717904,374.72045965008,374.80467177142,374.888757769278,374.972638662245,
375.056390419951,375.139928040355,375.219230840742,375.2966106512,375.374008856819,
375.451439244367,375.528956583214,375.606523574847,375.684196912104,375.718002031405,
375.797627176062,375.877179587509,375.956671565738,376.036115364159,376.115523198525,
376.194913589453,376.274295097278,376.353678792515,376.433075745719,376.512526321669,
376.592005300468,376.67155740066,376.71554441273,376.792275076439,376.868938759282,
376.945550144022,377.022124992601,377.098678402943,377.175235880253,377.214315603392,
377.298984567271,377.383798992803,377.468812286926,377.553911679802,377.63913104854,
377.713086794055,377.794655681762,377.876123286358,377.957527832752,378.038855906015,
378.08664702176),.UNSPECIFIED.);
#3446=B_SPLINE_CURVE_WITH_KNOTS('',3,(#62089,#62090,#62091,#62092,#62093,
#62094,#62095,#62096,#62097,#62098,#62099,#62100,#62101,#62102,#62103,#62104,
#62105,#62106,#62107,#62108,#62109,#62110,#62111,#62112,#62113,#62114,#62115,
#62116,#62117,#62118,#62119,#62120,#62121,#62122,#62123,#62124,#62125,#62126,
#62127,#62128,#62129,#62130,#62131,#62132,#62133,#62134,#62135,#62136,#62137,
#62138,#62139,#62140,#62141,#62142,#62143,#62144,#62145,#62146,#62147,#62148,
#62149,#62150,#62151,#62152,#62153,#62154,#62155,#62156,#62157,#62158,#62159,
#62160,#62161,#62162,#62163,#62164,#62165,#62166,#62167,#62168,#62169,#62170,
#62171,#62172,#62173,#62174,#62175,#62176,#62177,#62178,#62179,#62180,#62181,
#62182,#62183,#62184,#62185,#62186,#62187,#62188,#62189,#62190,#62191,#62192,
#62193,#62194,#62195,#62196,#62197,#62198,#62199,#62200,#62201,#62202,#62203,
#62204,#62205,#62206,#62207,#62208,#62209,#62210,#62211,#62212,#62213,#62214,
#62215,#62216,#62217,#62218,#62219,#62220,#62221,#62222,#62223,#62224,#62225,
#62226,#62227,#62228,#62229,#62230,#62231,#62232,#62233,#62234,#62235,#62236,
#62237,#62238,#62239,#62240,#62241,#62242,#62243,#62244,#62245),
 .UNSPECIFIED.,.F.,.F.,(4,3,3,3,3,3,3,3,3,3,3,3,3,3,3,3,3,3,3,3,3,3,3,3,
3,3,3,3,3,3,3,3,3,3,3,3,3,3,3,3,3,3,3,3,3,3,3,3,3,3,3,3,4),(380.132711084458,
380.215173290558,380.297635148361,380.380096664716,380.462557846474,380.545018700484,
380.627479233596,380.709939452659,380.792399364522,380.874858976034,380.957318294042,
381.039777325396,381.122236076943,381.204694555531,381.287152768006,381.369610721217,
381.45206842201,381.534525877232,381.61698309373,381.702995789013,381.786320587568,
381.86878719316,381.951252954543,382.033717899133,382.116182054341,382.198645447578,
382.28110810625,382.363570057761,382.446031329513,382.528491948906,382.610951943337,
382.693411340202,382.775870166892,382.858328450799,382.940786219312,383.023243499818,
383.107377615004,383.189843613364,383.27230798997,383.354770854466,383.437232316472,
383.519692485591,383.602151471407,383.684609383488,383.7702068784,383.852671615446,
383.935133387833,384.017592633998,384.100049792237,384.182512311319,384.26496998273,
384.347428773923,384.36938934279),.UNSPECIFIED.);
#3447=B_SPLINE_CURVE_WITH_KNOTS('',3,(#62246,#62247,#62248,#62249,#62250,
#62251,#62252,#62253,#62254,#62255,#62256,#62257,#62258,#62259,#62260,#62261,
#62262,#62263,#62264,#62265,#62266,#62267,#62268,#62269,#62270,#62271,#62272,
#62273,#62274,#62275,#62276,#62277,#62278,#62279,#62280,#62281,#62282,#62283,
#62284,#62285,#62286,#62287,#62288,#62289,#62290,#62291,#62292,#62293,#62294,
#62295,#62296,#62297,#62298,#62299,#62300,#62301,#62302,#62303,#62304,#62305,
#62306,#62307,#62308,#62309,#62310,#62311,#62312,#62313,#62314,#62315,#62316,
#62317,#62318,#62319,#62320,#62321),.UNSPECIFIED.,.F.,.F.,(4,3,3,3,3,3,
3,3,3,3,3,3,3,3,3,3,3,3,3,3,3,3,3,3,3,4),(378.08620403561,378.16866563934,
378.251126577192,378.333586876564,378.416046564852,378.49850566945,378.580964217751,
378.663422237143,378.745879755016,378.8325567131,378.915023498642,378.99748861171,
379.079952161957,379.162414259017,379.244875012498,379.327334531994,379.409792927079,
379.492250307313,379.574716692999,379.657179894507,379.739640350357,379.822098498912,
379.904564102665,379.987023981053,380.069488092306,380.132711084365),
 .UNSPECIFIED.);
#3448=B_SPLINE_CURVE_WITH_KNOTS('',3,(#62323,#62324,#62325,#62326,#62327,
#62328,#62329,#62330,#62331,#62332,#62333,#62334,#62335,#62336,#62337,#62338,
#62339,#62340,#62341,#62342,#62343,#62344,#62345,#62346,#62347,#62348,#62349,
#62350,#62351,#62352,#62353,#62354,#62355,#62356,#62357,#62358,#62359,#62360,
#62361,#62362,#62363,#62364,#62365,#62366,#62367,#62368,#62369,#62370,#62371,
#62372,#62373,#62374,#62375,#62376,#62377,#62378,#62379,#62380,#62381,#62382,
#62383,#62384,#62385,#62386,#62387,#62388,#62389,#62390,#62391,#62392,#62393,
#62394,#62395,#62396,#62397,#62398,#62399,#62400,#62401,#62402,#62403,#62404,
#62405,#62406,#62407),.UNSPECIFIED.,.F.,.F.,(4,3,3,3,3,3,3,3,3,3,3,3,3,
3,3,3,3,3,3,3,3,3,3,3,3,3,3,3,4),(378.08664702176,378.167878927395,378.211857984717,
378.291270024972,378.370700502916,378.450160177032,378.529692873023,378.609267277008,
378.688925280535,378.710629175379,378.789016903715,378.867338511619,378.945608399641,
379.023840930815,379.102050440153,379.180267905599,379.258493300237,379.336739611424,
379.415019836334,379.493392600461,379.571814937547,379.650353845682,379.708171556704,
379.790707299786,379.876208245931,379.958270423662,380.040165762441,380.121839947867,
380.132711084365),.UNSPECIFIED.);
#3449=B_SPLINE_CURVE_WITH_KNOTS('',3,(#62408,#62409,#62410,#62411,#62412,
#62413,#62414,#62415,#62416,#62417,#62418,#62419,#62420,#62421,#62422,#62423,
#62424,#62425,#62426,#62427,#62428,#62429,#62430,#62431,#62432,#62433,#62434,
#62435,#62436,#62437,#62438,#62439,#62440,#62441,#62442,#62443,#62444,#62445,
#62446,#62447,#62448,#62449,#62450,#62451,#62452,#62453,#62454,#62455,#62456,
#62457,#62458,#62459,#62460,#62461,#62462,#62463,#62464,#62465,#62466,#62467,
#62468,#62469,#62470,#62471,#62472,#62473,#62474,#62475,#62476,#62477,#62478,
#62479,#62480,#62481,#62482,#62483,#62484,#62485,#62486,#62487,#62488,#62489,
#62490,#62491,#62492,#62493,#62494,#62495,#62496,#62497,#62498,#62499,#62500,
#62501,#62502,#62503,#62504,#62505,#62506,#62507,#62508,#62509,#62510,#62511,
#62512,#62513,#62514,#62515,#62516,#62517,#62518,#62519,#62520,#62521,#62522,
#62523,#62524,#62525,#62526,#62527,#62528,#62529,#62530,#62531,#62532,#62533,
#62534,#62535,#62536,#62537,#62538,#62539,#62540,#62541,#62542,#62543,#62544,
#62545,#62546,#62547,#62548,#62549,#62550,#62551,#62552,#62553,#62554,#62555,
#62556,#62557,#62558,#62559,#62560,#62561,#62562,#62563,#62564),
 .UNSPECIFIED.,.F.,.F.,(4,3,3,3,3,3,3,3,3,3,3,3,3,3,3,3,3,3,3,3,3,3,3,3,
3,3,3,3,3,3,3,3,3,3,3,3,3,3,3,3,3,3,3,3,3,3,3,3,3,3,3,3,4),(380.132711084365,
380.215173290465,380.297635148268,380.380096664623,380.46255784638,380.545018700391,
380.627479233503,380.709939452566,380.792399364429,380.874858975941,380.95731829395,
381.039777325303,381.12223607685,381.204694555438,381.287152767914,381.369610721124,
381.452068421917,381.534525877139,381.616983093637,381.702995788923,381.786320587481,
381.868787193073,381.951252954456,382.033717899046,382.116182054254,382.198645447491,
382.281108106162,382.363570057674,382.446031329426,382.528491948819,382.61095194325,
382.693411340114,382.775870166804,382.858328450711,382.940786219224,383.023243499731,
383.107377614922,383.189843613282,383.272307989888,383.354770854383,383.43723231639,
383.519692485509,383.602151471325,383.684609383405,383.770206878328,383.852671615374,
383.935133387761,384.017592633926,384.100049792164,384.182512311247,384.264969982658,
384.347428773851,384.369389342789),.UNSPECIFIED.);
#3450=B_SPLINE_CURVE_WITH_KNOTS('',3,(#62568,#62569,#62570,#62571,#62572,
#62573,#62574,#62575),.UNSPECIFIED.,.F.,.F.,(4,2,2,4),(-4.09262915008374,
-3.25801350823578,-2.42309659634092,-2.07498647268394),.UNSPECIFIED.);
#3451=B_SPLINE_CURVE_WITH_KNOTS('',3,(#62579,#62580,#62581,#62582,#62583,
#62584,#62585,#62586,#62587,#62588,#62589,#62590,#62591,#62592,#62593,#62594,
#62595,#62596,#62597,#62598,#62599,#62600,#62601,#62602,#62603,#62604,#62605,
#62606,#62607,#62608,#62609,#62610,#62611,#62612,#62613,#62614,#62615,#62616,
#62617,#62618,#62619,#62620,#62621,#62622,#62623,#62624,#62625,#62626,#62627,
#62628,#62629,#62630,#62631,#62632,#62633,#62634,#62635,#62636,#62637,#62638,
#62639,#62640,#62641,#62642,#62643,#62644,#62645,#62646,#62647,#62648,#62649,
#62650,#62651,#62652,#62653,#62654,#62655,#62656,#62657,#62658,#62659,#62660,
#62661,#62662,#62663,#62664,#62665,#62666,#62667,#62668,#62669,#62670,#62671,
#62672,#62673,#62674,#62675,#62676,#62677,#62678,#62679,#62680,#62681,#62682,
#62683,#62684,#62685,#62686,#62687,#62688,#62689,#62690,#62691,#62692,#62693,
#62694,#62695,#62696,#62697,#62698,#62699,#62700,#62701,#62702,#62703,#62704,
#62705,#62706,#62707,#62708,#62709,#62710,#62711,#62712,#62713,#62714,#62715,
#62716,#62717,#62718,#62719,#62720,#62721,#62722,#62723,#62724,#62725,#62726,
#62727,#62728,#62729,#62730,#62731,#62732,#62733,#62734,#62735,#62736,#62737,
#62738,#62739,#62740,#62741,#62742,#62743,#62744,#62745,#62746,#62747,#62748,
#62749,#62750,#62751,#62752,#62753,#62754,#62755,#62756,#62757,#62758,#62759,
#62760,#62761,#62762,#62763,#62764,#62765,#62766,#62767,#62768,#62769,#62770,
#62771,#62772,#62773,#62774,#62775,#62776,#62777,#62778,#62779,#62780,#62781,
#62782,#62783,#62784,#62785,#62786,#62787,#62788,#62789,#62790,#62791,#62792,
#62793,#62794,#62795,#62796,#62797,#62798,#62799,#62800,#62801,#62802,#62803,
#62804,#62805,#62806,#62807,#62808,#62809,#62810,#62811,#62812,#62813,#62814,
#62815,#62816,#62817,#62818,#62819,#62820,#62821,#62822,#62823,#62824,#62825,
#62826,#62827,#62828,#62829,#62830,#62831,#62832,#62833,#62834,#62835,#62836,
#62837,#62838,#62839,#62840,#62841,#62842,#62843,#62844,#62845,#62846,#62847,
#62848,#62849,#62850,#62851,#62852,#62853,#62854,#62855,#62856,#62857,#62858,
#62859,#62860,#62861,#62862,#62863,#62864,#62865,#62866,#62867,#62868,#62869,
#62870,#62871,#62872,#62873,#62874,#62875,#62876,#62877,#62878,#62879,#62880,
#62881,#62882,#62883,#62884,#62885,#62886,#62887,#62888,#62889,#62890,#62891,
#62892,#62893,#62894,#62895,#62896,#62897,#62898,#62899,#62900,#62901,#62902,
#62903,#62904),.UNSPECIFIED.,.F.,.F.,(4,2,2,2,2,2,2,2,2,2,2,2,2,2,2,2,2,
2,2,2,2,2,2,2,2,2,2,2,2,2,2,2,2,2,2,2,2,2,2,2,2,2,2,2,2,2,2,2,2,2,2,2,2,
2,2,2,2,2,2,2,2,2,2,2,2,2,2,2,2,2,2,2,2,2,2,2,2,2,2,2,2,2,2,2,2,2,2,2,2,
2,2,2,2,2,2,2,2,2,2,2,2,2,2,2,2,2,2,2,2,2,2,2,2,2,2,2,2,2,2,2,2,2,2,2,2,
2,2,2,2,2,2,2,2,2,2,2,2,2,2,2,2,2,2,2,2,2,2,2,2,2,2,2,2,2,2,2,2,2,2,2,2,
2,4),(6.78680112922089E-5,0.00847455153472558,0.0205550808575541,0.0663470498539596,
0.113846171319888,0.148670368122606,0.162566725200985,0.176093744247133,
0.189517913141263,0.213396993878021,0.29182571289124,0.347515192132862,
0.375621647217002,0.376496789457627,0.376951840483764,0.377870037035494,
0.384922167581578,0.390912715358734,0.397240236351121,0.407290320413488,
0.462396926330204,0.510017537064033,0.530535865261965,0.543040465556326,
0.546604952112527,0.555812596781168,0.564937586640173,0.576899983176677,
0.595573980052425,0.692061246855429,0.764269280602125,0.772954681898515,
0.777327023684247,0.781408333482716,0.785360366438397,0.790575569363848,
0.804894630243167,0.907175577104357,0.996874648878195,1.05009922531605,
1.08495496264516,1.09695613786015,1.10426927752641,1.112186582686,1.12237897970457,
1.13942126892903,1.22471258407554,1.39856915012792,1.50642685078538,1.5426628802634,
1.54775465536353,1.55036026515212,1.55223446846513,1.55421913556645,1.55701010269284,
1.56442222085663,1.68156464426591,1.81040381737534,1.89782059794948,1.93530202771538,
1.94103643567307,1.94399614716539,1.94615941818338,1.94848220726541,1.95180292613558,
1.96094044356202,2.09645512034237,2.13809561274441,2.26936941226598,2.3256715145711,
2.34666926858975,2.3581252927114,2.36075262736178,2.36224606980681,2.36340087055794,
2.36470610779319,2.36714048051926,2.37546562613443,2.50755217540942,2.64920788246672,
2.72224383874213,2.75461875348397,2.7596640780648,2.76227587996437,2.76418792931182,
2.76624379134744,2.76979623942517,2.77969659684181,2.93425550300827,3.14938562823162,
3.16183313195867,3.16430258693048,3.16588452758889,3.16713921036186,3.1685452320664,
3.17088822391385,3.17949234546324,3.23792128164173,3.3847077591732,3.56961379748167,
3.5815420185984,3.58551685517584,3.58802917498927,3.59032009613806,3.59323422924214,
3.59917516221538,3.64707718078749,3.7273875888966,3.78903279180768,3.96680607018146,
3.98042837848918,3.9845680285147,3.98704628921796,3.9890336004651,3.99171066303711,
3.99675809051981,4.02607262921474,4.09545900454798,4.21940280188449,4.40371403835115,
4.42558154069455,4.43390964137369,4.43990048824899,4.44627492355155,4.45477968368953,
4.47377905635575,4.5511144003357,4.63185019722768,4.69211415017163,4.73720400888895,
4.74367540848441,4.74776175135428,4.75103482008021,4.75474172513869,4.76102742964408,
4.7859044486062,4.83384701287002,4.95040076617469,4.98732100802768,4.99186239933497,
5.04240155525838,5.05696691264538,5.06572878518261,5.07283354907773,5.08257688475351,
5.10192112115817,5.20462221176254,5.34868422153004,5.44352082377912,5.44549523237544,
5.44850610235358,5.44952028440821,5.45187024349439,5.456611140767,5.49702337793335,
5.50194083458181,5.50445131553751,5.50630142880113,5.50830504943557,5.51102849058975,
5.51725072199404,5.62175200668662,5.8680590994294),.UNSPECIFIED.);
#3452=B_SPLINE_CURVE_WITH_KNOTS('',3,(#62906,#62907,#62908,#62909,#62910,
#62911,#62912,#62913,#62914,#62915,#62916,#62917,#62918,#62919,#62920,#62921,
#62922,#62923,#62924,#62925,#62926,#62927,#62928,#62929,#62930,#62931,#62932,
#62933,#62934,#62935,#62936,#62937,#62938,#62939,#62940,#62941,#62942,#62943,
#62944,#62945,#62946,#62947,#62948,#62949,#62950,#62951,#62952,#62953,#62954,
#62955,#62956,#62957,#62958,#62959,#62960,#62961,#62962,#62963,#62964,#62965,
#62966,#62967,#62968,#62969,#62970,#62971,#62972,#62973,#62974,#62975,#62976,
#62977,#62978,#62979,#62980,#62981,#62982,#62983,#62984,#62985,#62986,#62987,
#62988,#62989,#62990,#62991,#62992,#62993,#62994,#62995,#62996,#62997,#62998,
#62999,#63000,#63001,#63002,#63003,#63004,#63005,#63006,#63007,#63008,#63009,
#63010,#63011,#63012,#63013,#63014,#63015,#63016,#63017,#63018,#63019,#63020,
#63021,#63022,#63023,#63024,#63025,#63026,#63027,#63028,#63029,#63030,#63031,
#63032,#63033,#63034,#63035,#63036,#63037,#63038,#63039,#63040,#63041,#63042,
#63043,#63044,#63045,#63046,#63047,#63048,#63049,#63050,#63051,#63052,#63053,
#63054,#63055,#63056,#63057,#63058,#63059,#63060,#63061,#63062,#63063,#63064,
#63065,#63066,#63067,#63068,#63069,#63070,#63071,#63072,#63073,#63074,#63075,
#63076,#63077,#63078,#63079,#63080,#63081,#63082,#63083,#63084,#63085,#63086,
#63087,#63088,#63089,#63090,#63091,#63092,#63093,#63094,#63095,#63096,#63097,
#63098,#63099,#63100,#63101,#63102,#63103,#63104,#63105,#63106,#63107,#63108,
#63109,#63110,#63111,#63112,#63113,#63114,#63115,#63116,#63117,#63118,#63119,
#63120,#63121,#63122,#63123,#63124,#63125,#63126,#63127,#63128,#63129,#63130,
#63131,#63132,#63133,#63134,#63135,#63136,#63137,#63138,#63139,#63140,#63141,
#63142,#63143,#63144,#63145,#63146,#63147,#63148,#63149,#63150,#63151,#63152,
#63153,#63154,#63155,#63156,#63157,#63158,#63159,#63160,#63161,#63162,#63163,
#63164,#63165,#63166,#63167,#63168,#63169,#63170,#63171,#63172,#63173,#63174,
#63175,#63176,#63177,#63178,#63179,#63180,#63181,#63182,#63183,#63184,#63185,
#63186,#63187,#63188,#63189,#63190,#63191,#63192,#63193,#63194,#63195,#63196,
#63197,#63198,#63199,#63200,#63201,#63202,#63203,#63204,#63205,#63206,#63207,
#63208,#63209,#63210,#63211,#63212,#63213,#63214,#63215,#63216,#63217,#63218,
#63219,#63220,#63221,#63222,#63223,#63224,#63225,#63226,#63227,#63228,#63229,
#63230,#63231,#63232,#63233,#63234,#63235,#63236,#63237,#63238,#63239,#63240,
#63241,#63242,#63243,#63244,#63245,#63246,#63247,#63248,#63249,#63250,#63251,
#63252,#63253,#63254,#63255,#63256,#63257,#63258,#63259,#63260,#63261,#63262,
#63263,#63264,#63265,#63266,#63267,#63268,#63269,#63270,#63271,#63272,#63273,
#63274,#63275,#63276,#63277,#63278,#63279,#63280,#63281,#63282,#63283,#63284,
#63285,#63286,#63287,#63288,#63289,#63290,#63291,#63292,#63293,#63294,#63295,
#63296,#63297,#63298,#63299,#63300,#63301,#63302,#63303,#63304,#63305,#63306,
#63307,#63308,#63309,#63310,#63311,#63312,#63313,#63314,#63315,#63316,#63317,
#63318,#63319,#63320,#63321,#63322,#63323,#63324,#63325,#63326,#63327,#63328,
#63329,#63330,#63331,#63332,#63333,#63334,#63335,#63336,#63337,#63338,#63339,
#63340,#63341,#63342,#63343,#63344,#63345,#63346,#63347,#63348,#63349,#63350,
#63351,#63352,#63353,#63354,#63355,#63356,#63357,#63358,#63359,#63360,#63361,
#63362,#63363,#63364,#63365,#63366,#63367,#63368,#63369,#63370,#63371,#63372,
#63373,#63374,#63375,#63376,#63377,#63378,#63379,#63380,#63381,#63382,#63383,
#63384,#63385,#63386,#63387,#63388,#63389,#63390,#63391,#63392,#63393,#63394,
#63395,#63396,#63397,#63398,#63399,#63400,#63401,#63402,#63403,#63404,#63405,
#63406,#63407,#63408,#63409,#63410,#63411,#63412,#63413,#63414,#63415,#63416,
#63417,#63418,#63419,#63420,#63421,#63422,#63423,#63424,#63425,#63426,#63427,
#63428,#63429,#63430,#63431,#63432,#63433,#63434,#63435,#63436,#63437,#63438,
#63439,#63440,#63441,#63442,#63443,#63444,#63445,#63446,#63447,#63448,#63449,
#63450,#63451,#63452,#63453,#63454,#63455,#63456,#63457),.UNSPECIFIED.,
 .F.,.F.,(4,2,2,2,2,2,2,2,2,2,2,2,2,2,2,2,2,2,2,2,2,2,2,2,2,2,2,2,2,2,2,
2,2,2,2,2,2,2,2,2,2,2,2,2,2,2,2,2,2,2,2,2,2,2,2,2,2,2,2,2,2,2,2,2,2,2,2,
2,2,2,2,2,2,2,2,2,2,2,2,2,2,2,2,2,2,2,2,2,2,2,2,2,2,2,2,2,2,2,2,2,2,2,2,
2,2,2,2,2,2,2,2,2,2,2,2,2,2,2,2,2,2,2,2,2,2,2,2,2,2,2,2,2,2,2,2,2,2,2,2,
2,2,2,2,2,2,2,2,2,2,2,2,2,2,2,2,2,2,2,2,2,2,2,2,2,2,2,2,2,2,2,2,2,2,2,2,
2,2,2,2,2,2,2,2,2,2,2,2,2,2,2,2,2,2,2,2,2,2,2,2,2,2,2,2,2,2,2,2,2,2,2,2,
2,2,2,2,2,2,2,2,2,2,2,2,2,2,2,2,2,2,2,2,2,2,2,2,2,2,2,2,2,2,2,2,2,2,2,2,
2,2,2,2,2,2,2,2,2,2,2,2,2,2,2,2,2,2,2,2,2,2,2,2,2,2,2,2,4),(0.00217771040208461,
0.0344816819576811,0.0484248271821416,0.0521712334234981,0.054811747531862,
0.0570944089203552,0.0594373547913961,0.062544548743391,0.0686216800216088,
0.103258803958561,0.116907225233592,0.386084646671751,0.407909550866978,
0.457150234070088,0.465711897345782,0.468514138207261,0.47031576693353,
0.472007196551051,0.474223837438873,0.477960414344228,0.500830479885667,
0.681373441914476,0.815521569378699,0.828147376720993,0.833788339008274,
0.837994401687425,0.841923286043086,0.848159861271726,0.854648156497679,
0.897991386954332,1.12014373129146,1.18237094795391,1.21016646677564,1.21464780424494,
1.21698723143654,1.21889087598737,1.22107727941822,1.22475672803362,1.23777966553735,
1.45437614170428,1.56092714026596,1.5885998748474,1.59935851109546,1.60469175229055,
1.60791278089858,1.61083687916309,1.61306691977316,1.615211148419,1.61818774248469,
1.62586810510941,1.72968406360318,1.8339137751426,1.84266881618924,1.87228075308603,
1.89472725344519,1.93367218232155,2.02940238011174,2.03323906857863,2.03491799477074,
2.03615229030273,2.03729050400955,2.03884038059485,2.0419356778204,2.06849902971469,
2.09264680115989,2.31947060272463,2.42592954404666,2.43354518016428,2.43666977374331,
2.43885351574569,2.44105512787418,2.44418555249449,2.45168029689903,2.56118703754135,
2.66286822169186,2.7073263880798,2.72254801315923,2.73998680039428,2.76106406127572,
2.8203574121549,2.82887850102236,2.83119497554349,2.83260877014012,2.8338857307499,
2.83551679414262,2.83884574870767,2.85904109596741,2.88682229798246,3.13282532712108,
3.23994190673852,3.24745286699174,3.25072070844132,3.25311660317803,3.25532210699968,
3.2583038710766,3.26558894973281,3.34042161917931,3.51656237394093,3.57739905987274,
3.60135200555828,3.63962409658751,3.6482655401533,3.65158437706126,3.65387301841201,
3.65611746533737,3.6588271326222,3.66561534248813,3.75059866651629,3.95019840490346,
4.08041416705069,4.0963917911434,4.1044757663243,4.11097749770821,4.11839621232373,
4.13085808084267,4.1775585690903,4.3292999960238,4.3803234026103,4.40547518838493,
4.41134209931604,4.41494402302441,4.41826245167875,4.42252857327128,4.42956852957163,
4.47233402474545,4.54340354635141,4.66150517648929,4.69189133376844,4.71479055677426,
4.72522133159218,4.73314822784188,4.74070060961517,4.75358406833934,4.79153713909647,
4.79387910800581,4.98073628656215,5.14057599251761,5.1415189278427,5.14807159666922,
5.16580787813688,5.16964324588156,5.17211829667321,5.17409712255343,5.17633220688715,
5.18010075917596,5.1944883575077,5.21801665042047,5.25056117768055,5.3121620721385,
5.50059500578965,5.57708633853893,5.58462729228998,5.58772044694801,5.59001084194445,
5.59250140730812,5.59590274983509,5.60374025755479,5.7197191232384,5.79933296225877,
5.87625286545862,5.99101534263647,5.99808106232236,6.00076779615096,6.00236511186596,
6.00387883070559,6.00599134367051,6.01023205924348,6.04411593020551,6.10228467925028,
6.24117697845001,6.34861725605406,6.36040364983722,6.36582787027085,6.37001281424483,
6.3745223491776,6.38166461220902,6.40344210444489,6.51947951209477,6.68416009053745,
6.68586366266339,6.70321996695705,6.74050031957775,6.74575396926641,6.74822322789528,
6.75014570448274,6.75223165541733,6.75555746921463,6.76638560277799,6.86791543534931,
6.9951640469647,7.12914754410345,7.13791749372051,7.14106620868783,7.14325668214021,
7.14528734221631,7.14805115338836,7.15335657347158,7.18639780753178,7.25898684382238,
7.42581419880193,7.53935989058403,7.56157534066716,7.56488673431875,7.56645000717925,
7.5676696971833,7.56899533666508,7.57114102184462,7.57856619954617,7.62596111303262,
7.70394218199319,7.7930142514309,7.95332457056652,7.96352395954735,7.96716003998187,
7.96925808625169,7.97120548146128,7.97385964332833,7.97896673839258,8.011131479465,
8.08277570423716,8.22116902770788,8.30546898708675,8.32885312813485,8.35788569015602,
8.36110491311141,8.36273585841622,8.36393481624283,8.36522996800554,8.36698279753809,
8.37095055516975,8.37628067679727,8.38947539675022,8.4362531619017,8.54619746064972,
8.76150045551478,8.77600834094723,8.78041803540703,8.78305745712411,8.7851737575176,
8.78802220488971,8.79338458500766,8.82393963711053,8.88098643322891,8.93335079496824,
8.96994528516527,9.06248712128003,9.07383123986138,9.17013383081191,9.17889014990768,
9.18233428559776,9.18441690452885,9.18663748648562,9.1888235379032,9.19170371650266,
9.19629762452744,9.20524962464218,9.22775296138128,9.30050572976896,9.3920157285172,
9.51340847384729,9.51472087286398,9.61175353227208,9.62575939980498,9.6341897590963,
9.64074631120598,9.64788641071334,9.65518949421774,9.66586118411138,9.74608359669902,
9.92246480992931,9.9376052360266,9.94274542543644,9.94585731953322,9.94902614956777,
9.95230193033657,9.95729471947809),.UNSPECIFIED.);
#3453=B_SPLINE_CURVE_WITH_KNOTS('',3,(#63459,#63460,#63461,#63462,#63463,
#63464,#63465,#63466,#63467,#63468,#63469,#63470,#63471,#63472,#63473,#63474,
#63475,#63476,#63477,#63478,#63479,#63480,#63481,#63482,#63483,#63484,#63485,
#63486,#63487,#63488,#63489,#63490,#63491,#63492,#63493,#63494,#63495,#63496,
#63497,#63498,#63499,#63500,#63501,#63502,#63503,#63504,#63505,#63506,#63507,
#63508,#63509,#63510,#63511,#63512,#63513,#63514,#63515,#63516,#63517,#63518,
#63519,#63520,#63521,#63522,#63523,#63524,#63525,#63526,#63527,#63528,#63529,
#63530,#63531,#63532,#63533,#63534,#63535,#63536,#63537,#63538,#63539,#63540,
#63541,#63542,#63543,#63544,#63545,#63546,#63547,#63548,#63549,#63550,#63551,
#63552,#63553,#63554,#63555,#63556,#63557,#63558,#63559,#63560,#63561,#63562,
#63563,#63564,#63565,#63566,#63567,#63568,#63569,#63570,#63571,#63572,#63573,
#63574,#63575,#63576,#63577,#63578,#63579,#63580,#63581,#63582,#63583,#63584,
#63585,#63586,#63587,#63588,#63589,#63590,#63591,#63592,#63593,#63594,#63595,
#63596,#63597,#63598,#63599,#63600,#63601,#63602,#63603,#63604,#63605,#63606,
#63607,#63608,#63609,#63610,#63611,#63612,#63613,#63614,#63615,#63616,#63617,
#63618,#63619,#63620,#63621,#63622,#63623,#63624,#63625,#63626,#63627,#63628,
#63629,#63630,#63631,#63632,#63633,#63634,#63635,#63636,#63637,#63638,#63639,
#63640,#63641,#63642,#63643,#63644,#63645,#63646,#63647,#63648,#63649,#63650,
#63651,#63652,#63653,#63654,#63655,#63656,#63657,#63658,#63659,#63660,#63661,
#63662,#63663,#63664,#63665,#63666,#63667,#63668,#63669,#63670,#63671,#63672,
#63673,#63674,#63675,#63676,#63677,#63678,#63679,#63680,#63681,#63682,#63683,
#63684,#63685,#63686,#63687,#63688,#63689,#63690,#63691,#63692,#63693,#63694,
#63695,#63696,#63697,#63698,#63699,#63700,#63701,#63702,#63703,#63704,#63705,
#63706,#63707,#63708,#63709,#63710,#63711,#63712,#63713,#63714,#63715,#63716,
#63717,#63718,#63719,#63720,#63721,#63722,#63723,#63724,#63725,#63726,#63727,
#63728,#63729,#63730,#63731,#63732,#63733,#63734,#63735,#63736,#63737,#63738,
#63739,#63740,#63741,#63742,#63743,#63744,#63745,#63746,#63747,#63748,#63749,
#63750,#63751,#63752,#63753,#63754,#63755,#63756,#63757,#63758,#63759,#63760,
#63761,#63762,#63763,#63764,#63765,#63766,#63767,#63768,#63769,#63770,#63771,
#63772,#63773,#63774,#63775,#63776,#63777,#63778,#63779,#63780,#63781,#63782,
#63783,#63784,#63785,#63786,#63787,#63788,#63789,#63790,#63791,#63792,#63793,
#63794,#63795,#63796,#63797,#63798,#63799,#63800,#63801,#63802,#63803,#63804,
#63805,#63806,#63807,#63808,#63809,#63810,#63811,#63812,#63813,#63814,#63815,
#63816,#63817,#63818,#63819,#63820,#63821,#63822,#63823,#63824,#63825,#63826,
#63827,#63828,#63829,#63830,#63831,#63832,#63833,#63834,#63835,#63836,#63837,
#63838,#63839,#63840,#63841,#63842,#63843,#63844,#63845,#63846,#63847,#63848,
#63849,#63850,#63851,#63852,#63853,#63854,#63855,#63856,#63857,#63858,#63859,
#63860,#63861,#63862,#63863,#63864,#63865,#63866,#63867,#63868,#63869,#63870,
#63871,#63872,#63873,#63874,#63875,#63876,#63877,#63878,#63879,#63880,#63881,
#63882,#63883,#63884,#63885,#63886,#63887,#63888,#63889,#63890,#63891,#63892,
#63893,#63894,#63895,#63896,#63897,#63898,#63899,#63900,#63901,#63902,#63903,
#63904,#63905,#63906,#63907,#63908,#63909,#63910,#63911,#63912,#63913,#63914,
#63915,#63916,#63917,#63918,#63919,#63920,#63921,#63922,#63923,#63924,#63925,
#63926,#63927,#63928,#63929,#63930,#63931,#63932,#63933,#63934,#63935,#63936,
#63937,#63938,#63939,#63940,#63941,#63942,#63943,#63944,#63945,#63946,#63947,
#63948,#63949,#63950,#63951,#63952,#63953,#63954,#63955,#63956,#63957,#63958,
#63959,#63960,#63961,#63962,#63963,#63964,#63965,#63966,#63967,#63968,#63969,
#63970,#63971,#63972),.UNSPECIFIED.,.F.,.F.,(4,2,2,2,2,2,2,2,2,2,2,2,2,
2,2,2,2,2,2,2,2,2,2,2,2,2,2,2,2,2,2,2,2,2,2,2,2,2,2,2,2,2,2,2,2,2,2,2,2,
2,2,2,2,2,2,2,2,2,2,2,2,2,2,2,2,2,2,2,2,2,2,2,2,2,2,2,2,2,2,2,2,2,2,2,2,
2,2,2,2,2,2,2,2,2,2,2,2,2,2,2,2,2,2,2,2,2,2,2,2,2,2,2,2,2,2,2,2,2,2,2,2,
2,2,2,2,2,2,2,2,2,2,2,2,2,2,2,2,2,2,2,2,2,2,2,2,2,2,2,2,2,2,2,2,2,2,2,2,
2,2,2,2,2,2,2,2,2,2,2,2,2,2,2,2,2,2,2,2,2,2,2,2,2,2,2,2,2,2,2,2,2,2,2,2,
2,2,2,2,2,2,2,2,2,2,2,2,2,2,2,2,2,2,2,2,2,2,2,2,2,2,2,2,2,2,2,2,2,2,2,2,
2,2,2,2,2,2,2,2,2,2,2,2,2,2,2,2,2,2,2,2,2,2,2,2,2,2,2,4),(0.00194477749240243,
0.00764117539682748,0.0205707215302883,0.123608016854099,0.232944908166683,
0.265444928942391,0.281957396127948,0.292272408635366,0.300069430396495,
0.308046128403578,0.315505729710164,0.325853021136944,0.353454688474741,
0.541987999039527,0.621661119734957,0.728341535143952,0.742092648891072,
0.744835619976621,0.746860767290477,0.748894394276984,0.750735103243517,
0.753177757034121,0.759297787650504,0.831007528441508,0.851939223796619,
0.869181819275023,0.922901943195041,1.03420307423587,1.11828356832654,1.15530219407324,
1.16110353069289,1.16411193066949,1.16631666673478,1.16868959273105,1.17209157643427,
1.18151197263578,1.33377915080775,1.41842981375281,1.5149151251787,1.55304456490883,
1.57172928729574,1.57515545893047,1.5768067271746,1.57849656556038,1.58008141127905,
1.58226990092565,1.58785372786726,1.68163760330582,1.82588791502246,1.89349259303035,
1.91717511494179,1.92838639431105,1.93489361230526,1.93943348808351,1.94390715913749,
1.94810767246972,1.95362384260449,1.9629532196991,2.01398853016757,2.02556237432937,
2.06239408044429,2.23802298288018,2.30852645512544,2.3157962683899,2.32121804646986,
2.3236094543644,2.32555893996895,2.32734571792745,2.32974970071864,2.33438685291171,
2.37169937210081,2.40978232197433,2.58896074070278,2.70781146615728,2.71469415054384,
2.71776799644888,2.72005309421383,2.72217893568093,2.72508733456416,2.73236692013362,
2.81542680738107,2.91208084175454,3.0392551871556,3.0946765201984,3.12381660852781,
3.13823497961957,3.14093596085108,3.14239071993551,3.14347994519846,3.14467494224146,
3.14683148707961,3.15355837715516,3.25593450946252,3.41944245987133,3.53393033868513,
3.54072153506419,3.54370342815266,3.54590010771965,3.54792950030269,3.55068415398807,
3.55746836619038,3.62889732834507,3.67399253262379,3.83362278464016,3.93301423190129,
3.93701495718578,3.93876636721242,3.94006125600189,3.94126090451689,3.94289428821171,
3.94694048060471,3.99017503945279,4.02026895794056,4.23234444654913,4.31368247927847,
4.3496085414292,4.35520430257812,4.35810196410263,4.36042627977323,4.36309963079874,
4.36766153565265,4.38349953150361,4.62886446591434,4.68798965132942,4.74371375886848,
4.75464123434014,4.75827980530834,4.7606370859362,4.76286367765137,4.76580225184959,
4.77080695806768,4.80347717727004,4.97939432843297,5.17631734566855,5.19948718183741,
5.20816726018814,5.21437887107058,5.2209609488926,5.22970003460272,5.24906602706153,
5.32733625708333,5.43065239659928,5.50915587406734,5.51706479988117,5.52104503069185,
5.52432825713613,5.52815365880615,5.53491641409147,5.56595248577434,5.676392452838,
5.80764159979335,5.82337816962009,5.83332134401914,5.84118907653832,5.8500535684336,
5.86515964221325,5.93057430909038,6.0170236802654,6.25232781759534,6.27282002157152,
6.2768516955123,6.27938736594753,6.28137295028718,6.28357247016948,6.28718091091564,
6.29989265467418,6.38083926219928,6.45801153462545,6.55759742784279,6.68319870529378,
6.69161029373078,6.69485237062276,6.69718190054875,6.69964879411393,6.70290421453076,
6.70994297239214,6.81553705884479,7.07247088653083,7.10312667819184,7.10746126189772,
7.10959330060459,7.11126669793772,7.11312407005727,7.11617886775548,7.12700464979704,
7.20259581491576,7.34328814727695,7.45663625451868,7.46828675097555,7.47377026069598,
7.47797972088986,7.48243490149179,7.48932438116171,7.50927471122013,7.60945208219588,
7.82878573450636,7.85031757557046,7.85432505269809,7.85680705859884,7.8587262610401,
7.86082750032375,7.86421895002785,7.87562726601466,8.03755863910899,8.23373758958363,
8.24578599762793,8.24977652481494,8.25200514974098,8.25422659455003,8.25695279280755,
8.26214721046688,8.26866910468058,8.28276375668469,8.32721379867204,8.41122430655572,
8.65811673957347,8.67174300598273,8.67429467748854,8.67585647188362,8.67707645528398,
8.6784038752094,8.68055584964091,8.68803449686276,8.73597358231969,8.81373966745279,
8.83739789020678,8.91156040404885,8.96491354203416,9.06665038216933,9.07404689353395,
9.0771606914931,9.07935959767508,9.08137894130742,9.08355814058727,9.08896382863302,
9.12963507267496,9.2330125263038,9.44533464322258,9.46822265725664,9.4715681397533,
9.47320008685845,9.47447791253375,9.47589284141639,9.47821158627288,9.48632909854615,
9.53881870096469,9.82662546545269,9.83952194870502,9.88318763120856,9.88898021637239,
9.89196131341892,9.89416749632007,9.89640363694041,9.89873794263655,9.90180675688963,
9.90667201140883,9.95997803070509),.UNSPECIFIED.);
#3454=B_SPLINE_CURVE_WITH_KNOTS('',3,(#63974,#63975,#63976,#63977,#63978,
#63979,#63980,#63981,#63982,#63983,#63984,#63985,#63986),.UNSPECIFIED.,
 .F.,.F.,(4,1,1,1,1,1,1,1,1,1,4),(32.539575242042,32.9188985837215,33.4176697743839,
33.9164409650463,34.4152121557088,34.9139833463713,35.9115257276962,36.4102969183586,
36.909068109021,37.906610490346,38.822750516815),.UNSPECIFIED.);
#3455=B_SPLINE_CURVE_WITH_KNOTS('',3,(#63988,#63989,#63990,#63991,#63992,
#63993,#63994,#63995,#63996,#63997,#63998,#63999,#64000,#64001,#64002,#64003,
#64004,#64005,#64006,#64007,#64008,#64009,#64010,#64011,#64012,#64013,#64014,
#64015,#64016,#64017,#64018,#64019,#64020,#64021,#64022,#64023,#64024,#64025,
#64026,#64027,#64028,#64029,#64030,#64031,#64032,#64033,#64034,#64035,#64036,
#64037,#64038,#64039,#64040,#64041,#64042,#64043,#64044,#64045,#64046,#64047,
#64048,#64049,#64050,#64051,#64052,#64053,#64054,#64055,#64056,#64057,#64058,
#64059,#64060,#64061,#64062,#64063,#64064,#64065,#64066,#64067,#64068,#64069,
#64070,#64071,#64072,#64073,#64074,#64075,#64076,#64077,#64078,#64079,#64080,
#64081,#64082,#64083,#64084,#64085,#64086,#64087,#64088,#64089,#64090,#64091,
#64092,#64093,#64094,#64095,#64096,#64097,#64098,#64099,#64100,#64101,#64102,
#64103,#64104,#64105,#64106,#64107,#64108,#64109,#64110,#64111,#64112,#64113,
#64114,#64115,#64116,#64117,#64118,#64119,#64120,#64121,#64122,#64123,#64124,
#64125,#64126,#64127,#64128,#64129,#64130,#64131,#64132,#64133,#64134,#64135,
#64136,#64137,#64138,#64139,#64140,#64141,#64142,#64143,#64144,#64145,#64146,
#64147,#64148,#64149,#64150,#64151,#64152,#64153,#64154,#64155,#64156,#64157,
#64158,#64159,#64160,#64161,#64162,#64163,#64164,#64165,#64166,#64167,#64168,
#64169,#64170,#64171,#64172,#64173,#64174,#64175,#64176,#64177,#64178,#64179,
#64180,#64181,#64182,#64183,#64184,#64185,#64186,#64187,#64188,#64189,#64190,
#64191,#64192,#64193,#64194,#64195,#64196,#64197,#64198,#64199,#64200,#64201,
#64202,#64203,#64204,#64205,#64206,#64207,#64208,#64209,#64210,#64211,#64212,
#64213,#64214,#64215,#64216,#64217,#64218,#64219,#64220,#64221,#64222,#64223,
#64224,#64225,#64226,#64227,#64228,#64229,#64230,#64231,#64232,#64233,#64234,
#64235,#64236,#64237,#64238,#64239,#64240,#64241,#64242,#64243,#64244,#64245,
#64246,#64247,#64248,#64249,#64250,#64251,#64252,#64253,#64254,#64255,#64256,
#64257,#64258,#64259,#64260,#64261,#64262,#64263,#64264,#64265,#64266,#64267,
#64268,#64269,#64270,#64271,#64272,#64273,#64274,#64275,#64276,#64277,#64278,
#64279,#64280,#64281,#64282,#64283,#64284,#64285,#64286,#64287,#64288,#64289,
#64290,#64291,#64292,#64293,#64294,#64295,#64296,#64297,#64298,#64299,#64300,
#64301,#64302,#64303,#64304,#64305,#64306,#64307,#64308,#64309,#64310,#64311,
#64312,#64313,#64314,#64315,#64316,#64317,#64318,#64319,#64320,#64321,#64322,
#64323,#64324,#64325,#64326,#64327,#64328,#64329,#64330,#64331,#64332,#64333,
#64334,#64335,#64336,#64337,#64338,#64339,#64340,#64341,#64342,#64343,#64344,
#64345,#64346,#64347,#64348,#64349,#64350,#64351,#64352,#64353,#64354,#64355,
#64356,#64357,#64358,#64359,#64360,#64361,#64362,#64363,#64364,#64365,#64366,
#64367,#64368,#64369,#64370,#64371,#64372,#64373,#64374,#64375,#64376,#64377,
#64378,#64379,#64380,#64381,#64382,#64383,#64384,#64385,#64386,#64387,#64388,
#64389,#64390,#64391,#64392,#64393,#64394,#64395,#64396,#64397,#64398,#64399,
#64400,#64401,#64402,#64403,#64404,#64405,#64406,#64407,#64408,#64409,#64410,
#64411,#64412,#64413,#64414,#64415,#64416,#64417,#64418,#64419,#64420,#64421,
#64422,#64423,#64424,#64425,#64426,#64427,#64428,#64429,#64430,#64431,#64432,
#64433,#64434,#64435,#64436,#64437,#64438,#64439,#64440,#64441,#64442,#64443,
#64444,#64445,#64446,#64447,#64448,#64449,#64450,#64451,#64452,#64453,#64454,
#64455,#64456,#64457,#64458,#64459,#64460,#64461,#64462,#64463,#64464,#64465,
#64466,#64467,#64468,#64469,#64470,#64471,#64472,#64473,#64474,#64475,#64476,
#64477,#64478,#64479,#64480,#64481,#64482,#64483,#64484,#64485,#64486,#64487,
#64488,#64489,#64490,#64491),.UNSPECIFIED.,.F.,.F.,(4,2,2,2,2,2,2,2,2,2,
2,2,2,2,2,2,2,2,2,2,2,2,2,2,2,2,2,2,2,2,2,2,2,2,2,2,2,2,2,2,2,2,2,2,2,2,
2,2,2,2,2,2,2,2,2,2,2,2,2,2,2,2,2,2,2,2,2,2,2,2,2,2,2,2,2,2,2,2,2,2,2,2,
2,2,2,2,2,2,2,2,2,2,2,2,2,2,2,2,2,2,2,2,2,2,2,2,2,2,2,2,2,2,2,2,2,2,2,2,
2,2,2,2,2,2,2,2,2,2,2,2,2,2,2,2,2,2,2,2,2,2,2,2,2,2,2,2,2,2,2,2,2,2,2,2,
2,2,2,2,2,2,2,2,2,2,2,2,2,2,2,2,2,2,2,2,2,2,2,2,2,2,2,2,2,2,2,2,2,2,2,2,
2,2,2,2,2,2,2,2,2,2,2,2,2,2,2,2,2,2,2,2,2,2,2,2,2,2,2,2,2,2,2,2,2,2,2,2,
2,2,2,2,2,2,2,2,2,2,2,2,2,2,2,2,2,2,2,2,2,2,2,2,2,4),(0.00201683040818403,
0.0555090148573186,0.0643938470318102,0.0667453893304715,0.0682885389994091,
0.0695126145659887,0.070759772446445,0.0720105510768564,0.0742187584978422,
0.0806712736091462,0.098794631135621,0.134664308353278,0.142909789112026,
0.394731574652877,0.451284979485798,0.480709374429789,0.486016146248271,
0.488852437752199,0.490967264442421,0.493614556785553,0.498060684350159,
0.512883024717616,0.779875996828031,0.878330599117946,0.886319569557424,
0.889535252192457,0.891581385738048,0.893782943749686,0.896789819988317,
0.903472637202945,0.994963931826603,1.08905422398927,1.2832828642102,1.31159029699064,
1.33187073976458,1.34075733881825,1.34736166025531,1.35352731229434,1.3637100421381,
1.39001257046794,1.61336825420023,1.64291287588334,1.64906101581913,1.65271773699212,
1.65602173627205,1.66010344654139,1.66811529807963,1.71930801783313,1.89347072082819,
1.92715086190482,1.95196284104676,1.96272899140048,1.97070719317361,1.97816100793995,
1.98848872299682,2.01591409124277,2.19555058260022,2.33061170284428,2.38058199148277,
2.40359001430013,2.40795733817389,2.41029062824737,2.41222107510303,2.41444830860626,
2.41821780726698,2.43159755842704,2.6734797861835,2.72781288053626,2.78766541481223,
2.81862361574562,2.82415558972066,2.82710640817316,2.82930412274633,2.83205201612524,
2.83665959634171,2.85195944840177,3.15105901313849,3.22562393469632,3.23633944006411,
3.23937993674284,3.2412339244301,3.24290769940844,3.24504494745871,3.24926351741359,
3.27441559198193,3.39285516533644,3.50415751185819,3.5810710723635,3.5975005465717,
3.6037698390979,3.60809285788579,3.61233824194844,3.61747761277771,3.63032259145596,
3.74535114362532,3.86402332411331,3.94880868234255,3.98055389663936,3.98518596978532,
3.98755732974932,3.98944646226141,3.99160521351217,3.99525501486511,4.00761509360781,
4.25311342240517,4.37142486387778,4.37836576164698,4.38145030812162,4.38373728632486,
4.38586053541421,4.3887586777808,4.39597977223854,4.47636307782149,4.64807404244438,
4.7915587504652,4.80250532020607,4.80498934433441,4.80639685901708,4.80748310361709,
4.80889436904514,4.81137271214354,4.8213790109683,4.97947149127639,5.05456119801861,
5.13258915746767,5.19255647557782,5.20301280056308,5.20668638922413,5.20879201342372,
5.21073767829631,5.21337617800424,5.21840839749931,5.24878815241691,5.31308318889736,
5.54076617068461,5.59683791743833,5.60098733944557,5.60263019297209,5.60383237417449,
5.60512574009732,5.60686692010724,5.61076952903634,5.70397167968519,5.77331660971036,
5.88460702817492,6.00934467255547,6.01767298000313,6.02083150543805,6.02308388823859,
6.02521647779603,6.02818938558461,6.03414708982201,6.08108271519217,6.15569128116155,
6.40333844189808,6.41769384945028,6.42190373724689,6.42438861014184,6.42656043992883,
6.42928373697768,6.4345962824552,6.47124126655081,6.57462033686866,6.74235668165456,
6.76362008225968,6.76839560237107,6.85407790019257,6.86714532992767,6.87539033085158,
6.88190869720229,6.88922692980271,6.90154829280269,6.95108510563445,7.04610699437988,
7.12947400693111,7.17423365011768,7.18142201371457,7.18531675587625,7.18826904971285,
7.19204670399925,7.19859096401319,7.22646619120977,7.28364788273798,7.44978565979028,
7.48239220537823,7.49435655521553,7.50173512027721,7.50976393041603,7.52082899722055,
7.54777232072478,7.76501222432846,7.91875159402629,7.91967829935442,7.93738056034355,
7.9412138328333,7.94368849481866,7.94566763856805,7.94790375404052,7.95167566216491,
7.96609493843499,8.12221678171655,8.20374990127786,8.34685604695653,8.3557030985563,
8.35901544273294,8.36136383030206,8.36377296774502,8.36687930296074,8.37028064746644,
8.3758428028379,8.38690112722841,8.41479250530208,8.51843367022146,8.75591379706171,
8.76884797332762,8.77219593555343,8.77413892185669,8.77563581126679,8.77757684437954,
8.78100716816862,8.7962572939637,9.00252260403534,9.12081850775346,9.12784056816598,
9.13494143749434,9.13966288628808,9.1433806041868,9.14818162921303,9.15663711802306,
9.19024694880289,9.42842525606427,9.47502219108499,9.4869489251703,9.51409036420894,
9.51840586847915,9.5209521972705,9.52288756188118,9.52494180505167,9.52812250013544,
9.53773588083188,9.625606287343,9.87038780447967,9.88320377903118,9.90795121349442,
9.91264828770526,9.91553688666106,9.91773482085342,9.91983692491677,9.92224212492766,
9.92562447892427,9.93716499782376,9.96015150473948),.UNSPECIFIED.);
#3456=B_SPLINE_CURVE_WITH_KNOTS('',3,(#64493,#64494,#64495,#64496,#64497,
#64498,#64499,#64500,#64501,#64502,#64503,#64504,#64505,#64506,#64507,#64508,
#64509,#64510,#64511,#64512,#64513,#64514,#64515,#64516,#64517,#64518,#64519,
#64520,#64521,#64522,#64523,#64524,#64525,#64526,#64527,#64528,#64529,#64530,
#64531,#64532,#64533,#64534,#64535,#64536,#64537,#64538,#64539,#64540,#64541,
#64542,#64543,#64544,#64545,#64546,#64547,#64548,#64549,#64550,#64551,#64552,
#64553,#64554,#64555,#64556,#64557,#64558,#64559,#64560,#64561,#64562,#64563,
#64564,#64565,#64566,#64567,#64568,#64569,#64570,#64571,#64572,#64573,#64574,
#64575,#64576,#64577,#64578,#64579,#64580,#64581,#64582,#64583,#64584,#64585,
#64586,#64587,#64588,#64589,#64590,#64591,#64592,#64593,#64594,#64595,#64596,
#64597,#64598,#64599,#64600,#64601,#64602,#64603,#64604,#64605,#64606,#64607,
#64608,#64609,#64610,#64611,#64612,#64613,#64614,#64615,#64616,#64617,#64618,
#64619,#64620,#64621,#64622,#64623,#64624,#64625,#64626,#64627,#64628,#64629,
#64630,#64631,#64632,#64633,#64634,#64635,#64636,#64637,#64638,#64639,#64640,
#64641,#64642,#64643,#64644,#64645,#64646,#64647,#64648,#64649,#64650,#64651,
#64652,#64653,#64654,#64655,#64656,#64657,#64658,#64659,#64660,#64661,#64662,
#64663,#64664,#64665,#64666,#64667,#64668,#64669,#64670,#64671,#64672,#64673,
#64674,#64675,#64676,#64677,#64678,#64679,#64680,#64681,#64682,#64683,#64684,
#64685,#64686,#64687,#64688,#64689,#64690,#64691,#64692,#64693,#64694,#64695,
#64696,#64697,#64698,#64699,#64700,#64701,#64702,#64703,#64704,#64705,#64706,
#64707,#64708,#64709,#64710,#64711,#64712,#64713,#64714,#64715,#64716,#64717,
#64718,#64719,#64720,#64721,#64722,#64723,#64724,#64725,#64726,#64727,#64728,
#64729,#64730,#64731,#64732,#64733,#64734,#64735,#64736,#64737,#64738,#64739,
#64740,#64741,#64742,#64743,#64744,#64745,#64746,#64747,#64748,#64749,#64750,
#64751,#64752,#64753,#64754,#64755,#64756,#64757,#64758,#64759,#64760,#64761,
#64762,#64763,#64764,#64765,#64766,#64767,#64768,#64769,#64770,#64771,#64772,
#64773,#64774,#64775,#64776,#64777,#64778,#64779,#64780,#64781,#64782,#64783,
#64784,#64785,#64786,#64787,#64788,#64789,#64790,#64791,#64792,#64793,#64794,
#64795,#64796,#64797,#64798,#64799,#64800,#64801,#64802,#64803,#64804,#64805,
#64806,#64807,#64808,#64809,#64810,#64811,#64812,#64813,#64814,#64815,#64816,
#64817,#64818,#64819,#64820,#64821,#64822,#64823,#64824,#64825,#64826,#64827,
#64828,#64829,#64830,#64831,#64832,#64833,#64834,#64835,#64836,#64837,#64838,
#64839,#64840,#64841,#64842,#64843,#64844,#64845,#64846,#64847,#64848,#64849,
#64850,#64851,#64852,#64853,#64854,#64855,#64856,#64857,#64858,#64859,#64860,
#64861,#64862,#64863,#64864,#64865,#64866,#64867,#64868,#64869,#64870,#64871,
#64872,#64873,#64874,#64875,#64876,#64877,#64878,#64879,#64880,#64881,#64882,
#64883,#64884,#64885,#64886,#64887,#64888,#64889,#64890,#64891,#64892,#64893,
#64894,#64895,#64896,#64897,#64898,#64899,#64900,#64901,#64902,#64903,#64904,
#64905,#64906,#64907,#64908,#64909,#64910,#64911,#64912,#64913,#64914,#64915,
#64916,#64917,#64918,#64919,#64920,#64921,#64922,#64923,#64924,#64925,#64926,
#64927,#64928,#64929,#64930,#64931,#64932,#64933,#64934,#64935,#64936,#64937,
#64938,#64939,#64940,#64941,#64942,#64943,#64944,#64945,#64946,#64947,#64948,
#64949,#64950,#64951,#64952,#64953,#64954,#64955,#64956,#64957,#64958,#64959,
#64960,#64961,#64962,#64963,#64964,#64965,#64966,#64967,#64968,#64969,#64970,
#64971,#64972,#64973,#64974,#64975,#64976,#64977,#64978,#64979,#64980,#64981,
#64982,#64983,#64984,#64985,#64986,#64987,#64988,#64989,#64990,#64991,#64992,
#64993,#64994),.UNSPECIFIED.,.F.,.F.,(4,2,2,2,2,2,2,2,2,2,2,2,2,2,2,2,2,
2,2,2,2,2,2,2,2,2,2,2,2,2,2,2,2,2,2,2,2,2,2,2,2,2,2,2,2,2,2,2,2,2,2,2,2,
2,2,2,2,2,2,2,2,2,2,2,2,2,2,2,2,2,2,2,2,2,2,2,2,2,2,2,2,2,2,2,2,2,2,2,2,
2,2,2,2,2,2,2,2,2,2,2,2,2,2,2,2,2,2,2,2,2,2,2,2,2,2,2,2,2,2,2,2,2,2,2,2,
2,2,2,2,2,2,2,2,2,2,2,2,2,2,2,2,2,2,2,2,2,2,2,2,2,2,2,2,2,2,2,2,2,2,2,2,
2,2,2,2,2,2,2,2,2,2,2,2,2,2,2,2,2,2,2,2,2,2,2,2,2,2,2,2,2,2,2,2,2,2,2,2,
2,2,2,2,2,2,2,2,2,2,2,2,2,2,2,2,2,2,2,2,2,2,2,2,2,2,2,2,2,2,2,2,2,2,2,2,
2,2,2,2,2,2,2,2,2,2,2,2,2,2,2,2,2,4),(0.00344090123650659,0.248215503652584,
0.325199316815864,0.361756705116737,0.379269440842161,0.382118691064504,
0.383605137854968,0.38481377710383,0.386200966519763,0.388571418706616,
0.397442785636797,0.53607390243376,0.660481583835621,0.774585618337096,
0.781830897072744,0.784892950856695,0.786922671225327,0.789113196444733,
0.792191701583214,0.799398275956577,0.890933199784602,0.962713797610933,
1.08220084343428,1.12716778187331,1.15950233024339,1.17611275782848,1.17894148503769,
1.18046789724749,1.18172478878023,1.18320777696307,1.18576514284896,1.19543545733353,
1.34968071181659,1.47255901722294,1.58683241729188,1.59244459257325,1.59582663168457,
1.59889364258051,1.60125195872541,1.60349103572916,1.60660048371062,1.6146305586267,
1.73099633663034,1.7921319566467,1.92598091506575,1.94965701599503,1.98765921406415,
1.99626351833744,1.99957722682606,2.00186528267131,2.00411147767362,2.00682608241167,
2.01364170415744,2.11691726059793,2.30772809841377,2.42912201463569,2.44470599321589,
2.45271241401749,2.45858616428045,2.46493753933213,2.47607619853322,2.5092210522027,
2.72540262717015,2.75347288492772,2.75953351936804,2.76317397202912,2.7664829986683,
2.77074510062788,2.77930860342132,2.85421491420867,2.98687678325841,3.05304462653619,
3.0681897549913,3.07707243341869,3.08493915069915,3.09486067908611,3.11064095711837,
3.1829083529179,3.43157172362452,3.48899017795257,3.51422330475956,3.51870572428563,
3.52109772642029,3.52287957618972,3.52510937108676,3.52885207873761,3.54130944968555,
3.73341763923747,3.84311546757308,3.90046394085057,3.92961409240206,3.93505546382703,
3.93798773546222,3.94018463669266,3.94294859765071,3.94762423044451,3.9634999859706,
4.24050283438229,4.34401242363817,4.34895863345328,4.35120928704915,4.35289950277004,
4.35448485343561,4.35667427896422,4.36226176518648,4.45678576035414,4.68005287595498,
4.70620435911724,4.71367229637033,4.71825595926134,4.72242146295673,4.7277887302769,
4.73853822592383,4.79792011029415,4.83680791943469,4.98338675358833,5.08928844506195,
5.09551091009682,5.09798604509323,5.09979140605412,5.10172864236923,5.10432999587132,
5.11013712266719,5.19288222117589,5.47270706664273,5.48735481936215,5.49166634742306,
5.49421411274008,5.49623859067265,5.49893981512383,5.50394930888009,5.53068127345038,
5.58260261832545,5.68831214052396,5.73061181366884,5.77684627313265,5.90580081121727,
5.9142130918677,5.91656519499312,5.91795711937655,5.91916538165629,5.92064723478159,
5.92353564752487,5.94316738170192,5.99072486899088,6.14933720109695,6.30487763657126,
6.31481721883493,6.31841494341739,6.320505527776,6.32245530823129,6.32512706874381,
6.33031736613628,6.36460342060074,6.45686138962944,6.5899170899621,6.70391939155122,
6.71134210036557,6.713641859677,6.71491086325772,6.71618159829422,6.71774575907195,
6.7207482121431,6.73933710428698,6.77918257480237,6.91479411669491,6.96344753718218,
7.11863684766936,7.12849935881802,7.13226850477425,7.13451616237806,7.13688756648348,
7.14000214788525,7.14667897027029,7.23706714479836,7.46432325042959,7.52561510674412,
7.53185821822271,7.53473550631765,7.53695245153251,7.53928607395297,7.54289747741423,
7.5471545839431,7.55520552041704,7.63410275899928,7.74479915888493,7.82389347000999,
7.84037715145234,7.95974472042592,7.97596878187591,7.98421109030493,7.99031195965339,
7.99697035698284,8.00615796422281,8.02810792439933,8.11097558117127,8.25133855539605,
8.28637548125199,8.29306698854525,8.29680127572277,8.29980075351515,8.30364414088957,
8.31048635971695,8.34275191622394,8.45355743324095,8.58318057775002,8.59889928398054,
8.60883841008606,8.61670748886037,8.62557831417302,8.64070727773233,8.70177915035901,
8.80940399575536,8.99715819998764,9.00770724202651,9.01133663400182,9.0139279428649,
9.02200672701579,9.0476622371378,9.05199984223864,9.05459993342341,9.0566008075898,
9.05844308231652,9.06148746617733,9.06955114981409,9.08094266348919,9.1117494300351,
9.16303364180909,9.39543957448968,9.46062652199351,9.46727645935126,9.47053311193938,
9.472866472814,9.47533133717993,9.47857387786533,9.48554531974914,9.58323440962424,
9.81656444638671,9.82633501963593,9.83311518614364,9.83476220081181,9.83767327265969,
9.87819248226354,9.88282569193085,9.88499285628806,9.88667566852092,9.88823944841706,
9.89003249905365,9.89256436907517,9.89687948353486,9.96138941159552),
 .UNSPECIFIED.);
#3457=B_SPLINE_CURVE_WITH_KNOTS('',3,(#64996,#64997,#64998,#64999,#65000,
#65001,#65002,#65003,#65004,#65005,#65006,#65007,#65008,#65009,#65010,#65011,
#65012,#65013,#65014,#65015,#65016,#65017,#65018,#65019,#65020,#65021,#65022,
#65023,#65024,#65025,#65026,#65027,#65028,#65029,#65030,#65031,#65032,#65033,
#65034,#65035,#65036,#65037,#65038,#65039,#65040,#65041,#65042,#65043,#65044,
#65045,#65046,#65047,#65048,#65049,#65050,#65051,#65052,#65053,#65054,#65055,
#65056,#65057,#65058,#65059,#65060,#65061,#65062,#65063,#65064,#65065,#65066,
#65067,#65068,#65069,#65070,#65071,#65072,#65073,#65074,#65075,#65076,#65077,
#65078,#65079,#65080,#65081,#65082,#65083,#65084,#65085,#65086,#65087,#65088,
#65089,#65090,#65091,#65092,#65093,#65094,#65095,#65096,#65097,#65098,#65099,
#65100,#65101,#65102,#65103,#65104,#65105,#65106,#65107,#65108,#65109,#65110,
#65111,#65112,#65113,#65114,#65115,#65116,#65117,#65118,#65119,#65120,#65121,
#65122,#65123,#65124,#65125,#65126,#65127,#65128,#65129,#65130,#65131,#65132,
#65133,#65134,#65135,#65136,#65137,#65138,#65139,#65140,#65141,#65142,#65143,
#65144,#65145,#65146,#65147,#65148,#65149,#65150,#65151,#65152,#65153,#65154,
#65155,#65156,#65157,#65158,#65159,#65160,#65161,#65162,#65163,#65164,#65165,
#65166,#65167,#65168,#65169,#65170,#65171,#65172,#65173,#65174,#65175,#65176,
#65177,#65178,#65179,#65180,#65181,#65182,#65183,#65184,#65185,#65186,#65187,
#65188,#65189,#65190,#65191,#65192,#65193,#65194,#65195,#65196,#65197,#65198,
#65199,#65200,#65201,#65202,#65203,#65204,#65205,#65206,#65207,#65208,#65209,
#65210,#65211,#65212,#65213,#65214,#65215,#65216,#65217,#65218,#65219,#65220,
#65221,#65222,#65223,#65224,#65225,#65226,#65227,#65228,#65229,#65230,#65231,
#65232,#65233,#65234,#65235,#65236,#65237,#65238,#65239,#65240,#65241,#65242,
#65243,#65244,#65245,#65246,#65247,#65248,#65249,#65250,#65251,#65252,#65253,
#65254,#65255,#65256,#65257),.UNSPECIFIED.,.F.,.F.,(4,3,3,3,3,3,3,3,3,3,
3,3,3,3,3,3,3,3,3,3,3,3,3,3,3,3,3,3,3,3,3,3,3,3,3,3,3,3,3,3,3,3,3,3,3,3,
3,3,3,3,3,3,3,3,3,3,3,3,3,3,3,3,3,3,3,3,3,3,3,3,3,3,3,3,3,3,3,3,3,3,3,3,
3,3,3,3,3,4),(63.9555017779399,64.0273228485219,64.0990874604196,64.1708067672796,
64.242499811206,64.3141860900314,64.3414835954556,64.4217776112221,64.5022162304088,
64.5867258693361,64.6675004145408,64.748375898319,64.8293859440099,64.840254786118,
64.9147955906901,64.9892604123256,65.0636631423213,65.1380176309775,65.2123376964115,
65.2905201302905,65.3648279193654,65.4391453967353,65.5134850498522,65.5878593755268,
65.662319405382,65.7368292336065,65.8114395065763,65.8377971674429,65.9109502594573,
65.9840155087585,66.057007839811,66.1299421083477,66.202833116744,66.2756956279024,
66.348558241444,66.4214246268581,66.4943081271963,66.5672220966958,66.6402228321809,
66.7132710318568,66.7864302035233,66.8353395487678,66.9108761820243,66.9863269401705,
67.0617047153914,67.1370223521918,67.2122926554366,67.2898663147686,67.3650860090466,
67.4402998249563,67.5155193091636,67.5907560093478,67.6660485392281,67.7413742748641,
67.8167704926212,67.8328819300927,67.9094806718979,67.9860143617395,68.0624926775479,
68.1389168138957,68.2153082200934,68.2916758052387,68.3316531207551,68.4097742707722,
68.4879403364027,68.5661560514746,68.6444625136851,68.7228171709755,68.8012571059632,
68.8304243114176,68.9123931124947,68.9942901248862,69.0780164691847,69.1596733426811,
69.2444344223806,69.3291955020801,69.4028225266105,69.4764443003387,69.5500738061759,
69.623755474427,69.6974644080224,69.771254988521,69.8279666927425,69.9121598020123,
69.9961817097602,70.080066989409,70.1636682981196,70.2386870851195),
 .UNSPECIFIED.);
#3458=B_SPLINE_CURVE_WITH_KNOTS('',3,(#65259,#65260,#65261,#65262,#65263,
#65264,#65265,#65266,#65267,#65268,#65269,#65270,#65271,#65272,#65273,#65274,
#65275,#65276,#65277,#65278,#65279,#65280,#65281,#65282,#65283,#65284,#65285,
#65286,#65287,#65288,#65289,#65290,#65291,#65292,#65293,#65294,#65295,#65296,
#65297,#65298,#65299,#65300,#65301,#65302,#65303,#65304,#65305,#65306,#65307,
#65308,#65309,#65310,#65311,#65312,#65313,#65314,#65315,#65316,#65317,#65318,
#65319,#65320,#65321,#65322,#65323,#65324,#65325,#65326,#65327,#65328,#65329,
#65330,#65331,#65332,#65333,#65334,#65335,#65336,#65337,#65338,#65339,#65340,
#65341,#65342,#65343,#65344,#65345,#65346,#65347,#65348,#65349,#65350,#65351,
#65352,#65353,#65354,#65355,#65356,#65357,#65358,#65359,#65360,#65361,#65362,
#65363,#65364,#65365,#65366,#65367,#65368,#65369,#65370,#65371,#65372,#65373,
#65374,#65375,#65376,#65377,#65378,#65379,#65380,#65381,#65382,#65383,#65384,
#65385,#65386,#65387,#65388,#65389,#65390,#65391,#65392,#65393,#65394,#65395,
#65396,#65397,#65398,#65399,#65400,#65401,#65402,#65403,#65404,#65405,#65406,
#65407,#65408,#65409,#65410,#65411,#65412,#65413,#65414,#65415,#65416,#65417,
#65418,#65419,#65420,#65421,#65422,#65423,#65424,#65425,#65426,#65427,#65428,
#65429,#65430,#65431,#65432,#65433,#65434,#65435,#65436,#65437,#65438,#65439,
#65440,#65441,#65442,#65443,#65444,#65445,#65446,#65447,#65448,#65449,#65450,
#65451,#65452,#65453,#65454,#65455,#65456,#65457,#65458,#65459,#65460,#65461,
#65462,#65463,#65464,#65465,#65466,#65467,#65468,#65469,#65470,#65471,#65472,
#65473,#65474,#65475,#65476,#65477,#65478,#65479,#65480,#65481,#65482,#65483,
#65484,#65485,#65486,#65487,#65488,#65489,#65490,#65491,#65492,#65493,#65494,
#65495,#65496,#65497,#65498,#65499,#65500,#65501,#65502,#65503,#65504,#65505,
#65506,#65507,#65508,#65509,#65510,#65511,#65512,#65513,#65514,#65515,#65516,
#65517,#65518,#65519,#65520,#65521,#65522,#65523,#65524,#65525,#65526,#65527,
#65528,#65529,#65530,#65531,#65532,#65533,#65534,#65535,#65536,#65537,#65538,
#65539,#65540,#65541,#65542,#65543,#65544,#65545,#65546,#65547,#65548,#65549,
#65550,#65551,#65552,#65553,#65554,#65555,#65556,#65557,#65558,#65559,#65560,
#65561,#65562,#65563,#65564,#65565,#65566,#65567,#65568,#65569,#65570,#65571,
#65572,#65573,#65574,#65575,#65576,#65577,#65578,#65579,#65580,#65581,#65582,
#65583,#65584,#65585,#65586,#65587,#65588,#65589,#65590,#65591,#65592,#65593,
#65594,#65595,#65596,#65597,#65598,#65599,#65600,#65601,#65602,#65603,#65604,
#65605,#65606,#65607,#65608,#65609,#65610,#65611,#65612,#65613,#65614,#65615,
#65616,#65617,#65618,#65619,#65620,#65621,#65622,#65623,#65624,#65625,#65626,
#65627,#65628,#65629,#65630,#65631,#65632,#65633,#65634,#65635,#65636,#65637,
#65638,#65639,#65640,#65641,#65642,#65643,#65644,#65645,#65646,#65647,#65648,
#65649,#65650,#65651,#65652,#65653,#65654,#65655,#65656,#65657,#65658,#65659,
#65660,#65661,#65662,#65663,#65664,#65665,#65666,#65667,#65668,#65669,#65670,
#65671,#65672,#65673,#65674,#65675,#65676,#65677,#65678,#65679,#65680,#65681,
#65682,#65683,#65684,#65685,#65686,#65687,#65688,#65689,#65690,#65691,#65692,
#65693,#65694,#65695,#65696,#65697,#65698,#65699,#65700,#65701,#65702,#65703,
#65704,#65705,#65706,#65707,#65708,#65709,#65710,#65711,#65712,#65713,#65714,
#65715,#65716,#65717,#65718,#65719,#65720,#65721,#65722,#65723,#65724,#65725,
#65726,#65727,#65728,#65729,#65730,#65731,#65732,#65733,#65734,#65735,#65736,
#65737,#65738,#65739,#65740,#65741,#65742,#65743,#65744,#65745,#65746,#65747,
#65748,#65749,#65750,#65751,#65752,#65753,#65754,#65755,#65756,#65757,#65758,
#65759,#65760,#65761,#65762,#65763,#65764,#65765,#65766,#65767,#65768,#65769,
#65770,#65771,#65772,#65773,#65774,#65775,#65776,#65777,#65778,#65779,#65780),
 .UNSPECIFIED.,.F.,.F.,(4,2,2,2,2,2,2,2,2,2,2,2,2,2,2,2,2,2,2,2,2,2,2,2,
2,2,2,2,2,2,2,2,2,2,2,2,2,2,2,2,2,2,2,2,2,2,2,2,2,2,2,2,2,2,2,2,2,2,2,2,
2,2,2,2,2,2,2,2,2,2,2,2,2,2,2,2,2,2,2,2,2,2,2,2,2,2,2,2,2,2,2,2,2,2,2,2,
2,2,2,2,2,2,2,2,2,2,2,2,2,2,2,2,2,2,2,2,2,2,2,2,2,2,2,2,2,2,2,2,2,2,2,2,
2,2,2,2,2,2,2,2,2,2,2,2,2,2,2,2,2,2,2,2,2,2,2,2,2,2,2,2,2,2,2,2,2,2,2,2,
2,2,2,2,2,2,2,2,2,2,2,2,2,2,2,2,2,2,2,2,2,2,2,2,2,2,2,2,2,2,2,2,2,2,2,2,
2,2,2,2,2,2,2,2,2,2,2,2,2,2,2,2,2,2,2,2,2,2,2,2,2,2,2,2,2,2,2,2,2,2,2,2,
2,2,2,2,2,2,2,2,2,2,2,2,2,2,2,2,2,2,2,2,4),(0.00129694875898375,0.0515987783487616,
0.0579315983892281,0.0616524198632641,0.0642824509151131,0.0665642669079207,
0.06902096133795,0.0721554590749639,0.0787458653004138,0.122088816665559,
0.135624312393474,0.419309483428982,0.467087289833786,0.475499538648496,
0.47828207959715,0.480078715752738,0.48177095281888,0.483996630800586,0.488757152293363,
0.527324243030715,0.543455291756894,0.580091470747238,0.797912365366847,
0.832480790485467,0.84068344018513,0.845429713381083,0.849567859465754,
0.854522299330115,0.86063168974179,0.866818642413719,0.933367426055363,
1.10932387546117,1.18879389011366,1.2196159892368,1.22421561324367,1.22658034225675,
1.22846901887263,1.23063256464335,1.23430335327822,1.24684569812093,1.46976274739697,
1.5717945851285,1.59870120534138,1.60923697814188,1.61448838982076,1.61767515413441,
1.62057395423146,1.62279988449253,1.62495139618924,1.62795625907131,1.63581026363364,
1.75069202825208,1.84920466485693,1.87552331137487,1.88857500144065,1.91733393988185,
1.9655198522596,2.03240806601917,2.0415369838651,2.04387578268745,2.04525107884274,
2.04646094724078,2.04796604364869,2.05031572992552,2.06148132802729,2.24613624434292,
2.35466482236293,2.42901694218986,2.44162291014305,2.44542580400804,2.44737146881613,
2.44931055266987,2.45175387043991,2.45592747540602,2.47110364085791,2.71894787937801,
2.73413579870909,2.83618901756261,2.84020343702775,2.84195749611482,2.84325310596444,
2.84445254354133,2.84608429095225,2.84928829498566,2.87448314663903,2.93800781358238,
3.15507418905987,3.2511431764564,3.25787932320395,3.2610052890772,3.26337845468242,
3.26562273089915,3.26937390680572,3.27912503611581,3.42928768362734,3.48981763431179,
3.6463159186215,3.65765448635228,3.6613445657696,3.66371318086919,3.66593478039991,
3.6688440210216,3.67374804535977,3.70423679147491,3.86285245162621,4.08476887733537,
4.10468221723066,4.11350560432419,4.12010048011816,4.12628442744884,4.13485785792976,
4.15720585646341,4.30194658241091,4.41163765282002,4.42005267520845,4.42411855427103,
4.42709432328931,4.43029573416651,4.43489238534155,4.44774729924116,4.5733072328144,
4.66618010028589,4.69968711428439,4.72440064207762,4.73515063352563,4.74312685038242,
4.75058599550718,4.7609326441586,4.7885324870106,4.97721827607555,4.98067963655022,
5.1107245669645,5.17340772595675,5.17944812526741,5.18187943361519,5.1839011156992,
5.18597030530872,5.18898462424538,5.19690768784088,5.29996220794026,5.50840655023033,
5.58758229262072,5.59518866361993,5.59829357893385,5.60058716850642,5.60307587179233,
5.60646513034973,5.61423305217746,5.72284503146046,5.80458174649608,5.88149149179126,
5.91713517503595,6.0040878790867,6.00940097908021,6.01154258487026,6.01311486597951,
6.01481151911871,6.0171046920646,6.02228594373892,6.02928164544955,6.1016138812219,
6.24693603180575,6.35915855771817,6.37103000659625,6.37647034996805,6.38065811436151,
6.38516120859008,6.39227313203665,6.41382349175461,6.52782787471184,6.71825792041728,
6.75153948075885,6.75662970314421,6.75909376201621,6.7610100634925,6.76311919601022,
6.76654804963408,6.77831199810844,6.84891065978739,6.9837203477293,7.13845156329159,
7.14836426696517,7.15204709638925,7.15421376584802,7.15625173751565,7.15907136173104,
7.16464473052532,7.20505716797788,7.30445053985152,7.44232976452885,7.5296394986223,
7.57141511572248,7.57528590094398,7.57684344509663,7.57798557582895,7.57921663354673,
7.58088596097316,7.58477232875091,7.68037287778771,7.78937065932108,7.96235823536435,
7.97398041910527,7.97781532979575,7.97995324809147,7.98208768105778,7.98475244937398,
7.98991016706385,8.02335231528796,8.09963760622958,8.23268406182601,8.32823386277435,
8.33811375127778,8.36867050466958,8.37229806711554,8.3739645843572,8.3752503821478,
8.37663344774641,8.37881229585316,8.38567793656397,8.41013789679968,8.46132840621596,
8.5581824132107,8.77244015912746,8.78687343317552,8.79127425252589,8.79391170375441,
8.79602832318765,8.79887966576661,8.80425555941238,8.83509323790803,8.88933565530832,
8.94281250228456,8.95935889398822,9.07181835074182,9.17801279561369,9.18904020936745,
9.19282977290266,9.19498040273328,9.19695547304308,9.19961648847194,9.20245806619031,
9.2133467861147,9.25837098703045,9.3739494212201,9.42683033353842,9.61130835573613,
9.6340927971425,9.64272057285285,9.64891788810083,9.65550601687633,9.66194249681023,
9.6704050576395,9.68385587133202,9.82027766387798,9.87187651067165,9.90044361465627,
9.94465420549725,9.95177921239289,9.9555352402523,9.95748298040422,9.95770791712911),
 .UNSPECIFIED.);
#3459=B_SPLINE_CURVE_WITH_KNOTS('',3,(#65782,#65783,#65784,#65785,#65786,
#65787,#65788,#65789,#65790,#65791,#65792,#65793,#65794,#65795,#65796,#65797,
#65798,#65799,#65800,#65801,#65802,#65803,#65804,#65805,#65806,#65807,#65808,
#65809,#65810,#65811,#65812,#65813,#65814,#65815,#65816,#65817,#65818,#65819,
#65820,#65821,#65822,#65823,#65824,#65825,#65826,#65827,#65828,#65829,#65830,
#65831,#65832,#65833,#65834,#65835,#65836,#65837,#65838,#65839,#65840,#65841,
#65842,#65843,#65844,#65845,#65846,#65847,#65848,#65849,#65850,#65851,#65852,
#65853,#65854,#65855,#65856,#65857,#65858,#65859,#65860,#65861,#65862,#65863,
#65864,#65865,#65866,#65867,#65868,#65869,#65870,#65871,#65872,#65873,#65874,
#65875,#65876,#65877,#65878,#65879,#65880,#65881,#65882,#65883,#65884,#65885,
#65886,#65887,#65888,#65889,#65890,#65891,#65892,#65893,#65894,#65895,#65896,
#65897,#65898,#65899,#65900,#65901,#65902,#65903,#65904,#65905,#65906,#65907,
#65908,#65909,#65910,#65911,#65912,#65913,#65914,#65915,#65916,#65917,#65918,
#65919,#65920,#65921,#65922,#65923,#65924,#65925,#65926,#65927,#65928,#65929,
#65930,#65931,#65932,#65933,#65934,#65935,#65936,#65937,#65938,#65939,#65940,
#65941,#65942,#65943,#65944,#65945,#65946,#65947,#65948,#65949,#65950,#65951,
#65952,#65953,#65954,#65955,#65956,#65957,#65958,#65959,#65960,#65961,#65962,
#65963,#65964,#65965,#65966,#65967,#65968,#65969,#65970,#65971,#65972,#65973,
#65974,#65975,#65976,#65977,#65978,#65979,#65980,#65981,#65982,#65983,#65984,
#65985,#65986,#65987,#65988,#65989,#65990,#65991,#65992,#65993,#65994,#65995,
#65996,#65997,#65998,#65999,#66000,#66001,#66002,#66003,#66004,#66005,#66006,
#66007,#66008,#66009,#66010,#66011,#66012,#66013,#66014,#66015,#66016,#66017,
#66018,#66019,#66020,#66021,#66022,#66023,#66024,#66025,#66026,#66027,#66028,
#66029,#66030,#66031,#66032,#66033,#66034,#66035,#66036,#66037,#66038,#66039,
#66040,#66041,#66042,#66043,#66044,#66045,#66046,#66047,#66048,#66049,#66050,
#66051,#66052,#66053,#66054,#66055,#66056,#66057,#66058,#66059,#66060,#66061,
#66062,#66063,#66064,#66065,#66066,#66067,#66068,#66069,#66070,#66071,#66072,
#66073,#66074,#66075,#66076,#66077,#66078,#66079,#66080,#66081,#66082,#66083,
#66084,#66085,#66086,#66087,#66088,#66089,#66090,#66091,#66092,#66093,#66094,
#66095,#66096,#66097,#66098,#66099,#66100,#66101,#66102,#66103,#66104,#66105,
#66106,#66107,#66108,#66109,#66110,#66111,#66112,#66113,#66114,#66115,#66116,
#66117,#66118,#66119,#66120,#66121,#66122,#66123,#66124,#66125,#66126,#66127,
#66128,#66129,#66130,#66131,#66132,#66133,#66134,#66135,#66136,#66137,#66138,
#66139,#66140,#66141,#66142,#66143,#66144,#66145,#66146,#66147,#66148,#66149,
#66150,#66151,#66152,#66153,#66154,#66155,#66156,#66157,#66158,#66159,#66160,
#66161,#66162,#66163,#66164,#66165,#66166,#66167,#66168,#66169,#66170,#66171,
#66172,#66173,#66174,#66175,#66176,#66177,#66178,#66179,#66180,#66181,#66182,
#66183,#66184,#66185,#66186,#66187,#66188,#66189,#66190,#66191,#66192,#66193,
#66194,#66195,#66196,#66197,#66198,#66199,#66200,#66201,#66202,#66203,#66204,
#66205,#66206,#66207,#66208,#66209,#66210,#66211,#66212,#66213,#66214,#66215,
#66216,#66217,#66218,#66219,#66220,#66221,#66222,#66223,#66224,#66225,#66226,
#66227,#66228,#66229,#66230,#66231,#66232,#66233,#66234,#66235,#66236,#66237,
#66238,#66239,#66240,#66241,#66242,#66243,#66244,#66245,#66246,#66247,#66248,
#66249,#66250,#66251,#66252,#66253,#66254,#66255,#66256,#66257,#66258,#66259,
#66260,#66261,#66262,#66263,#66264,#66265,#66266,#66267,#66268,#66269,#66270,
#66271,#66272,#66273,#66274,#66275,#66276,#66277,#66278,#66279,#66280,#66281,
#66282,#66283,#66284,#66285,#66286,#66287,#66288,#66289,#66290,#66291,#66292,
#66293,#66294,#66295,#66296,#66297,#66298,#66299,#66300,#66301,#66302,#66303,
#66304,#66305,#66306,#66307,#66308,#66309,#66310,#66311,#66312,#66313,#66314,
#66315,#66316,#66317,#66318,#66319,#66320,#66321),.UNSPECIFIED.,.F.,.F.,
(4,2,2,2,2,2,2,2,2,2,2,2,2,2,2,2,2,2,2,2,2,2,2,2,2,2,2,2,2,2,2,2,2,2,2,
2,2,2,2,2,2,2,2,2,2,2,2,2,2,2,2,2,2,2,2,2,2,2,2,2,2,2,2,2,2,2,2,2,2,2,2,
2,2,2,2,2,2,2,2,2,2,2,2,2,2,2,2,2,2,2,2,2,2,2,2,2,2,2,2,2,2,2,2,2,2,2,2,
2,2,2,2,2,2,2,2,2,2,2,2,2,2,2,2,2,2,2,2,2,2,2,2,2,2,2,2,2,2,2,2,2,2,2,2,
2,2,2,2,2,2,2,2,2,2,2,2,2,2,2,2,2,2,2,2,2,2,2,2,2,2,2,2,2,2,2,2,2,2,2,2,
2,2,2,2,2,2,2,2,2,2,2,2,2,2,2,2,2,2,2,2,2,2,2,2,2,2,2,2,2,2,2,2,2,2,2,2,
2,2,2,2,2,2,2,2,2,2,2,2,2,2,2,2,2,2,2,2,2,2,2,2,2,2,2,2,2,2,2,2,2,2,2,2,
2,2,2,2,2,2,2,2,2,2,2,2,2,2,2,2,2,2,4),(0.00194775596412896,0.00381997872219618,
0.00768310839873159,0.0152484757587718,0.0559984597130718,0.083180397964233,
0.141603609062754,0.281568043709847,0.29577685967244,0.305133092997627,
0.312618786027551,0.320391004818619,0.329437010716093,0.344977543044769,
0.407171949186138,0.529569080338524,0.579467614844668,0.695020815505125,
0.740230438163307,0.752480834329959,0.755225656791899,0.757756982232155,
0.759556661349348,0.761443168043385,0.764587308141118,0.772705215194654,
0.885796374400152,0.969917370966717,1.00161701331527,1.04416239589059,1.12860012040994,
1.16571568962566,1.17152115347068,1.17453053933954,1.17673552024678,1.17910825215584,
1.18250918222216,1.19192178345028,1.34399640189478,1.42848146596589,1.52430228347539,
1.56299389590896,1.58214427882464,1.58558882104827,1.58724228565145,1.58893334181055,
1.59051637566891,1.5926977117734,1.59823863487681,1.6836106975509,1.81377528024418,
1.92300136312492,1.94319569010465,1.94972146505349,1.9542342937265,1.95842016276534,
1.96384391559773,1.97553274987955,2.05117404459852,2.22194126280525,2.29747577116899,
2.32769181091046,2.33218901226991,2.33411863593633,2.33606691666687,2.33785543178008,
2.34026602623827,2.34492827465109,2.38304561380264,2.41974028034598,2.59942787629786,
2.71757480409718,2.72498126293383,2.72814885545142,2.73045053862573,2.7325548441317,
2.73537802188319,2.74231579157247,2.80921358088104,2.91722042949577,3.03771079095769,
3.12007098529017,3.14801992030683,3.15119504291634,3.15274836805141,3.15385036369931,
3.15500301689251,3.15661151412765,3.16086680968392,3.22656406429102,3.35973468255457,
3.46249309797955,3.5454151264851,3.55155702939721,3.55441879343791,3.55659616339199,
3.55865874627818,3.56153955503214,3.56906973653488,3.68111098019845,3.83987741549927,
3.89185180635349,3.93909737868554,3.94654593663412,3.94875820402481,3.95014880256214,
3.95143219807736,3.95308261314174,3.95579493363375,3.97061709213312,3.99147548980586,
4.01311132036521,4.0314363943299,4.24606181980214,4.3147854850443,4.35973119812096,
4.36563284404626,4.36859396060057,4.37072452768334,4.37298070659806,4.37615437337573,
4.38271482110138,4.45180781814634,4.67161188739609,4.70366351306464,4.73293746859321,
4.76254526789673,4.76758936827972,4.77025653768783,4.77244480974129,4.7746503277811,
4.77870263311201,4.79178798398156,4.97941733784476,5.08440355178165,5.09870751297555,
5.10738059298268,5.1995394552947,5.21311272659763,5.22150838411226,5.22804364873175,
5.23527609689005,5.24720687966689,5.29198020096143,5.51096158864603,5.52507467095399,
5.530118782356,5.53321490079805,5.53657043262342,5.54113540912274,5.55162621470125,
5.5661978061242,5.60567934643691,5.73534619065898,5.77322221779091,5.82372000327675,
5.83827123717776,5.84702497697012,5.85412325364556,5.86385721463642,5.88317767562645,
5.98996236103159,6.13860502199146,6.22773382494581,6.26026109465342,6.26864373907125,
6.2733967734793,6.28495033187981,6.28857731880631,6.29056134964699,6.29253617205298,
6.29495207591698,6.29954719009276,6.3278445684736,6.36447658544003,6.45893918096176,
6.63025565699961,6.69555549605877,6.70220815601105,6.70546537293365,6.70779878414219,
6.71026337773395,6.71350502023791,6.72047244318536,6.81776823400833,7.04738324766324,
7.11233152381124,7.11694702084774,7.11919145614331,7.12079103842894,7.12230438649885,
7.12441235554195,7.12862919563622,7.16160320049922,7.218982078648,7.36493159850798,
7.46729602080416,7.47875177350771,7.48419284906929,7.48839436964865,7.49286504517853,
7.49982755574733,7.52029443859662,7.62485329577888,7.83262165904118,7.85997588552478,
7.86430148654411,7.8668506429846,7.86878635605074,7.87083924446749,7.87401434139503,
7.88358492332504,7.93326603624882,7.97165775914461,7.99957161640136,8.023535714671,
8.24217625139083,8.25331107998278,8.25820415262086,8.26115111904945,8.26342417841739,
8.2658198612451,8.26954627521727,8.27389293719544,8.28202080286569,8.30095743108379,
8.35247464759818,8.44872518972948,8.66898692388438,8.68169923691979,8.68419037221864,
8.68575037442937,8.68696628511317,8.68830698146203,8.69052277982283,8.69864324276123,
8.75366487971037,8.82837158704511,8.85176347544509,8.9335817840705,8.98575243765326,
9.07662665733073,9.08383235532049,9.08691089921585,9.0891018395348,9.09129764140298,
9.0944770329609,9.10242444577524,9.22764342296318,9.33205812888859,9.47041845508612,
9.47914048175318,9.48158031118098,9.48302198049232,9.48428241132744,9.48586262699845,
9.48894135533289,9.50945390329011,9.5585081271307,9.84612709053324,9.85915041061506,
9.89314019931766,9.89902757463239,9.90202626448096,9.90428597411546,9.90648287202888,
9.90902129607769,9.91262006122599,9.92614792889703,9.95856693167306),
 .UNSPECIFIED.);
#3460=B_SPLINE_CURVE_WITH_KNOTS('',3,(#66323,#66324,#66325,#66326,#66327,
#66328,#66329,#66330,#66331,#66332,#66333,#66334,#66335,#66336,#66337,#66338,
#66339,#66340,#66341,#66342,#66343,#66344,#66345,#66346,#66347,#66348,#66349,
#66350,#66351,#66352,#66353,#66354,#66355,#66356,#66357,#66358,#66359,#66360,
#66361,#66362,#66363,#66364,#66365,#66366,#66367,#66368,#66369,#66370,#66371,
#66372,#66373,#66374,#66375,#66376,#66377,#66378,#66379,#66380,#66381,#66382,
#66383,#66384,#66385,#66386,#66387,#66388,#66389,#66390,#66391,#66392,#66393,
#66394,#66395,#66396,#66397,#66398,#66399,#66400,#66401,#66402,#66403,#66404,
#66405,#66406,#66407,#66408,#66409,#66410,#66411,#66412,#66413,#66414,#66415,
#66416,#66417,#66418,#66419,#66420,#66421,#66422,#66423,#66424,#66425,#66426,
#66427,#66428,#66429,#66430,#66431,#66432,#66433,#66434,#66435,#66436,#66437,
#66438,#66439,#66440,#66441,#66442,#66443,#66444,#66445,#66446,#66447,#66448,
#66449,#66450,#66451,#66452,#66453,#66454,#66455,#66456,#66457,#66458,#66459,
#66460,#66461,#66462,#66463,#66464,#66465,#66466,#66467,#66468,#66469,#66470,
#66471,#66472,#66473,#66474,#66475,#66476,#66477,#66478,#66479,#66480,#66481,
#66482,#66483,#66484,#66485,#66486,#66487,#66488,#66489,#66490,#66491,#66492,
#66493,#66494,#66495,#66496,#66497,#66498,#66499,#66500,#66501,#66502,#66503,
#66504,#66505,#66506,#66507,#66508,#66509,#66510,#66511,#66512,#66513,#66514,
#66515,#66516,#66517,#66518,#66519,#66520,#66521,#66522,#66523,#66524,#66525,
#66526,#66527,#66528,#66529,#66530,#66531,#66532,#66533,#66534,#66535,#66536,
#66537,#66538,#66539,#66540,#66541,#66542,#66543,#66544,#66545,#66546,#66547,
#66548,#66549,#66550,#66551,#66552,#66553,#66554,#66555,#66556,#66557,#66558,
#66559,#66560,#66561,#66562,#66563,#66564,#66565,#66566,#66567,#66568,#66569,
#66570,#66571,#66572,#66573,#66574,#66575,#66576,#66577,#66578,#66579,#66580,
#66581,#66582,#66583,#66584,#66585,#66586,#66587,#66588,#66589,#66590,#66591,
#66592,#66593,#66594,#66595,#66596,#66597,#66598,#66599,#66600,#66601,#66602,
#66603,#66604,#66605,#66606,#66607,#66608,#66609,#66610,#66611,#66612,#66613,
#66614,#66615,#66616,#66617,#66618,#66619,#66620,#66621,#66622,#66623,#66624,
#66625,#66626,#66627,#66628,#66629,#66630,#66631,#66632,#66633,#66634,#66635,
#66636,#66637,#66638,#66639,#66640,#66641,#66642,#66643,#66644,#66645,#66646,
#66647,#66648,#66649,#66650,#66651,#66652,#66653,#66654,#66655,#66656,#66657,
#66658,#66659,#66660,#66661,#66662,#66663,#66664,#66665,#66666,#66667,#66668,
#66669,#66670,#66671,#66672,#66673,#66674,#66675,#66676,#66677,#66678,#66679,
#66680,#66681,#66682,#66683,#66684,#66685,#66686,#66687,#66688,#66689,#66690,
#66691,#66692,#66693,#66694,#66695,#66696,#66697,#66698,#66699,#66700,#66701,
#66702,#66703,#66704,#66705,#66706,#66707,#66708,#66709,#66710,#66711,#66712,
#66713,#66714,#66715,#66716,#66717,#66718,#66719,#66720,#66721,#66722,#66723,
#66724,#66725,#66726,#66727,#66728,#66729,#66730,#66731,#66732,#66733,#66734,
#66735,#66736,#66737,#66738,#66739,#66740,#66741,#66742,#66743,#66744,#66745,
#66746,#66747,#66748,#66749,#66750,#66751,#66752,#66753,#66754,#66755,#66756,
#66757,#66758,#66759,#66760,#66761,#66762,#66763,#66764,#66765,#66766,#66767,
#66768,#66769,#66770,#66771,#66772,#66773,#66774,#66775,#66776,#66777,#66778,
#66779,#66780,#66781,#66782,#66783,#66784,#66785,#66786,#66787,#66788,#66789,
#66790,#66791,#66792,#66793,#66794,#66795,#66796,#66797,#66798,#66799,#66800,
#66801,#66802,#66803,#66804,#66805,#66806,#66807,#66808,#66809,#66810),
 .UNSPECIFIED.,.F.,.F.,(4,2,2,2,2,2,2,2,2,2,2,2,2,2,2,2,2,2,2,2,2,2,2,2,
2,2,2,2,2,2,2,2,2,2,2,2,2,2,2,2,2,2,2,2,2,2,2,2,2,2,2,2,2,2,2,2,2,2,2,2,
2,2,2,2,2,2,2,2,2,2,2,2,2,2,2,2,2,2,2,2,2,2,2,2,2,2,2,2,2,2,2,2,2,2,2,2,
2,2,2,2,2,2,2,2,2,2,2,2,2,2,2,2,2,2,2,2,2,2,2,2,2,2,2,2,2,2,2,2,2,2,2,2,
2,2,2,2,2,2,2,2,2,2,2,2,2,2,2,2,2,2,2,2,2,2,2,2,2,2,2,2,2,2,2,2,2,2,2,2,
2,2,2,2,2,2,2,2,2,2,2,2,2,2,2,2,2,2,2,2,2,2,2,2,2,2,2,2,2,2,2,2,2,2,2,2,
2,2,2,2,2,2,2,2,2,2,2,2,2,2,2,2,2,2,2,2,2,2,2,2,2,2,2,2,2,2,2,2,2,2,2,2,
2,2,2,4),(0.00333856859840685,0.284619736140031,0.310732212505619,0.341204881842414,
0.346286074758269,0.348961341292532,0.35115035079119,0.353351624430859,
0.357381848054998,0.370283360509686,0.512242771930392,0.683425176397613,
0.749100293442828,0.785617124075771,0.79668300737984,0.80372500210769,0.810321021216165,
0.818984859491134,0.825984092719778,0.865776294586179,1.08085965254399,
1.10271545327627,1.10833625502156,1.11189108252888,1.1152290492436,1.11961050853901,
1.12704189247446,1.18023216579261,1.35307036406388,1.38639369448937,1.41100405587999,
1.4217388175445,1.42971493079168,1.43718205057407,1.44755276556001,1.47515165607487,
1.67948408578306,1.79852651386993,1.83136480105587,1.86222139423072,1.86694345415087,
1.86938619252466,1.8713630694055,1.87333105338895,1.87688363769478,1.88780266618339,
2.03694253426517,2.16095073339868,2.24137431025706,2.26508824706165,2.27488746806926,
2.27997815779486,2.28318195949117,2.28614816543039,2.2885408080166,2.29130406454485,
2.29597554833943,2.31181169559806,2.61170011913439,2.6851685037231,2.69213542189016,
2.69740394062439,2.69971397595816,2.70141454983806,2.70298527420405,2.70511697552099,
2.70929076824488,2.74255834148684,2.87103138381762,3.04798852341164,3.05944545251147,
3.0648689488328,3.06904319378483,3.07304054716738,3.07870534618662,3.09046052495392,
3.21877077397897,3.35103580108738,3.41337285182702,3.44089056485544,3.44536334059358,
3.44770222782123,3.44960742422265,3.45179781827585,3.45548919106622,3.46860345086369,
3.64384199356018,3.81612051207427,3.83544714712346,3.83998455119368,3.84258343474566,
3.84460295376569,3.84724512380881,3.85185183240807,3.86984005514159,4.17674663343024,
4.25415149167353,4.2638868468881,4.26627857461073,4.26766642587972,4.26887617021122,
4.2703663933379,4.2726647070277,4.28315059430245,4.55456821585407,4.62928199678382,
4.66235120995652,4.66749733141106,4.67016081181622,4.67231630492058,4.67446258483323,
4.67833406637735,4.69022042633393,4.8671963040303,4.98727923519819,5.05859126307058,
5.06298012073654,5.06466216323046,5.06587504661516,5.0670342207453,5.06866750234386,
5.07200369103419,5.10127021238341,5.15237678373598,5.35326114791585,5.3983550956444,
5.47326243165098,5.48057622775057,5.48356452748619,5.48577296813408,5.4881702066483,
5.49143642960815,5.49892867814273,5.60436596498282,5.72688748951995,5.79064270534328,
5.87616617309477,5.88257971302819,5.88526968560489,5.88751078940089,5.88980663318107,
5.89315489002436,5.90198356407408,5.98747286290205,6.01574022020838,6.17140226368766,
6.23802872166707,6.2503559436341,6.31802460874426,6.33147353202305,6.33911584738048,
6.34554632366637,6.35333683076929,6.36783824853846,6.46141493080208,6.60214365347692,
6.63758686100609,6.64433441644536,6.64814482084694,6.65110085585758,6.65496447424074,
6.66189558421183,6.69560024833733,6.81312269773593,6.93439429375189,6.95019043201198,
6.96015467745225,6.96802870233841,6.97688932558825,6.99166439646711,7.04598141917512,
7.33646679683559,7.39788775490939,7.40391009743869,7.40633950346372,7.40836173379855,
7.41043366147188,7.41339564760077,7.42081395056037,7.52420116356839,7.62398292530944,
7.80645168097928,7.81830261827922,7.82246364043866,7.82484848851303,7.82705216266016,
7.83004067306684,7.83574154049665,7.87026241515591,7.94416352615619,8.13977662323811,
8.22841912104313,8.23436510486817,8.23661351353941,8.23821490069092,8.23972911876566,
8.24134958719679,8.24477750829023,8.26009300085787,8.2893354057991,8.36616526888381,
8.46784621397586,8.58455991286838,8.59651042472393,8.60196840379477,8.60616201397605,
8.61066380508279,8.61775762638676,8.63870261223748,8.72665519044293,8.87099790860996,
8.97540086341416,8.98162602183915,8.98410235528951,8.98590863520523,8.9878468999123,
8.98974446616838,8.99420011229206,9.02232103652388,9.05965205989318,9.11787644591066,
9.30409301029584,9.36882371713917,9.37508255233326,9.37811694411651,9.3802770610686,
9.38231928321416,9.38516132935038,9.39083889647657,9.43460552604944,9.50183645866207,
9.57765477149944,9.61032738298099,9.62679606690743,9.64550862587289,9.79058827780798,
9.80001130044398,9.80246697509114,9.80388342991624,9.80507944683785,9.80652777305202,
9.80925051369668,9.82486059692485,9.96649908929926),.UNSPECIFIED.);
#3461=B_SPLINE_CURVE_WITH_KNOTS('',3,(#66812,#66813,#66814,#66815,#66816,
#66817,#66818,#66819,#66820,#66821,#66822,#66823,#66824,#66825,#66826,#66827,
#66828,#66829,#66830,#66831,#66832,#66833,#66834,#66835,#66836,#66837,#66838,
#66839,#66840,#66841,#66842,#66843,#66844,#66845,#66846,#66847,#66848,#66849,
#66850,#66851,#66852,#66853,#66854,#66855,#66856,#66857,#66858,#66859,#66860,
#66861,#66862,#66863,#66864,#66865,#66866,#66867,#66868,#66869,#66870,#66871,
#66872,#66873,#66874,#66875,#66876,#66877,#66878,#66879,#66880,#66881,#66882,
#66883,#66884,#66885,#66886,#66887,#66888,#66889,#66890,#66891,#66892,#66893,
#66894,#66895,#66896,#66897,#66898,#66899,#66900,#66901,#66902,#66903,#66904,
#66905,#66906,#66907,#66908,#66909,#66910,#66911,#66912,#66913,#66914,#66915,
#66916,#66917,#66918,#66919,#66920,#66921,#66922,#66923,#66924,#66925,#66926,
#66927,#66928,#66929,#66930,#66931,#66932,#66933,#66934,#66935,#66936,#66937,
#66938,#66939,#66940,#66941,#66942,#66943,#66944,#66945,#66946,#66947,#66948,
#66949,#66950,#66951,#66952,#66953,#66954,#66955,#66956,#66957,#66958,#66959,
#66960,#66961,#66962,#66963,#66964,#66965,#66966,#66967,#66968,#66969,#66970,
#66971,#66972,#66973,#66974,#66975,#66976,#66977,#66978,#66979,#66980,#66981,
#66982,#66983,#66984,#66985,#66986,#66987,#66988,#66989,#66990,#66991,#66992,
#66993,#66994,#66995,#66996,#66997,#66998,#66999,#67000,#67001,#67002,#67003,
#67004,#67005,#67006,#67007,#67008,#67009,#67010,#67011,#67012,#67013,#67014,
#67015,#67016,#67017,#67018,#67019,#67020,#67021,#67022,#67023,#67024,#67025,
#67026,#67027,#67028,#67029,#67030,#67031,#67032,#67033,#67034,#67035,#67036,
#67037,#67038,#67039,#67040,#67041,#67042,#67043,#67044,#67045,#67046,#67047,
#67048,#67049,#67050,#67051,#67052,#67053,#67054,#67055,#67056,#67057,#67058,
#67059,#67060,#67061,#67062,#67063,#67064,#67065,#67066,#67067,#67068,#67069,
#67070),.UNSPECIFIED.,.F.,.F.,(4,3,3,3,3,3,3,3,3,3,3,3,3,3,3,3,3,3,3,3,
3,3,3,3,3,3,3,3,3,3,3,3,3,3,3,3,3,3,3,3,3,3,3,3,3,3,3,3,3,3,3,3,3,3,3,3,
3,3,3,3,3,3,3,3,3,3,3,3,3,3,3,3,3,3,3,3,3,3,3,3,3,3,3,3,3,3,4),(107.937798928197,
108.009679787755,108.081504421882,108.153288071956,108.225642008513,108.297402811625,
108.3691705556,108.440958965509,108.513749115235,108.585656546406,108.658888055409,
108.732119564413,108.807656197669,108.883106955815,108.958484731036,109.033802367837,
109.109072671081,109.186646330413,109.261866024691,109.337079840601,109.412299324809,
109.487536024993,109.562828554874,109.63815429051,109.713550508267,109.729661945738,
109.806260687544,109.882794377386,109.959272693195,110.035696829543,110.112088235741,
110.188455820887,110.228433136401,110.306554286418,110.384720352047,110.462936067119,
110.541242529328,110.619597186618,110.698037121605,110.727204327063,110.809173128142,
110.891070140534,110.974796484832,111.056453358329,111.141214438028,111.225975517726,
111.299602542256,111.373224315984,111.44685382182,111.520535490071,111.594244423666,
111.668035004164,111.724746708388,111.801252015151,111.877701493684,111.954106042787,
112.03047652894,112.106823793623,112.183756955634,112.260103916869,112.336461183379,
112.412838607712,112.490201228212,112.566677800309,112.644483445011,112.722289089713,
112.796982177518,112.871595457739,112.946141313354,113.02062162159,113.095063696886,
113.169480525979,113.221060280375,113.301354296142,113.381792915329,113.466302554256,
113.547077099462,113.627952583241,113.708962628932,113.719831471038,113.796253877641,
113.872580080563,113.948820155796,114.024960507632,114.101042441477,114.177062345978,
114.220984235377),.UNSPECIFIED.);
#3462=B_SPLINE_CURVE_WITH_KNOTS('',3,(#67072,#67073,#67074,#67075,#67076,
#67077,#67078,#67079,#67080,#67081,#67082,#67083,#67084,#67085,#67086,#67087,
#67088,#67089,#67090,#67091,#67092,#67093,#67094,#67095,#67096,#67097,#67098,
#67099,#67100,#67101,#67102,#67103,#67104,#67105,#67106,#67107,#67108,#67109,
#67110,#67111,#67112,#67113,#67114,#67115,#67116,#67117,#67118,#67119,#67120,
#67121,#67122,#67123,#67124,#67125,#67126,#67127,#67128,#67129,#67130,#67131,
#67132,#67133,#67134,#67135,#67136,#67137,#67138,#67139,#67140,#67141,#67142,
#67143,#67144,#67145,#67146,#67147,#67148,#67149,#67150,#67151,#67152,#67153,
#67154,#67155,#67156,#67157,#67158,#67159,#67160,#67161,#67162,#67163,#67164,
#67165,#67166,#67167,#67168,#67169,#67170,#67171,#67172,#67173,#67174,#67175,
#67176,#67177,#67178,#67179,#67180,#67181,#67182,#67183,#67184,#67185,#67186,
#67187,#67188,#67189,#67190,#67191,#67192,#67193,#67194,#67195,#67196,#67197,
#67198,#67199,#67200,#67201,#67202,#67203,#67204,#67205,#67206,#67207,#67208,
#67209,#67210,#67211,#67212,#67213,#67214,#67215,#67216,#67217,#67218,#67219,
#67220,#67221,#67222,#67223,#67224,#67225,#67226,#67227,#67228,#67229,#67230,
#67231,#67232,#67233,#67234,#67235,#67236,#67237,#67238,#67239,#67240,#67241,
#67242,#67243,#67244,#67245,#67246,#67247,#67248,#67249,#67250,#67251,#67252,
#67253,#67254,#67255,#67256,#67257,#67258,#67259,#67260,#67261,#67262,#67263,
#67264,#67265,#67266,#67267,#67268,#67269,#67270,#67271,#67272,#67273,#67274,
#67275,#67276,#67277,#67278,#67279,#67280,#67281,#67282,#67283,#67284,#67285,
#67286,#67287,#67288,#67289,#67290,#67291,#67292,#67293,#67294,#67295,#67296,
#67297,#67298,#67299,#67300,#67301,#67302,#67303,#67304,#67305,#67306,#67307,
#67308,#67309,#67310,#67311,#67312,#67313,#67314,#67315,#67316,#67317,#67318,
#67319,#67320,#67321,#67322,#67323,#67324,#67325,#67326,#67327,#67328,#67329,
#67330,#67331,#67332,#67333,#67334,#67335,#67336,#67337,#67338,#67339,#67340,
#67341,#67342,#67343,#67344,#67345,#67346,#67347,#67348,#67349,#67350,#67351,
#67352,#67353,#67354,#67355,#67356,#67357,#67358,#67359,#67360,#67361,#67362,
#67363,#67364,#67365,#67366,#67367,#67368,#67369,#67370,#67371,#67372,#67373,
#67374,#67375,#67376,#67377,#67378,#67379,#67380,#67381,#67382,#67383,#67384,
#67385,#67386,#67387,#67388,#67389,#67390,#67391,#67392,#67393,#67394,#67395,
#67396,#67397,#67398,#67399,#67400,#67401,#67402,#67403,#67404,#67405,#67406,
#67407,#67408,#67409,#67410,#67411,#67412,#67413,#67414,#67415,#67416,#67417,
#67418,#67419,#67420,#67421,#67422,#67423,#67424,#67425,#67426,#67427,#67428,
#67429,#67430,#67431,#67432,#67433,#67434,#67435,#67436,#67437,#67438,#67439,
#67440,#67441,#67442,#67443,#67444,#67445,#67446,#67447,#67448,#67449,#67450,
#67451,#67452,#67453,#67454,#67455,#67456,#67457,#67458,#67459,#67460,#67461,
#67462,#67463,#67464,#67465,#67466,#67467,#67468,#67469,#67470,#67471,#67472,
#67473,#67474,#67475,#67476,#67477,#67478,#67479,#67480,#67481,#67482,#67483,
#67484,#67485,#67486,#67487,#67488,#67489,#67490,#67491,#67492,#67493,#67494,
#67495,#67496,#67497,#67498,#67499,#67500,#67501,#67502,#67503,#67504,#67505,
#67506,#67507,#67508,#67509,#67510,#67511,#67512,#67513,#67514,#67515,#67516,
#67517,#67518,#67519,#67520,#67521,#67522,#67523,#67524,#67525,#67526,#67527,
#67528,#67529,#67530,#67531,#67532,#67533,#67534,#67535,#67536,#67537,#67538,
#67539,#67540,#67541,#67542,#67543,#67544,#67545,#67546,#67547,#67548,#67549,
#67550,#67551,#67552,#67553,#67554,#67555,#67556,#67557,#67558,#67559,#67560,
#67561,#67562,#67563),.UNSPECIFIED.,.F.,.F.,(4,2,2,2,2,2,2,2,2,2,2,2,2,
2,2,2,2,2,2,2,2,2,2,2,2,2,2,2,2,2,2,2,2,2,2,2,2,2,2,2,2,2,2,2,2,2,2,2,2,
2,2,2,2,2,2,2,2,2,2,2,2,2,2,2,2,2,2,2,2,2,2,2,2,2,2,2,2,2,2,2,2,2,2,2,2,
2,2,2,2,2,2,2,2,2,2,2,2,2,2,2,2,2,2,2,2,2,2,2,2,2,2,2,2,2,2,2,2,2,2,2,2,
2,2,2,2,2,2,2,2,2,2,2,2,2,2,2,2,2,2,2,2,2,2,2,2,2,2,2,2,2,2,2,2,2,2,2,2,
2,2,2,2,2,2,2,2,2,2,2,2,2,2,2,2,2,2,2,2,2,2,2,2,2,2,2,2,2,2,2,2,2,2,2,2,
2,2,2,2,2,2,2,2,2,2,2,2,2,2,2,2,2,2,2,2,2,2,2,2,2,2,2,2,2,2,2,2,2,2,2,2,
2,2,2,2,2,2,2,2,2,2,2,2,2,2,2,2,4),(0.00221101600796123,0.294940398990252,
0.344446393877704,0.383713958302492,0.390388737160091,0.392478778912742,
0.393798481889886,0.395020523282386,0.396602589473208,0.400096748693395,
0.428212751745557,0.558443357703154,0.678838207198895,0.783864754714538,
0.791453851911416,0.794574481125808,0.796599252041966,0.798775830731035,
0.801784919286611,0.808617074886337,0.882021864342784,0.950925230679804,
1.0517887987793,1.12987466538263,1.16809382664115,1.18582837742638,1.18870535529707,
1.19024209072519,1.19151147048997,1.19299046703209,1.19553015478069,1.20502108451035,
1.35604567688508,1.47998851801677,1.59760089107955,1.60521262038921,1.6084591886792,
1.61081990271752,1.61324032340629,1.61675119965368,1.62549257913985,1.76785871840477,
1.80078696537217,1.93577640908127,1.95952292585593,1.99759645681226,2.0062113202344,
2.00952694931874,2.01181563835611,2.01406190966798,2.01677594282218,2.02358659409667,
2.12850798601709,2.31861792216491,2.4391981145353,2.45474597810964,2.4627457942354,
2.46861951779537,2.47497550524169,2.4861344979523,2.51943074366916,2.73550553999271,
2.76353848718953,2.76959744638468,2.7732379386688,2.77654758082057,2.78081128979848,
2.78938072039188,2.86515069833341,2.99667471176583,3.06311730216262,3.07828158112576,
3.08716924191958,3.09503657908561,3.10495378619902,3.12071667741521,3.19287518759524,
3.44174246135284,3.49916223168841,3.5243970082556,3.52887999288524,3.53127232918688,
3.53305444193548,3.53528458424103,3.5390279186813,3.55148773864436,3.74367116865347,
3.85336807352492,3.91070505463629,3.93985038186923,3.9452920764229,3.94822467964108,
3.95042189818842,3.95318634924189,3.95786303100498,3.97374424946594,4.25075597417871,
4.35427050102661,4.35924338475827,4.36149920472045,4.36319044892995,4.36477468754753,
4.36695930353944,4.37251713184819,4.46017886987819,4.62492753594253,4.70236122872631,
4.71885994582954,4.72514128982581,4.72946807664061,4.73371359696599,4.73884877938826,
4.75166215720126,4.86467176742369,4.98305744504084,5.09485534761672,5.10451083367231,
5.10781619649007,5.10969073617289,5.11141045676678,5.11372401383544,5.11807811931325,
5.14294296563946,5.19905483631281,5.48389491152695,5.49585394677549,5.50062479700732,
5.50353543078471,5.50580300485759,5.50826448152365,5.5121908905702,5.52498314030815,
5.59893517270499,5.69757744690188,5.73787252713119,5.78212631037049,5.91561031599514,
5.92436788662219,5.92675616407122,5.92815648855939,5.92936409857323,5.93083496231428,
5.93366960720381,5.95187877210987,5.99377298573601,6.07958134449031,6.30933179438556,
6.32398282391089,6.32813507540859,6.3306055775919,6.33275858892246,6.33540675386594,
6.34048526669121,6.371955238811,6.44096127894161,6.5927106648339,6.71383373125756,
6.72160737267125,6.72394614543367,6.7252229402186,6.72649269597564,6.72804281514845,
6.73097927321507,6.74808150382576,6.78295419663718,6.84590352592249,7.05338004988117,
7.1324732241771,7.13988374260119,7.14288771553855,7.14509909415957,7.14749120277648,
7.15073565953597,7.15811415054995,7.25317940958819,7.5025354972263,7.53701136411819,
7.54264958725048,7.5454397677846,7.54755367352287,7.54992771626458,7.55372092425274,
7.55823942865708,7.56698663785587,7.65953860524462,7.82434624940749,7.93837725460838,
7.98038543844159,7.99238532626743,7.99963089933533,8.00551211502852,8.01355308937777,
8.02927349612929,8.04909715424871,8.09413513402357,8.18843500399108,8.22087459838905,
8.29505457010402,8.30282917325925,8.30676644446013,8.30988010404849,8.3135831303279,
8.31978998723772,8.34347473921566,8.38796827401687,8.57107521672241,8.60351769231569,
8.61582974758375,8.62327259492484,8.63125651718348,8.64205364243587,8.66731000722095,
8.75149090683794,8.84003632168467,9.02337590966357,9.0574898588092,9.06272989561353,
9.06527804985395,9.06726536338363,9.06941474496714,9.07282111865078,9.07683786077177,
9.0844296487899,9.10213787841623,9.13612606465791,9.19367068112901,9.45960045680476,
9.47570733634246,9.48040835006537,9.48317750583963,9.4855938413921,9.4886175874711,
9.49449327621657,9.53346434620623,9.62942854047248,9.83601851302572,9.8455306909787,
9.88858657029123,9.89328305854664,9.89546207937708,9.89714650969329,9.89870992134584,
9.90049714337201,9.90301477184182,9.9072952669435,9.96134643791026),
 .UNSPECIFIED.);
#3463=B_SPLINE_CURVE_WITH_KNOTS('',3,(#67565,#67566,#67567,#67568,#67569,
#67570,#67571,#67572,#67573,#67574,#67575,#67576,#67577,#67578,#67579,#67580,
#67581,#67582,#67583,#67584,#67585,#67586,#67587,#67588,#67589,#67590,#67591,
#67592,#67593,#67594,#67595,#67596,#67597,#67598,#67599,#67600,#67601,#67602,
#67603,#67604,#67605,#67606,#67607,#67608,#67609,#67610,#67611,#67612,#67613,
#67614,#67615,#67616,#67617,#67618,#67619,#67620,#67621,#67622,#67623,#67624,
#67625,#67626,#67627,#67628,#67629,#67630,#67631,#67632,#67633,#67634,#67635,
#67636,#67637,#67638,#67639,#67640,#67641,#67642,#67643,#67644,#67645,#67646,
#67647,#67648,#67649,#67650,#67651,#67652,#67653,#67654,#67655,#67656,#67657,
#67658,#67659,#67660,#67661,#67662,#67663,#67664,#67665,#67666,#67667,#67668,
#67669,#67670,#67671,#67672,#67673,#67674,#67675,#67676,#67677,#67678,#67679,
#67680,#67681,#67682,#67683,#67684,#67685,#67686,#67687,#67688,#67689,#67690,
#67691,#67692,#67693,#67694,#67695,#67696,#67697,#67698,#67699,#67700,#67701,
#67702,#67703,#67704,#67705,#67706,#67707,#67708,#67709,#67710,#67711,#67712,
#67713,#67714,#67715,#67716,#67717,#67718,#67719,#67720,#67721,#67722,#67723,
#67724,#67725,#67726,#67727,#67728,#67729,#67730,#67731,#67732,#67733,#67734,
#67735,#67736,#67737,#67738,#67739,#67740,#67741,#67742,#67743,#67744,#67745,
#67746,#67747,#67748,#67749,#67750,#67751,#67752,#67753,#67754,#67755,#67756,
#67757,#67758,#67759,#67760,#67761,#67762,#67763,#67764,#67765,#67766,#67767,
#67768,#67769,#67770,#67771,#67772,#67773,#67774,#67775,#67776,#67777,#67778,
#67779,#67780,#67781,#67782,#67783,#67784,#67785,#67786,#67787,#67788,#67789,
#67790,#67791,#67792,#67793,#67794,#67795,#67796,#67797,#67798,#67799,#67800,
#67801,#67802,#67803,#67804,#67805,#67806,#67807,#67808,#67809,#67810,#67811,
#67812,#67813,#67814,#67815,#67816,#67817,#67818,#67819,#67820,#67821,#67822,
#67823,#67824,#67825,#67826),.UNSPECIFIED.,.F.,.F.,(4,3,3,3,3,3,3,3,3,3,
3,3,3,3,3,3,3,3,3,3,3,3,3,3,3,3,3,3,3,3,3,3,3,3,3,3,3,3,3,3,3,3,3,3,3,3,
3,3,3,3,3,3,3,3,3,3,3,3,3,3,3,3,3,3,3,3,3,3,3,3,3,3,3,3,3,3,3,3,3,3,3,3,
3,3,3,3,3,4),(126.787354849736,126.859442342501,126.931470599143,127.003449731494,
127.075400049158,127.147341795895,127.186653618924,127.26694763469,127.347386253876,
127.431895892803,127.512670438008,127.593545921785,127.674555967475,127.685424809586,
127.759965614158,127.834430435794,127.90883316579,127.983187654446,128.05750771988,
128.135690153759,128.209997942834,128.284315420204,128.358655073321,128.433029398995,
128.507489428851,128.581999257075,128.656609530046,128.682967190911,128.756120282925,
128.829185532227,128.902177863279,128.975112131816,129.048003140213,129.120865651371,
129.193728264913,129.266594650327,129.339478150665,129.412392120165,129.48539285565,
129.558441055326,129.631600226992,129.680509572236,129.756046205493,129.831496963639,
129.90687473886,129.98219237566,130.057462678904,130.135036338236,130.210256032515,
130.285469848424,130.360689332632,130.435926032816,130.511218562696,130.586544298332,
130.661940516089,130.678051953561,130.754650695366,130.831184385207,130.907662701015,
130.984086837362,131.060478243558,131.136845828703,131.176823144223,131.254944294241,
131.333110359872,131.411326074945,131.489632537157,131.567987194449,131.646427129437,
131.675594334886,131.757563135962,131.839460148351,131.923186492651,132.004843366145,
132.089604445847,132.174365525548,132.247992550079,132.321614323809,132.395243829646,
132.468925497898,132.542634431494,132.616425011994,132.673136716211,132.758107903129,
132.842895618683,132.927528471115,133.011843765426,133.070540156915),
 .UNSPECIFIED.);
#3464=B_SPLINE_CURVE_WITH_KNOTS('',3,(#67828,#67829,#67830,#67831,#67832,
#67833,#67834,#67835,#67836,#67837,#67838,#67839,#67840,#67841,#67842,#67843,
#67844,#67845),.UNSPECIFIED.,.F.,.F.,(4,2,2,2,2,2,2,2,4),(133.070540156915,
133.90545706881,134.740373980705,135.5752908926,136.410207804495,137.24512471639,
138.080041628285,138.914958540179,139.353725464095),.UNSPECIFIED.);
#3465=B_SPLINE_CURVE_WITH_KNOTS('',3,(#67847,#67848,#67849,#67850,#67851,
#67852,#67853,#67854,#67855,#67856,#67857,#67858),.UNSPECIFIED.,.F.,.F.,
(4,1,1,1,1,1,1,1,1,4),(139.353725464095,139.655933385485,140.65347576681,
141.152246957472,141.651018148135,142.64856052946,143.646102910785,144.643645292109,
145.142416482772,145.636910654589),.UNSPECIFIED.);
#3466=B_SPLINE_CURVE_WITH_KNOTS('',3,(#67860,#67861,#67862,#67863,#67864,
#67865,#67866,#67867,#67868,#67869,#67870,#67871,#67872,#67873,#67874,#67875,
#67876,#67877,#67878,#67879,#67880,#67881,#67882,#67883,#67884,#67885,#67886,
#67887,#67888,#67889,#67890,#67891,#67892,#67893,#67894,#67895,#67896,#67897,
#67898,#67899,#67900,#67901,#67902,#67903,#67904,#67905,#67906,#67907,#67908,
#67909,#67910,#67911,#67912,#67913,#67914,#67915,#67916,#67917,#67918,#67919,
#67920,#67921,#67922,#67923,#67924,#67925,#67926,#67927,#67928,#67929,#67930,
#67931,#67932,#67933,#67934,#67935,#67936,#67937,#67938,#67939,#67940,#67941,
#67942,#67943,#67944,#67945,#67946,#67947,#67948,#67949,#67950,#67951,#67952,
#67953,#67954,#67955,#67956,#67957,#67958,#67959,#67960,#67961,#67962,#67963,
#67964,#67965,#67966,#67967,#67968,#67969,#67970,#67971,#67972,#67973,#67974,
#67975,#67976,#67977,#67978,#67979,#67980,#67981,#67982,#67983,#67984,#67985,
#67986,#67987,#67988,#67989,#67990,#67991,#67992,#67993,#67994,#67995,#67996,
#67997,#67998,#67999,#68000,#68001,#68002,#68003,#68004,#68005,#68006,#68007,
#68008,#68009,#68010,#68011,#68012,#68013,#68014,#68015,#68016,#68017,#68018,
#68019,#68020,#68021,#68022,#68023,#68024,#68025,#68026,#68027,#68028,#68029,
#68030,#68031,#68032,#68033,#68034,#68035,#68036,#68037,#68038,#68039,#68040,
#68041,#68042,#68043,#68044,#68045,#68046,#68047,#68048,#68049,#68050,#68051,
#68052,#68053,#68054,#68055,#68056,#68057,#68058,#68059,#68060,#68061,#68062,
#68063,#68064,#68065,#68066,#68067,#68068,#68069,#68070,#68071,#68072,#68073,
#68074,#68075,#68076,#68077,#68078,#68079,#68080,#68081,#68082,#68083,#68084,
#68085,#68086,#68087,#68088,#68089,#68090,#68091,#68092,#68093,#68094,#68095,
#68096,#68097,#68098,#68099,#68100,#68101,#68102,#68103,#68104,#68105,#68106,
#68107,#68108,#68109,#68110,#68111,#68112,#68113,#68114,#68115,#68116,#68117,
#68118,#68119,#68120,#68121),.UNSPECIFIED.,.F.,.F.,(4,3,3,3,3,3,3,3,3,3,
3,3,3,3,3,3,3,3,3,3,3,3,3,3,3,3,3,3,3,3,3,3,3,3,3,3,3,3,3,3,3,3,3,3,3,3,
3,3,3,3,3,3,3,3,3,3,3,3,3,3,3,3,3,3,3,3,3,3,3,3,3,3,3,3,3,3,3,3,3,3,3,3,
3,3,3,3,3,4),(145.636910771275,145.641187673434,145.723156474513,145.805053486906,
145.888779831204,145.970436704702,146.0551977844,146.139958864097,146.213585888627,
146.287207662355,146.36083716819,146.434518836441,146.508227770035,146.582018350533,
146.638730054759,146.715235361522,146.791684840055,146.868089389159,146.944459875312,
147.020807139994,147.097740302005,147.17408726324,147.25044452975,147.326821954083,
147.404184574583,147.480661146681,147.558466791382,147.636272436084,147.71096552389,
147.785578804112,147.860124659728,147.934604967965,148.009047043262,148.083463872356,
148.135043626747,148.215337642513,148.295776261699,148.380285900626,148.46106044583,
148.541935929607,148.622945975298,148.633814817409,148.708355621981,148.782820443617,
148.857223173613,148.931577662269,149.005897727703,149.084080161582,149.158387950657,
149.232705428027,149.307045081143,149.381419406818,149.455879436673,149.530389264898,
149.604999537868,149.631357198734,149.704510290748,149.77757554005,149.850567871102,
149.923502139639,149.996393148036,150.069255659195,150.142118272736,150.21498465815,
150.287868158489,150.360782127988,150.433782863474,150.506831063149,150.579990234816,
150.628899580059,150.704436213315,150.779886971462,150.855264746683,150.930582383483,
151.005852686728,151.08342634606,151.158646040338,151.233859856247,151.309079340455,
151.384316040639,151.45960857052,151.534934306156,151.610330523913,151.626441961384,
151.708619166871,151.790681921113,151.872549033798,151.920096078454),
 .UNSPECIFIED.);
#3467=B_SPLINE_CURVE_WITH_KNOTS('',3,(#68123,#68124,#68125,#68126,#68127,
#68128,#68129,#68130,#68131,#68132,#68133,#68134,#68135),.UNSPECIFIED.,
 .F.,.F.,(4,1,1,1,1,1,1,1,1,1,4),(151.920097103546,152.125213152046,152.623984342709,
153.122755533371,153.621526724033,154.619069105358,155.117840296021,155.616611486683,
156.614153868008,157.611696249333,158.203281385634),.UNSPECIFIED.);
#3468=B_SPLINE_CURVE_WITH_KNOTS('',3,(#68137,#68138,#68139,#68140,#68141,
#68142,#68143,#68144,#68145,#68146,#68147,#68148,#68149,#68150,#68151,#68152,
#68153,#68154,#68155,#68156,#68157,#68158,#68159,#68160,#68161,#68162,#68163,
#68164,#68165,#68166,#68167,#68168,#68169,#68170,#68171,#68172,#68173,#68174,
#68175,#68176,#68177,#68178,#68179,#68180,#68181,#68182,#68183,#68184,#68185,
#68186,#68187,#68188,#68189,#68190,#68191,#68192,#68193,#68194,#68195,#68196,
#68197,#68198,#68199,#68200,#68201,#68202,#68203,#68204,#68205,#68206,#68207,
#68208,#68209,#68210,#68211,#68212,#68213,#68214,#68215,#68216,#68217,#68218,
#68219,#68220,#68221,#68222,#68223,#68224,#68225,#68226,#68227,#68228,#68229,
#68230,#68231,#68232,#68233,#68234,#68235,#68236,#68237,#68238,#68239,#68240,
#68241,#68242,#68243,#68244,#68245,#68246,#68247,#68248,#68249,#68250,#68251,
#68252,#68253,#68254,#68255,#68256,#68257,#68258,#68259,#68260,#68261,#68262,
#68263,#68264,#68265,#68266,#68267,#68268,#68269,#68270,#68271,#68272,#68273,
#68274,#68275,#68276,#68277,#68278,#68279,#68280,#68281,#68282,#68283,#68284,
#68285,#68286,#68287,#68288,#68289,#68290,#68291,#68292,#68293,#68294,#68295,
#68296,#68297,#68298,#68299,#68300,#68301,#68302,#68303,#68304,#68305,#68306,
#68307,#68308,#68309,#68310,#68311,#68312,#68313,#68314,#68315,#68316,#68317,
#68318,#68319,#68320,#68321,#68322,#68323,#68324,#68325,#68326,#68327,#68328,
#68329,#68330,#68331,#68332,#68333,#68334,#68335,#68336,#68337,#68338,#68339,
#68340,#68341,#68342,#68343,#68344,#68345,#68346,#68347,#68348,#68349,#68350,
#68351,#68352,#68353,#68354,#68355,#68356,#68357,#68358,#68359,#68360,#68361,
#68362,#68363,#68364,#68365,#68366,#68367,#68368,#68369,#68370,#68371,#68372,
#68373,#68374,#68375,#68376,#68377,#68378,#68379,#68380,#68381,#68382,#68383,
#68384,#68385,#68386,#68387,#68388,#68389,#68390,#68391,#68392,#68393,#68394,
#68395,#68396,#68397,#68398,#68399,#68400,#68401,#68402,#68403,#68404,#68405,
#68406,#68407,#68408,#68409,#68410,#68411,#68412,#68413,#68414,#68415,#68416,
#68417,#68418,#68419,#68420,#68421,#68422,#68423,#68424,#68425,#68426,#68427,
#68428,#68429,#68430,#68431,#68432,#68433,#68434,#68435,#68436,#68437,#68438,
#68439,#68440,#68441,#68442,#68443,#68444,#68445,#68446,#68447,#68448,#68449,
#68450,#68451,#68452,#68453,#68454,#68455,#68456,#68457,#68458,#68459,#68460,
#68461,#68462,#68463,#68464,#68465,#68466,#68467,#68468,#68469,#68470,#68471,
#68472,#68473,#68474,#68475,#68476,#68477,#68478,#68479,#68480,#68481,#68482,
#68483,#68484,#68485,#68486,#68487,#68488,#68489,#68490,#68491,#68492,#68493,
#68494,#68495,#68496,#68497,#68498,#68499,#68500,#68501,#68502,#68503,#68504,
#68505,#68506,#68507,#68508,#68509,#68510,#68511,#68512,#68513,#68514,#68515,
#68516,#68517,#68518,#68519,#68520,#68521,#68522,#68523,#68524,#68525,#68526,
#68527,#68528,#68529,#68530,#68531,#68532,#68533,#68534,#68535,#68536,#68537,
#68538,#68539,#68540,#68541,#68542,#68543,#68544,#68545,#68546,#68547,#68548,
#68549,#68550,#68551,#68552,#68553,#68554,#68555,#68556,#68557,#68558,#68559,
#68560,#68561,#68562,#68563,#68564,#68565,#68566,#68567,#68568,#68569,#68570,
#68571,#68572,#68573,#68574,#68575,#68576,#68577,#68578,#68579,#68580,#68581,
#68582,#68583,#68584,#68585,#68586,#68587,#68588,#68589,#68590,#68591,#68592,
#68593,#68594,#68595,#68596,#68597,#68598,#68599,#68600,#68601,#68602,#68603,
#68604,#68605,#68606,#68607,#68608,#68609,#68610,#68611,#68612,#68613,#68614,
#68615,#68616,#68617,#68618,#68619,#68620,#68621,#68622,#68623,#68624,#68625,
#68626,#68627,#68628,#68629,#68630,#68631,#68632),.UNSPECIFIED.,.F.,.F.,
(4,2,2,2,2,2,2,2,2,2,2,2,2,2,2,2,2,2,2,2,2,2,2,2,2,2,2,2,2,2,2,2,2,2,2,
2,2,2,2,2,2,2,2,2,2,2,2,2,2,2,2,2,2,2,2,2,2,2,2,2,2,2,2,2,2,2,2,2,2,2,2,
2,2,2,2,2,2,2,2,2,2,2,2,2,2,2,2,2,2,2,2,2,2,2,2,2,2,2,2,2,2,2,2,2,2,2,2,
2,2,2,2,2,2,2,2,2,2,2,2,2,2,2,2,2,2,2,2,2,2,2,2,2,2,2,2,2,2,2,2,2,2,2,2,
2,2,2,2,2,2,2,2,2,2,2,2,2,2,2,2,2,2,2,2,2,2,2,2,2,2,2,2,2,2,2,2,2,2,2,2,
2,2,2,2,2,2,2,2,2,2,2,2,2,2,2,2,2,2,2,2,2,2,2,2,2,2,2,2,2,2,2,2,2,2,2,2,
2,2,2,2,2,2,2,2,2,2,2,2,2,2,2,2,2,2,2,2,2,2,2,2,2,2,2,2,2,2,2,2,4),(0.00169003533835,
0.288045268131539,0.3421649754555,0.352897314127812,0.356511362344053,0.35886362064682,
0.361093357559019,0.364047709823501,0.370707227972985,0.442332842734841,
0.553486978526161,0.721924589962906,0.790429699342945,0.803628054006262,
0.811134702086208,0.817631552265838,0.825604117743465,0.840226111381366,
0.925902576319046,1.04179377793575,1.0876109905549,1.11105807856665,1.1168026467886,
1.12038141760047,1.12370929125231,1.12803099258193,1.13525779442268,1.18245076316577,
1.29557218641728,1.39601527720204,1.41981986101972,1.43041383167253,1.43836701163681,
1.44587239467617,1.4563938410042,1.4850127795495,1.73291434717376,1.83583175380349,
1.87060145820998,1.87545827301694,1.87792884037744,1.87988976742142,1.88183871419,
1.88529722956237,1.89551770627139,2.0455736074636,2.16955647699158,2.2499487325598,
2.273656327109,2.28345336733454,2.28854310404211,2.29174640771982,2.29470645520424,
2.29709911169969,2.29986035696478,2.30452354372262,2.32028947619084,2.59743706295665,
2.70094992659311,2.70589756609823,2.70814853753967,2.70983885537649,2.71142420213534,
2.71361346480929,2.719199696416,2.81325162794002,3.0358079018886,3.06296054239148,
3.07052783073283,3.07513371026124,3.07929421316157,3.0846199652116,3.0931293275506,
3.13244813077903,3.18565168884913,3.34177547450781,3.44739244230559,3.4529785443134,
3.45553882922208,3.45746949207241,3.45928520831361,3.4622984099423,3.47000893796097,
3.55858672557251,3.68411785111851,3.76515927735238,3.81648028330425,3.84260563460912,
3.84758289254568,3.85027766461067,3.85250001119127,3.85512658474137,3.85966750128629,
3.87697756782417,4.15856610215374,4.2420145107666,4.27015734919051,4.27333856827254,
4.27489371555689,4.27599656177498,4.27714970603676,4.27875821813101,4.28300957378941,
4.34831745570499,4.54478956791381,4.60133112417586,4.64156248758237,4.66985013688603,
4.67478924687912,4.6774089121329,4.67956154729329,4.68205721528173,4.68631306593921,
4.70192958191256,4.98446823060957,5.06570553957838,5.07053025402685,5.07227614263959,
5.07350638376477,5.07465899674675,5.07624643299506,5.07935678014783,5.10069670862331,
5.16410639704356,5.35903238238304,5.39488458972281,5.48066484784574,5.48823050148015,
5.49126287501233,5.49348284510885,5.49587250632902,5.49909301511976,5.50632976726016,
5.62739806970566,5.73629016666609,5.79419089698692,5.88396812674939,5.88984025441354,
5.89274299618139,5.89483390822586,5.89705320831283,5.89998976572733,5.90637525978894,
6.0376358521255,6.1209643238565,6.31112246315615,6.33407420911135,6.34273009277626,
6.34893844711936,6.35552992995728,6.36430347086444,6.38383794866738,6.46333374718156,
6.56897853803143,6.64390275262583,6.65181980446199,6.65580348478561,6.65908929512506,
6.66291740915685,6.669684170347,6.70072476662585,6.83288257014554,6.89888425020493,
6.94811642061838,6.96254481853922,6.97127493888006,6.9783829702625,6.98816966159238,
7.00656066468097,7.09523491404739,7.21017253699412,7.34725655588969,7.35168892904982,
7.35571884955472,7.36483173529657,7.40613770690696,7.41110727325242,7.41363989236017,
7.41550419290297,7.41752114702744,7.4202044165012,7.42604366359072,7.43376957197959,
7.50320462907729,7.61064298740999,7.81245160560922,7.82549710603779,7.82982382596968,
7.83224183686882,7.83465989409483,7.83768488996447,7.8435601124925,7.88242944237892,
7.97858683471607,8.16314800407253,8.23702651438012,8.24218926455461,8.24430558395608,
8.24587224583045,8.24757536373241,8.2498526634701,8.2549628546333,8.26190975543162,
8.27927792730486,8.34265486956678,8.44570122038853,8.591681994606,8.60387341595175,
8.60937545021437,8.61357591650927,8.61805883459946,8.62506812299598,8.64541119977553,
8.73969685526377,8.89589993370086,8.94583370350186,8.98439969078601,8.98917830281284,
8.99161726783138,8.99341383871419,8.99535848634535,8.99726771833799,9.00183442329845,
9.03305394982638,9.07979359689901,9.12293051843789,9.2918436804488,9.37553913867367,
9.38280018796745,9.38570643089234,9.38783254851848,9.39011971559718,9.39319960740163,
9.40010936714799,9.51573800276529,9.59268743958876,9.62642247510404,9.64352603435034,
9.6626715083179,9.79892639731796,9.80753916787733,9.80991308308417,9.81131045280769,
9.81239815070129,9.81382195085477,9.81642728596756,9.81964282068652,9.96333031754118),
 .UNSPECIFIED.);
#3469=B_SPLINE_CURVE_WITH_KNOTS('',3,(#68634,#68635,#68636,#68637,#68638,
#68639,#68640,#68641,#68642,#68643,#68644,#68645,#68646,#68647,#68648,#68649,
#68650,#68651,#68652,#68653,#68654,#68655,#68656,#68657,#68658,#68659,#68660,
#68661,#68662,#68663,#68664,#68665,#68666,#68667,#68668,#68669,#68670,#68671,
#68672,#68673,#68674,#68675,#68676,#68677,#68678,#68679,#68680,#68681,#68682,
#68683,#68684,#68685,#68686,#68687,#68688,#68689,#68690,#68691,#68692,#68693,
#68694,#68695,#68696,#68697,#68698,#68699,#68700,#68701,#68702,#68703,#68704,
#68705,#68706,#68707,#68708,#68709,#68710,#68711,#68712,#68713,#68714,#68715,
#68716,#68717,#68718,#68719,#68720,#68721,#68722,#68723,#68724,#68725,#68726,
#68727,#68728,#68729,#68730,#68731,#68732,#68733,#68734,#68735,#68736,#68737,
#68738,#68739,#68740,#68741,#68742,#68743,#68744,#68745,#68746,#68747,#68748,
#68749,#68750,#68751,#68752,#68753,#68754,#68755,#68756,#68757,#68758,#68759,
#68760,#68761,#68762,#68763,#68764,#68765,#68766,#68767,#68768,#68769,#68770,
#68771,#68772,#68773,#68774,#68775,#68776,#68777,#68778,#68779,#68780,#68781,
#68782,#68783,#68784,#68785,#68786,#68787,#68788,#68789,#68790,#68791,#68792,
#68793,#68794,#68795,#68796,#68797,#68798,#68799,#68800,#68801,#68802,#68803,
#68804,#68805,#68806,#68807,#68808,#68809,#68810,#68811,#68812,#68813,#68814,
#68815,#68816,#68817,#68818,#68819,#68820,#68821,#68822,#68823,#68824,#68825,
#68826,#68827,#68828,#68829,#68830,#68831,#68832,#68833,#68834,#68835,#68836,
#68837,#68838,#68839,#68840,#68841,#68842,#68843,#68844,#68845,#68846,#68847,
#68848,#68849,#68850,#68851,#68852,#68853,#68854,#68855,#68856,#68857,#68858,
#68859,#68860,#68861,#68862,#68863,#68864,#68865,#68866,#68867,#68868,#68869,
#68870,#68871,#68872,#68873,#68874,#68875,#68876,#68877,#68878,#68879,#68880,
#68881,#68882,#68883,#68884,#68885,#68886,#68887,#68888,#68889,#68890,#68891,
#68892,#68893,#68894,#68895),.UNSPECIFIED.,.F.,.F.,(4,3,3,3,3,3,3,3,3,3,
3,3,3,3,3,3,3,3,3,3,3,3,3,3,3,3,3,3,3,3,3,3,3,3,3,3,3,3,3,3,3,3,3,3,3,3,
3,3,3,3,3,3,3,3,3,3,3,3,3,3,3,3,3,3,3,3,3,3,3,3,3,3,3,3,3,3,3,3,3,3,3,3,
3,3,3,3,3,4),(170.769651999993,170.841525264034,170.913339268465,170.985109276191,
171.059131815152,171.130872259162,171.202617263185,171.274380554809,171.346175885099,
171.418054342032,171.489982494379,171.562008735186,171.577289587882,171.652826221117,
171.728276979241,171.80365475444,171.878972391218,171.954242694441,172.031816353787,
172.107036048043,172.182249863931,172.257469348117,172.332706048281,172.407998578141,
172.483324313756,172.558720531494,172.574831969206,172.651430711188,172.727964401205,
172.804442717187,172.880866853705,172.957258260071,173.033625845381,173.073603159869,
173.151724309452,173.229890374643,173.308106089272,173.386412551037,173.464767207882,
173.543207142429,173.572374350531,173.654343152433,173.736240165645,173.819966509533,
173.901623383812,173.986384462503,174.071145541194,174.144772565293,174.218394338589,
174.292023843992,174.36570551181,174.439414444971,174.513205025037,174.569916731856,
174.646422038254,174.722871516419,174.799276065152,174.875646550934,174.951993815244,
175.028926977486,175.105273938351,175.181631204493,175.258008628461,175.335371249641,
175.411847821384,175.489653467282,175.567459113181,175.642152203854,175.716765486922,
175.79131134536,175.865791656376,175.940233734425,176.014650566224,176.066230303844,
176.146524313229,176.226962925813,176.311472567986,176.392247106257,176.473122583034,
176.554132621711,176.565001494506,176.641798271613,176.718494678783,176.795100070023,
176.871597528246,176.948031146194,177.024393963857,177.052837307172),
 .UNSPECIFIED.);
#3470=B_SPLINE_CURVE_WITH_KNOTS('',3,(#68897,#68898,#68899,#68900,#68901,
#68902,#68903,#68904,#68905,#68906,#68907,#68908,#68909),.UNSPECIFIED.,
 .F.,.F.,(4,1,1,1,1,1,1,1,1,1,4),(177.052840192605,177.562543875831,178.560086257156,
179.557628638481,180.056399829143,180.555171019806,181.053942210468,181.55271340113,
182.550255782455,183.049026973118,183.336022614352),.UNSPECIFIED.);
#3471=B_SPLINE_CURVE_WITH_KNOTS('',3,(#68911,#68912,#68913,#68914,#68915,
#68916,#68917,#68918,#68919,#68920,#68921,#68922,#68923,#68924,#68925,#68926,
#68927,#68928,#68929,#68930,#68931,#68932,#68933,#68934,#68935,#68936,#68937,
#68938,#68939,#68940,#68941,#68942,#68943,#68944,#68945,#68946,#68947,#68948,
#68949,#68950,#68951,#68952,#68953,#68954,#68955,#68956,#68957,#68958,#68959,
#68960,#68961,#68962,#68963,#68964,#68965,#68966,#68967,#68968,#68969,#68970,
#68971,#68972,#68973,#68974,#68975,#68976,#68977,#68978,#68979,#68980,#68981,
#68982,#68983,#68984,#68985,#68986,#68987,#68988,#68989,#68990,#68991,#68992,
#68993,#68994,#68995,#68996,#68997,#68998,#68999,#69000,#69001,#69002,#69003,
#69004,#69005,#69006,#69007,#69008,#69009,#69010,#69011,#69012,#69013,#69014,
#69015,#69016,#69017,#69018,#69019,#69020,#69021,#69022,#69023,#69024,#69025,
#69026,#69027,#69028,#69029,#69030,#69031,#69032,#69033,#69034,#69035,#69036,
#69037,#69038,#69039,#69040,#69041,#69042,#69043,#69044,#69045,#69046,#69047,
#69048,#69049,#69050,#69051,#69052,#69053,#69054,#69055,#69056,#69057,#69058,
#69059,#69060,#69061,#69062,#69063,#69064,#69065,#69066,#69067,#69068,#69069,
#69070,#69071,#69072,#69073,#69074,#69075,#69076,#69077,#69078,#69079,#69080,
#69081,#69082,#69083,#69084,#69085,#69086,#69087,#69088,#69089,#69090,#69091,
#69092,#69093,#69094,#69095,#69096,#69097,#69098,#69099,#69100,#69101,#69102,
#69103,#69104,#69105,#69106,#69107,#69108,#69109,#69110,#69111,#69112,#69113,
#69114,#69115,#69116,#69117,#69118,#69119,#69120,#69121,#69122,#69123,#69124,
#69125,#69126,#69127,#69128,#69129,#69130,#69131,#69132,#69133,#69134,#69135,
#69136,#69137,#69138,#69139,#69140,#69141,#69142,#69143,#69144,#69145,#69146,
#69147,#69148,#69149,#69150,#69151,#69152,#69153,#69154,#69155,#69156,#69157,
#69158,#69159,#69160,#69161,#69162,#69163,#69164,#69165,#69166,#69167,#69168,
#69169,#69170,#69171,#69172,#69173,#69174,#69175,#69176,#69177,#69178,#69179,
#69180,#69181,#69182,#69183,#69184,#69185,#69186,#69187,#69188,#69189,#69190,
#69191,#69192,#69193,#69194,#69195,#69196,#69197,#69198,#69199,#69200,#69201,
#69202,#69203,#69204,#69205,#69206,#69207,#69208,#69209,#69210,#69211,#69212,
#69213,#69214,#69215,#69216,#69217,#69218,#69219,#69220,#69221,#69222,#69223,
#69224,#69225,#69226,#69227,#69228,#69229,#69230,#69231,#69232,#69233,#69234,
#69235,#69236,#69237,#69238,#69239,#69240,#69241,#69242,#69243,#69244,#69245,
#69246,#69247,#69248,#69249,#69250,#69251,#69252,#69253,#69254,#69255,#69256,
#69257,#69258,#69259,#69260,#69261,#69262,#69263,#69264,#69265,#69266,#69267,
#69268,#69269,#69270,#69271,#69272,#69273,#69274,#69275,#69276,#69277,#69278,
#69279,#69280,#69281,#69282,#69283,#69284,#69285,#69286,#69287,#69288,#69289,
#69290,#69291,#69292,#69293,#69294,#69295,#69296,#69297,#69298,#69299,#69300,
#69301,#69302,#69303,#69304,#69305,#69306,#69307,#69308,#69309,#69310,#69311,
#69312,#69313,#69314,#69315,#69316,#69317,#69318,#69319,#69320,#69321,#69322,
#69323,#69324,#69325,#69326,#69327,#69328,#69329,#69330,#69331,#69332,#69333,
#69334,#69335,#69336,#69337,#69338,#69339,#69340,#69341,#69342,#69343,#69344,
#69345,#69346,#69347,#69348,#69349,#69350,#69351,#69352,#69353,#69354,#69355,
#69356,#69357,#69358,#69359,#69360,#69361,#69362,#69363,#69364,#69365,#69366,
#69367,#69368,#69369,#69370,#69371,#69372,#69373,#69374,#69375,#69376,#69377,
#69378,#69379,#69380,#69381,#69382,#69383,#69384,#69385,#69386,#69387,#69388,
#69389,#69390,#69391,#69392,#69393,#69394,#69395,#69396,#69397,#69398,#69399,
#69400,#69401,#69402,#69403,#69404,#69405,#69406,#69407,#69408,#69409,#69410,
#69411,#69412,#69413,#69414,#69415,#69416,#69417,#69418,#69419,#69420,#69421,
#69422,#69423,#69424,#69425,#69426,#69427,#69428,#69429,#69430,#69431,#69432,
#69433,#69434,#69435,#69436),.UNSPECIFIED.,.F.,.F.,(4,2,2,2,2,2,2,2,2,2,
2,2,2,2,2,2,2,2,2,2,2,2,2,2,2,2,2,2,2,2,2,2,2,2,2,2,2,2,2,2,2,2,2,2,2,2,
2,2,2,2,2,2,2,2,2,2,2,2,2,2,2,2,2,2,2,2,2,2,2,2,2,2,2,2,2,2,2,2,2,2,2,2,
2,2,2,2,2,2,2,2,2,2,2,2,2,2,2,2,2,2,2,2,2,2,2,2,2,2,2,2,2,2,2,2,2,2,2,2,
2,2,2,2,2,2,2,2,2,2,2,2,2,2,2,2,2,2,2,2,2,2,2,2,2,2,2,2,2,2,2,2,2,2,2,2,
2,2,2,2,2,2,2,2,2,2,2,2,2,2,2,2,2,2,2,2,2,2,2,2,2,2,2,2,2,2,2,2,2,2,2,2,
2,2,2,2,2,2,2,2,2,2,2,2,2,2,2,2,2,2,2,2,2,2,2,2,2,2,2,2,2,2,2,2,2,2,2,2,
2,2,2,2,2,2,2,2,2,2,2,2,2,2,2,2,2,2,2,2,2,2,2,2,2,2,2,2,2,2,2,2,2,2,2,2,
4),(0.0016813894720157,0.126276306325587,0.13171521603428,0.134813406577695,
0.136946061564364,0.139024362305826,0.140949491087562,0.143435306169637,
0.148776093342873,0.193897711692965,0.246102946707196,0.262390167713752,
0.285794126424522,0.320087296011645,0.390930867775347,0.485193343825969,
0.523841633721814,0.529356059979522,0.532163536424868,0.534199789165854,
0.536371278942309,0.540078880990494,0.55015100646069,0.703271582382227,
0.786515340473811,0.837834333923844,0.898749772576009,0.934487678758292,
0.951930512613121,0.954776619796794,0.956262337919711,0.957470845359138,
0.95885842686672,0.961231062647402,0.97012383177081,1.10932618782953,1.21324590937667,
1.22952058161868,1.28967045517663,1.32228293571319,1.35064336093572,1.3555840756948,
1.35820327475134,1.36014694378895,1.36256792176654,1.3666051285224,1.37982219166346,
1.57974775715462,1.68081352872921,1.72878753413955,1.74858909682943,1.75155845237035,
1.75311421988214,1.75438426268061,1.75565816326952,1.75798093028333,1.76529594289006,
1.88614788006614,2.04264049383793,2.12675154087064,2.1634520484143,2.16907819905463,
2.17198237838747,2.17410521645429,2.17638469223063,2.17964376928181,2.18861168275333,
2.32551285696637,2.40033690502228,2.55668586642739,2.56419023975228,2.57001760980649,
2.57284691400218,2.57505424225381,2.57715459668584,2.58069488373071,2.59008662487545,
2.59956634908852,2.77849466405771,2.97819699447958,2.99951156471404,3.01583034022543,
3.02398112487448,3.02987030007139,3.03704367692439,3.04871724978831,3.08630892509699,
3.29837489785931,3.32565291715049,3.33163007837961,3.33520984563063,3.338470970241,
3.34268134126249,3.34948834652552,3.38865188205523,3.4633678688153,3.57917791198519,
3.61165470575163,3.63566084974347,3.64613919301554,3.65392119967909,3.66120041674774,
3.67129379245727,3.69802893611616,3.89723498840701,4.00078157447208,4.06037241668731,
4.08622825317741,4.09072286391114,4.09310963705833,4.09488254910694,4.09709458467479,
4.10079186163325,4.11296881461358,4.37751463807427,4.49888786919302,4.50600147471296,
4.50926060213944,4.51171744566247,4.5140280226436,4.51722865218343,4.52368818499514,
4.58302392657759,4.78216342476303,4.91459760855396,4.91958658164072,4.92181566607141,
4.92347316137414,4.92501587927965,4.92712775282223,4.93131721565626,4.96700764764638,
4.9783119243875,5.03820072641067,5.14045933275398,5.2687654109915,5.28016785829196,
5.28479123282316,5.28865760875609,5.29263767700519,5.29848486017698,5.31403133582179,
5.38497045258501,5.48997559611325,5.64385776023696,5.66602124321873,5.66989689859193,
5.67223342344906,5.67403846093759,5.6759828719288,5.67905278079114,5.68879275401658,
5.8466369787072,5.98972677624834,6.06231919088305,6.06925759987435,6.07208077907739,
6.07416281593377,6.07641857225871,6.07948443059417,6.08648323198734,6.20155412509249,
6.3562060278163,6.44620500024421,6.45920845028298,6.48651817069122,6.48967901172627,
6.49126137817559,6.49242532117264,6.49368700087476,6.4954022498206,6.49931815638298,
6.59739814063084,6.66030634366478,6.73021428129816,6.87684417251856,6.88655021229513,
6.89020646477263,6.89237166783306,6.89441759817212,6.89726309859609,6.90294131270436,
6.94648917205556,7.01372562470065,7.14419844825498,7.25042281028484,7.27879888185834,
7.28247762272717,7.28420454223694,7.28555417995817,7.28702328333278,7.28937510291162,
7.29710255340587,7.40042222325123,7.56652690397069,7.60680990235306,7.64786719661048,
7.66709479081452,7.67202388171467,7.67485317424848,7.67701711106436,7.67980353641607,
7.68457647867163,7.70432611529756,7.73906828330887,7.82540200164722,7.91621938068956,
8.05378211301946,8.06210642614992,8.06462787814728,8.06598445504395,8.06730768978272,
8.06891519961576,8.07189971496406,8.08972346998265,8.11829715700733,8.21764864857086,
8.31646351631789,8.44515448611735,8.45324832920377,8.45629593936965,8.45846221265475,
8.46050759660477,8.46334985266736,8.46889945219032,8.50890533921324,8.5666422744989,
8.65315760038643,8.84314085372879,8.85448300920299,8.85691016024225,8.85846827826325,
8.85970739684579,8.86109950313883,8.86345756859054,8.87285251805831,8.94423938042643,
9.01678332376981,9.08549889170928,9.08899262232838,9.2019562060884,9.26563155247367,
9.27180455449668,9.274793389,9.27691903974772,9.27892693456711,9.2817184373797,
9.28728458515085,9.32972109297728,9.42295236817236,9.43920789903987,9.45082249532382,
9.48848413968528,9.66150548935551,9.67222315597415,9.67554106896341,9.67734051887701,
9.67910603031286,9.68126471039495,9.68530468990907,9.70776609406871,9.7564964949981,
9.95504525777298),.UNSPECIFIED.);
#3472=B_SPLINE_CURVE_WITH_KNOTS('',3,(#69438,#69439,#69440,#69441,#69442,
#69443,#69444,#69445,#69446,#69447,#69448,#69449,#69450,#69451,#69452,#69453,
#69454,#69455,#69456,#69457,#69458,#69459,#69460,#69461,#69462,#69463,#69464,
#69465,#69466,#69467,#69468,#69469,#69470,#69471,#69472,#69473,#69474,#69475,
#69476,#69477,#69478,#69479,#69480,#69481,#69482,#69483,#69484,#69485,#69486,
#69487,#69488,#69489,#69490,#69491,#69492,#69493,#69494,#69495,#69496,#69497,
#69498,#69499,#69500,#69501,#69502,#69503,#69504,#69505,#69506,#69507,#69508,
#69509,#69510,#69511,#69512,#69513,#69514,#69515,#69516,#69517,#69518,#69519,
#69520,#69521,#69522,#69523,#69524,#69525,#69526,#69527,#69528,#69529,#69530,
#69531,#69532,#69533,#69534,#69535,#69536,#69537,#69538,#69539,#69540,#69541,
#69542,#69543,#69544,#69545,#69546,#69547,#69548,#69549,#69550,#69551,#69552,
#69553,#69554,#69555,#69556,#69557,#69558,#69559,#69560,#69561,#69562,#69563,
#69564,#69565,#69566,#69567,#69568,#69569,#69570,#69571,#69572,#69573,#69574,
#69575,#69576,#69577,#69578,#69579,#69580,#69581,#69582,#69583,#69584,#69585,
#69586,#69587,#69588,#69589,#69590,#69591,#69592,#69593,#69594,#69595,#69596,
#69597,#69598,#69599,#69600,#69601,#69602,#69603,#69604,#69605,#69606,#69607,
#69608,#69609,#69610,#69611,#69612,#69613,#69614,#69615,#69616,#69617,#69618,
#69619,#69620,#69621,#69622,#69623,#69624,#69625,#69626,#69627,#69628,#69629,
#69630,#69631,#69632,#69633,#69634,#69635,#69636,#69637,#69638,#69639,#69640,
#69641,#69642,#69643,#69644,#69645,#69646,#69647,#69648,#69649,#69650,#69651,
#69652,#69653,#69654,#69655,#69656,#69657,#69658,#69659,#69660,#69661,#69662,
#69663,#69664,#69665,#69666,#69667,#69668,#69669,#69670,#69671,#69672,#69673,
#69674,#69675,#69676,#69677,#69678,#69679,#69680,#69681,#69682,#69683,#69684,
#69685,#69686,#69687,#69688,#69689,#69690,#69691,#69692,#69693,#69694,#69695,
#69696,#69697,#69698,#69699,#69700,#69701,#69702,#69703,#69704,#69705,#69706,
#69707,#69708,#69709,#69710,#69711,#69712,#69713,#69714,#69715,#69716,#69717,
#69718,#69719,#69720,#69721,#69722,#69723,#69724,#69725,#69726,#69727,#69728,
#69729,#69730,#69731,#69732,#69733,#69734,#69735,#69736,#69737,#69738,#69739,
#69740,#69741,#69742,#69743,#69744,#69745,#69746,#69747,#69748,#69749,#69750,
#69751,#69752,#69753,#69754,#69755,#69756,#69757,#69758,#69759,#69760,#69761,
#69762,#69763,#69764,#69765,#69766,#69767,#69768,#69769,#69770,#69771,#69772,
#69773,#69774,#69775,#69776,#69777,#69778,#69779,#69780,#69781,#69782,#69783,
#69784,#69785,#69786,#69787,#69788,#69789,#69790,#69791,#69792,#69793,#69794,
#69795,#69796,#69797,#69798,#69799,#69800,#69801,#69802,#69803,#69804,#69805,
#69806,#69807,#69808,#69809,#69810,#69811,#69812,#69813,#69814,#69815,#69816,
#69817,#69818,#69819,#69820,#69821,#69822,#69823,#69824,#69825,#69826,#69827,
#69828,#69829,#69830,#69831,#69832,#69833,#69834,#69835,#69836,#69837,#69838,
#69839,#69840,#69841,#69842,#69843,#69844,#69845,#69846,#69847,#69848,#69849,
#69850,#69851,#69852,#69853,#69854,#69855,#69856,#69857,#69858,#69859,#69860,
#69861,#69862,#69863,#69864,#69865,#69866,#69867,#69868,#69869,#69870,#69871,
#69872,#69873,#69874,#69875,#69876,#69877,#69878,#69879,#69880,#69881,#69882,
#69883,#69884,#69885,#69886,#69887,#69888,#69889,#69890,#69891,#69892,#69893,
#69894,#69895,#69896,#69897,#69898,#69899,#69900,#69901,#69902,#69903,#69904,
#69905,#69906,#69907,#69908,#69909,#69910,#69911,#69912,#69913,#69914,#69915,
#69916,#69917,#69918,#69919,#69920,#69921,#69922,#69923,#69924,#69925,#69926,
#69927),.UNSPECIFIED.,.F.,.F.,(4,2,2,2,2,2,2,2,2,2,2,2,2,2,2,2,2,2,2,2,
2,2,2,2,2,2,2,2,2,2,2,2,2,2,2,2,2,2,2,2,2,2,2,2,2,2,2,2,2,2,2,2,2,2,2,2,
2,2,2,2,2,2,2,2,2,2,2,2,2,2,2,2,2,2,2,2,2,2,2,2,2,2,2,2,2,2,2,2,2,2,2,2,
2,2,2,2,2,2,2,2,2,2,2,2,2,2,2,2,2,2,2,2,2,2,2,2,2,2,2,2,2,2,2,2,2,2,2,2,
2,2,2,2,2,2,2,2,2,2,2,2,2,2,2,2,2,2,2,2,2,2,2,2,2,2,2,2,2,2,2,2,2,2,2,2,
2,2,2,2,2,2,2,2,2,2,2,2,2,2,2,2,2,2,2,2,2,2,2,2,2,2,2,2,2,2,2,2,2,2,2,2,
2,2,2,2,2,2,2,2,2,2,2,2,2,2,2,2,2,2,2,2,2,2,2,2,2,2,2,2,2,2,2,2,2,2,2,2,
2,2,2,2,2,2,2,2,4),(0.0021147162426415,0.0857262217385641,0.0959123132725421,
0.101817668638507,0.105952423517762,0.109510120672382,0.113321414548935,
0.118219462115226,0.128355303510646,0.198457205571982,0.218864102215348,
0.255164213476987,0.455011656366761,0.470031775693596,0.473395464028391,
0.475296187041642,0.476760751229038,0.478410875300978,0.481474133588517,
0.491622758632171,0.662151770789466,0.714975847791071,0.773859001783566,
0.875910873483415,0.882889809062308,0.886123944905947,0.888577389939866,
0.890896201465588,0.894126531781061,0.902525128685859,1.02961162784532,
1.0945067501913,1.20524360683114,1.28553165208685,1.29817116256545,1.30176031498023,
1.30394827115179,1.30592352168945,1.30844611491447,1.31245710765836,1.33283936785151,
1.5691885282616,1.65665791247992,1.72040189980086,1.73512615034882,1.74364682219264,
1.75085877779597,1.75999003059328,1.77694684805219,1.90332017671288,2.03590229083718,
2.04753685223959,2.05606067100292,2.06030458264268,2.06358258447306,2.06667617038536,
2.07101759104478,2.08401702036005,2.18618316659222,2.32731586969064,2.34510604146755,
2.35534739163738,2.36247298112973,2.36928828667622,2.37569464315755,2.38417294501723,
2.39834975895669,2.49607255557145,2.53627412163732,2.70121754018261,2.80311492162715,
2.81229754901474,2.81906637785889,2.82206919057242,2.82429470788258,2.82636000871468,
2.82917824160068,2.83620048021959,2.94636996472043,3.10348583461963,3.21225025704563,
3.21976968678328,3.22303925051097,3.22543566974893,3.22764106093274,3.23062175623667,
3.23789980232397,3.31153014271453,3.3524873607049,3.52832814665662,3.58743433757029,
3.62228162836511,3.63933743746729,3.64227148225394,3.6438209823814,3.64496800991523,
3.64621354827629,3.64801746784966,3.65325286924985,3.74074304237537,3.893129084531,
3.9780306526427,4.01210247075576,4.03111539136288,4.03550078693162,4.03799930145634,
4.03993449712372,4.04245722562997,4.04683288981786,4.06366584341291,4.09538118112343,
4.32176810585032,4.38195140900454,4.43025672223563,4.43776984183809,4.43992504461529,
4.4412527775106,4.44247207562142,4.44403165486226,4.44732324429486,4.46909558516888,
4.51865677483036,4.54506074473599,4.72669198960786,4.78424848556279,4.84701286593956,
4.85853798828355,4.86231304553642,4.86474074815425,4.86702033528734,4.87000798487978,
4.87660151829323,4.92973260715549,4.98045002030486,5.10221443593992,5.24427235548077,
5.25286462314312,5.25648552926838,5.25863738208686,5.26035379641356,5.26265348515541,
5.26694779951379,5.29064318860111,5.3424512558368,5.55487224215899,5.62040553019814,
5.63162385262355,5.63701008483504,5.64117602700476,5.64574583987469,5.6531591034371,
5.67880068867541,5.90227415500722,5.99698321796197,6.0025684084701,6.00475682972833,
6.00634141745119,6.00803078653048,6.01028025482486,6.01522362882187,6.11870399110965,
6.39560652566407,6.41148141879393,6.41615544755748,6.41891814931392,6.42111387769637,
6.42404436306647,6.42948172166862,6.45859474640228,6.51585878091743,6.59837308969972,
6.81737700530157,6.82999182706921,6.83375169501524,6.83598457633156,6.83794438819199,
6.84041241834021,6.84526053629908,6.87981678440402,6.98139824630425,7.14044784617825,
7.19958194660694,7.25317064917875,7.26762837768704,7.27635186016815,7.28424439102001,
7.29442715688286,7.31598237815389,7.39889254138972,7.50522005637645,7.57889164068016,
7.58744346266093,7.59170194898351,7.5950092039627,7.59864875319175,7.60471078440443,
7.63283569665676,7.84915699449695,7.8820564085455,7.8931604814945,7.89950316613594,
7.90537568559607,7.91339087638862,7.92902912279261,8.05170023959194,8.24358712398681,
8.32079868164036,8.34071194170864,8.34982230593964,8.35325066704535,8.35554262923877,
8.35777152310636,8.36077827902947,8.36755214703489,8.52719912658739,8.60332595975835,
8.74182593331619,8.75088262286138,8.75415517434681,8.75643829392326,8.75855997761165,
8.76145559654793,8.7670412572037,8.80270679867144,8.88309602807962,9.01392933675127,
9.08038255757393,9.16777949685675,9.17296213874511,9.17493819556321,9.17626191955968,
9.17752614030541,9.17925754118248,9.18314414459356,9.27023665215949,9.47933248011572,
9.55880443390468,9.56576996403643,9.56855572667082,9.57059288847095,9.572783554419,
9.57573197884494,9.58234014556836,9.69690744402141,9.95834822127454),
 .UNSPECIFIED.);
#3473=B_SPLINE_CURVE_WITH_KNOTS('',3,(#69929,#69930,#69931,#69932,#69933,
#69934,#69935,#69936,#69937,#69938,#69939,#69940,#69941,#69942,#69943,#69944),
 .UNSPECIFIED.,.F.,.F.,(4,3,1,1,1,1,1,1,1,1,1,4),(208.46876384307,208.486357696903,
209.483900078227,209.98267126889,210.481442459552,211.478984840877,211.97775603154,
212.476527222202,212.975298412865,213.474069603527,214.471611984852,214.75194915025),
 .UNSPECIFIED.);
#3474=B_SPLINE_CURVE_WITH_KNOTS('',3,(#69946,#69947,#69948,#69949,#69950,
#69951,#69952,#69953,#69954,#69955,#69956,#69957,#69958,#69959,#69960,#69961,
#69962,#69963),.UNSPECIFIED.,.F.,.F.,(4,2,2,2,2,2,2,2,4),(214.75194915025,
215.586866062145,216.42178297404,217.256699885934,218.091616797829,218.926533709724,
219.761450621619,220.596367533514,221.035134457429),.UNSPECIFIED.);
#3475=B_SPLINE_CURVE_WITH_KNOTS('',3,(#69965,#69966,#69967,#69968,#69969,
#69970,#69971,#69972,#69973,#69974,#69975,#69976,#69977,#69978,#69979,#69980,
#69981,#69982,#69983,#69984,#69985,#69986,#69987,#69988,#69989,#69990,#69991,
#69992,#69993,#69994,#69995,#69996,#69997,#69998,#69999,#70000,#70001,#70002,
#70003,#70004,#70005,#70006,#70007,#70008,#70009,#70010,#70011,#70012,#70013,
#70014,#70015,#70016,#70017,#70018,#70019,#70020,#70021,#70022,#70023,#70024,
#70025,#70026,#70027,#70028,#70029,#70030,#70031,#70032,#70033,#70034,#70035,
#70036,#70037,#70038,#70039,#70040,#70041,#70042,#70043,#70044,#70045,#70046,
#70047,#70048,#70049,#70050,#70051,#70052,#70053,#70054,#70055,#70056,#70057,
#70058,#70059,#70060,#70061,#70062,#70063,#70064,#70065,#70066,#70067,#70068,
#70069,#70070,#70071,#70072,#70073,#70074,#70075,#70076,#70077,#70078,#70079,
#70080,#70081,#70082,#70083,#70084,#70085,#70086,#70087,#70088,#70089,#70090,
#70091,#70092,#70093,#70094,#70095,#70096,#70097,#70098,#70099,#70100,#70101,
#70102,#70103,#70104,#70105,#70106,#70107,#70108,#70109,#70110,#70111,#70112,
#70113,#70114,#70115,#70116,#70117,#70118,#70119,#70120,#70121,#70122,#70123,
#70124,#70125,#70126,#70127,#70128,#70129,#70130,#70131,#70132,#70133,#70134,
#70135,#70136,#70137,#70138,#70139,#70140,#70141,#70142,#70143,#70144,#70145,
#70146,#70147,#70148,#70149,#70150,#70151,#70152,#70153,#70154,#70155,#70156,
#70157,#70158,#70159,#70160,#70161,#70162,#70163,#70164,#70165,#70166,#70167,
#70168,#70169,#70170,#70171,#70172,#70173,#70174,#70175,#70176,#70177,#70178,
#70179,#70180,#70181,#70182,#70183,#70184,#70185,#70186,#70187,#70188,#70189,
#70190,#70191,#70192,#70193,#70194,#70195,#70196,#70197,#70198,#70199,#70200,
#70201,#70202,#70203,#70204,#70205,#70206,#70207,#70208,#70209,#70210,#70211,
#70212,#70213,#70214,#70215,#70216,#70217,#70218,#70219,#70220,#70221,#70222,
#70223,#70224,#70225,#70226,#70227,#70228,#70229,#70230,#70231,#70232,#70233,
#70234,#70235,#70236,#70237,#70238,#70239,#70240,#70241,#70242,#70243,#70244,
#70245,#70246,#70247,#70248,#70249,#70250,#70251,#70252,#70253,#70254,#70255,
#70256,#70257,#70258,#70259,#70260,#70261,#70262,#70263,#70264,#70265,#70266,
#70267,#70268,#70269,#70270,#70271,#70272,#70273,#70274,#70275,#70276,#70277,
#70278,#70279,#70280,#70281,#70282,#70283,#70284,#70285,#70286,#70287,#70288,
#70289,#70290,#70291,#70292,#70293,#70294,#70295,#70296,#70297,#70298,#70299,
#70300,#70301,#70302,#70303,#70304,#70305,#70306,#70307,#70308,#70309,#70310,
#70311,#70312,#70313,#70314,#70315,#70316,#70317,#70318,#70319,#70320,#70321,
#70322,#70323,#70324,#70325,#70326,#70327,#70328,#70329,#70330,#70331,#70332,
#70333,#70334,#70335,#70336,#70337,#70338,#70339,#70340,#70341,#70342,#70343,
#70344,#70345,#70346,#70347,#70348,#70349,#70350,#70351,#70352,#70353,#70354,
#70355,#70356,#70357,#70358,#70359,#70360,#70361,#70362,#70363,#70364,#70365,
#70366,#70367,#70368,#70369,#70370,#70371,#70372,#70373,#70374,#70375,#70376,
#70377,#70378,#70379,#70380,#70381,#70382,#70383,#70384,#70385,#70386,#70387,
#70388,#70389,#70390,#70391,#70392,#70393,#70394,#70395,#70396,#70397,#70398,
#70399,#70400,#70401,#70402,#70403,#70404,#70405,#70406,#70407,#70408,#70409,
#70410,#70411,#70412,#70413,#70414,#70415,#70416,#70417,#70418,#70419,#70420,
#70421,#70422,#70423,#70424,#70425,#70426,#70427,#70428,#70429,#70430,#70431,
#70432,#70433,#70434,#70435,#70436,#70437,#70438,#70439,#70440,#70441,#70442,
#70443,#70444,#70445,#70446,#70447,#70448,#70449,#70450,#70451,#70452,#70453,
#70454,#70455,#70456,#70457,#70458,#70459,#70460,#70461,#70462,#70463,#70464,
#70465,#70466,#70467,#70468,#70469,#70470,#70471,#70472,#70473,#70474,#70475,
#70476),.UNSPECIFIED.,.F.,.F.,(4,2,2,2,2,2,2,2,2,2,2,2,2,2,2,2,2,2,2,2,
2,2,2,2,2,2,2,2,2,2,2,2,2,2,2,2,2,2,2,2,2,2,2,2,2,2,2,2,2,2,2,2,2,2,2,2,
2,2,2,2,2,2,2,2,2,2,2,2,2,2,2,2,2,2,2,2,2,2,2,2,2,2,2,2,2,2,2,2,2,2,2,2,
2,2,2,2,2,2,2,2,2,2,2,2,2,2,2,2,2,2,2,2,2,2,2,2,2,2,2,2,2,2,2,2,2,2,2,2,
2,2,2,2,2,2,2,2,2,2,2,2,2,2,2,2,2,2,2,2,2,2,2,2,2,2,2,2,2,2,2,2,2,2,2,2,
2,2,2,2,2,2,2,2,2,2,2,2,2,2,2,2,2,2,2,2,2,2,2,2,2,2,2,2,2,2,2,2,2,2,2,2,
2,2,2,2,2,2,2,2,2,2,2,2,2,2,2,2,2,2,2,2,2,2,2,2,2,2,2,2,2,2,2,2,2,2,2,2,
2,2,2,2,2,2,2,2,2,2,2,2,2,2,2,2,2,2,2,4),(0.001951533452596,0.265717321319917,
0.317341835588869,0.325376765827814,0.3276862666474,0.329098702429905,0.330376332518678,
0.332010874754853,0.335372120405849,0.358662092625752,0.468281733597388,
0.513763873343083,0.625751409145384,0.678173822325819,0.702169775743808,
0.711754552531524,0.716600773823633,0.71957768741308,0.722301751833663,
0.724427670951214,0.72651042615492,0.730068199531644,0.739742890751326,
0.86679288798981,0.932468076113923,1.06479302989476,1.1148141875318,1.12248808645428,
1.12465969487064,1.12599099474889,1.12720932880081,1.12878788765383,1.13208996362533,
1.15408845654518,1.40067870042842,1.48692095471947,1.52224758592459,1.53520376879134,
1.54415054073146,1.54762243776647,1.54972395080898,1.55199708911254,1.55494587748327,
1.56133228351188,1.60872715456636,1.77046056621364,1.92378574489667,1.93791121758729,
1.94156891021233,1.94372919789255,1.94563596959493,1.94801293825857,1.95167978020016,
1.96833939088765,2.20193778182021,2.29453324672734,2.31356028958412,2.32031261628281,
2.32473663289401,2.32888166679184,2.33373674581061,2.34439136981965,2.41822995509492,
2.61366578679574,2.66276485204052,2.68492429917379,2.68875207706807,2.69077878143689,
2.69244247480863,2.69411840443413,2.69719857924694,2.707096048162,2.86954481235853,
3.00695456765383,3.06509469256782,3.09462892661599,3.10008845123357,3.10302369330253,
3.10521984983143,3.10797896116196,3.11263695265344,3.12837172638961,3.39000425700505,
3.44961594014936,3.50526871698629,3.51563632510471,3.51898307737978,3.52112388466973,
3.52312639600432,3.52574069798841,3.53012854201908,3.55677322438013,3.56187419452147,
3.72388371425758,3.81789483571181,3.92905919796076,3.94875337225157,3.95855780456448,
3.96566268896484,3.97436915348954,3.98871242628505,4.03720416782415,4.20204883044425,
4.26493151031742,4.2729496446515,4.27704190884932,4.28001777630835,4.28365558147312,
4.28970695684892,4.31328579112865,4.33275778340722,4.39638497584167,4.47694045371521,
4.55326950616606,4.57237571540609,4.5810670358198,4.58764122971028,4.59386618453668,
4.60259885639249,4.62618463315842,4.86646835244077,4.9802976591868,5.03008595353589,
5.03621390297851,5.03911228356299,5.0413318367125,5.0437043405124,5.04741303121301,
5.05890604606681,5.21514715136939,5.29002839264698,5.42699189963121,5.4359622488642,
5.43922173549449,5.44150134993598,5.44362420134704,5.44652822038162,5.45215344948398,
5.4888278860254,5.57283460630526,5.66635969382606,5.70968686148662,5.76190687894718,
5.85249190898214,5.85790764595199,5.85996149324299,5.86118160575228,5.86233677909754,
5.86394674216659,5.86718354382573,5.89751972062914,5.9537159215645,6.14691719609207,
6.22524993965214,6.24723500148468,6.25162210435026,6.25438569981103,6.25654944593365,
6.25894548235369,6.26287313209285,6.27665186113409,6.3624633135438,6.52541776152828,
6.59335055712837,6.65118777322531,6.65531443229296,6.65690161242639,6.65804871462973,
6.65927607772336,6.66091672090075,6.66454590252395,6.73263988988279,6.90637352692446,
7.06513602481122,7.07535705906912,7.07908685011856,7.08126242001413,7.08329678031912,
7.08609274200448,7.09155331373573,7.12867475289864,7.22220798761413,7.36833388769845,
7.46380067968375,7.47093998728375,7.47356285250664,7.47540687358606,7.47713128231082,
7.47950171757497,7.48413211656161,7.51535882400722,7.59744225875962,7.68971340294352,
7.74131872925907,7.83500813165633,7.84610484627746,7.85159682793949,7.85554550976842,
7.85973585256492,7.86518099353552,7.87685990441749,7.89214738329876,8.11574406924228,
8.21324159148531,8.21883332103305,8.22102267943941,8.22260738279229,8.22429635074362,
8.22654438819321,8.23148101705829,8.23791374389157,8.25343561837247,8.31302842062166,
8.41634128144384,8.61536988972848,8.62804401933215,8.63231778230145,8.63472345864302,
8.63691981004058,8.63985893388704,8.64533726327819,8.67524077685549,8.73408589683472,
8.77386514206112,8.84503634559689,8.90114113979982,9.03541020197952,9.04595398625163,
9.04945487878885,9.05141149103592,9.05338834388455,9.05584819133908,9.06065792786725,
9.09346093759942,9.18355932857806,9.25345509573954,9.36880202776115,9.45790793168817,
9.47860278410875,9.48859631016876,9.49646600978707,9.5037870682281,9.51239369813437,
9.5377496250476,9.608828896354,9.67154750433572,9.69699547766963,9.79426533363515,
9.80272985902464,9.80696967029066,9.81027419058992,9.81333205485562,9.81687702618506,
9.82198829068213,9.84212776085011,9.95551597770185),.UNSPECIFIED.);
#3476=B_SPLINE_CURVE_WITH_KNOTS('',3,(#70478,#70479,#70480,#70481,#70482,
#70483,#70484,#70485,#70486,#70487,#70488,#70489),.UNSPECIFIED.,.F.,.F.,
(4,1,1,1,1,1,1,1,1,4),(233.601505071788,233.923688420687,234.42245961135,
235.420001992675,236.417544374,237.415086755324,237.913857945987,238.412629136649,
239.410171517974,239.884387681578),.UNSPECIFIED.);
#3477=B_SPLINE_CURVE_WITH_KNOTS('',3,(#70491,#70492,#70493,#70494,#70495,
#70496,#70497,#70498,#70499,#70500,#70501,#70502,#70503,#70504,#70505,#70506,
#70507,#70508,#70509,#70510,#70511,#70512,#70513,#70514,#70515,#70516,#70517,
#70518,#70519,#70520,#70521,#70522,#70523,#70524,#70525,#70526,#70527,#70528,
#70529,#70530,#70531,#70532,#70533,#70534,#70535,#70536,#70537,#70538,#70539,
#70540,#70541,#70542,#70543,#70544,#70545,#70546,#70547,#70548,#70549,#70550,
#70551,#70552,#70553,#70554,#70555,#70556,#70557,#70558,#70559,#70560,#70561,
#70562,#70563,#70564,#70565,#70566,#70567,#70568,#70569,#70570,#70571,#70572,
#70573,#70574,#70575,#70576,#70577,#70578,#70579,#70580,#70581,#70582,#70583,
#70584,#70585,#70586,#70587,#70588,#70589,#70590,#70591,#70592,#70593,#70594,
#70595,#70596,#70597,#70598,#70599,#70600,#70601,#70602,#70603,#70604,#70605,
#70606,#70607,#70608,#70609,#70610,#70611,#70612,#70613,#70614,#70615,#70616,
#70617,#70618,#70619,#70620,#70621,#70622,#70623,#70624,#70625,#70626,#70627,
#70628,#70629,#70630,#70631,#70632,#70633,#70634,#70635,#70636,#70637,#70638,
#70639,#70640,#70641,#70642,#70643,#70644,#70645,#70646,#70647,#70648,#70649,
#70650,#70651,#70652,#70653,#70654,#70655,#70656,#70657,#70658,#70659,#70660,
#70661,#70662,#70663,#70664,#70665,#70666,#70667,#70668,#70669,#70670,#70671,
#70672,#70673,#70674,#70675,#70676,#70677,#70678,#70679,#70680,#70681,#70682,
#70683,#70684,#70685,#70686,#70687,#70688,#70689,#70690,#70691,#70692,#70693,
#70694,#70695,#70696,#70697,#70698,#70699,#70700,#70701,#70702,#70703,#70704,
#70705,#70706,#70707,#70708,#70709,#70710,#70711,#70712,#70713,#70714,#70715,
#70716,#70717,#70718,#70719,#70720,#70721,#70722,#70723,#70724,#70725,#70726,
#70727,#70728,#70729,#70730,#70731,#70732,#70733,#70734,#70735,#70736,#70737,
#70738,#70739,#70740,#70741,#70742,#70743,#70744,#70745,#70746,#70747,#70748,
#70749,#70750,#70751,#70752,#70753,#70754,#70755,#70756,#70757,#70758,#70759,
#70760,#70761,#70762,#70763,#70764,#70765,#70766,#70767,#70768,#70769,#70770,
#70771,#70772,#70773,#70774,#70775,#70776,#70777,#70778,#70779,#70780,#70781,
#70782,#70783,#70784,#70785,#70786,#70787,#70788,#70789,#70790,#70791,#70792,
#70793,#70794,#70795,#70796,#70797,#70798,#70799,#70800,#70801,#70802,#70803,
#70804,#70805,#70806,#70807,#70808,#70809,#70810,#70811,#70812,#70813,#70814,
#70815,#70816,#70817,#70818,#70819,#70820,#70821,#70822,#70823,#70824,#70825,
#70826,#70827,#70828,#70829,#70830,#70831,#70832,#70833,#70834,#70835,#70836,
#70837,#70838,#70839,#70840,#70841,#70842,#70843,#70844,#70845,#70846,#70847,
#70848,#70849,#70850,#70851,#70852,#70853,#70854,#70855,#70856,#70857,#70858,
#70859,#70860,#70861,#70862,#70863,#70864,#70865,#70866,#70867,#70868,#70869,
#70870,#70871,#70872,#70873,#70874,#70875,#70876,#70877,#70878,#70879,#70880,
#70881,#70882,#70883,#70884,#70885,#70886,#70887,#70888,#70889,#70890,#70891,
#70892,#70893,#70894,#70895,#70896,#70897,#70898,#70899,#70900,#70901,#70902,
#70903,#70904,#70905,#70906,#70907,#70908,#70909,#70910,#70911,#70912,#70913,
#70914,#70915,#70916,#70917,#70918,#70919,#70920,#70921,#70922,#70923,#70924,
#70925,#70926,#70927,#70928,#70929,#70930,#70931,#70932,#70933,#70934,#70935,
#70936,#70937,#70938,#70939,#70940,#70941,#70942,#70943,#70944,#70945,#70946,
#70947,#70948,#70949,#70950,#70951,#70952,#70953,#70954,#70955,#70956,#70957,
#70958,#70959,#70960,#70961,#70962,#70963,#70964,#70965,#70966,#70967,#70968,
#70969,#70970,#70971,#70972,#70973,#70974,#70975,#70976,#70977,#70978,#70979,
#70980,#70981,#70982,#70983,#70984,#70985,#70986,#70987,#70988,#70989,#70990,
#70991,#70992,#70993,#70994,#70995,#70996,#70997,#70998,#70999,#71000,#71001,
#71002,#71003,#71004,#71005,#71006,#71007,#71008,#71009,#71010,#71011,#71012,
#71013,#71014,#71015,#71016,#71017,#71018,#71019,#71020),.UNSPECIFIED.,
 .F.,.F.,(4,2,2,2,2,2,2,2,2,2,2,2,2,2,2,2,2,2,2,2,2,2,2,2,2,2,2,2,2,2,2,
2,2,2,2,2,2,2,2,2,2,2,2,2,2,2,2,2,2,2,2,2,2,2,2,2,2,2,2,2,2,2,2,2,2,2,2,
2,2,2,2,2,2,2,2,2,2,2,2,2,2,2,2,2,2,2,2,2,2,2,2,2,2,2,2,2,2,2,2,2,2,2,2,
2,2,2,2,2,2,2,2,2,2,2,2,2,2,2,2,2,2,2,2,2,2,2,2,2,2,2,2,2,2,2,2,2,2,2,2,
2,2,2,2,2,2,2,2,2,2,2,2,2,2,2,2,2,2,2,2,2,2,2,2,2,2,2,2,2,2,2,2,2,2,2,2,
2,2,2,2,2,2,2,2,2,2,2,2,2,2,2,2,2,2,2,2,2,2,2,2,2,2,2,2,2,2,2,2,2,2,2,2,
2,2,2,2,2,2,2,2,2,2,2,2,2,2,2,2,2,2,2,2,2,2,2,2,2,2,2,2,2,2,2,2,2,2,2,2,
2,2,2,2,2,2,2,2,2,2,2,2,2,2,2,2,2,4),(0.00168357070064361,0.043274643150003,
0.0685334213659095,0.0790143023288335,0.0868883847257787,0.0944095737450267,
0.101794669849645,0.111844750673594,0.137179843959166,0.187514130969224,
0.348804161845356,0.395630614416885,0.401053194682952,0.40476130467354,
0.407874528067813,0.410826942683271,0.414759726605491,0.422149101631073,
0.473392987687212,0.599416728122072,0.659951264051369,0.684273679179953,
0.70264868932782,0.711167356501013,0.71736127507081,0.723515572225275,0.733619732738534,
0.759806628156653,1.00552198108395,1.11994345884837,1.1614787140408,1.16694204752024,
1.16969627850224,1.1716832892601,1.17379299161084,1.17737463862252,1.18698109954257,
1.33744860748507,1.43810358227347,1.55707301404325,1.56638839060558,1.56995495490699,
1.57240962086844,1.57481237876229,1.57770526665601,1.58491466487181,1.65048588343432,
1.76165733730261,1.91767263470405,1.96617116888262,1.98654282058554,1.98961633476199,
1.99119548508848,1.99245584574268,1.9938982926654,1.99634151682156,2.00509666039586,
2.14264997082273,2.23057096430205,2.32100147617026,2.37068103478181,2.37721333124266,
2.38241336843127,2.38508732538944,2.38703755530943,2.38912752643311,2.39210847017446,
2.4002663549463,2.52979483294095,2.68438994542906,2.74044181455745,2.77885985730339,
2.78538427343791,2.78743033279388,2.78873513635092,2.78996287069773,2.79157541648948,
2.79501400647715,2.82140638814894,2.82751990163162,2.83660450070032,2.95132069539436,
3.09341302873435,3.20116883242843,3.20774986988387,3.21076815783328,3.21304461862589,
3.21518639661658,3.21815446026977,3.22414855576671,3.27924054223989,3.33239290271546,
3.4968045191568,3.58737237586432,3.60050340732827,3.60407006443767,3.60621030717788,
3.6081206209944,3.61053039058114,3.61430227953695,3.63234109374042,3.84101922941899,
3.95384819270381,3.97526619925623,3.98236072417324,3.98686041628649,3.99105030173818,
3.99650091327692,4.00842509728725,4.12389661021933,4.261496858014,4.337810877864,
4.34869478025052,4.3517550751624,4.35361346850431,4.35528628656936,4.35741553140064,
4.3617373398443,4.39204436367251,4.64932441583501,4.75392478935123,4.76165115962004,
4.76503283428499,4.76752005624028,4.76981515934972,4.77292650576448,4.78057040761326,
4.86136463807988,4.98004174955559,5.16637169849527,5.17766385897107,5.18126343289091,
5.18324027520222,5.1852149745882,5.18763867139315,5.19227328777566,5.22094577653925,
5.28986735475889,5.45380212274526,5.50673042731537,5.59144336014785,5.61097632404609,
5.62087719515763,5.62873961860188,5.63763025679442,5.65282088438884,5.71976501883445,
5.84884556444085,5.92631971252463,5.93489428125943,5.93915785682697,5.94246613149657,
5.94610384682777,5.95215469550854,5.9800910435969,6.19580005924466,6.22937383641455,
6.24056460513399,6.24692477810978,6.25279384330619,6.26077430473703,6.27623871959087,
6.39512736434397,6.58371822501153,6.64730144268971,6.69278254782892,6.69885602671975,
6.70170066128268,6.70391174563339,6.70630770680104,6.71012212382932,6.72251131492311,
6.88945756757099,7.08501760065372,7.09748773553116,7.10163853312632,7.10396184639994,
7.1060750799815,7.10889132043101,7.11410353876239,7.1417033118507,7.19542408957702,
7.29841788700904,7.45353450326594,7.51654393343234,7.52098954510073,7.52269013153598,
7.52390737952985,7.52506365398733,7.52663701096129,7.52954974089529,7.53336257806554,
7.68846427894584,7.76416277075836,7.90316101507657,7.91248538292321,7.91598820482693,
7.91805971104074,7.92001519078334,7.92273178028472,7.92814120193399,7.96902508966463,
8.07295424057414,8.21097632125331,8.3106574593564,8.31717035203294,8.31929913182466,
8.32048872185174,8.32157872486837,8.32304297502124,8.32573374116278,8.34001488629136,
8.36888139613217,8.42697714040849,8.48700246648982,8.57220064211512,8.72784692789641,
8.73790840655419,8.74161403909164,8.74378491614204,8.74582094258979,8.74862865194153,
8.75414546465156,8.79288417693994,8.88749002208078,8.93480333594175,8.95079901121166,
8.96468383112629,8.97690411286408,8.98778701709875,9.09277672768747,9.10323636555463,
9.12278109258072,9.13251740174098,9.13583582760789,9.13771132707051,9.13959166752094,
9.14192552192337,9.14641871298226,9.15215657573219,9.16490875767532,9.20349591930505,
9.26140221976965,9.3785123105631,9.49672382518336,9.50962581335401,9.5147745998946,
9.51902209129393,9.52334155339519,9.52959537643696,9.54592576675249,9.62206746974412,
9.80168187512738,9.81350051881362,9.855726000521,9.86261140856199,9.87880304855279,
9.88213450575607,9.88425196908999,9.88592334351232,9.88748078326666,9.88930186190153,
9.89190202184739,9.89635244352137,9.95673900561715),.UNSPECIFIED.);
#3478=B_SPLINE_CURVE_WITH_KNOTS('',3,(#71022,#71023,#71024,#71025,#71026,
#71027,#71028,#71029,#71030,#71031,#71032,#71033,#71034,#71035,#71036,#71037,
#71038,#71039,#71040,#71041,#71042,#71043,#71044,#71045,#71046,#71047,#71048,
#71049,#71050,#71051,#71052,#71053,#71054,#71055,#71056,#71057,#71058,#71059,
#71060,#71061,#71062,#71063,#71064,#71065,#71066,#71067,#71068,#71069,#71070,
#71071,#71072,#71073,#71074,#71075,#71076,#71077,#71078,#71079,#71080,#71081,
#71082,#71083,#71084,#71085,#71086,#71087,#71088,#71089,#71090,#71091,#71092,
#71093,#71094,#71095,#71096,#71097,#71098,#71099,#71100,#71101,#71102,#71103,
#71104,#71105,#71106,#71107,#71108,#71109,#71110,#71111,#71112,#71113,#71114,
#71115,#71116,#71117,#71118,#71119,#71120,#71121,#71122,#71123,#71124,#71125,
#71126,#71127,#71128,#71129,#71130,#71131,#71132,#71133,#71134,#71135,#71136,
#71137,#71138,#71139,#71140,#71141,#71142,#71143,#71144,#71145,#71146,#71147,
#71148,#71149,#71150,#71151,#71152,#71153,#71154,#71155,#71156,#71157,#71158,
#71159,#71160,#71161,#71162,#71163,#71164,#71165,#71166,#71167,#71168,#71169,
#71170,#71171,#71172,#71173,#71174,#71175,#71176,#71177,#71178,#71179,#71180,
#71181,#71182,#71183,#71184,#71185,#71186,#71187,#71188,#71189,#71190,#71191,
#71192,#71193,#71194,#71195,#71196,#71197,#71198,#71199,#71200,#71201,#71202,
#71203,#71204,#71205,#71206,#71207,#71208,#71209,#71210,#71211,#71212,#71213,
#71214,#71215,#71216,#71217,#71218,#71219,#71220,#71221,#71222,#71223,#71224,
#71225,#71226,#71227,#71228,#71229,#71230,#71231,#71232,#71233,#71234,#71235,
#71236,#71237,#71238,#71239,#71240,#71241,#71242,#71243,#71244,#71245,#71246,
#71247,#71248,#71249,#71250,#71251,#71252,#71253,#71254,#71255,#71256,#71257,
#71258,#71259,#71260,#71261,#71262,#71263,#71264,#71265,#71266,#71267,#71268,
#71269,#71270,#71271,#71272,#71273,#71274,#71275,#71276,#71277,#71278,#71279,
#71280,#71281,#71282,#71283,#71284,#71285,#71286,#71287,#71288,#71289,#71290,
#71291,#71292,#71293,#71294,#71295,#71296,#71297,#71298,#71299,#71300,#71301,
#71302,#71303,#71304,#71305,#71306,#71307,#71308,#71309,#71310,#71311,#71312,
#71313,#71314,#71315,#71316,#71317,#71318,#71319,#71320,#71321,#71322,#71323,
#71324,#71325,#71326,#71327,#71328,#71329,#71330,#71331,#71332,#71333,#71334,
#71335,#71336,#71337,#71338,#71339,#71340,#71341,#71342,#71343,#71344,#71345,
#71346,#71347,#71348,#71349,#71350,#71351,#71352,#71353,#71354,#71355,#71356,
#71357,#71358,#71359,#71360,#71361,#71362,#71363,#71364,#71365,#71366,#71367,
#71368,#71369,#71370,#71371,#71372,#71373,#71374,#71375,#71376,#71377,#71378,
#71379,#71380,#71381,#71382,#71383,#71384,#71385,#71386,#71387,#71388,#71389,
#71390,#71391,#71392,#71393,#71394,#71395,#71396,#71397,#71398,#71399,#71400,
#71401,#71402,#71403,#71404,#71405,#71406,#71407,#71408,#71409,#71410,#71411,
#71412,#71413,#71414,#71415,#71416,#71417,#71418,#71419,#71420,#71421,#71422,
#71423,#71424,#71425,#71426,#71427,#71428,#71429,#71430,#71431,#71432,#71433,
#71434,#71435,#71436,#71437,#71438,#71439,#71440,#71441,#71442,#71443,#71444,
#71445,#71446,#71447,#71448,#71449,#71450,#71451,#71452,#71453,#71454,#71455,
#71456,#71457,#71458,#71459,#71460,#71461,#71462,#71463,#71464,#71465,#71466,
#71467,#71468,#71469,#71470,#71471,#71472,#71473,#71474,#71475,#71476,#71477,
#71478,#71479,#71480,#71481,#71482,#71483,#71484,#71485,#71486,#71487,#71488,
#71489,#71490,#71491,#71492,#71493,#71494,#71495,#71496,#71497,#71498,#71499,
#71500,#71501,#71502,#71503,#71504,#71505,#71506,#71507,#71508,#71509,#71510,
#71511,#71512,#71513,#71514,#71515,#71516,#71517,#71518,#71519,#71520,#71521,
#71522,#71523,#71524,#71525),.UNSPECIFIED.,.F.,.F.,(4,2,2,2,2,2,2,2,2,2,
2,2,2,2,2,2,2,2,2,2,2,2,2,2,2,2,2,2,2,2,2,2,2,2,2,2,2,2,2,2,2,2,2,2,2,2,
2,2,2,2,2,2,2,2,2,2,2,2,2,2,2,2,2,2,2,2,2,2,2,2,2,2,2,2,2,2,2,2,2,2,2,2,
2,2,2,2,2,2,2,2,2,2,2,2,2,2,2,2,2,2,2,2,2,2,2,2,2,2,2,2,2,2,2,2,2,2,2,2,
2,2,2,2,2,2,2,2,2,2,2,2,2,2,2,2,2,2,2,2,2,2,2,2,2,2,2,2,2,2,2,2,2,2,2,2,
2,2,2,2,2,2,2,2,2,2,2,2,2,2,2,2,2,2,2,2,2,2,2,2,2,2,2,2,2,2,2,2,2,2,2,2,
2,2,2,2,2,2,2,2,2,2,2,2,2,2,2,2,2,2,2,2,2,2,2,2,2,2,2,2,2,2,2,2,2,2,2,2,
2,2,2,2,2,2,2,2,2,2,2,2,2,2,2,2,2,2,2,2,2,2,2,2,2,4),(0.00251010222491945,
0.243787391938942,0.303585856625084,0.334265125341356,0.339783302168653,
0.342731196990903,0.344928651576325,0.347678715786094,0.3522958866643,0.367677234091077,
0.665375547270404,0.719529836939747,0.753106403301528,0.757805985350203,
0.760250090460091,0.76217375969946,0.764103766158577,0.76746238785199,0.776997208265284,
0.821072968260817,0.827425971333189,0.993027291007421,1.09349735049628,
1.16892839688559,1.1888067752484,1.19864822603004,1.20575936414824,1.21336448320816,
1.22653290570935,1.2649723820318,1.42001696008981,1.47913703997041,1.50759999993778,
1.5141869737241,1.51797399058619,1.52101238571232,1.52481872651664,1.5318846130407,
1.57414022287303,1.70078210174418,1.76721092418276,1.79310006757511,1.81253704887497,
1.82128950858579,1.82787420813396,1.8340828171777,1.84274982024407,1.86581413092087,
2.05981437474254,2.14034417212541,2.26694614174772,2.27276444203969,2.27742084528508,
2.27988431817427,2.28202981459984,2.28421901795791,2.28819874845734,2.30064121003661,
2.54839057286477,2.66730110349389,2.67668283694365,2.68025928556359,2.68271579951296,
2.68511649989536,2.68800225265757,2.69516952013211,2.75933417950786,2.88413027690822,
2.99667146727563,3.09510287243425,3.09927062972646,3.10105921414451,3.10236081307502,
3.10355184308957,3.10515108928364,3.10904212056815,3.15223125590808,3.36090907023271,
3.45193753704296,3.48750015054709,3.49273659358103,3.49541773321685,3.4973685061179,
3.49945461486889,3.50303073822689,3.51282882315481,3.66019078512744,3.74152808340484,
3.88874758038838,3.89558483034534,3.89766658668889,3.8989786908732,3.90020300531344,
3.90179632911577,3.90514044211941,3.92912546097264,4.00784067621214,4.21752717165338,
4.2823982203165,4.31359471287522,4.31882072478056,4.3215676574711,4.32359623307228,
4.32579446509543,4.32897150358384,4.33793103731674,4.47446455387964,4.54935502043155,
4.70042907417598,4.7111671047788,4.71448236650469,4.71656580958623,4.71848878622497,
4.72096259656022,4.72503398324502,4.74764638332562,4.86333868376048,4.98068554299978,
5.07608863377555,5.08723110589535,5.09273514103766,5.09668712426034,5.10087604412859,
5.10642261388538,5.11854635663474,5.27017147221037,5.43419298400449,5.4365305035406,
5.45685573816647,5.4604520103869,5.46262621580172,5.46430952145124,5.46612643741112,
5.46900275353824,5.47819225007716,5.53407272110727,5.60032482683932,5.65840683785703,
5.85671900096459,5.86912187188425,5.8733587166141,5.87575701510525,5.87795477467401,
5.88090786164873,5.88645125552013,5.91764970183465,5.97721099953278,6.15247583005955,
6.1946485071903,6.28093150267365,6.28816864312843,6.2908622399433,6.29276755757812,
6.29455863897503,6.29703568431977,6.30192831496201,6.3379244699221,6.4493918238998,
6.68995834198289,6.71660076234272,6.72682798178216,6.73425510724238,6.7422474801572,
6.75310850774865,6.77849032336773,6.81317417511326,6.91167960312419,7.02881368071915,
7.04204919188353,7.04670177144201,7.04991790532169,7.05288858733531,7.05691898099624,
7.06512729949014,7.07610674974359,7.20439964912853,7.330927269013,7.34601481188863,
7.35391560012106,7.36042224379344,7.36779311781667,7.38037858621192,7.43635714613673,
7.61417255428127,7.77095324968326,7.80275128373853,7.80771547691403,7.81064176492888,
7.81286564864252,7.8152263839659,7.81888312459723,7.8299603614273,7.88694314649619,
7.92111440052267,7.94682652387992,8.15137793326954,8.202012073061,8.20871835137869,
8.2118039707384,8.21417809096293,8.21667465695087,8.22054175137566,8.22505071786973,
8.23346362786466,8.25301875274464,8.30911523315822,8.38817373028602,8.53488096606999,
8.60600104584896,8.62697798083178,8.63034524485487,8.63198361762719,8.6332610889448,
8.63467014239525,8.63696687632437,8.64528009632667,8.70207682131942,8.77152871803475,
8.7920770617834,8.88521330564611,9.01157424389431,9.02096127464029,9.02447339770842,
9.02654638867801,9.02863016613432,9.03135243079927,9.03685380321987,9.04392303384984,
9.05987136615499,9.10697552250956,9.16472826375648,9.29460673284835,9.38594217404497,
9.42282230595951,9.42658272608822,9.42806498559548,9.42929890458283,9.43056714537261,
9.43242347950637,9.43734521202508,9.53928660437817,9.74725342253797,9.75959851262685,
9.84016579236699,9.84738741128452,9.85028499635874,9.8524073356124,9.85455428594291,
9.85677670138773,9.8596816472686,9.86426249311313,9.95742286907103),
 .UNSPECIFIED.);
#3479=B_SPLINE_CURVE_WITH_KNOTS('',3,(#71527,#71528,#71529,#71530,#71531,
#71532,#71533,#71534,#71535,#71536,#71537,#71538,#71539,#71540,#71541,#71542,
#71543,#71544,#71545,#71546,#71547,#71548,#71549,#71550,#71551,#71552,#71553,
#71554,#71555,#71556,#71557,#71558,#71559,#71560,#71561,#71562,#71563,#71564,
#71565,#71566,#71567,#71568,#71569,#71570,#71571,#71572,#71573,#71574,#71575,
#71576,#71577,#71578,#71579,#71580,#71581,#71582,#71583,#71584,#71585,#71586,
#71587,#71588,#71589,#71590,#71591,#71592,#71593,#71594,#71595,#71596,#71597,
#71598,#71599,#71600,#71601,#71602,#71603,#71604,#71605,#71606,#71607,#71608,
#71609,#71610,#71611,#71612,#71613,#71614,#71615,#71616,#71617,#71618,#71619,
#71620,#71621,#71622,#71623,#71624,#71625,#71626,#71627,#71628,#71629,#71630,
#71631,#71632,#71633,#71634,#71635,#71636,#71637,#71638,#71639,#71640,#71641,
#71642,#71643,#71644,#71645,#71646,#71647,#71648,#71649,#71650,#71651,#71652,
#71653,#71654,#71655,#71656,#71657,#71658,#71659,#71660,#71661,#71662,#71663,
#71664,#71665,#71666,#71667,#71668,#71669,#71670,#71671,#71672,#71673,#71674,
#71675,#71676,#71677,#71678,#71679,#71680,#71681,#71682,#71683,#71684,#71685,
#71686,#71687,#71688,#71689,#71690,#71691,#71692,#71693,#71694,#71695,#71696,
#71697,#71698,#71699,#71700,#71701,#71702,#71703,#71704,#71705,#71706,#71707,
#71708,#71709,#71710,#71711,#71712,#71713,#71714,#71715,#71716,#71717,#71718,
#71719,#71720,#71721,#71722,#71723,#71724,#71725,#71726,#71727,#71728,#71729,
#71730,#71731,#71732,#71733,#71734,#71735,#71736,#71737,#71738,#71739,#71740,
#71741,#71742,#71743,#71744,#71745,#71746,#71747,#71748,#71749,#71750,#71751,
#71752,#71753,#71754,#71755,#71756,#71757,#71758,#71759,#71760,#71761,#71762,
#71763,#71764,#71765,#71766,#71767,#71768,#71769,#71770,#71771,#71772,#71773,
#71774,#71775,#71776,#71777,#71778,#71779,#71780,#71781,#71782,#71783,#71784,
#71785,#71786,#71787,#71788,#71789,#71790,#71791,#71792,#71793,#71794,#71795,
#71796,#71797,#71798,#71799,#71800,#71801,#71802,#71803,#71804,#71805,#71806,
#71807,#71808,#71809,#71810,#71811,#71812,#71813,#71814,#71815,#71816,#71817,
#71818,#71819,#71820,#71821,#71822,#71823,#71824,#71825,#71826,#71827,#71828,
#71829,#71830,#71831,#71832,#71833,#71834,#71835,#71836,#71837,#71838,#71839,
#71840,#71841,#71842,#71843,#71844,#71845,#71846,#71847,#71848,#71849,#71850,
#71851,#71852,#71853,#71854,#71855,#71856,#71857,#71858,#71859,#71860,#71861,
#71862,#71863,#71864,#71865,#71866,#71867,#71868,#71869,#71870,#71871,#71872,
#71873,#71874,#71875,#71876,#71877,#71878,#71879,#71880,#71881,#71882,#71883,
#71884,#71885,#71886,#71887,#71888,#71889,#71890,#71891,#71892,#71893,#71894,
#71895,#71896,#71897,#71898,#71899,#71900,#71901,#71902,#71903,#71904,#71905,
#71906,#71907,#71908,#71909,#71910,#71911,#71912,#71913,#71914,#71915,#71916,
#71917,#71918,#71919,#71920,#71921,#71922,#71923,#71924,#71925,#71926,#71927,
#71928,#71929,#71930,#71931,#71932,#71933,#71934,#71935,#71936,#71937,#71938,
#71939,#71940,#71941,#71942,#71943,#71944,#71945,#71946,#71947,#71948,#71949,
#71950,#71951,#71952,#71953,#71954,#71955,#71956,#71957,#71958,#71959,#71960,
#71961,#71962,#71963,#71964,#71965,#71966,#71967,#71968,#71969,#71970,#71971,
#71972,#71973,#71974,#71975,#71976,#71977,#71978,#71979,#71980,#71981,#71982,
#71983,#71984,#71985,#71986,#71987,#71988,#71989,#71990,#71991,#71992,#71993,
#71994,#71995,#71996,#71997,#71998,#71999,#72000,#72001,#72002,#72003,#72004,
#72005,#72006,#72007,#72008,#72009,#72010,#72011,#72012,#72013,#72014,#72015,
#72016,#72017,#72018,#72019,#72020,#72021,#72022,#72023,#72024,#72025,#72026,
#72027,#72028,#72029,#72030,#72031,#72032,#72033,#72034,#72035,#72036,#72037,
#72038,#72039,#72040,#72041,#72042,#72043,#72044,#72045,#72046,#72047,#72048,
#72049,#72050,#72051,#72052,#72053,#72054,#72055,#72056),.UNSPECIFIED.,
 .F.,.F.,(4,2,2,2,2,2,2,2,2,2,2,2,2,2,2,2,2,2,2,2,2,2,2,2,2,2,2,2,2,2,2,
2,2,2,2,2,2,2,2,2,2,2,2,2,2,2,2,2,2,2,2,2,2,2,2,2,2,2,2,2,2,2,2,2,2,2,2,
2,2,2,2,2,2,2,2,2,2,2,2,2,2,2,2,2,2,2,2,2,2,2,2,2,2,2,2,2,2,2,2,2,2,2,2,
2,2,2,2,2,2,2,2,2,2,2,2,2,2,2,2,2,2,2,2,2,2,2,2,2,2,2,2,2,2,2,2,2,2,2,2,
2,2,2,2,2,2,2,2,2,2,2,2,2,2,2,2,2,2,2,2,2,2,2,2,2,2,2,2,2,2,2,2,2,2,2,2,
2,2,2,2,2,2,2,2,2,2,2,2,2,2,2,2,2,2,2,2,2,2,2,2,2,2,2,2,2,2,2,2,2,2,2,2,
2,2,2,2,2,2,2,2,2,2,2,2,2,2,2,2,2,2,2,2,2,2,2,2,2,2,2,2,2,2,2,2,2,2,2,2,
2,2,2,2,2,2,2,2,2,2,2,2,2,2,2,2,2,4),(0.00309469634645156,0.224719887751486,
0.262433627837547,0.285214875920883,0.289466113176118,0.291757187350233,
0.293474235860959,0.295359849641409,0.298722341888027,0.308803625459528,
0.549626391594619,0.642918507831922,0.662033156729555,0.668799520237496,
0.673227324591152,0.67735443317442,0.682852864260989,0.694580657859646,
0.812759013597112,1.01883049575864,1.03426833278783,1.03771171899465,1.0396554936354,
1.04115232103902,1.04309216526864,1.04642720178532,1.0592142306045,1.28282484245239,
1.35265975418497,1.41249861493508,1.43278181691983,1.44150342361149,1.44817114029072,
1.45134673197699,1.45381104455684,1.45614459990585,1.4594026790858,1.46605918984373,
1.53151068475513,1.66512180306669,1.76645673300713,1.85877163432735,1.86537200414604,
1.86817197563305,1.87019871776286,1.87204727014748,1.87452132427924,1.88082548367989,
1.98034717375737,2.10112255881258,2.27221666046685,2.29546951003967,2.30592719309536,
2.31385709756275,2.32219156103465,2.33522503618132,2.37459332398833,2.5286672647815,
2.61108190335055,2.62064894285417,2.62504537978011,2.62837252159074,2.63151223062196,
2.63590168280702,2.64900532091202,2.78209897772558,2.90815257233216,2.92330003024977,
2.93122200645702,2.93708820872066,2.94421158040537,2.9558308356711,2.99638804728661,
3.11090925815809,3.27623062293508,3.37678768202605,3.38416999129581,3.38728417606207,
3.38953251963091,3.3915778656314,3.39430741218754,3.40095041360982,3.46486382262876,
3.68947080484061,3.74907612239742,3.78107720553494,3.78650640920955,3.78936881130532,
3.79171218456978,3.79441929102231,3.79901266879074,3.81564653179389,4.11578768838679,
4.1637054322703,4.20058417583274,4.20711678014725,4.2092549857036,4.21062907802626,
4.21191845006874,4.2136066843205,4.21735441760319,4.25182846441527,4.49704387422664,
4.56526773305332,4.59653605460805,4.60160542766454,4.60425137813528,4.60640387838646,
4.60855647492885,4.61246543439191,4.62465802407176,4.811918192958,4.93023847044749,
4.98209070115221,5.00243293872193,5.00561094204973,5.007149990671,5.00836273374973,
5.00971628922986,5.01195907799621,5.02005971781845,5.07391517684984,5.13239006679914,
5.35824453427294,5.41978632594383,5.42666026502501,5.42942482998162,5.43172342319774,
5.43407408342837,5.43749381958586,5.44644882676684,5.56309423210432,5.78056665645007,
5.81695700212397,5.82208040794227,5.82452443071683,5.8264434546441,5.82854181405301,
5.83192278327131,5.843248492938,5.91829036322231,6.05515733954,6.18411661874727,
6.19587202496579,6.2015348668477,6.20552982875455,6.20970067724296,6.21511829421865,
6.22655730815366,6.40117302670314,6.52695079547495,6.53299776476238,6.56501597657014,
6.56959898718664,6.57175640007582,6.57343740542144,6.57526257129168,6.57817498867056,
6.58767707680309,6.64701878425076,6.82690648528476,6.9697968914167,6.97925218850127,
6.98265892355394,6.98503275984224,6.98723645608052,6.99024055115944,6.99602375843549,
7.03261853306109,7.11511872343908,7.26404271985294,7.3889518932205,7.39704502058058,
7.40018454020166,7.40206974185838,7.40406969127019,7.40671417659079,7.41245584296766,
7.52905549586341,7.61604258409039,7.79764505975827,7.82524305582067,7.83560981363484,
7.84307294750416,7.85026364059302,7.86029388583745,7.87127442237592,7.88940235554483,
8.01638831306692,8.13822056002897,8.15122007998795,8.15583773937631,8.15904445601183,
8.16201788539676,8.16515289989451,8.17150897411593,8.20866382550621,8.30871545843223,
8.44012717552391,8.45391861469426,8.46230348423881,8.46869222771516,8.46872718864108,
8.46876105285513,8.46879384137152,8.4688255952888,8.46885635440215,8.46888615175129,
8.46890916974447,8.46893201552123,8.468954689056,8.46897719200031,8.46899952597806,
8.46902169262842,8.46904369352656,8.46906553025354,8.46908720432959,8.46910871734257,
8.4691300708164,8.46915126624619,8.46917230513227,8.46919318894168,8.46921391910887,
8.46923449708225,8.46925492429996,8.47621949401905,8.48770710851714,8.50159772175201,
8.52958141995862,8.61050599383194,8.71797921403125,8.89001164282994,8.89591080933983,
8.90534597246996,8.91536689607916,8.91900733887831,8.92113024104654,8.92311505307131,
8.92584282379479,8.93117600392541,8.96899290060652,9.01363917538949,9.07123810151026,
9.12804824249409,9.30504596556728,9.31609810353664,9.32004985896535,9.32233348697841,
9.32445534686691,9.32735075169056,9.33293444719636,9.36853840224448,9.46500284625107,
9.4967972322281,9.52913341068263,9.71290888733782,9.73640839333331,9.73989425423439,
9.74153865014484,9.742821111323,9.74421446735353,9.74643924439886,9.75400969021246,
9.80253514951666,9.95802914947034),.UNSPECIFIED.);
#3480=B_SPLINE_CURVE_WITH_KNOTS('',3,(#72058,#72059,#72060,#72061,#72062,
#72063,#72064,#72065,#72066,#72067,#72068,#72069,#72070,#72071,#72072,#72073,
#72074,#72075),.UNSPECIFIED.,.F.,.F.,(4,2,2,2,2,2,2,2,4),(277.583802222045,
278.41871913394,279.253636045835,280.08855295773,280.923469869625,281.75838678152,
282.593303693415,283.42822060531,283.866987529225),.UNSPECIFIED.);
#3481=B_SPLINE_CURVE_WITH_KNOTS('',3,(#72077,#72078,#72079,#72080,#72081,
#72082,#72083,#72084,#72085,#72086,#72087,#72088,#72089,#72090,#72091,#72092,
#72093,#72094,#72095,#72096,#72097,#72098,#72099,#72100,#72101,#72102,#72103,
#72104,#72105,#72106,#72107,#72108,#72109,#72110,#72111,#72112,#72113,#72114,
#72115,#72116,#72117,#72118,#72119,#72120,#72121,#72122,#72123,#72124,#72125,
#72126,#72127,#72128,#72129,#72130,#72131,#72132,#72133,#72134,#72135,#72136,
#72137,#72138,#72139,#72140,#72141,#72142,#72143,#72144,#72145,#72146,#72147,
#72148,#72149,#72150,#72151,#72152,#72153,#72154,#72155,#72156,#72157,#72158,
#72159,#72160,#72161,#72162,#72163,#72164,#72165,#72166,#72167,#72168,#72169,
#72170,#72171,#72172,#72173,#72174,#72175,#72176,#72177,#72178,#72179,#72180,
#72181,#72182,#72183,#72184,#72185,#72186,#72187,#72188,#72189,#72190,#72191,
#72192,#72193,#72194,#72195,#72196,#72197,#72198,#72199,#72200,#72201,#72202,
#72203,#72204,#72205,#72206,#72207,#72208,#72209,#72210,#72211,#72212,#72213,
#72214,#72215,#72216,#72217,#72218,#72219,#72220,#72221,#72222,#72223,#72224,
#72225,#72226,#72227,#72228,#72229,#72230,#72231,#72232,#72233,#72234,#72235,
#72236,#72237,#72238,#72239,#72240,#72241,#72242,#72243,#72244,#72245,#72246,
#72247,#72248,#72249,#72250,#72251,#72252,#72253,#72254,#72255,#72256,#72257,
#72258,#72259,#72260,#72261,#72262,#72263,#72264,#72265,#72266,#72267,#72268,
#72269,#72270,#72271,#72272,#72273,#72274,#72275,#72276,#72277,#72278,#72279,
#72280,#72281,#72282,#72283,#72284,#72285,#72286,#72287,#72288,#72289,#72290,
#72291,#72292,#72293,#72294,#72295,#72296,#72297,#72298,#72299,#72300,#72301,
#72302,#72303,#72304,#72305,#72306,#72307,#72308,#72309,#72310,#72311,#72312,
#72313,#72314,#72315,#72316,#72317,#72318,#72319,#72320,#72321,#72322,#72323,
#72324,#72325,#72326,#72327,#72328,#72329,#72330,#72331,#72332,#72333,#72334,
#72335,#72336,#72337,#72338,#72339,#72340,#72341,#72342,#72343,#72344,#72345,
#72346,#72347,#72348,#72349,#72350,#72351,#72352,#72353,#72354,#72355,#72356,
#72357,#72358,#72359,#72360,#72361,#72362,#72363,#72364,#72365,#72366,#72367,
#72368,#72369,#72370,#72371,#72372,#72373,#72374,#72375,#72376,#72377,#72378,
#72379,#72380,#72381,#72382,#72383,#72384,#72385,#72386,#72387,#72388,#72389,
#72390,#72391,#72392,#72393,#72394,#72395,#72396,#72397,#72398,#72399,#72400,
#72401,#72402,#72403,#72404,#72405,#72406,#72407,#72408,#72409,#72410,#72411,
#72412,#72413,#72414,#72415,#72416,#72417,#72418,#72419,#72420,#72421,#72422,
#72423,#72424,#72425,#72426,#72427,#72428,#72429,#72430,#72431,#72432,#72433,
#72434,#72435,#72436,#72437,#72438,#72439,#72440,#72441,#72442,#72443,#72444,
#72445,#72446,#72447,#72448,#72449,#72450,#72451,#72452,#72453,#72454,#72455,
#72456,#72457,#72458,#72459,#72460,#72461,#72462,#72463,#72464,#72465,#72466,
#72467,#72468,#72469,#72470,#72471,#72472,#72473,#72474,#72475,#72476,#72477,
#72478,#72479,#72480,#72481,#72482,#72483,#72484,#72485,#72486,#72487,#72488,
#72489,#72490,#72491,#72492,#72493,#72494,#72495,#72496,#72497,#72498,#72499,
#72500,#72501,#72502,#72503,#72504,#72505,#72506,#72507,#72508,#72509,#72510,
#72511,#72512,#72513,#72514,#72515,#72516,#72517,#72518,#72519,#72520,#72521,
#72522,#72523,#72524,#72525,#72526,#72527,#72528,#72529,#72530,#72531,#72532,
#72533,#72534,#72535,#72536,#72537,#72538,#72539,#72540,#72541,#72542,#72543,
#72544,#72545,#72546,#72547,#72548,#72549,#72550,#72551,#72552,#72553,#72554,
#72555,#72556,#72557,#72558,#72559,#72560,#72561,#72562,#72563,#72564,#72565,
#72566,#72567,#72568,#72569,#72570,#72571,#72572,#72573,#72574,#72575,#72576,
#72577,#72578,#72579,#72580,#72581,#72582,#72583,#72584,#72585,#72586,#72587,
#72588,#72589,#72590,#72591,#72592,#72593,#72594,#72595,#72596,#72597,#72598,
#72599,#72600,#72601,#72602),.UNSPECIFIED.,.F.,.F.,(4,2,2,2,2,2,2,2,2,2,
2,2,2,2,2,2,2,2,2,2,2,2,2,2,2,2,2,2,2,2,2,2,2,2,2,2,2,2,2,2,2,2,2,2,2,2,
2,2,2,2,2,2,2,2,2,2,2,2,2,2,2,2,2,2,2,2,2,2,2,2,2,2,2,2,2,2,2,2,2,2,2,2,
2,2,2,2,2,2,2,2,2,2,2,2,2,2,2,2,2,2,2,2,2,2,2,2,2,2,2,2,2,2,2,2,2,2,2,2,
2,2,2,2,2,2,2,2,2,2,2,2,2,2,2,2,2,2,2,2,2,2,2,2,2,2,2,2,2,2,2,2,2,2,2,2,
2,2,2,2,2,2,2,2,2,2,2,2,2,2,2,2,2,2,2,2,2,2,2,2,2,2,2,2,2,2,2,2,2,2,2,2,
2,2,2,2,2,2,2,2,2,2,2,2,2,2,2,2,2,2,2,2,2,2,2,2,2,2,2,2,2,2,2,2,2,2,2,2,
2,2,2,2,2,2,2,2,2,2,2,2,2,2,2,2,2,2,2,2,2,2,2,2,2,2,2,2,2,2,2,2,2,2,2,2,
4),(0.00198225243763518,0.266615072056633,0.314441300500113,0.334641517799556,
0.337708435595375,0.339286156902143,0.34043680491537,0.341669770816142,
0.343427590865343,0.348341092477681,0.430473500897858,0.483897354527935,
0.60921972497755,0.712024641181708,0.722038038549978,0.727042778428079,
0.730085961804466,0.732856084557811,0.734989039660594,0.737054349361429,
0.739944730530766,0.747532377017718,0.862309904946988,0.924634325421874,
1.03559976262637,1.13064497942464,1.13430874801485,1.13593891570679,1.13716391827038,
1.13831649649319,1.13991360821256,1.14313898836948,1.17228018560106,1.21761096157214,
1.4459763678948,1.5183423097778,1.54000712921983,1.54899459573558,1.5536716600765,
1.55758630132628,1.56004427966134,1.56229971101897,1.56516709850484,1.56969331072979,
1.59192903224698,1.75936817351546,1.87253162650479,1.92331778826061,1.94727193321419,
1.95158208883212,1.9538857748097,1.95578821732426,1.95800480438475,1.96181298087984,
1.97613406469955,2.12485827810235,2.23372919887249,2.30804055964423,2.32472192340326,
2.33110904665255,2.33545633208363,2.33965478370078,2.34470846983821,2.3564289454588,
2.47462750722216,2.680710954984,2.69615950032377,2.69960385795793,2.70154795524276,
2.70304492550759,2.70473051940944,2.70785668537208,2.71814549595555,2.87832043608914,
3.0144889970319,3.07435018640052,3.10522771842819,3.11075707410745,3.11370794239236,
3.11590631965682,3.11865585281012,3.12326811748487,3.13859965815366,3.3976220229261,
3.45822810659263,3.51584845164515,3.52643624975621,3.52981042887143,3.53195783349664,
3.53395884418568,3.53656025493411,3.54090255764027,3.56664961729996,3.77085053262592,
3.93525659107231,3.95824445959824,3.96865763316827,3.97658295715926,3.98413755300539,
3.9970411790911,4.03365134483239,4.04020249684436,4.13416726246233,4.24056174647398,
4.26004278481672,4.27339291106414,4.2831935789027,4.28763405210317,4.29096872969093,
4.29409671977725,4.29843686622211,4.31102664746692,4.43651056067615,4.57075285843747,
4.58598576323042,4.59392662578966,4.59979612478252,4.60618422209085,4.61749963670284,
4.65262195319419,4.86021660274821,4.98116045187684,5.04111614054903,5.04757498980902,
5.05049251097247,5.05271575208749,5.05508160058148,5.05875810647169,5.06998444302561,
5.22674932224136,5.30159467473023,5.43852673742968,5.44749505364594,5.45075479126959,
5.45303488796546,5.45515843067035,5.45806376850237,5.4636928368299,5.50043471317159,
5.58466896581577,5.67639352389981,5.7188608708688,5.7698112880867,5.82148422408315,
5.82742769798544,5.86621604705074,5.8702289973981,5.87181440906204,5.87300224097223,
5.87430740876504,5.87611457455958,5.88044499963987,5.9769466772595,6.16188931190439,
6.20406072287318,6.25658624508628,6.26233272291347,6.26517834142509,6.26723170262753,
6.26941409851677,6.27230741377316,6.27861468613636,6.3813668760207,6.54084947979132,
6.61003418774181,6.62354643585024,6.63384254405937,6.66400913015447,6.66757269096298,
6.66916728573966,6.67039116971523,6.67170539942978,6.67377107641829,6.68024182919464,
6.71759161580657,6.7722359060442,6.92261475698076,7.07730472686564,7.08736225664695,
7.09106793264123,7.09323924909741,7.09527595478646,7.09808501897963,7.10360597228759,
7.14243030451987,7.23734819603142,7.38358283627325,7.47567261873065,7.48297160925171,
7.48561972276589,7.4874711020023,7.489194170405,7.49155007210844,7.49601658005833,
7.5238281934931,7.58604186629975,7.83506009462097,7.85611928487344,7.86344239835313,
7.8675385485098,7.87126845106183,7.87615153375793,7.88506898416066,7.89607581049333,
7.97269604367384,8.11205672686641,8.17961394039693,8.21188191530798,8.21793454416393,
8.2295247890045,8.23276036223944,8.23467649113636,8.23634112964606,8.23838203712901,
8.24227615455492,8.24708830857299,8.2574063793657,8.28836137685172,8.32992307416076,
8.42689301207743,8.62756784135761,8.64049819772866,8.64480723530506,8.64722034940708,
8.64941605330347,8.65234340316962,8.65776510825396,8.68657565691866,8.74316135186546,
8.78404525961025,8.86783976403443,8.91949911711619,9.04951659666925,9.05889847716958,
9.06223723304688,9.0641616489134,9.0659473004337,9.06838078613387,9.07306261287258,
9.10239780555826,9.17284454773263,9.24973913035732,9.36264035722129,9.38650447145289,
9.4718304670089,9.49149272889614,9.50141955536032,9.50928400021423,9.51661192825482,
9.52526030213393,9.55106232405648,9.62837413482203,9.69183076576367,9.79954507771061,
9.81309704146065,9.81831218670084,9.82144892687799,9.82458699357909,9.82779203661205,
9.83193125727591,9.83870063406499,9.85258264854099,9.95778309923622),
 .UNSPECIFIED.);
#3482=B_SPLINE_CURVE_WITH_KNOTS('',3,(#72604,#72605,#72606,#72607,#72608,
#72609,#72610,#72611,#72612,#72613,#72614,#72615),.UNSPECIFIED.,.F.,.F.,
(4,1,1,1,1,1,1,1,1,4),(296.433358143584,296.768858444156,297.267629634818,
298.265172016143,299.262714397468,300.260256778793,300.759027969455,301.257799160118,
302.255341541442,302.716255299813),.UNSPECIFIED.);
#3483=B_SPLINE_CURVE_WITH_KNOTS('',3,(#72617,#72618,#72619,#72620,#72621,
#72622,#72623,#72624,#72625,#72626,#72627,#72628,#72629,#72630,#72631,#72632,
#72633,#72634,#72635,#72636,#72637,#72638,#72639,#72640,#72641,#72642,#72643,
#72644,#72645,#72646,#72647,#72648,#72649,#72650,#72651,#72652,#72653,#72654,
#72655,#72656,#72657,#72658,#72659,#72660,#72661,#72662,#72663,#72664,#72665,
#72666,#72667,#72668,#72669,#72670,#72671,#72672,#72673,#72674,#72675,#72676,
#72677,#72678,#72679,#72680,#72681,#72682,#72683,#72684,#72685,#72686,#72687,
#72688,#72689,#72690,#72691,#72692,#72693,#72694,#72695,#72696,#72697,#72698,
#72699,#72700,#72701,#72702,#72703,#72704,#72705,#72706,#72707,#72708,#72709,
#72710,#72711,#72712,#72713,#72714,#72715,#72716,#72717,#72718,#72719,#72720,
#72721,#72722,#72723,#72724,#72725,#72726,#72727,#72728,#72729,#72730,#72731,
#72732,#72733,#72734,#72735,#72736,#72737,#72738,#72739,#72740,#72741,#72742,
#72743,#72744,#72745,#72746,#72747,#72748,#72749,#72750,#72751,#72752,#72753,
#72754,#72755,#72756,#72757,#72758,#72759,#72760,#72761,#72762,#72763,#72764,
#72765,#72766,#72767,#72768,#72769,#72770,#72771,#72772,#72773,#72774,#72775,
#72776,#72777,#72778,#72779,#72780,#72781,#72782,#72783,#72784,#72785,#72786,
#72787,#72788,#72789,#72790,#72791,#72792,#72793,#72794,#72795,#72796,#72797,
#72798,#72799,#72800,#72801,#72802,#72803,#72804,#72805,#72806,#72807,#72808,
#72809,#72810,#72811,#72812,#72813,#72814,#72815,#72816,#72817,#72818,#72819,
#72820,#72821,#72822,#72823,#72824,#72825,#72826,#72827,#72828,#72829,#72830,
#72831,#72832,#72833,#72834,#72835,#72836,#72837,#72838,#72839,#72840,#72841,
#72842,#72843,#72844,#72845,#72846,#72847,#72848,#72849,#72850,#72851,#72852,
#72853,#72854,#72855,#72856,#72857,#72858,#72859,#72860,#72861,#72862,#72863,
#72864,#72865,#72866,#72867,#72868,#72869,#72870,#72871,#72872,#72873,#72874,
#72875,#72876,#72877,#72878,#72879,#72880,#72881,#72882,#72883,#72884,#72885,
#72886,#72887,#72888,#72889,#72890,#72891,#72892,#72893,#72894,#72895,#72896,
#72897,#72898,#72899,#72900,#72901,#72902,#72903,#72904,#72905,#72906,#72907,
#72908,#72909,#72910,#72911,#72912,#72913,#72914,#72915,#72916,#72917,#72918,
#72919,#72920,#72921,#72922,#72923,#72924,#72925,#72926,#72927,#72928,#72929,
#72930,#72931,#72932,#72933,#72934,#72935,#72936,#72937,#72938,#72939,#72940,
#72941,#72942,#72943,#72944,#72945,#72946,#72947,#72948,#72949,#72950,#72951,
#72952,#72953,#72954,#72955,#72956,#72957,#72958,#72959,#72960,#72961,#72962,
#72963,#72964,#72965,#72966,#72967,#72968,#72969,#72970,#72971,#72972,#72973,
#72974,#72975,#72976,#72977,#72978,#72979,#72980,#72981,#72982,#72983,#72984,
#72985,#72986,#72987,#72988,#72989,#72990,#72991,#72992,#72993,#72994,#72995,
#72996,#72997,#72998,#72999,#73000,#73001,#73002,#73003,#73004,#73005,#73006,
#73007,#73008,#73009,#73010,#73011,#73012,#73013,#73014,#73015,#73016,#73017,
#73018,#73019,#73020,#73021,#73022,#73023,#73024,#73025,#73026,#73027,#73028,
#73029,#73030,#73031,#73032,#73033,#73034,#73035,#73036,#73037,#73038,#73039,
#73040,#73041,#73042,#73043,#73044,#73045,#73046,#73047,#73048,#73049,#73050,
#73051,#73052,#73053,#73054,#73055,#73056,#73057,#73058,#73059,#73060,#73061,
#73062,#73063,#73064,#73065,#73066,#73067,#73068,#73069,#73070,#73071,#73072,
#73073,#73074,#73075,#73076,#73077,#73078,#73079,#73080,#73081,#73082,#73083,
#73084,#73085,#73086,#73087,#73088,#73089,#73090,#73091,#73092,#73093,#73094,
#73095,#73096,#73097,#73098,#73099,#73100,#73101,#73102,#73103,#73104,#73105,
#73106,#73107,#73108,#73109,#73110,#73111,#73112,#73113,#73114,#73115,#73116,
#73117,#73118,#73119,#73120,#73121,#73122,#73123,#73124,#73125,#73126,#73127,
#73128,#73129,#73130,#73131,#73132,#73133,#73134,#73135,#73136,#73137,#73138,
#73139,#73140,#73141,#73142,#73143,#73144,#73145,#73146,#73147,#73148,#73149,
#73150,#73151,#73152,#73153,#73154,#73155,#73156,#73157,#73158,#73159,#73160,
#73161,#73162,#73163,#73164,#73165,#73166,#73167,#73168,#73169,#73170,#73171,
#73172,#73173,#73174,#73175,#73176,#73177,#73178,#73179,#73180),
 .UNSPECIFIED.,.F.,.F.,(4,2,2,2,2,2,2,2,2,2,2,2,2,2,2,2,2,2,2,2,2,2,2,2,
2,2,2,2,2,2,2,2,2,2,2,2,2,2,2,2,2,2,2,2,2,2,2,2,2,2,2,2,2,2,2,2,2,2,2,2,
2,2,2,2,2,2,2,2,2,2,2,2,2,2,2,2,2,2,2,2,2,2,2,2,2,2,2,2,2,2,2,2,2,2,2,2,
2,2,2,2,2,2,2,2,2,2,2,2,2,2,2,2,2,2,2,2,2,2,2,2,2,2,2,2,2,2,2,2,2,2,2,2,
2,2,2,2,2,2,2,2,2,2,2,2,2,2,2,2,2,2,2,2,2,2,2,2,2,2,2,2,2,2,2,2,2,2,2,2,
2,2,2,2,2,2,2,2,2,2,2,2,2,2,2,2,2,2,2,2,2,2,2,2,2,2,2,2,2,2,2,2,2,2,2,2,
2,2,2,2,2,2,2,2,2,2,2,2,2,2,2,2,2,2,2,2,2,2,2,2,2,2,2,2,2,2,2,2,2,2,2,2,
2,2,2,2,2,2,2,2,2,2,2,2,2,2,2,2,2,2,2,2,2,2,2,2,2,2,2,2,2,2,2,2,2,2,2,2,
2,2,2,2,2,4),(0.00168353385591401,0.0498777725783733,0.079003186553249,
0.0895156419589813,0.0974007412312368,0.104915212734958,0.112289681583754,
0.124232755713915,0.154184803611029,0.204113212361754,0.390295019998446,
0.409493031083788,0.413812283128153,0.417094354289524,0.420423817961922,
0.423560710051339,0.427937381600568,0.440899503587822,0.545448952708169,
0.629479438484531,0.67755807686016,0.698309917290908,0.714482280281196,
0.722576845810815,0.728897071836187,0.735237297706495,0.746310083480894,
0.779527291000484,1.01324258215097,1.13599247224734,1.17232186988904,1.17762337879856,
1.18034426807877,1.18232680519458,1.18445023670214,1.18810136647382,1.19816950966103,
1.34640236540742,1.44865603901265,1.5675992262831,1.57695568485988,1.58052855253191,
1.58298454179852,1.58538623977395,1.58827501156116,1.59545928201116,1.66017201985687,
1.76921009663314,1.89063114455488,1.97243364729558,1.99685057948197,2.00005878378817,
2.00166569926628,2.00282040079342,2.00404168752873,2.00610208564028,2.01170845117154,
2.10070766806404,2.10077395529731,2.10091211990214,2.101187452584,2.10169349540269,
2.10251776573483,2.10368731986464,2.10516188595958,2.10687849259004,2.16980160606017,
2.28622622708861,2.37580530142592,2.38973034856071,2.39378866124825,2.39621455204496,
2.39837368431185,2.40108880468321,2.40531683540522,2.42510133383884,2.50604430803166,
2.53979261107383,2.68836841443852,2.74615531093579,2.77854810093646,2.79455970257573,
2.79730056715374,2.79875229629633,2.79994796798825,2.80136036330358,2.80379996790127,
2.81306464078964,2.95661978409542,3.09012507541166,3.14572114533918,3.20536908080192,
3.21652977092373,3.22025913287162,3.22267704257178,3.22496154657145,3.2279762319077,
3.23471489081541,3.29227508613932,3.35229405093857,3.52397726557653,3.59902294881875,
3.61115988384797,3.61462809852094,3.61674631861868,3.61866099038122,3.62110923163744,
3.62611839070542,3.65758831406184,3.840940533774,3.96295214523924,3.9853897282661,
3.99262099900004,3.99715105393213,4.00133071207611,4.00671403653279,4.0182776372746,
4.11500547720755,4.24014635113042,4.2790064466594,4.34882749600617,4.35568774037037,
4.36078926225323,4.36306815486034,4.36476261847292,4.36633886777264,4.36849514971075,
4.37275971680104,4.4176221802148,4.41952602532707,4.66314860298935,4.73354229690831,
4.76741381591787,4.77308291044379,4.77606327952662,4.77826454219667,4.78065027084908,
4.78482191023632,4.79676045438706,4.97994016275531,5.17538295130353,5.18789307138019,
5.19164138272884,5.19387207417756,5.19565326728428,5.19804262159615,5.20251436275363,
5.22754477696715,5.28427901639821,5.4901758164607,5.49888674407132,5.56953400597466,
5.59328173306116,5.61847426478226,5.62846629335407,5.63583652377428,5.64387655236454,
5.65500081752022,5.68197162116042,5.81136460128152,5.93029902217239,5.94345903054978,
5.94810132611293,5.95131527057692,5.954287739056,5.9583263358495,5.96657811711028,
5.97763113072634,6.10022074232059,6.23253370119179,6.24631816563436,6.25470193609506,
6.26125326417265,6.26841682978343,6.28004742930654,6.32259183306286,6.51678739911555,
6.66559673606709,6.69896007466199,6.70809118169648,6.7115927283139,6.71368805519725,
6.71590340827373,6.71882317805519,6.72512592889425,6.87167365461539,7.09459737471727,
7.10811816849245,7.11240626760737,7.11475750211263,7.11710211855158,7.11997486685529,
7.12545052913383,7.1584559018588,7.22847409834317,7.4551879189228,7.47858769823266,
7.51195871758507,7.522769412867,7.53106992517631,7.53351145478206,7.53480945510939,
7.5359515105539,7.53737866264054,7.53983876033695,7.55016936974492,7.64627327967203,
7.90652536288647,7.9225139827139,7.92680587190077,7.92930889939954,7.931459552461,
7.93406646017141,7.93895084429497,7.96616590176265,8.01841922259449,8.05164230803548,
8.07578157943914,8.22746345528132,8.30300532163895,8.32681226677966,8.3301004256536,
8.33166704303511,8.33288653224296,8.33421261027509,8.33628991055581,8.34283483538172,
8.35311217620763,8.38514955306603,8.47970781201078,8.67792042524294,8.7441485597068,
8.75045795653661,8.75350386494422,8.75566604118089,8.75770514333178,8.76053483818278,
8.76615843540553,8.80824886870022,8.91619915555595,8.93775711878854,8.95584827275764,
8.97141534766263,8.98504177726917,8.99713095477215,9.00799735478284,9.12288842701972,
9.14252623037617,9.14642127403559,9.14887136066608,9.15078580291964,9.15285952187365,
9.15619593669478,9.16017138664598,9.16787948793886,9.18699026160615,9.2423309841501,
9.37872978869866,9.47119618921288,9.47744072684706,9.51438152226805,9.52270159349194,
9.5279676107825,9.53211959901976,9.53675557002965,9.54446428009804,9.57313598191909,
9.71969638076577,9.8260614980944,9.83730722237228,9.84572006054629,9.85472697793631,
9.85935372777375,9.88924730077025,9.89374171754815,9.89590502436992,9.89758176239949,
9.89913672284857,9.9009334025763,9.90347438119731,9.907782335338,9.95796125064517),
 .UNSPECIFIED.);
#3484=B_SPLINE_CURVE_WITH_KNOTS('',3,(#73182,#73183,#73184,#73185,#73186,
#73187,#73188,#73189,#73190,#73191,#73192,#73193),.UNSPECIFIED.,.F.,.F.,
(4,1,1,1,1,1,1,1,1,4),(315.282914065123,316.220934879991,316.719706070653,
317.218477261316,317.717248451978,318.216019642641,319.213562023966,320.211104405291,
321.208646786615,321.566097918198),.UNSPECIFIED.);
#3485=B_SPLINE_CURVE_WITH_KNOTS('',3,(#73195,#73196,#73197,#73198,#73199,
#73200,#73201,#73202,#73203,#73204,#73205,#73206,#73207,#73208,#73209,#73210,
#73211,#73212,#73213,#73214,#73215,#73216,#73217,#73218,#73219,#73220,#73221,
#73222,#73223,#73224,#73225,#73226,#73227,#73228,#73229,#73230,#73231,#73232,
#73233,#73234,#73235,#73236,#73237,#73238,#73239,#73240,#73241,#73242,#73243,
#73244,#73245,#73246,#73247,#73248,#73249,#73250,#73251,#73252,#73253,#73254,
#73255,#73256,#73257,#73258,#73259,#73260,#73261,#73262,#73263,#73264,#73265,
#73266,#73267,#73268,#73269,#73270,#73271,#73272,#73273,#73274,#73275,#73276,
#73277,#73278,#73279,#73280,#73281,#73282,#73283,#73284,#73285,#73286,#73287,
#73288,#73289,#73290,#73291,#73292,#73293,#73294,#73295,#73296,#73297,#73298,
#73299,#73300,#73301,#73302,#73303,#73304,#73305,#73306,#73307,#73308,#73309,
#73310,#73311,#73312,#73313,#73314,#73315,#73316,#73317,#73318,#73319,#73320,
#73321,#73322,#73323,#73324,#73325,#73326,#73327,#73328,#73329,#73330,#73331,
#73332,#73333,#73334,#73335,#73336,#73337,#73338,#73339,#73340,#73341,#73342,
#73343,#73344,#73345,#73346,#73347,#73348,#73349,#73350,#73351,#73352,#73353,
#73354,#73355,#73356,#73357,#73358,#73359,#73360,#73361,#73362,#73363,#73364,
#73365,#73366,#73367,#73368,#73369,#73370,#73371,#73372,#73373,#73374,#73375,
#73376,#73377,#73378,#73379,#73380,#73381,#73382,#73383,#73384,#73385,#73386,
#73387,#73388,#73389,#73390,#73391,#73392,#73393,#73394,#73395,#73396,#73397,
#73398,#73399,#73400,#73401,#73402,#73403,#73404,#73405,#73406,#73407,#73408,
#73409,#73410,#73411,#73412,#73413,#73414,#73415,#73416,#73417,#73418,#73419,
#73420,#73421,#73422,#73423,#73424,#73425,#73426,#73427,#73428,#73429,#73430,
#73431,#73432,#73433,#73434,#73435,#73436,#73437,#73438,#73439,#73440,#73441,
#73442,#73443,#73444,#73445,#73446,#73447,#73448,#73449,#73450,#73451,#73452,
#73453),.UNSPECIFIED.,.F.,.F.,(4,3,3,3,3,3,3,3,3,3,3,3,3,3,3,3,3,3,3,3,
3,3,3,3,3,3,3,3,3,3,3,3,3,3,3,3,3,3,3,3,3,3,3,3,3,3,3,3,3,3,3,3,3,3,3,3,
3,3,3,3,3,3,3,3,3,3,3,3,3,3,3,3,3,3,3,3,3,3,3,3,3,3,3,3,3,3,4),(321.566099372302,
321.639562907717,321.707417977278,321.781834369621,321.856267530736,321.930729723134,
322.005273658581,322.07986197705,322.154554403333,322.20618916794,322.282764990038,
322.359273326325,322.43572511814,322.512131266634,322.588502640109,322.665406253753,
322.741748751244,322.818090793491,322.894442226529,322.971764557213,323.048188724363,
323.125960136814,323.203731549265,323.277523615233,323.351253473926,323.424934185762,
323.498579583122,323.572203530935,323.645831596629,323.702502739928,323.783929205766,
323.865490499842,323.949436357529,324.031269866712,324.116271898651,324.20127393059,
324.279707563597,324.358071614971,324.43637092051,324.514591494691,324.592762239732,
324.670875258101,324.700045121253,324.776415149011,324.852802028157,324.929215329136,
325.005697368984,325.082216747814,325.158818071272,325.198816311915,325.274202690607,
325.349527667363,325.42480405076,325.500044616947,325.575262117461,325.652899189433,
325.728126958421,325.803371452636,325.878644229176,325.953956858419,326.029358435394,
326.104812705547,326.180364874505,326.19635869324,326.269516707425,326.342586099395,
326.415581797685,326.488518661238,326.561411494871,326.634275063227,326.707137573486,
326.780003140076,326.852885105631,326.92579682345,326.99879421002,327.071838442305,
327.144992679506,327.193901074565,327.26973914768,327.345446257123,327.421075129875,
327.496636972093,327.572142950378,327.647597845216,327.723022264868,327.798430624931,
327.849284679482),.UNSPECIFIED.);
#3486=B_SPLINE_CURVE_WITH_KNOTS('',3,(#73455,#73456,#73457,#73458,#73459,
#73460,#73461,#73462,#73463,#73464,#73465,#73466,#73467,#73468,#73469,#73470,
#73471,#73472,#73473,#73474,#73475,#73476,#73477,#73478,#73479,#73480,#73481,
#73482,#73483,#73484,#73485,#73486,#73487,#73488,#73489,#73490,#73491,#73492,
#73493,#73494,#73495,#73496,#73497,#73498,#73499,#73500,#73501,#73502,#73503,
#73504,#73505,#73506,#73507,#73508,#73509,#73510,#73511,#73512,#73513,#73514,
#73515,#73516,#73517,#73518,#73519,#73520,#73521,#73522,#73523,#73524,#73525,
#73526,#73527,#73528,#73529,#73530,#73531,#73532,#73533,#73534,#73535,#73536,
#73537,#73538,#73539,#73540,#73541,#73542,#73543,#73544,#73545,#73546,#73547,
#73548,#73549,#73550,#73551,#73552,#73553,#73554,#73555,#73556,#73557,#73558,
#73559,#73560,#73561,#73562,#73563,#73564,#73565,#73566,#73567,#73568,#73569,
#73570,#73571,#73572,#73573,#73574,#73575,#73576,#73577,#73578,#73579,#73580,
#73581,#73582,#73583,#73584,#73585,#73586,#73587,#73588,#73589,#73590,#73591,
#73592,#73593,#73594,#73595,#73596,#73597,#73598,#73599,#73600,#73601,#73602,
#73603,#73604,#73605,#73606,#73607,#73608,#73609,#73610,#73611,#73612,#73613,
#73614,#73615,#73616,#73617,#73618,#73619,#73620,#73621,#73622,#73623,#73624,
#73625,#73626,#73627,#73628,#73629,#73630,#73631,#73632,#73633,#73634,#73635,
#73636,#73637,#73638,#73639,#73640,#73641,#73642,#73643,#73644,#73645,#73646,
#73647,#73648,#73649,#73650,#73651,#73652,#73653,#73654,#73655,#73656,#73657,
#73658,#73659,#73660,#73661,#73662,#73663,#73664,#73665,#73666,#73667,#73668,
#73669,#73670,#73671,#73672,#73673,#73674,#73675,#73676,#73677,#73678,#73679,
#73680,#73681,#73682,#73683,#73684,#73685,#73686,#73687,#73688,#73689,#73690,
#73691,#73692,#73693,#73694,#73695,#73696,#73697,#73698,#73699,#73700,#73701,
#73702,#73703,#73704,#73705,#73706,#73707,#73708,#73709,#73710,#73711,#73712,
#73713,#73714,#73715,#73716,#73717,#73718,#73719,#73720,#73721,#73722,#73723,
#73724,#73725,#73726,#73727,#73728,#73729,#73730,#73731,#73732,#73733,#73734,
#73735,#73736,#73737,#73738,#73739,#73740,#73741,#73742,#73743,#73744,#73745,
#73746,#73747,#73748,#73749,#73750,#73751,#73752,#73753,#73754,#73755,#73756,
#73757,#73758,#73759,#73760,#73761,#73762,#73763,#73764,#73765,#73766,#73767,
#73768,#73769,#73770,#73771,#73772,#73773,#73774,#73775,#73776,#73777,#73778,
#73779,#73780,#73781,#73782,#73783,#73784,#73785,#73786,#73787,#73788,#73789,
#73790,#73791,#73792,#73793,#73794,#73795,#73796,#73797,#73798,#73799,#73800,
#73801,#73802,#73803,#73804,#73805,#73806,#73807,#73808,#73809,#73810,#73811,
#73812,#73813,#73814,#73815,#73816,#73817,#73818,#73819,#73820,#73821,#73822,
#73823,#73824,#73825,#73826,#73827,#73828,#73829,#73830,#73831,#73832,#73833,
#73834,#73835,#73836,#73837,#73838,#73839,#73840,#73841,#73842,#73843,#73844,
#73845,#73846,#73847,#73848,#73849,#73850,#73851,#73852,#73853,#73854,#73855,
#73856,#73857,#73858,#73859,#73860,#73861,#73862,#73863,#73864,#73865,#73866,
#73867,#73868,#73869,#73870,#73871,#73872,#73873,#73874,#73875,#73876,#73877,
#73878,#73879,#73880,#73881,#73882,#73883,#73884,#73885,#73886,#73887,#73888,
#73889,#73890,#73891,#73892,#73893,#73894,#73895,#73896,#73897,#73898,#73899,
#73900,#73901,#73902,#73903,#73904,#73905,#73906,#73907,#73908,#73909,#73910,
#73911,#73912,#73913,#73914,#73915,#73916,#73917,#73918,#73919,#73920,#73921,
#73922,#73923,#73924,#73925,#73926,#73927,#73928,#73929,#73930,#73931,#73932,
#73933,#73934,#73935,#73936,#73937,#73938,#73939,#73940,#73941,#73942,#73943,
#73944,#73945,#73946,#73947,#73948,#73949,#73950),.UNSPECIFIED.,.F.,.F.,
(4,2,2,2,2,2,2,2,2,2,2,2,2,2,2,2,2,2,2,2,2,2,2,2,2,2,2,2,2,2,2,2,2,2,2,
2,2,2,2,2,2,2,2,2,2,2,2,2,2,2,2,2,2,2,2,2,2,2,2,2,2,2,2,2,2,2,2,2,2,2,2,
2,2,2,2,2,2,2,2,2,2,2,2,2,2,2,2,2,2,2,2,2,2,2,2,2,2,2,2,2,2,2,2,2,2,2,2,
2,2,2,2,2,2,2,2,2,2,2,2,2,2,2,2,2,2,2,2,2,2,2,2,2,2,2,2,2,2,2,2,2,2,2,2,
2,2,2,2,2,2,2,2,2,2,2,2,2,2,2,2,2,2,2,2,2,2,2,2,2,2,2,2,2,2,2,2,2,2,2,2,
2,2,2,2,2,2,2,2,2,2,2,2,2,2,2,2,2,2,2,2,2,2,2,2,2,2,2,2,2,2,2,2,2,2,2,2,
2,2,2,2,2,2,2,2,2,2,2,2,2,2,2,2,2,2,2,2,2,2,2,2,2,2,2,2,2,2,2,2,4),(0.00198922818128111,
0.236183877542624,0.272854307600681,0.294822807650427,0.299030406213339,
0.301312088887494,0.303028329272993,0.30491931832674,0.308308476588276,
0.318584789539833,0.559208678639797,0.652459493438587,0.67156912176654,
0.678334765277876,0.682762433727734,0.686889650910601,0.692388579016866,
0.704118744927879,0.822382316496041,1.02860731611399,1.04383306888064,1.04726138975409,
1.04920185227845,1.05069856678751,1.05264169890295,1.0559908342161,1.06894166926308,
1.30639838012157,1.3939299335222,1.43253332457032,1.44661779578641,1.45643706072953,
1.4601553805191,1.4624361584321,1.46490890829546,1.46814748561117,1.47528654622001,
1.53269229438039,1.68098511292506,1.79909040532422,1.84223199734028,1.87143150913627,
1.87605932057005,1.87848197893651,1.88045701740972,1.88243681468299,1.88604344122846,
1.8974279115671,2.05854355971327,2.18991595825875,2.28905433085235,2.30767206141563,
2.31726643519325,2.32434806478356,2.33318985934922,2.34753042178583,2.39885191546709,
2.40512897751166,2.49853317154152,2.588456026089,2.60745601719949,2.6205802810811,
2.63025107918723,2.63466719100882,2.63799770453316,2.64113213820639,2.6454993194314,
2.65837529646984,2.76719764834364,2.91729375116296,2.93278328648167,2.9407762474667,
2.9466508643795,2.95373159719259,2.96516426117223,3.00376511867622,3.21178573994249,
3.25897309158952,3.37706979077462,3.38446558967613,3.39344689395539,3.39681685337303,
3.39911628918255,3.40135218509615,3.40402551600192,3.41060475931895,3.50973555301615,
3.63104127870229,3.74590361341228,3.79008372879148,3.79596218226843,3.79891878581283,
3.8010488771777,3.80330714313027,3.80648785107587,3.81307509940703,3.88260556633153,
4.05562322016617,4.2040097025033,4.21541741319343,4.21802142936888,4.21949956439709,
4.22064155763814,4.22212632891757,4.22469123363908,4.23506271096358,4.41329212317539,
4.52199816333728,4.60387237982322,4.61000243473734,4.6128619386028,4.61503898019725,
4.61710227060373,4.61998570609533,4.62753195724338,4.73936091549275,4.92276967741616,
4.98071285511311,5.01094685390791,5.01451238828769,5.0161072648194,5.01733111634852,
5.01864507514235,5.02070983223992,5.02717379164662,5.0644619037052,5.1189502509723,
5.34045677191975,5.42803574855811,5.43541096081708,5.4383356882947,5.44046576788778,
5.44274815766424,5.44580575853961,5.45260005077582,5.61661074564287,5.81665138729238,
5.8287898116107,5.83241363952725,5.83456638341725,5.83628303512172,5.83858243497155,
5.84287425935348,5.86650944873605,5.91812446072802,6.13359423381958,6.19658530492327,
6.20752542067062,6.21287492770743,6.21704856225871,6.2215934740388,6.22889288984193,
6.25344306470296,6.47680113779414,6.57295769993393,6.57854740615174,6.58073665153315,
6.58232150842026,6.58401085926164,6.58625978128018,6.59119985802725,6.6946889010257,
6.84660903857566,6.98032329318788,6.98910616799941,6.99240792195616,6.99475325509561,
6.99696645441848,7.0000399965982,7.00615702996334,7.05242662136879,7.12328351322218,
7.2802246409017,7.29444222228421,7.40066858456703,7.40728160689274,7.40987433864081,
7.41175291418941,7.41375694874064,7.41642580659961,7.42229618074848,7.43016200465765,
7.51158729562236,7.61121233767283,7.80743060968919,7.83504689160474,7.84539478393793,
7.85285393545266,7.86067023627787,7.87104298152544,7.88252912544297,7.90189377934439,
7.94261746555521,8.09148070970994,8.15488619146199,8.16327541451296,8.16750021120826,
8.17080389293221,8.17386363203754,8.17925342636621,8.19857936923149,8.23324694023105,
8.43769230459801,8.46089409090767,8.46960139265026,8.47582013150466,8.48226225872685,
8.49010033441227,8.5068702301573,8.52925831275699,8.58669913376713,8.7465037095287,
8.90657701057071,8.91604544717839,8.92549838760043,8.92905162308387,8.93115696268724,
8.93336756206607,8.93625562121796,8.94239292077128,8.97396052408427,9.00026170834061,
9.06687491676023,9.12609830984473,9.22412600025835,9.23160590966397,9.23705958717135,
9.31970204207281,9.32716434948363,9.33017709377742,9.33239051371326,9.33478061134552,
9.33801503840048,9.34533944247983,9.4634722039409,9.50705389168326,9.52698316382605,
9.55023543880307,9.7363667131148,9.74732266012034,9.74976205280237,9.7513463374906,
9.75261827946431,9.75406013419233,9.75650244224091,9.76652286260011,9.85174569816709,
9.95699582782369),.UNSPECIFIED.);
#3487=B_SPLINE_CURVE_WITH_KNOTS('',3,(#73952,#73953,#73954,#73955,#73956,
#73957,#73958,#73959,#73960,#73961,#73962,#73963,#73964,#73965,#73966,#73967,
#73968,#73969),.UNSPECIFIED.,.F.,.F.,(4,2,2,2,2,2,2,2,4),(340.415655293841,
341.250572205736,342.085489117631,342.920406029526,343.755322941421,344.590239853315,
345.42515676521,346.260073677105,346.698840601021),.UNSPECIFIED.);
#3488=B_SPLINE_CURVE_WITH_KNOTS('',3,(#73971,#73972,#73973,#73974,#73975,
#73976,#73977,#73978,#73979,#73980,#73981,#73982,#73983,#73984,#73985,#73986,
#73987,#73988,#73989,#73990,#73991,#73992,#73993,#73994,#73995,#73996,#73997,
#73998,#73999,#74000,#74001,#74002,#74003,#74004,#74005,#74006,#74007,#74008,
#74009,#74010,#74011,#74012,#74013,#74014,#74015,#74016,#74017,#74018,#74019,
#74020,#74021,#74022,#74023,#74024,#74025,#74026,#74027,#74028,#74029,#74030,
#74031,#74032,#74033,#74034,#74035,#74036,#74037,#74038,#74039,#74040,#74041,
#74042,#74043,#74044,#74045,#74046,#74047,#74048,#74049,#74050,#74051,#74052,
#74053,#74054,#74055,#74056,#74057,#74058,#74059,#74060,#74061,#74062,#74063,
#74064,#74065,#74066,#74067,#74068,#74069,#74070,#74071,#74072,#74073,#74074,
#74075,#74076,#74077,#74078,#74079,#74080,#74081,#74082,#74083,#74084,#74085,
#74086,#74087,#74088,#74089,#74090,#74091,#74092,#74093,#74094,#74095,#74096,
#74097,#74098,#74099,#74100,#74101,#74102,#74103,#74104,#74105,#74106,#74107,
#74108,#74109,#74110,#74111,#74112,#74113,#74114,#74115,#74116,#74117,#74118,
#74119,#74120,#74121,#74122,#74123,#74124,#74125,#74126,#74127,#74128,#74129,
#74130,#74131,#74132,#74133,#74134,#74135,#74136,#74137,#74138,#74139,#74140,
#74141,#74142,#74143,#74144,#74145,#74146,#74147,#74148,#74149,#74150,#74151,
#74152,#74153,#74154,#74155,#74156,#74157,#74158,#74159,#74160,#74161,#74162,
#74163,#74164,#74165,#74166,#74167,#74168,#74169,#74170,#74171,#74172,#74173,
#74174,#74175,#74176,#74177,#74178,#74179,#74180,#74181,#74182,#74183,#74184,
#74185,#74186,#74187,#74188,#74189,#74190,#74191,#74192,#74193,#74194,#74195,
#74196,#74197,#74198,#74199,#74200,#74201,#74202,#74203,#74204,#74205,#74206,
#74207,#74208,#74209,#74210,#74211,#74212,#74213,#74214,#74215,#74216,#74217,
#74218,#74219,#74220,#74221,#74222,#74223,#74224,#74225,#74226,#74227,#74228,
#74229,#74230,#74231,#74232,#74233,#74234,#74235,#74236,#74237,#74238,#74239,
#74240,#74241,#74242,#74243,#74244,#74245,#74246,#74247,#74248,#74249,#74250,
#74251,#74252,#74253,#74254,#74255,#74256,#74257,#74258,#74259,#74260,#74261,
#74262,#74263,#74264,#74265,#74266,#74267,#74268,#74269,#74270,#74271,#74272,
#74273,#74274,#74275,#74276,#74277,#74278,#74279,#74280,#74281,#74282,#74283,
#74284,#74285,#74286,#74287,#74288,#74289,#74290,#74291,#74292,#74293,#74294,
#74295,#74296,#74297,#74298,#74299,#74300,#74301,#74302,#74303,#74304,#74305,
#74306,#74307,#74308,#74309,#74310,#74311,#74312,#74313,#74314,#74315,#74316,
#74317,#74318,#74319,#74320,#74321,#74322,#74323,#74324,#74325,#74326,#74327,
#74328,#74329,#74330,#74331,#74332,#74333,#74334,#74335,#74336,#74337,#74338,
#74339,#74340,#74341,#74342,#74343,#74344,#74345,#74346,#74347,#74348,#74349,
#74350,#74351,#74352,#74353,#74354,#74355,#74356,#74357,#74358,#74359,#74360,
#74361,#74362,#74363,#74364,#74365,#74366,#74367,#74368,#74369,#74370,#74371,
#74372,#74373,#74374,#74375,#74376,#74377,#74378,#74379,#74380,#74381,#74382,
#74383,#74384,#74385,#74386,#74387,#74388,#74389,#74390,#74391,#74392,#74393,
#74394,#74395,#74396,#74397,#74398,#74399,#74400,#74401,#74402,#74403,#74404,
#74405,#74406,#74407,#74408,#74409,#74410,#74411,#74412,#74413,#74414,#74415,
#74416,#74417,#74418,#74419,#74420,#74421,#74422,#74423,#74424,#74425,#74426,
#74427,#74428,#74429,#74430,#74431,#74432,#74433,#74434,#74435,#74436,#74437,
#74438,#74439,#74440,#74441,#74442,#74443,#74444,#74445,#74446,#74447,#74448,
#74449,#74450,#74451,#74452,#74453,#74454,#74455,#74456,#74457,#74458,#74459,
#74460,#74461,#74462,#74463,#74464,#74465,#74466,#74467,#74468,#74469,#74470,
#74471,#74472,#74473,#74474,#74475,#74476,#74477,#74478,#74479,#74480,#74481,
#74482,#74483,#74484,#74485,#74486),.UNSPECIFIED.,.F.,.F.,(4,2,2,2,2,2,
2,2,2,2,2,2,2,2,2,2,2,2,2,2,2,2,2,2,2,2,2,2,2,2,2,2,2,2,2,2,2,2,2,2,2,2,
2,2,2,2,2,2,2,2,2,2,2,2,2,2,2,2,2,2,2,2,2,2,2,2,2,2,2,2,2,2,2,2,2,2,2,2,
2,2,2,2,2,2,2,2,2,2,2,2,2,2,2,2,2,2,2,2,2,2,2,2,2,2,2,2,2,2,2,2,2,2,2,2,
2,2,2,2,2,2,2,2,2,2,2,2,2,2,2,2,2,2,2,2,2,2,2,2,2,2,2,2,2,2,2,2,2,2,2,2,
2,2,2,2,2,2,2,2,2,2,2,2,2,2,2,2,2,2,2,2,2,2,2,2,2,2,2,2,2,2,2,2,2,2,2,2,
2,2,2,2,2,2,2,2,2,2,2,2,2,2,2,2,2,2,2,2,2,2,2,2,2,2,2,2,2,2,2,2,2,2,2,2,
2,2,2,2,2,2,2,2,2,2,2,2,2,2,2,2,2,2,2,2,2,2,2,2,2,2,2,2,2,2,2,2,2,2,2,4),
(0.00201172098188263,0.26785772850997,0.336857823383509,0.346341844779204,
0.348790531623013,0.350234150731159,0.35150641770642,0.353089494729013,
0.355522927949294,0.367173556294413,0.61641885642891,0.732383385343184,
0.740170432410955,0.74332318988102,0.745513237332233,0.747708768708506,
0.750811159704312,0.758150621232473,0.856660079940925,0.915920330777643,
1.01131517256049,1.0872275531088,1.13635125872654,1.14394057562209,1.1461031432124,
1.14743227276947,1.14865076128787,1.15020643452794,1.15347907616869,1.17485044651468,
1.42262349848926,1.50584868045553,1.54279547640015,1.55619405281239,1.5624737103579,
1.56750517355141,1.57019711971199,1.57243428466372,1.57468451831813,1.5787871612878,
1.59171101200624,1.78669000326812,1.94811466511878,1.95971868454392,1.96312974970139,
1.9652344312891,1.96715099015463,1.96962142125009,1.97474648119242,2.0088629671186,
2.02595144789495,2.14118090651002,2.30773034059313,2.33290597661399,2.34047794924219,
2.34508209565747,2.34923912489801,2.3543968663223,2.3645024658482,2.42490062362265,
2.63501688132774,2.68385780569144,2.70592756902931,2.70975065833207,2.71177614841906,
2.71343950102428,2.71511564282012,2.71819780833977,2.72811504021162,2.89581916126414,
3.03810262379446,3.1057656921007,3.11815354878818,3.12223321602547,3.12486288116367,
3.12733654813598,3.13058510284429,3.1360700444179,3.16969808690455,3.45296143876884,
3.52434995656347,3.53630651696089,3.53983508604457,3.54201619766115,3.54400521418938,
3.54657339107814,3.55191870659064,3.58862326122928,3.59112629064559,3.5941580942748,
3.60589132120185,3.60804128041258,3.61062450907206,3.72820514770246,3.93957400625043,
3.96649696857761,3.9775564112426,3.98558204304256,3.99295830280372,4.00492030425341,
4.03495101972908,4.19845562922461,4.25942722184311,4.28843584675888,4.29506018532236,
4.2988546586122,4.30180604973414,4.30567928455193,4.3127602458724,4.35465198551136,
4.39648202516114,4.49634347355929,4.57408995776118,4.59338435610224,4.60210937166159,
4.60868817207238,4.6149020810814,4.62359414162019,4.64686757126827,4.84700225921339,
4.98014546872586,5.0503407855483,5.05697759015036,5.05992698481809,5.06215502858731,
5.06450744202789,5.06812562234812,5.07889829876476,5.13336633417323,5.19116823361091,
5.44053566966038,5.4553627135643,5.45980899203634,5.46245607750361,5.46457057284833,
5.46740620449709,5.47271105002696,5.50210821774037,5.55864007014396,5.67191545187263,
5.71919451972143,5.77378411346617,5.85521600423813,5.87647321545384,5.87985435183502,
5.88149547809999,5.88277328780646,5.88418088049476,5.8864711188375,5.89471523202358,
5.95069907347356,6.04945136834659,6.16188021070765,6.20717207483633,6.26524119445543,
6.27114320731447,6.27402671579624,6.27608941466102,6.27826524853656,6.28112222820834,
6.2872432673312,6.36837618381505,6.54132711455869,6.60722517412876,6.67161264542583,
6.67584617814019,6.67745079435046,6.67860212432523,6.67970401266425,6.68125908222952,
6.68444499569772,6.71292051338696,6.79899987135283,6.93507335710241,7.08563288839093,
7.09576935119661,7.09948584939378,7.10165848778219,7.10369320427128,7.1064944826526,
7.11198237196928,7.14990676712809,7.24266649478576,7.39314191534718,7.4838138174065,
7.49116657838417,7.49382205924072,7.49567484370405,7.49739627132081,7.49974540373852,
7.5041839075335,7.53136198294643,7.59330462925065,7.82726968508707,7.8610618831827,
7.86910390750369,7.87428252257254,7.87842405211085,7.88229674326543,7.88924415942943,
7.91089580081731,8.03356739936528,8.15266598084587,8.1852523471671,8.19747536371011,
8.20034717474997,8.23490581711722,8.23911935969333,8.24125983362429,8.24283145486047,
8.2445276718186,8.24682237612872,8.25173469297441,8.25827461499044,8.2741862114308,
8.31447112604205,8.42791900126448,8.6343598522704,8.64785971055778,8.65224260197667,
8.65466964122223,8.65710543600497,8.6601129411165,8.6659171427816,8.70310007140037,
8.78782717693791,8.86041969121024,8.92383943212682,9.05499123177181,9.06577426419802,
9.06930660433383,9.07126906258101,9.07324411601817,9.07569016843109,9.08043619647743,
9.11149746112447,9.15785056291941,9.24268266709482,9.3545572047712,9.472130522821,
9.49621907773396,9.5059188575557,9.51394201092931,9.52127052255671,9.52927707275944,
9.54859043813267,9.64010979152572,9.70678561614486,9.76949118288661,9.8148868318222,
9.82204284743874,9.82634158260985,9.82966314592016,9.83271634113912,9.83619805523396,
9.84112763116791,9.86117115424333,9.95401133408935),.UNSPECIFIED.);
#3489=B_SPLINE_CURVE_WITH_KNOTS('',3,(#74488,#74489,#74490,#74491,#74492,
#74493,#74494,#74495,#74496,#74497,#74498,#74499),.UNSPECIFIED.,.F.,.F.,
(4,1,1,1,1,1,1,1,1,4),(359.26521121538,359.614028467624,360.112799658286,
361.110342039611,362.107884420936,363.105426802261,363.604197992924,364.102969183586,
365.100511564911,365.54819074432),.UNSPECIFIED.);
#3490=B_SPLINE_CURVE_WITH_KNOTS('',3,(#74501,#74502,#74503,#74504,#74505,
#74506,#74507,#74508,#74509,#74510,#74511,#74512,#74513,#74514,#74515,#74516,
#74517,#74518),.UNSPECIFIED.,.F.,.F.,(4,2,2,2,2,2,2,2,4),(365.548432642184,
366.383313434454,367.218230346349,368.053147258244,368.888064170139,369.722981082033,
370.557897993928,371.392814905823,371.831581829739),.UNSPECIFIED.);
#3491=B_SPLINE_CURVE_WITH_KNOTS('',3,(#74520,#74521,#74522,#74523,#74524,
#74525,#74526,#74527,#74528,#74529,#74530,#74531,#74532,#74533,#74534,#74535),
 .UNSPECIFIED.,.F.,.F.,(4,2,2,2,2,2,2,4),(371.831581829739,372.666498741634,
373.501415653529,374.336332565424,375.171249477318,376.006166389213,376.841083301108,
376.991118430775),.UNSPECIFIED.);
#3492=B_SPLINE_CURVE_WITH_KNOTS('',3,(#74539,#74540,#74541,#74542,#74543,
#74544,#74545,#74546,#74547,#74548,#74549,#74550,#74551,#74552,#74553,#74554,
#74555,#74556,#74557,#74558,#74559,#74560,#74561,#74562,#74563,#74564,#74565,
#74566,#74567,#74568,#74569,#74570,#74571,#74572,#74573,#74574,#74575,#74576,
#74577,#74578,#74579,#74580,#74581,#74582,#74583,#74584,#74585,#74586,#74587,
#74588,#74589,#74590,#74591,#74592,#74593,#74594,#74595,#74596,#74597,#74598,
#74599,#74600,#74601,#74602,#74603,#74604,#74605,#74606,#74607,#74608,#74609,
#74610,#74611,#74612,#74613,#74614,#74615,#74616,#74617,#74618,#74619,#74620,
#74621,#74622,#74623,#74624,#74625,#74626,#74627,#74628,#74629,#74630,#74631,
#74632,#74633,#74634,#74635,#74636,#74637,#74638,#74639,#74640,#74641,#74642,
#74643,#74644,#74645,#74646,#74647,#74648,#74649,#74650,#74651,#74652,#74653,
#74654,#74655,#74656,#74657,#74658,#74659,#74660,#74661,#74662,#74663,#74664,
#74665,#74666,#74667,#74668,#74669,#74670,#74671,#74672,#74673,#74674,#74675,
#74676,#74677,#74678,#74679,#74680,#74681,#74682,#74683,#74684,#74685,#74686,
#74687,#74688,#74689,#74690,#74691,#74692,#74693,#74694,#74695,#74696,#74697,
#74698,#74699,#74700,#74701,#74702,#74703,#74704,#74705,#74706,#74707,#74708,
#74709,#74710),.UNSPECIFIED.,.F.,.F.,(4,3,3,3,3,3,3,3,3,3,3,3,3,3,3,3,3,
3,3,3,3,3,3,3,3,3,3,3,3,3,3,3,3,3,3,3,3,3,3,3,3,3,3,3,3,3,3,3,3,3,3,3,3,
3,3,3,3,4),(-379.066104903459,-378.984591704675,-378.90305453626,-378.819124330394,
-378.737584607012,-378.652459159905,-378.567333712797,-378.493243868417,
-378.41917720065,-378.345120941409,-378.271041497686,-378.196950707724,
-378.122805283221,-378.068562522134,-377.984413927215,-377.90024800538,
-377.816140290729,-377.732108414648,-377.648267189574,-377.569791331472,
-377.494854902038,-377.419925132161,-377.34499010411,-377.270011093797,
-377.195008711992,-377.119937164651,-377.071020140809,-376.995535332464,
-376.92010901322,-376.844728552861,-376.769381352133,-376.69405483498,-376.616482700543,
-376.541140898997,-376.46578071888,-376.390390754318,-376.311162505609,
-376.235638571276,-376.160060519903,-376.08438514796,-376.073477759484,
-376.000482344579,-375.927575454631,-375.854742076552,-375.781967271272,
-375.709236157044,-375.636533894427,-375.563831707361,-375.491125918639,
-375.418403117554,-375.345649881171,-375.272809217739,-375.199921024411,
-375.126920336245,-375.07593537816,-374.972030919384,-374.871429316071,
-374.800863543725),.UNSPECIFIED.);
#3493=B_SPLINE_CURVE_WITH_KNOTS('',3,(#74712,#74713,#74714,#74715,#74716,
#74717,#74718,#74719,#74720,#74721,#74722,#74723,#74724,#74725,#74726,#74727,
#74728,#74729),.UNSPECIFIED.,.F.,.F.,(4,2,2,2,2,2,2,2,4),(-374.800863543725,
-373.965946631831,-373.131029719936,-372.296112808041,-371.461195896146,
-370.626278984251,-369.791362072357,-368.956445160462,-368.517678236546),
 .UNSPECIFIED.);
#3494=B_SPLINE_CURVE_WITH_KNOTS('',3,(#74731,#74732,#74733,#74734,#74735,
#74736,#74737,#74738,#74739,#74740,#74741,#74742,#74743),.UNSPECIFIED.,
 .F.,.F.,(4,1,1,1,1,1,1,1,1,1,4),(-368.517678236546,-368.093138708885,-367.09559632756,
-366.596825136898,-366.098053946236,-365.599282755573,-365.100511564911,
-364.102969183586,-363.604197992923,-363.105426802261,-362.234492929366),
 .UNSPECIFIED.);
#3495=B_SPLINE_CURVE_WITH_KNOTS('',3,(#74745,#74746,#74747,#74748,#74749,
#74750,#74751,#74752,#74753,#74754,#74755,#74756,#74757,#74758),
 .UNSPECIFIED.,.F.,.F.,(4,1,1,1,1,1,1,1,1,1,1,4),(-362.234492929366,-362.107884420936,
-361.110342039611,-360.112799658286,-359.614028467624,-359.115257276961,
-358.616486086299,-358.117714895636,-357.120172514312,-356.621401323649,
-356.122630132987,-355.951307622187),.UNSPECIFIED.);
#3496=B_SPLINE_CURVE_WITH_KNOTS('',3,(#74760,#74761,#74762,#74763,#74764,
#74765,#74766,#74767,#74768,#74769,#74770,#74771),.UNSPECIFIED.,.F.,.F.,
(4,1,1,1,1,1,1,1,1,4),(-355.951307622187,-355.125087751662,-354.127545370337,
-353.130002989012,-352.631231798349,-352.132460607687,-351.633689417025,
-351.134918226362,-350.137375845037,-349.668188319012),.UNSPECIFIED.);
#3497=B_SPLINE_CURVE_WITH_KNOTS('',3,(#74773,#74774,#74775,#74776,#74777,
#74778,#74779,#74780,#74781,#74782,#74783,#74784,#74785,#74786,#74787,#74788,
#74789,#74790),.UNSPECIFIED.,.F.,.F.,(4,2,2,2,2,2,2,2,4),(-349.668100404495,
-348.833205403112,-347.998288491218,-347.163371579323,-346.328454667428,
-345.493537755533,-344.658620843638,-343.823703931743,-343.384937007828),
 .UNSPECIFIED.);
#3498=B_SPLINE_CURVE_WITH_KNOTS('',3,(#74792,#74793,#74794,#74795,#74796,
#74797,#74798,#74799,#74800,#74801,#74802,#74803,#74804,#74805,#74806,#74807,
#74808,#74809),.UNSPECIFIED.,.F.,.F.,(4,2,2,2,2,2,2,2,4),(-343.384937007828,
-342.550020095933,-341.715103184038,-340.880186272143,-340.045269360248,
-339.210352448353,-338.375435536458,-337.540518624564,-337.101751700648),
 .UNSPECIFIED.);
#3499=B_SPLINE_CURVE_WITH_KNOTS('',3,(#74811,#74812,#74813,#74814,#74815,
#74816,#74817,#74818,#74819,#74820,#74821,#74822,#74823,#74824,#74825,#74826,
#74827,#74828),.UNSPECIFIED.,.F.,.F.,(4,2,2,2,2,2,2,2,4),(-337.101751700648,
-336.266834788753,-335.431917876858,-334.597000964963,-333.762084053069,
-332.927167141174,-332.092250229279,-331.257333317384,-330.818566393468),
 .UNSPECIFIED.);
#3500=B_SPLINE_CURVE_WITH_KNOTS('',3,(#74830,#74831,#74832,#74833,#74834,
#74835,#74836,#74837,#74838,#74839,#74840,#74841,#74842,#74843,#74844,#74845,
#74846,#74847),.UNSPECIFIED.,.F.,.F.,(4,2,2,2,2,2,2,2,4),(-330.818566393468,
-329.983649481574,-329.148732569679,-328.313815657784,-327.478898745889,
-326.643981833994,-325.809064922099,-324.974148010204,-324.535381086289),
 .UNSPECIFIED.);
#3501=B_SPLINE_CURVE_WITH_KNOTS('',3,(#74849,#74850,#74851,#74852,#74853,
#74854,#74855,#74856,#74857,#74858,#74859,#74860),.UNSPECIFIED.,.F.,.F.,
(4,1,1,1,1,1,1,1,1,4),(-324.535381086289,-324.20127393059,-323.702502739928,
-323.203731549265,-322.20618916794,-321.707417977278,-321.208646786615,
-320.21110440529,-319.213562023966,-318.252195779109),.UNSPECIFIED.);
#3502=B_SPLINE_CURVE_WITH_KNOTS('',3,(#74862,#74863,#74864,#74865,#74866,
#74867,#74868,#74869,#74870,#74871,#74872,#74873,#74874,#74875,#74876),
 .UNSPECIFIED.,.F.,.F.,(4,2,1,1,1,1,1,1,1,1,1,4),(-318.252195779109,-318.216019642641,
-317.717248451978,-317.218477261316,-316.719706070653,-316.220934879991,
-315.223392498666,-314.724621308004,-314.225850117341,-313.228307736016,
-312.230765354691,-311.96901047193),.UNSPECIFIED.);
#3503=B_SPLINE_CURVE_WITH_KNOTS('',3,(#74878,#74879,#74880,#74881,#74882,
#74883,#74884,#74885,#74886,#74887,#74888,#74889,#74890,#74891,#74892,#74893,
#74894,#74895),.UNSPECIFIED.,.F.,.F.,(4,2,2,2,2,2,2,2,4),(-311.96901047193,
-311.134093560035,-310.29917664814,-309.464259736245,-308.62934282435,-307.794425912455,
-306.959509000561,-306.124592088666,-305.68582516475),.UNSPECIFIED.);
#3504=B_SPLINE_CURVE_WITH_KNOTS('',3,(#74897,#74898,#74899,#74900,#74901,
#74902,#74903,#74904,#74905,#74906,#74907,#74908,#74909),.UNSPECIFIED.,
 .F.,.F.,(4,1,1,1,1,1,1,1,1,1,4),(-305.68582516475,-305.247968685417,-304.250426304092,
-303.75165511343,-303.252883922767,-302.754112732105,-302.255341541442,
-301.257799160117,-300.759027969455,-300.260256778793,-299.402639857571),
 .UNSPECIFIED.);
#3505=B_SPLINE_CURVE_WITH_KNOTS('',3,(#74911,#74912,#74913,#74914,#74915,
#74916,#74917,#74918,#74919,#74920,#74921,#74922,#74923,#74924),
 .UNSPECIFIED.,.F.,.F.,(4,1,1,1,1,1,1,1,1,1,1,4),(-299.402639857571,-299.262714397468,
-298.265172016143,-297.267629634818,-296.768858444155,-296.270087253493,
-295.771316062831,-295.272544872168,-294.275002490843,-293.776231300181,
-293.277460109518,-293.119454550391),.UNSPECIFIED.);
#3506=B_SPLINE_CURVE_WITH_KNOTS('',3,(#74926,#74927,#74928,#74929,#74930,
#74931,#74932,#74933,#74934,#74935,#74936,#74937),.UNSPECIFIED.,.F.,.F.,
(4,1,1,1,1,1,1,1,1,4),(-293.119454550391,-292.279917728194,-291.282375346869,
-290.284832965544,-289.786061774881,-289.287290584219,-288.788519393556,
-288.289748202894,-287.292205821569,-286.836289777759),.UNSPECIFIED.);
#3507=B_SPLINE_CURVE_WITH_KNOTS('',3,(#74939,#74940,#74941,#74942,#74943,
#74944,#74945,#74946,#74947,#74948,#74949,#74950,#74951,#74952,#74953,#74954,
#74955,#74956),.UNSPECIFIED.,.F.,.F.,(4,2,2,2,2,2,2,2,4),(-286.836262713003,
-286.001352331317,-285.166435419422,-284.331518507527,-283.496601595632,
-282.661684683737,-281.826767771843,-280.991850859948,-280.553083936032),
 .UNSPECIFIED.);
#3508=B_SPLINE_CURVE_WITH_KNOTS('',3,(#74958,#74959,#74960,#74961,#74962,
#74963,#74964,#74965,#74966,#74967,#74968,#74969,#74970,#74971,#74972,#74973,
#74974,#74975),.UNSPECIFIED.,.F.,.F.,(4,2,2,2,2,2,2,2,4),(-280.553083936032,
-279.718167024137,-278.883250112242,-278.048333200347,-277.213416288452,
-276.378499376558,-275.543582464663,-274.708665552768,-274.269898628852),
 .UNSPECIFIED.);
#3509=B_SPLINE_CURVE_WITH_KNOTS('',3,(#74977,#74978,#74979,#74980,#74981,
#74982,#74983,#74984,#74985,#74986,#74987,#74988,#74989,#74990,#74991,#74992,
#74993,#74994),.UNSPECIFIED.,.F.,.F.,(4,2,2,2,2,2,2,2,4),(-274.269898628852,
-273.434981716958,-272.600064805063,-271.765147893168,-270.930230981273,
-270.095314069378,-269.260397157483,-268.425480245589,-267.986713321673),
 .UNSPECIFIED.);
#3510=B_SPLINE_CURVE_WITH_KNOTS('',3,(#74996,#74997,#74998,#74999,#75000,
#75001,#75002,#75003,#75004,#75005,#75006,#75007,#75008,#75009,#75010,#75011,
#75012,#75013),.UNSPECIFIED.,.F.,.F.,(4,2,2,2,2,2,2,2,4),(-267.986713321673,
-267.151796409778,-266.316879497883,-265.481962585988,-264.647045674093,
-263.812128762198,-262.977211850304,-262.142294938409,-261.703528014493),
 .UNSPECIFIED.);
#3511=B_SPLINE_CURVE_WITH_KNOTS('',3,(#75015,#75016,#75017,#75018,#75019,
#75020,#75021,#75022,#75023,#75024,#75025,#75026),.UNSPECIFIED.,.F.,.F.,
(4,1,1,1,1,1,1,1,1,4),(-261.703528014493,-261.356103907122,-260.857332716459,
-260.358561525797,-259.361019144472,-258.86224795381,-258.363476763147,
-257.365934381822,-256.368392000497,-255.420342707314),.UNSPECIFIED.);
#3512=B_SPLINE_CURVE_WITH_KNOTS('',3,(#75028,#75029,#75030,#75031,#75032,
#75033,#75034,#75035,#75036,#75037,#75038,#75039,#75040,#75041,#75042),
 .UNSPECIFIED.,.F.,.F.,(4,2,1,1,1,1,1,1,1,1,1,4),(-255.420342707314,-255.370849619172,
-254.87207842851,-254.373307237848,-253.874536047185,-253.375764856523,
-252.378222475198,-251.879451284535,-251.380680093873,-250.383137712548,
-249.385595331223,-249.137157400134),.UNSPECIFIED.);
#3513=B_SPLINE_CURVE_WITH_KNOTS('',3,(#75044,#75045,#75046,#75047,#75048,
#75049,#75050,#75051,#75052,#75053,#75054,#75055,#75056,#75057,#75058,#75059,
#75060,#75061),.UNSPECIFIED.,.F.,.F.,(4,2,2,2,2,2,2,2,4),(-249.137157400134,
-248.302240488239,-247.467323576344,-246.632406664449,-245.797489752555,
-244.96257284066,-244.127655928765,-243.29273901687,-242.853972092955),
 .UNSPECIFIED.);
#3514=B_SPLINE_CURVE_WITH_KNOTS('',3,(#75063,#75064,#75065,#75066,#75067,
#75068,#75069,#75070,#75071,#75072,#75073,#75074,#75075),.UNSPECIFIED.,
 .F.,.F.,(4,1,1,1,1,1,1,1,1,1,4),(-242.853972092955,-242.402798661949,-241.405256280624,
-240.906485089962,-240.407713899299,-239.908942708637,-239.410171517974,
-238.412629136649,-237.913857945987,-237.415086755324,-236.570786785775),
 .UNSPECIFIED.);
#3515=B_SPLINE_CURVE_WITH_KNOTS('',3,(#75077,#75078,#75079,#75080,#75081,
#75082,#75083,#75084,#75085,#75086,#75087,#75088,#75089,#75090),
 .UNSPECIFIED.,.F.,.F.,(4,1,1,1,1,1,1,1,1,1,1,4),(-236.570786785775,-236.417544374,
-235.420001992675,-234.42245961135,-233.923688420687,-233.424917230025,
-232.926146039362,-232.4273748487,-231.429832467375,-230.931061276713,-230.43229008605,
-230.287601478595),.UNSPECIFIED.);
#3516=B_SPLINE_CURVE_WITH_KNOTS('',3,(#75092,#75093,#75094,#75095,#75096,
#75097,#75098,#75099,#75100,#75101,#75102,#75103),.UNSPECIFIED.,.F.,.F.,
(4,1,1,1,1,1,1,1,1,4),(-230.287601478595,-229.434747704725,-228.4372053234,
-227.439662942076,-226.940891751413,-226.442120560751,-225.943349370088,
-225.444578179426,-224.447035798101,-224.004416171416),.UNSPECIFIED.);
#3517=B_SPLINE_CURVE_WITH_KNOTS('',3,(#75105,#75106,#75107,#75108,#75109,
#75110,#75111,#75112,#75113,#75114,#75115,#75116,#75117,#75118,#75119,#75120,
#75121,#75122),.UNSPECIFIED.,.F.,.F.,(4,2,2,2,2,2,2,2,4),(-224.004416171416,
-223.169499259521,-222.334582347626,-221.499665435731,-220.664748523836,
-219.829831611942,-218.994914700047,-218.159997788152,-217.721230864236),
 .UNSPECIFIED.);
#3518=B_SPLINE_CURVE_WITH_KNOTS('',3,(#75124,#75125,#75126,#75127,#75128,
#75129,#75130,#75131,#75132,#75133,#75134,#75135,#75136,#75137,#75138,#75139,
#75140,#75141),.UNSPECIFIED.,.F.,.F.,(4,2,2,2,2,2,2,2,4),(-217.721230864236,
-216.886313952342,-216.051397040447,-215.216480128552,-214.381563216657,
-213.546646304762,-212.711729392867,-211.876812480973,-211.438045557057),
 .UNSPECIFIED.);
#3519=B_SPLINE_CURVE_WITH_KNOTS('',3,(#75143,#75144,#75145,#75146,#75147,
#75148,#75149,#75150,#75151,#75152,#75153,#75154,#75155,#75156,#75157,#75158,
#75159,#75160),.UNSPECIFIED.,.F.,.F.,(4,2,2,2,2,2,2,2,4),(-211.438045557057,
-210.603128645162,-209.768211733267,-208.933294821372,-208.098377909478,
-207.263460997583,-206.428544085688,-205.593627173793,-205.154860249877),
 .UNSPECIFIED.);
#3520=B_SPLINE_CURVE_WITH_KNOTS('',3,(#75162,#75163,#75164,#75165,#75166,
#75167,#75168,#75169,#75170,#75171,#75172,#75173,#75174,#75175,#75176,#75177,
#75178,#75179),.UNSPECIFIED.,.F.,.F.,(4,2,2,2,2,2,2,2,4),(-205.154860249877,
-204.319943337982,-203.485026426088,-202.650109514193,-201.815192602298,
-200.980275690403,-200.145358778508,-199.310441866613,-198.871674942698),
 .UNSPECIFIED.);
#3521=B_SPLINE_CURVE_WITH_KNOTS('',3,(#75181,#75182,#75183,#75184,#75185,
#75186,#75187,#75188,#75189,#75190,#75191,#75192),.UNSPECIFIED.,.F.,.F.,
(4,1,1,1,1,1,1,1,1,4),(-198.871674942698,-198.510933883654,-198.012162692991,
-197.513391502329,-196.515849121004,-196.017077930341,-195.518306739679,
-194.520764358354,-193.523221977029,-192.588489635518),.UNSPECIFIED.);
#3522=B_SPLINE_CURVE_WITH_KNOTS('',3,(#75194,#75195,#75196,#75197,#75198,
#75199,#75200,#75201,#75202,#75203,#75204,#75205,#75206,#75207),
 .UNSPECIFIED.,.F.,.F.,(4,1,1,1,1,1,1,1,1,1,1,4),(-192.588489635518,-192.525679595704,
-191.528137214379,-190.530594833054,-190.031823642392,-189.53305245173,
-188.535510070405,-188.036738879742,-187.53796768908,-187.039196498417,
-186.540425307755,-186.305304328339),.UNSPECIFIED.);
#3523=B_SPLINE_CURVE_WITH_KNOTS('',3,(#75209,#75210,#75211,#75212,#75213,
#75214,#75215,#75216,#75217,#75218,#75219,#75220,#75221),.UNSPECIFIED.,
 .F.,.F.,(4,1,1,1,1,1,1,1,1,1,4),(-186.305304328339,-185.54288292643,-184.545340545105,
-183.54779816378,-183.049026973118,-182.550255782455,-181.55271340113,-181.053942210468,
-180.555171019806,-180.056399829143,-180.022119021159),.UNSPECIFIED.);
#3524=B_SPLINE_CURVE_WITH_KNOTS('',3,(#75223,#75224,#75225,#75226,#75227,
#75228,#75229,#75230,#75231,#75232,#75233,#75234,#75235,#75236,#75237,#75238,
#75239,#75240),.UNSPECIFIED.,.F.,.F.,(4,2,2,2,2,2,2,2,4),(-180.022119021159,
-179.187202109264,-178.352285197369,-177.517368285475,-176.68245137358,
-175.847534461685,-175.01261754979,-174.177700637896,-173.738933713979),
 .UNSPECIFIED.);
#3525=B_SPLINE_CURVE_WITH_KNOTS('',3,(#75242,#75243,#75244,#75245,#75246,
#75247,#75248,#75249,#75250,#75251,#75252,#75253,#75254,#75255,#75256,#75257,
#75258,#75259),.UNSPECIFIED.,.F.,.F.,(4,2,2,2,2,2,2,2,4),(-173.738933713979,
-172.904016802084,-172.06909989019,-171.234182978295,-170.3992660664,-169.564349154505,
-168.72943224261,-167.894515330715,-167.4557484068),.UNSPECIFIED.);
#3526=B_SPLINE_CURVE_WITH_KNOTS('',3,(#75261,#75262,#75263,#75264,#75265,
#75266,#75267,#75268,#75269,#75270,#75271,#75272,#75273,#75274,#75275,#75276,
#75277,#75278),.UNSPECIFIED.,.F.,.F.,(4,2,2,2,2,2,2,2,4),(-167.4557484068,
-166.620831494905,-165.78591458301,-164.950997671115,-164.116080759221,
-163.281163847326,-162.446246935431,-161.611330023536,-161.172570307997),
 .UNSPECIFIED.);
#3527=B_SPLINE_CURVE_WITH_KNOTS('',3,(#75280,#75281,#75282,#75283,#75284,
#75285,#75286,#75287,#75288,#75289,#75290,#75291,#75292,#75293,#75294,#75295,
#75296,#75297,#75298,#75299,#75300,#75301,#75302,#75303,#75304,#75305,#75306,
#75307,#75308,#75309,#75310,#75311,#75312,#75313,#75314,#75315,#75316,#75317,
#75318,#75319,#75320,#75321,#75322,#75323,#75324,#75325,#75326,#75327,#75328,
#75329,#75330,#75331,#75332,#75333,#75334,#75335,#75336,#75337,#75338,#75339,
#75340,#75341,#75342,#75343,#75344,#75345,#75346,#75347,#75348,#75349,#75350,
#75351,#75352,#75353,#75354,#75355,#75356,#75357,#75358,#75359,#75360,#75361,
#75362,#75363,#75364,#75365,#75366,#75367,#75368,#75369,#75370,#75371,#75372,
#75373,#75374,#75375,#75376,#75377,#75378,#75379,#75380,#75381,#75382,#75383,
#75384,#75385,#75386,#75387,#75388,#75389,#75390,#75391,#75392,#75393,#75394,
#75395,#75396,#75397,#75398,#75399,#75400,#75401,#75402,#75403,#75404,#75405,
#75406,#75407,#75408,#75409,#75410,#75411,#75412,#75413,#75414,#75415,#75416,
#75417,#75418,#75419,#75420,#75421,#75422,#75423,#75424,#75425,#75426,#75427,
#75428,#75429,#75430,#75431,#75432,#75433,#75434,#75435,#75436,#75437,#75438,
#75439,#75440,#75441,#75442,#75443,#75444,#75445,#75446,#75447,#75448,#75449,
#75450,#75451,#75452,#75453,#75454,#75455,#75456,#75457,#75458,#75459,#75460,
#75461,#75462,#75463,#75464,#75465,#75466,#75467,#75468,#75469,#75470,#75471,
#75472,#75473,#75474,#75475,#75476,#75477,#75478,#75479,#75480,#75481,#75482,
#75483,#75484,#75485,#75486,#75487,#75488,#75489,#75490,#75491,#75492,#75493,
#75494,#75495,#75496,#75497,#75498,#75499,#75500,#75501,#75502),
 .UNSPECIFIED.,.F.,.F.,(4,3,3,3,3,3,3,3,3,3,3,3,3,3,3,3,3,3,3,3,3,3,3,3,
3,3,3,3,3,3,3,3,3,3,3,3,3,3,3,3,3,3,3,3,3,3,3,3,3,3,3,3,3,3,3,3,3,3,3,3,
3,3,3,3,3,3,3,3,3,3,3,3,3,3,4),(-161.172534268608,-161.076875819595,-160.980846673946,
-160.8848438716,-160.789080703855,-160.693626747646,-160.605015379132,-160.510966660752,
-160.462380492166,-160.400013339945,-160.337646187725,-160.179613361151,
-160.105498696632,-159.942312798227,-159.774631179198,-159.60694956017,
-159.502729275831,-159.390898384637,-159.276901723327,-159.160779303066,
-159.108140809998,-158.992014088384,-158.877377248298,-158.767600041595,
-158.667812363936,-158.60923644261,-158.511423045628,-158.413466381551,
-158.315490462468,-158.250353907988,-158.160753613792,-158.071253574473,
-157.982706110331,-157.896329266241,-157.832895452041,-157.737989653359,
-157.644824200271,-157.612044871271,-157.517597734643,-157.422345400126,
-157.327747638583,-157.251013998931,-157.176302298935,-157.101083416223,
-157.02585745876,-156.997978540146,-156.920734393649,-156.843609945958,
-156.766681221241,-156.689979154557,-156.614102931111,-156.53741871234,
-156.461002677123,-156.416097087036,-156.34345143238,-156.270329100991,
-156.196539751135,-156.163061628251,-156.065396634053,-155.967246292825,
-155.868970620973,-155.770933922614,-155.673436224496,-155.616863151268,
-155.52069496055,-155.461230458469,-155.401501838647,-155.341815438617,
-155.328144716356,-155.234430212384,-155.139022723453,-155.118013022302,
-155.022163018909,-154.927201558076,-154.889377792441),.UNSPECIFIED.);
#3528=B_SPLINE_CURVE_WITH_KNOTS('',3,(#75504,#75505,#75506,#75507,#75508,
#75509,#75510,#75511,#75512,#75513,#75514,#75515,#75516),.UNSPECIFIED.,
 .F.,.F.,(4,1,1,1,1,1,1,1,1,1,4),(-154.889377792441,-154.619069105358,-153.621526724033,
-153.122755533371,-152.623984342709,-152.125213152046,-151.626441961384,
-150.628899580059,-149.631357198734,-148.633814817409,-148.60619306022),
 .UNSPECIFIED.);
#3529=B_SPLINE_CURVE_WITH_KNOTS('',3,(#75518,#75519,#75520,#75521,#75522,
#75523,#75524,#75525,#75526,#75527,#75528,#75529,#75530,#75531,#75532,#75533,
#75534,#75535,#75536,#75537,#75538,#75539,#75540,#75541,#75542,#75543,#75544,
#75545,#75546,#75547,#75548,#75549,#75550,#75551,#75552,#75553,#75554,#75555,
#75556,#75557,#75558,#75559,#75560,#75561,#75562,#75563,#75564,#75565,#75566,
#75567,#75568,#75569,#75570,#75571,#75572,#75573,#75574,#75575,#75576,#75577,
#75578,#75579,#75580,#75581,#75582,#75583,#75584,#75585,#75586,#75587,#75588,
#75589,#75590,#75591,#75592,#75593,#75594,#75595,#75596,#75597,#75598,#75599,
#75600,#75601,#75602,#75603,#75604,#75605,#75606,#75607,#75608,#75609,#75610,
#75611,#75612,#75613,#75614,#75615,#75616,#75617,#75618,#75619,#75620,#75621,
#75622,#75623,#75624,#75625,#75626,#75627,#75628,#75629,#75630,#75631,#75632,
#75633,#75634,#75635,#75636,#75637,#75638,#75639,#75640,#75641,#75642,#75643,
#75644,#75645,#75646,#75647,#75648,#75649,#75650,#75651,#75652,#75653,#75654,
#75655,#75656,#75657,#75658,#75659,#75660,#75661,#75662,#75663,#75664,#75665,
#75666,#75667,#75668,#75669,#75670,#75671,#75672,#75673,#75674,#75675,#75676,
#75677,#75678,#75679,#75680,#75681,#75682,#75683,#75684,#75685,#75686,#75687,
#75688,#75689,#75690,#75691,#75692,#75693,#75694,#75695,#75696,#75697,#75698,
#75699,#75700,#75701,#75702,#75703,#75704,#75705,#75706,#75707,#75708,#75709,
#75710,#75711,#75712,#75713,#75714,#75715,#75716,#75717,#75718,#75719,#75720,
#75721,#75722,#75723,#75724,#75725,#75726,#75727,#75728,#75729,#75730,#75731,
#75732,#75733,#75734,#75735,#75736,#75737,#75738,#75739,#75740,#75741,#75742,
#75743,#75744,#75745,#75746,#75747,#75748,#75749,#75750,#75751,#75752,#75753,
#75754,#75755,#75756,#75757,#75758,#75759,#75760,#75761,#75762,#75763,#75764,
#75765,#75766,#75767,#75768,#75769,#75770,#75771,#75772,#75773),
 .UNSPECIFIED.,.F.,.F.,(4,3,3,3,3,3,3,3,3,3,3,3,3,3,3,3,3,3,3,3,3,3,3,3,
3,3,3,3,3,3,3,3,3,3,3,3,3,3,3,3,3,3,3,3,3,3,3,3,3,3,3,3,3,3,3,3,3,3,3,3,
3,3,3,3,3,3,3,3,3,3,3,3,3,3,3,3,3,3,3,3,3,3,3,3,3,4),(-148.606192485261,
-148.52636985924,-148.446664288587,-148.367133225438,-148.28770796962,-148.208444972183,
-148.135043626747,-148.0606272344,-147.986194073281,-147.911731880879,-147.837187945428,
-147.762599626954,-147.687907200668,-147.636272436084,-147.559696613986,
-147.4831882777,-147.406736485885,-147.330330337391,-147.253958963917,-147.177055350273,
-147.100712852782,-147.024370810536,-146.948019377498,-146.870697046813,
-146.794272879664,-146.716501467211,-146.638730054759,-146.564937988792,
-146.491208130101,-146.417527418265,-146.343882020907,-146.270258073095,
-146.196630007403,-146.139958864097,-146.058532398256,-145.976971104177,
-145.893025246491,-145.811191737305,-145.72618970537,-145.641187673434,
-145.562754040429,-145.484389989058,-145.40609068352,-145.327870109342,
-145.249699364303,-145.171586345936,-145.142416482772,-145.066046455012,
-144.989659575864,-144.913246274884,-144.836764235035,-144.760244856203,
-144.683643532744,-144.643645292109,-144.568258913417,-144.492933936661,
-144.417657553264,-144.342416987077,-144.267199486563,-144.189562414591,
-144.114334645603,-144.039090151388,-143.963817374849,-143.888504745606,
-143.813103168631,-143.737648898478,-143.662096729519,-143.646102910784,
-143.5729448966,-143.49987550463,-143.42687980634,-143.353942942787,-143.281050109155,
-143.2081865408,-143.135324030541,-143.062458463952,-142.989576498397,-142.916664780578,
-142.843667394008,-142.770623161723,-142.697468924523,-142.64856052946,
-142.555235922819,-142.462568780342,-142.371289963649,-142.323007313817),
 .UNSPECIFIED.);
#3530=B_SPLINE_CURVE_WITH_KNOTS('',3,(#75775,#75776,#75777,#75778,#75779,
#75780,#75781,#75782,#75783,#75784,#75785,#75786,#75787),.UNSPECIFIED.,
 .F.,.F.,(4,1,1,1,1,1,1,1,1,1,4),(-142.323007178082,-141.651018148135,-141.152246957472,
-140.65347576681,-139.655933385485,-139.157162194822,-138.65839100416,-138.159619813498,
-137.660848622835,-136.66330624151,-136.039821870902),.UNSPECIFIED.);
#3531=B_SPLINE_CURVE_WITH_KNOTS('',3,(#75789,#75790,#75791,#75792,#75793,
#75794,#75795,#75796,#75797,#75798,#75799,#75800,#75801),.UNSPECIFIED.,
 .F.,.F.,(4,1,1,1,1,1,1,1,1,1,4),(-136.039821870902,-135.665763860185,-134.66822147886,
-134.169450288198,-133.670679097536,-132.673136716211,-132.174365525548,
-131.675594334886,-131.176823144223,-130.678051953561,-129.756636563722),
 .UNSPECIFIED.);
#3532=B_SPLINE_CURVE_WITH_KNOTS('',3,(#75803,#75804,#75805,#75806,#75807,
#75808,#75809,#75810,#75811,#75812,#75813,#75814,#75815,#75816,#75817),
 .UNSPECIFIED.,.F.,.F.,(4,2,1,1,1,1,1,1,1,1,1,4),(-129.756636563722,-129.680509572236,
-128.682967190911,-127.685424809586,-127.186653618924,-126.687882428261,
-125.690340046936,-125.191568856274,-124.692797665612,-124.194026474949,
-123.695255284287,-123.473451256543),.UNSPECIFIED.);
#3533=B_SPLINE_CURVE_WITH_KNOTS('',3,(#75819,#75820,#75821,#75822,#75823,
#75824,#75825,#75826,#75827,#75828,#75829,#75830,#75831),.UNSPECIFIED.,
 .F.,.F.,(4,1,1,1,1,1,1,1,1,1,4),(-123.473451256543,-122.697712902962,-121.700170521637,
-120.702628140312,-120.20385694965,-119.705085758987,-118.707543377662,
-118.208772187,-117.710000996337,-117.211229805675,-117.190265949363),
 .UNSPECIFIED.);
#3534=B_SPLINE_CURVE_WITH_KNOTS('',3,(#75833,#75834,#75835,#75836,#75837,
#75838,#75839,#75840,#75841,#75842,#75843,#75844,#75845,#75846,#75847,#75848,
#75849,#75850),.UNSPECIFIED.,.F.,.F.,(4,2,2,2,2,2,2,2,4),(-117.190265949363,
-116.355349037468,-115.520432125574,-114.685515213679,-113.850598301784,
-113.015681389889,-112.180764477994,-111.345847566099,-110.907080642184),
 .UNSPECIFIED.);
#3535=B_SPLINE_CURVE_WITH_KNOTS('',3,(#75852,#75853,#75854,#75855,#75856,
#75857,#75858,#75859,#75860,#75861,#75862,#75863,#75864,#75865,#75866,#75867,
#75868,#75869),.UNSPECIFIED.,.F.,.F.,(4,2,2,2,2,2,2,2,4),(-110.907080642184,
-110.072163730289,-109.237246818394,-108.402329906499,-107.567412994604,
-106.732496082709,-105.897579170815,-105.06266225892,-104.623895335004),
 .UNSPECIFIED.);
#3536=B_SPLINE_CURVE_WITH_KNOTS('',3,(#75871,#75872,#75873,#75874,#75875,
#75876,#75877,#75878,#75879,#75880,#75881,#75882,#75883,#75884,#75885,#75886,
#75887,#75888),.UNSPECIFIED.,.F.,.F.,(4,2,2,2,2,2,2,2,4),(-104.623895335004,
-103.788978423109,-102.954061511214,-102.119144599319,-101.284227687425,
-100.44931077553,-99.6143938636348,-98.7794769517399,-98.3407182225155),
 .UNSPECIFIED.);
#3537=B_SPLINE_CURVE_WITH_KNOTS('',3,(#75890,#75891,#75892,#75893,#75894,
#75895,#75896,#75897,#75898,#75899,#75900,#75901,#75902,#75903,#75904,#75905,
#75906,#75907,#75908,#75909,#75910,#75911,#75912,#75913,#75914,#75915,#75916,
#75917,#75918,#75919,#75920,#75921,#75922,#75923,#75924,#75925,#75926,#75927,
#75928,#75929,#75930,#75931,#75932,#75933,#75934,#75935,#75936,#75937,#75938,
#75939,#75940,#75941,#75942,#75943,#75944,#75945,#75946,#75947,#75948,#75949,
#75950,#75951,#75952,#75953,#75954,#75955,#75956,#75957,#75958,#75959,#75960,
#75961,#75962,#75963,#75964,#75965,#75966,#75967,#75968,#75969,#75970,#75971,
#75972,#75973,#75974,#75975,#75976,#75977,#75978,#75979,#75980,#75981,#75982,
#75983,#75984,#75985,#75986,#75987,#75988,#75989,#75990,#75991,#75992,#75993,
#75994,#75995,#75996,#75997,#75998,#75999,#76000,#76001,#76002,#76003,#76004,
#76005,#76006,#76007,#76008,#76009,#76010,#76011,#76012,#76013,#76014,#76015,
#76016,#76017,#76018,#76019,#76020,#76021,#76022,#76023,#76024,#76025,#76026,
#76027,#76028,#76029,#76030,#76031,#76032,#76033,#76034,#76035,#76036,#76037,
#76038,#76039,#76040,#76041,#76042,#76043,#76044,#76045,#76046,#76047,#76048,
#76049,#76050,#76051,#76052,#76053,#76054,#76055,#76056,#76057,#76058,#76059,
#76060,#76061,#76062,#76063,#76064,#76065,#76066,#76067,#76068,#76069,#76070,
#76071,#76072,#76073,#76074,#76075,#76076,#76077,#76078,#76079,#76080,#76081,
#76082,#76083,#76084,#76085,#76086,#76087,#76088,#76089,#76090,#76091,#76092,
#76093,#76094,#76095,#76096,#76097,#76098,#76099,#76100,#76101,#76102,#76103,
#76104,#76105,#76106,#76107,#76108,#76109,#76110,#76111,#76112,#76113,#76114,
#76115),.UNSPECIFIED.,.F.,.F.,(4,3,3,3,3,3,3,3,3,3,3,3,3,3,3,3,3,3,3,3,
3,3,3,3,3,3,3,3,3,3,3,3,3,3,3,3,3,3,3,3,3,3,3,3,3,3,3,3,3,3,3,3,3,3,3,3,
3,3,3,3,3,3,3,3,3,3,3,3,3,3,3,3,3,3,3,4),(-98.3406829019419,-98.2437434225405,
-98.1464170814034,-98.0490921798296,-97.952002419303,-97.8552294380063,
-97.7598399901283,-97.6646221079338,-97.6235044607133,-97.5640891355954,
-97.5057931159296,-97.3426521359185,-97.2603547490666,-97.0941106891489,
-96.9279359782203,-96.7712320269567,-96.7617612672917,-96.6708762040348,
-96.5585454252642,-96.4438414670671,-96.3267705129137,-96.2629476276435,
-96.1459381539855,-96.0305291061737,-95.9199121328771,-95.8359592921399,
-95.7640576214475,-95.6654509547965,-95.566675161101,-95.4678165237561,
-95.4185008361925,-95.3290566577505,-95.2394267731222,-95.1506720310447,
-95.0641128465456,-95.0010423802451,-94.9076334079712,-94.8159559204494,
-94.7668960523893,-94.6740601804583,-94.5804783923981,-94.487591502431,
-94.4191609271352,-94.3450524977225,-94.2703865386836,-94.1955565765706,
-94.1661254683502,-94.0887540337746,-94.0088013892139,-93.9316962686835,
-93.854758696316,-93.7779778643584,-93.768943455532,-93.6921690976646,-93.6157128298723,
-93.5842440152404,-93.5061151209651,-93.4272088502916,-93.3472535258137,
-93.3312085564554,-93.2277417440618,-93.1234262934822,-93.0189022010898,
-92.9146773684954,-92.8109975883665,-92.7717831578707,-92.6695455287042,
-92.5794481812869,-92.5275488857113,-92.4962916445605,-92.4021323038907,
-92.3061118569842,-92.2728410231873,-92.1763014953801,-92.0805228281303,
-92.0575247206449),.UNSPECIFIED.);
#3538=B_SPLINE_CURVE_WITH_KNOTS('',3,(#76117,#76118,#76119,#76120,#76121,
#76122,#76123,#76124,#76125,#76126,#76127,#76128,#76129),.UNSPECIFIED.,
 .F.,.F.,(4,1,1,1,1,1,1,1,1,1,4),(-92.0575247206449,-91.7738990818901,-90.7763567005652,
-90.2775855099027,-89.7788143192403,-89.2800431285779,-88.7812719379154,
-87.7837295565905,-86.7861871752656,-85.7886447939407,-85.7743411505574),
 .UNSPECIFIED.);
#3539=B_SPLINE_CURVE_WITH_KNOTS('',3,(#76131,#76132,#76133,#76134,#76135,
#76136,#76137,#76138,#76139,#76140,#76141,#76142,#76143,#76144,#76145,#76146,
#76147,#76148,#76149,#76150,#76151,#76152,#76153,#76154,#76155,#76156,#76157,
#76158,#76159,#76160,#76161,#76162,#76163,#76164,#76165,#76166,#76167,#76168,
#76169,#76170,#76171,#76172,#76173,#76174,#76175,#76176,#76177,#76178,#76179,
#76180,#76181,#76182,#76183,#76184,#76185,#76186,#76187,#76188,#76189,#76190,
#76191,#76192,#76193,#76194,#76195,#76196,#76197,#76198,#76199,#76200,#76201,
#76202,#76203,#76204,#76205,#76206,#76207,#76208,#76209,#76210,#76211,#76212,
#76213,#76214,#76215,#76216,#76217,#76218,#76219,#76220,#76221,#76222,#76223,
#76224,#76225,#76226,#76227,#76228,#76229,#76230,#76231,#76232,#76233,#76234,
#76235,#76236,#76237,#76238,#76239,#76240,#76241,#76242,#76243,#76244,#76245,
#76246,#76247,#76248,#76249,#76250,#76251,#76252,#76253,#76254,#76255,#76256,
#76257,#76258,#76259,#76260,#76261,#76262,#76263,#76264,#76265,#76266,#76267,
#76268,#76269,#76270,#76271,#76272,#76273,#76274,#76275,#76276,#76277,#76278,
#76279,#76280,#76281,#76282,#76283,#76284,#76285,#76286,#76287,#76288,#76289,
#76290,#76291,#76292,#76293,#76294,#76295,#76296,#76297,#76298,#76299,#76300,
#76301,#76302,#76303,#76304,#76305,#76306,#76307,#76308,#76309,#76310,#76311,
#76312,#76313,#76314,#76315,#76316,#76317,#76318,#76319,#76320,#76321,#76322,
#76323,#76324,#76325,#76326,#76327,#76328,#76329,#76330,#76331,#76332,#76333,
#76334,#76335,#76336,#76337,#76338,#76339,#76340,#76341,#76342,#76343,#76344,
#76345,#76346,#76347,#76348,#76349,#76350,#76351,#76352,#76353,#76354,#76355,
#76356,#76357,#76358,#76359,#76360,#76361,#76362,#76363,#76364,#76365,#76366,
#76367,#76368,#76369,#76370,#76371,#76372,#76373,#76374,#76375,#76376,#76377,
#76378,#76379,#76380,#76381,#76382,#76383,#76384,#76385,#76386),
 .UNSPECIFIED.,.F.,.F.,(4,3,3,3,3,3,3,3,3,3,3,3,3,3,3,3,3,3,3,3,3,3,3,3,
3,3,3,3,3,3,3,3,3,3,3,3,3,3,3,3,3,3,3,3,3,3,3,3,3,3,3,3,3,3,3,3,3,3,3,3,
3,3,3,3,3,3,3,3,3,3,3,3,3,3,3,3,3,3,3,3,3,3,3,3,3,4),(-85.7743394134653,
-85.6939733990312,-85.6137248761189,-85.5327620579087,-85.4528102675906,
-85.3713419354345,-85.2898736032783,-85.2154572109321,-85.1410240498145,
-85.0665618574138,-84.9920179219637,-84.9174296034911,-84.8427371772053,
-84.7911024126159,-84.7145265905183,-84.6380182542315,-84.5615664624167,
-84.4851603139229,-84.4087889404489,-84.3318853268042,-84.2555428293141,
-84.1792007870672,-84.1028493540296,-84.0255270233449,-83.9491028561956,
-83.8713314437433,-83.793560031291,-83.7197679653234,-83.6460381066311,
-83.572357394795,-83.4987119974357,-83.425088049623,-83.3514599839301,-83.2947888406285,
-83.213362374789,-83.1318010807113,-83.047855223025,-82.9660217138412,-82.8810196819036,
-82.7960176499661,-82.7175840169603,-82.6392199655877,-82.5609206600491,
-82.4827000858693,-82.4045293408292,-82.3264163224614,-82.2972464593036,
-82.2208764315444,-82.1444895523973,-82.0680762514176,-81.9915942115689,
-81.9150748327382,-81.8384735092794,-81.7984752686412,-81.7230888899497,
-81.6477639131932,-81.5724875297967,-81.4972469636097,-81.4220294630957,
-81.3443923911233,-81.269164622136,-81.193920127921,-81.1186473513818,-81.0433347221388,
-80.9679331451636,-80.8924788750111,-80.8169267060524,-80.8009328873163,
-80.7277748731317,-80.6547054811617,-80.5817097828716,-80.5087729193186,
-80.4358800856856,-80.3630165173305,-80.2901540070714,-80.2172884404815,
-80.1444064749265,-80.0714947571072,-79.9984973705371,-79.9254531382524,
-79.8522989010521,-79.8033905059914,-79.7082675746029,-79.6139520835005,
-79.5212737556616,-79.4911542246076),.UNSPECIFIED.);
#3540=B_SPLINE_CURVE_WITH_KNOTS('',3,(#76388,#76389,#76390,#76391,#76392,
#76393,#76394,#76395,#76396,#76397,#76398,#76399,#76400),.UNSPECIFIED.,
 .F.,.F.,(4,1,1,1,1,1,1,1,1,1,4),(-79.4911541062857,-78.8058481246665,-78.3070769340041,
-77.8083057433416,-76.8107633620167,-76.3119921713543,-75.8132209806918,
-75.3144497900294,-74.8156785993669,-73.818136218042,-73.2079687991061),
 .UNSPECIFIED.);
#3541=B_SPLINE_CURVE_WITH_KNOTS('',3,(#76402,#76403,#76404,#76405,#76406,
#76407,#76408,#76409,#76410,#76411,#76412,#76413,#76414),.UNSPECIFIED.,
 .F.,.F.,(4,1,1,1,1,1,1,1,1,1,4),(-73.2079687991061,-72.8205938367171,-71.8230514553922,
-71.3242802647298,-70.8255090740674,-69.8279666927425,-69.32919550208,-68.8304243114176,
-68.3316531207551,-67.8328819300927,-66.9247834919265),.UNSPECIFIED.);
#3542=B_SPLINE_CURVE_WITH_KNOTS('',3,(#76416,#76417,#76418,#76419,#76420,
#76421,#76422,#76423,#76424,#76425,#76426,#76427,#76428,#76429),
 .UNSPECIFIED.,.F.,.F.,(4,1,1,1,1,1,1,1,1,1,1,4),(-66.9247834919265,-66.8353395487678,
-65.8377971674429,-64.840254786118,-64.3414835954556,-63.8427124047931,
-62.8451700234682,-62.3463988328058,-61.8476276421433,-61.3488564514809,
-60.8500852608184,-60.6415981847469),.UNSPECIFIED.);
#3543=B_SPLINE_CURVE_WITH_KNOTS('',3,(#76431,#76432,#76433,#76434,#76435,
#76436,#76437,#76438,#76439,#76440,#76441,#76442,#76443),.UNSPECIFIED.,
 .F.,.F.,(4,1,1,1,1,1,1,1,1,1,4),(-60.6415981847469,-59.8525428794935,-58.8550004981687,
-57.8574581168438,-57.3586869261813,-56.8599157355189,-55.862373354194,
-55.3636021635315,-54.8648309728691,-54.3660597822066,-54.3584128775673),
 .UNSPECIFIED.);
#3544=B_SPLINE_CURVE_WITH_KNOTS('',3,(#76445,#76446,#76447,#76448,#76449,
#76450,#76451,#76452,#76453,#76454,#76455,#76456,#76457,#76458,#76459,#76460,
#76461,#76462),.UNSPECIFIED.,.F.,.F.,(4,2,2,2,2,2,2,2,4),(-54.3584128775673,
-53.5234959656725,-52.6885790537776,-51.8536621418828,-51.0187452299879,
-50.183828318093,-49.3489114061982,-48.5139944943033,-48.0752275703878),
 .UNSPECIFIED.);
#3545=B_SPLINE_CURVE_WITH_KNOTS('',3,(#76464,#76465,#76466,#76467,#76468,
#76469,#76470,#76471,#76472,#76473,#76474,#76475,#76476,#76477,#76478,#76479,
#76480,#76481),.UNSPECIFIED.,.F.,.F.,(4,2,2,2,2,2,2,2,4),(-48.0752275703878,
-47.2403106584929,-46.405393746598,-45.5704768347032,-44.7355599228083,
-43.9006430109135,-43.0657260990186,-42.2308091871237,-41.7920422632082),
 .UNSPECIFIED.);
#3546=B_SPLINE_CURVE_WITH_KNOTS('',3,(#76483,#76484,#76485,#76486,#76487,
#76488,#76489,#76490,#76491,#76492,#76493,#76494,#76495,#76496,#76497,#76498,
#76499,#76500),.UNSPECIFIED.,.F.,.F.,(4,2,2,2,2,2,2,2,4),(-41.7920422632082,
-40.9571253513133,-40.1222084394185,-39.2872915275236,-38.4523746156287,
-37.6174577037339,-36.782540791839,-35.9476238799442,-35.5088569560286),
 .UNSPECIFIED.);
#3547=B_SPLINE_CURVE_WITH_KNOTS('',3,(#76502,#76503,#76504,#76505,#76506,
#76507,#76508,#76509,#76510,#76511,#76512,#76513,#76514,#76515,#76516,#76517,
#76518,#76519),.UNSPECIFIED.,.F.,.F.,(4,2,2,2,2,2,2,2,4),(-35.5088569560286,
-34.6739400441337,-33.8390231322389,-33.004106220344,-32.1691893084491,
-31.3342723965543,-30.4993554846594,-29.6644385727646,-29.225671648849),
 .UNSPECIFIED.);
#3548=B_SPLINE_CURVE_WITH_KNOTS('',3,(#76521,#76522,#76523,#76524,#76525,
#76526,#76527,#76528,#76529,#76530,#76531,#76532,#76533),.UNSPECIFIED.,
 .F.,.F.,(4,1,1,1,1,1,1,1,2,4),(-29.225671648849,-28.9287290584219,-27.931186677097,
-27.4324154864345,-26.9336442957721,-26.4348731051097,-25.9361019144472,
-24.9385595331223,-23.9410171517974,-22.9424863416694),.UNSPECIFIED.);
#3549=B_SPLINE_CURVE_WITH_KNOTS('',3,(#76535,#76536,#76537,#76538,#76539,
#76540,#76541,#76542,#76543,#76544,#76545,#76546,#76547),.UNSPECIFIED.,
 .F.,.F.,(4,1,1,1,1,1,1,1,1,1,4),(-22.9424863416694,-22.4447035798101,-21.9459323891476,
-20.9483900078227,-20.4496188171603,-19.9508476264979,-19.4520764358354,
-18.953305245173,-17.9557628638481,-16.9582204825232,-16.6593010344898),
 .UNSPECIFIED.);
#3550=B_SPLINE_CURVE_WITH_KNOTS('',3,(#76549,#76550,#76551,#76552,#76553,
#76554,#76555,#76556,#76557,#76558,#76559,#76560,#76561),.UNSPECIFIED.,
 .F.,.F.,(4,1,1,1,1,1,1,1,1,1,4),(-16.6593010344898,-15.9606781011983,-15.4619069105358,
-14.9631357198734,-13.9655933385485,-13.4668221478861,-12.9680509572236,
-12.4692797665612,-11.9705085758987,-10.9729661945738,-10.3761157273102),
 .UNSPECIFIED.);
#3551=B_SPLINE_CURVE_WITH_KNOTS('',3,(#76562,#76563,#76564,#76565,#76566,
#76567,#76568,#76569,#76570,#76571,#76572,#76573,#76574,#76575,#76576,#76577,
#76578,#76579,#76580,#76581,#76582,#76583,#76584,#76585,#76586,#76587,#76588,
#76589,#76590,#76591,#76592,#76593,#76594,#76595,#76596,#76597,#76598,#76599,
#76600,#76601,#76602,#76603,#76604,#76605,#76606,#76607,#76608,#76609,#76610,
#76611,#76612,#76613,#76614,#76615,#76616,#76617,#76618,#76619,#76620,#76621,
#76622,#76623,#76624,#76625,#76626,#76627,#76628,#76629,#76630,#76631,#76632,
#76633,#76634,#76635,#76636,#76637,#76638,#76639,#76640,#76641,#76642,#76643,
#76644,#76645,#76646,#76647,#76648,#76649,#76650,#76651,#76652,#76653,#76654,
#76655,#76656,#76657,#76658,#76659,#76660,#76661,#76662,#76663,#76664,#76665,
#76666,#76667,#76668,#76669,#76670,#76671,#76672,#76673,#76674,#76675,#76676,
#76677,#76678,#76679,#76680,#76681,#76682,#76683,#76684,#76685,#76686,#76687,
#76688,#76689,#76690,#76691,#76692,#76693,#76694,#76695,#76696,#76697,#76698,
#76699,#76700,#76701,#76702,#76703,#76704,#76705,#76706,#76707,#76708,#76709,
#76710,#76711,#76712,#76713,#76714,#76715,#76716,#76717,#76718,#76719,#76720,
#76721,#76722,#76723,#76724,#76725,#76726,#76727,#76728,#76729,#76730,#76731,
#76732,#76733,#76734,#76735,#76736,#76737,#76738,#76739,#76740,#76741,#76742,
#76743,#76744,#76745,#76746,#76747,#76748,#76749,#76750,#76751,#76752,#76753,
#76754,#76755,#76756,#76757,#76758,#76759,#76760,#76761,#76762,#76763,#76764,
#76765,#76766,#76767,#76768,#76769,#76770,#76771,#76772,#76773,#76774,#76775,
#76776,#76777,#76778,#76779,#76780,#76781,#76782,#76783,#76784,#76785,#76786,
#76787,#76788,#76789,#76790,#76791,#76792,#76793,#76794,#76795,#76796,#76797,
#76798,#76799,#76800,#76801,#76802,#76803,#76804,#76805,#76806,#76807,#76808,
#76809,#76810,#76811,#76812,#76813,#76814,#76815,#76816,#76817),
 .UNSPECIFIED.,.F.,.F.,(4,3,3,3,3,3,3,3,3,3,3,3,3,3,3,3,3,3,3,3,3,3,3,3,
3,3,3,3,3,3,3,3,3,3,3,3,3,3,3,3,3,3,3,3,3,3,3,3,3,3,3,3,3,3,3,3,3,3,3,3,
3,3,3,3,3,3,3,3,3,3,3,3,3,3,3,3,3,3,3,3,3,3,3,3,3,4),(-10.3761155991787,
-10.295606520528,-10.2146913962069,-10.133569882389,-10.0521153589786,-9.97542381324893,
-9.90082242327339,-9.82630646970646,-9.75186202983587,-9.67747522823774,
-9.60313222764775,-9.52497587818229,-9.45066896650611,-9.37636110658798,
-9.3020398161475,-9.22769260816435,-9.15327268902442,-9.07881051078405,
-9.00425886052311,-8.97788143192403,-8.89691300520634,-8.81606084545914,
-8.73182319440975,-8.65128703682939,-8.57087370924006,-8.49063373416483,
-8.47911024126159,-8.40467232653595,-8.33021746049187,-8.25573340166718,
-8.18116743951215,-8.10655699125635,-8.03184239740111,-7.98033905059914,
-7.90377167175971,-7.82727181501515,-7.75082852206479,-7.67443087479399,
-7.59806798792931,-7.52115907309743,-7.44482494298547,-7.36849119936814,
-7.29214798104616,-7.21481015310318,-7.13839390388424,-7.06059528657925,
-6.98279666927425,-6.9090272294558,-6.83532000708233,-6.761661926602,-6.68803909799174,
-6.61443769154234,-6.54083204558264,-6.4840254786118,-6.40241867513602,
-6.32067125792403,-6.23681701543036,-6.15479073653799,-6.07002251224367,
-5.98525428794935,-5.90721271412927,-5.82923946759867,-5.75132842618543,
-5.67348967314702,-5.59569614859377,-5.51795162298141,-5.48648309728691,
-5.40960063427011,-5.33269517011168,-5.25575826443357,-5.17874823782564,
-5.101698651857,-5.02456717534387,-4.98771190662446,-4.91378147830581,-4.83991642829119,
-4.76610243408189,-4.69232520981352,-4.61740086548968,-4.54364068820302,
-4.46987217167397,-4.39608241444794,-4.32029442464165,-4.24638719604415,
-4.16965882563346,-4.09293045522277),.UNSPECIFIED.);
#3552=B_SPLINE_CURVE_WITH_KNOTS('',3,(#76820,#76821,#76822,#76823,#76824,
#76825,#76826,#76827,#76828,#76829,#76830,#76831,#76832,#76833,#76834,#76835,
#76836,#76837,#76838,#76839,#76840,#76841,#76842,#76843,#76844,#76845,#76846,
#76847,#76848,#76849,#76850,#76851,#76852,#76853,#76854,#76855,#76856,#76857,
#76858,#76859,#76860,#76861,#76862,#76863,#76864,#76865,#76866,#76867,#76868,
#76869,#76870,#76871,#76872,#76873,#76874,#76875,#76876,#76877,#76878,#76879,
#76880,#76881,#76882,#76883,#76884,#76885,#76886,#76887,#76888,#76889,#76890,
#76891,#76892,#76893,#76894,#76895),.UNSPECIFIED.,.F.,.F.,(4,3,3,3,3,3,
3,3,3,3,3,3,3,3,3,3,3,3,3,3,3,3,3,3,3,4),(384.369389342789,384.451850946519,
384.534311884371,384.616772183743,384.699231872031,384.78169097663,384.86414952493,
384.946607544323,385.029065062195,385.11574202028,385.198208805821,385.280673918889,
385.363137469137,385.445599566196,385.528060319677,385.610519839173,385.692978234258,
385.775435614492,385.857902000178,385.940365201686,386.022825657536,386.105283806091,
386.187749409844,386.270209288232,386.352673399484,386.415896391544),
 .UNSPECIFIED.);
#3553=B_SPLINE_CURVE_WITH_KNOTS('',3,(#76897,#76898,#76899,#76900,#76901,
#76902,#76903,#76904,#76905,#76906,#76907,#76908,#76909,#76910,#76911,#76912,
#76913,#76914,#76915,#76916,#76917,#76918,#76919,#76920,#76921,#76922,#76923,
#76924,#76925,#76926,#76927,#76928,#76929,#76930,#76931,#76932,#76933,#76934,
#76935,#76936,#76937,#76938,#76939,#76940,#76941,#76942,#76943,#76944,#76945,
#76946,#76947,#76948,#76949,#76950,#76951,#76952,#76953,#76954,#76955,#76956,
#76957,#76958,#76959,#76960,#76961,#76962,#76963,#76964,#76965,#76966,#76967,
#76968,#76969,#76970,#76971,#76972,#76973,#76974,#76975,#76976,#76977,#76978,
#76979,#76980,#76981,#76982,#76983,#76984),.UNSPECIFIED.,.F.,.F.,(4,3,3,
3,3,3,3,3,3,3,3,3,3,3,3,3,3,3,3,3,3,3,3,3,3,3,3,3,3,4),(386.415896391544,
386.519916896913,386.627595730804,386.690968225979,386.766875587204,386.842686706208,
386.918418464482,386.994087656886,387.069711011893,387.14706096132,387.222657598836,
387.298261456307,387.373887613424,387.452543361894,387.528302185255,387.604118054994,
387.680040881299,387.688510607304,387.766536949769,387.844470266106,387.9223257434,
388.000118514048,388.077861083107,388.155576186865,388.233277447859,388.310978478188,
388.388721898678,388.466486616982,388.544326454714,388.606135786806),
 .UNSPECIFIED.);
#3554=B_SPLINE_CURVE_WITH_KNOTS('',3,(#76988,#76989,#76990,#76991,#76992,
#76993,#76994,#76995,#76996,#76997,#76998,#76999,#77000,#77001,#77002,#77003,
#77004,#77005,#77006,#77007,#77008,#77009,#77010,#77011,#77012,#77013,#77014,
#77015,#77016,#77017,#77018,#77019,#77020,#77021,#77022,#77023,#77024),
 .UNSPECIFIED.,.F.,.F.,(4,3,3,3,3,3,3,3,3,3,3,3,4),(386.416228946818,386.492961263492,
386.569655033906,386.646335793747,386.723006668584,386.799707977879,386.868462967424,
386.953194636385,387.037962795978,387.122762791903,387.207557598771,387.292327469878,
387.367234158086),.UNSPECIFIED.);
#3555=B_SPLINE_CURVE_WITH_KNOTS('',3,(#77025,#77026,#77027,#77028,#77029,
#77030,#77031,#77032,#77033,#77034,#77035,#77036,#77037,#77038,#77039,#77040,
#77041,#77042,#77043,#77044,#77045,#77046,#77047,#77048,#77049,#77050,#77051,
#77052,#77053,#77054,#77055,#77056,#77057,#77058,#77059,#77060,#77061,#77062,
#77063,#77064,#77065,#77066,#77067,#77068,#77069,#77070,#77071,#77072,#77073,
#77074,#77075,#77076,#77077,#77078,#77079,#77080,#77081,#77082,#77083,#77084,
#77085,#77086,#77087,#77088,#77089,#77090,#77091,#77092,#77093,#77094,#77095,
#77096,#77097,#77098,#77099,#77100),.UNSPECIFIED.,.F.,.F.,(4,3,3,3,3,3,
3,3,3,3,3,3,3,3,3,3,3,3,3,3,3,3,3,3,3,4),(384.36938934279,384.45185094652,
384.534311884372,384.616772183744,384.699231872032,384.78169097663,384.864149524931,
384.946607544324,385.029065062196,385.115742020281,385.198208805822,385.28067391889,
385.363137469137,385.445599566197,385.528060319678,385.610519839174,385.69297823426,
385.775435614493,385.857902000179,385.940365201687,386.022825657537,386.105283806092,
386.187749409845,386.270209288233,386.352673399486,386.415896391545),
 .UNSPECIFIED.);
#3556=B_SPLINE_CURVE_WITH_KNOTS('',3,(#79285,#79286,#79287,#79288,#79289,
#79290,#79291,#79292,#79293,#79294,#79295,#79296,#79297,#79298,#79299,#79300,
#79301,#79302,#79303,#79304,#79305,#79306,#79307,#79308,#79309,#79310,#79311,
#79312,#79313,#79314,#79315,#79316,#79317,#79318,#79319,#79320,#79321,#79322,
#79323,#79324,#79325,#79326,#79327,#79328,#79329,#79330,#79331,#79332,#79333,
#79334,#79335,#79336,#79337,#79338,#79339,#79340,#79341,#79342,#79343,#79344,
#79345,#79346,#79347,#79348,#79349,#79350,#79351,#79352,#79353,#79354,#79355,
#79356,#79357,#79358,#79359,#79360,#79361,#79362,#79363,#79364,#79365,#79366,
#79367,#79368,#79369,#79370,#79371,#79372,#79373,#79374,#79375,#79376,#79377,
#79378,#79379,#79380,#79381,#79382,#79383,#79384,#79385,#79386,#79387,#79388,
#79389,#79390,#79391,#79392,#79393,#79394,#79395,#79396),.UNSPECIFIED.,
 .F.,.F.,(4,3,3,3,3,3,3,3,3,3,3,3,3,3,3,3,3,3,3,3,3,3,3,3,3,3,3,3,3,3,3,
3,3,3,3,3,3,4),(-1.5287061066451,-1.46563278609545,-1.40366848264018,-1.34172139311797,
-1.32648945379474,-1.31592687441394,-1.25478040828007,-1.1937868575411,
-1.13659146157303,-1.12365124112427,-1.11392990179138,-1.07958806715143,
-1.0175020583394,-0.95735980222339,-0.897594901146072,-0.838755474514921,
-0.831244031903299,-0.822278048496474,-0.763680893830734,-0.706297406799082,
-0.647448671960985,-0.588997675249399,-0.558591305544723,-0.547035837801617,
-0.538520796827503,-0.481016200558624,-0.423876489176745,-0.367086474483784,
-0.346349267967161,-0.288951741053603,-0.28370495096647,-0.272562553273686,
-0.262826912836319,-0.20680074940186,-0.150577776627783,-0.0947036602514006,
-0.039876806877971,0.),.UNSPECIFIED.);
#3557=B_SPLINE_CURVE_WITH_KNOTS('',3,(#79397,#79398,#79399,#79400,#79401,
#79402,#79403,#79404,#79405,#79406,#79407,#79408,#79409,#79410,#79411,#79412,
#79413,#79414,#79415,#79416,#79417,#79418,#79419,#79420,#79421,#79422,#79423,
#79424,#79425,#79426,#79427,#79428,#79429,#79430,#79431,#79432,#79433,#79434,
#79435,#79436,#79437,#79438,#79439,#79440,#79441,#79442,#79443,#79444,#79445,
#79446,#79447,#79448,#79449,#79450,#79451,#79452,#79453,#79454,#79455,#79456,
#79457,#79458,#79459,#79460,#79461,#79462,#79463,#79464,#79465,#79466,#79467,
#79468,#79469,#79470,#79471,#79472,#79473,#79474,#79475,#79476,#79477,#79478,
#79479,#79480,#79481,#79482,#79483,#79484,#79485,#79486,#79487,#79488,#79489,
#79490,#79491,#79492,#79493,#79494,#79495,#79496,#79497,#79498,#79499,#79500,
#79501,#79502,#79503,#79504,#79505,#79506,#79507,#79508),.UNSPECIFIED.,
 .F.,.F.,(4,3,3,3,3,3,3,3,3,3,3,3,3,3,3,3,3,3,3,3,3,3,3,3,3,3,3,3,3,3,3,
3,3,3,3,3,3,4),(0.,0.0545106824407012,0.108992246219552,0.164300448223578,
0.220448606574958,0.265804300761185,0.27240010972656,0.328717061982265,
0.386064106174773,0.403165036736809,0.460671233468054,0.518311395019354,
0.53396435510986,0.542259344152256,0.549928427684927,0.608631374891456,
0.667610836158375,0.726335850589568,0.765244330794922,0.809377107743138,
0.821963747402437,0.832575451855005,0.890877486210268,0.950588397110567,
1.01065953636793,1.07043858295781,1.11830654638065,1.12643018240209,1.14048721636953,
1.20067707539853,1.26153051799682,1.29492746657787,1.31795046485262,1.32913658579,
1.39094257766379,1.45298891535971,1.51475741177567,1.5287061066452),
 .UNSPECIFIED.);
#3558=B_SPLINE_CURVE_WITH_KNOTS('',3,(#81693,#81694,#81695,#81696,#81697,
#81698,#81699,#81700,#81701,#81702,#81703,#81704,#81705,#81706,#81707,#81708,
#81709,#81710,#81711,#81712,#81713,#81714,#81715,#81716,#81717,#81718,#81719,
#81720,#81721,#81722,#81723,#81724,#81725,#81726,#81727,#81728,#81729,#81730,
#81731,#81732,#81733,#81734,#81735,#81736,#81737,#81738,#81739,#81740,#81741,
#81742,#81743,#81744,#81745,#81746,#81747,#81748,#81749,#81750,#81751,#81752,
#81753,#81754,#81755,#81756,#81757,#81758,#81759,#81760,#81761,#81762,#81763,
#81764,#81765,#81766,#81767,#81768,#81769,#81770,#81771,#81772,#81773,#81774,
#81775,#81776,#81777,#81778,#81779,#81780,#81781,#81782,#81783,#81784,#81785,
#81786,#81787,#81788,#81789,#81790,#81791,#81792,#81793,#81794,#81795,#81796,
#81797,#81798),.UNSPECIFIED.,.F.,.F.,(4,3,3,3,3,3,3,3,3,3,3,3,3,3,3,3,3,
3,3,3,3,3,3,3,3,3,3,3,3,3,3,3,3,3,3,4),(-1.5337369924873,-1.47910110659077,
-1.42364061709559,-1.3681801276004,-1.35627281297634,-1.3472470912004,-1.29117883986854,
-1.23440724571817,-1.17721536336885,-1.16839365668255,-1.16075205045248,
-1.13001159231546,-1.07138046030213,-1.01314818419106,-0.954317624226592,
-0.895487064262123,-0.888451348769209,-0.881320522452671,-0.821738837487018,
-0.766771277739479,-0.708056182374627,-0.648681097977743,-0.602036123386777,
-0.595834923297491,-0.535881606952541,-0.475330179668211,-0.414610032838359,
-0.390005676689811,-0.329435956673073,-0.309660837375982,-0.299293319274086,
-0.238580681129937,-0.176748134609211,-0.114706770089442,-0.0530932525039872,
0.),.UNSPECIFIED.);
#3559=B_SPLINE_CURVE_WITH_KNOTS('',3,(#81799,#81800,#81801,#81802,#81803,
#81804,#81805,#81806,#81807,#81808,#81809,#81810,#81811,#81812,#81813,#81814,
#81815,#81816,#81817,#81818,#81819,#81820,#81821,#81822,#81823,#81824,#81825,
#81826,#81827,#81828,#81829,#81830,#81831,#81832,#81833,#81834,#81835,#81836,
#81837,#81838,#81839,#81840,#81841,#81842,#81843,#81844,#81845,#81846,#81847,
#81848,#81849,#81850,#81851,#81852,#81853,#81854,#81855,#81856,#81857,#81858,
#81859,#81860,#81861,#81862,#81863,#81864,#81865,#81866,#81867,#81868,#81869,
#81870,#81871,#81872,#81873,#81874,#81875,#81876,#81877,#81878,#81879,#81880,
#81881,#81882,#81883,#81884,#81885,#81886,#81887,#81888,#81889,#81890,#81891,
#81892,#81893,#81894,#81895,#81896,#81897,#81898,#81899,#81900,#81901,#81902,
#81903,#81904,#81905,#81906,#81907,#81908,#81909,#81910,#81911,#81912,#81913),
 .UNSPECIFIED.,.F.,.F.,(4,3,3,3,3,3,3,3,3,3,3,3,3,3,3,3,3,3,3,3,3,3,3,3,
3,3,3,3,3,3,3,3,3,3,3,3,3,3,4),(0.,0.0633019324654129,0.12491271385973,
0.186949391078483,0.248706534299387,0.299397460630789,0.309169279515443,
0.369823137865797,0.43050954289667,0.451329337802415,0.512095985193222,
0.572332100986119,0.588852907602698,0.599399630443956,0.607101257943028,
0.623405281176508,0.68288782162807,0.742060156956974,0.800329933464109,
0.82591160309259,0.86860772496703,0.880796950572916,0.888966192736701,0.902581013409931,
0.960529646986361,1.01866415529143,1.07634930727061,1.13279238012094,1.16748057808811,
1.18322808695813,1.18681525711862,1.24385416478557,1.3008962452759,1.3498146643194,
1.35813634882905,1.41433556809954,1.46986785043297,1.52519276368421,1.53373699248745),
 .UNSPECIFIED.);
#3920=LINE('',#33019,#4390);
#3921=LINE('',#33241,#4391);
#3922=LINE('',#33740,#4392);
#3923=LINE('',#34236,#4393);
#3924=LINE('',#34744,#4394);
#3925=LINE('',#35252,#4395);
#3926=LINE('',#35748,#4396);
#3927=LINE('',#36250,#4397);
#3928=LINE('',#36746,#4398);
#3929=LINE('',#37233,#4399);
#3930=LINE('',#37732,#4400);
#3931=LINE('',#38240,#4401);
#3932=LINE('',#38733,#4402);
#3933=LINE('',#39229,#4403);
#3934=LINE('',#39737,#4404);
#3935=LINE('',#40245,#4405);
#3936=LINE('',#40744,#4406);
#3937=LINE('',#41240,#4407);
#3938=LINE('',#41733,#4408);
#3939=LINE('',#42220,#4409);
#3940=LINE('',#42722,#4410);
#3941=LINE('',#43230,#4411);
#3942=LINE('',#43723,#4412);
#3943=LINE('',#44225,#4413);
#3944=LINE('',#44733,#4414);
#3945=LINE('',#45238,#4415);
#3946=LINE('',#45734,#4416);
#3947=LINE('',#46230,#4417);
#3948=LINE('',#46723,#4418);
#3949=LINE('',#47207,#4419);
#3950=LINE('',#47709,#4420);
#3951=LINE('',#48217,#4421);
#3952=LINE('',#48722,#4422);
#3953=LINE('',#49215,#4423);
#3954=LINE('',#49714,#4424);
#3955=LINE('',#50198,#4425);
#3956=LINE('',#50679,#4426);
#3957=LINE('',#51181,#4427);
#3958=LINE('',#51683,#4428);
#3959=LINE('',#52188,#4429);
#3960=LINE('',#52675,#4430);
#3961=LINE('',#53168,#4431);
#3962=LINE('',#53679,#4432);
#3963=LINE('',#54172,#4433);
#3964=LINE('',#54671,#4434);
#3965=LINE('',#55155,#4435);
#3966=LINE('',#55636,#4436);
#3967=LINE('',#56135,#4437);
#3968=LINE('',#56640,#4438);
#3969=LINE('',#57136,#4439);
#3970=LINE('',#57629,#4440);
#3971=LINE('',#58125,#4441);
#3972=LINE('',#58633,#4442);
#3973=LINE('',#59120,#4443);
#3974=LINE('',#59625,#4444);
#3975=LINE('',#60109,#4445);
#3976=LINE('',#60587,#4446);
#3977=LINE('',#61086,#4447);
#3978=LINE('',#61591,#4448);
#3979=LINE('',#62087,#4449);
#3980=LINE('',#81918,#4450);
#3981=LINE('',#81924,#4451);
#3982=LINE('',#81930,#4452);
#3983=LINE('',#81936,#4453);
#3984=LINE('',#81951,#4454);
#4390=VECTOR('',#15844,6.767);
#4391=VECTOR('',#15849,6.767);
#4392=VECTOR('',#15852,6.767);
#4393=VECTOR('',#15855,6.767);
#4394=VECTOR('',#15858,6.767);
#4395=VECTOR('',#15861,6.767);
#4396=VECTOR('',#15864,6.767);
#4397=VECTOR('',#15867,6.767);
#4398=VECTOR('',#15870,6.767);
#4399=VECTOR('',#15873,6.767);
#4400=VECTOR('',#15876,6.767);
#4401=VECTOR('',#15879,6.767);
#4402=VECTOR('',#15882,6.767);
#4403=VECTOR('',#15885,6.767);
#4404=VECTOR('',#15888,6.767);
#4405=VECTOR('',#15891,6.767);
#4406=VECTOR('',#15894,6.767);
#4407=VECTOR('',#15897,6.767);
#4408=VECTOR('',#15900,6.767);
#4409=VECTOR('',#15903,6.767);
#4410=VECTOR('',#15906,6.767);
#4411=VECTOR('',#15909,6.767);
#4412=VECTOR('',#15912,6.767);
#4413=VECTOR('',#15915,6.767);
#4414=VECTOR('',#15918,6.767);
#4415=VECTOR('',#15921,6.767);
#4416=VECTOR('',#15924,6.767);
#4417=VECTOR('',#15927,6.767);
#4418=VECTOR('',#15930,6.767);
#4419=VECTOR('',#15933,6.767);
#4420=VECTOR('',#15936,6.767);
#4421=VECTOR('',#15939,6.767);
#4422=VECTOR('',#15942,6.767);
#4423=VECTOR('',#15945,6.767);
#4424=VECTOR('',#15948,6.767);
#4425=VECTOR('',#15951,6.767);
#4426=VECTOR('',#15954,6.767);
#4427=VECTOR('',#15957,6.767);
#4428=VECTOR('',#15960,6.767);
#4429=VECTOR('',#15963,6.767);
#4430=VECTOR('',#15966,6.767);
#4431=VECTOR('',#15969,6.767);
#4432=VECTOR('',#15972,6.767);
#4433=VECTOR('',#15975,6.767);
#4434=VECTOR('',#15978,6.767);
#4435=VECTOR('',#15981,6.767);
#4436=VECTOR('',#15984,6.767);
#4437=VECTOR('',#15987,6.767);
#4438=VECTOR('',#15990,6.767);
#4439=VECTOR('',#15993,6.767);
#4440=VECTOR('',#15996,6.767);
#4441=VECTOR('',#15999,6.767);
#4442=VECTOR('',#16002,6.767);
#4443=VECTOR('',#16005,6.767);
#4444=VECTOR('',#16008,6.767);
#4445=VECTOR('',#16011,6.767);
#4446=VECTOR('',#16014,6.767);
#4447=VECTOR('',#16017,6.767);
#4448=VECTOR('',#16020,6.767);
#4449=VECTOR('',#16023,6.767);
#4450=VECTOR('',#16038,2.);
#4451=VECTOR('',#16045,2.);
#4452=VECTOR('',#16052,2.);
#4453=VECTOR('',#16059,2.);
#4454=VECTOR('',#16078,20.);
#5303=VERTEX_POINT('',#33017);
#5304=VERTEX_POINT('',#33018);
#5305=VERTEX_POINT('',#33020);
#5306=VERTEX_POINT('',#33154);
#5307=VERTEX_POINT('',#33239);
#5308=VERTEX_POINT('',#33240);
#5309=VERTEX_POINT('',#33242);
#5310=VERTEX_POINT('',#33482);
#5311=VERTEX_POINT('',#33738);
#5312=VERTEX_POINT('',#33739);
#5313=VERTEX_POINT('',#33741);
#5314=VERTEX_POINT('',#33987);
#5315=VERTEX_POINT('',#34234);
#5316=VERTEX_POINT('',#34235);
#5317=VERTEX_POINT('',#34237);
#5318=VERTEX_POINT('',#34492);
#5319=VERTEX_POINT('',#34742);
#5320=VERTEX_POINT('',#34743);
#5321=VERTEX_POINT('',#34745);
#5322=VERTEX_POINT('',#34997);
#5323=VERTEX_POINT('',#35250);
#5324=VERTEX_POINT('',#35251);
#5325=VERTEX_POINT('',#35253);
#5326=VERTEX_POINT('',#35505);
#5327=VERTEX_POINT('',#35746);
#5328=VERTEX_POINT('',#35747);
#5329=VERTEX_POINT('',#35749);
#5330=VERTEX_POINT('',#36004);
#5331=VERTEX_POINT('',#36248);
#5332=VERTEX_POINT('',#36249);
#5333=VERTEX_POINT('',#36251);
#5334=VERTEX_POINT('',#36503);
#5335=VERTEX_POINT('',#36744);
#5336=VERTEX_POINT('',#36745);
#5337=VERTEX_POINT('',#36747);
#5338=VERTEX_POINT('',#36996);
#5339=VERTEX_POINT('',#37231);
#5340=VERTEX_POINT('',#37232);
#5341=VERTEX_POINT('',#37234);
#5342=VERTEX_POINT('',#37483);
#5343=VERTEX_POINT('',#37730);
#5344=VERTEX_POINT('',#37731);
#5345=VERTEX_POINT('',#37733);
#5346=VERTEX_POINT('',#37988);
#5347=VERTEX_POINT('',#38238);
#5348=VERTEX_POINT('',#38239);
#5349=VERTEX_POINT('',#38241);
#5350=VERTEX_POINT('',#38478);
#5351=VERTEX_POINT('',#38731);
#5352=VERTEX_POINT('',#38732);
#5353=VERTEX_POINT('',#38734);
#5354=VERTEX_POINT('',#38980);
#5355=VERTEX_POINT('',#39227);
#5356=VERTEX_POINT('',#39228);
#5357=VERTEX_POINT('',#39230);
#5358=VERTEX_POINT('',#39485);
#5359=VERTEX_POINT('',#39735);
#5360=VERTEX_POINT('',#39736);
#5361=VERTEX_POINT('',#39738);
#5362=VERTEX_POINT('',#39990);
#5363=VERTEX_POINT('',#40243);
#5364=VERTEX_POINT('',#40244);
#5365=VERTEX_POINT('',#40246);
#5366=VERTEX_POINT('',#40498);
#5367=VERTEX_POINT('',#40742);
#5368=VERTEX_POINT('',#40743);
#5369=VERTEX_POINT('',#40745);
#5370=VERTEX_POINT('',#40994);
#5371=VERTEX_POINT('',#41238);
#5372=VERTEX_POINT('',#41239);
#5373=VERTEX_POINT('',#41241);
#5374=VERTEX_POINT('',#41490);
#5375=VERTEX_POINT('',#41731);
#5376=VERTEX_POINT('',#41732);
#5377=VERTEX_POINT('',#41734);
#5378=VERTEX_POINT('',#41983);
#5379=VERTEX_POINT('',#42218);
#5380=VERTEX_POINT('',#42219);
#5381=VERTEX_POINT('',#42221);
#5382=VERTEX_POINT('',#42473);
#5383=VERTEX_POINT('',#42720);
#5384=VERTEX_POINT('',#42721);
#5385=VERTEX_POINT('',#42723);
#5386=VERTEX_POINT('',#42975);
#5387=VERTEX_POINT('',#43228);
#5388=VERTEX_POINT('',#43229);
#5389=VERTEX_POINT('',#43231);
#5390=VERTEX_POINT('',#43468);
#5391=VERTEX_POINT('',#43721);
#5392=VERTEX_POINT('',#43722);
#5393=VERTEX_POINT('',#43724);
#5394=VERTEX_POINT('',#43970);
#5395=VERTEX_POINT('',#44223);
#5396=VERTEX_POINT('',#44224);
#5397=VERTEX_POINT('',#44226);
#5398=VERTEX_POINT('',#44481);
#5399=VERTEX_POINT('',#44731);
#5400=VERTEX_POINT('',#44732);
#5401=VERTEX_POINT('',#44734);
#5402=VERTEX_POINT('',#44983);
#5403=VERTEX_POINT('',#45236);
#5404=VERTEX_POINT('',#45237);
#5405=VERTEX_POINT('',#45239);
#5406=VERTEX_POINT('',#45488);
#5407=VERTEX_POINT('',#45732);
#5408=VERTEX_POINT('',#45733);
#5409=VERTEX_POINT('',#45735);
#5410=VERTEX_POINT('',#45984);
#5411=VERTEX_POINT('',#46228);
#5412=VERTEX_POINT('',#46229);
#5413=VERTEX_POINT('',#46231);
#5414=VERTEX_POINT('',#46480);
#5415=VERTEX_POINT('',#46721);
#5416=VERTEX_POINT('',#46722);
#5417=VERTEX_POINT('',#46724);
#5418=VERTEX_POINT('',#46970);
#5419=VERTEX_POINT('',#47205);
#5420=VERTEX_POINT('',#47206);
#5421=VERTEX_POINT('',#47208);
#5422=VERTEX_POINT('',#47460);
#5423=VERTEX_POINT('',#47707);
#5424=VERTEX_POINT('',#47708);
#5425=VERTEX_POINT('',#47710);
#5426=VERTEX_POINT('',#47962);
#5427=VERTEX_POINT('',#48215);
#5428=VERTEX_POINT('',#48216);
#5429=VERTEX_POINT('',#48218);
#5430=VERTEX_POINT('',#48470);
#5431=VERTEX_POINT('',#48720);
#5432=VERTEX_POINT('',#48721);
#5433=VERTEX_POINT('',#48723);
#5434=VERTEX_POINT('',#48972);
#5435=VERTEX_POINT('',#49213);
#5436=VERTEX_POINT('',#49214);
#5437=VERTEX_POINT('',#49216);
#5438=VERTEX_POINT('',#49468);
#5439=VERTEX_POINT('',#49712);
#5440=VERTEX_POINT('',#49713);
#5441=VERTEX_POINT('',#49715);
#5442=VERTEX_POINT('',#49955);
#5443=VERTEX_POINT('',#50196);
#5444=VERTEX_POINT('',#50197);
#5445=VERTEX_POINT('',#50199);
#5446=VERTEX_POINT('',#50442);
#5447=VERTEX_POINT('',#50677);
#5448=VERTEX_POINT('',#50678);
#5449=VERTEX_POINT('',#50680);
#5450=VERTEX_POINT('',#50932);
#5451=VERTEX_POINT('',#51179);
#5452=VERTEX_POINT('',#51180);
#5453=VERTEX_POINT('',#51182);
#5454=VERTEX_POINT('',#51428);
#5455=VERTEX_POINT('',#51681);
#5456=VERTEX_POINT('',#51682);
#5457=VERTEX_POINT('',#51684);
#5458=VERTEX_POINT('',#51939);
#5459=VERTEX_POINT('',#52186);
#5460=VERTEX_POINT('',#52187);
#5461=VERTEX_POINT('',#52189);
#5462=VERTEX_POINT('',#52429);
#5463=VERTEX_POINT('',#52673);
#5464=VERTEX_POINT('',#52674);
#5465=VERTEX_POINT('',#52676);
#5466=VERTEX_POINT('',#52922);
#5467=VERTEX_POINT('',#53166);
#5468=VERTEX_POINT('',#53167);
#5469=VERTEX_POINT('',#53169);
#5470=VERTEX_POINT('',#53421);
#5471=VERTEX_POINT('',#53677);
#5472=VERTEX_POINT('',#53678);
#5473=VERTEX_POINT('',#53680);
#5474=VERTEX_POINT('',#53929);
#5475=VERTEX_POINT('',#54170);
#5476=VERTEX_POINT('',#54171);
#5477=VERTEX_POINT('',#54173);
#5478=VERTEX_POINT('',#54425);
#5479=VERTEX_POINT('',#54669);
#5480=VERTEX_POINT('',#54670);
#5481=VERTEX_POINT('',#54672);
#5482=VERTEX_POINT('',#54912);
#5483=VERTEX_POINT('',#55153);
#5484=VERTEX_POINT('',#55154);
#5485=VERTEX_POINT('',#55156);
#5486=VERTEX_POINT('',#55399);
#5487=VERTEX_POINT('',#55634);
#5488=VERTEX_POINT('',#55635);
#5489=VERTEX_POINT('',#55637);
#5490=VERTEX_POINT('',#55889);
#5491=VERTEX_POINT('',#56133);
#5492=VERTEX_POINT('',#56134);
#5493=VERTEX_POINT('',#56136);
#5494=VERTEX_POINT('',#56385);
#5495=VERTEX_POINT('',#56638);
#5496=VERTEX_POINT('',#56639);
#5497=VERTEX_POINT('',#56641);
#5498=VERTEX_POINT('',#56884);
#5499=VERTEX_POINT('',#57134);
#5500=VERTEX_POINT('',#57135);
#5501=VERTEX_POINT('',#57137);
#5502=VERTEX_POINT('',#57383);
#5503=VERTEX_POINT('',#57627);
#5504=VERTEX_POINT('',#57628);
#5505=VERTEX_POINT('',#57630);
#5506=VERTEX_POINT('',#57879);
#5507=VERTEX_POINT('',#58123);
#5508=VERTEX_POINT('',#58124);
#5509=VERTEX_POINT('',#58126);
#5510=VERTEX_POINT('',#58375);
#5511=VERTEX_POINT('',#58631);
#5512=VERTEX_POINT('',#58632);
#5513=VERTEX_POINT('',#58634);
#5514=VERTEX_POINT('',#58880);
#5515=VERTEX_POINT('',#59118);
#5516=VERTEX_POINT('',#59119);
#5517=VERTEX_POINT('',#59121);
#5518=VERTEX_POINT('',#59376);
#5519=VERTEX_POINT('',#59623);
#5520=VERTEX_POINT('',#59624);
#5521=VERTEX_POINT('',#59626);
#5522=VERTEX_POINT('',#59866);
#5523=VERTEX_POINT('',#60107);
#5524=VERTEX_POINT('',#60108);
#5525=VERTEX_POINT('',#60110);
#5526=VERTEX_POINT('',#60350);
#5527=VERTEX_POINT('',#60585);
#5528=VERTEX_POINT('',#60586);
#5529=VERTEX_POINT('',#60588);
#5530=VERTEX_POINT('',#60840);
#5531=VERTEX_POINT('',#61084);
#5532=VERTEX_POINT('',#61085);
#5533=VERTEX_POINT('',#61087);
#5534=VERTEX_POINT('',#61339);
#5535=VERTEX_POINT('',#61589);
#5536=VERTEX_POINT('',#61590);
#5537=VERTEX_POINT('',#61592);
#5538=VERTEX_POINT('',#61835);
#5539=VERTEX_POINT('',#62085);
#5540=VERTEX_POINT('',#62086);
#5541=VERTEX_POINT('',#62088);
#5542=VERTEX_POINT('',#62322);
#5543=VERTEX_POINT('',#62566);
#5544=VERTEX_POINT('',#62567);
#5545=VERTEX_POINT('',#62576);
#5546=VERTEX_POINT('',#62578);
#5547=VERTEX_POINT('',#62905);
#5548=VERTEX_POINT('',#63458);
#5549=VERTEX_POINT('',#63973);
#5550=VERTEX_POINT('',#63987);
#5551=VERTEX_POINT('',#64492);
#5552=VERTEX_POINT('',#64995);
#5553=VERTEX_POINT('',#65258);
#5554=VERTEX_POINT('',#65781);
#5555=VERTEX_POINT('',#66322);
#5556=VERTEX_POINT('',#66811);
#5557=VERTEX_POINT('',#67071);
#5558=VERTEX_POINT('',#67564);
#5559=VERTEX_POINT('',#67827);
#5560=VERTEX_POINT('',#67846);
#5561=VERTEX_POINT('',#67859);
#5562=VERTEX_POINT('',#68122);
#5563=VERTEX_POINT('',#68136);
#5564=VERTEX_POINT('',#68633);
#5565=VERTEX_POINT('',#68896);
#5566=VERTEX_POINT('',#68910);
#5567=VERTEX_POINT('',#69437);
#5568=VERTEX_POINT('',#69928);
#5569=VERTEX_POINT('',#69945);
#5570=VERTEX_POINT('',#69964);
#5571=VERTEX_POINT('',#70477);
#5572=VERTEX_POINT('',#70490);
#5573=VERTEX_POINT('',#71021);
#5574=VERTEX_POINT('',#71526);
#5575=VERTEX_POINT('',#72057);
#5576=VERTEX_POINT('',#72076);
#5577=VERTEX_POINT('',#72603);
#5578=VERTEX_POINT('',#72616);
#5579=VERTEX_POINT('',#73181);
#5580=VERTEX_POINT('',#73194);
#5581=VERTEX_POINT('',#73454);
#5582=VERTEX_POINT('',#73951);
#5583=VERTEX_POINT('',#73970);
#5584=VERTEX_POINT('',#74487);
#5585=VERTEX_POINT('',#74500);
#5586=VERTEX_POINT('',#74519);
#5587=VERTEX_POINT('',#74536);
#5588=VERTEX_POINT('',#74538);
#5589=VERTEX_POINT('',#74711);
#5590=VERTEX_POINT('',#74730);
#5591=VERTEX_POINT('',#74744);
#5592=VERTEX_POINT('',#74759);
#5593=VERTEX_POINT('',#74772);
#5594=VERTEX_POINT('',#74791);
#5595=VERTEX_POINT('',#74810);
#5596=VERTEX_POINT('',#74829);
#5597=VERTEX_POINT('',#74848);
#5598=VERTEX_POINT('',#74861);
#5599=VERTEX_POINT('',#74877);
#5600=VERTEX_POINT('',#74896);
#5601=VERTEX_POINT('',#74910);
#5602=VERTEX_POINT('',#74925);
#5603=VERTEX_POINT('',#74938);
#5604=VERTEX_POINT('',#74957);
#5605=VERTEX_POINT('',#74976);
#5606=VERTEX_POINT('',#74995);
#5607=VERTEX_POINT('',#75014);
#5608=VERTEX_POINT('',#75027);
#5609=VERTEX_POINT('',#75043);
#5610=VERTEX_POINT('',#75062);
#5611=VERTEX_POINT('',#75076);
#5612=VERTEX_POINT('',#75091);
#5613=VERTEX_POINT('',#75104);
#5614=VERTEX_POINT('',#75123);
#5615=VERTEX_POINT('',#75142);
#5616=VERTEX_POINT('',#75161);
#5617=VERTEX_POINT('',#75180);
#5618=VERTEX_POINT('',#75193);
#5619=VERTEX_POINT('',#75208);
#5620=VERTEX_POINT('',#75222);
#5621=VERTEX_POINT('',#75241);
#5622=VERTEX_POINT('',#75260);
#5623=VERTEX_POINT('',#75279);
#5624=VERTEX_POINT('',#75503);
#5625=VERTEX_POINT('',#75517);
#5626=VERTEX_POINT('',#75774);
#5627=VERTEX_POINT('',#75788);
#5628=VERTEX_POINT('',#75802);
#5629=VERTEX_POINT('',#75818);
#5630=VERTEX_POINT('',#75832);
#5631=VERTEX_POINT('',#75851);
#5632=VERTEX_POINT('',#75870);
#5633=VERTEX_POINT('',#75889);
#5634=VERTEX_POINT('',#76116);
#5635=VERTEX_POINT('',#76130);
#5636=VERTEX_POINT('',#76387);
#5637=VERTEX_POINT('',#76401);
#5638=VERTEX_POINT('',#76415);
#5639=VERTEX_POINT('',#76430);
#5640=VERTEX_POINT('',#76444);
#5641=VERTEX_POINT('',#76463);
#5642=VERTEX_POINT('',#76482);
#5643=VERTEX_POINT('',#76501);
#5644=VERTEX_POINT('',#76520);
#5645=VERTEX_POINT('',#76534);
#5646=VERTEX_POINT('',#76548);
#5647=VERTEX_POINT('',#76819);
#5648=VERTEX_POINT('',#76896);
#5649=VERTEX_POINT('',#76985);
#5650=VERTEX_POINT('',#76987);
#5651=VERTEX_POINT('',#81915);
#5652=VERTEX_POINT('',#81917);
#5653=VERTEX_POINT('',#81921);
#5654=VERTEX_POINT('',#81923);
#5655=VERTEX_POINT('',#81927);
#5656=VERTEX_POINT('',#81929);
#5657=VERTEX_POINT('',#81933);
#5658=VERTEX_POINT('',#81935);
#5659=VERTEX_POINT('',#81939);
#5660=VERTEX_POINT('',#81940);
#5661=VERTEX_POINT('',#81942);
#5662=VERTEX_POINT('',#81947);
#5663=VERTEX_POINT('',#81948);
#5664=VERTEX_POINT('',#81954);
#7058=EDGE_CURVE('',#5303,#5304,#3920,.T.);
#7059=EDGE_CURVE('',#5305,#5303,#3212,.T.);
#7060=EDGE_CURVE('',#5306,#5305,#2598,.T.);
#7061=EDGE_CURVE('',#5306,#5304,#3213,.T.);
#7062=EDGE_CURVE('',#5307,#5308,#3921,.T.);
#7063=EDGE_CURVE('',#5309,#5307,#3214,.T.);
#7064=EDGE_CURVE('',#5303,#5309,#3215,.T.);
#7065=EDGE_CURVE('',#5304,#5310,#3216,.T.);
#7066=EDGE_CURVE('',#5310,#5308,#3217,.T.);
#7067=EDGE_CURVE('',#5311,#5312,#3922,.T.);
#7068=EDGE_CURVE('',#5313,#5311,#3218,.T.);
#7069=EDGE_CURVE('',#5307,#5313,#3219,.T.);
#7070=EDGE_CURVE('',#5308,#5314,#3220,.T.);
#7071=EDGE_CURVE('',#5314,#5312,#3221,.T.);
#7072=EDGE_CURVE('',#5315,#5316,#3923,.T.);
#7073=EDGE_CURVE('',#5317,#5315,#3222,.T.);
#7074=EDGE_CURVE('',#5311,#5317,#3223,.T.);
#7075=EDGE_CURVE('',#5312,#5318,#3224,.T.);
#7076=EDGE_CURVE('',#5318,#5316,#3225,.T.);
#7077=EDGE_CURVE('',#5319,#5320,#3924,.T.);
#7078=EDGE_CURVE('',#5321,#5319,#3226,.T.);
#7079=EDGE_CURVE('',#5315,#5321,#3227,.T.);
#7080=EDGE_CURVE('',#5316,#5322,#3228,.T.);
#7081=EDGE_CURVE('',#5322,#5320,#3229,.T.);
#7082=EDGE_CURVE('',#5323,#5324,#3925,.T.);
#7083=EDGE_CURVE('',#5325,#5323,#3230,.T.);
#7084=EDGE_CURVE('',#5319,#5325,#3231,.T.);
#7085=EDGE_CURVE('',#5320,#5326,#3232,.T.);
#7086=EDGE_CURVE('',#5326,#5324,#3233,.T.);
#7087=EDGE_CURVE('',#5327,#5328,#3926,.T.);
#7088=EDGE_CURVE('',#5329,#5327,#3234,.T.);
#7089=EDGE_CURVE('',#5323,#5329,#3235,.T.);
#7090=EDGE_CURVE('',#5324,#5330,#3236,.T.);
#7091=EDGE_CURVE('',#5330,#5328,#3237,.T.);
#7092=EDGE_CURVE('',#5331,#5332,#3927,.T.);
#7093=EDGE_CURVE('',#5333,#5331,#3238,.T.);
#7094=EDGE_CURVE('',#5327,#5333,#3239,.T.);
#7095=EDGE_CURVE('',#5328,#5334,#3240,.T.);
#7096=EDGE_CURVE('',#5334,#5332,#3241,.T.);
#7097=EDGE_CURVE('',#5335,#5336,#3928,.T.);
#7098=EDGE_CURVE('',#5337,#5335,#3242,.T.);
#7099=EDGE_CURVE('',#5331,#5337,#3243,.T.);
#7100=EDGE_CURVE('',#5332,#5338,#3244,.T.);
#7101=EDGE_CURVE('',#5338,#5336,#3245,.T.);
#7102=EDGE_CURVE('',#5339,#5340,#3929,.T.);
#7103=EDGE_CURVE('',#5341,#5339,#3246,.T.);
#7104=EDGE_CURVE('',#5335,#5341,#3247,.T.);
#7105=EDGE_CURVE('',#5336,#5342,#3248,.T.);
#7106=EDGE_CURVE('',#5342,#5340,#3249,.T.);
#7107=EDGE_CURVE('',#5343,#5344,#3930,.T.);
#7108=EDGE_CURVE('',#5345,#5343,#3250,.T.);
#7109=EDGE_CURVE('',#5339,#5345,#3251,.T.);
#7110=EDGE_CURVE('',#5340,#5346,#3252,.T.);
#7111=EDGE_CURVE('',#5346,#5344,#3253,.T.);
#7112=EDGE_CURVE('',#5347,#5348,#3931,.T.);
#7113=EDGE_CURVE('',#5349,#5347,#3254,.T.);
#7114=EDGE_CURVE('',#5343,#5349,#3255,.T.);
#7115=EDGE_CURVE('',#5344,#5350,#3256,.T.);
#7116=EDGE_CURVE('',#5350,#5348,#3257,.T.);
#7117=EDGE_CURVE('',#5351,#5352,#3932,.T.);
#7118=EDGE_CURVE('',#5353,#5351,#3258,.T.);
#7119=EDGE_CURVE('',#5347,#5353,#3259,.T.);
#7120=EDGE_CURVE('',#5348,#5354,#3260,.T.);
#7121=EDGE_CURVE('',#5354,#5352,#3261,.T.);
#7122=EDGE_CURVE('',#5355,#5356,#3933,.T.);
#7123=EDGE_CURVE('',#5357,#5355,#3262,.T.);
#7124=EDGE_CURVE('',#5351,#5357,#3263,.T.);
#7125=EDGE_CURVE('',#5352,#5358,#3264,.T.);
#7126=EDGE_CURVE('',#5358,#5356,#3265,.T.);
#7127=EDGE_CURVE('',#5359,#5360,#3934,.T.);
#7128=EDGE_CURVE('',#5361,#5359,#3266,.T.);
#7129=EDGE_CURVE('',#5355,#5361,#3267,.T.);
#7130=EDGE_CURVE('',#5356,#5362,#3268,.T.);
#7131=EDGE_CURVE('',#5362,#5360,#3269,.T.);
#7132=EDGE_CURVE('',#5363,#5364,#3935,.T.);
#7133=EDGE_CURVE('',#5365,#5363,#3270,.T.);
#7134=EDGE_CURVE('',#5359,#5365,#3271,.T.);
#7135=EDGE_CURVE('',#5360,#5366,#3272,.T.);
#7136=EDGE_CURVE('',#5366,#5364,#3273,.T.);
#7137=EDGE_CURVE('',#5367,#5368,#3936,.T.);
#7138=EDGE_CURVE('',#5369,#5367,#3274,.T.);
#7139=EDGE_CURVE('',#5363,#5369,#3275,.T.);
#7140=EDGE_CURVE('',#5364,#5370,#3276,.T.);
#7141=EDGE_CURVE('',#5370,#5368,#3277,.T.);
#7142=EDGE_CURVE('',#5371,#5372,#3937,.T.);
#7143=EDGE_CURVE('',#5373,#5371,#3278,.T.);
#7144=EDGE_CURVE('',#5367,#5373,#3279,.T.);
#7145=EDGE_CURVE('',#5368,#5374,#3280,.T.);
#7146=EDGE_CURVE('',#5374,#5372,#3281,.T.);
#7147=EDGE_CURVE('',#5375,#5376,#3938,.T.);
#7148=EDGE_CURVE('',#5377,#5375,#3282,.T.);
#7149=EDGE_CURVE('',#5371,#5377,#3283,.T.);
#7150=EDGE_CURVE('',#5372,#5378,#3284,.T.);
#7151=EDGE_CURVE('',#5378,#5376,#3285,.T.);
#7152=EDGE_CURVE('',#5379,#5380,#3939,.T.);
#7153=EDGE_CURVE('',#5381,#5379,#3286,.T.);
#7154=EDGE_CURVE('',#5375,#5381,#3287,.T.);
#7155=EDGE_CURVE('',#5376,#5382,#3288,.T.);
#7156=EDGE_CURVE('',#5382,#5380,#3289,.T.);
#7157=EDGE_CURVE('',#5383,#5384,#3940,.T.);
#7158=EDGE_CURVE('',#5385,#5383,#3290,.T.);
#7159=EDGE_CURVE('',#5379,#5385,#3291,.T.);
#7160=EDGE_CURVE('',#5380,#5386,#3292,.T.);
#7161=EDGE_CURVE('',#5386,#5384,#3293,.T.);
#7162=EDGE_CURVE('',#5387,#5388,#3941,.T.);
#7163=EDGE_CURVE('',#5389,#5387,#3294,.T.);
#7164=EDGE_CURVE('',#5383,#5389,#3295,.T.);
#7165=EDGE_CURVE('',#5384,#5390,#3296,.T.);
#7166=EDGE_CURVE('',#5390,#5388,#3297,.T.);
#7167=EDGE_CURVE('',#5391,#5392,#3942,.T.);
#7168=EDGE_CURVE('',#5393,#5391,#3298,.T.);
#7169=EDGE_CURVE('',#5387,#5393,#3299,.T.);
#7170=EDGE_CURVE('',#5388,#5394,#3300,.T.);
#7171=EDGE_CURVE('',#5394,#5392,#3301,.T.);
#7172=EDGE_CURVE('',#5395,#5396,#3943,.T.);
#7173=EDGE_CURVE('',#5397,#5395,#3302,.T.);
#7174=EDGE_CURVE('',#5391,#5397,#3303,.T.);
#7175=EDGE_CURVE('',#5392,#5398,#3304,.T.);
#7176=EDGE_CURVE('',#5398,#5396,#3305,.T.);
#7177=EDGE_CURVE('',#5399,#5400,#3944,.T.);
#7178=EDGE_CURVE('',#5401,#5399,#3306,.T.);
#7179=EDGE_CURVE('',#5395,#5401,#3307,.T.);
#7180=EDGE_CURVE('',#5396,#5402,#3308,.T.);
#7181=EDGE_CURVE('',#5402,#5400,#3309,.T.);
#7182=EDGE_CURVE('',#5403,#5404,#3945,.T.);
#7183=EDGE_CURVE('',#5405,#5403,#3310,.T.);
#7184=EDGE_CURVE('',#5399,#5405,#3311,.T.);
#7185=EDGE_CURVE('',#5400,#5406,#3312,.T.);
#7186=EDGE_CURVE('',#5406,#5404,#3313,.T.);
#7187=EDGE_CURVE('',#5407,#5408,#3946,.T.);
#7188=EDGE_CURVE('',#5409,#5407,#3314,.T.);
#7189=EDGE_CURVE('',#5403,#5409,#3315,.T.);
#7190=EDGE_CURVE('',#5404,#5410,#3316,.T.);
#7191=EDGE_CURVE('',#5410,#5408,#3317,.T.);
#7192=EDGE_CURVE('',#5411,#5412,#3947,.T.);
#7193=EDGE_CURVE('',#5413,#5411,#3318,.T.);
#7194=EDGE_CURVE('',#5407,#5413,#3319,.T.);
#7195=EDGE_CURVE('',#5408,#5414,#3320,.T.);
#7196=EDGE_CURVE('',#5414,#5412,#3321,.T.);
#7197=EDGE_CURVE('',#5415,#5416,#3948,.T.);
#7198=EDGE_CURVE('',#5417,#5415,#3322,.T.);
#7199=EDGE_CURVE('',#5411,#5417,#3323,.T.);
#7200=EDGE_CURVE('',#5412,#5418,#3324,.T.);
#7201=EDGE_CURVE('',#5418,#5416,#3325,.T.);
#7202=EDGE_CURVE('',#5419,#5420,#3949,.T.);
#7203=EDGE_CURVE('',#5421,#5419,#3326,.T.);
#7204=EDGE_CURVE('',#5415,#5421,#3327,.T.);
#7205=EDGE_CURVE('',#5416,#5422,#3328,.T.);
#7206=EDGE_CURVE('',#5422,#5420,#3329,.T.);
#7207=EDGE_CURVE('',#5423,#5424,#3950,.T.);
#7208=EDGE_CURVE('',#5425,#5423,#3330,.T.);
#7209=EDGE_CURVE('',#5419,#5425,#3331,.T.);
#7210=EDGE_CURVE('',#5420,#5426,#3332,.T.);
#7211=EDGE_CURVE('',#5426,#5424,#3333,.T.);
#7212=EDGE_CURVE('',#5427,#5428,#3951,.T.);
#7213=EDGE_CURVE('',#5429,#5427,#3334,.T.);
#7214=EDGE_CURVE('',#5423,#5429,#3335,.T.);
#7215=EDGE_CURVE('',#5424,#5430,#3336,.T.);
#7216=EDGE_CURVE('',#5430,#5428,#3337,.T.);
#7217=EDGE_CURVE('',#5431,#5432,#3952,.T.);
#7218=EDGE_CURVE('',#5433,#5431,#3338,.T.);
#7219=EDGE_CURVE('',#5427,#5433,#3339,.T.);
#7220=EDGE_CURVE('',#5428,#5434,#3340,.T.);
#7221=EDGE_CURVE('',#5434,#5432,#3341,.T.);
#7222=EDGE_CURVE('',#5435,#5436,#3953,.T.);
#7223=EDGE_CURVE('',#5437,#5435,#3342,.T.);
#7224=EDGE_CURVE('',#5431,#5437,#3343,.T.);
#7225=EDGE_CURVE('',#5432,#5438,#3344,.T.);
#7226=EDGE_CURVE('',#5438,#5436,#3345,.T.);
#7227=EDGE_CURVE('',#5439,#5440,#3954,.T.);
#7228=EDGE_CURVE('',#5441,#5439,#3346,.T.);
#7229=EDGE_CURVE('',#5435,#5441,#3347,.T.);
#7230=EDGE_CURVE('',#5436,#5442,#3348,.T.);
#7231=EDGE_CURVE('',#5442,#5440,#3349,.T.);
#7232=EDGE_CURVE('',#5443,#5444,#3955,.T.);
#7233=EDGE_CURVE('',#5445,#5443,#3350,.T.);
#7234=EDGE_CURVE('',#5439,#5445,#3351,.T.);
#7235=EDGE_CURVE('',#5440,#5446,#3352,.T.);
#7236=EDGE_CURVE('',#5446,#5444,#3353,.T.);
#7237=EDGE_CURVE('',#5447,#5448,#3956,.T.);
#7238=EDGE_CURVE('',#5449,#5447,#3354,.T.);
#7239=EDGE_CURVE('',#5443,#5449,#3355,.T.);
#7240=EDGE_CURVE('',#5444,#5450,#3356,.T.);
#7241=EDGE_CURVE('',#5450,#5448,#3357,.T.);
#7242=EDGE_CURVE('',#5451,#5452,#3957,.T.);
#7243=EDGE_CURVE('',#5453,#5451,#3358,.T.);
#7244=EDGE_CURVE('',#5447,#5453,#3359,.T.);
#7245=EDGE_CURVE('',#5448,#5454,#3360,.T.);
#7246=EDGE_CURVE('',#5454,#5452,#3361,.T.);
#7247=EDGE_CURVE('',#5455,#5456,#3958,.T.);
#7248=EDGE_CURVE('',#5457,#5455,#3362,.T.);
#7249=EDGE_CURVE('',#5451,#5457,#3363,.T.);
#7250=EDGE_CURVE('',#5452,#5458,#3364,.T.);
#7251=EDGE_CURVE('',#5458,#5456,#3365,.T.);
#7252=EDGE_CURVE('',#5459,#5460,#3959,.T.);
#7253=EDGE_CURVE('',#5461,#5459,#3366,.T.);
#7254=EDGE_CURVE('',#5455,#5461,#3367,.T.);
#7255=EDGE_CURVE('',#5456,#5462,#3368,.T.);
#7256=EDGE_CURVE('',#5462,#5460,#3369,.T.);
#7257=EDGE_CURVE('',#5463,#5464,#3960,.T.);
#7258=EDGE_CURVE('',#5465,#5463,#3370,.T.);
#7259=EDGE_CURVE('',#5459,#5465,#3371,.T.);
#7260=EDGE_CURVE('',#5460,#5466,#3372,.T.);
#7261=EDGE_CURVE('',#5466,#5464,#3373,.T.);
#7262=EDGE_CURVE('',#5467,#5468,#3961,.T.);
#7263=EDGE_CURVE('',#5469,#5467,#3374,.T.);
#7264=EDGE_CURVE('',#5463,#5469,#3375,.T.);
#7265=EDGE_CURVE('',#5464,#5470,#3376,.T.);
#7266=EDGE_CURVE('',#5470,#5468,#3377,.T.);
#7267=EDGE_CURVE('',#5471,#5472,#3962,.T.);
#7268=EDGE_CURVE('',#5473,#5471,#3378,.T.);
#7269=EDGE_CURVE('',#5467,#5473,#3379,.T.);
#7270=EDGE_CURVE('',#5468,#5474,#3380,.T.);
#7271=EDGE_CURVE('',#5474,#5472,#3381,.T.);
#7272=EDGE_CURVE('',#5475,#5476,#3963,.T.);
#7273=EDGE_CURVE('',#5477,#5475,#3382,.T.);
#7274=EDGE_CURVE('',#5471,#5477,#3383,.T.);
#7275=EDGE_CURVE('',#5472,#5478,#3384,.T.);
#7276=EDGE_CURVE('',#5478,#5476,#3385,.T.);
#7277=EDGE_CURVE('',#5479,#5480,#3964,.T.);
#7278=EDGE_CURVE('',#5481,#5479,#3386,.T.);
#7279=EDGE_CURVE('',#5475,#5481,#3387,.T.);
#7280=EDGE_CURVE('',#5476,#5482,#3388,.T.);
#7281=EDGE_CURVE('',#5482,#5480,#3389,.T.);
#7282=EDGE_CURVE('',#5483,#5484,#3965,.T.);
#7283=EDGE_CURVE('',#5485,#5483,#3390,.T.);
#7284=EDGE_CURVE('',#5479,#5485,#3391,.T.);
#7285=EDGE_CURVE('',#5480,#5486,#3392,.T.);
#7286=EDGE_CURVE('',#5486,#5484,#3393,.T.);
#7287=EDGE_CURVE('',#5487,#5488,#3966,.T.);
#7288=EDGE_CURVE('',#5489,#5487,#3394,.T.);
#7289=EDGE_CURVE('',#5483,#5489,#3395,.T.);
#7290=EDGE_CURVE('',#5484,#5490,#3396,.T.);
#7291=EDGE_CURVE('',#5490,#5488,#3397,.T.);
#7292=EDGE_CURVE('',#5491,#5492,#3967,.T.);
#7293=EDGE_CURVE('',#5493,#5491,#3398,.T.);
#7294=EDGE_CURVE('',#5487,#5493,#3399,.T.);
#7295=EDGE_CURVE('',#5488,#5494,#3400,.T.);
#7296=EDGE_CURVE('',#5494,#5492,#3401,.T.);
#7297=EDGE_CURVE('',#5495,#5496,#3968,.T.);
#7298=EDGE_CURVE('',#5497,#5495,#3402,.T.);
#7299=EDGE_CURVE('',#5491,#5497,#3403,.T.);
#7300=EDGE_CURVE('',#5492,#5498,#3404,.T.);
#7301=EDGE_CURVE('',#5498,#5496,#3405,.T.);
#7302=EDGE_CURVE('',#5499,#5500,#3969,.T.);
#7303=EDGE_CURVE('',#5501,#5499,#3406,.T.);
#7304=EDGE_CURVE('',#5495,#5501,#3407,.T.);
#7305=EDGE_CURVE('',#5496,#5502,#3408,.T.);
#7306=EDGE_CURVE('',#5502,#5500,#3409,.T.);
#7307=EDGE_CURVE('',#5503,#5504,#3970,.T.);
#7308=EDGE_CURVE('',#5505,#5503,#3410,.T.);
#7309=EDGE_CURVE('',#5499,#5505,#3411,.T.);
#7310=EDGE_CURVE('',#5500,#5506,#3412,.T.);
#7311=EDGE_CURVE('',#5506,#5504,#3413,.T.);
#7312=EDGE_CURVE('',#5507,#5508,#3971,.T.);
#7313=EDGE_CURVE('',#5509,#5507,#3414,.T.);
#7314=EDGE_CURVE('',#5503,#5509,#3415,.T.);
#7315=EDGE_CURVE('',#5504,#5510,#3416,.T.);
#7316=EDGE_CURVE('',#5510,#5508,#3417,.T.);
#7317=EDGE_CURVE('',#5511,#5512,#3972,.T.);
#7318=EDGE_CURVE('',#5513,#5511,#3418,.T.);
#7319=EDGE_CURVE('',#5507,#5513,#3419,.T.);
#7320=EDGE_CURVE('',#5508,#5514,#3420,.T.);
#7321=EDGE_CURVE('',#5514,#5512,#3421,.T.);
#7322=EDGE_CURVE('',#5515,#5516,#3973,.T.);
#7323=EDGE_CURVE('',#5517,#5515,#3422,.T.);
#7324=EDGE_CURVE('',#5511,#5517,#3423,.T.);
#7325=EDGE_CURVE('',#5512,#5518,#3424,.T.);
#7326=EDGE_CURVE('',#5518,#5516,#3425,.T.);
#7327=EDGE_CURVE('',#5519,#5520,#3974,.T.);
#7328=EDGE_CURVE('',#5521,#5519,#3426,.T.);
#7329=EDGE_CURVE('',#5515,#5521,#3427,.T.);
#7330=EDGE_CURVE('',#5516,#5522,#3428,.T.);
#7331=EDGE_CURVE('',#5522,#5520,#3429,.T.);
#7332=EDGE_CURVE('',#5523,#5524,#3975,.T.);
#7333=EDGE_CURVE('',#5525,#5523,#3430,.T.);
#7334=EDGE_CURVE('',#5519,#5525,#3431,.T.);
#7335=EDGE_CURVE('',#5520,#5526,#3432,.T.);
#7336=EDGE_CURVE('',#5526,#5524,#3433,.T.);
#7337=EDGE_CURVE('',#5527,#5528,#3976,.T.);
#7338=EDGE_CURVE('',#5529,#5527,#3434,.T.);
#7339=EDGE_CURVE('',#5523,#5529,#3435,.T.);
#7340=EDGE_CURVE('',#5524,#5530,#3436,.T.);
#7341=EDGE_CURVE('',#5530,#5528,#3437,.T.);
#7342=EDGE_CURVE('',#5531,#5532,#3977,.T.);
#7343=EDGE_CURVE('',#5533,#5531,#3438,.T.);
#7344=EDGE_CURVE('',#5527,#5533,#3439,.T.);
#7345=EDGE_CURVE('',#5528,#5534,#3440,.T.);
#7346=EDGE_CURVE('',#5534,#5532,#3441,.T.);
#7347=EDGE_CURVE('',#5535,#5536,#3978,.T.);
#7348=EDGE_CURVE('',#5537,#5535,#3442,.T.);
#7349=EDGE_CURVE('',#5531,#5537,#3443,.T.);
#7350=EDGE_CURVE('',#5532,#5538,#3444,.T.);
#7351=EDGE_CURVE('',#5538,#5536,#3445,.T.);
#7352=EDGE_CURVE('',#5539,#5540,#3979,.T.);
#7353=EDGE_CURVE('',#5541,#5539,#3446,.T.);
#7354=EDGE_CURVE('',#5535,#5541,#3447,.T.);
#7355=EDGE_CURVE('',#5536,#5542,#3448,.T.);
#7356=EDGE_CURVE('',#5542,#5540,#3449,.T.);
#7357=EDGE_CURVE('',#5543,#5544,#3450,.T.);
#7358=EDGE_CURVE('',#5545,#5544,#2599,.T.);
#7359=EDGE_CURVE('',#5545,#5546,#3451,.T.);
#7360=EDGE_CURVE('',#5546,#5547,#3452,.T.);
#7361=EDGE_CURVE('',#5547,#5548,#3453,.T.);
#7362=EDGE_CURVE('',#5548,#5549,#3454,.T.);
#7363=EDGE_CURVE('',#5549,#5550,#3455,.T.);
#7364=EDGE_CURVE('',#5550,#5551,#3456,.T.);
#7365=EDGE_CURVE('',#5551,#5552,#3457,.T.);
#7366=EDGE_CURVE('',#5552,#5553,#3458,.T.);
#7367=EDGE_CURVE('',#5553,#5554,#3459,.T.);
#7368=EDGE_CURVE('',#5554,#5555,#3460,.T.);
#7369=EDGE_CURVE('',#5555,#5556,#3461,.T.);
#7370=EDGE_CURVE('',#5556,#5557,#3462,.T.);
#7371=EDGE_CURVE('',#5557,#5558,#3463,.T.);
#7372=EDGE_CURVE('',#5558,#5559,#3464,.T.);
#7373=EDGE_CURVE('',#5559,#5560,#3465,.T.);
#7374=EDGE_CURVE('',#5560,#5561,#3466,.T.);
#7375=EDGE_CURVE('',#5561,#5562,#3467,.T.);
#7376=EDGE_CURVE('',#5562,#5563,#3468,.T.);
#7377=EDGE_CURVE('',#5563,#5564,#3469,.T.);
#7378=EDGE_CURVE('',#5564,#5565,#3470,.T.);
#7379=EDGE_CURVE('',#5565,#5566,#3471,.T.);
#7380=EDGE_CURVE('',#5566,#5567,#3472,.T.);
#7381=EDGE_CURVE('',#5567,#5568,#3473,.T.);
#7382=EDGE_CURVE('',#5568,#5569,#3474,.T.);
#7383=EDGE_CURVE('',#5569,#5570,#3475,.T.);
#7384=EDGE_CURVE('',#5570,#5571,#3476,.T.);
#7385=EDGE_CURVE('',#5571,#5572,#3477,.T.);
#7386=EDGE_CURVE('',#5572,#5573,#3478,.T.);
#7387=EDGE_CURVE('',#5573,#5574,#3479,.T.);
#7388=EDGE_CURVE('',#5574,#5575,#3480,.T.);
#7389=EDGE_CURVE('',#5575,#5576,#3481,.T.);
#7390=EDGE_CURVE('',#5576,#5577,#3482,.T.);
#7391=EDGE_CURVE('',#5577,#5578,#3483,.T.);
#7392=EDGE_CURVE('',#5578,#5579,#3484,.T.);
#7393=EDGE_CURVE('',#5579,#5580,#3485,.T.);
#7394=EDGE_CURVE('',#5580,#5581,#3486,.T.);
#7395=EDGE_CURVE('',#5581,#5582,#3487,.T.);
#7396=EDGE_CURVE('',#5582,#5583,#3488,.T.);
#7397=EDGE_CURVE('',#5583,#5584,#3489,.T.);
#7398=EDGE_CURVE('',#5584,#5585,#3490,.T.);
#7399=EDGE_CURVE('',#5585,#5586,#3491,.T.);
#7400=EDGE_CURVE('',#5587,#5586,#2600,.F.);
#7401=EDGE_CURVE('',#5587,#5588,#3492,.T.);
#7402=EDGE_CURVE('',#5588,#5589,#3493,.T.);
#7403=EDGE_CURVE('',#5589,#5590,#3494,.T.);
#7404=EDGE_CURVE('',#5590,#5591,#3495,.T.);
#7405=EDGE_CURVE('',#5591,#5592,#3496,.T.);
#7406=EDGE_CURVE('',#5592,#5593,#3497,.T.);
#7407=EDGE_CURVE('',#5593,#5594,#3498,.T.);
#7408=EDGE_CURVE('',#5594,#5595,#3499,.T.);
#7409=EDGE_CURVE('',#5595,#5596,#3500,.T.);
#7410=EDGE_CURVE('',#5596,#5597,#3501,.T.);
#7411=EDGE_CURVE('',#5597,#5598,#3502,.T.);
#7412=EDGE_CURVE('',#5598,#5599,#3503,.T.);
#7413=EDGE_CURVE('',#5599,#5600,#3504,.T.);
#7414=EDGE_CURVE('',#5600,#5601,#3505,.T.);
#7415=EDGE_CURVE('',#5601,#5602,#3506,.T.);
#7416=EDGE_CURVE('',#5602,#5603,#3507,.T.);
#7417=EDGE_CURVE('',#5603,#5604,#3508,.T.);
#7418=EDGE_CURVE('',#5604,#5605,#3509,.T.);
#7419=EDGE_CURVE('',#5605,#5606,#3510,.T.);
#7420=EDGE_CURVE('',#5606,#5607,#3511,.T.);
#7421=EDGE_CURVE('',#5607,#5608,#3512,.T.);
#7422=EDGE_CURVE('',#5608,#5609,#3513,.T.);
#7423=EDGE_CURVE('',#5609,#5610,#3514,.T.);
#7424=EDGE_CURVE('',#5610,#5611,#3515,.T.);
#7425=EDGE_CURVE('',#5611,#5612,#3516,.T.);
#7426=EDGE_CURVE('',#5612,#5613,#3517,.T.);
#7427=EDGE_CURVE('',#5613,#5614,#3518,.T.);
#7428=EDGE_CURVE('',#5614,#5615,#3519,.T.);
#7429=EDGE_CURVE('',#5615,#5616,#3520,.T.);
#7430=EDGE_CURVE('',#5616,#5617,#3521,.T.);
#7431=EDGE_CURVE('',#5617,#5618,#3522,.T.);
#7432=EDGE_CURVE('',#5618,#5619,#3523,.T.);
#7433=EDGE_CURVE('',#5619,#5620,#3524,.T.);
#7434=EDGE_CURVE('',#5620,#5621,#3525,.T.);
#7435=EDGE_CURVE('',#5621,#5622,#3526,.T.);
#7436=EDGE_CURVE('',#5622,#5623,#3527,.T.);
#7437=EDGE_CURVE('',#5623,#5624,#3528,.T.);
#7438=EDGE_CURVE('',#5624,#5625,#3529,.T.);
#7439=EDGE_CURVE('',#5625,#5626,#3530,.T.);
#7440=EDGE_CURVE('',#5626,#5627,#3531,.T.);
#7441=EDGE_CURVE('',#5627,#5628,#3532,.T.);
#7442=EDGE_CURVE('',#5628,#5629,#3533,.T.);
#7443=EDGE_CURVE('',#5629,#5630,#3534,.T.);
#7444=EDGE_CURVE('',#5630,#5631,#3535,.T.);
#7445=EDGE_CURVE('',#5631,#5632,#3536,.T.);
#7446=EDGE_CURVE('',#5632,#5633,#3537,.T.);
#7447=EDGE_CURVE('',#5633,#5634,#3538,.T.);
#7448=EDGE_CURVE('',#5634,#5635,#3539,.T.);
#7449=EDGE_CURVE('',#5635,#5636,#3540,.T.);
#7450=EDGE_CURVE('',#5636,#5637,#3541,.T.);
#7451=EDGE_CURVE('',#5637,#5638,#3542,.T.);
#7452=EDGE_CURVE('',#5638,#5639,#3543,.T.);
#7453=EDGE_CURVE('',#5639,#5640,#3544,.T.);
#7454=EDGE_CURVE('',#5640,#5641,#3545,.T.);
#7455=EDGE_CURVE('',#5641,#5642,#3546,.T.);
#7456=EDGE_CURVE('',#5642,#5643,#3547,.T.);
#7457=EDGE_CURVE('',#5643,#5644,#3548,.T.);
#7458=EDGE_CURVE('',#5644,#5645,#3549,.T.);
#7459=EDGE_CURVE('',#5645,#5646,#3550,.T.);
#7460=EDGE_CURVE('',#5646,#5543,#3551,.T.);
#7461=EDGE_CURVE('',#5540,#5647,#3552,.T.);
#7462=EDGE_CURVE('',#5647,#5648,#3553,.T.);
#7463=EDGE_CURVE('',#5649,#5648,#2601,.T.);
#7464=EDGE_CURVE('',#5650,#5649,#3554,.T.);
#7465=EDGE_CURVE('',#5539,#5650,#3555,.T.);
#7466=EDGE_CURVE('',#5586,#5649,#3556,.T.);
#7467=EDGE_CURVE('',#5305,#5545,#3557,.T.);
#7468=EDGE_CURVE('',#5648,#5587,#3558,.T.);
#7469=EDGE_CURVE('',#5544,#5306,#3559,.T.);
#7470=EDGE_CURVE('',#5651,#5651,#2602,.T.);
#7471=EDGE_CURVE('',#5651,#5652,#3980,.T.);
#7472=EDGE_CURVE('',#5652,#5652,#2603,.T.);
#7473=EDGE_CURVE('',#5653,#5653,#2604,.T.);
#7474=EDGE_CURVE('',#5653,#5654,#3981,.T.);
#7475=EDGE_CURVE('',#5654,#5654,#2605,.T.);
#7476=EDGE_CURVE('',#5655,#5655,#2606,.T.);
#7477=EDGE_CURVE('',#5655,#5656,#3982,.T.);
#7478=EDGE_CURVE('',#5656,#5656,#2607,.T.);
#7479=EDGE_CURVE('',#5657,#5657,#2608,.T.);
#7480=EDGE_CURVE('',#5657,#5658,#3983,.T.);
#7481=EDGE_CURVE('',#5658,#5658,#2609,.T.);
#7482=EDGE_CURVE('',#5659,#5660,#2610,.T.);
#7483=EDGE_CURVE('',#5660,#5661,#2611,.T.);
#7484=EDGE_CURVE('',#5661,#5661,#2612,.T.);
#7485=EDGE_CURVE('',#5660,#5659,#2613,.T.);
#7486=EDGE_CURVE('',#5662,#5663,#2614,.T.);
#7487=EDGE_CURVE('',#5663,#5662,#2615,.T.);
#7488=EDGE_CURVE('',#5663,#5659,#3984,.T.);
#7489=EDGE_CURVE('',#5664,#5664,#2616,.T.);
#7490=EDGE_CURVE('',#5664,#5662,#2617,.T.);
#10092=ORIENTED_EDGE('',*,*,#7058,.F.);
#10093=ORIENTED_EDGE('',*,*,#7059,.F.);
#10094=ORIENTED_EDGE('',*,*,#7060,.F.);
#10095=ORIENTED_EDGE('',*,*,#7061,.T.);
#10096=ORIENTED_EDGE('',*,*,#7062,.F.);
#10097=ORIENTED_EDGE('',*,*,#7063,.F.);
#10098=ORIENTED_EDGE('',*,*,#7064,.F.);
#10099=ORIENTED_EDGE('',*,*,#7058,.T.);
#10100=ORIENTED_EDGE('',*,*,#7065,.T.);
#10101=ORIENTED_EDGE('',*,*,#7066,.T.);
#10102=ORIENTED_EDGE('',*,*,#7067,.F.);
#10103=ORIENTED_EDGE('',*,*,#7068,.F.);
#10104=ORIENTED_EDGE('',*,*,#7069,.F.);
#10105=ORIENTED_EDGE('',*,*,#7062,.T.);
#10106=ORIENTED_EDGE('',*,*,#7070,.T.);
#10107=ORIENTED_EDGE('',*,*,#7071,.T.);
#10108=ORIENTED_EDGE('',*,*,#7072,.F.);
#10109=ORIENTED_EDGE('',*,*,#7073,.F.);
#10110=ORIENTED_EDGE('',*,*,#7074,.F.);
#10111=ORIENTED_EDGE('',*,*,#7067,.T.);
#10112=ORIENTED_EDGE('',*,*,#7075,.T.);
#10113=ORIENTED_EDGE('',*,*,#7076,.T.);
#10114=ORIENTED_EDGE('',*,*,#7077,.F.);
#10115=ORIENTED_EDGE('',*,*,#7078,.F.);
#10116=ORIENTED_EDGE('',*,*,#7079,.F.);
#10117=ORIENTED_EDGE('',*,*,#7072,.T.);
#10118=ORIENTED_EDGE('',*,*,#7080,.T.);
#10119=ORIENTED_EDGE('',*,*,#7081,.T.);
#10120=ORIENTED_EDGE('',*,*,#7082,.F.);
#10121=ORIENTED_EDGE('',*,*,#7083,.F.);
#10122=ORIENTED_EDGE('',*,*,#7084,.F.);
#10123=ORIENTED_EDGE('',*,*,#7077,.T.);
#10124=ORIENTED_EDGE('',*,*,#7085,.T.);
#10125=ORIENTED_EDGE('',*,*,#7086,.T.);
#10126=ORIENTED_EDGE('',*,*,#7087,.F.);
#10127=ORIENTED_EDGE('',*,*,#7088,.F.);
#10128=ORIENTED_EDGE('',*,*,#7089,.F.);
#10129=ORIENTED_EDGE('',*,*,#7082,.T.);
#10130=ORIENTED_EDGE('',*,*,#7090,.T.);
#10131=ORIENTED_EDGE('',*,*,#7091,.T.);
#10132=ORIENTED_EDGE('',*,*,#7092,.F.);
#10133=ORIENTED_EDGE('',*,*,#7093,.F.);
#10134=ORIENTED_EDGE('',*,*,#7094,.F.);
#10135=ORIENTED_EDGE('',*,*,#7087,.T.);
#10136=ORIENTED_EDGE('',*,*,#7095,.T.);
#10137=ORIENTED_EDGE('',*,*,#7096,.T.);
#10138=ORIENTED_EDGE('',*,*,#7097,.F.);
#10139=ORIENTED_EDGE('',*,*,#7098,.F.);
#10140=ORIENTED_EDGE('',*,*,#7099,.F.);
#10141=ORIENTED_EDGE('',*,*,#7092,.T.);
#10142=ORIENTED_EDGE('',*,*,#7100,.T.);
#10143=ORIENTED_EDGE('',*,*,#7101,.T.);
#10144=ORIENTED_EDGE('',*,*,#7102,.F.);
#10145=ORIENTED_EDGE('',*,*,#7103,.F.);
#10146=ORIENTED_EDGE('',*,*,#7104,.F.);
#10147=ORIENTED_EDGE('',*,*,#7097,.T.);
#10148=ORIENTED_EDGE('',*,*,#7105,.T.);
#10149=ORIENTED_EDGE('',*,*,#7106,.T.);
#10150=ORIENTED_EDGE('',*,*,#7107,.F.);
#10151=ORIENTED_EDGE('',*,*,#7108,.F.);
#10152=ORIENTED_EDGE('',*,*,#7109,.F.);
#10153=ORIENTED_EDGE('',*,*,#7102,.T.);
#10154=ORIENTED_EDGE('',*,*,#7110,.T.);
#10155=ORIENTED_EDGE('',*,*,#7111,.T.);
#10156=ORIENTED_EDGE('',*,*,#7112,.F.);
#10157=ORIENTED_EDGE('',*,*,#7113,.F.);
#10158=ORIENTED_EDGE('',*,*,#7114,.F.);
#10159=ORIENTED_EDGE('',*,*,#7107,.T.);
#10160=ORIENTED_EDGE('',*,*,#7115,.T.);
#10161=ORIENTED_EDGE('',*,*,#7116,.T.);
#10162=ORIENTED_EDGE('',*,*,#7117,.F.);
#10163=ORIENTED_EDGE('',*,*,#7118,.F.);
#10164=ORIENTED_EDGE('',*,*,#7119,.F.);
#10165=ORIENTED_EDGE('',*,*,#7112,.T.);
#10166=ORIENTED_EDGE('',*,*,#7120,.T.);
#10167=ORIENTED_EDGE('',*,*,#7121,.T.);
#10168=ORIENTED_EDGE('',*,*,#7122,.F.);
#10169=ORIENTED_EDGE('',*,*,#7123,.F.);
#10170=ORIENTED_EDGE('',*,*,#7124,.F.);
#10171=ORIENTED_EDGE('',*,*,#7117,.T.);
#10172=ORIENTED_EDGE('',*,*,#7125,.T.);
#10173=ORIENTED_EDGE('',*,*,#7126,.T.);
#10174=ORIENTED_EDGE('',*,*,#7127,.F.);
#10175=ORIENTED_EDGE('',*,*,#7128,.F.);
#10176=ORIENTED_EDGE('',*,*,#7129,.F.);
#10177=ORIENTED_EDGE('',*,*,#7122,.T.);
#10178=ORIENTED_EDGE('',*,*,#7130,.T.);
#10179=ORIENTED_EDGE('',*,*,#7131,.T.);
#10180=ORIENTED_EDGE('',*,*,#7132,.F.);
#10181=ORIENTED_EDGE('',*,*,#7133,.F.);
#10182=ORIENTED_EDGE('',*,*,#7134,.F.);
#10183=ORIENTED_EDGE('',*,*,#7127,.T.);
#10184=ORIENTED_EDGE('',*,*,#7135,.T.);
#10185=ORIENTED_EDGE('',*,*,#7136,.T.);
#10186=ORIENTED_EDGE('',*,*,#7137,.F.);
#10187=ORIENTED_EDGE('',*,*,#7138,.F.);
#10188=ORIENTED_EDGE('',*,*,#7139,.F.);
#10189=ORIENTED_EDGE('',*,*,#7132,.T.);
#10190=ORIENTED_EDGE('',*,*,#7140,.T.);
#10191=ORIENTED_EDGE('',*,*,#7141,.T.);
#10192=ORIENTED_EDGE('',*,*,#7142,.F.);
#10193=ORIENTED_EDGE('',*,*,#7143,.F.);
#10194=ORIENTED_EDGE('',*,*,#7144,.F.);
#10195=ORIENTED_EDGE('',*,*,#7137,.T.);
#10196=ORIENTED_EDGE('',*,*,#7145,.T.);
#10197=ORIENTED_EDGE('',*,*,#7146,.T.);
#10198=ORIENTED_EDGE('',*,*,#7147,.F.);
#10199=ORIENTED_EDGE('',*,*,#7148,.F.);
#10200=ORIENTED_EDGE('',*,*,#7149,.F.);
#10201=ORIENTED_EDGE('',*,*,#7142,.T.);
#10202=ORIENTED_EDGE('',*,*,#7150,.T.);
#10203=ORIENTED_EDGE('',*,*,#7151,.T.);
#10204=ORIENTED_EDGE('',*,*,#7152,.F.);
#10205=ORIENTED_EDGE('',*,*,#7153,.F.);
#10206=ORIENTED_EDGE('',*,*,#7154,.F.);
#10207=ORIENTED_EDGE('',*,*,#7147,.T.);
#10208=ORIENTED_EDGE('',*,*,#7155,.T.);
#10209=ORIENTED_EDGE('',*,*,#7156,.T.);
#10210=ORIENTED_EDGE('',*,*,#7157,.F.);
#10211=ORIENTED_EDGE('',*,*,#7158,.F.);
#10212=ORIENTED_EDGE('',*,*,#7159,.F.);
#10213=ORIENTED_EDGE('',*,*,#7152,.T.);
#10214=ORIENTED_EDGE('',*,*,#7160,.T.);
#10215=ORIENTED_EDGE('',*,*,#7161,.T.);
#10216=ORIENTED_EDGE('',*,*,#7162,.F.);
#10217=ORIENTED_EDGE('',*,*,#7163,.F.);
#10218=ORIENTED_EDGE('',*,*,#7164,.F.);
#10219=ORIENTED_EDGE('',*,*,#7157,.T.);
#10220=ORIENTED_EDGE('',*,*,#7165,.T.);
#10221=ORIENTED_EDGE('',*,*,#7166,.T.);
#10222=ORIENTED_EDGE('',*,*,#7167,.F.);
#10223=ORIENTED_EDGE('',*,*,#7168,.F.);
#10224=ORIENTED_EDGE('',*,*,#7169,.F.);
#10225=ORIENTED_EDGE('',*,*,#7162,.T.);
#10226=ORIENTED_EDGE('',*,*,#7170,.T.);
#10227=ORIENTED_EDGE('',*,*,#7171,.T.);
#10228=ORIENTED_EDGE('',*,*,#7172,.F.);
#10229=ORIENTED_EDGE('',*,*,#7173,.F.);
#10230=ORIENTED_EDGE('',*,*,#7174,.F.);
#10231=ORIENTED_EDGE('',*,*,#7167,.T.);
#10232=ORIENTED_EDGE('',*,*,#7175,.T.);
#10233=ORIENTED_EDGE('',*,*,#7176,.T.);
#10234=ORIENTED_EDGE('',*,*,#7177,.F.);
#10235=ORIENTED_EDGE('',*,*,#7178,.F.);
#10236=ORIENTED_EDGE('',*,*,#7179,.F.);
#10237=ORIENTED_EDGE('',*,*,#7172,.T.);
#10238=ORIENTED_EDGE('',*,*,#7180,.T.);
#10239=ORIENTED_EDGE('',*,*,#7181,.T.);
#10240=ORIENTED_EDGE('',*,*,#7182,.F.);
#10241=ORIENTED_EDGE('',*,*,#7183,.F.);
#10242=ORIENTED_EDGE('',*,*,#7184,.F.);
#10243=ORIENTED_EDGE('',*,*,#7177,.T.);
#10244=ORIENTED_EDGE('',*,*,#7185,.T.);
#10245=ORIENTED_EDGE('',*,*,#7186,.T.);
#10246=ORIENTED_EDGE('',*,*,#7187,.F.);
#10247=ORIENTED_EDGE('',*,*,#7188,.F.);
#10248=ORIENTED_EDGE('',*,*,#7189,.F.);
#10249=ORIENTED_EDGE('',*,*,#7182,.T.);
#10250=ORIENTED_EDGE('',*,*,#7190,.T.);
#10251=ORIENTED_EDGE('',*,*,#7191,.T.);
#10252=ORIENTED_EDGE('',*,*,#7192,.F.);
#10253=ORIENTED_EDGE('',*,*,#7193,.F.);
#10254=ORIENTED_EDGE('',*,*,#7194,.F.);
#10255=ORIENTED_EDGE('',*,*,#7187,.T.);
#10256=ORIENTED_EDGE('',*,*,#7195,.T.);
#10257=ORIENTED_EDGE('',*,*,#7196,.T.);
#10258=ORIENTED_EDGE('',*,*,#7197,.F.);
#10259=ORIENTED_EDGE('',*,*,#7198,.F.);
#10260=ORIENTED_EDGE('',*,*,#7199,.F.);
#10261=ORIENTED_EDGE('',*,*,#7192,.T.);
#10262=ORIENTED_EDGE('',*,*,#7200,.T.);
#10263=ORIENTED_EDGE('',*,*,#7201,.T.);
#10264=ORIENTED_EDGE('',*,*,#7202,.F.);
#10265=ORIENTED_EDGE('',*,*,#7203,.F.);
#10266=ORIENTED_EDGE('',*,*,#7204,.F.);
#10267=ORIENTED_EDGE('',*,*,#7197,.T.);
#10268=ORIENTED_EDGE('',*,*,#7205,.T.);
#10269=ORIENTED_EDGE('',*,*,#7206,.T.);
#10270=ORIENTED_EDGE('',*,*,#7207,.F.);
#10271=ORIENTED_EDGE('',*,*,#7208,.F.);
#10272=ORIENTED_EDGE('',*,*,#7209,.F.);
#10273=ORIENTED_EDGE('',*,*,#7202,.T.);
#10274=ORIENTED_EDGE('',*,*,#7210,.T.);
#10275=ORIENTED_EDGE('',*,*,#7211,.T.);
#10276=ORIENTED_EDGE('',*,*,#7212,.F.);
#10277=ORIENTED_EDGE('',*,*,#7213,.F.);
#10278=ORIENTED_EDGE('',*,*,#7214,.F.);
#10279=ORIENTED_EDGE('',*,*,#7207,.T.);
#10280=ORIENTED_EDGE('',*,*,#7215,.T.);
#10281=ORIENTED_EDGE('',*,*,#7216,.T.);
#10282=ORIENTED_EDGE('',*,*,#7217,.F.);
#10283=ORIENTED_EDGE('',*,*,#7218,.F.);
#10284=ORIENTED_EDGE('',*,*,#7219,.F.);
#10285=ORIENTED_EDGE('',*,*,#7212,.T.);
#10286=ORIENTED_EDGE('',*,*,#7220,.T.);
#10287=ORIENTED_EDGE('',*,*,#7221,.T.);
#10288=ORIENTED_EDGE('',*,*,#7222,.F.);
#10289=ORIENTED_EDGE('',*,*,#7223,.F.);
#10290=ORIENTED_EDGE('',*,*,#7224,.F.);
#10291=ORIENTED_EDGE('',*,*,#7217,.T.);
#10292=ORIENTED_EDGE('',*,*,#7225,.T.);
#10293=ORIENTED_EDGE('',*,*,#7226,.T.);
#10294=ORIENTED_EDGE('',*,*,#7227,.F.);
#10295=ORIENTED_EDGE('',*,*,#7228,.F.);
#10296=ORIENTED_EDGE('',*,*,#7229,.F.);
#10297=ORIENTED_EDGE('',*,*,#7222,.T.);
#10298=ORIENTED_EDGE('',*,*,#7230,.T.);
#10299=ORIENTED_EDGE('',*,*,#7231,.T.);
#10300=ORIENTED_EDGE('',*,*,#7232,.F.);
#10301=ORIENTED_EDGE('',*,*,#7233,.F.);
#10302=ORIENTED_EDGE('',*,*,#7234,.F.);
#10303=ORIENTED_EDGE('',*,*,#7227,.T.);
#10304=ORIENTED_EDGE('',*,*,#7235,.T.);
#10305=ORIENTED_EDGE('',*,*,#7236,.T.);
#10306=ORIENTED_EDGE('',*,*,#7237,.F.);
#10307=ORIENTED_EDGE('',*,*,#7238,.F.);
#10308=ORIENTED_EDGE('',*,*,#7239,.F.);
#10309=ORIENTED_EDGE('',*,*,#7232,.T.);
#10310=ORIENTED_EDGE('',*,*,#7240,.T.);
#10311=ORIENTED_EDGE('',*,*,#7241,.T.);
#10312=ORIENTED_EDGE('',*,*,#7242,.F.);
#10313=ORIENTED_EDGE('',*,*,#7243,.F.);
#10314=ORIENTED_EDGE('',*,*,#7244,.F.);
#10315=ORIENTED_EDGE('',*,*,#7237,.T.);
#10316=ORIENTED_EDGE('',*,*,#7245,.T.);
#10317=ORIENTED_EDGE('',*,*,#7246,.T.);
#10318=ORIENTED_EDGE('',*,*,#7247,.F.);
#10319=ORIENTED_EDGE('',*,*,#7248,.F.);
#10320=ORIENTED_EDGE('',*,*,#7249,.F.);
#10321=ORIENTED_EDGE('',*,*,#7242,.T.);
#10322=ORIENTED_EDGE('',*,*,#7250,.T.);
#10323=ORIENTED_EDGE('',*,*,#7251,.T.);
#10324=ORIENTED_EDGE('',*,*,#7252,.F.);
#10325=ORIENTED_EDGE('',*,*,#7253,.F.);
#10326=ORIENTED_EDGE('',*,*,#7254,.F.);
#10327=ORIENTED_EDGE('',*,*,#7247,.T.);
#10328=ORIENTED_EDGE('',*,*,#7255,.T.);
#10329=ORIENTED_EDGE('',*,*,#7256,.T.);
#10330=ORIENTED_EDGE('',*,*,#7257,.F.);
#10331=ORIENTED_EDGE('',*,*,#7258,.F.);
#10332=ORIENTED_EDGE('',*,*,#7259,.F.);
#10333=ORIENTED_EDGE('',*,*,#7252,.T.);
#10334=ORIENTED_EDGE('',*,*,#7260,.T.);
#10335=ORIENTED_EDGE('',*,*,#7261,.T.);
#10336=ORIENTED_EDGE('',*,*,#7262,.F.);
#10337=ORIENTED_EDGE('',*,*,#7263,.F.);
#10338=ORIENTED_EDGE('',*,*,#7264,.F.);
#10339=ORIENTED_EDGE('',*,*,#7257,.T.);
#10340=ORIENTED_EDGE('',*,*,#7265,.T.);
#10341=ORIENTED_EDGE('',*,*,#7266,.T.);
#10342=ORIENTED_EDGE('',*,*,#7267,.F.);
#10343=ORIENTED_EDGE('',*,*,#7268,.F.);
#10344=ORIENTED_EDGE('',*,*,#7269,.F.);
#10345=ORIENTED_EDGE('',*,*,#7262,.T.);
#10346=ORIENTED_EDGE('',*,*,#7270,.T.);
#10347=ORIENTED_EDGE('',*,*,#7271,.T.);
#10348=ORIENTED_EDGE('',*,*,#7272,.F.);
#10349=ORIENTED_EDGE('',*,*,#7273,.F.);
#10350=ORIENTED_EDGE('',*,*,#7274,.F.);
#10351=ORIENTED_EDGE('',*,*,#7267,.T.);
#10352=ORIENTED_EDGE('',*,*,#7275,.T.);
#10353=ORIENTED_EDGE('',*,*,#7276,.T.);
#10354=ORIENTED_EDGE('',*,*,#7277,.F.);
#10355=ORIENTED_EDGE('',*,*,#7278,.F.);
#10356=ORIENTED_EDGE('',*,*,#7279,.F.);
#10357=ORIENTED_EDGE('',*,*,#7272,.T.);
#10358=ORIENTED_EDGE('',*,*,#7280,.T.);
#10359=ORIENTED_EDGE('',*,*,#7281,.T.);
#10360=ORIENTED_EDGE('',*,*,#7282,.F.);
#10361=ORIENTED_EDGE('',*,*,#7283,.F.);
#10362=ORIENTED_EDGE('',*,*,#7284,.F.);
#10363=ORIENTED_EDGE('',*,*,#7277,.T.);
#10364=ORIENTED_EDGE('',*,*,#7285,.T.);
#10365=ORIENTED_EDGE('',*,*,#7286,.T.);
#10366=ORIENTED_EDGE('',*,*,#7287,.F.);
#10367=ORIENTED_EDGE('',*,*,#7288,.F.);
#10368=ORIENTED_EDGE('',*,*,#7289,.F.);
#10369=ORIENTED_EDGE('',*,*,#7282,.T.);
#10370=ORIENTED_EDGE('',*,*,#7290,.T.);
#10371=ORIENTED_EDGE('',*,*,#7291,.T.);
#10372=ORIENTED_EDGE('',*,*,#7292,.F.);
#10373=ORIENTED_EDGE('',*,*,#7293,.F.);
#10374=ORIENTED_EDGE('',*,*,#7294,.F.);
#10375=ORIENTED_EDGE('',*,*,#7287,.T.);
#10376=ORIENTED_EDGE('',*,*,#7295,.T.);
#10377=ORIENTED_EDGE('',*,*,#7296,.T.);
#10378=ORIENTED_EDGE('',*,*,#7297,.F.);
#10379=ORIENTED_EDGE('',*,*,#7298,.F.);
#10380=ORIENTED_EDGE('',*,*,#7299,.F.);
#10381=ORIENTED_EDGE('',*,*,#7292,.T.);
#10382=ORIENTED_EDGE('',*,*,#7300,.T.);
#10383=ORIENTED_EDGE('',*,*,#7301,.T.);
#10384=ORIENTED_EDGE('',*,*,#7302,.F.);
#10385=ORIENTED_EDGE('',*,*,#7303,.F.);
#10386=ORIENTED_EDGE('',*,*,#7304,.F.);
#10387=ORIENTED_EDGE('',*,*,#7297,.T.);
#10388=ORIENTED_EDGE('',*,*,#7305,.T.);
#10389=ORIENTED_EDGE('',*,*,#7306,.T.);
#10390=ORIENTED_EDGE('',*,*,#7307,.F.);
#10391=ORIENTED_EDGE('',*,*,#7308,.F.);
#10392=ORIENTED_EDGE('',*,*,#7309,.F.);
#10393=ORIENTED_EDGE('',*,*,#7302,.T.);
#10394=ORIENTED_EDGE('',*,*,#7310,.T.);
#10395=ORIENTED_EDGE('',*,*,#7311,.T.);
#10396=ORIENTED_EDGE('',*,*,#7312,.F.);
#10397=ORIENTED_EDGE('',*,*,#7313,.F.);
#10398=ORIENTED_EDGE('',*,*,#7314,.F.);
#10399=ORIENTED_EDGE('',*,*,#7307,.T.);
#10400=ORIENTED_EDGE('',*,*,#7315,.T.);
#10401=ORIENTED_EDGE('',*,*,#7316,.T.);
#10402=ORIENTED_EDGE('',*,*,#7317,.F.);
#10403=ORIENTED_EDGE('',*,*,#7318,.F.);
#10404=ORIENTED_EDGE('',*,*,#7319,.F.);
#10405=ORIENTED_EDGE('',*,*,#7312,.T.);
#10406=ORIENTED_EDGE('',*,*,#7320,.T.);
#10407=ORIENTED_EDGE('',*,*,#7321,.T.);
#10408=ORIENTED_EDGE('',*,*,#7322,.F.);
#10409=ORIENTED_EDGE('',*,*,#7323,.F.);
#10410=ORIENTED_EDGE('',*,*,#7324,.F.);
#10411=ORIENTED_EDGE('',*,*,#7317,.T.);
#10412=ORIENTED_EDGE('',*,*,#7325,.T.);
#10413=ORIENTED_EDGE('',*,*,#7326,.T.);
#10414=ORIENTED_EDGE('',*,*,#7327,.F.);
#10415=ORIENTED_EDGE('',*,*,#7328,.F.);
#10416=ORIENTED_EDGE('',*,*,#7329,.F.);
#10417=ORIENTED_EDGE('',*,*,#7322,.T.);
#10418=ORIENTED_EDGE('',*,*,#7330,.T.);
#10419=ORIENTED_EDGE('',*,*,#7331,.T.);
#10420=ORIENTED_EDGE('',*,*,#7332,.F.);
#10421=ORIENTED_EDGE('',*,*,#7333,.F.);
#10422=ORIENTED_EDGE('',*,*,#7334,.F.);
#10423=ORIENTED_EDGE('',*,*,#7327,.T.);
#10424=ORIENTED_EDGE('',*,*,#7335,.T.);
#10425=ORIENTED_EDGE('',*,*,#7336,.T.);
#10426=ORIENTED_EDGE('',*,*,#7337,.F.);
#10427=ORIENTED_EDGE('',*,*,#7338,.F.);
#10428=ORIENTED_EDGE('',*,*,#7339,.F.);
#10429=ORIENTED_EDGE('',*,*,#7332,.T.);
#10430=ORIENTED_EDGE('',*,*,#7340,.T.);
#10431=ORIENTED_EDGE('',*,*,#7341,.T.);
#10432=ORIENTED_EDGE('',*,*,#7342,.F.);
#10433=ORIENTED_EDGE('',*,*,#7343,.F.);
#10434=ORIENTED_EDGE('',*,*,#7344,.F.);
#10435=ORIENTED_EDGE('',*,*,#7337,.T.);
#10436=ORIENTED_EDGE('',*,*,#7345,.T.);
#10437=ORIENTED_EDGE('',*,*,#7346,.T.);
#10438=ORIENTED_EDGE('',*,*,#7347,.F.);
#10439=ORIENTED_EDGE('',*,*,#7348,.F.);
#10440=ORIENTED_EDGE('',*,*,#7349,.F.);
#10441=ORIENTED_EDGE('',*,*,#7342,.T.);
#10442=ORIENTED_EDGE('',*,*,#7350,.T.);
#10443=ORIENTED_EDGE('',*,*,#7351,.T.);
#10444=ORIENTED_EDGE('',*,*,#7352,.F.);
#10445=ORIENTED_EDGE('',*,*,#7353,.F.);
#10446=ORIENTED_EDGE('',*,*,#7354,.F.);
#10447=ORIENTED_EDGE('',*,*,#7347,.T.);
#10448=ORIENTED_EDGE('',*,*,#7355,.T.);
#10449=ORIENTED_EDGE('',*,*,#7356,.T.);
#10450=ORIENTED_EDGE('',*,*,#7357,.T.);
#10451=ORIENTED_EDGE('',*,*,#7358,.F.);
#10452=ORIENTED_EDGE('',*,*,#7359,.T.);
#10453=ORIENTED_EDGE('',*,*,#7360,.T.);
#10454=ORIENTED_EDGE('',*,*,#7361,.T.);
#10455=ORIENTED_EDGE('',*,*,#7362,.T.);
#10456=ORIENTED_EDGE('',*,*,#7363,.T.);
#10457=ORIENTED_EDGE('',*,*,#7364,.T.);
#10458=ORIENTED_EDGE('',*,*,#7365,.T.);
#10459=ORIENTED_EDGE('',*,*,#7366,.T.);
#10460=ORIENTED_EDGE('',*,*,#7367,.T.);
#10461=ORIENTED_EDGE('',*,*,#7368,.T.);
#10462=ORIENTED_EDGE('',*,*,#7369,.T.);
#10463=ORIENTED_EDGE('',*,*,#7370,.T.);
#10464=ORIENTED_EDGE('',*,*,#7371,.T.);
#10465=ORIENTED_EDGE('',*,*,#7372,.T.);
#10466=ORIENTED_EDGE('',*,*,#7373,.T.);
#10467=ORIENTED_EDGE('',*,*,#7374,.T.);
#10468=ORIENTED_EDGE('',*,*,#7375,.T.);
#10469=ORIENTED_EDGE('',*,*,#7376,.T.);
#10470=ORIENTED_EDGE('',*,*,#7377,.T.);
#10471=ORIENTED_EDGE('',*,*,#7378,.T.);
#10472=ORIENTED_EDGE('',*,*,#7379,.T.);
#10473=ORIENTED_EDGE('',*,*,#7380,.T.);
#10474=ORIENTED_EDGE('',*,*,#7381,.T.);
#10475=ORIENTED_EDGE('',*,*,#7382,.T.);
#10476=ORIENTED_EDGE('',*,*,#7383,.T.);
#10477=ORIENTED_EDGE('',*,*,#7384,.T.);
#10478=ORIENTED_EDGE('',*,*,#7385,.T.);
#10479=ORIENTED_EDGE('',*,*,#7386,.T.);
#10480=ORIENTED_EDGE('',*,*,#7387,.T.);
#10481=ORIENTED_EDGE('',*,*,#7388,.T.);
#10482=ORIENTED_EDGE('',*,*,#7389,.T.);
#10483=ORIENTED_EDGE('',*,*,#7390,.T.);
#10484=ORIENTED_EDGE('',*,*,#7391,.T.);
#10485=ORIENTED_EDGE('',*,*,#7392,.T.);
#10486=ORIENTED_EDGE('',*,*,#7393,.T.);
#10487=ORIENTED_EDGE('',*,*,#7394,.T.);
#10488=ORIENTED_EDGE('',*,*,#7395,.T.);
#10489=ORIENTED_EDGE('',*,*,#7396,.T.);
#10490=ORIENTED_EDGE('',*,*,#7397,.T.);
#10491=ORIENTED_EDGE('',*,*,#7398,.T.);
#10492=ORIENTED_EDGE('',*,*,#7399,.T.);
#10493=ORIENTED_EDGE('',*,*,#7400,.F.);
#10494=ORIENTED_EDGE('',*,*,#7401,.T.);
#10495=ORIENTED_EDGE('',*,*,#7402,.T.);
#10496=ORIENTED_EDGE('',*,*,#7403,.T.);
#10497=ORIENTED_EDGE('',*,*,#7404,.T.);
#10498=ORIENTED_EDGE('',*,*,#7405,.T.);
#10499=ORIENTED_EDGE('',*,*,#7406,.T.);
#10500=ORIENTED_EDGE('',*,*,#7407,.T.);
#10501=ORIENTED_EDGE('',*,*,#7408,.T.);
#10502=ORIENTED_EDGE('',*,*,#7409,.T.);
#10503=ORIENTED_EDGE('',*,*,#7410,.T.);
#10504=ORIENTED_EDGE('',*,*,#7411,.T.);
#10505=ORIENTED_EDGE('',*,*,#7412,.T.);
#10506=ORIENTED_EDGE('',*,*,#7413,.T.);
#10507=ORIENTED_EDGE('',*,*,#7414,.T.);
#10508=ORIENTED_EDGE('',*,*,#7415,.T.);
#10509=ORIENTED_EDGE('',*,*,#7416,.T.);
#10510=ORIENTED_EDGE('',*,*,#7417,.T.);
#10511=ORIENTED_EDGE('',*,*,#7418,.T.);
#10512=ORIENTED_EDGE('',*,*,#7419,.T.);
#10513=ORIENTED_EDGE('',*,*,#7420,.T.);
#10514=ORIENTED_EDGE('',*,*,#7421,.T.);
#10515=ORIENTED_EDGE('',*,*,#7422,.T.);
#10516=ORIENTED_EDGE('',*,*,#7423,.T.);
#10517=ORIENTED_EDGE('',*,*,#7424,.T.);
#10518=ORIENTED_EDGE('',*,*,#7425,.T.);
#10519=ORIENTED_EDGE('',*,*,#7426,.T.);
#10520=ORIENTED_EDGE('',*,*,#7427,.T.);
#10521=ORIENTED_EDGE('',*,*,#7428,.T.);
#10522=ORIENTED_EDGE('',*,*,#7429,.T.);
#10523=ORIENTED_EDGE('',*,*,#7430,.T.);
#10524=ORIENTED_EDGE('',*,*,#7431,.T.);
#10525=ORIENTED_EDGE('',*,*,#7432,.T.);
#10526=ORIENTED_EDGE('',*,*,#7433,.T.);
#10527=ORIENTED_EDGE('',*,*,#7434,.T.);
#10528=ORIENTED_EDGE('',*,*,#7435,.T.);
#10529=ORIENTED_EDGE('',*,*,#7436,.T.);
#10530=ORIENTED_EDGE('',*,*,#7437,.T.);
#10531=ORIENTED_EDGE('',*,*,#7438,.T.);
#10532=ORIENTED_EDGE('',*,*,#7439,.T.);
#10533=ORIENTED_EDGE('',*,*,#7440,.T.);
#10534=ORIENTED_EDGE('',*,*,#7441,.T.);
#10535=ORIENTED_EDGE('',*,*,#7442,.T.);
#10536=ORIENTED_EDGE('',*,*,#7443,.T.);
#10537=ORIENTED_EDGE('',*,*,#7444,.T.);
#10538=ORIENTED_EDGE('',*,*,#7445,.T.);
#10539=ORIENTED_EDGE('',*,*,#7446,.T.);
#10540=ORIENTED_EDGE('',*,*,#7447,.T.);
#10541=ORIENTED_EDGE('',*,*,#7448,.T.);
#10542=ORIENTED_EDGE('',*,*,#7449,.T.);
#10543=ORIENTED_EDGE('',*,*,#7450,.T.);
#10544=ORIENTED_EDGE('',*,*,#7451,.T.);
#10545=ORIENTED_EDGE('',*,*,#7452,.T.);
#10546=ORIENTED_EDGE('',*,*,#7453,.T.);
#10547=ORIENTED_EDGE('',*,*,#7454,.T.);
#10548=ORIENTED_EDGE('',*,*,#7455,.T.);
#10549=ORIENTED_EDGE('',*,*,#7456,.T.);
#10550=ORIENTED_EDGE('',*,*,#7457,.T.);
#10551=ORIENTED_EDGE('',*,*,#7458,.T.);
#10552=ORIENTED_EDGE('',*,*,#7459,.T.);
#10553=ORIENTED_EDGE('',*,*,#7460,.T.);
#10554=ORIENTED_EDGE('',*,*,#7352,.T.);
#10555=ORIENTED_EDGE('',*,*,#7461,.T.);
#10556=ORIENTED_EDGE('',*,*,#7462,.T.);
#10557=ORIENTED_EDGE('',*,*,#7463,.F.);
#10558=ORIENTED_EDGE('',*,*,#7464,.F.);
#10559=ORIENTED_EDGE('',*,*,#7465,.F.);
#10560=ORIENTED_EDGE('',*,*,#7466,.F.);
#10561=ORIENTED_EDGE('',*,*,#7399,.F.);
#10562=ORIENTED_EDGE('',*,*,#7398,.F.);
#10563=ORIENTED_EDGE('',*,*,#7397,.F.);
#10564=ORIENTED_EDGE('',*,*,#7396,.F.);
#10565=ORIENTED_EDGE('',*,*,#7395,.F.);
#10566=ORIENTED_EDGE('',*,*,#7394,.F.);
#10567=ORIENTED_EDGE('',*,*,#7393,.F.);
#10568=ORIENTED_EDGE('',*,*,#7392,.F.);
#10569=ORIENTED_EDGE('',*,*,#7391,.F.);
#10570=ORIENTED_EDGE('',*,*,#7390,.F.);
#10571=ORIENTED_EDGE('',*,*,#7389,.F.);
#10572=ORIENTED_EDGE('',*,*,#7388,.F.);
#10573=ORIENTED_EDGE('',*,*,#7387,.F.);
#10574=ORIENTED_EDGE('',*,*,#7386,.F.);
#10575=ORIENTED_EDGE('',*,*,#7385,.F.);
#10576=ORIENTED_EDGE('',*,*,#7384,.F.);
#10577=ORIENTED_EDGE('',*,*,#7383,.F.);
#10578=ORIENTED_EDGE('',*,*,#7382,.F.);
#10579=ORIENTED_EDGE('',*,*,#7381,.F.);
#10580=ORIENTED_EDGE('',*,*,#7380,.F.);
#10581=ORIENTED_EDGE('',*,*,#7379,.F.);
#10582=ORIENTED_EDGE('',*,*,#7378,.F.);
#10583=ORIENTED_EDGE('',*,*,#7377,.F.);
#10584=ORIENTED_EDGE('',*,*,#7376,.F.);
#10585=ORIENTED_EDGE('',*,*,#7375,.F.);
#10586=ORIENTED_EDGE('',*,*,#7374,.F.);
#10587=ORIENTED_EDGE('',*,*,#7373,.F.);
#10588=ORIENTED_EDGE('',*,*,#7372,.F.);
#10589=ORIENTED_EDGE('',*,*,#7371,.F.);
#10590=ORIENTED_EDGE('',*,*,#7370,.F.);
#10591=ORIENTED_EDGE('',*,*,#7369,.F.);
#10592=ORIENTED_EDGE('',*,*,#7368,.F.);
#10593=ORIENTED_EDGE('',*,*,#7367,.F.);
#10594=ORIENTED_EDGE('',*,*,#7366,.F.);
#10595=ORIENTED_EDGE('',*,*,#7365,.F.);
#10596=ORIENTED_EDGE('',*,*,#7364,.F.);
#10597=ORIENTED_EDGE('',*,*,#7363,.F.);
#10598=ORIENTED_EDGE('',*,*,#7362,.F.);
#10599=ORIENTED_EDGE('',*,*,#7361,.F.);
#10600=ORIENTED_EDGE('',*,*,#7360,.F.);
#10601=ORIENTED_EDGE('',*,*,#7359,.F.);
#10602=ORIENTED_EDGE('',*,*,#7467,.F.);
#10603=ORIENTED_EDGE('',*,*,#7059,.T.);
#10604=ORIENTED_EDGE('',*,*,#7064,.T.);
#10605=ORIENTED_EDGE('',*,*,#7063,.T.);
#10606=ORIENTED_EDGE('',*,*,#7069,.T.);
#10607=ORIENTED_EDGE('',*,*,#7068,.T.);
#10608=ORIENTED_EDGE('',*,*,#7074,.T.);
#10609=ORIENTED_EDGE('',*,*,#7073,.T.);
#10610=ORIENTED_EDGE('',*,*,#7079,.T.);
#10611=ORIENTED_EDGE('',*,*,#7078,.T.);
#10612=ORIENTED_EDGE('',*,*,#7084,.T.);
#10613=ORIENTED_EDGE('',*,*,#7083,.T.);
#10614=ORIENTED_EDGE('',*,*,#7089,.T.);
#10615=ORIENTED_EDGE('',*,*,#7088,.T.);
#10616=ORIENTED_EDGE('',*,*,#7094,.T.);
#10617=ORIENTED_EDGE('',*,*,#7093,.T.);
#10618=ORIENTED_EDGE('',*,*,#7099,.T.);
#10619=ORIENTED_EDGE('',*,*,#7098,.T.);
#10620=ORIENTED_EDGE('',*,*,#7104,.T.);
#10621=ORIENTED_EDGE('',*,*,#7103,.T.);
#10622=ORIENTED_EDGE('',*,*,#7109,.T.);
#10623=ORIENTED_EDGE('',*,*,#7108,.T.);
#10624=ORIENTED_EDGE('',*,*,#7114,.T.);
#10625=ORIENTED_EDGE('',*,*,#7113,.T.);
#10626=ORIENTED_EDGE('',*,*,#7119,.T.);
#10627=ORIENTED_EDGE('',*,*,#7118,.T.);
#10628=ORIENTED_EDGE('',*,*,#7124,.T.);
#10629=ORIENTED_EDGE('',*,*,#7123,.T.);
#10630=ORIENTED_EDGE('',*,*,#7129,.T.);
#10631=ORIENTED_EDGE('',*,*,#7128,.T.);
#10632=ORIENTED_EDGE('',*,*,#7134,.T.);
#10633=ORIENTED_EDGE('',*,*,#7133,.T.);
#10634=ORIENTED_EDGE('',*,*,#7139,.T.);
#10635=ORIENTED_EDGE('',*,*,#7138,.T.);
#10636=ORIENTED_EDGE('',*,*,#7144,.T.);
#10637=ORIENTED_EDGE('',*,*,#7143,.T.);
#10638=ORIENTED_EDGE('',*,*,#7149,.T.);
#10639=ORIENTED_EDGE('',*,*,#7148,.T.);
#10640=ORIENTED_EDGE('',*,*,#7154,.T.);
#10641=ORIENTED_EDGE('',*,*,#7153,.T.);
#10642=ORIENTED_EDGE('',*,*,#7159,.T.);
#10643=ORIENTED_EDGE('',*,*,#7158,.T.);
#10644=ORIENTED_EDGE('',*,*,#7164,.T.);
#10645=ORIENTED_EDGE('',*,*,#7163,.T.);
#10646=ORIENTED_EDGE('',*,*,#7169,.T.);
#10647=ORIENTED_EDGE('',*,*,#7168,.T.);
#10648=ORIENTED_EDGE('',*,*,#7174,.T.);
#10649=ORIENTED_EDGE('',*,*,#7173,.T.);
#10650=ORIENTED_EDGE('',*,*,#7179,.T.);
#10651=ORIENTED_EDGE('',*,*,#7178,.T.);
#10652=ORIENTED_EDGE('',*,*,#7184,.T.);
#10653=ORIENTED_EDGE('',*,*,#7183,.T.);
#10654=ORIENTED_EDGE('',*,*,#7189,.T.);
#10655=ORIENTED_EDGE('',*,*,#7188,.T.);
#10656=ORIENTED_EDGE('',*,*,#7194,.T.);
#10657=ORIENTED_EDGE('',*,*,#7193,.T.);
#10658=ORIENTED_EDGE('',*,*,#7199,.T.);
#10659=ORIENTED_EDGE('',*,*,#7198,.T.);
#10660=ORIENTED_EDGE('',*,*,#7204,.T.);
#10661=ORIENTED_EDGE('',*,*,#7203,.T.);
#10662=ORIENTED_EDGE('',*,*,#7209,.T.);
#10663=ORIENTED_EDGE('',*,*,#7208,.T.);
#10664=ORIENTED_EDGE('',*,*,#7214,.T.);
#10665=ORIENTED_EDGE('',*,*,#7213,.T.);
#10666=ORIENTED_EDGE('',*,*,#7219,.T.);
#10667=ORIENTED_EDGE('',*,*,#7218,.T.);
#10668=ORIENTED_EDGE('',*,*,#7224,.T.);
#10669=ORIENTED_EDGE('',*,*,#7223,.T.);
#10670=ORIENTED_EDGE('',*,*,#7229,.T.);
#10671=ORIENTED_EDGE('',*,*,#7228,.T.);
#10672=ORIENTED_EDGE('',*,*,#7234,.T.);
#10673=ORIENTED_EDGE('',*,*,#7233,.T.);
#10674=ORIENTED_EDGE('',*,*,#7239,.T.);
#10675=ORIENTED_EDGE('',*,*,#7238,.T.);
#10676=ORIENTED_EDGE('',*,*,#7244,.T.);
#10677=ORIENTED_EDGE('',*,*,#7243,.T.);
#10678=ORIENTED_EDGE('',*,*,#7249,.T.);
#10679=ORIENTED_EDGE('',*,*,#7248,.T.);
#10680=ORIENTED_EDGE('',*,*,#7254,.T.);
#10681=ORIENTED_EDGE('',*,*,#7253,.T.);
#10682=ORIENTED_EDGE('',*,*,#7259,.T.);
#10683=ORIENTED_EDGE('',*,*,#7258,.T.);
#10684=ORIENTED_EDGE('',*,*,#7264,.T.);
#10685=ORIENTED_EDGE('',*,*,#7263,.T.);
#10686=ORIENTED_EDGE('',*,*,#7269,.T.);
#10687=ORIENTED_EDGE('',*,*,#7268,.T.);
#10688=ORIENTED_EDGE('',*,*,#7274,.T.);
#10689=ORIENTED_EDGE('',*,*,#7273,.T.);
#10690=ORIENTED_EDGE('',*,*,#7279,.T.);
#10691=ORIENTED_EDGE('',*,*,#7278,.T.);
#10692=ORIENTED_EDGE('',*,*,#7284,.T.);
#10693=ORIENTED_EDGE('',*,*,#7283,.T.);
#10694=ORIENTED_EDGE('',*,*,#7289,.T.);
#10695=ORIENTED_EDGE('',*,*,#7288,.T.);
#10696=ORIENTED_EDGE('',*,*,#7294,.T.);
#10697=ORIENTED_EDGE('',*,*,#7293,.T.);
#10698=ORIENTED_EDGE('',*,*,#7299,.T.);
#10699=ORIENTED_EDGE('',*,*,#7298,.T.);
#10700=ORIENTED_EDGE('',*,*,#7304,.T.);
#10701=ORIENTED_EDGE('',*,*,#7303,.T.);
#10702=ORIENTED_EDGE('',*,*,#7309,.T.);
#10703=ORIENTED_EDGE('',*,*,#7308,.T.);
#10704=ORIENTED_EDGE('',*,*,#7314,.T.);
#10705=ORIENTED_EDGE('',*,*,#7313,.T.);
#10706=ORIENTED_EDGE('',*,*,#7319,.T.);
#10707=ORIENTED_EDGE('',*,*,#7318,.T.);
#10708=ORIENTED_EDGE('',*,*,#7324,.T.);
#10709=ORIENTED_EDGE('',*,*,#7323,.T.);
#10710=ORIENTED_EDGE('',*,*,#7329,.T.);
#10711=ORIENTED_EDGE('',*,*,#7328,.T.);
#10712=ORIENTED_EDGE('',*,*,#7334,.T.);
#10713=ORIENTED_EDGE('',*,*,#7333,.T.);
#10714=ORIENTED_EDGE('',*,*,#7339,.T.);
#10715=ORIENTED_EDGE('',*,*,#7338,.T.);
#10716=ORIENTED_EDGE('',*,*,#7344,.T.);
#10717=ORIENTED_EDGE('',*,*,#7343,.T.);
#10718=ORIENTED_EDGE('',*,*,#7349,.T.);
#10719=ORIENTED_EDGE('',*,*,#7348,.T.);
#10720=ORIENTED_EDGE('',*,*,#7354,.T.);
#10721=ORIENTED_EDGE('',*,*,#7353,.T.);
#10722=ORIENTED_EDGE('',*,*,#7465,.T.);
#10723=ORIENTED_EDGE('',*,*,#7464,.T.);
#10724=ORIENTED_EDGE('',*,*,#7468,.F.);
#10725=ORIENTED_EDGE('',*,*,#7462,.F.);
#10726=ORIENTED_EDGE('',*,*,#7461,.F.);
#10727=ORIENTED_EDGE('',*,*,#7356,.F.);
#10728=ORIENTED_EDGE('',*,*,#7355,.F.);
#10729=ORIENTED_EDGE('',*,*,#7351,.F.);
#10730=ORIENTED_EDGE('',*,*,#7350,.F.);
#10731=ORIENTED_EDGE('',*,*,#7346,.F.);
#10732=ORIENTED_EDGE('',*,*,#7345,.F.);
#10733=ORIENTED_EDGE('',*,*,#7341,.F.);
#10734=ORIENTED_EDGE('',*,*,#7340,.F.);
#10735=ORIENTED_EDGE('',*,*,#7336,.F.);
#10736=ORIENTED_EDGE('',*,*,#7335,.F.);
#10737=ORIENTED_EDGE('',*,*,#7331,.F.);
#10738=ORIENTED_EDGE('',*,*,#7330,.F.);
#10739=ORIENTED_EDGE('',*,*,#7326,.F.);
#10740=ORIENTED_EDGE('',*,*,#7325,.F.);
#10741=ORIENTED_EDGE('',*,*,#7321,.F.);
#10742=ORIENTED_EDGE('',*,*,#7320,.F.);
#10743=ORIENTED_EDGE('',*,*,#7316,.F.);
#10744=ORIENTED_EDGE('',*,*,#7315,.F.);
#10745=ORIENTED_EDGE('',*,*,#7311,.F.);
#10746=ORIENTED_EDGE('',*,*,#7310,.F.);
#10747=ORIENTED_EDGE('',*,*,#7306,.F.);
#10748=ORIENTED_EDGE('',*,*,#7305,.F.);
#10749=ORIENTED_EDGE('',*,*,#7301,.F.);
#10750=ORIENTED_EDGE('',*,*,#7300,.F.);
#10751=ORIENTED_EDGE('',*,*,#7296,.F.);
#10752=ORIENTED_EDGE('',*,*,#7295,.F.);
#10753=ORIENTED_EDGE('',*,*,#7291,.F.);
#10754=ORIENTED_EDGE('',*,*,#7290,.F.);
#10755=ORIENTED_EDGE('',*,*,#7286,.F.);
#10756=ORIENTED_EDGE('',*,*,#7285,.F.);
#10757=ORIENTED_EDGE('',*,*,#7281,.F.);
#10758=ORIENTED_EDGE('',*,*,#7280,.F.);
#10759=ORIENTED_EDGE('',*,*,#7276,.F.);
#10760=ORIENTED_EDGE('',*,*,#7275,.F.);
#10761=ORIENTED_EDGE('',*,*,#7271,.F.);
#10762=ORIENTED_EDGE('',*,*,#7270,.F.);
#10763=ORIENTED_EDGE('',*,*,#7266,.F.);
#10764=ORIENTED_EDGE('',*,*,#7265,.F.);
#10765=ORIENTED_EDGE('',*,*,#7261,.F.);
#10766=ORIENTED_EDGE('',*,*,#7260,.F.);
#10767=ORIENTED_EDGE('',*,*,#7256,.F.);
#10768=ORIENTED_EDGE('',*,*,#7255,.F.);
#10769=ORIENTED_EDGE('',*,*,#7251,.F.);
#10770=ORIENTED_EDGE('',*,*,#7250,.F.);
#10771=ORIENTED_EDGE('',*,*,#7246,.F.);
#10772=ORIENTED_EDGE('',*,*,#7245,.F.);
#10773=ORIENTED_EDGE('',*,*,#7241,.F.);
#10774=ORIENTED_EDGE('',*,*,#7240,.F.);
#10775=ORIENTED_EDGE('',*,*,#7236,.F.);
#10776=ORIENTED_EDGE('',*,*,#7235,.F.);
#10777=ORIENTED_EDGE('',*,*,#7231,.F.);
#10778=ORIENTED_EDGE('',*,*,#7230,.F.);
#10779=ORIENTED_EDGE('',*,*,#7226,.F.);
#10780=ORIENTED_EDGE('',*,*,#7225,.F.);
#10781=ORIENTED_EDGE('',*,*,#7221,.F.);
#10782=ORIENTED_EDGE('',*,*,#7220,.F.);
#10783=ORIENTED_EDGE('',*,*,#7216,.F.);
#10784=ORIENTED_EDGE('',*,*,#7215,.F.);
#10785=ORIENTED_EDGE('',*,*,#7211,.F.);
#10786=ORIENTED_EDGE('',*,*,#7210,.F.);
#10787=ORIENTED_EDGE('',*,*,#7206,.F.);
#10788=ORIENTED_EDGE('',*,*,#7205,.F.);
#10789=ORIENTED_EDGE('',*,*,#7201,.F.);
#10790=ORIENTED_EDGE('',*,*,#7200,.F.);
#10791=ORIENTED_EDGE('',*,*,#7196,.F.);
#10792=ORIENTED_EDGE('',*,*,#7195,.F.);
#10793=ORIENTED_EDGE('',*,*,#7191,.F.);
#10794=ORIENTED_EDGE('',*,*,#7190,.F.);
#10795=ORIENTED_EDGE('',*,*,#7186,.F.);
#10796=ORIENTED_EDGE('',*,*,#7185,.F.);
#10797=ORIENTED_EDGE('',*,*,#7181,.F.);
#10798=ORIENTED_EDGE('',*,*,#7180,.F.);
#10799=ORIENTED_EDGE('',*,*,#7176,.F.);
#10800=ORIENTED_EDGE('',*,*,#7175,.F.);
#10801=ORIENTED_EDGE('',*,*,#7171,.F.);
#10802=ORIENTED_EDGE('',*,*,#7170,.F.);
#10803=ORIENTED_EDGE('',*,*,#7166,.F.);
#10804=ORIENTED_EDGE('',*,*,#7165,.F.);
#10805=ORIENTED_EDGE('',*,*,#7161,.F.);
#10806=ORIENTED_EDGE('',*,*,#7160,.F.);
#10807=ORIENTED_EDGE('',*,*,#7156,.F.);
#10808=ORIENTED_EDGE('',*,*,#7155,.F.);
#10809=ORIENTED_EDGE('',*,*,#7151,.F.);
#10810=ORIENTED_EDGE('',*,*,#7150,.F.);
#10811=ORIENTED_EDGE('',*,*,#7146,.F.);
#10812=ORIENTED_EDGE('',*,*,#7145,.F.);
#10813=ORIENTED_EDGE('',*,*,#7141,.F.);
#10814=ORIENTED_EDGE('',*,*,#7140,.F.);
#10815=ORIENTED_EDGE('',*,*,#7136,.F.);
#10816=ORIENTED_EDGE('',*,*,#7135,.F.);
#10817=ORIENTED_EDGE('',*,*,#7131,.F.);
#10818=ORIENTED_EDGE('',*,*,#7130,.F.);
#10819=ORIENTED_EDGE('',*,*,#7126,.F.);
#10820=ORIENTED_EDGE('',*,*,#7125,.F.);
#10821=ORIENTED_EDGE('',*,*,#7121,.F.);
#10822=ORIENTED_EDGE('',*,*,#7120,.F.);
#10823=ORIENTED_EDGE('',*,*,#7116,.F.);
#10824=ORIENTED_EDGE('',*,*,#7115,.F.);
#10825=ORIENTED_EDGE('',*,*,#7111,.F.);
#10826=ORIENTED_EDGE('',*,*,#7110,.F.);
#10827=ORIENTED_EDGE('',*,*,#7106,.F.);
#10828=ORIENTED_EDGE('',*,*,#7105,.F.);
#10829=ORIENTED_EDGE('',*,*,#7101,.F.);
#10830=ORIENTED_EDGE('',*,*,#7100,.F.);
#10831=ORIENTED_EDGE('',*,*,#7096,.F.);
#10832=ORIENTED_EDGE('',*,*,#7095,.F.);
#10833=ORIENTED_EDGE('',*,*,#7091,.F.);
#10834=ORIENTED_EDGE('',*,*,#7090,.F.);
#10835=ORIENTED_EDGE('',*,*,#7086,.F.);
#10836=ORIENTED_EDGE('',*,*,#7085,.F.);
#10837=ORIENTED_EDGE('',*,*,#7081,.F.);
#10838=ORIENTED_EDGE('',*,*,#7080,.F.);
#10839=ORIENTED_EDGE('',*,*,#7076,.F.);
#10840=ORIENTED_EDGE('',*,*,#7075,.F.);
#10841=ORIENTED_EDGE('',*,*,#7071,.F.);
#10842=ORIENTED_EDGE('',*,*,#7070,.F.);
#10843=ORIENTED_EDGE('',*,*,#7066,.F.);
#10844=ORIENTED_EDGE('',*,*,#7065,.F.);
#10845=ORIENTED_EDGE('',*,*,#7061,.F.);
#10846=ORIENTED_EDGE('',*,*,#7469,.F.);
#10847=ORIENTED_EDGE('',*,*,#7357,.F.);
#10848=ORIENTED_EDGE('',*,*,#7460,.F.);
#10849=ORIENTED_EDGE('',*,*,#7459,.F.);
#10850=ORIENTED_EDGE('',*,*,#7458,.F.);
#10851=ORIENTED_EDGE('',*,*,#7457,.F.);
#10852=ORIENTED_EDGE('',*,*,#7456,.F.);
#10853=ORIENTED_EDGE('',*,*,#7455,.F.);
#10854=ORIENTED_EDGE('',*,*,#7454,.F.);
#10855=ORIENTED_EDGE('',*,*,#7453,.F.);
#10856=ORIENTED_EDGE('',*,*,#7452,.F.);
#10857=ORIENTED_EDGE('',*,*,#7451,.F.);
#10858=ORIENTED_EDGE('',*,*,#7450,.F.);
#10859=ORIENTED_EDGE('',*,*,#7449,.F.);
#10860=ORIENTED_EDGE('',*,*,#7448,.F.);
#10861=ORIENTED_EDGE('',*,*,#7447,.F.);
#10862=ORIENTED_EDGE('',*,*,#7446,.F.);
#10863=ORIENTED_EDGE('',*,*,#7445,.F.);
#10864=ORIENTED_EDGE('',*,*,#7444,.F.);
#10865=ORIENTED_EDGE('',*,*,#7443,.F.);
#10866=ORIENTED_EDGE('',*,*,#7442,.F.);
#10867=ORIENTED_EDGE('',*,*,#7441,.F.);
#10868=ORIENTED_EDGE('',*,*,#7440,.F.);
#10869=ORIENTED_EDGE('',*,*,#7439,.F.);
#10870=ORIENTED_EDGE('',*,*,#7438,.F.);
#10871=ORIENTED_EDGE('',*,*,#7437,.F.);
#10872=ORIENTED_EDGE('',*,*,#7436,.F.);
#10873=ORIENTED_EDGE('',*,*,#7435,.F.);
#10874=ORIENTED_EDGE('',*,*,#7434,.F.);
#10875=ORIENTED_EDGE('',*,*,#7433,.F.);
#10876=ORIENTED_EDGE('',*,*,#7432,.F.);
#10877=ORIENTED_EDGE('',*,*,#7431,.F.);
#10878=ORIENTED_EDGE('',*,*,#7430,.F.);
#10879=ORIENTED_EDGE('',*,*,#7429,.F.);
#10880=ORIENTED_EDGE('',*,*,#7428,.F.);
#10881=ORIENTED_EDGE('',*,*,#7427,.F.);
#10882=ORIENTED_EDGE('',*,*,#7426,.F.);
#10883=ORIENTED_EDGE('',*,*,#7425,.F.);
#10884=ORIENTED_EDGE('',*,*,#7424,.F.);
#10885=ORIENTED_EDGE('',*,*,#7423,.F.);
#10886=ORIENTED_EDGE('',*,*,#7422,.F.);
#10887=ORIENTED_EDGE('',*,*,#7421,.F.);
#10888=ORIENTED_EDGE('',*,*,#7420,.F.);
#10889=ORIENTED_EDGE('',*,*,#7419,.F.);
#10890=ORIENTED_EDGE('',*,*,#7418,.F.);
#10891=ORIENTED_EDGE('',*,*,#7417,.F.);
#10892=ORIENTED_EDGE('',*,*,#7416,.F.);
#10893=ORIENTED_EDGE('',*,*,#7415,.F.);
#10894=ORIENTED_EDGE('',*,*,#7414,.F.);
#10895=ORIENTED_EDGE('',*,*,#7413,.F.);
#10896=ORIENTED_EDGE('',*,*,#7412,.F.);
#10897=ORIENTED_EDGE('',*,*,#7411,.F.);
#10898=ORIENTED_EDGE('',*,*,#7410,.F.);
#10899=ORIENTED_EDGE('',*,*,#7409,.F.);
#10900=ORIENTED_EDGE('',*,*,#7408,.F.);
#10901=ORIENTED_EDGE('',*,*,#7407,.F.);
#10902=ORIENTED_EDGE('',*,*,#7406,.F.);
#10903=ORIENTED_EDGE('',*,*,#7405,.F.);
#10904=ORIENTED_EDGE('',*,*,#7404,.F.);
#10905=ORIENTED_EDGE('',*,*,#7403,.F.);
#10906=ORIENTED_EDGE('',*,*,#7402,.F.);
#10907=ORIENTED_EDGE('',*,*,#7401,.F.);
#10908=ORIENTED_EDGE('',*,*,#7470,.F.);
#10909=ORIENTED_EDGE('',*,*,#7471,.T.);
#10910=ORIENTED_EDGE('',*,*,#7472,.F.);
#10911=ORIENTED_EDGE('',*,*,#7471,.F.);
#10912=ORIENTED_EDGE('',*,*,#7473,.F.);
#10913=ORIENTED_EDGE('',*,*,#7474,.T.);
#10914=ORIENTED_EDGE('',*,*,#7475,.F.);
#10915=ORIENTED_EDGE('',*,*,#7474,.F.);
#10916=ORIENTED_EDGE('',*,*,#7476,.F.);
#10917=ORIENTED_EDGE('',*,*,#7477,.T.);
#10918=ORIENTED_EDGE('',*,*,#7478,.F.);
#10919=ORIENTED_EDGE('',*,*,#7477,.F.);
#10920=ORIENTED_EDGE('',*,*,#7479,.F.);
#10921=ORIENTED_EDGE('',*,*,#7480,.T.);
#10922=ORIENTED_EDGE('',*,*,#7481,.F.);
#10923=ORIENTED_EDGE('',*,*,#7480,.F.);
#10924=ORIENTED_EDGE('',*,*,#7482,.T.);
#10925=ORIENTED_EDGE('',*,*,#7483,.T.);
#10926=ORIENTED_EDGE('',*,*,#7484,.T.);
#10927=ORIENTED_EDGE('',*,*,#7483,.F.);
#10928=ORIENTED_EDGE('',*,*,#7485,.T.);
#10929=ORIENTED_EDGE('',*,*,#7486,.F.);
#10930=ORIENTED_EDGE('',*,*,#7487,.F.);
#10931=ORIENTED_EDGE('',*,*,#7488,.T.);
#10932=ORIENTED_EDGE('',*,*,#7485,.F.);
#10933=ORIENTED_EDGE('',*,*,#7482,.F.);
#10934=ORIENTED_EDGE('',*,*,#7488,.F.);
#10935=ORIENTED_EDGE('',*,*,#7484,.F.);
#10936=ORIENTED_EDGE('',*,*,#7400,.T.);
#10937=ORIENTED_EDGE('',*,*,#7466,.T.);
#10938=ORIENTED_EDGE('',*,*,#7463,.T.);
#10939=ORIENTED_EDGE('',*,*,#7468,.T.);
#10940=ORIENTED_EDGE('',*,*,#7481,.T.);
#10941=ORIENTED_EDGE('',*,*,#7478,.T.);
#10942=ORIENTED_EDGE('',*,*,#7475,.T.);
#10943=ORIENTED_EDGE('',*,*,#7472,.T.);
#10944=ORIENTED_EDGE('',*,*,#7489,.T.);
#10945=ORIENTED_EDGE('',*,*,#7490,.T.);
#10946=ORIENTED_EDGE('',*,*,#7486,.T.);
#10947=ORIENTED_EDGE('',*,*,#7487,.T.);
#10948=ORIENTED_EDGE('',*,*,#7490,.F.);
#10949=ORIENTED_EDGE('',*,*,#7489,.F.);
#10950=ORIENTED_EDGE('',*,*,#7470,.T.);
#10951=ORIENTED_EDGE('',*,*,#7473,.T.);
#10952=ORIENTED_EDGE('',*,*,#7476,.T.);
#10953=ORIENTED_EDGE('',*,*,#7479,.T.);
#10954=ORIENTED_EDGE('',*,*,#7467,.T.);
#10955=ORIENTED_EDGE('',*,*,#7358,.T.);
#10956=ORIENTED_EDGE('',*,*,#7469,.T.);
#10957=ORIENTED_EDGE('',*,*,#7060,.T.);
#12169=CYLINDRICAL_SURFACE('',#13736,6.767);
#12170=CYLINDRICAL_SURFACE('',#13738,6.767);
#12171=CYLINDRICAL_SURFACE('',#13739,6.767);
#12172=CYLINDRICAL_SURFACE('',#13740,6.767);
#12173=CYLINDRICAL_SURFACE('',#13741,6.767);
#12174=CYLINDRICAL_SURFACE('',#13742,6.767);
#12175=CYLINDRICAL_SURFACE('',#13743,6.767);
#12176=CYLINDRICAL_SURFACE('',#13744,6.767);
#12177=CYLINDRICAL_SURFACE('',#13745,6.767);
#12178=CYLINDRICAL_SURFACE('',#13746,6.767);
#12179=CYLINDRICAL_SURFACE('',#13747,6.767);
#12180=CYLINDRICAL_SURFACE('',#13748,6.767);
#12181=CYLINDRICAL_SURFACE('',#13749,6.767);
#12182=CYLINDRICAL_SURFACE('',#13750,6.767);
#12183=CYLINDRICAL_SURFACE('',#13751,6.767);
#12184=CYLINDRICAL_SURFACE('',#13752,6.767);
#12185=CYLINDRICAL_SURFACE('',#13753,6.767);
#12186=CYLINDRICAL_SURFACE('',#13754,6.767);
#12187=CYLINDRICAL_SURFACE('',#13755,6.767);
#12188=CYLINDRICAL_SURFACE('',#13756,6.767);
#12189=CYLINDRICAL_SURFACE('',#13757,6.767);
#12190=CYLINDRICAL_SURFACE('',#13758,6.767);
#12191=CYLINDRICAL_SURFACE('',#13759,6.767);
#12192=CYLINDRICAL_SURFACE('',#13760,6.767);
#12193=CYLINDRICAL_SURFACE('',#13761,6.767);
#12194=CYLINDRICAL_SURFACE('',#13762,6.767);
#12195=CYLINDRICAL_SURFACE('',#13763,6.767);
#12196=CYLINDRICAL_SURFACE('',#13764,6.767);
#12197=CYLINDRICAL_SURFACE('',#13765,6.767);
#12198=CYLINDRICAL_SURFACE('',#13766,6.767);
#12199=CYLINDRICAL_SURFACE('',#13767,6.767);
#12200=CYLINDRICAL_SURFACE('',#13768,6.767);
#12201=CYLINDRICAL_SURFACE('',#13769,6.767);
#12202=CYLINDRICAL_SURFACE('',#13770,6.767);
#12203=CYLINDRICAL_SURFACE('',#13771,6.767);
#12204=CYLINDRICAL_SURFACE('',#13772,6.767);
#12205=CYLINDRICAL_SURFACE('',#13773,6.767);
#12206=CYLINDRICAL_SURFACE('',#13774,6.767);
#12207=CYLINDRICAL_SURFACE('',#13775,6.767);
#12208=CYLINDRICAL_SURFACE('',#13776,6.767);
#12209=CYLINDRICAL_SURFACE('',#13777,6.767);
#12210=CYLINDRICAL_SURFACE('',#13778,6.767);
#12211=CYLINDRICAL_SURFACE('',#13779,6.767);
#12212=CYLINDRICAL_SURFACE('',#13780,6.767);
#12213=CYLINDRICAL_SURFACE('',#13781,6.767);
#12214=CYLINDRICAL_SURFACE('',#13782,6.767);
#12215=CYLINDRICAL_SURFACE('',#13783,6.767);
#12216=CYLINDRICAL_SURFACE('',#13784,6.767);
#12217=CYLINDRICAL_SURFACE('',#13785,6.767);
#12218=CYLINDRICAL_SURFACE('',#13786,6.767);
#12219=CYLINDRICAL_SURFACE('',#13787,6.767);
#12220=CYLINDRICAL_SURFACE('',#13788,6.767);
#12221=CYLINDRICAL_SURFACE('',#13789,6.767);
#12222=CYLINDRICAL_SURFACE('',#13790,6.767);
#12223=CYLINDRICAL_SURFACE('',#13791,6.767);
#12224=CYLINDRICAL_SURFACE('',#13792,6.767);
#12225=CYLINDRICAL_SURFACE('',#13793,6.767);
#12226=CYLINDRICAL_SURFACE('',#13794,6.767);
#12227=CYLINDRICAL_SURFACE('',#13795,6.767);
#12228=CYLINDRICAL_SURFACE('',#13796,6.767);
#12229=CYLINDRICAL_SURFACE('',#13797,7.911);
#12230=CYLINDRICAL_SURFACE('',#13800,6.767);
#12231=CYLINDRICAL_SURFACE('',#13802,2.);
#12232=CYLINDRICAL_SURFACE('',#13805,2.);
#12233=CYLINDRICAL_SURFACE('',#13808,2.);
#12234=CYLINDRICAL_SURFACE('',#13811,2.);
#12235=CYLINDRICAL_SURFACE('',#13819,20.);
#12652=ADVANCED_FACE('',(#1122),#12169,.T.);
#12653=ADVANCED_FACE('',(#1123),#12170,.T.);
#12654=ADVANCED_FACE('',(#1124),#12171,.T.);
#12655=ADVANCED_FACE('',(#1125),#12172,.T.);
#12656=ADVANCED_FACE('',(#1126),#12173,.T.);
#12657=ADVANCED_FACE('',(#1127),#12174,.T.);
#12658=ADVANCED_FACE('',(#1128),#12175,.T.);
#12659=ADVANCED_FACE('',(#1129),#12176,.T.);
#12660=ADVANCED_FACE('',(#1130),#12177,.T.);
#12661=ADVANCED_FACE('',(#1131),#12178,.T.);
#12662=ADVANCED_FACE('',(#1132),#12179,.T.);
#12663=ADVANCED_FACE('',(#1133),#12180,.T.);
#12664=ADVANCED_FACE('',(#1134),#12181,.T.);
#12665=ADVANCED_FACE('',(#1135),#12182,.T.);
#12666=ADVANCED_FACE('',(#1136),#12183,.T.);
#12667=ADVANCED_FACE('',(#1137),#12184,.T.);
#12668=ADVANCED_FACE('',(#1138),#12185,.T.);
#12669=ADVANCED_FACE('',(#1139),#12186,.T.);
#12670=ADVANCED_FACE('',(#1140),#12187,.T.);
#12671=ADVANCED_FACE('',(#1141),#12188,.T.);
#12672=ADVANCED_FACE('',(#1142),#12189,.T.);
#12673=ADVANCED_FACE('',(#1143),#12190,.T.);
#12674=ADVANCED_FACE('',(#1144),#12191,.T.);
#12675=ADVANCED_FACE('',(#1145),#12192,.T.);
#12676=ADVANCED_FACE('',(#1146),#12193,.T.);
#12677=ADVANCED_FACE('',(#1147),#12194,.T.);
#12678=ADVANCED_FACE('',(#1148),#12195,.T.);
#12679=ADVANCED_FACE('',(#1149),#12196,.T.);
#12680=ADVANCED_FACE('',(#1150),#12197,.T.);
#12681=ADVANCED_FACE('',(#1151),#12198,.T.);
#12682=ADVANCED_FACE('',(#1152),#12199,.T.);
#12683=ADVANCED_FACE('',(#1153),#12200,.T.);
#12684=ADVANCED_FACE('',(#1154),#12201,.T.);
#12685=ADVANCED_FACE('',(#1155),#12202,.T.);
#12686=ADVANCED_FACE('',(#1156),#12203,.T.);
#12687=ADVANCED_FACE('',(#1157),#12204,.T.);
#12688=ADVANCED_FACE('',(#1158),#12205,.T.);
#12689=ADVANCED_FACE('',(#1159),#12206,.T.);
#12690=ADVANCED_FACE('',(#1160),#12207,.T.);
#12691=ADVANCED_FACE('',(#1161),#12208,.T.);
#12692=ADVANCED_FACE('',(#1162),#12209,.T.);
#12693=ADVANCED_FACE('',(#1163),#12210,.T.);
#12694=ADVANCED_FACE('',(#1164),#12211,.T.);
#12695=ADVANCED_FACE('',(#1165),#12212,.T.);
#12696=ADVANCED_FACE('',(#1166),#12213,.T.);
#12697=ADVANCED_FACE('',(#1167),#12214,.T.);
#12698=ADVANCED_FACE('',(#1168),#12215,.T.);
#12699=ADVANCED_FACE('',(#1169),#12216,.T.);
#12700=ADVANCED_FACE('',(#1170),#12217,.T.);
#12701=ADVANCED_FACE('',(#1171),#12218,.T.);
#12702=ADVANCED_FACE('',(#1172),#12219,.T.);
#12703=ADVANCED_FACE('',(#1173),#12220,.T.);
#12704=ADVANCED_FACE('',(#1174),#12221,.T.);
#12705=ADVANCED_FACE('',(#1175),#12222,.T.);
#12706=ADVANCED_FACE('',(#1176),#12223,.T.);
#12707=ADVANCED_FACE('',(#1177),#12224,.T.);
#12708=ADVANCED_FACE('',(#1178),#12225,.T.);
#12709=ADVANCED_FACE('',(#1179),#12226,.T.);
#12710=ADVANCED_FACE('',(#1180),#12227,.T.);
#12711=ADVANCED_FACE('',(#1181),#12228,.T.);
#12712=ADVANCED_FACE('',(#1182),#12229,.T.);
#12713=ADVANCED_FACE('',(#1183),#12230,.T.);
#12714=ADVANCED_FACE('',(#1184),#756,.F.);
#12715=ADVANCED_FACE('',(#1185),#757,.F.);
#12716=ADVANCED_FACE('',(#1186),#12231,.F.);
#12717=ADVANCED_FACE('',(#1187),#12232,.F.);
#12718=ADVANCED_FACE('',(#1188),#12233,.F.);
#12719=ADVANCED_FACE('',(#1189),#12234,.F.);
#12720=ADVANCED_FACE('',(#1190),#171,.T.);
#12721=ADVANCED_FACE('',(#1191),#12235,.T.);
#12722=ADVANCED_FACE('',(#1192,#357,#358,#359,#360,#361),#516,.F.);
#12723=ADVANCED_FACE('',(#1193),#172,.T.);
#12724=ADVANCED_FACE('',(#1194,#362,#363,#364,#365),#517,.T.);
#12725=ADVANCED_FACE('',(#1195),#518,.F.);
#12994=CLOSED_SHELL('',(#12652,#12653,#12654,#12655,#12656,#12657,#12658,
#12659,#12660,#12661,#12662,#12663,#12664,#12665,#12666,#12667,#12668,#12669,
#12670,#12671,#12672,#12673,#12674,#12675,#12676,#12677,#12678,#12679,#12680,
#12681,#12682,#12683,#12684,#12685,#12686,#12687,#12688,#12689,#12690,#12691,
#12692,#12693,#12694,#12695,#12696,#12697,#12698,#12699,#12700,#12701,#12702,
#12703,#12704,#12705,#12706,#12707,#12708,#12709,#12710,#12711,#12712,#12713,
#12714,#12715,#12716,#12717,#12718,#12719,#12720,#12721,#12722,#12723,#12724,
#12725));
#13735=AXIS2_PLACEMENT_3D('',#33015,#15840,#15841);
#13736=AXIS2_PLACEMENT_3D('',#33016,#15842,#15843);
#13737=AXIS2_PLACEMENT_3D('',#33155,#15845,#15846);
#13738=AXIS2_PLACEMENT_3D('',#33238,#15847,#15848);
#13739=AXIS2_PLACEMENT_3D('',#33737,#15850,#15851);
#13740=AXIS2_PLACEMENT_3D('',#34233,#15853,#15854);
#13741=AXIS2_PLACEMENT_3D('',#34741,#15856,#15857);
#13742=AXIS2_PLACEMENT_3D('',#35249,#15859,#15860);
#13743=AXIS2_PLACEMENT_3D('',#35745,#15862,#15863);
#13744=AXIS2_PLACEMENT_3D('',#36247,#15865,#15866);
#13745=AXIS2_PLACEMENT_3D('',#36743,#15868,#15869);
#13746=AXIS2_PLACEMENT_3D('',#37230,#15871,#15872);
#13747=AXIS2_PLACEMENT_3D('',#37729,#15874,#15875);
#13748=AXIS2_PLACEMENT_3D('',#38237,#15877,#15878);
#13749=AXIS2_PLACEMENT_3D('',#38730,#15880,#15881);
#13750=AXIS2_PLACEMENT_3D('',#39226,#15883,#15884);
#13751=AXIS2_PLACEMENT_3D('',#39734,#15886,#15887);
#13752=AXIS2_PLACEMENT_3D('',#40242,#15889,#15890);
#13753=AXIS2_PLACEMENT_3D('',#40741,#15892,#15893);
#13754=AXIS2_PLACEMENT_3D('',#41237,#15895,#15896);
#13755=AXIS2_PLACEMENT_3D('',#41730,#15898,#15899);
#13756=AXIS2_PLACEMENT_3D('',#42217,#15901,#15902);
#13757=AXIS2_PLACEMENT_3D('',#42719,#15904,#15905);
#13758=AXIS2_PLACEMENT_3D('',#43227,#15907,#15908);
#13759=AXIS2_PLACEMENT_3D('',#43720,#15910,#15911);
#13760=AXIS2_PLACEMENT_3D('',#44222,#15913,#15914);
#13761=AXIS2_PLACEMENT_3D('',#44730,#15916,#15917);
#13762=AXIS2_PLACEMENT_3D('',#45235,#15919,#15920);
#13763=AXIS2_PLACEMENT_3D('',#45731,#15922,#15923);
#13764=AXIS2_PLACEMENT_3D('',#46227,#15925,#15926);
#13765=AXIS2_PLACEMENT_3D('',#46720,#15928,#15929);
#13766=AXIS2_PLACEMENT_3D('',#47204,#15931,#15932);
#13767=AXIS2_PLACEMENT_3D('',#47706,#15934,#15935);
#13768=AXIS2_PLACEMENT_3D('',#48214,#15937,#15938);
#13769=AXIS2_PLACEMENT_3D('',#48719,#15940,#15941);
#13770=AXIS2_PLACEMENT_3D('',#49212,#15943,#15944);
#13771=AXIS2_PLACEMENT_3D('',#49711,#15946,#15947);
#13772=AXIS2_PLACEMENT_3D('',#50195,#15949,#15950);
#13773=AXIS2_PLACEMENT_3D('',#50676,#15952,#15953);
#13774=AXIS2_PLACEMENT_3D('',#51178,#15955,#15956);
#13775=AXIS2_PLACEMENT_3D('',#51680,#15958,#15959);
#13776=AXIS2_PLACEMENT_3D('',#52185,#15961,#15962);
#13777=AXIS2_PLACEMENT_3D('',#52672,#15964,#15965);
#13778=AXIS2_PLACEMENT_3D('',#53165,#15967,#15968);
#13779=AXIS2_PLACEMENT_3D('',#53676,#15970,#15971);
#13780=AXIS2_PLACEMENT_3D('',#54169,#15973,#15974);
#13781=AXIS2_PLACEMENT_3D('',#54668,#15976,#15977);
#13782=AXIS2_PLACEMENT_3D('',#55152,#15979,#15980);
#13783=AXIS2_PLACEMENT_3D('',#55633,#15982,#15983);
#13784=AXIS2_PLACEMENT_3D('',#56132,#15985,#15986);
#13785=AXIS2_PLACEMENT_3D('',#56637,#15988,#15989);
#13786=AXIS2_PLACEMENT_3D('',#57133,#15991,#15992);
#13787=AXIS2_PLACEMENT_3D('',#57626,#15994,#15995);
#13788=AXIS2_PLACEMENT_3D('',#58122,#15997,#15998);
#13789=AXIS2_PLACEMENT_3D('',#58630,#16000,#16001);
#13790=AXIS2_PLACEMENT_3D('',#59117,#16003,#16004);
#13791=AXIS2_PLACEMENT_3D('',#59622,#16006,#16007);
#13792=AXIS2_PLACEMENT_3D('',#60106,#16009,#16010);
#13793=AXIS2_PLACEMENT_3D('',#60584,#16012,#16013);
#13794=AXIS2_PLACEMENT_3D('',#61083,#16015,#16016);
#13795=AXIS2_PLACEMENT_3D('',#61588,#16018,#16019);
#13796=AXIS2_PLACEMENT_3D('',#62084,#16021,#16022);
#13797=AXIS2_PLACEMENT_3D('',#62565,#16024,#16025);
#13798=AXIS2_PLACEMENT_3D('',#62577,#16026,#16027);
#13799=AXIS2_PLACEMENT_3D('',#74537,#16028,#16029);
#13800=AXIS2_PLACEMENT_3D('',#76818,#16030,#16031);
#13801=AXIS2_PLACEMENT_3D('',#76986,#16032,#16033);
#13802=AXIS2_PLACEMENT_3D('',#81914,#16034,#16035);
#13803=AXIS2_PLACEMENT_3D('',#81916,#16036,#16037);
#13804=AXIS2_PLACEMENT_3D('',#81919,#16039,#16040);
#13805=AXIS2_PLACEMENT_3D('',#81920,#16041,#16042);
#13806=AXIS2_PLACEMENT_3D('',#81922,#16043,#16044);
#13807=AXIS2_PLACEMENT_3D('',#81925,#16046,#16047);
#13808=AXIS2_PLACEMENT_3D('',#81926,#16048,#16049);
#13809=AXIS2_PLACEMENT_3D('',#81928,#16050,#16051);
#13810=AXIS2_PLACEMENT_3D('',#81931,#16053,#16054);
#13811=AXIS2_PLACEMENT_3D('',#81932,#16055,#16056);
#13812=AXIS2_PLACEMENT_3D('',#81934,#16057,#16058);
#13813=AXIS2_PLACEMENT_3D('',#81937,#16060,#16061);
#13814=AXIS2_PLACEMENT_3D('',#81938,#16062,#16063);
#13815=AXIS2_PLACEMENT_3D('',#81941,#16064,#16065);
#13816=AXIS2_PLACEMENT_3D('',#81943,#16066,#16067);
#13817=AXIS2_PLACEMENT_3D('',#81944,#16068,#16069);
#13818=AXIS2_PLACEMENT_3D('',#81945,#16070,#16071);
#13819=AXIS2_PLACEMENT_3D('',#81946,#16072,#16073);
#13820=AXIS2_PLACEMENT_3D('',#81949,#16074,#16075);
#13821=AXIS2_PLACEMENT_3D('',#81950,#16076,#16077);
#13822=AXIS2_PLACEMENT_3D('',#81952,#16079,#16080);
#13823=AXIS2_PLACEMENT_3D('',#81953,#16081,#16082);
#13824=AXIS2_PLACEMENT_3D('',#81955,#16083,#16084);
#13825=AXIS2_PLACEMENT_3D('',#81956,#16085,#16086);
#13826=AXIS2_PLACEMENT_3D('',#81957,#16087,#16088);
#13827=AXIS2_PLACEMENT_3D('',#81958,#16089,#16090);
#15840=DIRECTION('axis',(0.,0.,1.));
#15841=DIRECTION('refdir',(1.,0.,0.));
#15842=DIRECTION('center_axis',(0.,0.,1.));
#15843=DIRECTION('ref_axis',(-0.457970371486214,-0.888967456570137,0.));
#15844=DIRECTION('',(0.,0.,-1.));
#15845=DIRECTION('center_axis',(0.,0.,-1.));
#15846=DIRECTION('ref_axis',(1.,-9.05137471385603E-13,0.));
#15847=DIRECTION('center_axis',(0.,0.,1.));
#15848=DIRECTION('ref_axis',(-0.457970371486214,-0.888967456570137,0.));
#15849=DIRECTION('',(0.,0.,-1.));
#15850=DIRECTION('center_axis',(0.,0.,1.));
#15851=DIRECTION('ref_axis',(-0.457970371486214,-0.888967456570137,0.));
#15852=DIRECTION('',(0.,0.,-1.));
#15853=DIRECTION('center_axis',(0.,0.,1.));
#15854=DIRECTION('ref_axis',(-0.457970371486214,-0.888967456570137,0.));
#15855=DIRECTION('',(0.,0.,-1.));
#15856=DIRECTION('center_axis',(0.,0.,1.));
#15857=DIRECTION('ref_axis',(-0.457970371486214,-0.888967456570137,0.));
#15858=DIRECTION('',(0.,0.,-1.));
#15859=DIRECTION('center_axis',(0.,0.,1.));
#15860=DIRECTION('ref_axis',(-0.457970371486214,-0.888967456570137,0.));
#15861=DIRECTION('',(0.,0.,-1.));
#15862=DIRECTION('center_axis',(0.,0.,1.));
#15863=DIRECTION('ref_axis',(-0.457970371486214,-0.888967456570137,0.));
#15864=DIRECTION('',(0.,0.,-1.));
#15865=DIRECTION('center_axis',(0.,0.,1.));
#15866=DIRECTION('ref_axis',(-0.457970371486214,-0.888967456570137,0.));
#15867=DIRECTION('',(0.,0.,-1.));
#15868=DIRECTION('center_axis',(0.,0.,1.));
#15869=DIRECTION('ref_axis',(-0.457970371486214,-0.888967456570137,0.));
#15870=DIRECTION('',(0.,0.,-1.));
#15871=DIRECTION('center_axis',(0.,0.,1.));
#15872=DIRECTION('ref_axis',(-0.457970371486214,-0.888967456570137,0.));
#15873=DIRECTION('',(0.,0.,-1.));
#15874=DIRECTION('center_axis',(0.,0.,1.));
#15875=DIRECTION('ref_axis',(-0.457970371486214,-0.888967456570137,0.));
#15876=DIRECTION('',(0.,0.,-1.));
#15877=DIRECTION('center_axis',(0.,0.,1.));
#15878=DIRECTION('ref_axis',(-0.457970371486214,-0.888967456570137,0.));
#15879=DIRECTION('',(0.,0.,-1.));
#15880=DIRECTION('center_axis',(0.,0.,1.));
#15881=DIRECTION('ref_axis',(-0.457970371486214,-0.888967456570137,0.));
#15882=DIRECTION('',(0.,0.,-1.));
#15883=DIRECTION('center_axis',(0.,0.,1.));
#15884=DIRECTION('ref_axis',(-0.457970371486214,-0.888967456570137,0.));
#15885=DIRECTION('',(0.,0.,-1.));
#15886=DIRECTION('center_axis',(0.,0.,1.));
#15887=DIRECTION('ref_axis',(-0.457970371486214,-0.888967456570137,0.));
#15888=DIRECTION('',(0.,0.,-1.));
#15889=DIRECTION('center_axis',(0.,0.,1.));
#15890=DIRECTION('ref_axis',(-0.457970371486214,-0.888967456570137,0.));
#15891=DIRECTION('',(0.,0.,-1.));
#15892=DIRECTION('center_axis',(0.,0.,1.));
#15893=DIRECTION('ref_axis',(-0.457970371486214,-0.888967456570137,0.));
#15894=DIRECTION('',(0.,0.,-1.));
#15895=DIRECTION('center_axis',(0.,0.,1.));
#15896=DIRECTION('ref_axis',(-0.457970371486214,-0.888967456570137,0.));
#15897=DIRECTION('',(0.,0.,-1.));
#15898=DIRECTION('center_axis',(0.,0.,1.));
#15899=DIRECTION('ref_axis',(-0.457970371486214,-0.888967456570137,0.));
#15900=DIRECTION('',(0.,0.,-1.));
#15901=DIRECTION('center_axis',(0.,0.,1.));
#15902=DIRECTION('ref_axis',(-0.457970371486214,-0.888967456570137,0.));
#15903=DIRECTION('',(0.,0.,-1.));
#15904=DIRECTION('center_axis',(0.,0.,1.));
#15905=DIRECTION('ref_axis',(-0.457970371486214,-0.888967456570137,0.));
#15906=DIRECTION('',(0.,0.,-1.));
#15907=DIRECTION('center_axis',(0.,0.,1.));
#15908=DIRECTION('ref_axis',(-0.457970371486214,-0.888967456570137,0.));
#15909=DIRECTION('',(0.,0.,-1.));
#15910=DIRECTION('center_axis',(0.,0.,1.));
#15911=DIRECTION('ref_axis',(-0.457970371486214,-0.888967456570137,0.));
#15912=DIRECTION('',(0.,0.,-1.));
#15913=DIRECTION('center_axis',(0.,0.,1.));
#15914=DIRECTION('ref_axis',(-0.457970371486214,-0.888967456570137,0.));
#15915=DIRECTION('',(0.,0.,-1.));
#15916=DIRECTION('center_axis',(0.,0.,1.));
#15917=DIRECTION('ref_axis',(-0.457970371486214,-0.888967456570137,0.));
#15918=DIRECTION('',(0.,0.,-1.));
#15919=DIRECTION('center_axis',(0.,0.,1.));
#15920=DIRECTION('ref_axis',(-0.457970371486214,-0.888967456570137,0.));
#15921=DIRECTION('',(0.,0.,-1.));
#15922=DIRECTION('center_axis',(0.,0.,1.));
#15923=DIRECTION('ref_axis',(-0.457970371486214,-0.888967456570137,0.));
#15924=DIRECTION('',(0.,0.,-1.));
#15925=DIRECTION('center_axis',(0.,0.,1.));
#15926=DIRECTION('ref_axis',(-0.457970371486214,-0.888967456570137,0.));
#15927=DIRECTION('',(0.,0.,-1.));
#15928=DIRECTION('center_axis',(0.,0.,1.));
#15929=DIRECTION('ref_axis',(-0.457970371486214,-0.888967456570137,0.));
#15930=DIRECTION('',(0.,0.,-1.));
#15931=DIRECTION('center_axis',(0.,0.,1.));
#15932=DIRECTION('ref_axis',(-0.457970371486214,-0.888967456570137,0.));
#15933=DIRECTION('',(0.,0.,-1.));
#15934=DIRECTION('center_axis',(0.,0.,1.));
#15935=DIRECTION('ref_axis',(-0.457970371486214,-0.888967456570137,0.));
#15936=DIRECTION('',(0.,0.,-1.));
#15937=DIRECTION('center_axis',(0.,0.,1.));
#15938=DIRECTION('ref_axis',(-0.457970371486214,-0.888967456570137,0.));
#15939=DIRECTION('',(0.,0.,-1.));
#15940=DIRECTION('center_axis',(0.,0.,1.));
#15941=DIRECTION('ref_axis',(-0.457970371486214,-0.888967456570137,0.));
#15942=DIRECTION('',(0.,0.,-1.));
#15943=DIRECTION('center_axis',(0.,0.,1.));
#15944=DIRECTION('ref_axis',(-0.457970371486214,-0.888967456570137,0.));
#15945=DIRECTION('',(0.,0.,-1.));
#15946=DIRECTION('center_axis',(0.,0.,1.));
#15947=DIRECTION('ref_axis',(-0.457970371486214,-0.888967456570137,0.));
#15948=DIRECTION('',(0.,0.,-1.));
#15949=DIRECTION('center_axis',(0.,0.,1.));
#15950=DIRECTION('ref_axis',(-0.457970371486214,-0.888967456570137,0.));
#15951=DIRECTION('',(0.,0.,-1.));
#15952=DIRECTION('center_axis',(0.,0.,1.));
#15953=DIRECTION('ref_axis',(-0.457970371486214,-0.888967456570137,0.));
#15954=DIRECTION('',(0.,0.,-1.));
#15955=DIRECTION('center_axis',(0.,0.,1.));
#15956=DIRECTION('ref_axis',(-0.457970371486214,-0.888967456570137,0.));
#15957=DIRECTION('',(0.,0.,-1.));
#15958=DIRECTION('center_axis',(0.,0.,1.));
#15959=DIRECTION('ref_axis',(-0.457970371486214,-0.888967456570137,0.));
#15960=DIRECTION('',(0.,0.,-1.));
#15961=DIRECTION('center_axis',(0.,0.,1.));
#15962=DIRECTION('ref_axis',(-0.457970371486214,-0.888967456570137,0.));
#15963=DIRECTION('',(0.,0.,-1.));
#15964=DIRECTION('center_axis',(0.,0.,1.));
#15965=DIRECTION('ref_axis',(-0.457970371486214,-0.888967456570137,0.));
#15966=DIRECTION('',(0.,0.,-1.));
#15967=DIRECTION('center_axis',(0.,0.,1.));
#15968=DIRECTION('ref_axis',(-0.457970371486214,-0.888967456570137,0.));
#15969=DIRECTION('',(0.,0.,-1.));
#15970=DIRECTION('center_axis',(0.,0.,1.));
#15971=DIRECTION('ref_axis',(-0.457970371486214,-0.888967456570137,0.));
#15972=DIRECTION('',(0.,0.,-1.));
#15973=DIRECTION('center_axis',(0.,0.,1.));
#15974=DIRECTION('ref_axis',(-0.457970371486214,-0.888967456570137,0.));
#15975=DIRECTION('',(0.,0.,-1.));
#15976=DIRECTION('center_axis',(0.,0.,1.));
#15977=DIRECTION('ref_axis',(-0.457970371486214,-0.888967456570137,0.));
#15978=DIRECTION('',(0.,0.,-1.));
#15979=DIRECTION('center_axis',(0.,0.,1.));
#15980=DIRECTION('ref_axis',(-0.457970371486214,-0.888967456570137,0.));
#15981=DIRECTION('',(0.,0.,-1.));
#15982=DIRECTION('center_axis',(0.,0.,1.));
#15983=DIRECTION('ref_axis',(-0.457970371486214,-0.888967456570137,0.));
#15984=DIRECTION('',(0.,0.,-1.));
#15985=DIRECTION('center_axis',(0.,0.,1.));
#15986=DIRECTION('ref_axis',(-0.457970371486214,-0.888967456570137,0.));
#15987=DIRECTION('',(0.,0.,-1.));
#15988=DIRECTION('center_axis',(0.,0.,1.));
#15989=DIRECTION('ref_axis',(-0.457970371486214,-0.888967456570137,0.));
#15990=DIRECTION('',(0.,0.,-1.));
#15991=DIRECTION('center_axis',(0.,0.,1.));
#15992=DIRECTION('ref_axis',(-0.457970371486214,-0.888967456570137,0.));
#15993=DIRECTION('',(0.,0.,-1.));
#15994=DIRECTION('center_axis',(0.,0.,1.));
#15995=DIRECTION('ref_axis',(-0.457970371486214,-0.888967456570137,0.));
#15996=DIRECTION('',(0.,0.,-1.));
#15997=DIRECTION('center_axis',(0.,0.,1.));
#15998=DIRECTION('ref_axis',(-0.457970371486214,-0.888967456570137,0.));
#15999=DIRECTION('',(0.,0.,-1.));
#16000=DIRECTION('center_axis',(0.,0.,1.));
#16001=DIRECTION('ref_axis',(-0.457970371486214,-0.888967456570137,0.));
#16002=DIRECTION('',(0.,0.,-1.));
#16003=DIRECTION('center_axis',(0.,0.,1.));
#16004=DIRECTION('ref_axis',(-0.457970371486214,-0.888967456570137,0.));
#16005=DIRECTION('',(0.,0.,-1.));
#16006=DIRECTION('center_axis',(0.,0.,1.));
#16007=DIRECTION('ref_axis',(-0.457970371486214,-0.888967456570137,0.));
#16008=DIRECTION('',(0.,0.,-1.));
#16009=DIRECTION('center_axis',(0.,0.,1.));
#16010=DIRECTION('ref_axis',(-0.457970371486214,-0.888967456570137,0.));
#16011=DIRECTION('',(0.,0.,-1.));
#16012=DIRECTION('center_axis',(0.,0.,1.));
#16013=DIRECTION('ref_axis',(-0.457970371486214,-0.888967456570137,0.));
#16014=DIRECTION('',(0.,0.,-1.));
#16015=DIRECTION('center_axis',(0.,0.,1.));
#16016=DIRECTION('ref_axis',(-0.457970371486214,-0.888967456570137,0.));
#16017=DIRECTION('',(0.,0.,-1.));
#16018=DIRECTION('center_axis',(0.,0.,1.));
#16019=DIRECTION('ref_axis',(-0.457970371486214,-0.888967456570137,0.));
#16020=DIRECTION('',(0.,0.,-1.));
#16021=DIRECTION('center_axis',(0.,0.,1.));
#16022=DIRECTION('ref_axis',(-0.457970371486214,-0.888967456570137,0.));
#16023=DIRECTION('',(0.,0.,-1.));
#16024=DIRECTION('center_axis',(0.,0.,1.));
#16025=DIRECTION('ref_axis',(1.,0.,0.));
#16026=DIRECTION('center_axis',(0.,0.,-1.));
#16027=DIRECTION('ref_axis',(1.,0.,0.));
#16028=DIRECTION('center_axis',(0.,0.,-1.));
#16029=DIRECTION('ref_axis',(1.,0.,0.));
#16030=DIRECTION('center_axis',(0.,0.,1.));
#16031=DIRECTION('ref_axis',(-0.457970371486214,-0.888967456570137,0.));
#16032=DIRECTION('center_axis',(0.,0.,1.));
#16033=DIRECTION('ref_axis',(1.,-9.05137471385603E-13,0.));
#16034=DIRECTION('center_axis',(0.,0.,-1.));
#16035=DIRECTION('ref_axis',(-1.,0.,0.));
#16036=DIRECTION('center_axis',(0.,0.,-1.));
#16037=DIRECTION('ref_axis',(-1.,0.,0.));
#16038=DIRECTION('',(0.,0.,-1.));
#16039=DIRECTION('center_axis',(0.,0.,1.));
#16040=DIRECTION('ref_axis',(-1.,0.,0.));
#16041=DIRECTION('center_axis',(0.,0.,-1.));
#16042=DIRECTION('ref_axis',(-1.,0.,0.));
#16043=DIRECTION('center_axis',(0.,0.,-1.));
#16044=DIRECTION('ref_axis',(-1.,0.,0.));
#16045=DIRECTION('',(0.,0.,-1.));
#16046=DIRECTION('center_axis',(0.,0.,1.));
#16047=DIRECTION('ref_axis',(-1.,0.,0.));
#16048=DIRECTION('center_axis',(0.,0.,-1.));
#16049=DIRECTION('ref_axis',(-1.,0.,0.));
#16050=DIRECTION('center_axis',(0.,0.,-1.));
#16051=DIRECTION('ref_axis',(-1.,0.,0.));
#16052=DIRECTION('',(0.,0.,-1.));
#16053=DIRECTION('center_axis',(0.,0.,1.));
#16054=DIRECTION('ref_axis',(-1.,0.,0.));
#16055=DIRECTION('center_axis',(0.,0.,-1.));
#16056=DIRECTION('ref_axis',(-1.,0.,0.));
#16057=DIRECTION('center_axis',(0.,0.,-1.));
#16058=DIRECTION('ref_axis',(-1.,0.,0.));
#16059=DIRECTION('',(0.,0.,-1.));
#16060=DIRECTION('center_axis',(0.,0.,1.));
#16061=DIRECTION('ref_axis',(-1.,0.,0.));
#16062=DIRECTION('center_axis',(0.,0.,1.));
#16063=DIRECTION('ref_axis',(1.,0.,0.));
#16064=DIRECTION('center_axis',(0.,0.,-1.));
#16065=DIRECTION('ref_axis',(-1.,0.,0.));
#16066=DIRECTION('center_axis',(1.22464679914735E-16,-1.,0.));
#16067=DIRECTION('ref_axis',(-1.,-1.22464679914735E-16,0.));
#16068=DIRECTION('center_axis',(0.,0.,1.));
#16069=DIRECTION('ref_axis',(-1.,0.,0.));
#16070=DIRECTION('center_axis',(0.,0.,-1.));
#16071=DIRECTION('ref_axis',(-1.,0.,0.));
#16072=DIRECTION('center_axis',(0.,0.,1.));
#16073=DIRECTION('ref_axis',(-1.,0.,0.));
#16074=DIRECTION('center_axis',(0.,0.,1.));
#16075=DIRECTION('ref_axis',(-1.,0.,0.));
#16076=DIRECTION('center_axis',(0.,0.,1.));
#16077=DIRECTION('ref_axis',(-1.,0.,0.));
#16078=DIRECTION('',(0.,0.,-1.));
#16079=DIRECTION('center_axis',(0.,0.,1.));
#16080=DIRECTION('ref_axis',(-1.,0.,0.));
#16081=DIRECTION('center_axis',(0.,0.,1.));
#16082=DIRECTION('ref_axis',(1.,0.,0.));
#16083=DIRECTION('center_axis',(0.,0.,-1.));
#16084=DIRECTION('ref_axis',(-1.,0.,0.));
#16085=DIRECTION('center_axis',(1.22464679914735E-16,-1.,0.));
#16086=DIRECTION('ref_axis',(-1.,-1.22464679914735E-16,0.));
#16087=DIRECTION('center_axis',(0.,0.,1.));
#16088=DIRECTION('ref_axis',(-1.,0.,0.));
#16089=DIRECTION('center_axis',(0.,0.,1.));
#16090=DIRECTION('ref_axis',(1.,0.,0.));
#33015=CARTESIAN_POINT('',(0.,0.,0.));
#33016=CARTESIAN_POINT('Origin',(0.,0.,-63.6971797838103));
#33017=CARTESIAN_POINT('',(3.09908550384722,6.01564277861011,-58.9542133848184));
#33018=CARTESIAN_POINT('',(3.09908550384721,6.01564277861012,-59.3485564563465));
#33019=CARTESIAN_POINT('',(3.09908550384721,6.01564277861012,-63.6971797838103));
#33020=CARTESIAN_POINT('',(-3.92879594989319,-5.50970519938253,-59.9999154487532));
#33021=CARTESIAN_POINT('Ctrl Pts',(-3.92879594989319,-5.50970519938253,
-59.9999154487532));
#33022=CARTESIAN_POINT('Ctrl Pts',(-3.78616780238278,-5.61140880565578,
-59.9916558525619));
#33023=CARTESIAN_POINT('Ctrl Pts',(-3.63945151853262,-5.70766793724715,
-59.9833962563706));
#33024=CARTESIAN_POINT('Ctrl Pts',(-3.48909951756589,-5.79814397514597,
-59.9751366601792));
#33025=CARTESIAN_POINT('Ctrl Pts',(-3.33886313431323,-5.88855043876168,
-59.9668834154539));
#33026=CARTESIAN_POINT('Ctrl Pts',(-3.18499690519244,-5.97318248597719,
-59.9586301707286));
#33027=CARTESIAN_POINT('Ctrl Pts',(-3.02798303470171,-6.05174419002973,
-59.9503769260034));
#33028=CARTESIAN_POINT('Ctrl Pts',(-2.87105955583084,-6.13026066674238,
-59.9421284326045));
#33029=CARTESIAN_POINT('Ctrl Pts',(-2.71099236144859,-6.20271360500805,
-59.9338799392057));
#33030=CARTESIAN_POINT('Ctrl Pts',(-2.54828924529006,-6.26885244062572,
-59.9256314458069));
#33031=CARTESIAN_POINT('Ctrl Pts',(-2.38564835479305,-6.33496598150475,
-59.917386107037));
#33032=CARTESIAN_POINT('Ctrl Pts',(-2.22037387867933,-6.39477009881011,
-59.9091407682672));
#33033=CARTESIAN_POINT('Ctrl Pts',(-2.0529947640175,-6.44806184050035,-59.9008954294973));
#33034=CARTESIAN_POINT('Ctrl Pts',(-1.88561604710717,-6.50135345555071,
-59.8926501103212));
#33035=CARTESIAN_POINT('Ctrl Pts',(-1.71613303568899,-6.54813260926387,
-59.8844047911452));
#33036=CARTESIAN_POINT('Ctrl Pts',(-1.54509150386976,-6.58824568794072,
-59.8761594719691));
#33037=CARTESIAN_POINT('Ctrl Pts',(-1.37404290093257,-6.62836042495346,
-59.867913811919));
#33038=CARTESIAN_POINT('Ctrl Pts',(-1.20143599365608,-6.66180845615694,
-59.8596681518688));
#33039=CARTESIAN_POINT('Ctrl Pts',(-1.02782835956988,-6.68848696367601,
-59.8514224918187));
#33040=CARTESIAN_POINT('Ctrl Pts',(-0.854183138462646,-6.71517124724075,
-59.8431750465372));
#33041=CARTESIAN_POINT('Ctrl Pts',(-0.679537108659508,-6.73508303288056,
-59.8349276012556));
#33042=CARTESIAN_POINT('Ctrl Pts',(-0.50445472251315,-6.74817119173293,
-59.8266801559741));
#33043=CARTESIAN_POINT('Ctrl Pts',(-0.329303761043839,-6.76126447688464,
-59.8184294803778));
#33044=CARTESIAN_POINT('Ctrl Pts',(-0.153716455416029,-6.76752878371977,
-59.8101788047815));
#33045=CARTESIAN_POINT('Ctrl Pts',(0.0217408595481048,-6.76696507564699,
-59.8019281291851));
#33046=CARTESIAN_POINT('Ctrl Pts',(0.197400711700603,-6.76640071686411,
-59.7936679295137));
#33047=CARTESIAN_POINT('Ctrl Pts',(0.372929919136183,-6.75899259768538,
-59.7854077298423));
#33048=CARTESIAN_POINT('Ctrl Pts',(0.547764280922616,-6.74479379169929,
-59.777147530171));
#33049=CARTESIAN_POINT('Ctrl Pts',(0.722705693314107,-6.73058629182285,
-59.7688822728017));
#33050=CARTESIAN_POINT('Ctrl Pts',(0.896951061004835,-6.70957985753265,
-59.7606170154325));
#33051=CARTESIAN_POINT('Ctrl Pts',(1.06994451776254,-6.68187905674069,-59.7523517580633));
#33052=CARTESIAN_POINT('Ctrl Pts',(1.24319838124092,-6.65413655798612,-59.7440740590179));
#33053=CARTESIAN_POINT('Ctrl Pts',(1.41519622119219,-6.6196796249656,-59.7357963599725));
#33054=CARTESIAN_POINT('Ctrl Pts',(1.58539423346844,-6.57866355154944,-59.7275186609271));
#33055=CARTESIAN_POINT('Ctrl Pts',(1.71981373436326,-6.54626975303482,-59.7209810747394));
#33056=CARTESIAN_POINT('Ctrl Pts',(1.85311081155622,-6.50978565693524,-59.7144434885516));
#33057=CARTESIAN_POINT('Ctrl Pts',(1.98502604839901,-6.46930912750175,-59.7079059023639));
#33058=CARTESIAN_POINT('Ctrl Pts',(2.14752882658301,-6.41944719614633,-59.6998524284548));
#33059=CARTESIAN_POINT('Ctrl Pts',(2.30845684016059,-6.36336465789081,-59.6917989545457));
#33060=CARTESIAN_POINT('Ctrl Pts',(2.46728415220246,-6.30117432803526,-59.6837454806366));
#33061=CARTESIAN_POINT('Ctrl Pts',(2.62591184948028,-6.23906215922054,-59.6757021283639));
#33062=CARTESIAN_POINT('Ctrl Pts',(2.78244375381319,-6.17085760612302,-59.6676587760911));
#33063=CARTESIAN_POINT('Ctrl Pts',(2.93636597617378,-6.09672402639065,-59.6596154238184));
#33064=CARTESIAN_POINT('Ctrl Pts',(3.09012877219892,-6.02266723118471,-59.6515804025206));
#33065=CARTESIAN_POINT('Ctrl Pts',(3.24128693032771,-5.94269379026002,-59.6435453812228));
#33066=CARTESIAN_POINT('Ctrl Pts',(3.38934366436051,-5.85701617932368,-59.635510359925));
#33067=CARTESIAN_POINT('Ctrl Pts',(3.53727971653349,-5.77140840468016,-59.6274818880173));
#33068=CARTESIAN_POINT('Ctrl Pts',(3.68211905324582,-5.68010589995175,-59.6194534161096));
#33069=CARTESIAN_POINT('Ctrl Pts',(3.82338687555638,-5.58336832027256,-59.611424944202));
#33070=CARTESIAN_POINT('Ctrl Pts',(3.96457068211584,-5.48668827301855,-59.6034012470412));
#33071=CARTESIAN_POINT('Ctrl Pts',(4.10218689409652,-5.38457979610277,-59.5953775498804));
#33072=CARTESIAN_POINT('Ctrl Pts',(4.23578736063623,-5.27734729153525,-59.5873538527197));
#33073=CARTESIAN_POINT('Ctrl Pts',(4.37244519402079,-5.16766083517663,-59.5791465380439));
#33074=CARTESIAN_POINT('Ctrl Pts',(4.50490092736726,-5.05261321034467,-59.5709392233681));
#33075=CARTESIAN_POINT('Ctrl Pts',(4.63270806050258,-4.93257590171245,-59.5627319086923));
#33076=CARTESIAN_POINT('Ctrl Pts',(4.75761514036353,-4.81526234238441,-59.5547108250133));
#33077=CARTESIAN_POINT('Ctrl Pts',(4.87808203600149,-4.69318338095779,-59.5466897413343));
#33078=CARTESIAN_POINT('Ctrl Pts',(4.99372736342137,-4.56672486797888,-59.5386686576553));
#33079=CARTESIAN_POINT('Ctrl Pts',(5.10938492623287,-4.44025297556245,-59.5306467253376));
#33080=CARTESIAN_POINT('Ctrl Pts',(5.22021965194513,-4.30940088575895,-59.5226247930199));
#33081=CARTESIAN_POINT('Ctrl Pts',(5.32588903417308,-4.17458920082862,-59.5146028607022));
#33082=CARTESIAN_POINT('Ctrl Pts',(5.4315906722701,-4.03973636426131,-59.5065784796676));
#33083=CARTESIAN_POINT('Ctrl Pts',(5.53212359742655,-3.90092182192332,-59.4985540986331));
#33084=CARTESIAN_POINT('Ctrl Pts',(5.6271874968476,-3.75859679605595,-59.4905297175985));
#33085=CARTESIAN_POINT('Ctrl Pts',(5.72606100290402,-3.61056821325239,-59.4821837661737));
#33086=CARTESIAN_POINT('Ctrl Pts',(5.81901783100488,-3.45874234298609,-59.4738378147489));
#33087=CARTESIAN_POINT('Ctrl Pts',(5.9057722739808,-3.30365598207194,-59.4654918633241));
#33088=CARTESIAN_POINT('Ctrl Pts',(5.98933252273465,-3.15427971439291,-59.4574531997903));
#33089=CARTESIAN_POINT('Ctrl Pts',(6.06713887644236,-3.00187913474258,-59.4494145362565));
#33090=CARTESIAN_POINT('Ctrl Pts',(6.13898512302111,-2.8469546289545,-59.4413758727227));
#33091=CARTESIAN_POINT('Ctrl Pts',(6.21088610655917,-2.69191209199885,-59.4333310848328));
#33092=CARTESIAN_POINT('Ctrl Pts',(6.2768177989628,-2.53434214405691,-59.4252862969429));
#33093=CARTESIAN_POINT('Ctrl Pts',(6.33662354414647,-2.37476126374181,-59.417241509053));
#33094=CARTESIAN_POINT('Ctrl Pts',(6.39651438611868,-2.21495331794356,-59.4091852743429));
#33095=CARTESIAN_POINT('Ctrl Pts',(6.45026177378931,-2.05312908358832,-59.4011290396328));
#33096=CARTESIAN_POINT('Ctrl Pts',(6.49775974844085,-1.88981672432591,-59.3930728049227));
#33097=CARTESIAN_POINT('Ctrl Pts',(6.50305517106833,-1.87160946456526,-59.3921746367821));
#33098=CARTESIAN_POINT('Ctrl Pts',(6.50827297002536,-1.85338371455738,-59.3912764686414));
#33099=CARTESIAN_POINT('Ctrl Pts',(6.51341303837296,-1.83514021032541,-59.3903783005008));
#33100=CARTESIAN_POINT('Ctrl Pts',(6.56098236751811,-1.66630368931335,-59.3820661044326));
#33101=CARTESIAN_POINT('Ctrl Pts',(6.60204676745149,-1.49538953721762,-59.3737539083644));
#33102=CARTESIAN_POINT('Ctrl Pts',(6.6364246288501,-1.32293504964979,-59.3654417122962));
#33103=CARTESIAN_POINT('Ctrl Pts',(6.67076098999591,-1.15068874562037,-59.3571395505415));
#33104=CARTESIAN_POINT('Ctrl Pts',(6.69842682295797,-0.976906150286582,
-59.3488373887868));
#33105=CARTESIAN_POINT('Ctrl Pts',(6.71929018662497,-0.802139880522974,
-59.3405352270321));
#33106=CARTESIAN_POINT('Ctrl Pts',(6.74013227686411,-0.627551812016343,
-59.332241530616));
#33107=CARTESIAN_POINT('Ctrl Pts',(6.75418567433934,-0.451982412657481,
-59.3239478342));
#33108=CARTESIAN_POINT('Ctrl Pts',(6.76136937595525,-0.27599485845678,-59.3156541377839));
#33109=CARTESIAN_POINT('Ctrl Pts',(6.76854709903521,-0.100153767454843,
-59.3073673436816));
#33110=CARTESIAN_POINT('Ctrl Pts',(6.7688665030028,0.0761044366957623,-59.2990805495792));
#33111=CARTESIAN_POINT('Ctrl Pts',(6.76229832759216,0.252210881296477,-59.2907937554769));
#33112=CARTESIAN_POINT('Ctrl Pts',(6.75573438801983,0.428203754261234,-59.2825123055558));
#33113=CARTESIAN_POINT('Ctrl Pts',(6.74229173332196,0.604044713762333,-59.2742308556347));
#33114=CARTESIAN_POINT('Ctrl Pts',(6.72199317861293,0.779164107670035,-59.2659494057136));
#33115=CARTESIAN_POINT('Ctrl Pts',(6.70170311045125,0.954210286560716,-59.2576714181532));
#33116=CARTESIAN_POINT('Ctrl Pts',(6.6745628934783,1.12853515361881,-59.2493934305928));
#33117=CARTESIAN_POINT('Ctrl Pts',(6.64064728551256,1.30157313640636,-59.2411154430323));
#33118=CARTESIAN_POINT('Ctrl Pts',(6.60673902095445,1.47457365300886,-59.2328392478218));
#33119=CARTESIAN_POINT('Ctrl Pts',(6.56605835500911,1.64628749694697,-59.2245630526113));
#33120=CARTESIAN_POINT('Ctrl Pts',(6.51873139201793,1.81615804343124,-59.2162868574008));
#33121=CARTESIAN_POINT('Ctrl Pts',(6.4714066414513,1.98602064886578,-59.208011049083));
#33122=CARTESIAN_POINT('Ctrl Pts',(6.41743630702645,2.15403979126329,-59.1997352407652));
#33123=CARTESIAN_POINT('Ctrl Pts',(6.35699676481274,2.31967263469663,-59.1914594324474));
#33124=CARTESIAN_POINT('Ctrl Pts',(6.29654978744763,2.48532585395053,-59.1831826060562));
#33125=CARTESIAN_POINT('Ctrl Pts',(6.22963213723469,2.6485918605976,-59.174905779665));
#33126=CARTESIAN_POINT('Ctrl Pts',(6.15646892023154,2.80894632099353,-59.1666289532739));
#33127=CARTESIAN_POINT('Ctrl Pts',(6.08325293945296,2.96941642565832,-59.1583461578094));
#33128=CARTESIAN_POINT('Ctrl Pts',(6.00378253740903,3.12697046947339,-59.1500633623449));
#33129=CARTESIAN_POINT('Ctrl Pts',(5.91832991542423,3.28110652253088,-59.1417805668804));
#33130=CARTESIAN_POINT('Ctrl Pts',(5.83284544338531,3.43530002545378,-59.1334946842375));
#33131=CARTESIAN_POINT('Ctrl Pts',(5.74137448411693,3.58607269616141,-59.1252088015947));
#33132=CARTESIAN_POINT('Ctrl Pts',(5.64423353598856,3.73295014582597,-59.1169229189518));
#33133=CARTESIAN_POINT('Ctrl Pts',(5.54698573089441,3.8799891635925,-59.108627921674));
#33134=CARTESIAN_POINT('Ctrl Pts',(5.44405567499194,4.0231241113357,-59.1003329243962));
#33135=CARTESIAN_POINT('Ctrl Pts',(5.33580190541095,4.1619114630435,-59.0920379271185));
#33136=CARTESIAN_POINT('Ctrl Pts',(5.25233433488648,4.26892152940345,-59.0856421842916));
#33137=CARTESIAN_POINT('Ctrl Pts',(5.1657026947281,4.3733475872308,-59.0792464414647));
#33138=CARTESIAN_POINT('Ctrl Pts',(5.07608662186546,4.47500096171146,-59.0728506986378));
#33139=CARTESIAN_POINT('Ctrl Pts',(4.95683725234456,4.61026800063953,-59.0643400791098));
#33140=CARTESIAN_POINT('Ctrl Pts',(4.83208539855738,4.74087032477467,-59.0558294595818));
#33141=CARTESIAN_POINT('Ctrl Pts',(4.70221964422388,4.86635586630027,-59.0473188400538));
#33142=CARTESIAN_POINT('Ctrl Pts',(4.57250400499067,4.99169635592401,-59.0388180581656));
#33143=CARTESIAN_POINT('Ctrl Pts',(4.43768648991991,5.11193163799852,-59.0303172762773));
#33144=CARTESIAN_POINT('Ctrl Pts',(4.29819366261953,5.22664521836113,-59.021816494389));
#33145=CARTESIAN_POINT('Ctrl Pts',(4.1587975426097,5.34127927033681,-59.0133216059048));
#33146=CARTESIAN_POINT('Ctrl Pts',(4.01473282041731,5.45039904588738,-59.0048267174205));
#33147=CARTESIAN_POINT('Ctrl Pts',(3.86646118280567,5.55362646582006,-58.9963318289362));
#33148=CARTESIAN_POINT('Ctrl Pts',(3.71829552336917,5.65678010324271,-58.987843012232));
#33149=CARTESIAN_POINT('Ctrl Pts',(3.56592921152458,5.75404960117541,-58.9793541955279));
#33150=CARTESIAN_POINT('Ctrl Pts',(3.40985530824554,5.84509844030276,-58.9708653788237));
#33151=CARTESIAN_POINT('Ctrl Pts',(3.30780175581451,5.90463342521983,-58.9653147141553));
#33152=CARTESIAN_POINT('Ctrl Pts',(3.20416364447007,5.96150955388916,-58.9597640494868));
#33153=CARTESIAN_POINT('Ctrl Pts',(3.09908550384722,6.01564277861012,-58.9542133848184));
#33154=CARTESIAN_POINT('',(3.92888236737293,-5.50964357679751,-60.));
#33155=CARTESIAN_POINT('Origin',(0.,0.,-60.));
#33156=CARTESIAN_POINT('Ctrl Pts',(3.92888236737219,-5.50964357679804,-60.));
#33157=CARTESIAN_POINT('Ctrl Pts',(4.08454665498865,-5.39864062963439,-59.9910067718568));
#33158=CARTESIAN_POINT('Ctrl Pts',(4.23546571391035,-5.28106458098038,-59.9820135437135));
#33159=CARTESIAN_POINT('Ctrl Pts',(4.38111815764509,-5.15733387408189,-59.9730203155703));
#33160=CARTESIAN_POINT('Ctrl Pts',(4.52681461814809,-5.03356577525429,-59.9640243696365));
#33161=CARTESIAN_POINT('Ctrl Pts',(4.66724109992879,-4.9036394621831,-59.9550284237026));
#33162=CARTESIAN_POINT('Ctrl Pts',(4.8019104597316,-4.76801268210565,-59.9460324777688));
#33163=CARTESIAN_POINT('Ctrl Pts',(4.93660339059607,-4.63236216339008,-59.9370349572824));
#33164=CARTESIAN_POINT('Ctrl Pts',(5.06553701451811,-4.49100935692313,-59.9280374367959));
#33165=CARTESIAN_POINT('Ctrl Pts',(5.18826127518279,-4.34444863480266,-59.9190399163094));
#33166=CARTESIAN_POINT('Ctrl Pts',(5.31096445637577,-4.19791308637299,-59.910043941263));
#33167=CARTESIAN_POINT('Ctrl Pts',(5.42746025016464,-4.04617159716448,-59.9010479662165));
#33168=CARTESIAN_POINT('Ctrl Pts',(5.53733860434853,-3.88975194334954,-59.89205199117));
#33169=CARTESIAN_POINT('Ctrl Pts',(5.64716492430394,-3.73340636396049,-59.8830602762767));
#33170=CARTESIAN_POINT('Ctrl Pts',(5.75037992649799,-3.57238724563523,-59.8740685613834));
#33171=CARTESIAN_POINT('Ctrl Pts',(5.84661613452195,-3.40725237919759,-59.8650768464901));
#33172=CARTESIAN_POINT('Ctrl Pts',(5.93166974709466,-3.26130609514683,-59.8571299640162));
#33173=CARTESIAN_POINT('Ctrl Pts',(6.01127273786878,-3.11214551538678,-59.8491830815423));
#33174=CARTESIAN_POINT('Ctrl Pts',(6.08520006302371,-2.96017384505982,-59.8412361990685));
#33175=CARTESIAN_POINT('Ctrl Pts',(6.16124224316641,-2.8038546882748,-59.833061978408));
#33176=CARTESIAN_POINT('Ctrl Pts',(6.2313015947187,-2.6445121253944,-59.8248877577476));
#33177=CARTESIAN_POINT('Ctrl Pts',(6.29513685779775,-2.48264796972834,-59.8167135370872));
#33178=CARTESIAN_POINT('Ctrl Pts',(6.35895158460461,-2.320835886948,-59.8085419461335));
#33179=CARTESIAN_POINT('Ctrl Pts',(6.41654607795235,-2.15650416350157,-59.8003703551797));
#33180=CARTESIAN_POINT('Ctrl Pts',(6.46772691028241,-1.99017527218303,-59.792198764226));
#33181=CARTESIAN_POINT('Ctrl Pts',(6.51890081155432,-1.82386890560989,-59.7840282798931));
#33182=CARTESIAN_POINT('Ctrl Pts',(6.56366267642554,-1.65556625626644,-59.7758577955601));
#33183=CARTESIAN_POINT('Ctrl Pts',(6.60186871410054,-1.48580566756911,-59.7676873112272));
#33184=CARTESIAN_POINT('Ctrl Pts',(6.64008724617722,-1.31598956259443,-59.7595141549262));
#33185=CARTESIAN_POINT('Ctrl Pts',(6.67174558567356,-1.14471491876742,-59.7513409986251));
#33186=CARTESIAN_POINT('Ctrl Pts',(6.69675082102834,-0.972531460188462,
-59.7431678423241));
#33187=CARTESIAN_POINT('Ctrl Pts',(6.72176059840295,-0.800316725731716,
-59.7349932014285));
#33188=CARTESIAN_POINT('Ctrl Pts',(6.7401148193439,-0.627193207152181,-59.7268185605328));
#33189=CARTESIAN_POINT('Ctrl Pts',(6.75177239074758,-0.453716413124641,
-59.7186439196372));
#33190=CARTESIAN_POINT('Ctrl Pts',(6.76343839782527,-0.280114087489199,
-59.7104633633923));
#33191=CARTESIAN_POINT('Ctrl Pts',(6.76839806132776,-0.106158337728105,
-59.7022828071475));
#33192=CARTESIAN_POINT('Ctrl Pts',(6.76666240052332,0.0675940629346515,
-59.6941022509026));
#33193=CARTESIAN_POINT('Ctrl Pts',(6.76583990227248,0.149932181798813,-59.6902256333141));
#33194=CARTESIAN_POINT('Ctrl Pts',(6.76351463202272,0.232224668894347,-59.6863490157255));
#33195=CARTESIAN_POINT('Ctrl Pts',(6.75969183463654,0.314412628162514,-59.6824723981369));
#33196=CARTESIAN_POINT('Ctrl Pts',(6.75053673949748,0.511241941980218,-59.6731884107173));
#33197=CARTESIAN_POINT('Ctrl Pts',(6.73278303022695,0.707614036394523,-59.6639044232977));
#33198=CARTESIAN_POINT('Ctrl Pts',(6.70650466938329,0.902820092565595,-59.6546204358781));
#33199=CARTESIAN_POINT('Ctrl Pts',(6.68022095811821,1.09806589378281,-59.6453345581866));
#33200=CARTESIAN_POINT('Ctrl Pts',(6.64540915427849,1.29214499852165,-59.6360486804952));
#33201=CARTESIAN_POINT('Ctrl Pts',(6.60219482000945,1.48435594068281,-59.6267628028037));
#33202=CARTESIAN_POINT('Ctrl Pts',(6.55901279252097,1.67642318708115,-59.6174838671795));
#33203=CARTESIAN_POINT('Ctrl Pts',(6.50744083197316,1.86662488169894,-59.6082049315553));
#33204=CARTESIAN_POINT('Ctrl Pts',(6.44765515910135,2.05427163474398,-59.598925995931));
#33205=CARTESIAN_POINT('Ctrl Pts',(6.38792781219889,2.24173532254547,-59.5896561126916));
#33206=CARTESIAN_POINT('Ctrl Pts',(6.32000281232516,2.42664886995839,-59.5803862294521));
#33207=CARTESIAN_POINT('Ctrl Pts',(6.24410612644912,2.60833810723238,-59.5711163462127));
#33208=CARTESIAN_POINT('Ctrl Pts',(6.16838528934056,2.78960637976899,-59.561867940822));
#33209=CARTESIAN_POINT('Ctrl Pts',(6.08472971602274,2.96766508685266,-59.5526195354313));
#33210=CARTESIAN_POINT('Ctrl Pts',(5.99341314440184,3.14186057623683,-59.5433711300406));
#33211=CARTESIAN_POINT('Ctrl Pts',(5.92869874186293,3.26530976864924,-59.5368169524289));
#33212=CARTESIAN_POINT('Ctrl Pts',(5.86013778368322,3.38681906079107,-59.5302627748172));
#33213=CARTESIAN_POINT('Ctrl Pts',(5.78784254158412,3.50616139300933,-59.5237085972055));
#33214=CARTESIAN_POINT('Ctrl Pts',(5.69664729943196,3.65670315163194,-59.5154409740943));
#33215=CARTESIAN_POINT('Ctrl Pts',(5.59955034278513,3.80372530703444,-59.5071733509831));
#33216=CARTESIAN_POINT('Ctrl Pts',(5.49685920736974,3.9467490234818,-59.4989057278719));
#33217=CARTESIAN_POINT('Ctrl Pts',(5.39417722332246,4.0897599943044,-59.4906388415338));
#33218=CARTESIAN_POINT('Ctrl Pts',(5.28590225919402,4.22877295083797,-59.4823719551956));
#33219=CARTESIAN_POINT('Ctrl Pts',(5.17238440972565,4.36333914772013,-59.4741050688575));
#33220=CARTESIAN_POINT('Ctrl Pts',(5.05885715554715,4.49791649312282,-59.4658374976256));
#33221=CARTESIAN_POINT('Ctrl Pts',(4.94008637812876,4.62804607686222,-59.4575699263937));
#33222=CARTESIAN_POINT('Ctrl Pts',(4.81646166447886,4.75331316395265,-59.4493023551617));
#33223=CARTESIAN_POINT('Ctrl Pts',(4.69276225450659,4.87865593971764,-59.4410297885115));
#33224=CARTESIAN_POINT('Ctrl Pts',(4.56420329656194,4.99913009910557,-59.4327572218612));
#33225=CARTESIAN_POINT('Ctrl Pts',(4.43121088660897,5.11435812965793,-59.4244846552109));
#33226=CARTESIAN_POINT('Ctrl Pts',(4.29817261410477,5.22962589669944,-59.4162092357586));
#33227=CARTESIAN_POINT('Ctrl Pts',(4.16069811336844,5.3396437052627,-59.4079338163063));
#33228=CARTESIAN_POINT('Ctrl Pts',(4.01924569645935,5.44407503911298,-59.399658396854));
#33229=CARTESIAN_POINT('Ctrl Pts',(3.87766517540032,5.54860094955335,-59.3913754828987));
#33230=CARTESIAN_POINT('Ctrl Pts',(3.73209983098276,5.64753007916108,-59.3830925689433));
#33231=CARTESIAN_POINT('Ctrl Pts',(3.58303667177545,5.74056941502429,-59.3748096549879));
#33232=CARTESIAN_POINT('Ctrl Pts',(3.52385914830318,5.77750568761618,-59.3715213687499));
#33233=CARTESIAN_POINT('Ctrl Pts',(3.46413062657364,5.81351419890145,-59.368233082512));
#33234=CARTESIAN_POINT('Ctrl Pts',(3.40388261093338,5.84857864536208,-59.364944796274));
#33235=CARTESIAN_POINT('Ctrl Pts',(3.30379349775918,5.90683067761398,-59.3594820162981));
#33236=CARTESIAN_POINT('Ctrl Pts',(3.20214889935663,5.96254749241124,-59.3540192363223));
#33237=CARTESIAN_POINT('Ctrl Pts',(3.09908550384721,6.01564277861012,-59.3485564563465));
#33238=CARTESIAN_POINT('Origin',(0.,0.,-63.6971797838103));
#33239=CARTESIAN_POINT('',(3.0990855038472,6.01564277861012,-56.9542436419538));
#33240=CARTESIAN_POINT('',(3.09908550384721,6.01564277861012,-57.3484848024));
#33241=CARTESIAN_POINT('',(3.09908550384721,6.01564277861012,-63.6971797838103));
#33242=CARTESIAN_POINT('',(-6.767,9.61385986553327E-13,-58.30282021619));
#33243=CARTESIAN_POINT('Ctrl Pts',(-6.767,1.03350959928159E-12,-58.30282021619));
#33244=CARTESIAN_POINT('Ctrl Pts',(-6.76700000000003,-0.186007249558951,
-58.2940707043773));
#33245=CARTESIAN_POINT('Ctrl Pts',(-6.75932637294252,-0.372014355815112,
-58.2853211925645));
#33246=CARTESIAN_POINT('Ctrl Pts',(-6.74400518263371,-0.557389537585464,
-58.2765716807518));
#33247=CARTESIAN_POINT('Ctrl Pts',(-6.72868405703739,-0.742763936381938,
-58.2678222058946));
#33248=CARTESIAN_POINT('Ctrl Pts',(-6.70571545643574,-0.927506130404251,
-58.2590727310374));
#33249=CARTESIAN_POINT('Ctrl Pts',(-6.67517739401586,-1.11098864009477,
-58.2503232561802));
#33250=CARTESIAN_POINT('Ctrl Pts',(-6.64463945804403,-1.29447039004469,
-58.2415738175517));
#33251=CARTESIAN_POINT('Ctrl Pts',(-6.60653217002741,-1.47669218339202,
-58.2328243789232));
#33252=CARTESIAN_POINT('Ctrl Pts',(-6.560984960855,-1.65703510627703,-58.2240749402946));
#33253=CARTESIAN_POINT('Ctrl Pts',(-6.51543793649581,-1.83737729739921,
-58.215325537168));
#33254=CARTESIAN_POINT('Ctrl Pts',(-6.46245112156926,-2.01584035544857,
-58.2065761340414));
#33255=CARTESIAN_POINT('Ctrl Pts',(-6.40220448361752,-2.19181813797306,
-58.1978267309148));
#33256=CARTESIAN_POINT('Ctrl Pts',(-6.34195808512012,-2.36779522106198,
-58.1890773625632));
#33257=CARTESIAN_POINT('Ctrl Pts',(-6.27445201416397,-2.54128677725638,
-58.1803279942117));
#33258=CARTESIAN_POINT('Ctrl Pts',(-6.19991555052772,-2.7117035542855,-58.1715786258602));
#33259=CARTESIAN_POINT('Ctrl Pts',(-6.12537937695159,-2.88211966813434,
-58.162829291557));
#33260=CARTESIAN_POINT('Ctrl Pts',(-6.0438129802838,-3.04946076419812,-58.1540799572538));
#33261=CARTESIAN_POINT('Ctrl Pts',(-5.95549339308897,-3.21315848424469,
-58.1453306229506));
#33262=CARTESIAN_POINT('Ctrl Pts',(-5.86717414225717,-3.37685558085242,
-58.1365813219691));
#33263=CARTESIAN_POINT('Ctrl Pts',(-5.77210188843968,-3.53690907700161,
-58.1278320209875));
#33264=CARTESIAN_POINT('Ctrl Pts',(-5.67059953311265,-3.69277537024154,
-58.1190827200059));
#33265=CARTESIAN_POINT('Ctrl Pts',(-5.56909755592591,-3.84864108281195,
-58.1103334516193));
#33266=CARTESIAN_POINT('Ctrl Pts',(-5.46116568154839,-4.00031938355002,
-58.1015841832327));
#33267=CARTESIAN_POINT('Ctrl Pts',(-5.34717048488239,-4.14729511918343,
-58.0928349148461));
#33268=CARTESIAN_POINT('Ctrl Pts',(-5.23317570343164,-4.29427031947351,
-58.0840856783277));
#33269=CARTESIAN_POINT('Ctrl Pts',(-5.11311781951404,-4.4365427624972,-58.0753364418094));
#33270=CARTESIAN_POINT('Ctrl Pts',(-4.98740458929099,-4.57362924412541,
-58.066587205291));
#33271=CARTESIAN_POINT('Ctrl Pts',(-4.86169180652584,-4.71071523781429,
-58.0578379999143));
#33272=CARTESIAN_POINT('Ctrl Pts',(-4.73032391141404,-4.84261509584654,
-58.0490887945376));
#33273=CARTESIAN_POINT('Ctrl Pts',(-4.59374706947147,-4.96888084599765,
-58.0403395891609));
#33274=CARTESIAN_POINT('Ctrl Pts',(-4.45717070231349,-5.0951461572088,-58.0315904141992));
#33275=CARTESIAN_POINT('Ctrl Pts',(-4.31538563497227,-5.21577720520694,
-58.0228412392375));
#33276=CARTESIAN_POINT('Ctrl Pts',(-4.1688734095193,-5.33036429293561,-58.0140920642758));
#33277=CARTESIAN_POINT('Ctrl Pts',(-4.02236168122419,-5.44495099183754,
-58.0053429190025));
#33278=CARTESIAN_POINT('Ctrl Pts',(-3.87112305263127,-5.55349359497965,
-57.9965937737293));
#33279=CARTESIAN_POINT('Ctrl Pts',(-3.71567116928955,-5.65562346357238,
-57.9878446284561));
#33280=CARTESIAN_POINT('Ctrl Pts',(-3.56021980053291,-5.75775299408939,
-57.9790955121447));
#33281=CARTESIAN_POINT('Ctrl Pts',(-3.40055544442085,-5.85346967519877,
-57.9703463958333));
#33282=CARTESIAN_POINT('Ctrl Pts',(-3.23722035886867,-5.9424484304137,-57.961597279522));
#33283=CARTESIAN_POINT('Ctrl Pts',(-3.07388580043522,-6.03142689847434,
-57.952848191446));
#33284=CARTESIAN_POINT('Ctrl Pts',(-2.90688078789264,-6.11366734707882,
-57.94409910337));
#33285=CARTESIAN_POINT('Ctrl Pts',(-2.73677250610444,-6.18889047001406,
-57.935350015294));
#33286=CARTESIAN_POINT('Ctrl Pts',(-2.56666475916994,-6.26411335643309,
-57.9266009547268));
#33287=CARTESIAN_POINT('Ctrl Pts',(-2.3934540245716,-6.3323188454523,-57.9178518941596));
#33288=CARTESIAN_POINT('Ctrl Pts',(-2.21772855944141,-6.39327529804856,
-57.9091028335925));
#33289=CARTESIAN_POINT('Ctrl Pts',(-2.04200363223706,-6.45423156404665,
-57.9003537998077));
#33290=CARTESIAN_POINT('Ctrl Pts',(-1.86376426061188,-6.50793874412408,
-57.8916047660229));
#33291=CARTESIAN_POINT('Ctrl Pts',(-1.68361577621882,-6.55421443943263,
-57.8828557322381));
#33292=CARTESIAN_POINT('Ctrl Pts',(-1.50346782833416,-6.60048999692542,
-57.8741067245092));
#33293=CARTESIAN_POINT('Ctrl Pts',(-1.32141105657594,-6.63933404265121,
-57.8653577167803));
#33294=CARTESIAN_POINT('Ctrl Pts',(-1.13806375346749,-6.67061465631493,
-57.8566087090514));
#33295=CARTESIAN_POINT('Ctrl Pts',(-0.954716981172254,-6.70189517941739,
-57.847859726652));
#33296=CARTESIAN_POINT('Ctrl Pts',(-0.770079967444639,-6.72561226608977,
-57.8391107442526));
#33297=CARTESIAN_POINT('Ctrl Pts',(-0.584779764075532,-6.74168536995963,
-57.8303617618531));
#33298=CARTESIAN_POINT('Ctrl Pts',(-0.391489587595349,-6.75845153117859,
-57.8212355314375));
#33299=CARTESIAN_POINT('Ctrl Pts',(-0.197478091807549,-6.76689985146387,
-57.8121093010219));
#33300=CARTESIAN_POINT('Ctrl Pts',(-0.00346214753326795,-6.76699911434415,
-57.8029830706063));
#33301=CARTESIAN_POINT('Ctrl Pts',(0.184490798482439,-6.76709527525941,
-57.7941420348912));
#33302=CARTESIAN_POINT('Ctrl Pts',(0.372447602152615,-6.75935633790775,
-57.785300999176));
#33303=CARTESIAN_POINT('Ctrl Pts',(0.559756448192091,-6.74380914014531,
-57.7764599634609));
#33304=CARTESIAN_POINT('Ctrl Pts',(0.745136131041261,-6.72842206873178,
-57.7677099848476));
#33305=CARTESIAN_POINT('Ctrl Pts',(0.929880851942979,-6.70538686355752,
-57.7589600062343));
#33306=CARTESIAN_POINT('Ctrl Pts',(1.1133630505726,-6.67478177303346,-57.750210027621));
#33307=CARTESIAN_POINT('Ctrl Pts',(1.2968433708992,-6.644176995813,-57.741460138581));
#33308=CARTESIAN_POINT('Ctrl Pts',(1.47906091204987,-6.60600253548105,-57.732710249541));
#33309=CARTESIAN_POINT('Ctrl Pts',(1.65939671095019,-6.56038806441263,-57.723960360501));
#33310=CARTESIAN_POINT('Ctrl Pts',(1.83973072368972,-6.51477404513903,-57.7152105581255));
#33311=CARTESIAN_POINT('Ctrl Pts',(2.01818275356862,-6.46172023288715,-57.70646075575));
#33312=CARTESIAN_POINT('Ctrl Pts',(2.19414664033166,-6.40140683918163,-57.6977109533745));
#33313=CARTESIAN_POINT('Ctrl Pts',(2.37010884271092,-6.34109402281559,-57.688961234755));
#33314=CARTESIAN_POINT('Ctrl Pts',(2.54358267847633,-6.27352185699862,-57.6802115161355));
#33315=CARTESIAN_POINT('Ctrl Pts',(2.71397890841562,-6.1989198643534,-57.6714617975159));
#33316=CARTESIAN_POINT('Ctrl Pts',(2.88437356388773,-6.12431856103323,-57.6627121597441));
#33317=CARTESIAN_POINT('Ctrl Pts',(3.05169040787014,-6.04268767582637,-57.6539625219723));
#33318=CARTESIAN_POINT('Ctrl Pts',(3.21536112511906,-5.95430447954025,-57.6452128842005));
#33319=CARTESIAN_POINT('Ctrl Pts',(3.37903038442696,-5.86592207055127,-57.6364633243684));
#33320=CARTESIAN_POINT('Ctrl Pts',(3.53905332979827,-5.77078760703466,-57.6277137645363));
#33321=CARTESIAN_POINT('Ctrl Pts',(3.69488643041747,-5.66922422085393,-57.6189642047043));
#33322=CARTESIAN_POINT('Ctrl Pts',(3.85071819468604,-5.56766170563254,-57.6102147199043));
#33323=CARTESIAN_POINT('Ctrl Pts',(4.00235994599093,-5.45967053456348,-57.6014652351043));
#33324=CARTESIAN_POINT('Ctrl Pts',(4.14929662974176,-5.34561750206781,-57.5927157503043));
#33325=CARTESIAN_POINT('Ctrl Pts',(4.2962321022492,-5.23156540974568,-57.5839663376289));
#33326=CARTESIAN_POINT('Ctrl Pts',(4.43846235841994,-5.11145173172293,-57.5752169249536));
#33327=CARTESIAN_POINT('Ctrl Pts',(4.57550431797306,-4.98568443006674,-57.5664675122782));
#33328=CARTESIAN_POINT('Ctrl Pts',(4.71254519337388,-4.85991812336793,-57.5577181688203));
#33329=CARTESIAN_POINT('Ctrl Pts',(4.84439764314893,-4.72849847631194,-57.5489688253624));
#33330=CARTESIAN_POINT('Ctrl Pts',(4.9706138419661,-4.59187184425426,-57.5402194819045));
#33331=CARTESIAN_POINT('Ctrl Pts',(5.09682908420133,-4.45524624767831,-57.5314702047571));
#33332=CARTESIAN_POINT('Ctrl Pts',(5.217407966501,-4.31341395556978,-57.5227209276098));
#33333=CARTESIAN_POINT('Ctrl Pts',(5.33194095942183,-4.16685668162943,-57.5139716504624));
#33334=CARTESIAN_POINT('Ctrl Pts',(5.44647312235069,-4.02030046975302,-57.5052224367189));
#33335=CARTESIAN_POINT('Ctrl Pts',(5.55495930712227,-3.86901957035635,-57.4964732229753));
#33336=CARTESIAN_POINT('Ctrl Pts',(5.65703106079737,-3.71352778058462,-57.4877240092318));
#33337=CARTESIAN_POINT('Ctrl Pts',(5.75910210868671,-3.55803706597707,-57.4789748559856));
#33338=CARTESIAN_POINT('Ctrl Pts',(5.85475865698478,-3.39833575881021,-57.4702257027394));
#33339=CARTESIAN_POINT('Ctrl Pts',(5.94367583068987,-3.23496624706859,-57.4614765494932));
#33340=CARTESIAN_POINT('Ctrl Pts',(6.03259241910004,-3.07159781070243,-57.4527274538381));
#33341=CARTESIAN_POINT('Ctrl Pts',(6.11476958470897,-2.90456146975982,-57.443978358183));
#33342=CARTESIAN_POINT('Ctrl Pts',(6.18992823574318,-2.7344245164841,-57.4352292625279));
#33343=CARTESIAN_POINT('Ctrl Pts',(6.26508641700876,-2.56428862662561,-57.4264802215577));
#33344=CARTESIAN_POINT('Ctrl Pts',(6.33322605570246,-2.39105242531414,-57.4177311805876));
#33345=CARTESIAN_POINT('Ctrl Pts',(6.39411573747723,-2.21530425353857,-57.4089821396175));
#33346=CARTESIAN_POINT('Ctrl Pts',(6.45500505889087,-2.03955712188685,-57.4002331504265));
#33347=CARTESIAN_POINT('Ctrl Pts',(6.50864441544895,-1.86129832025691,-57.3914841612355));
#33348=CARTESIAN_POINT('Ctrl Pts',(6.55485164049877,-1.68113324012423,-57.3827351720445));
#33349=CARTESIAN_POINT('Ctrl Pts',(6.60199852639086,-1.49730435913003,-57.3738082651676));
#33350=CARTESIAN_POINT('Ctrl Pts',(6.64140767440991,-1.31149113173747,-57.3648813582907));
#33351=CARTESIAN_POINT('Ctrl Pts',(6.67293975269588,-1.12435050446518,-57.3559544514138));
#33352=CARTESIAN_POINT('Ctrl Pts',(6.70384664831495,-0.940920291564619,
-57.3472045372298));
#33353=CARTESIAN_POINT('Ctrl Pts',(6.72718585889656,-0.756215114278821,
-57.3384546230458));
#33354=CARTESIAN_POINT('Ctrl Pts',(6.74287810451857,-0.570862389376028,
-57.3297047088619));
#33355=CARTESIAN_POINT('Ctrl Pts',(6.75857004154118,-0.385513309569033,
-57.3209549667513));
#33356=CARTESIAN_POINT('Ctrl Pts',(6.76661529035553,-0.199516993260188,
-57.3122052246407));
#33357=CARTESIAN_POINT('Ctrl Pts',(6.76698652348896,-0.013505218206075,
-57.3034554825301));
#33358=CARTESIAN_POINT('Ctrl Pts',(6.76735774981526,0.172503146036848,-57.2947059008595));
#33359=CARTESIAN_POINT('Ctrl Pts',(6.7600552414749,0.358526681831404,-57.2859563191888));
#33360=CARTESIAN_POINT('Ctrl Pts',(6.74510380214898,0.543933542112777,-57.2772067375182));
#33361=CARTESIAN_POINT('Ctrl Pts',(6.73015261711002,0.729337249082645,-57.2684573046563));
#33362=CARTESIAN_POINT('Ctrl Pts',(6.70755278444634,0.914124015852599,-57.2597078717943));
#33363=CARTESIAN_POINT('Ctrl Pts',(6.67738106408323,1.09766621749181,-57.2509584389324));
#33364=CARTESIAN_POINT('Ctrl Pts',(6.64720981677293,1.28120554143119,-57.24220914325));
#33365=CARTESIAN_POINT('Ctrl Pts',(6.60946696581567,1.46350005650419,-57.2334598475677));
#33366=CARTESIAN_POINT('Ctrl Pts',(6.56428070011044,1.64393062206335,-57.2247105518853));
#33367=CARTESIAN_POINT('Ctrl Pts',(6.51909508282795,1.82435859844456,-57.2159613817554));
#33368=CARTESIAN_POINT('Ctrl Pts',(6.46646633415721,2.00292240086371,-57.2072122116254));
#33369=CARTESIAN_POINT('Ctrl Pts',(6.40657319597256,2.17901557696266,-57.1984630414954));
#33370=CARTESIAN_POINT('Ctrl Pts',(6.34668083768363,2.35510646007252,-57.1897139852923));
#33371=CARTESIAN_POINT('Ctrl Pts',(6.27952437143956,2.52872650996354,-57.1809649290892));
#33372=CARTESIAN_POINT('Ctrl Pts',(6.2053318733521,2.69928607997755,-57.1722158728861));
#33373=CARTESIAN_POINT('Ctrl Pts',(6.12831449784328,2.87633970115236,-57.1631336965973));
#33374=CARTESIAN_POINT('Ctrl Pts',(6.0437148946323,3.05009490562197,-57.1540515203084));
#33375=CARTESIAN_POINT('Ctrl Pts',(5.95184265120568,3.21991584599488,-57.1449693440196));
#33376=CARTESIAN_POINT('Ctrl Pts',(5.86333281335572,3.38352155905163,-57.1362195636652));
#33377=CARTESIAN_POINT('Ctrl Pts',(5.76807337235766,3.54347560903692,-57.1274697833108));
#33378=CARTESIAN_POINT('Ctrl Pts',(5.66638790086438,3.6992346717852,-57.1187200029563));
#33379=CARTESIAN_POINT('Ctrl Pts',(5.56470608502828,3.85498813489641,-57.1099705371621));
#33380=CARTESIAN_POINT('Ctrl Pts',(5.4565988576704,4.00654667256142,-57.1012210713678));
#33381=CARTESIAN_POINT('Ctrl Pts',(5.34243340580597,4.15339551506095,-57.0924716055735));
#33382=CARTESIAN_POINT('Ctrl Pts',(5.22827145140687,4.30023985883757,-57.0837224078197));
#33383=CARTESIAN_POINT('Ctrl Pts',(5.10805181978186,4.44237456992932,-57.0749732100658));
#33384=CARTESIAN_POINT('Ctrl Pts',(4.98218281282651,4.5793169162634,-57.0662240123119));
#33385=CARTESIAN_POINT('Ctrl Pts',(4.85631699296328,4.71625579512059,-57.0574750360939));
#33386=CARTESIAN_POINT('Ctrl Pts',(4.72480227791936,4.84800236135674,-57.0487260598759));
#33387=CARTESIAN_POINT('Ctrl Pts',(4.5880853084821,4.97410918678819,-57.0399770836579));
#33388=CARTESIAN_POINT('Ctrl Pts',(4.45135945057063,5.10022421088928,-57.0312275386367));
#33389=CARTESIAN_POINT('Ctrl Pts',(4.30943087208128,5.22069856611914,-57.0224779936155));
#33390=CARTESIAN_POINT('Ctrl Pts',(4.1627816432255,5.33512305301619,-57.0137284485943));
#33391=CARTESIAN_POINT('Ctrl Pts',(4.01614103534475,5.44954081331364,-57.0049794179271));
#33392=CARTESIAN_POINT('Ctrl Pts',(3.864780558335,5.55790924068277,-56.9962303872598));
#33393=CARTESIAN_POINT('Ctrl Pts',(3.7092142581204,5.65986029751233,-56.9874813565925));
#33394=CARTESIAN_POINT('Ctrl Pts',(3.55364584530212,5.76181273884597,-56.9787322071127));
#33395=CARTESIAN_POINT('Ctrl Pts',(3.39387173464441,5.85734747818007,-56.9699830576328));
#33396=CARTESIAN_POINT('Ctrl Pts',(3.23043456092505,5.94614005448753,-56.961233908153));
#33397=CARTESIAN_POINT('Ctrl Pts',(3.18690768806459,5.96978744811246,-56.9589038194199));
#33398=CARTESIAN_POINT('Ctrl Pts',(3.14312114982915,5.99295688499283,-56.9565737306869));
#33399=CARTESIAN_POINT('Ctrl Pts',(3.0990855038472,6.01564277861012,-56.9542436419538));
#33400=CARTESIAN_POINT('Ctrl Pts',(3.09908550384722,6.01564277861012,-58.9542133848184));
#33401=CARTESIAN_POINT('Ctrl Pts',(2.9385078993557,6.09836772499351,-58.9457310075084));
#33402=CARTESIAN_POINT('Ctrl Pts',(2.77456632796542,6.1746848698411,-58.9372486301984));
#33403=CARTESIAN_POINT('Ctrl Pts',(2.60779751086059,6.24433192121858,-58.9287662528885));
#33404=CARTESIAN_POINT('Ctrl Pts',(2.51159575789531,6.28450830759401,-58.9238731344944));
#33405=CARTESIAN_POINT('Ctrl Pts',(2.41445365413025,6.32246597896167,-58.9189800161003));
#33406=CARTESIAN_POINT('Ctrl Pts',(2.31647755692632,6.35816174127842,-58.9140868977063));
#33407=CARTESIAN_POINT('Ctrl Pts',(2.14471510779725,6.42074018371518,-58.9055087442257));
#33408=CARTESIAN_POINT('Ctrl Pts',(1.97046722237144,6.47633555656743,-58.8969305907451));
#33409=CARTESIAN_POINT('Ctrl Pts',(1.79432006926173,6.52477620221909,-58.8883524372645));
#33410=CARTESIAN_POINT('Ctrl Pts',(1.61808399810324,6.57324130042429,-58.8797699535824));
#33411=CARTESIAN_POINT('Ctrl Pts',(1.43994704554636,6.61454438269761,-58.8711874699003));
#33412=CARTESIAN_POINT('Ctrl Pts',(1.26050759114,6.64856447759052,-58.8626049862182));
#33413=CARTESIAN_POINT('Ctrl Pts',(1.07359002331164,6.68400235503898,-58.8536648287646));
#33414=CARTESIAN_POINT('Ctrl Pts',(0.885259433514967,6.71153712926666,-58.844724671311));
#33415=CARTESIAN_POINT('Ctrl Pts',(0.696199858256236,6.73109164678093,-58.8357845138573));
#33416=CARTESIAN_POINT('Ctrl Pts',(0.514391573134188,6.74989616007148,-58.827187251893));
#33417=CARTESIAN_POINT('Ctrl Pts',(0.331909494109158,6.76132118859279,-58.8185899899287));
#33418=CARTESIAN_POINT('Ctrl Pts',(0.149363924244205,6.76535138911013,-58.8099927279644));
#33419=CARTESIAN_POINT('Ctrl Pts',(-0.0332950379045321,6.76938409307712,
-58.8013901256175));
#33420=CARTESIAN_POINT('Ctrl Pts',(-0.216017259489319,6.76601280294623,
-58.7927875232707));
#33421=CARTESIAN_POINT('Ctrl Pts',(-0.398194069133422,6.75527427150867,
-58.7841849209238));
#33422=CARTESIAN_POINT('Ctrl Pts',(-0.58056151314086,6.74452450300363,-58.7755733165991));
#33423=CARTESIAN_POINT('Ctrl Pts',(-0.762382095803028,6.72639211564653,
-58.7669617122743));
#33424=CARTESIAN_POINT('Ctrl Pts',(-0.943052648207334,6.70096565449407,
-58.7583501079495));
#33425=CARTESIAN_POINT('Ctrl Pts',(-0.964221440163454,6.69798648905093,
-58.7573411042246));
#33426=CARTESIAN_POINT('Ctrl Pts',(-0.985374455570215,6.69490724591875,
-58.7563321004997));
#33427=CARTESIAN_POINT('Ctrl Pts',(-1.00651073389821,6.6917281133163,-58.7553230967747));
#33428=CARTESIAN_POINT('Ctrl Pts',(-1.19639319196643,6.66316766839261,-58.7462584873617));
#33429=CARTESIAN_POINT('Ctrl Pts',(-1.38510326363246,6.62651425917618,-58.7371938779487));
#33430=CARTESIAN_POINT('Ctrl Pts',(-1.5719757120565,6.58188281274473,-58.7281292685357));
#33431=CARTESIAN_POINT('Ctrl Pts',(-1.75868033247639,6.53729144930379,-58.7190727999445));
#33432=CARTESIAN_POINT('Ctrl Pts',(-1.94355039732936,6.48473640864038,-58.7100163313533));
#33433=CARTESIAN_POINT('Ctrl Pts',(-2.12593175892476,6.42438348453726,-58.7009598627621));
#33434=CARTESIAN_POINT('Ctrl Pts',(-2.3079879218244,6.36413817390973,-58.6919195424865));
#33435=CARTESIAN_POINT('Ctrl Pts',(-2.48756402096188,6.29612281874464,-58.6828792222108));
#33436=CARTESIAN_POINT('Ctrl Pts',(-2.66402210667442,6.22055264547693,-58.6738389019351));
#33437=CARTESIAN_POINT('Ctrl Pts',(-2.8402535542687,6.14507953254961,-58.6648101928088));
#33438=CARTESIAN_POINT('Ctrl Pts',(-3.01337476617588,6.06207105819907,-58.6557814836824));
#33439=CARTESIAN_POINT('Ctrl Pts',(-3.18276633312787,5.97179097664242,-58.646752774556));
#33440=CARTESIAN_POINT('Ctrl Pts',(-3.35176147924415,5.88172217423043,-58.6377451949846));
#33441=CARTESIAN_POINT('Ctrl Pts',(-3.51704419658996,5.78441584249337,-58.6287376154131));
#33442=CARTESIAN_POINT('Ctrl Pts',(-3.67801877212276,5.68018194355714,-58.6197300358416));
#33443=CARTESIAN_POINT('Ctrl Pts',(-3.81604697405473,5.59080622939292,-58.6120064558422));
#33444=CARTESIAN_POINT('Ctrl Pts',(-3.95090794947756,5.4963379921662,-58.6042828758427));
#33445=CARTESIAN_POINT('Ctrl Pts',(-4.08223937590867,5.39700015543643,-58.5965592958432));
#33446=CARTESIAN_POINT('Ctrl Pts',(-4.22032311992663,5.29255493016897,-58.5884386131359));
#33447=CARTESIAN_POINT('Ctrl Pts',(-4.35444043945768,5.18277314809975,-58.5803179304286));
#33448=CARTESIAN_POINT('Ctrl Pts',(-4.4841587435886,5.06799855586975,-58.5721972477212));
#33449=CARTESIAN_POINT('Ctrl Pts',(-4.61386773174815,4.95323220639951,-58.5640771482165));
#33450=CARTESIAN_POINT('Ctrl Pts',(-4.73917805946965,4.83347400370038,-58.5559570487117));
#33451=CARTESIAN_POINT('Ctrl Pts',(-4.85969140119417,4.70910697321259,-58.5478369492069));
#33452=CARTESIAN_POINT('Ctrl Pts',(-4.98021909909504,4.58472512747699,-58.5397158823937));
#33453=CARTESIAN_POINT('Ctrl Pts',(-5.09594841911797,4.45573362459593,-58.5315948155804));
#33454=CARTESIAN_POINT('Ctrl Pts',(-5.20651902378243,4.32255117436354,-58.5234737487671));
#33455=CARTESIAN_POINT('Ctrl Pts',(-5.31717012042056,4.18927177143464,-58.5153467700689));
#33456=CARTESIAN_POINT('Ctrl Pts',(-5.42265476702151,4.05179560985903,-58.5072197913706));
#33457=CARTESIAN_POINT('Ctrl Pts',(-5.52265355950414,3.91057369981647,-58.4990928126724));
#33458=CARTESIAN_POINT('Ctrl Pts',(-5.62269307460422,3.76929427982127,-58.4909625244157));
#33459=CARTESIAN_POINT('Ctrl Pts',(-5.71724208271152,3.62426637746686,-58.4828322361591));
#33460=CARTESIAN_POINT('Ctrl Pts',(-5.80602556896683,3.47596836759247,-58.4747019479024));
#33461=CARTESIAN_POINT('Ctrl Pts',(-5.8949056740352,3.32750897210123,-58.4665628118427));
#33462=CARTESIAN_POINT('Ctrl Pts',(-5.97800754972974,3.17577268211546,-58.458423675783));
#33463=CARTESIAN_POINT('Ctrl Pts',(-6.0551026827931,3.02126140888732,-58.4502845397233));
#33464=CARTESIAN_POINT('Ctrl Pts',(-6.09453539262529,2.94223180013108,-58.4461215247861));
#33465=CARTESIAN_POINT('Ctrl Pts',(-6.1323974378594,2.86247654218005,-58.4419585098489));
#33466=CARTESIAN_POINT('Ctrl Pts',(-6.16866320271028,2.78206457357269,-58.4377954949117));
#33467=CARTESIAN_POINT('Ctrl Pts',(-6.24890574610109,2.60414302947599,-58.4285843033621));
#33468=CARTESIAN_POINT('Ctrl Pts',(-6.32146502909445,2.42270742807501,-58.4193731118125));
#33469=CARTESIAN_POINT('Ctrl Pts',(-6.38606698025806,2.23840066200352,-58.4101619202629));
#33470=CARTESIAN_POINT('Ctrl Pts',(-6.45054079326273,2.05445946894117,-58.4009689991387));
#33471=CARTESIAN_POINT('Ctrl Pts',(-6.50708872917064,1.86765867644806,-58.3917760780145));
#33472=CARTESIAN_POINT('Ctrl Pts',(-6.55548604261071,1.67865772125712,-58.3825831568902));
#33473=CARTESIAN_POINT('Ctrl Pts',(-6.60380870361076,1.48994829841517,-58.3734044157678));
#33474=CARTESIAN_POINT('Ctrl Pts',(-6.64400578671844,1.29904568319861,-58.3642256746454));
#33475=CARTESIAN_POINT('Ctrl Pts',(-6.67590239598728,1.10662378397148,-58.355046933523));
#33476=CARTESIAN_POINT('Ctrl Pts',(-6.70769975114459,0.91480065260973,-58.3458967543016));
#33477=CARTESIAN_POINT('Ctrl Pts',(-6.73124814657676,0.721467872861489,
-58.3367465750801));
#33478=CARTESIAN_POINT('Ctrl Pts',(-6.74642391635618,0.527307633945599,
-58.3275963958587));
#33479=CARTESIAN_POINT('Ctrl Pts',(-6.76012119264503,0.352063381074478,
-58.3193376693025));
#33480=CARTESIAN_POINT('Ctrl Pts',(-6.76699835261893,0.176145328877515,
-58.3110789427462));
#33481=CARTESIAN_POINT('Ctrl Pts',(-6.76699999970395,6.32990448600232E-5,
-58.30282021619));
#33482=CARTESIAN_POINT('',(-6.76699969186032,0.00204214650334386,-58.697179783784));
#33483=CARTESIAN_POINT('Ctrl Pts',(3.09908550384721,6.01564277861012,-59.3485564563465));
#33484=CARTESIAN_POINT('Ctrl Pts',(2.94204903435842,6.09654343446331,-59.3402328834935));
#33485=CARTESIAN_POINT('Ctrl Pts',(2.78171749018946,6.17135568762416,-59.3319093106405));
#33486=CARTESIAN_POINT('Ctrl Pts',(2.61859746282639,6.23981060030504,-59.3235857377875));
#33487=CARTESIAN_POINT('Ctrl Pts',(2.45558899639079,6.30821869535309,-59.3152678575863));
#33488=CARTESIAN_POINT('Ctrl Pts',(2.28979616522525,6.3702779803494,-59.306949977385));
#33489=CARTESIAN_POINT('Ctrl Pts',(2.12174835011713,6.42576633085699,-59.2986320971838));
#33490=CARTESIAN_POINT('Ctrl Pts',(1.95378515990411,6.48122673874694,-59.2903184056698));
#33491=CARTESIAN_POINT('Ctrl Pts',(1.78356957698955,6.5301226983669,-59.2820047141558));
#33492=CARTESIAN_POINT('Ctrl Pts',(1.61164929851767,6.5722808475131,-59.2736910226418));
#33493=CARTESIAN_POINT('Ctrl Pts',(1.43978460285766,6.61442536668793,-59.2653800189919));
#33494=CARTESIAN_POINT('Ctrl Pts',(1.26621664615083,6.64983633512498,-59.257069015342));
#33495=CARTESIAN_POINT('Ctrl Pts',(1.09150680360186,6.67839066674681,-59.2487580116922));
#33496=CARTESIAN_POINT('Ctrl Pts',(0.91515314059552,6.7072136620786,-59.2403688109721));
#33497=CARTESIAN_POINT('Ctrl Pts',(0.737636340209878,6.72905024018178,-59.2319796102521));
#33498=CARTESIAN_POINT('Ctrl Pts',(0.559543225414115,6.74382683488338,-59.223590409532));
#33499=CARTESIAN_POINT('Ctrl Pts',(0.38308548831206,6.75846774037885,-59.2152782444219));
#33500=CARTESIAN_POINT('Ctrl Pts',(0.206062329101349,6.76617778150654,-59.2069660793118));
#33501=CARTESIAN_POINT('Ctrl Pts',(0.0290485527314963,6.76693765166964,
-59.1986539142017));
#33502=CARTESIAN_POINT('Ctrl Pts',(-0.148006811632621,6.76769770035826,
-59.1903397962138));
#33503=CARTESIAN_POINT('Ctrl Pts',(-0.325052442269068,6.76150432174146,
-59.1820256782259));
#33504=CARTESIAN_POINT('Ctrl Pts',(-0.50151435591173,6.74839035258146,-59.1737115602379));
#33505=CARTESIAN_POINT('Ctrl Pts',(-0.678046593149869,6.73527115724293,
-59.165394128908));
#33506=CARTESIAN_POINT('Ctrl Pts',(-0.85399430440421,6.71522589991034,-59.1570766975781));
#33507=CARTESIAN_POINT('Ctrl Pts',(-1.0287892300239,6.68833923483153,-59.1487592662482));
#33508=CARTESIAN_POINT('Ctrl Pts',(-1.20626870261506,6.66103963719731,-59.1403140935951));
#33509=CARTESIAN_POINT('Ctrl Pts',(-1.38255932370079,6.62668682920984,-59.131868920942));
#33510=CARTESIAN_POINT('Ctrl Pts',(-1.55707840793328,6.58542298045828,-59.1234237482889));
#33511=CARTESIAN_POINT('Ctrl Pts',(-1.72926629274015,6.54471032793222,-59.1150913849696));
#33512=CARTESIAN_POINT('Ctrl Pts',(-1.89972935757813,6.49727027205983,-59.1067590216504));
#33513=CARTESIAN_POINT('Ctrl Pts',(-2.06792469169362,6.44328925856071,-59.0984266583311));
#33514=CARTESIAN_POINT('Ctrl Pts',(-2.23953574405249,6.38821199626507,-59.0899250810111));
#33515=CARTESIAN_POINT('Ctrl Pts',(-2.40878561572041,6.32632540951042,-59.081423503691));
#33516=CARTESIAN_POINT('Ctrl Pts',(-2.57512064742921,6.25787844650116,-59.072921926371));
#33517=CARTESIAN_POINT('Ctrl Pts',(-2.74145567913801,6.1894314834919,-59.0644203490509));
#33518=CARTESIAN_POINT('Ctrl Pts',(-2.90487555119516,6.11442435236039,-59.0559187717309));
#33519=CARTESIAN_POINT('Ctrl Pts',(-3.06485477752562,6.03315458053897,-59.0474171944109));
#33520=CARTESIAN_POINT('Ctrl Pts',(-3.21640177601162,5.95616839758458,-59.0393637205018));
#33521=CARTESIAN_POINT('Ctrl Pts',(-3.36533074803328,5.87332373605608,-59.0313102465927));
#33522=CARTESIAN_POINT('Ctrl Pts',(-3.51114288843178,5.78482191748501,-59.0232567726836));
#33523=CARTESIAN_POINT('Ctrl Pts',(-3.65677177158295,5.69643132833291,-59.0152134204109));
#33524=CARTESIAN_POINT('Ctrl Pts',(-3.79929130074251,5.60239791966642,-59.0071700681381));
#33525=CARTESIAN_POINT('Ctrl Pts',(-3.93822320620494,5.50297074116417,-58.9991267158654));
#33526=CARTESIAN_POINT('Ctrl Pts',(-4.07701121168828,5.40364654526234,-58.9910916945676));
#33527=CARTESIAN_POINT('Ctrl Pts',(-4.21221868567955,5.29893991223907,-58.9830566732698));
#33528=CARTESIAN_POINT('Ctrl Pts',(-4.34339262978699,5.18914535000824,-58.975021651972));
#33529=CARTESIAN_POINT('Ctrl Pts',(-4.47445965328987,5.07944028192999,-58.9669931800643));
#33530=CARTESIAN_POINT('Ctrl Pts',(-4.6014994043802,4.96465577743627,-58.9589647081566));
#33531=CARTESIAN_POINT('Ctrl Pts',(-4.72408863568108,4.84512905527076,-58.950936236249));
#33532=CARTESIAN_POINT('Ctrl Pts',(-4.8466049598885,4.72567341884265,-58.9429125390882));
#33533=CARTESIAN_POINT('Ctrl Pts',(-4.96467576547952,4.60148143953182,-58.9348888419275));
#33534=CARTESIAN_POINT('Ctrl Pts',(-5.07791173080715,4.47292985124193,-58.9268651447667));
#33535=CARTESIAN_POINT('Ctrl Pts',(-5.19373903353787,4.3414364366692,-58.9186578300909));
#33536=CARTESIAN_POINT('Ctrl Pts',(-5.30450724105058,4.20538173634522,-58.9104505154151));
#33537=CARTESIAN_POINT('Ctrl Pts',(-5.40984015990395,4.06520829039428,-58.9022432007393));
#33538=CARTESIAN_POINT('Ctrl Pts',(-5.51278298464656,3.92821549994307,-58.8942221170603));
#33539=CARTESIAN_POINT('Ctrl Pts',(-5.61053430555352,3.78728918931021,-58.8862010333813));
#33540=CARTESIAN_POINT('Ctrl Pts',(-5.70278454423253,3.64287488696258,-58.8781799497023));
#33541=CARTESIAN_POINT('Ctrl Pts',(-5.79504454307941,3.49844530543676,-58.8701580173846));
#33542=CARTESIAN_POINT('Ctrl Pts',(-5.8818020988733,3.35052731348723,-58.8621360850669));
#33543=CARTESIAN_POINT('Ctrl Pts',(-5.96279189361212,3.19959401072598,-58.8541141527492));
#33544=CARTESIAN_POINT('Ctrl Pts',(-6.04380641070806,3.04861463515984,-58.8460897717146));
#33545=CARTESIAN_POINT('Ctrl Pts',(-6.11904948530044,2.89461844711971,-58.8380653906801));
#33546=CARTESIAN_POINT('Ctrl Pts',(-6.1883026182268,2.7381014782596,-58.8300410096455));
#33547=CARTESIAN_POINT('Ctrl Pts',(-6.26033101280687,2.57531222216166,-58.8216950582207));
#33548=CARTESIAN_POINT('Ctrl Pts',(-6.32587926744313,2.40979638277819,-58.8133491067959));
#33549=CARTESIAN_POINT('Ctrl Pts',(-6.38475794488179,2.24213179480353,-58.8050031553711));
#33550=CARTESIAN_POINT('Ctrl Pts',(-6.44146878025008,2.08064041525226,-58.7969644918373));
#33551=CARTESIAN_POINT('Ctrl Pts',(-6.49199238196718,1.91715607036079,-58.7889258283035));
#33552=CARTESIAN_POINT('Ctrl Pts',(-6.53621138762681,1.75220709285677,-58.7808871647698));
#33553=CARTESIAN_POINT('Ctrl Pts',(-6.58046408208749,1.58713244691668,-58.7728423768799));
#33554=CARTESIAN_POINT('Ctrl Pts',(-6.61840253497921,1.42059130980724,-58.76479758899));
#33555=CARTESIAN_POINT('Ctrl Pts',(-6.64996096528673,1.25311937187275,-58.7567528011001));
#33556=CARTESIAN_POINT('Ctrl Pts',(-6.68156429965934,1.08540914037527,-58.74869656639));
#33557=CARTESIAN_POINT('Ctrl Pts',(-6.70676944525687,0.916765832943588,
-58.7406403316799));
#33558=CARTESIAN_POINT('Ctrl Pts',(-6.72556257117393,0.747727959370447,
-58.7325840969698));
#33559=CARTESIAN_POINT('Ctrl Pts',(-6.72765776670496,0.728882377275807,
-58.7316859288292));
#33560=CARTESIAN_POINT('Ctrl Pts',(-6.72967331775269,0.710031888070401,
-58.7307877606885));
#33561=CARTESIAN_POINT('Ctrl Pts',(-6.73160924515994,0.691177235213417,
-58.7298895925479));
#33562=CARTESIAN_POINT('Ctrl Pts',(-6.75511034417722,0.462292070372445,
-58.7189863229686));
#33563=CARTESIAN_POINT('Ctrl Pts',(-6.76693020279762,0.232305909665429,
-58.7080830533894));
#33564=CARTESIAN_POINT('Ctrl Pts',(-6.76699969186015,0.0020421470552204,
-58.6971797838101));
#33565=CARTESIAN_POINT('Ctrl Pts',(-6.76699969186032,0.00204214650334836,
-58.697179783784));
#33566=CARTESIAN_POINT('Ctrl Pts',(-6.76705174932313,-0.170459108531269,
-58.6890116392827));
#33567=CARTESIAN_POINT('Ctrl Pts',(-6.760503606502,-0.343228945885599,-58.6808434947815));
#33568=CARTESIAN_POINT('Ctrl Pts',(-6.74731979635412,-0.51571752513159,
-58.6726753502803));
#33569=CARTESIAN_POINT('Ctrl Pts',(-6.73415147684863,-0.688003434673666,
-58.6645168031416));
#33570=CARTESIAN_POINT('Ctrl Pts',(-6.71436303929249,-0.860008384080678,
-58.6563582560029));
#33571=CARTESIAN_POINT('Ctrl Pts',(-6.68797097171816,-1.03118052806252,
-58.6481997088642));
#33572=CARTESIAN_POINT('Ctrl Pts',(-6.66160439981937,-1.20218731366787,
-58.6400490431721));
#33573=CARTESIAN_POINT('Ctrl Pts',(-6.62864695501451,-1.37236253781669,
-58.63189837748));
#33574=CARTESIAN_POINT('Ctrl Pts',(-6.58916706896801,-1.54115746672023,
-58.6237477117878));
#33575=CARTESIAN_POINT('Ctrl Pts',(-6.54971707722324,-1.7098245835392,-58.615603217807));
#33576=CARTESIAN_POINT('Ctrl Pts',(-6.5037545622998,-1.87711313297762,-58.6074587238262));
#33577=CARTESIAN_POINT('Ctrl Pts',(-6.45139937517315,-2.04248258303848,
-58.5993142298454));
#33578=CARTESIAN_POINT('Ctrl Pts',(-6.3990721435299,-2.20776373271935,-58.5911740846843));
#33579=CARTESIAN_POINT('Ctrl Pts',(-6.34035914781289,-2.37112747711318,
-58.5830339395231));
#33580=CARTESIAN_POINT('Ctrl Pts',(-6.27543063422767,-2.53204647567869,
-58.574893794362));
#33581=CARTESIAN_POINT('Ctrl Pts',(-6.21052006539869,-2.69292099991323,
-58.5667558989508));
#33582=CARTESIAN_POINT('Ctrl Pts',(-6.13939753469528,-2.85135178557048,
-58.5586180035396));
#33583=CARTESIAN_POINT('Ctrl Pts',(-6.06228219297214,-3.0068294951282,-58.5504801081284));
#33584=CARTESIAN_POINT('Ctrl Pts',(-5.98517358418205,-3.16229362994209,
-58.5423429232361));
#33585=CARTESIAN_POINT('Ctrl Pts',(-5.90207336845691,-3.31480487554985,
-58.5342057383437));
#33586=CARTESIAN_POINT('Ctrl Pts',(-5.81324759547167,-3.46387664239691,
-58.5260685534514));
#33587=CARTESIAN_POINT('Ctrl Pts',(-5.72441278368444,-3.61296357860458,
-58.5179305405291));
#33588=CARTESIAN_POINT('Ctrl Pts',(-5.62985144195675,-3.75861002640123,
-58.5097925276068));
#33589=CARTESIAN_POINT('Ctrl Pts',(-5.52987404155567,-3.90035666119508,
-58.5016545146845));
#33590=CARTESIAN_POINT('Ctrl Pts',(-5.4298244899644,-4.04220559099123,-58.4935106287617));
#33591=CARTESIAN_POINT('Ctrl Pts',(-5.3243512822683,-4.18014878748545,-58.4853667428389));
#33592=CARTESIAN_POINT('Ctrl Pts',(-5.2138068521877,-4.31375788704937,-58.4772228569162));
#33593=CARTESIAN_POINT('Ctrl Pts',(-5.10321950396809,-4.44741885945667,
-58.4690758091839));
#33594=CARTESIAN_POINT('Ctrl Pts',(-4.98755725111889,-4.57674210857437,
-58.4609287614517));
#33595=CARTESIAN_POINT('Ctrl Pts',(-4.86721064423119,-4.70133486838394,
-58.4527817137194));
#33596=CARTESIAN_POINT('Ctrl Pts',(-4.74672937326799,-4.82606704358085,
-58.4446255496965));
#33597=CARTESIAN_POINT('Ctrl Pts',(-4.62155353956678,-4.94605790233777,
-58.4364693856735));
#33598=CARTESIAN_POINT('Ctrl Pts',(-4.49210876334145,-5.06095325589072,
-58.4283132216506));
#33599=CARTESIAN_POINT('Ctrl Pts',(-4.40772254464528,-5.13585457454431,
-58.422996144662));
#33600=CARTESIAN_POINT('Ctrl Pts',(-4.321522767971,-5.20859120198429,-58.4176790676734));
#33601=CARTESIAN_POINT('Ctrl Pts',(-4.23363416781977,-5.27907479896516,
-58.4123619906848));
#33602=CARTESIAN_POINT('Ctrl Pts',(-4.09297788917386,-5.39187623669255,
-58.4038525792116));
#33603=CARTESIAN_POINT('Ctrl Pts',(-3.94770173405893,-5.49914015861868,
-58.3953431677384));
#33604=CARTESIAN_POINT('Ctrl Pts',(-3.79826584460406,-5.60048797639225,
-58.3868337562653));
#33605=CARTESIAN_POINT('Ctrl Pts',(-3.64896159635609,-5.7017465147491,-58.378331840911));
#33606=CARTESIAN_POINT('Ctrl Pts',(-3.49550518616764,-5.79709915785418,
-58.3698299255567));
#33607=CARTESIAN_POINT('Ctrl Pts',(-3.33838846695244,-5.88620857969873,
-58.3613280102024));
#33608=CARTESIAN_POINT('Ctrl Pts',(-3.18139142156546,-5.97525012801782,
-58.3528325706501));
#33609=CARTESIAN_POINT('Ctrl Pts',(-3.02073990693433,-6.05805777719225,
-58.3443371310978));
#33610=CARTESIAN_POINT('Ctrl Pts',(-2.856953699825,-6.13433815150879,-58.3358416915454));
#33611=CARTESIAN_POINT('Ctrl Pts',(-2.6932945390989,-6.21055935633945,-58.3273528417719));
#33612=CARTESIAN_POINT('Ctrl Pts',(-2.52650582994074,-6.2802632510887,-58.3188639919983));
#33613=CARTESIAN_POINT('Ctrl Pts',(-2.35713103877984,-6.34320283973489,
-58.3103751422247));
#33614=CARTESIAN_POINT('Ctrl Pts',(-2.18783652024992,-6.40611259911109,
-58.3018903156137));
#33615=CARTESIAN_POINT('Ctrl Pts',(-2.01595866646391,-6.46226433152078,
-58.2934054890026));
#33616=CARTESIAN_POINT('Ctrl Pts',(-1.842060715962,-6.51145923113319,-58.2849206623915));
#33617=CARTESIAN_POINT('Ctrl Pts',(-1.66823269249806,-6.56063434872054,
-58.2764392476596));
#33618=CARTESIAN_POINT('Ctrl Pts',(-1.49238650401947,-6.6028581257128,-58.2679578329277));
#33619=CARTESIAN_POINT('Ctrl Pts',(-1.31510071641706,-6.63798155358083,
-58.2594764181957));
#33620=CARTESIAN_POINT('Ctrl Pts',(-1.27414346293795,-6.6460959047519,-58.2575170087149));
#33621=CARTESIAN_POINT('Ctrl Pts',(-1.23310943135344,-6.65383150798569,
-58.2555575992342));
#33622=CARTESIAN_POINT('Ctrl Pts',(-1.19200584984678,-6.66118691029842,
-58.2535981897534));
#33623=CARTESIAN_POINT('Ctrl Pts',(-1.01205733259058,-6.69338833147594,
-58.2450200362728));
#33624=CARTESIAN_POINT('Ctrl Pts',(-0.830857499226969,-6.71828394247207,
-58.2364418827922));
#33625=CARTESIAN_POINT('Ctrl Pts',(-0.649013270227526,-6.73580513191026,
-58.2278637293117));
#33626=CARTESIAN_POINT('Ctrl Pts',(-0.46707724732893,-6.75333516594201,
-58.2192812456296));
#33627=CARTESIAN_POINT('Ctrl Pts',(-0.284496488699637,-6.76348332093542,
-58.2106987619475));
#33628=CARTESIAN_POINT('Ctrl Pts',(-0.1018812542915,-6.76623301475969,-58.2021162782654));
#33629=CARTESIAN_POINT('Ctrl Pts',(0.0883444437133825,-6.76909730167812,
-58.1931761208118));
#33630=CARTESIAN_POINT('Ctrl Pts',(0.278607176176113,-6.76393324505317,
-58.1842359633581));
#33631=CARTESIAN_POINT('Ctrl Pts',(0.468219807672953,-6.75078211851802,
-58.1752958059045));
#33632=CARTESIAN_POINT('Ctrl Pts',(0.650559936823868,-6.73813539718956,
-58.1666985439402));
#33633=CARTESIAN_POINT('Ctrl Pts',(0.832298598842978,-6.71810294428104,
-58.1581012819758));
#33634=CARTESIAN_POINT('Ctrl Pts',(1.01283189780068,-6.69077428604474,-58.1495040200115));
#33635=CARTESIAN_POINT('Ctrl Pts',(1.19347733907426,-6.6634286519982,-58.1409014176647));
#33636=CARTESIAN_POINT('Ctrl Pts',(1.3729156176953,-6.62877782194559,-58.1322988153179));
#33637=CARTESIAN_POINT('Ctrl Pts',(1.55055337761689,-6.58696236691549,-58.1236962129711));
#33638=CARTESIAN_POINT('Ctrl Pts',(1.7283770221265,-6.54510315514901,-58.1150846086463));
#33639=CARTESIAN_POINT('Ctrl Pts',(1.9043960833695,-6.49606441709743,-58.1064730043216));
#33640=CARTESIAN_POINT('Ctrl Pts',(2.07803150655507,-6.44003680562188,-58.0978613999968));
#33641=CARTESIAN_POINT('Ctrl Pts',(2.09837600708972,-6.43347216719323,-58.0968523962718));
#33642=CARTESIAN_POINT('Ctrl Pts',(2.11868780543457,-6.42681163814909,-58.0958433925468));
#33643=CARTESIAN_POINT('Ctrl Pts',(2.13896598755644,-6.42005556861284,-58.0948343888218));
#33644=CARTESIAN_POINT('Ctrl Pts',(2.32113954745933,-6.35936091506975,-58.0857697794088));
#33645=CARTESIAN_POINT('Ctrl Pts',(2.50077046684595,-6.29089416141631,-58.0767051699957));
#33646=CARTESIAN_POINT('Ctrl Pts',(2.67722306560071,-6.21488259398483,-58.0676405605827));
#33647=CARTESIAN_POINT('Ctrl Pts',(2.8535171942986,-6.13893929167099,-58.0585840919915));
#33648=CARTESIAN_POINT('Ctrl Pts',(3.02663848676848,-6.05546479693483,-58.0495276234003));
#33649=CARTESIAN_POINT('Ctrl Pts',(3.19597090940745,-5.96473460819686,-58.0404711548091));
#33650=CARTESIAN_POINT('Ctrl Pts',(3.36500140051961,-5.87416619771721,-58.0314308345334));
#33651=CARTESIAN_POINT('Ctrl Pts',(3.53025630660027,-5.77636803855244,-58.0223905142577));
#33652=CARTESIAN_POINT('Ctrl Pts',(3.6911440278994,-5.67166155242911,-58.013350193982));
#33653=CARTESIAN_POINT('Ctrl Pts',(3.85182510924757,-5.56708954855827,-58.0043214848556));
#33654=CARTESIAN_POINT('Ctrl Pts',(4.0081500044057,-5.45562705271022,-57.9952927757291));
#33655=CARTESIAN_POINT('Ctrl Pts',(4.15955370000717,-5.3376401168266,-57.9862640666026));
#33656=CARTESIAN_POINT('Ctrl Pts',(4.31060307112361,-5.21992930141765,-57.9772564870312));
#33657=CARTESIAN_POINT('Ctrl Pts',(4.45675404689378,-5.09572466732177,-57.9682489074597));
#33658=CARTESIAN_POINT('Ctrl Pts',(4.59747288204903,-4.96543372716058,-57.9592413278882));
#33659=CARTESIAN_POINT('Ctrl Pts',(4.71813272991491,-4.85371531362478,-57.9515177478889));
#33660=CARTESIAN_POINT('Ctrl Pts',(4.83479909263464,-4.73752284250249,-57.9437941678896));
#33661=CARTESIAN_POINT('Ctrl Pts',(4.94715323566637,-4.61713805975474,-57.9360705878902));
#33662=CARTESIAN_POINT('Ctrl Pts',(5.06528399193408,-4.49056377379272,-57.9279499051829));
#33663=CARTESIAN_POINT('Ctrl Pts',(5.1785920583601,-4.35941204046347,-57.9198292224756));
#33664=CARTESIAN_POINT('Ctrl Pts',(5.28671018883337,-4.22409568775205,-57.9117085397683));
#33665=CARTESIAN_POINT('Ctrl Pts',(5.39482055459339,-4.08878905304696,-57.9035884402635));
#33666=CARTESIAN_POINT('Ctrl Pts',(5.49774149818126,-3.94931868085896,-57.8954683407588));
#33667=CARTESIAN_POINT('Ctrl Pts',(5.59514626613433,-3.80613022117782,-57.887348241254));
#33668=CARTESIAN_POINT('Ctrl Pts',(5.69256263745054,-3.66292470414177,-57.8792271744407));
#33669=CARTESIAN_POINT('Ctrl Pts',(5.784461319662,-3.51600052118882,-57.8711061076275));
#33670=CARTESIAN_POINT('Ctrl Pts',(5.87055910324752,-3.36583196480124,-57.8629850408142));
#33671=CARTESIAN_POINT('Ctrl Pts',(5.95671956335136,-3.21555409035823,-57.8548580621159));
#33672=CARTESIAN_POINT('Ctrl Pts',(6.03707050829024,-3.06202744342804,-57.8467310834177));
#33673=CARTESIAN_POINT('Ctrl Pts',(6.11137459397512,-2.90575112012633,-57.8386041047194));
#33674=CARTESIAN_POINT('Ctrl Pts',(6.18570893859352,-2.74941115624775,-57.8304738164628));
#33675=CARTESIAN_POINT('Ctrl Pts',(6.25399137123533,-2.59031962037084,-57.8223435282062));
#33676=CARTESIAN_POINT('Ctrl Pts',(6.31603297161226,-2.42899495707726,-57.8142132399496));
#33677=CARTESIAN_POINT('Ctrl Pts',(6.3781420888897,-2.26749473188369,-57.8060741038899));
#33678=CARTESIAN_POINT('Ctrl Pts',(6.43399669087256,-2.10375687163168,-57.7979349678302));
#33679=CARTESIAN_POINT('Ctrl Pts',(6.483457705782,-1.93831503562658,-57.7897958317704));
#33680=CARTESIAN_POINT('Ctrl Pts',(6.50875608418085,-1.85369464969391,-57.7856328168332));
#33681=CARTESIAN_POINT('Ctrl Pts',(6.53238263822974,-1.76862866598685,-57.781469801896));
#33682=CARTESIAN_POINT('Ctrl Pts',(6.55432395165231,-1.6831893942147,-57.7773067869588));
#33683=CARTESIAN_POINT('Ctrl Pts',(6.5988065897061,-1.50997441256694,-57.7688669145091));
#33684=CARTESIAN_POINT('Ctrl Pts',(6.63645154722509,-1.33486650797698,-57.7604270420594));
#33685=CARTESIAN_POINT('Ctrl Pts',(6.66710754627038,-1.15843254722258,-57.7519871696097));
#33686=CARTESIAN_POINT('Ctrl Pts',(6.6977403006791,-0.98213236593789,-57.7435536966177));
#33687=CARTESIAN_POINT('Ctrl Pts',(6.72139460354281,-0.804508460243176,
-57.7351202236257));
#33688=CARTESIAN_POINT('Ctrl Pts',(6.73796991017135,-0.626139353199828,
-57.7266867506337));
#33689=CARTESIAN_POINT('Ctrl Pts',(6.75453519834567,-0.447878056091589,
-57.7182583750051));
#33690=CARTESIAN_POINT('Ctrl Pts',(6.76402998967732,-0.268872786861646,
-57.7098299993766));
#33691=CARTESIAN_POINT('Ctrl Pts',(6.76640534414454,-0.0897090783152398,
-57.7014016237481));
#33692=CARTESIAN_POINT('Ctrl Pts',(6.76877962787636,0.0893738688426241,
-57.6929770473673));
#33693=CARTESIAN_POINT('Ctrl Pts',(6.76404086914789,0.268614779974892,-57.6845524709865));
#33694=CARTESIAN_POINT('Ctrl Pts',(6.7521921726132,0.447425819662907,-57.6761278946058));
#33695=CARTESIAN_POINT('Ctrl Pts',(6.74034699804638,0.626183708632252,-57.6677058223897));
#33696=CARTESIAN_POINT('Ctrl Pts',(6.7213961222744,0.804511648534019,-57.6592837501736));
#33697=CARTESIAN_POINT('Ctrl Pts',(6.69539469960215,0.981824228942961,-57.6508616779575));
#33698=CARTESIAN_POINT('Ctrl Pts',(6.66939289198227,1.15913943444125,-57.6424394810537));
#33699=CARTESIAN_POINT('Ctrl Pts',(6.63634037071619,1.33543891953788,-57.63401728415));
#33700=CARTESIAN_POINT('Ctrl Pts',(6.59634396466023,1.51014413215779,-57.6255950872462));
#33701=CARTESIAN_POINT('Ctrl Pts',(6.55634621297761,1.68485522250557,-57.6171726069887));
#33702=CARTESIAN_POINT('Ctrl Pts',(6.50940418498622,1.85797160819041,-57.6087501267312));
#33703=CARTESIAN_POINT('Ctrl Pts',(6.45567551203003,2.02892648545378,-57.6003276464736));
#33704=CARTESIAN_POINT('Ctrl Pts',(6.40193752585657,2.19991099568271,-57.5919037062808));
#33705=CARTESIAN_POINT('Ctrl Pts',(6.34141064938845,2.36873293225993,-57.5834797660879));
#33706=CARTESIAN_POINT('Ctrl Pts',(6.27430202976855,2.53484181740049,-57.575055825895));
#33707=CARTESIAN_POINT('Ctrl Pts',(6.2071724001284,2.70100270705346,-57.5666292483784));
#33708=CARTESIAN_POINT('Ctrl Pts',(6.13345704402997,2.8644485426354,-57.5582026708618));
#33709=CARTESIAN_POINT('Ctrl Pts',(6.05341091752872,3.0246496100448,-57.5497760933452));
#33710=CARTESIAN_POINT('Ctrl Pts',(5.97329300358367,3.18499434992935,-57.5413419586552));
#33711=CARTESIAN_POINT('Ctrl Pts',(5.8868331238357,3.34208820835713,-57.5329078239652));
#33712=CARTESIAN_POINT('Ctrl Pts',(5.79433234132488,3.49542582788943,-57.5244736892752));
#33713=CARTESIAN_POINT('Ctrl Pts',(5.70178685276455,3.64883755619169,-57.5160354783295));
#33714=CARTESIAN_POINT('Ctrl Pts',(5.6031948177927,3.79848914375275,-57.5075972673837));
#33715=CARTESIAN_POINT('Ctrl Pts',(5.49890045757043,3.94390450666997,-57.499159056438));
#33716=CARTESIAN_POINT('Ctrl Pts',(5.39449009093992,4.08948161480446,-57.4907114596871));
#33717=CARTESIAN_POINT('Ctrl Pts',(5.28436492650002,4.23081281689812,-57.4822638629363));
#33718=CARTESIAN_POINT('Ctrl Pts',(5.16891001645091,4.3674544350037,-57.4738162661854));
#33719=CARTESIAN_POINT('Ctrl Pts',(5.10496086490121,4.44313866134377,-57.4691372391555));
#33720=CARTESIAN_POINT('Ctrl Pts',(5.03937727196056,4.51738478329513,-57.4644582121256));
#33721=CARTESIAN_POINT('Ctrl Pts',(4.97222950422016,4.59012230309418,-57.4597791850957));
#33722=CARTESIAN_POINT('Ctrl Pts',(4.85390604080383,4.718295666894,-57.4515341055909));
#33723=CARTESIAN_POINT('Ctrl Pts',(4.73046040637767,4.84206744563971,-57.443289026086));
#33724=CARTESIAN_POINT('Ctrl Pts',(4.60225118473719,4.96100524416021,-57.4350439465811));
#33725=CARTESIAN_POINT('Ctrl Pts',(4.47422936691191,5.07976919093333,-57.4268109189344));
#33726=CARTESIAN_POINT('Ctrl Pts',(4.34145809775002,5.19371299996821,-57.4185778912877));
#33727=CARTESIAN_POINT('Ctrl Pts',(4.20433473594713,5.3024389131897,-57.410344863641));
#33728=CARTESIAN_POINT('Ctrl Pts',(4.06732711311721,5.41107305630459,-57.4021187850813));
#33729=CARTESIAN_POINT('Ctrl Pts',(3.92597498720908,5.51449785168672,-57.3938927065215));
#33730=CARTESIAN_POINT('Ctrl Pts',(3.78071153043142,5.61235327858671,-57.3856666279618));
#33731=CARTESIAN_POINT('Ctrl Pts',(3.63556788838887,5.71012799336326,-57.3774473343529));
#33732=CARTESIAN_POINT('Ctrl Pts',(3.48651963768592,5.80234229538776,-57.3692280407441));
#33733=CARTESIAN_POINT('Ctrl Pts',(3.33403176483176,5.88867737196502,-57.3610087471353));
#33734=CARTESIAN_POINT('Ctrl Pts',(3.25658189369875,5.93252768235372,-57.3568340988902));
#33735=CARTESIAN_POINT('Ctrl Pts',(3.17824519961803,5.97486198848,-57.3526594506451));
#33736=CARTESIAN_POINT('Ctrl Pts',(3.09908550384721,6.01564277861012,-57.3484848024));
#33737=CARTESIAN_POINT('Origin',(0.,0.,-63.6971797838103));
#33738=CARTESIAN_POINT('',(3.09908550384721,6.01564277861012,-54.9544629019808));
#33739=CARTESIAN_POINT('',(3.09908550384722,6.01564277861011,-55.3486963765549));
#33740=CARTESIAN_POINT('',(3.09908550384721,6.01564277861012,-63.6971797838103));
#33741=CARTESIAN_POINT('',(-6.76699956244302,-0.00224392468289009,-56.30282021619));
#33742=CARTESIAN_POINT('Ctrl Pts',(-6.76699948538929,-0.00263907960515001,
-56.30282021619));
#33743=CARTESIAN_POINT('Ctrl Pts',(-6.76692693805531,-0.188661422665976,
-56.2940962489685));
#33744=CARTESIAN_POINT('Ctrl Pts',(-6.75917963189646,-0.37450585182449,
-56.285372281747));
#33745=CARTESIAN_POINT('Ctrl Pts',(-6.74382674775489,-0.559544275518678,
-56.2766483145255));
#33746=CARTESIAN_POINT('Ctrl Pts',(-6.72845327550817,-0.744830834383355,
-56.2679126485278));
#33747=CARTESIAN_POINT('Ctrl Pts',(-6.70545389015303,-0.929308946509522,
-56.2591769825302));
#33748=CARTESIAN_POINT('Ctrl Pts',(-6.67494911439005,-1.11235934854863,
-56.2504413165326));
#33749=CARTESIAN_POINT('Ctrl Pts',(-6.64438168603178,-1.29578571082576,
-56.2416877086838));
#33750=CARTESIAN_POINT('Ctrl Pts',(-6.60627809895353,-1.47777821971559,
-56.232934100835));
#33751=CARTESIAN_POINT('Ctrl Pts',(-6.56080958945618,-1.65772932980626,
-56.2241804929862));
#33752=CARTESIAN_POINT('Ctrl Pts',(-6.54509139510451,-1.71993736243086,
-56.2211544226143));
#33753=CARTESIAN_POINT('Ctrl Pts',(-6.52849349090117,-1.7819015937994,-56.2181283522424));
#33754=CARTESIAN_POINT('Ctrl Pts',(-6.51102430173979,-1.84359744579825,
-56.2151022818704));
#33755=CARTESIAN_POINT('Ctrl Pts',(-6.4622969571836,-2.01568757604209,-56.206661571068));
#33756=CARTESIAN_POINT('Ctrl Pts',(-6.40670677850405,-2.18597184016191,
-56.1982208602656));
#33757=CARTESIAN_POINT('Ctrl Pts',(-6.34440843207874,-2.35388416175652,
-56.1897801494632));
#33758=CARTESIAN_POINT('Ctrl Pts',(-6.28215717440228,-2.52166956535741,
-56.1813458186457));
#33759=CARTESIAN_POINT('Ctrl Pts',(-6.21320797213382,-2.68708628890399,
-56.1729114878282));
#33760=CARTESIAN_POINT('Ctrl Pts',(-6.13776519577141,-2.8495837242617,-56.1644771570107));
#33761=CARTESIAN_POINT('Ctrl Pts',(-6.06236785829259,-3.01198328806158,
-56.156047906157));
#33762=CARTESIAN_POINT('Ctrl Pts',(-5.98048488404462,-3.17146676740238,
-56.1476186553034));
#33763=CARTESIAN_POINT('Ctrl Pts',(-5.89236876185276,-3.32750347473023,
-56.1391894044497));
#33764=CARTESIAN_POINT('Ctrl Pts',(-5.80429219518604,-3.48347013682976,
-56.1307639375057));
#33765=CARTESIAN_POINT('Ctrl Pts',(-5.70998822331743,-3.63599282215774,
-56.1223384705617));
#33766=CARTESIAN_POINT('Ctrl Pts',(-5.60975546457031,-3.78456505132671,
-56.1139130036177));
#33767=CARTESIAN_POINT('Ctrl Pts',(-5.50955233830795,-3.93309335708809,
-56.1054900275511));
#33768=CARTESIAN_POINT('Ctrl Pts',(-5.40342410685413,-4.07767325964716,
-56.0970670514846));
#33769=CARTESIAN_POINT('Ctrl Pts',(-5.29171314321519,-4.21782657418766,
-56.0886440754181));
#33770=CARTESIAN_POINT('Ctrl Pts',(-5.18000033079129,-4.35798220822601,
-56.0802209599536));
#33771=CARTESIAN_POINT('Ctrl Pts',(-5.06270480417671,-4.49371084309492,
-56.0717978444892));
#33772=CARTESIAN_POINT('Ctrl Pts',(-4.94021013663323,-4.62456622894583,
-56.0633747290248));
#33773=CARTESIAN_POINT('Ctrl Pts',(-4.81771123355154,-4.75542613942625,
-56.0549513223116));
#33774=CARTESIAN_POINT('Ctrl Pts',(-4.69001305889338,-4.88141222132429,
-56.0465279155983));
#33775=CARTESIAN_POINT('Ctrl Pts',(-4.55753717157229,-5.00211394609687,
-56.0381045088851));
#33776=CARTESIAN_POINT('Ctrl Pts',(-4.42503822772495,-5.12283667818289,
-56.0296796361353));
#33777=CARTESIAN_POINT('Ctrl Pts',(-4.28776015990397,-5.23827299492014,
-56.0212547633854));
#33778=CARTESIAN_POINT('Ctrl Pts',(-4.1461590977859,-5.34805139614862,-56.0128298906356));
#33779=CARTESIAN_POINT('Ctrl Pts',(-4.00451363635481,-5.45786421862739,
-56.0044023762491));
#33780=CARTESIAN_POINT('Ctrl Pts',(-3.85854274161604,-5.56201538436767,
-55.9959748618625));
#33781=CARTESIAN_POINT('Ctrl Pts',(-3.70873340663003,-5.66017539644722,
-55.987547347476));
#33782=CARTESIAN_POINT('Ctrl Pts',(-3.55878972829389,-5.75842343471601,
-55.9791122756131));
#33783=CARTESIAN_POINT('Ctrl Pts',(-3.40500101097334,-5.85066940107159,
-55.9706772037501));
#33784=CARTESIAN_POINT('Ctrl Pts',(-3.2478818329335,-5.93662804960025,-55.9622421318872));
#33785=CARTESIAN_POINT('Ctrl Pts',(-3.09068671811301,-6.02262824253566,
-55.9538029832959));
#33786=CARTESIAN_POINT('Ctrl Pts',(-2.93015822857286,-6.10233490447294,
-55.9453638347046));
#33787=CARTESIAN_POINT('Ctrl Pts',(-2.7668335065865,-6.17550980460968,-55.9369246861134));
#33788=CARTESIAN_POINT('Ctrl Pts',(-2.60332728413809,-6.2487660229818,-55.9284761592152));
#33789=CARTESIAN_POINT('Ctrl Pts',(-2.43701892780129,-6.31547584685385,
-55.920027632317));
#33790=CARTESIAN_POINT('Ctrl Pts',(-2.26846455665855,-6.37544959631742,
-55.9115791054189));
#33791=CARTESIAN_POINT('Ctrl Pts',(-2.17533166904081,-6.40858744039074,
-55.9069109636151));
#33792=CARTESIAN_POINT('Ctrl Pts',(-2.08151335051161,-6.43966964643707,
-55.9022428218113));
#33793=CARTESIAN_POINT('Ctrl Pts',(-1.98710511392526,-6.46867082685555,
-55.8975746800075));
#33794=CARTESIAN_POINT('Ctrl Pts',(-1.82044403495016,-6.51986729227915,
-55.8893338995633));
#33795=CARTESIAN_POINT('Ctrl Pts',(-1.65157302759785,-6.56468945802155,
-55.8810931191192));
#33796=CARTESIAN_POINT('Ctrl Pts',(-1.48101887055946,-6.60294419975262,
-55.872852338675));
#33797=CARTESIAN_POINT('Ctrl Pts',(-1.31065362102099,-6.64115657014695,
-55.8646206858022));
#33798=CARTESIAN_POINT('Ctrl Pts',(-1.13860927801477,-6.67281592349907,
-55.8563890329293));
#33799=CARTESIAN_POINT('Ctrl Pts',(-0.965429278168779,-6.69777838606612,
-55.8481573800565));
#33800=CARTESIAN_POINT('Ctrl Pts',(-0.792410232061655,-6.72271764848486,
-55.8399333776935));
#33801=CARTESIAN_POINT('Ctrl Pts',(-0.618257981217408,-6.74097236515085,
-55.8317093753306));
#33802=CARTESIAN_POINT('Ctrl Pts',(-0.443527794631489,-6.75244934045338,
-55.8234853729677));
#33803=CARTESIAN_POINT('Ctrl Pts',(-0.2689519837863,-6.76391617574177,-55.8152686365871));
#33804=CARTESIAN_POINT('Ctrl Pts',(-0.0937996085672701,-6.76861718154645,
-55.8070519002066));
#33805=CARTESIAN_POINT('Ctrl Pts',(0.0813673975475972,-6.76651079557377,
-55.798835163826));
#33806=CARTESIAN_POINT('Ctrl Pts',(0.25644465855948,-6.76440548878735,-55.79062263721));
#33807=CARTESIAN_POINT('Ctrl Pts',(0.431536180653232,-6.75549974061508,
-55.782410110594));
#33808=CARTESIAN_POINT('Ctrl Pts',(0.606078053571137,-6.73980403223858,
-55.774197583978));
#33809=CARTESIAN_POINT('Ctrl Pts',(0.780561557681218,-6.72411357268731,
-55.7659878037253));
#33810=CARTESIAN_POINT('Ctrl Pts',(0.954495424817928,-6.70163770814786,
-55.7577780234726));
#33811=CARTESIAN_POINT('Ctrl Pts',(1.1273187995095,-6.67243893372375,-55.7495682432198));
#33812=CARTESIAN_POINT('Ctrl Pts',(1.20280291385807,-6.65968577674251,-55.7459824551719));
#33813=CARTESIAN_POINT('Ctrl Pts',(1.27807524536973,-6.64565076977929,-55.7423966671239));
#33814=CARTESIAN_POINT('Ctrl Pts',(1.35308947604327,-6.63034221362827,-55.738810879076));
#33815=CARTESIAN_POINT('Ctrl Pts',(1.5384126622837,-6.59252231762753,-55.7299521643993));
#33816=CARTESIAN_POINT('Ctrl Pts',(1.72196784688877,-6.54696537009473,-55.7210934497226));
#33817=CARTESIAN_POINT('Ctrl Pts',(1.9031332698811,-6.4938719387644,-55.7122347350459));
#33818=CARTESIAN_POINT('Ctrl Pts',(2.08463762197831,-6.44067917882677,-55.7033594472496));
#33819=CARTESIAN_POINT('Ctrl Pts',(2.26374302893443,-6.37992183123153,-55.6944841594532));
#33820=CARTESIAN_POINT('Ctrl Pts',(2.43984584190009,-6.31184927479759,-55.6856088716569));
#33821=CARTESIAN_POINT('Ctrl Pts',(2.61644882401098,-6.24358337794057,-55.6767083761705));
#33822=CARTESIAN_POINT('Ctrl Pts',(2.79003190314272,-6.16796078954175,-55.6678078806842));
#33823=CARTESIAN_POINT('Ctrl Pts',(2.96001146623973,-6.08527905027611,-55.6589073851979));
#33824=CARTESIAN_POINT('Ctrl Pts',(3.13022112985471,-6.00248538513724,-55.6499948411536));
#33825=CARTESIAN_POINT('Ctrl Pts',(3.2968173029028,-5.912613599898,-55.6410822971093));
#33826=CARTESIAN_POINT('Ctrl Pts',(3.45924252893128,-5.81600637259221,-55.632169753065));
#33827=CARTESIAN_POINT('Ctrl Pts',(3.62202640506276,-5.71918582748553,-55.6232375292892));
#33828=CARTESIAN_POINT('Ctrl Pts',(3.78062068915887,-5.61560022599677,-55.6143053055134));
#33829=CARTESIAN_POINT('Ctrl Pts',(3.93449600083651,-5.50563622294477,-55.6053730817375));
#33830=CARTESIAN_POINT('Ctrl Pts',(4.07992625405044,-5.40170731691095,-55.5969310805398));
#33831=CARTESIAN_POINT('Ctrl Pts',(4.22114142569898,-5.29208138818329,-55.5884890793421));
#33832=CARTESIAN_POINT('Ctrl Pts',(4.3577229824198,-5.17711690118065,-55.5800470781444));
#33833=CARTESIAN_POINT('Ctrl Pts',(4.49077712664718,-5.06512153517421,-55.5718231036057));
#33834=CARTESIAN_POINT('Ctrl Pts',(4.61968740222887,-4.94784506964502,-55.563599129067));
#33835=CARTESIAN_POINT('Ctrl Pts',(4.74400940944454,-4.8256257338403,-55.5553751545283));
#33836=CARTESIAN_POINT('Ctrl Pts',(4.8682001205618,-4.70353547350902,-55.5471598653044));
#33837=CARTESIAN_POINT('Ctrl Pts',(4.98781195904097,-4.5765129872896,-55.5389445760806));
#33838=CARTESIAN_POINT('Ctrl Pts',(5.10243315790944,-4.44493699269925,-55.5307292868567));
#33839=CARTESIAN_POINT('Ctrl Pts',(5.21695629624148,-4.31347356378383,-55.5225210259633));
#33840=CARTESIAN_POINT('Ctrl Pts',(5.32649706405495,-4.17746465385995,-55.5143127650699));
#33841=CARTESIAN_POINT('Ctrl Pts',(5.43068011653878,-4.03732615375949,-55.5061045041765));
#33842=CARTESIAN_POINT('Ctrl Pts',(5.53479492945887,-3.89727944392511,-55.4979016196676));
#33843=CARTESIAN_POINT('Ctrl Pts',(5.63355880399971,-3.75310881848125,-55.4896987351586));
#33844=CARTESIAN_POINT('Ctrl Pts',(5.72663626209239,-3.60526366881655,-55.4814958506497));
#33845=CARTESIAN_POINT('Ctrl Pts',(5.81967141497185,-3.4574857171685,-55.4732966944847));
#33846=CARTESIAN_POINT('Ctrl Pts',(5.90702510988222,-3.30603687147461,-55.4650975383197));
#33847=CARTESIAN_POINT('Ctrl Pts',(5.98840480156228,-3.15139602916323,-55.4568983821547));
#33848=CARTESIAN_POINT('Ctrl Pts',(6.06977741517949,-2.99676863686106,-55.4486999391178));
#33849=CARTESIAN_POINT('Ctrl Pts',(6.14517688609919,-2.83895011405359,-55.4405014960809));
#33850=CARTESIAN_POINT('Ctrl Pts',(6.2143561395723,-2.67844484179907,-55.432303053044));
#33851=CARTESIAN_POINT('Ctrl Pts',(6.28353470409734,-2.51794116799774,-55.4241046916544));
#33852=CARTESIAN_POINT('Ctrl Pts',(6.34649303161368,-2.3547511270299,-55.4159063302648));
#33853=CARTESIAN_POINT('Ctrl Pts',(6.4030318683709,-2.18939989326452,-55.4077079688752));
#33854=CARTESIAN_POINT('Ctrl Pts',(6.45958041274809,-2.02402026897978,-55.3995081998413));
#33855=CARTESIAN_POINT('Ctrl Pts',(6.50970715437334,-1.8564790520249,-55.3913084308073));
#33856=CARTESIAN_POINT('Ctrl Pts',(6.55326245241661,-1.68731746560824,-55.3831086617733));
#33857=CARTESIAN_POINT('Ctrl Pts',(6.59683314104232,-1.5180961047105,-55.3749059952911));
#33858=CARTESIAN_POINT('Ctrl Pts',(6.6338276711041,-1.34725358093727,-55.3667033288089));
#33859=CARTESIAN_POINT('Ctrl Pts',(6.66414732397989,-1.17534226687024,-55.3585006623267));
#33860=CARTESIAN_POINT('Ctrl Pts',(6.69450141239539,-1.00323570456255,-55.3502886796676));
#33861=CARTESIAN_POINT('Ctrl Pts',(6.71816541592229,-0.830058280472868,
-55.3420766970086));
#33862=CARTESIAN_POINT('Ctrl Pts',(6.73509228255465,-0.656369519000377,
-55.3338647143496));
#33863=CARTESIAN_POINT('Ctrl Pts',(6.75202913287981,-0.4825783135686,-55.3256478881531));
#33864=CARTESIAN_POINT('Ctrl Pts',(6.76222090449828,-0.308275527055722,
-55.3174310619567));
#33865=CARTESIAN_POINT('Ctrl Pts',(6.76567271029664,-0.134021554786235,
-55.3092142357602));
#33866=CARTESIAN_POINT('Ctrl Pts',(6.76912983927692,0.0405011422167447,
-55.3009847380338));
#33867=CARTESIAN_POINT('Ctrl Pts',(6.76582623826288,0.214974516173924,-55.2927552403074));
#33868=CARTESIAN_POINT('Ctrl Pts',(6.75581909213108,0.388841091446277,-55.284525742581));
#33869=CARTESIAN_POINT('Ctrl Pts',(6.74689915031543,0.543818316190675,-55.2771903204811));
#33870=CARTESIAN_POINT('Ctrl Pts',(6.73265387911371,0.698313339590443,-55.2698548983812));
#33871=CARTESIAN_POINT('Ctrl Pts',(6.71315796159024,0.851938485301359,-55.2625194762814));
#33872=CARTESIAN_POINT('Ctrl Pts',(6.69170690993703,1.02096981875415,-55.2544484266284));
#33873=CARTESIAN_POINT('Ctrl Pts',(6.66382835574612,1.18949909330404,-55.2463773769754));
#33874=CARTESIAN_POINT('Ctrl Pts',(6.62954566461423,1.35698683884359,-55.2383063273224));
#33875=CARTESIAN_POINT('Ctrl Pts',(6.59530579751382,1.52426536800451,-55.2302453595759));
#33876=CARTESIAN_POINT('Ctrl Pts',(6.55467778501534,1.69050459604163,-55.2221843918294));
#33877=CARTESIAN_POINT('Ctrl Pts',(6.50773684329409,1.85516850405365,-55.2141234240828));
#33878=CARTESIAN_POINT('Ctrl Pts',(6.46084424350325,2.01966283363607,-55.2060707578898));
#33879=CARTESIAN_POINT('Ctrl Pts',(6.40765175409085,2.1825847160492,-55.1980180916969));
#33880=CARTESIAN_POINT('Ctrl Pts',(6.34828588222641,2.34340678447531,-55.1899654255039));
#33881=CARTESIAN_POINT('Ctrl Pts',(6.28896814852193,2.5040984466897,-55.1819192889974));
#33882=CARTESIAN_POINT('Ctrl Pts',(6.22348712451107,2.66269333576979,-55.173873152491));
#33883=CARTESIAN_POINT('Ctrl Pts',(6.15201951764226,2.81867785575946,-55.1658270159845));
#33884=CARTESIAN_POINT('Ctrl Pts',(6.08059422865249,2.97457001314822,-55.1577856438104));
#33885=CARTESIAN_POINT('Ctrl Pts',(6.0031895687952,3.1278545403016,-55.1497442716363));
#33886=CARTESIAN_POINT('Ctrl Pts',(5.92003083518417,3.27803659382695,-55.1417028994622));
#33887=CARTESIAN_POINT('Ctrl Pts',(5.8368929307542,3.42818103050739,-55.1336635414505));
#33888=CARTESIAN_POINT('Ctrl Pts',(5.748003996651,3.57522421132448,-55.1256241834388));
#33889=CARTESIAN_POINT('Ctrl Pts',(5.65363590927376,3.7186946641759,-55.1175848254271));
#33890=CARTESIAN_POINT('Ctrl Pts',(5.559277401509,3.86215055287348,-55.1095462835169));
#33891=CARTESIAN_POINT('Ctrl Pts',(5.4594410517705,4.00203412297442,-55.1015077416067));
#33892=CARTESIAN_POINT('Ctrl Pts',(5.35444269168022,4.13790193957183,-55.0934691996965));
#33893=CARTESIAN_POINT('Ctrl Pts',(5.24943420515712,4.27378285976739,-55.0854298825193));
#33894=CARTESIAN_POINT('Ctrl Pts',(5.13926294560076,4.40564696001497,-55.0773905653422));
#33895=CARTESIAN_POINT('Ctrl Pts',(5.02428564383119,4.53308314165886,-55.0693512481651));
#33896=CARTESIAN_POINT('Ctrl Pts',(4.90927448809729,4.66055684566483,-55.0613095638881));
#33897=CARTESIAN_POINT('Ctrl Pts',(4.78945472376362,4.78359975919453,-55.0532678796111));
#33898=CARTESIAN_POINT('Ctrl Pts',(4.66522049469816,4.90183707765244,-55.0452261953341));
#33899=CARTESIAN_POINT('Ctrl Pts',(4.54085398567013,5.02020029078671,-55.0371759485723));
#33900=CARTESIAN_POINT('Ctrl Pts',(4.41206389566123,5.13374743267266,-55.0291257018105));
#33901=CARTESIAN_POINT('Ctrl Pts',(4.2792786470111,5.24214300274562,-55.0210754550487));
#33902=CARTESIAN_POINT('Ctrl Pts',(4.14641810207679,5.3506000388604,-55.0130206433697));
#33903=CARTESIAN_POINT('Ctrl Pts',(4.00955818376298,5.45389946088245,-55.0049658316907));
#33904=CARTESIAN_POINT('Ctrl Pts',(3.86915651691859,5.55174898996581,-54.9969110200117));
#33905=CARTESIAN_POINT('Ctrl Pts',(3.7285473720021,5.64974311584853,-54.9888443053629));
#33906=CARTESIAN_POINT('Ctrl Pts',(3.58438633853291,5.74227106255868,-54.9807775907141));
#33907=CARTESIAN_POINT('Ctrl Pts',(3.43715672144868,5.82908592081127,-54.9727108760654));
#33908=CARTESIAN_POINT('Ctrl Pts',(3.32613910754568,5.89454814645175,-54.9666282180372));
#33909=CARTESIAN_POINT('Ctrl Pts',(3.21337727196016,5.95676295897932,-54.960545560009));
#33910=CARTESIAN_POINT('Ctrl Pts',(3.09908550384721,6.01564277861012,-54.9544629019808));
#33911=CARTESIAN_POINT('Ctrl Pts',(3.0990855038472,6.01564277861012,-56.9542436419538));
#33912=CARTESIAN_POINT('Ctrl Pts',(2.93373232018328,6.1008279655248,-56.9454941940545));
#33913=CARTESIAN_POINT('Ctrl Pts',(2.76486502144425,6.17919158180191,-56.9367447461552));
#33914=CARTESIAN_POINT('Ctrl Pts',(2.59305716434349,6.2504674659138,-56.927995298256));
#33915=CARTESIAN_POINT('Ctrl Pts',(2.42125069459281,6.32174277447225,-56.9192459210085));
#33916=CARTESIAN_POINT('Ctrl Pts',(2.24650397871057,6.38593035557826,-56.9104965437611));
#33917=CARTESIAN_POINT('Ctrl Pts',(2.06941053323771,6.44281220003539,-56.9017471665137));
#33918=CARTESIAN_POINT('Ctrl Pts',(1.8923184589668,6.49969360406686,-56.8929978570111));
#33919=CARTESIAN_POINT('Ctrl Pts',(1.71287996431499,6.54926929700882,-56.8842485475085));
#33920=CARTESIAN_POINT('Ctrl Pts',(1.53170449173495,6.59137090065481,-56.8754992380059));
#33921=CARTESIAN_POINT('Ctrl Pts',(1.35053036178164,6.63347219230085,-56.8667499933413));
#33922=CARTESIAN_POINT('Ctrl Pts',(1.1676195587884,6.66809944062455,-56.8580007486767));
#33923=CARTESIAN_POINT('Ctrl Pts',(0.983593309310466,6.69513503985392,-56.8492515040121));
#33924=CARTESIAN_POINT('Ctrl Pts',(0.799568362460043,6.72217044771213,-56.840502321279));
#33925=CARTESIAN_POINT('Ctrl Pts',(0.614428268438739,6.74161427235976,-56.8317531385458));
#33926=CARTESIAN_POINT('Ctrl Pts',(0.428801816330496,6.75340047696801,-56.8230039558126));
#33927=CARTESIAN_POINT('Ctrl Pts',(0.243176616522996,6.76518660206241,-56.8142548321045));
#33928=CARTESIAN_POINT('Ctrl Pts',(0.0570653511656601,6.76931519233997,
-56.8055057083964));
#33929=CARTESIAN_POINT('Ctrl Pts',(-0.128899900799846,6.76577222610796,
-56.7967565846882));
#33930=CARTESIAN_POINT('Ctrl Pts',(-0.314863959941722,6.76222928260134,
-56.788007517099));
#33931=CARTESIAN_POINT('Ctrl Pts',(-0.500681721080267,6.75101488651279,
-56.7792584495097));
#33932=CARTESIAN_POINT('Ctrl Pts',(-0.685722110172772,6.73216712415996,
-56.7705093819205));
#33933=CARTESIAN_POINT('Ctrl Pts',(-0.870761373826947,6.71331947644153,
-56.7617603675441));
#33934=CARTESIAN_POINT('Ctrl Pts',(-1.05502298984263,6.68683858440009,-56.7530113531678));
#33935=CARTESIAN_POINT('Ctrl Pts',(-1.23788117675966,6.65281438131443,-56.7442623387914));
#33936=CARTESIAN_POINT('Ctrl Pts',(-1.43009641451704,6.61704912302397,-56.7350656279039));
#33937=CARTESIAN_POINT('Ctrl Pts',(-1.62076048992612,6.57294837083186,-56.7258689170163));
#33938=CARTESIAN_POINT('Ctrl Pts',(-1.80915798961053,6.52067760042071,-56.7166722061288));
#33939=CARTESIAN_POINT('Ctrl Pts',(-1.98840443002927,6.47094578577435,-56.7079222084223));
#33940=CARTESIAN_POINT('Ctrl Pts',(-2.16559895952101,6.41381888474506,-56.6991722107158));
#33941=CARTESIAN_POINT('Ctrl Pts',(-2.34013966242226,6.3494909528527,-56.6904222130093));
#33942=CARTESIAN_POINT('Ctrl Pts',(-2.51467682553918,6.28516432556724,-56.6816723927577));
#33943=CARTESIAN_POINT('Ctrl Pts',(-2.68656000078745,6.21363705879703,-56.6729225725061));
#33944=CARTESIAN_POINT('Ctrl Pts',(-2.85520533840792,6.13515211510904,-56.6641727522545));
#33945=CARTESIAN_POINT('Ctrl Pts',(-3.02384747998232,6.05666865881169,-56.6554230978233));
#33946=CARTESIAN_POINT('Ctrl Pts',(-3.18925164684443,5.97122791039894,-56.646673443392));
#33947=CARTESIAN_POINT('Ctrl Pts',(-3.35085601829066,5.8791200825196,-56.6379237889608));
#33948=CARTESIAN_POINT('Ctrl Pts',(-3.51245754191324,5.78701387778231,-56.6291742887176));
#33949=CARTESIAN_POINT('Ctrl Pts',(-3.6702591551084,5.68824097061044,-56.6204247884745));
#33950=CARTESIAN_POINT('Ctrl Pts',(-3.82372487928737,5.58313684656921,-56.6116752882314));
#33951=CARTESIAN_POINT('Ctrl Pts',(-3.97718810300709,5.47803443501838,-56.6029259305462));
#33952=CARTESIAN_POINT('Ctrl Pts',(-4.12631534262945,5.36660117496438,-56.5941765728611));
#33953=CARTESIAN_POINT('Ctrl Pts',(-4.27060009886153,5.24921554097409,-56.585427215176));
#33954=CARTESIAN_POINT('Ctrl Pts',(-4.41488269594157,5.13183166360341,-56.5766779884208));
#33955=CARTESIAN_POINT('Ctrl Pts',(-4.55432273235047,5.00849577139509,-56.5679287616656));
#33956=CARTESIAN_POINT('Ctrl Pts',(-4.68844662480179,4.87962675277369,-56.5591795349104));
#33957=CARTESIAN_POINT('Ctrl Pts',(-4.82256868835105,4.75075949139934,-56.5504304274589));
#33958=CARTESIAN_POINT('Ctrl Pts',(-4.95137454637787,4.61635945312604,-56.5416813200075));
#33959=CARTESIAN_POINT('Ctrl Pts',(-5.07442674460983,4.47688309134699,-56.532932212556));
#33960=CARTESIAN_POINT('Ctrl Pts',(-5.19747742838454,4.33740844616453,-56.5241832127836));
#33961=CARTESIAN_POINT('Ctrl Pts',(-5.31477440450853,4.19285781736123,-56.5154342130112));
#33962=CARTESIAN_POINT('Ctrl Pts',(-5.42591931531088,4.04372211999493,-56.5066852132389));
#33963=CARTESIAN_POINT('Ctrl Pts',(-5.53707636462921,3.89457013500887,-56.4979352579583));
#33964=CARTESIAN_POINT('Ctrl Pts',(-5.64207983273414,3.74083230916506,-56.4891853026777));
#33965=CARTESIAN_POINT('Ctrl Pts',(-5.74057303468694,3.58303087251913,-56.4804353473971));
#33966=CARTESIAN_POINT('Ctrl Pts',(-5.83906243363715,3.42523552887516,-56.4716857299683));
#33967=CARTESIAN_POINT('Ctrl Pts',(-5.93104191768379,3.26337713157077,-56.4629361125395));
#33968=CARTESIAN_POINT('Ctrl Pts',(-6.01619906699613,3.09800545291239,-56.4541864951107));
#33969=CARTESIAN_POINT('Ctrl Pts',(-6.10135338095344,2.93263928039677,-56.4454371690053));
#33970=CARTESIAN_POINT('Ctrl Pts',(-6.17968568352803,2.76376031540304,-56.4366878428999));
#33971=CARTESIAN_POINT('Ctrl Pts',(-6.25092992694854,2.5919421383162,-56.4279385167945));
#33972=CARTESIAN_POINT('Ctrl Pts',(-6.32217217691057,2.42012876880939,-56.4191894355007));
#33973=CARTESIAN_POINT('Ctrl Pts',(-6.38632665483793,2.2453766164783,-56.410440354207));
#33974=CARTESIAN_POINT('Ctrl Pts',(-6.44317547869285,2.06827917621659,-56.4016912729132));
#33975=CARTESIAN_POINT('Ctrl Pts',(-6.50002944235876,1.89116572423629,-56.3929414005982));
#33976=CARTESIAN_POINT('Ctrl Pts',(-6.54957634250344,1.71170683289406,-56.3841915282833));
#33977=CARTESIAN_POINT('Ctrl Pts',(-6.59164787708347,1.53051209225574,-56.3754416559683));
#33978=CARTESIAN_POINT('Ctrl Pts',(-6.63371649074968,1.34932993148233,-56.3666923911335));
#33979=CARTESIAN_POINT('Ctrl Pts',(-6.6683107125709,1.16641244174199,-56.3579431262987));
#33980=CARTESIAN_POINT('Ctrl Pts',(-6.69531304840305,0.982380875161888,
-56.3491938614639));
#33981=CARTESIAN_POINT('Ctrl Pts',(-6.72231677033021,0.798339861797759,
-56.3404441475083));
#33982=CARTESIAN_POINT('Ctrl Pts',(-6.74172778477872,0.613184940732107,
-56.3316944335526));
#33983=CARTESIAN_POINT('Ctrl Pts',(-6.75348015835505,0.427545027692543,
-56.322944719597));
#33984=CARTESIAN_POINT('Ctrl Pts',(-6.76249038365215,0.285219953548515,
-56.3162365517946));
#33985=CARTESIAN_POINT('Ctrl Pts',(-6.76699999999998,0.142609995758698,
-56.3095283839923));
#33986=CARTESIAN_POINT('Ctrl Pts',(-6.767,1.01112582279511E-12,-56.30282021619));
#33987=CARTESIAN_POINT('',(-6.76699856490775,0.00440710069189511,-56.6971797838425));
#33988=CARTESIAN_POINT('Ctrl Pts',(3.09908550384721,6.01564277861012,-57.3484848024));
#33989=CARTESIAN_POINT('Ctrl Pts',(2.94333909626799,6.09587883180818,-57.3402711974745));
#33990=CARTESIAN_POINT('Ctrl Pts',(2.78440536102775,6.170098280044,-57.3320575925491));
#33991=CARTESIAN_POINT('Ctrl Pts',(2.62278972093599,6.23804962145642,-57.3238439876236));
#33992=CARTESIAN_POINT('Ctrl Pts',(2.47306012011007,6.30100347431057,-57.3162344531372));
#33993=CARTESIAN_POINT('Ctrl Pts',(2.32102905734274,6.35857765802904,-57.3086249186507));
#33994=CARTESIAN_POINT('Ctrl Pts',(2.167115085328,6.41060848960096,-57.3010153841643));
#33995=CARTESIAN_POINT('Ctrl Pts',(1.98797087251385,6.47116843904546,-57.2921584620303));
#33996=CARTESIAN_POINT('Ctrl Pts',(1.8064616568237,6.52415593640569,-57.2833015398964));
#33997=CARTESIAN_POINT('Ctrl Pts',(1.62322537182426,6.56943135988694,-57.2744446177625));
#33998=CARTESIAN_POINT('Ctrl Pts',(1.43964794173174,6.61479107610835,-57.265571206015));
#33999=CARTESIAN_POINT('Ctrl Pts',(1.25433726871447,6.65240996260301,-57.2566977942675));
#34000=CARTESIAN_POINT('Ctrl Pts',(1.06794020261944,6.68219969198985,-57.24782438252));
#34001=CARTESIAN_POINT('Ctrl Pts',(0.881015653119109,6.71207372306785,-57.2389258599833));
#34002=CARTESIAN_POINT('Ctrl Pts',(0.692998816427942,6.73407421991262,-57.2300273374466));
#34003=CARTESIAN_POINT('Ctrl Pts',(0.504543460320005,6.74816455761478,-57.2211288149098));
#34004=CARTESIAN_POINT('Ctrl Pts',(0.315833885501937,6.76227390261687,-57.2122182886234));
#34005=CARTESIAN_POINT('Ctrl Pts',(0.126684869057916,6.76845176086734,-57.203307762337));
#34006=CARTESIAN_POINT('Ctrl Pts',(-0.062249707707935,6.76671367606834,
-57.1943972360506));
#34007=CARTESIAN_POINT('Ctrl Pts',(-0.251600724309423,6.76497176027259,
-57.1854670696423));
#34008=CARTESIAN_POINT('Ctrl Pts',(-0.440736095090732,6.75527900524688,
-57.1765369032341));
#34009=CARTESIAN_POINT('Ctrl Pts',(-0.629004072485149,6.73770308612639,
-57.1676067368259));
#34010=CARTESIAN_POINT('Ctrl Pts',(-0.807185279317851,6.72106882615598,
-57.1591550189615));
#34011=CARTESIAN_POINT('Ctrl Pts',(-0.984589419232587,6.69737393988361,
-57.1507033010971));
#34012=CARTESIAN_POINT('Ctrl Pts',(-1.16067243003436,6.66671797139778,-57.1422515832327));
#34013=CARTESIAN_POINT('Ctrl Pts',(-1.33201456931112,6.63688738639106,-57.1340274200221));
#34014=CARTESIAN_POINT('Ctrl Pts',(-1.50243299280958,6.60040750138087,-57.1258032568115));
#34015=CARTESIAN_POINT('Ctrl Pts',(-1.67137344457976,6.55734700993882,-57.1175790936009));
#34016=CARTESIAN_POINT('Ctrl Pts',(-1.84013553582849,6.5143319800285,-57.1093636131304));
#34017=CARTESIAN_POINT('Ctrl Pts',(-2.0074224180065,6.46475026641791,-57.10114813266));
#34018=CARTESIAN_POINT('Ctrl Pts',(-2.17268766443286,6.40872197187718,-57.0929326521895));
#34019=CARTESIAN_POINT('Ctrl Pts',(-2.33781157417631,6.35274159335915,-57.0847241976896));
#34020=CARTESIAN_POINT('Ctrl Pts',(-2.50091695382658,6.29032572847284,-57.0765157431897));
#34021=CARTESIAN_POINT('Ctrl Pts',(-2.66147014843813,6.22164493112334,-57.0683072886898));
#34022=CARTESIAN_POINT('Ctrl Pts',(-2.82191822571081,6.15300910044465,-57.0601042084267));
#34023=CARTESIAN_POINT('Ctrl Pts',(-2.97981711783748,6.07811664814091,-57.0519011281637));
#34024=CARTESIAN_POINT('Ctrl Pts',(-3.13465076611339,5.99718713852626,-57.0436980479006));
#34025=CARTESIAN_POINT('Ctrl Pts',(-3.28941407823135,5.91629439269541,-57.0354986940443));
#34026=CARTESIAN_POINT('Ctrl Pts',(-3.44111460348834,5.82937021899216,-57.027299340188));
#34027=CARTESIAN_POINT('Ctrl Pts',(-3.58925853872999,5.73668128295044,-57.0190999863316));
#34028=CARTESIAN_POINT('Ctrl Pts',(-3.73738963002714,5.6440003829552,-57.0109013433518));
#34029=CARTESIAN_POINT('Ctrl Pts',(-3.88196443722821,5.54555589895962,-57.002702700372));
#34030=CARTESIAN_POINT('Ctrl Pts',(-4.02251562939745,5.441659398681,-56.9945040573922));
#34031=CARTESIAN_POINT('Ctrl Pts',(-4.16306544503295,5.33776391594649,-56.9863054947085));
#34032=CARTESIAN_POINT('Ctrl Pts',(-4.29959143506934,5.22841673564294,-56.9781069320248));
#34033=CARTESIAN_POINT('Ctrl Pts',(-4.43165713198777,5.1139714571458,-56.969908369341));
#34034=CARTESIAN_POINT('Ctrl Pts',(-4.56374552258772,4.99950651279475,-56.9617083978466));
#34035=CARTESIAN_POINT('Ctrl Pts',(-4.69137182202745,4.8799419598243,-56.9535084263521));
#34036=CARTESIAN_POINT('Ctrl Pts',(-4.81413436184852,4.75567023100524,-56.9453084548577));
#34037=CARTESIAN_POINT('Ctrl Pts',(-4.93694029433773,4.63135457606753,-56.9371055849331));
#34038=CARTESIAN_POINT('Ctrl Pts',(-5.05487879064621,4.50232868589586,-56.9289027150085));
#34039=CARTESIAN_POINT('Ctrl Pts',(-5.16758657796395,4.36902025164073,-56.920699845084));
#34040=CARTESIAN_POINT('Ctrl Pts',(-5.28042237586932,4.23556040911639,-56.912487658552));
#34041=CARTESIAN_POINT('Ctrl Pts',(-5.38801536420717,4.09780857935904,-56.9042754720201));
#34042=CARTESIAN_POINT('Ctrl Pts',(-5.49004332048786,3.95622463204084,-56.8960632854882));
#34043=CARTESIAN_POINT('Ctrl Pts',(-5.59213145950119,3.81455716929061,-56.8878462548739));
#34044=CARTESIAN_POINT('Ctrl Pts',(-5.68864782508761,3.66905338152276,-56.8796292242596));
#34045=CARTESIAN_POINT('Ctrl Pts',(-5.77931483598359,3.52020014013124,-56.8714121936453));
#34046=CARTESIAN_POINT('Ctrl Pts',(-5.87012165340361,3.3711173703361,-56.8631824925517));
#34047=CARTESIAN_POINT('Ctrl Pts',(-5.95506091731349,3.21867513890646,-56.854952791458));
#34048=CARTESIAN_POINT('Ctrl Pts',(-6.03390151478836,3.06338399647102,-56.8467230903644));
#34049=CARTESIAN_POINT('Ctrl Pts',(-6.10415205719658,2.92501255667112,-56.8393900540328));
#34050=CARTESIAN_POINT('Ctrl Pts',(-6.16956110168431,2.78437964804174,-56.8320570177012));
#34051=CARTESIAN_POINT('Ctrl Pts',(-6.2299982336486,2.64185749213226,-56.8247239813697));
#34052=CARTESIAN_POINT('Ctrl Pts',(-6.30414378120452,2.46700830678371,-56.8157276578119));
#34053=CARTESIAN_POINT('Ctrl Pts',(-6.37101372039897,2.28882562406587,-56.8067313342542));
#34054=CARTESIAN_POINT('Ctrl Pts',(-6.43032076247517,2.1079050955109,-56.7977350106965));
#34055=CARTESIAN_POINT('Ctrl Pts',(-6.48936336453937,1.92779126081666,-56.7887788002152));
#34056=CARTESIAN_POINT('Ctrl Pts',(-6.54091023374025,1.74496415253537,-56.7798225897338));
#34057=CARTESIAN_POINT('Ctrl Pts',(-6.58472273487644,1.5600370203304,-56.7708663792525));
#34058=CARTESIAN_POINT('Ctrl Pts',(-6.62841626139362,1.37561206523308,-56.761934489723));
#34059=CARTESIAN_POINT('Ctrl Pts',(-6.66441723913493,1.18909868970128,-56.7530026001935));
#34060=CARTESIAN_POINT('Ctrl Pts',(-6.69253560599246,1.0011274456947,-56.744070710664));
#34061=CARTESIAN_POINT('Ctrl Pts',(-6.72053001562576,0.813984855562639,
-56.7351781965449));
#34062=CARTESIAN_POINT('Ctrl Pts',(-6.74071105790939,0.625397449691096,
-56.7262856824257));
#34063=CARTESIAN_POINT('Ctrl Pts',(-6.7529391756948,0.436006295099548,-56.7173931683065));
#34064=CARTESIAN_POINT('Ctrl Pts',(-6.76220433373509,0.292505961727163,
-56.7106553734852));
#34065=CARTESIAN_POINT('Ctrl Pts',(-6.76690469337939,0.148544605610245,
-56.7039175786638));
#34066=CARTESIAN_POINT('Ctrl Pts',(-6.76699856490775,0.00440710069191697,
-56.6971797838425));
#34067=CARTESIAN_POINT('Ctrl Pts',(-6.7669985649082,0.00440709999955857,
-56.6971797838101));
#34068=CARTESIAN_POINT('Ctrl Pts',(-6.76711176756178,-0.169412916424865,
-56.6890544620406));
#34069=CARTESIAN_POINT('Ctrl Pts',(-6.760523406653,-0.343245640998958,-56.6809291402712));
#34070=CARTESIAN_POINT('Ctrl Pts',(-6.74725724048585,-0.51653531409893,
-56.6728038185017));
#34071=CARTESIAN_POINT('Ctrl Pts',(-6.73398872311116,-0.689855699914266,
-56.664677056654));
#34072=CARTESIAN_POINT('Ctrl Pts',(-6.7140400698679,-0.862632479764062,
-56.6565502948063));
#34073=CARTESIAN_POINT('Ctrl Pts',(-6.68748697795196,-1.03431471019365,
-56.6484235329585));
#34074=CARTESIAN_POINT('Ctrl Pts',(-6.66092419577455,-1.20605959418192,
-56.6402938053376));
#34075=CARTESIAN_POINT('Ctrl Pts',(-6.62775222944934,-1.37670877380828,
-56.6321640777167));
#34076=CARTESIAN_POINT('Ctrl Pts',(-6.58809797633348,-1.54572120844306,
-56.6240343500958));
#34077=CARTESIAN_POINT('Ctrl Pts',(-6.54842180790742,-1.71482704945025,
-56.6159001295016));
#34078=CARTESIAN_POINT('Ctrl Pts',(-6.50225629983729,-1.88229399027416,
-56.6077659089073));
#34079=CARTESIAN_POINT('Ctrl Pts',(-6.44977830005002,-2.04759587814683,
-56.5996316883131));
#34080=CARTESIAN_POINT('Ctrl Pts',(-6.39722493119822,-2.21313517309873,
-56.5914857853262));
#34081=CARTESIAN_POINT('Ctrl Pts',(-6.33834107144428,-2.37650285742089,
-56.5833398823394));
#34082=CARTESIAN_POINT('Ctrl Pts',(-6.27335225792795,-2.53719144881703,
-56.5751939793525));
#34083=CARTESIAN_POINT('Ctrl Pts',(-6.20831329348684,-2.69800404126851,
-56.5670417902905));
#34084=CARTESIAN_POINT('Ctrl Pts',(-6.13716013734437,-2.85613309152384,
-56.5588896012284));
#34085=CARTESIAN_POINT('Ctrl Pts',(-6.06016429834327,-3.01109576019855,
-56.5507374121664));
#34086=CARTESIAN_POINT('Ctrl Pts',(-5.9830309230542,-3.16633523591242,-56.542570660995));
#34087=CARTESIAN_POINT('Ctrl Pts',(-5.90003418832372,-3.31839671261976,
-56.5344039098237));
#34088=CARTESIAN_POINT('Ctrl Pts',(-5.8114896335024,-3.46682523927788,-56.5262371586524));
#34089=CARTESIAN_POINT('Ctrl Pts',(-5.74267576135428,-3.58217893524706,
-56.5198902322705));
#34090=CARTESIAN_POINT('Ctrl Pts',(-5.67051196301427,-3.69533894750056,
-56.5135433058886));
#34091=CARTESIAN_POINT('Ctrl Pts',(-5.59516271184839,-3.80610604528321,
-56.5071963795066));
#34092=CARTESIAN_POINT('Ctrl Pts',(-5.49622606261029,-3.95154777603536,
-56.4988626055212));
#34093=CARTESIAN_POINT('Ctrl Pts',(-5.39148830522668,-4.09331550672587,
-56.4905288315358));
#34094=CARTESIAN_POINT('Ctrl Pts',(-5.28124753162088,-4.23092348190657,
-56.4821950575504));
#34095=CARTESIAN_POINT('Ctrl Pts',(-5.17113670044219,-4.36836925653569,
-56.4738711067074));
#34096=CARTESIAN_POINT('Ctrl Pts',(-5.05553599034082,-4.50166477403508,
-56.4655471558644));
#34097=CARTESIAN_POINT('Ctrl Pts',(-4.93478703369493,-4.63035267901662,
-56.4572232050214));
#34098=CARTESIAN_POINT('Ctrl Pts',(-4.8141582648331,-4.7589124941615,-56.4489075394442));
#34099=CARTESIAN_POINT('Ctrl Pts',(-4.68839169532107,-4.882873581931,-56.440591873867));
#34100=CARTESIAN_POINT('Ctrl Pts',(-4.55786966514336,-5.00181098359044,
-56.4322762082899));
#34101=CARTESIAN_POINT('Ctrl Pts',(-4.42745363360745,-5.12065179463588,
-56.4239672959731));
#34102=CARTESIAN_POINT('Ctrl Pts',(-4.29229009275337,-5.23447681567917,
-56.4156583836563));
#34103=CARTESIAN_POINT('Ctrl Pts',(-4.15279888755748,-5.34289719155267,
-56.4073494713396));
#34104=CARTESIAN_POINT('Ctrl Pts',(-4.01339541871077,-5.45124937382253,
-56.3990457851131));
#34105=CARTESIAN_POINT('Ctrl Pts',(-3.86966998402319,-5.55420347266158,
-56.3907420988866));
#34106=CARTESIAN_POINT('Ctrl Pts',(-3.72207639083078,-5.65141011967988,
-56.3824384126601));
#34107=CARTESIAN_POINT('Ctrl Pts',(-3.57454272183674,-5.74857730000946,
-56.3741380977978));
#34108=CARTESIAN_POINT('Ctrl Pts',(-3.42314431371191,-5.84000148720765,
-56.3658377829354));
#34109=CARTESIAN_POINT('Ctrl Pts',(-3.26836514484309,-5.9253757923,-56.357537468073));
#34110=CARTESIAN_POINT('Ctrl Pts',(-3.11361861699007,-6.01073209300544,
-56.3492389036445));
#34111=CARTESIAN_POINT('Ctrl Pts',(-2.95549305315079,-6.09004088551378,
-56.3409403392161));
#34112=CARTESIAN_POINT('Ctrl Pts',(-2.79449850700662,-6.16304040992251,
-56.3326417747876));
#34113=CARTESIAN_POINT('Ctrl Pts',(-2.63351118738645,-6.23603665761889,
-56.3243435828548));
#34114=CARTESIAN_POINT('Ctrl Pts',(-2.46965545889241,-6.30272405811027,
-56.3160453909221));
#34115=CARTESIAN_POINT('Ctrl Pts',(-2.30346307484728,-6.36288824849338,
-56.3077471989893));
#34116=CARTESIAN_POINT('Ctrl Pts',(-2.13725056377429,-6.42305972516907,
-56.2994480020891));
#34117=CARTESIAN_POINT('Ctrl Pts',(-1.96870116047762,-6.4767062997432,-56.2911488051888));
#34118=CARTESIAN_POINT('Ctrl Pts',(-1.79836374314003,-6.52366283979785,
-56.2828496082886));
#34119=CARTESIAN_POINT('Ctrl Pts',(-1.62790670984997,-6.57065235411824,
-56.2745445834478));
#34120=CARTESIAN_POINT('Ctrl Pts',(-1.45565948931181,-6.61094235407167,
-56.266239558607));
#34121=CARTESIAN_POINT('Ctrl Pts',(-1.28218405512426,-6.64441818737993,
-56.2579345337662));
#34122=CARTESIAN_POINT('Ctrl Pts',(-1.10864535746443,-6.67790622874208,
-56.2496264802274));
#34123=CARTESIAN_POINT('Ctrl Pts',(-0.933877896255326,-6.70457509187546,
-56.2413184266885));
#34124=CARTESIAN_POINT('Ctrl Pts',(-0.758451057576164,-6.72436175359875,
-56.2330103731497));
#34125=CARTESIAN_POINT('Ctrl Pts',(-0.582837719315061,-6.74416945089542,
-56.2246934871624));
#34126=CARTESIAN_POINT('Ctrl Pts',(-0.406563949608596,-6.75708029673793,
-56.2163766011751));
#34127=CARTESIAN_POINT('Ctrl Pts',(-0.230202543461308,-6.76308330489755,
-56.2080597151878));
#34128=CARTESIAN_POINT('Ctrl Pts',(-0.100207911230814,-6.76750807591199,
-56.201929402673));
#34129=CARTESIAN_POINT('Ctrl Pts',(0.0298342774740913,-6.76818087208289,
-56.1957990901583));
#34130=CARTESIAN_POINT('Ctrl Pts',(0.159695758183085,-6.76511539183319,
-56.1896687776436));
#34131=CARTESIAN_POINT('Ctrl Pts',(0.338719994825503,-6.76088938687276,
-56.1812176610204));
#34132=CARTESIAN_POINT('Ctrl Pts',(0.51772782472298,-6.74954924328847,-56.1727665443972));
#34133=CARTESIAN_POINT('Ctrl Pts',(0.696130930947859,-6.73109877560697,
-56.164315427774));
#34134=CARTESIAN_POINT('Ctrl Pts',(0.874376954411912,-6.71266455344083,
-56.1558717523034));
#34135=CARTESIAN_POINT('Ctrl Pts',(1.05201898730338,-6.68713251967139,-56.1474280768328));
#34136=CARTESIAN_POINT('Ctrl Pts',(1.22847073063158,-6.6545584875318,-56.1389844013622));
#34137=CARTESIAN_POINT('Ctrl Pts',(1.40479109173087,-6.62200870932627,-56.1305470128734));
#34138=CARTESIAN_POINT('Ctrl Pts',(1.57992260509171,-6.5824274450482,-56.1221096243846));
#34139=CARTESIAN_POINT('Ctrl Pts',(1.75328570422906,-6.5359221414691,-56.1136722358958));
#34140=CARTESIAN_POINT('Ctrl Pts',(1.92652510020139,-6.48945002172942,-56.1052408679019));
#34141=CARTESIAN_POINT('Ctrl Pts',(2.09799827954512,-6.43606380331171,-56.0968094999081));
#34142=CARTESIAN_POINT('Ctrl Pts',(2.26713724714957,-6.37592171396317,-56.0883781319142));
#34143=CARTESIAN_POINT('Ctrl Pts',(2.43620370120311,-6.31580540883526,-56.0799503786311));
#34144=CARTESIAN_POINT('Ctrl Pts',(2.60293762676839,-6.24893911770795,-56.0715226253479));
#34145=CARTESIAN_POINT('Ctrl Pts',(2.76678690873883,-6.17553068178205,-56.0630948720647));
#34146=CARTESIAN_POINT('Ctrl Pts',(2.93058572378656,-6.10214485625649,-56.0546697145987));
#34147=CARTESIAN_POINT('Ctrl Pts',(3.09150136497608,-6.02222103979339,-56.0462445571326));
#34148=CARTESIAN_POINT('Ctrl Pts',(3.24900205829669,-5.93601504590276,-56.0378193996666));
#34149=CARTESIAN_POINT('Ctrl Pts',(3.29208835128823,-5.91243231345828,-56.0355145920151));
#34150=CARTESIAN_POINT('Ctrl Pts',(3.33491921080571,-5.88837971668314,-56.0332097843636));
#34151=CARTESIAN_POINT('Ctrl Pts',(3.37748405502412,-5.86386310021455,-56.0309049767121));
#34152=CARTESIAN_POINT('Ctrl Pts',(3.53665745527955,-5.7721819657544,-56.0222860312523));
#34153=CARTESIAN_POINT('Ctrl Pts',(3.69203774818405,-5.67404935571939,-56.0136670857925));
#34154=CARTESIAN_POINT('Ctrl Pts',(3.84311305874793,-5.56980888520254,-56.0050481403327));
#34155=CARTESIAN_POINT('Ctrl Pts',(3.99427886399721,-5.46550597424754,-55.9964240320917));
#34156=CARTESIAN_POINT('Ctrl Pts',(4.14113429025835,-5.35508807403767,-55.9877999238508));
#34157=CARTESIAN_POINT('Ctrl Pts',(4.28319857888049,-5.23894063087912,-55.9791758156099));
#34158=CARTESIAN_POINT('Ctrl Pts',(4.43012971213035,-5.11881420352095,-55.9702562622908));
#34159=CARTESIAN_POINT('Ctrl Pts',(4.57193535247314,-4.99255894827847,-55.9613367089717));
#34160=CARTESIAN_POINT('Ctrl Pts',(4.70812351663489,-4.86064419106249,-55.9524171556526));
#34161=CARTESIAN_POINT('Ctrl Pts',(4.84004596352177,-4.73286129847755,-55.943776982652));
#34162=CARTESIAN_POINT('Ctrl Pts',(4.96669733450544,-4.59976832619409,-55.9351368096513));
#34163=CARTESIAN_POINT('Ctrl Pts',(5.0876699251174,-4.46182739839362,-55.9264966366507));
#34164=CARTESIAN_POINT('Ctrl Pts',(5.2145099956208,-4.31719598297125,-55.9174373931724));
#34165=CARTESIAN_POINT('Ctrl Pts',(5.33510647330544,-4.16723494342464,-55.908378149694));
#34166=CARTESIAN_POINT('Ctrl Pts',(5.4490386102138,-4.01251382856175,-55.8993189062157));
#34167=CARTESIAN_POINT('Ctrl Pts',(5.56297074712216,-3.85779271369887,-55.8902596627373));
#34168=CARTESIAN_POINT('Ctrl Pts',(5.67023835718177,-3.69831185952653,-55.881200419259));
#34169=CARTESIAN_POINT('Ctrl Pts',(5.77047404941831,-3.5346737112483,-55.8721411757806));
#34170=CARTESIAN_POINT('Ctrl Pts',(5.8705354600804,-3.37132008351845,-55.8630976837694));
#34171=CARTESIAN_POINT('Ctrl Pts',(5.96368229599236,-3.20367354758897,-55.8540541917582));
#34172=CARTESIAN_POINT('Ctrl Pts',(6.04957529512622,-3.03231392645922,-55.8450106997471));
#34173=CARTESIAN_POINT('Ctrl Pts',(6.13538972613476,-2.86111105156402,-55.8359754800075));
#34174=CARTESIAN_POINT('Ctrl Pts',(6.2139634610426,-2.68620208513048,-55.8269402602678));
#34175=CARTESIAN_POINT('Ctrl Pts',(6.28500326369497,-2.50819117599588,-55.8179050405282));
#34176=CARTESIAN_POINT('Ctrl Pts',(6.35591790733133,-2.33049388921657,-55.8088857391776));
#34177=CARTESIAN_POINT('Ctrl Pts',(6.41932503590296,-2.14970579360339,-55.799866437827));
#34178=CARTESIAN_POINT('Ctrl Pts',(6.47497962988298,-1.96645055686649,-55.7908471364763));
#34179=CARTESIAN_POINT('Ctrl Pts',(6.53056440038258,-1.78342522960366,-55.7818391506159));
#34180=CARTESIAN_POINT('Ctrl Pts',(6.5784159775054,-1.59793916539026,-55.7728311647554));
#34181=CARTESIAN_POINT('Ctrl Pts',(6.6183383989632,-1.41063313331614,-55.763823178895));
#34182=CARTESIAN_POINT('Ctrl Pts',(6.65817065333218,-1.22375014270622,-55.7548355380895));
#34183=CARTESIAN_POINT('Ctrl Pts',(6.69010944941164,-1.03505562160223,-55.7458478972841));
#34184=CARTESIAN_POINT('Ctrl Pts',(6.7140094194478,-0.845202056058933,-55.7368602564786));
#34185=CARTESIAN_POINT('Ctrl Pts',(6.73482467673501,-0.679852442327279,
-55.7290326292688));
#34186=CARTESIAN_POINT('Ctrl Pts',(6.74954301569771,-0.513624002901764,
-55.7212050020589));
#34187=CARTESIAN_POINT('Ctrl Pts',(6.75809963956551,-0.346955705680907,
-55.713377374849));
#34188=CARTESIAN_POINT('Ctrl Pts',(6.76697932707497,-0.173994685082054,
-55.7052542079741));
#34189=CARTESIAN_POINT('Ctrl Pts',(6.76921759228954,-0.00063720007779014,
-55.6971310410991));
#34190=CARTESIAN_POINT('Ctrl Pts',(6.76479937800053,0.172564119687984,-55.6890078742242));
#34191=CARTESIAN_POINT('Ctrl Pts',(6.76038147514405,0.345753230782343,-55.6808852799377));
#34192=CARTESIAN_POINT('Ctrl Pts',(6.74930803672678,0.518785832660119,-55.6727626856512));
#34193=CARTESIAN_POINT('Ctrl Pts',(6.73161612080699,0.69111026767913,-55.6646400913647));
#34194=CARTESIAN_POINT('Ctrl Pts',(6.71392207873954,0.863455411998051,-55.6565165209355));
#34195=CARTESIAN_POINT('Ctrl Pts',(6.68960801394717,1.03509185601515,-55.6483929505063));
#34196=CARTESIAN_POINT('Ctrl Pts',(6.6587627423749,1.20547407303511,-55.6402693800771));
#34197=CARTESIAN_POINT('Ctrl Pts',(6.62789500306871,1.37598039667254,-55.6321398924292));
#34198=CARTESIAN_POINT('Ctrl Pts',(6.59048662059584,1.54523030811715,-55.6240104047812));
#34199=CARTESIAN_POINT('Ctrl Pts',(6.54667747308637,1.71268884021105,-55.6158809171333));
#34200=CARTESIAN_POINT('Ctrl Pts',(6.5028504648281,1.88021564422865,-55.6077481151379));
#34201=CARTESIAN_POINT('Ctrl Pts',(6.45261759600558,2.0459492630818,-55.5996153131425));
#34202=CARTESIAN_POINT('Ctrl Pts',(6.39616825237131,2.20937110675353,-55.5914825111471));
#34203=CARTESIAN_POINT('Ctrl Pts',(6.33965752792579,2.3729706489545,-55.5833408658605));
#34204=CARTESIAN_POINT('Ctrl Pts',(6.27691696022806,2.53425305454727,-55.5751992205739));
#34205=CARTESIAN_POINT('Ctrl Pts',(6.20818387171808,2.69272018875699,-55.5670575752873));
#34206=CARTESIAN_POINT('Ctrl Pts',(6.17316577985995,2.77345592728628,-55.5629095748307));
#34207=CARTESIAN_POINT('Ctrl Pts',(6.13659295702548,2.85346129374103,-55.5587615743741));
#34208=CARTESIAN_POINT('Ctrl Pts',(6.09850128228009,2.93267303155809,-55.5546135739175));
#34209=CARTESIAN_POINT('Ctrl Pts',(6.01971100139163,3.09651762789013,-55.5460336906941));
#34210=CARTESIAN_POINT('Ctrl Pts',(5.93425450913703,3.25730806693052,-55.5374538074706));
#34211=CARTESIAN_POINT('Ctrl Pts',(5.84239419721187,3.4144866443413,-55.5288739242472));
#34212=CARTESIAN_POINT('Ctrl Pts',(5.75209760226665,3.56898960694923,-55.5204400944041));
#34213=CARTESIAN_POINT('Ctrl Pts',(5.6556136276282,3.72000238227505,-55.5120062645611));
#34214=CARTESIAN_POINT('Ctrl Pts',(5.55323872585679,3.86701805706212,-55.5035724347181));
#34215=CARTESIAN_POINT('Ctrl Pts',(5.45092220118252,4.01394989930645,-55.495143414086));
#34216=CARTESIAN_POINT('Ctrl Pts',(5.34272163532201,4.15688891143084,-55.486714393454));
#34217=CARTESIAN_POINT('Ctrl Pts',(5.22897745193762,4.29535607454469,-55.478285372822));
#34218=CARTESIAN_POINT('Ctrl Pts',(5.11528224480755,4.43376361612192,-55.4698599815787));
#34219=CARTESIAN_POINT('Ctrl Pts',(4.99604839027207,4.56770289028908,-55.4614345903354));
#34220=CARTESIAN_POINT('Ctrl Pts',(4.8716575757501,4.69672667553017,-55.4530091990921));
#34221=CARTESIAN_POINT('Ctrl Pts',(4.74331974761238,4.82984448201438,-55.4443164638807));
#34222=CARTESIAN_POINT('Ctrl Pts',(4.60949252562073,4.95772942708577,-55.4356237286692));
#34223=CARTESIAN_POINT('Ctrl Pts',(4.47063809897705,5.07992952588664,-55.4269309934578));
#34224=CARTESIAN_POINT('Ctrl Pts',(4.33610052849683,5.19833053622895,-55.4185085073733));
#34225=CARTESIAN_POINT('Ctrl Pts',(4.19684392465754,5.31139465328017,-55.4100860212888));
#34226=CARTESIAN_POINT('Ctrl Pts',(4.0533241961618,5.41875003675288,-55.4016635352044));
#34227=CARTESIAN_POINT('Ctrl Pts',(3.90289687275794,5.53127242763291,-55.3928356754295));
#34228=CARTESIAN_POINT('Ctrl Pts',(3.74778621850906,5.63752272742884,-55.3840078156545));
#34229=CARTESIAN_POINT('Ctrl Pts',(3.58855372598737,5.73712220156606,-55.3751799558796));
#34230=CARTESIAN_POINT('Ctrl Pts',(3.42932123346567,5.83672167570329,-55.3663520961047));
#34231=CARTESIAN_POINT('Ctrl Pts',(3.26596726665884,5.92967011184458,-55.3575242363298));
#34232=CARTESIAN_POINT('Ctrl Pts',(3.09908550384722,6.01564277861012,-55.3486963765549));
#34233=CARTESIAN_POINT('Origin',(0.,0.,-63.6971797838103));
#34234=CARTESIAN_POINT('',(3.09908550384721,6.01564277861012,-52.953975806663));
#34235=CARTESIAN_POINT('',(3.0990855038472,6.01564277861013,-53.3487566918479));
#34236=CARTESIAN_POINT('',(3.09908550384721,6.01564277861012,-63.6971797838103));
#34237=CARTESIAN_POINT('',(-6.76699999907272,0.000112025758056779,-54.3028202161463));
#34238=CARTESIAN_POINT('Ctrl Pts',(-6.76699999907272,0.000112025758070302,
-54.3028202161463));
#34239=CARTESIAN_POINT('Ctrl Pts',(-6.76700315016816,-0.190232259186009,
-54.2938337921293));
#34240=CARTESIAN_POINT('Ctrl Pts',(-6.75897086966551,-0.380644028120085,
-54.2848473681123));
#34241=CARTESIAN_POINT('Ctrl Pts',(-6.74291213548057,-0.570460281867895,
-54.2758609440953));
#34242=CARTESIAN_POINT('Ctrl Pts',(-6.72686977671977,-0.760082976047031,
-54.2668836837212));
#34243=CARTESIAN_POINT('Ctrl Pts',(-6.70281732287362,-0.949111119762301,
-54.257906423347));
#34244=CARTESIAN_POINT('Ctrl Pts',(-6.67081572306745,-1.1368845978709,-54.2489291629729));
#34245=CARTESIAN_POINT('Ctrl Pts',(-6.6388707111414,-1.32432603935843,-54.2399677769343));
#34246=CARTESIAN_POINT('Ctrl Pts',(-6.59900466007583,-1.5105170002127,-54.2310063908957));
#34247=CARTESIAN_POINT('Ctrl Pts',(-6.5513299045297,-1.69480544075564,-54.2220450048571));
#34248=CARTESIAN_POINT('Ctrl Pts',(-6.5037136720446,-1.87886765835247,-54.213094619352));
#34249=CARTESIAN_POINT('Ctrl Pts',(-6.44830792390815,-2.06103177573666,
-54.2041442338468));
#34250=CARTESIAN_POINT('Ctrl Pts',(-6.38527585279149,-2.24065644036695,
-54.1951938483417));
#34251=CARTESIAN_POINT('Ctrl Pts',(-6.3223714695473,-2.41991722846802,-54.1862615941729));
#34252=CARTESIAN_POINT('Ctrl Pts',(-6.25187168159047,-2.59664859765189,
-54.1773293400041));
#34253=CARTESIAN_POINT('Ctrl Pts',(-6.1739891715736,-2.77022502863792,-54.1683970858353));
#34254=CARTESIAN_POINT('Ctrl Pts',(-6.12392845320755,-2.88179514655903,
-54.1626556804771));
#34255=CARTESIAN_POINT('Ctrl Pts',(-6.0708185362946,-2.99206203359894,-54.1569142751189));
#34256=CARTESIAN_POINT('Ctrl Pts',(-6.01472678269943,-3.10086290078716,
-54.1511728697608));
#34257=CARTESIAN_POINT('Ctrl Pts',(-5.93536603808171,-3.25479850239856,
-54.1430497112718));
#34258=CARTESIAN_POINT('Ctrl Pts',(-5.85006649384746,-3.40573474770476,
-54.1349265527829));
#34259=CARTESIAN_POINT('Ctrl Pts',(-5.75909322121416,-3.55318649515687,
-54.126803394294));
#34260=CARTESIAN_POINT('Ctrl Pts',(-5.66812636266667,-3.70062784649884,
-54.1186808085297));
#34261=CARTESIAN_POINT('Ctrl Pts',(-5.57148676472573,-3.8445848778403,-54.1105582227654));
#34262=CARTESIAN_POINT('Ctrl Pts',(-5.46948404592724,-3.98459951203974,
-54.1024356370011));
#34263=CARTESIAN_POINT('Ctrl Pts',(-5.3674690704458,-4.12463097044742,-54.094312075224));
#34264=CARTESIAN_POINT('Ctrl Pts',(-5.26008990737592,-4.26071879329549,
-54.086188513447));
#34265=CARTESIAN_POINT('Ctrl Pts',(-5.14769781774396,-4.39243624622988,
-54.0780649516699));
#34266=CARTESIAN_POINT('Ctrl Pts',(-5.03522386380352,-4.5242496397081,-54.0699354728414));
#34267=CARTESIAN_POINT('Ctrl Pts',(-4.91772992847697,-4.65168602667329,
-54.061805994013));
#34268=CARTESIAN_POINT('Ctrl Pts',(-4.79560608559244,-4.77435349255046,
-54.0536765151845));
#34269=CARTESIAN_POINT('Ctrl Pts',(-4.6734324549609,-4.89707096780019,-54.0455437221103));
#34270=CARTESIAN_POINT('Ctrl Pts',(-4.54662542218313,-5.01501539747717,
-54.037410929036));
#34271=CARTESIAN_POINT('Ctrl Pts',(-4.41560960305938,-5.12783393192192,
-54.0292781359618));
#34272=CARTESIAN_POINT('Ctrl Pts',(-4.28445132410331,-5.24077513941186,
-54.0211364997085));
#34273=CARTESIAN_POINT('Ctrl Pts',(-4.14907540421544,-5.3485790916189,-54.0129948634553));
#34274=CARTESIAN_POINT('Ctrl Pts',(-4.00993759149697,-5.45093473748306,
-54.004853227202));
#34275=CARTESIAN_POINT('Ctrl Pts',(-3.93904877082046,-5.50308354507984,
-54.0007051744111));
#34276=CARTESIAN_POINT('Ctrl Pts',(-3.86718389971976,-5.55381880843328,
-53.9965571216202));
#34277=CARTESIAN_POINT('Ctrl Pts',(-3.79440581706842,-5.6031039161698,-53.9924090688293));
#34278=CARTESIAN_POINT('Ctrl Pts',(-3.64631246278333,-5.70339230870645,
-53.9839683538615));
#34279=CARTESIAN_POINT('Ctrl Pts',(-3.49413123723308,-5.79787991970299,
-53.9755276388938));
#34280=CARTESIAN_POINT('Ctrl Pts',(-3.33834498347224,-5.88623324132894,
-53.967086923926));
#34281=CARTESIAN_POINT('Ctrl Pts',(-3.18267648030597,-5.97451978134929,
-53.9586525888486));
#34282=CARTESIAN_POINT('Ctrl Pts',(-3.0234086697346,-6.056681110859,-53.9502182537711));
#34283=CARTESIAN_POINT('Ctrl Pts',(-2.86105246267856,-6.13242756221392,
-53.9417839186936));
#34284=CARTESIAN_POINT('Ctrl Pts',(-2.69879404044821,-6.20812839256256,
-53.9333546634958));
#34285=CARTESIAN_POINT('Ctrl Pts',(-2.5334512315112,-6.27742190678962,-53.9249254082979));
#34286=CARTESIAN_POINT('Ctrl Pts',(-2.36555893444202,-6.34006466273662,
-53.9164961531));
#34287=CARTESIAN_POINT('Ctrl Pts',(-2.19774200309267,-6.40267929877295,
-53.908070681738));
#34288=CARTESIAN_POINT('Ctrl Pts',(-2.02737817738107,-6.45864901290426,
-53.8996452103759));
#34289=CARTESIAN_POINT('Ctrl Pts',(-1.85502206103716,-6.50777858820239,
-53.8912197390139));
#34290=CARTESIAN_POINT('Ctrl Pts',(-1.68271689816403,-6.55689363937203,
-53.8827967584657));
#34291=CARTESIAN_POINT('Ctrl Pts',(-1.50842093951769,-6.5991724930234,-53.8743737779176));
#34292=CARTESIAN_POINT('Ctrl Pts',(-1.33270404571539,-6.63446975473804,
-53.8659507973694));
#34293=CARTESIAN_POINT('Ctrl Pts',(-1.15698424240966,-6.66976760090135,
-53.8575276773543));
#34294=CARTESIAN_POINT('Ctrl Pts',(-0.979843782440087,-6.69808355203235,
-53.8491045573393));
#34295=CARTESIAN_POINT('Ctrl Pts',(-0.801863484820748,-6.71932317660872,
-53.8406814373242));
#34296=CARTESIAN_POINT('Ctrl Pts',(-0.623877032347734,-6.74056353568651,
-53.8322580260237));
#34297=CARTESIAN_POINT('Ctrl Pts',(-0.445051015453118,-6.75472704060123,
-53.8238346147232));
#34298=CARTESIAN_POINT('Ctrl Pts',(-0.265972313979574,-6.76177104967303,
-53.8154112034227));
#34299=CARTESIAN_POINT('Ctrl Pts',(-0.0868624445075006,-6.76881628472907,
-53.806986326058));
#34300=CARTESIAN_POINT('Ctrl Pts',(0.0924998639961541,-6.76873954039166,
-53.7985614486933));
#34301=CARTESIAN_POINT('Ctrl Pts',(0.27152641305435,-6.76155029612395,-53.7901365713286));
#34302=CARTESIAN_POINT('Ctrl Pts',(0.450609096630224,-6.75435879763885,
-53.7817090523086));
#34303=CARTESIAN_POINT('Ctrl Pts',(0.62935547777268,-6.74005036627477,-53.7732815332886));
#34304=CARTESIAN_POINT('Ctrl Pts',(0.807180791421248,-6.71868649141784,
-53.7648540142686));
#34305=CARTESIAN_POINT('Ctrl Pts',(0.985165571938591,-6.6973034582636,-53.7564189377753));
#34306=CARTESIAN_POINT('Ctrl Pts',(1.16222730311712,-6.66885237908188,-53.747983861282));
#34307=CARTESIAN_POINT('Ctrl Pts',(1.33778860880441,-6.63344636204689,-53.7395487847887));
#34308=CARTESIAN_POINT('Ctrl Pts',(1.5134347644261,-6.59802323305087,-53.7311096315674));
#34309=CARTESIAN_POINT('Ctrl Pts',(1.68757872324648,-6.5556385361644,-53.722670478346));
#34310=CARTESIAN_POINT('Ctrl Pts',(1.85965611955421,-6.5064558798938,-53.7142313251247));
#34311=CARTESIAN_POINT('Ctrl Pts',(2.0319247420978,-6.45721856790182,-53.705782793638));
#34312=CARTESIAN_POINT('Ctrl Pts',(2.20212189499794,-6.40116830115896,-53.6973342621512));
#34313=CARTESIAN_POINT('Ctrl Pts',(2.36969995644507,-6.33851805364821,-53.6888857306644));
#34314=CARTESIAN_POINT('Ctrl Pts',(2.46229227524887,-6.3039017581704,-53.684217642765));
#34315=CARTESIAN_POINT('Ctrl Pts',(2.55408536270464,-6.26727139338636,-53.6795495548656));
#34316=CARTESIAN_POINT('Ctrl Pts',(2.64498979819252,-6.22866903659662,-53.6748814669662));
#34317=CARTESIAN_POINT('Ctrl Pts',(2.8054672934996,-6.1605226420085,-53.6666406913654));
#34318=CARTESIAN_POINT('Ctrl Pts',(2.96353105095224,-6.08607630748875,-53.6583999157647));
#34319=CARTESIAN_POINT('Ctrl Pts',(3.11865367989214,-6.00552147818116,-53.6501591401639));
#34320=CARTESIAN_POINT('Ctrl Pts',(3.27360449370238,-5.92505587208063,-53.6419274921155));
#34321=CARTESIAN_POINT('Ctrl Pts',(3.42562035253868,-5.83849540570367,-53.6336958440672));
#34322=CARTESIAN_POINT('Ctrl Pts',(3.57419283431532,-5.74607993184302,-53.6254641960189));
#34323=CARTESIAN_POINT('Ctrl Pts',(3.72262723296485,-5.65375034883826,-53.6172401984566));
#34324=CARTESIAN_POINT('Ctrl Pts',(3.86762432766157,-5.55557678236179,-53.6090162008943));
#34325=CARTESIAN_POINT('Ctrl Pts',(4.00869927613141,-5.45184547777572,-53.6007922033321));
#34326=CARTESIAN_POINT('Ctrl Pts',(4.1496495843348,-5.34820582020128,-53.5925754717037));
#34327=CARTESIAN_POINT('Ctrl Pts',(4.28668436733827,-5.23901842118942,-53.5843587400753));
#34328=CARTESIAN_POINT('Ctrl Pts',(4.41934693165567,-5.1246133217703,-53.5761420084469));
#34329=CARTESIAN_POINT('Ctrl Pts',(4.55194152802915,-5.0102668363198,-53.5679294865544));
#34330=CARTESIAN_POINT('Ctrl Pts',(4.68016809823934,-4.89070820624697,-53.5597169646619));
#34331=CARTESIAN_POINT('Ctrl Pts',(4.80360194823375,-4.76630856354527,-53.5515044427694));
#34332=CARTESIAN_POINT('Ctrl Pts',(4.92699452135417,-4.64195052068328,-53.5432946671837));
#34333=CARTESIAN_POINT('Ctrl Pts',(5.04559731672299,-4.51275494242931,-53.5350848915981));
#34334=CARTESIAN_POINT('Ctrl Pts',(5.15902147030627,-4.37913078919995,-53.5268751160124));
#34335=CARTESIAN_POINT('Ctrl Pts',(5.20856219346421,-4.32076723105808,-53.5232892993532));
#34336=CARTESIAN_POINT('Ctrl Pts',(5.25711545816215,-4.26155929676581,-53.519703482694));
#34337=CARTESIAN_POINT('Ctrl Pts',(5.30465117116476,-4.20154316320329,-53.5161176660348));
#34338=CARTESIAN_POINT('Ctrl Pts',(5.42208758626565,-4.05327401715283,-53.5072589485134));
#34339=CARTESIAN_POINT('Ctrl Pts',(5.53318926672605,-3.90022376079815,-53.498400230992));
#34340=CARTESIAN_POINT('Ctrl Pts',(5.63760965823033,-3.74294621139926,-53.4895415134706));
#34341=CARTESIAN_POINT('Ctrl Pts',(5.74222540351655,-3.58537442096521,-53.4806662227115));
#34342=CARTESIAN_POINT('Ctrl Pts',(5.84013473676203,-3.42355974877974,-53.4717909319523));
#34343=CARTESIAN_POINT('Ctrl Pts',(5.93103639079377,-3.25808169496715,-53.4629156411932));
#34344=CARTESIAN_POINT('Ctrl Pts',(6.02219622596247,-3.09213364627349,-53.4540151426127));
#34345=CARTESIAN_POINT('Ctrl Pts',(6.10630842715907,-2.92250162334648,-53.4451146440322));
#34346=CARTESIAN_POINT('Ctrl Pts',(6.18311806884459,-2.74978907313408,-53.4362141454517));
#34347=CARTESIAN_POINT('Ctrl Pts',(6.26003168784538,-2.57684272171012,-53.4273015982543));
#34348=CARTESIAN_POINT('Ctrl Pts',(6.32962290111525,-2.400807752545,-53.4183890510568));
#34349=CARTESIAN_POINT('Ctrl Pts',(6.3916858602023,-2.22230530406827,-53.4094765038594));
#34350=CARTESIAN_POINT('Ctrl Pts',(6.45388586036458,-2.04340870475132,-53.4005442768873));
#34351=CARTESIAN_POINT('Ctrl Pts',(6.50852427183568,-1.86203397431315,-53.3916120499152));
#34352=CARTESIAN_POINT('Ctrl Pts',(6.55544504450166,-1.67881781873992,-53.3826798229431));
#34353=CARTESIAN_POINT('Ctrl Pts',(6.59979059289516,-1.5056573946505,-53.3742378369965));
#34354=CARTESIAN_POINT('Ctrl Pts',(6.63724280979381,-1.3308524048672,-53.3657958510498));
#34355=CARTESIAN_POINT('Ctrl Pts',(6.66771230148169,-1.154946606848,-53.3573538651031));
#34356=CARTESIAN_POINT('Ctrl Pts',(6.69739492849889,-0.983583518607065,
-53.3491298906862));
#34357=CARTESIAN_POINT('Ctrl Pts',(6.72050650524564,-0.810848222265133,
-53.3409059162692));
#34358=CARTESIAN_POINT('Ctrl Pts',(6.73692481753425,-0.63728565250693,-53.3326819418522));
#34359=CARTESIAN_POINT('Ctrl Pts',(6.75332579049209,-0.463906381662319,
-53.3244666527502));
#34360=CARTESIAN_POINT('Ctrl Pts',(6.76304754173078,-0.289701931241656,
-53.3162513636481));
#34361=CARTESIAN_POINT('Ctrl Pts',(6.76601889535557,-0.115227200310467,
-53.3080360745461));
#34362=CARTESIAN_POINT('Ctrl Pts',(6.76898770693284,0.0590982642884879,
-53.2998278137745));
#34363=CARTESIAN_POINT('Ctrl Pts',(6.76521761649876,0.23369319236014,-53.291619553003));
#34364=CARTESIAN_POINT('Ctrl Pts',(6.75468925113634,0.40799769678658,-53.2834112922314));
#34365=CARTESIAN_POINT('Ctrl Pts',(6.74416778181926,0.582188032325334,-53.2752084078442));
#34366=CARTESIAN_POINT('Ctrl Pts',(6.72689687653686,0.756087966466645,-53.2670055234569));
#34367=CARTESIAN_POINT('Ctrl Pts',(6.70290923580914,0.929137652075598,-53.2588026390697));
#34368=CARTESIAN_POINT('Ctrl Pts',(6.6789324978523,1.1021086838021,-53.2506034830261));
#34369=CARTESIAN_POINT('Ctrl Pts',(6.64824515568848,1.27422988244227,-53.2424043269826));
#34370=CARTESIAN_POINT('Ctrl Pts',(6.61093175694738,1.44494647132155,-53.234205170939));
#34371=CARTESIAN_POINT('Ctrl Pts',(6.57362160356463,1.61564821200889,-53.2260067280227));
#34372=CARTESIAN_POINT('Ctrl Pts',(6.52968660969767,1.78494523439371,-53.2178082851063));
#34373=CARTESIAN_POINT('Ctrl Pts',(6.47926252155291,1.95229254385705,-53.20960984219));
#34374=CARTESIAN_POINT('Ctrl Pts',(6.4288389355724,2.11963818673923,-53.2014114809204));
#34375=CARTESIAN_POINT('Ctrl Pts',(6.37192648650464,2.28503381162324,-53.1932131196509));
#34376=CARTESIAN_POINT('Ctrl Pts',(6.30871089728012,2.44794930800028,-53.1850147583813));
#34377=CARTESIAN_POINT('Ctrl Pts',(6.24548445404361,2.61089277669829,-53.1768149894667));
#34378=CARTESIAN_POINT('Ctrl Pts',(6.17595284427489,2.77135493408912,-53.1686152205521));
#34379=CARTESIAN_POINT('Ctrl Pts',(6.10035008355252,2.92882533758856,-53.1604154516375));
#34380=CARTESIAN_POINT('Ctrl Pts',(6.02472060803572,3.08635138441928,-53.1522127852739));
#34381=CARTESIAN_POINT('Ctrl Pts',(5.94301586327166,3.24088324831998,-53.1440101189103));
#34382=CARTESIAN_POINT('Ctrl Pts',(5.85551600434688,3.39193474625288,-53.1358074525467));
#34383=CARTESIAN_POINT('Ctrl Pts',(5.76791676745299,3.54315780093203,-53.1275954700044));
#34384=CARTESIAN_POINT('Ctrl Pts',(5.67450944722322,3.69089228197221,-53.1193834874621));
#34385=CARTESIAN_POINT('Ctrl Pts',(5.57561833368542,3.83467980372169,-53.1111715049198));
#34386=CARTESIAN_POINT('Ctrl Pts',(5.47666889283215,3.97855213329507,-53.1029546788392));
#34387=CARTESIAN_POINT('Ctrl Pts',(5.37222942552659,4.11847257613394,-53.0947378527586));
#34388=CARTESIAN_POINT('Ctrl Pts',(5.26266469357066,4.25401567028671,-53.0865210266779));
#34389=CARTESIAN_POINT('Ctrl Pts',(5.15293099697428,4.38976779146632,-53.0782915290648));
#34390=CARTESIAN_POINT('Ctrl Pts',(5.03805647683891,4.52112880420129,-53.0700620314517));
#34391=CARTESIAN_POINT('Ctrl Pts',(4.91844385480994,4.64770901058601,-53.0618325338385));
#34392=CARTESIAN_POINT('Ctrl Pts',(4.8118262599465,4.76053721327173,-53.0544971103058));
#34393=CARTESIAN_POINT('Ctrl Pts',(4.70144479333497,4.86956739768718,-53.047161686773));
#34394=CARTESIAN_POINT('Ctrl Pts',(4.58760622732013,4.97455104537621,-53.0398262632402));
#34395=CARTESIAN_POINT('Ctrl Pts',(4.46236151905179,5.09005360999957,-53.0317558613321));
#34396=CARTESIAN_POINT('Ctrl Pts',(4.33252320066664,5.20103397968373,-53.0236854594239));
#34397=CARTESIAN_POINT('Ctrl Pts',(4.19845643524763,5.3070945498764,-53.0156150575158));
#34398=CARTESIAN_POINT('Ctrl Pts',(4.06453646939973,5.41303898654285,-53.0075534924848));
#34399=CARTESIAN_POINT('Ctrl Pts',(3.92639755208268,5.51407410735804,-52.9994919274538));
#34400=CARTESIAN_POINT('Ctrl Pts',(3.78444247203027,5.6098381595099,-52.9914303624229));
#34401=CARTESIAN_POINT('Ctrl Pts',(3.64265125331076,5.70549166947318,-52.9833781030032));
#34402=CARTESIAN_POINT('Ctrl Pts',(3.49705294931979,5.79588601843103,-52.9753258435834));
#34403=CARTESIAN_POINT('Ctrl Pts',(3.34808386484208,5.88069923002224,-52.9672735841637));
#34404=CARTESIAN_POINT('Ctrl Pts',(3.26607964562807,5.92738704595367,-52.9628409916635));
#34405=CARTESIAN_POINT('Ctrl Pts',(3.18305458350682,5.97238433273468,-52.9584083991633));
#34406=CARTESIAN_POINT('Ctrl Pts',(3.09908550384721,6.01564277861012,-52.953975806663));
#34407=CARTESIAN_POINT('Ctrl Pts',(3.09908550384721,6.01564277861012,-54.9544629019808));
#34408=CARTESIAN_POINT('Ctrl Pts',(3.0397660155061,6.04620246660676,-54.9513058927933));
#34409=CARTESIAN_POINT('Ctrl Pts',(2.98003448412068,6.07586403636278,-54.9481488836058));
#34410=CARTESIAN_POINT('Ctrl Pts',(2.91992138371238,6.10461695054974,-54.9449918744183));
#34411=CARTESIAN_POINT('Ctrl Pts',(2.76123539795879,6.180518617575,-54.9366580318525));
#34412=CARTESIAN_POINT('Ctrl Pts',(2.59938502055361,6.25032607350716,-54.9283241892866));
#34413=CARTESIAN_POINT('Ctrl Pts',(2.43487229791274,6.31376954701842,-54.9199903467208));
#34414=CARTESIAN_POINT('Ctrl Pts',(2.2705534743535,6.37713824436008,-54.911666326644));
#34415=CARTESIAN_POINT('Ctrl Pts',(2.10357887834545,6.434157777379,-54.9033423065672));
#34416=CARTESIAN_POINT('Ctrl Pts',(1.93447389087424,6.48460482724475,-54.8950182864904));
#34417=CARTESIAN_POINT('Ctrl Pts',(1.76553720989281,6.53500166826681,-54.8867025511284));
#34418=CARTESIAN_POINT('Ctrl Pts',(1.59447469311592,6.57883896006349,-54.8783868157665));
#34419=CARTESIAN_POINT('Ctrl Pts',(1.42183059699803,6.61594186442416,-54.8700710804045));
#34420=CARTESIAN_POINT('Ctrl Pts',(1.24932669690675,6.65301463928788,-54.8617620978542));
#34421=CARTESIAN_POINT('Ctrl Pts',(1.07524411522569,6.68336385079959,-54.8534531153038));
#34422=CARTESIAN_POINT('Ctrl Pts',(0.90014135101851,6.70686473310642,-54.8451441327535));
#34423=CARTESIAN_POINT('Ctrl Pts',(0.725148713666631,6.73035083507395,-54.8368403759466));
#34424=CARTESIAN_POINT('Ctrl Pts',(0.549137516245436,6.74699714528917,-54.8285366191396));
#34425=CARTESIAN_POINT('Ctrl Pts',(0.372675736634933,6.75673011117979,-54.8202328623327));
#34426=CARTESIAN_POINT('Ctrl Pts',(0.196285596261459,6.76645912572042,-54.8119324766513));
#34427=CARTESIAN_POINT('Ctrl Pts',(0.0194455849327746,6.7692803692821,-54.8036320909699));
#34428=CARTESIAN_POINT('Ctrl Pts',(-0.157271622801084,6.76517218085848,
-54.7953317052884));
#34429=CARTESIAN_POINT('Ctrl Pts',(-0.333951565470907,6.76106485874498,
-54.7870330699425));
#34430=CARTESIAN_POINT('Ctrl Pts',(-0.510508408640314,6.7500310238645,-54.7787344345966));
#34431=CARTESIAN_POINT('Ctrl Pts',(-0.686369653741176,6.73210113548684,
-54.7704357992507));
#34432=CARTESIAN_POINT('Ctrl Pts',(-0.862223005230163,6.71417205190037,
-54.7621375363927));
#34433=CARTESIAN_POINT('Ctrl Pts',(-1.03738047491462,6.68934756708489,-54.7538392735348));
#34434=CARTESIAN_POINT('Ctrl Pts',(-1.21127466263797,6.65771001859132,-54.7455410106769));
#34435=CARTESIAN_POINT('Ctrl Pts',(-1.38518990820995,6.62606863892481,-54.7372417429346));
#34436=CARTESIAN_POINT('Ctrl Pts',(-1.55784122495393,6.58761261444436,-54.7289424751922));
#34437=CARTESIAN_POINT('Ctrl Pts',(-1.72867118702229,6.54247544337455,-54.7206432074499));
#34438=CARTESIAN_POINT('Ctrl Pts',(-1.8996210992816,6.4973065787293,-54.7123381122828));
#34439=CARTESIAN_POINT('Ctrl Pts',(-2.06874676477396,6.44544728251986,-54.7040330171157));
#34440=CARTESIAN_POINT('Ctrl Pts',(-2.23550484287439,6.38708126592148,-54.6957279219486));
#34441=CARTESIAN_POINT('Ctrl Pts',(-2.40232372965176,6.32869396603484,-54.6874197983114));
#34442=CARTESIAN_POINT('Ctrl Pts',(-2.56677298250584,6.26379533852226,-54.6791116746742));
#34443=CARTESIAN_POINT('Ctrl Pts',(-2.72832883504125,6.19261744078241,-54.6708035510371));
#34444=CARTESIAN_POINT('Ctrl Pts',(-2.89005642055325,6.12136388133143,-54.6624865959105));
#34445=CARTESIAN_POINT('Ctrl Pts',(-3.04888414519265,6.0438178625554,-54.6541696407839));
#34446=CARTESIAN_POINT('Ctrl Pts',(-3.20431148179891,5.96025812592137,-54.6458526856573));
#34447=CARTESIAN_POINT('Ctrl Pts',(-3.31885909485103,5.89867585482487,-54.6397232146233));
#34448=CARTESIAN_POINT('Ctrl Pts',(-3.43156029632883,5.83382822072068,-54.6335937435893));
#34449=CARTESIAN_POINT('Ctrl Pts',(-3.54222479973134,5.76584186985459,-54.6274642725554));
#34450=CARTESIAN_POINT('Ctrl Pts',(-3.69480376105335,5.67210551826684,-54.6190132490107));
#34451=CARTESIAN_POINT('Ctrl Pts',(-3.84378878812548,5.57222972919851,-54.610562225466));
#34452=CARTESIAN_POINT('Ctrl Pts',(-3.98867340368538,5.46651383230052,-54.6021112019213));
#34453=CARTESIAN_POINT('Ctrl Pts',(-4.13343045263647,5.36089101511573,-54.5936676192524));
#34454=CARTESIAN_POINT('Ctrl Pts',(-4.27409401953163,5.24943853364486,-54.5852240365834));
#34455=CARTESIAN_POINT('Ctrl Pts',(-4.41018553649275,5.13249963796493,-54.5767804539144));
#34456=CARTESIAN_POINT('Ctrl Pts',(-4.54617572906893,5.0156478069452,-54.5683431577564));
#34457=CARTESIAN_POINT('Ctrl Pts',(-4.67760040689393,4.89331791991543,-54.5599058615985));
#34458=CARTESIAN_POINT('Ctrl Pts',(-4.80401280203065,4.76589445937755,-54.5514685654405));
#34459=CARTESIAN_POINT('Ctrl Pts',(-4.93033501154598,4.63856190577927,-54.5430372886511));
#34460=CARTESIAN_POINT('Ctrl Pts',(-5.05165183817416,4.50614326180706,-54.5346060118617));
#34461=CARTESIAN_POINT('Ctrl Pts',(-5.16755206655165,4.36906107069674,-54.5261747350723));
#34462=CARTESIAN_POINT('Ctrl Pts',(-5.2834026158868,4.23203763798641,-54.5177470722339));
#34463=CARTESIAN_POINT('Ctrl Pts',(-5.39384098185699,4.09035489583673,-54.5093194093956));
#34464=CARTESIAN_POINT('Ctrl Pts',(-5.49849463773981,3.94447027099287,-54.5008917465573));
#34465=CARTESIAN_POINT('Ctrl Pts',(-5.60311607707546,3.79863055522418,-54.492466678088));
#34466=CARTESIAN_POINT('Ctrl Pts',(-5.70195616462208,3.64859180537235,-54.4840416096186));
#34467=CARTESIAN_POINT('Ctrl Pts',(-5.79468409162147,3.494842668606,-54.4756165411493));
#34468=CARTESIAN_POINT('Ctrl Pts',(-5.82005728957281,3.45277220064388,-54.4733111846408));
#34469=CARTESIAN_POINT('Ctrl Pts',(-5.84497309589304,3.41042409212107,-54.4710058281323));
#34470=CARTESIAN_POINT('Ctrl Pts',(-5.86942530269911,3.36780872616535,-54.4687004716238));
#34471=CARTESIAN_POINT('Ctrl Pts',(-5.96084426146999,3.20848354074512,-54.4600814830281));
#34472=CARTESIAN_POINT('Ctrl Pts',(-6.04573886810129,3.04549186441933,-54.4514624944324));
#34473=CARTESIAN_POINT('Ctrl Pts',(-6.12383968349658,2.87938822162496,-54.4428435058367));
#34474=CARTESIAN_POINT('Ctrl Pts',(-6.20198728826842,2.71318506788629,-54.4342193536956));
#34475=CARTESIAN_POINT('Ctrl Pts',(-6.27333284973063,2.5438665022574,-54.4255952015546));
#34476=CARTESIAN_POINT('Ctrl Pts',(-6.33765486817745,2.3720075404321,-54.4169710494135));
#34477=CARTESIAN_POINT('Ctrl Pts',(-6.40417993222563,2.19426236516003,-54.4080515178534));
#34478=CARTESIAN_POINT('Ctrl Pts',(-6.4631917009667,2.01380003230584,-54.3991319862933));
#34479=CARTESIAN_POINT('Ctrl Pts',(-6.51450118719296,1.83127367754293,-54.3902124547332));
#34480=CARTESIAN_POINT('Ctrl Pts',(-6.5642039255264,1.65446310474291,-54.381572236797));
#34481=CARTESIAN_POINT('Ctrl Pts',(-6.60667944680759,1.4757161298277,-54.3729320188608));
#34482=CARTESIAN_POINT('Ctrl Pts',(-6.64180796657907,1.29563726987412,-54.3642918009246));
#34483=CARTESIAN_POINT('Ctrl Pts',(-6.67863989375865,1.10682625536108,-54.3552326125526));
#34484=CARTESIAN_POINT('Ctrl Pts',(-6.70739452440246,0.916551359942948,
-54.3461734241805));
#34485=CARTESIAN_POINT('Ctrl Pts',(-6.72799486069623,0.7255164742755,-54.3371142358084));
#34486=CARTESIAN_POINT('Ctrl Pts',(-6.74859519698999,0.53448158860806,-54.3280550474364));
#34487=CARTESIAN_POINT('Ctrl Pts',(-6.76104124721361,0.342687096659948,
-54.3189958590643));
#34488=CARTESIAN_POINT('Ctrl Pts',(-6.76531867369208,0.150838467882794,
-54.3099366706923));
#34489=CARTESIAN_POINT('Ctrl Pts',(-6.76643871924403,0.100602840364678,
-54.3075645191915));
#34490=CARTESIAN_POINT('Ctrl Pts',(-6.76699916726937,0.0503573167275674,
-54.3051923676907));
#34491=CARTESIAN_POINT('Ctrl Pts',(-6.76699999907271,0.000112026683497747,
-54.30282021619));
#34492=CARTESIAN_POINT('',(-6.76699743900148,-0.00588732090316101,-54.6971797837852));
#34493=CARTESIAN_POINT('Ctrl Pts',(3.09908550384722,6.01564277861012,-55.3486963765549));
#34494=CARTESIAN_POINT('Ctrl Pts',(2.93976283080413,6.09772122053783,-55.3402683842273));
#34495=CARTESIAN_POINT('Ctrl Pts',(2.77722522026857,6.17344176643959,-55.3318403918997));
#34496=CARTESIAN_POINT('Ctrl Pts',(2.61201193932657,6.24257019414403,-55.3234123995721));
#34497=CARTESIAN_POINT('Ctrl Pts',(2.44664966910367,6.31176096184121,-55.3149768068839));
#34498=CARTESIAN_POINT('Ctrl Pts',(2.27860721536357,6.37434760490997,-55.3065412141957));
#34499=CARTESIAN_POINT('Ctrl Pts',(2.10844277015434,6.43014448398976,-55.2981056215075));
#34500=CARTESIAN_POINT('Ctrl Pts',(1.93819294341394,6.48596935965229,-55.2896657961853));
#34501=CARTESIAN_POINT('Ctrl Pts',(1.76581932084211,6.53499758082109,-55.281225970863));
#34502=CARTESIAN_POINT('Ctrl Pts',(1.59189359642014,6.57709387021932,-55.2727861455408));
#34503=CARTESIAN_POINT('Ctrl Pts',(1.41778013607079,6.61923559847345,-55.2643372102468));
#34504=CARTESIAN_POINT('Ctrl Pts',(1.24211155260136,6.65443037598622,-55.2558882749528));
#34505=CARTESIAN_POINT('Ctrl Pts',(1.06546914519395,6.68259414453996,-55.2474393396589));
#34506=CARTESIAN_POINT('Ctrl Pts',(0.993316315092483,6.69409815219757,-55.2439882171241));
#34507=CARTESIAN_POINT('Ctrl Pts',(0.921001067625565,6.70442966308823,-55.2405370945893));
#34508=CARTESIAN_POINT('Ctrl Pts',(0.848563193888828,6.71358544341079,-55.2370859720545));
#34509=CARTESIAN_POINT('Ctrl Pts',(0.675592049779231,6.73544811987978,-55.2288451916103));
#34510=CARTESIAN_POINT('Ctrl Pts',(0.50153663813381,6.7506519793541,-55.2206044111662));
#34511=CARTESIAN_POINT('Ctrl Pts',(0.326949049670479,6.75909707867253,-55.212363630722));
#34512=CARTESIAN_POINT('Ctrl Pts',(0.152554836175986,6.76753282411403,-55.2041319778492));
#34513=CARTESIAN_POINT('Ctrl Pts',(-0.0223700281979955,6.76922469849558,
-55.1959003249763));
#34514=CARTESIAN_POINT('Ctrl Pts',(-0.197265485963421,6.76412413606134,
-55.1876686721034));
#34515=CARTESIAN_POINT('Ctrl Pts',(-0.371998395639786,6.75902831409715,
-55.1794446697405));
#34516=CARTESIAN_POINT('Ctrl Pts',(-0.546701599591087,6.74715263797038,
-55.1712206673777));
#34517=CARTESIAN_POINT('Ctrl Pts',(-0.720812072433768,6.72850049834536,
-55.1629966650148));
#34518=CARTESIAN_POINT('Ctrl Pts',(-0.894768717059198,6.70986483805866,
-55.1547799286342));
#34519=CARTESIAN_POINT('Ctrl Pts',(-1.06813332192174,6.6844646848864,-55.1465631922537));
#34520=CARTESIAN_POINT('Ctrl Pts',(-1.24034514887233,6.65235544086971,-55.1383464558732));
#34521=CARTESIAN_POINT('Ctrl Pts',(-1.41246874477662,6.62026264771036,-55.1301339292572));
#34522=CARTESIAN_POINT('Ctrl Pts',(-1.58344039014235,6.58146767457903,-55.1219214026412));
#34523=CARTESIAN_POINT('Ctrl Pts',(-1.75270632266394,6.5360775352266,-55.1137088760253));
#34524=CARTESIAN_POINT('Ctrl Pts',(-1.92191565071386,6.49070257485803,-55.1054990957725));
#34525=CARTESIAN_POINT('Ctrl Pts',(-2.08942005897657,6.43873693393464,-55.0972893155198));
#34526=CARTESIAN_POINT('Ctrl Pts',(-2.25467771297685,6.38033834609149,-55.089079535267));
#34527=CARTESIAN_POINT('Ctrl Pts',(-2.32685734535631,6.35483157832634,-55.085493747219));
#34528=CARTESIAN_POINT('Ctrl Pts',(-2.39860854577049,6.3280982554676,-55.081907959171));
#34529=CARTESIAN_POINT('Ctrl Pts',(-2.46988710538396,6.30015449704673,-55.0783221711229));
#34530=CARTESIAN_POINT('Ctrl Pts',(-2.64598128990308,6.2311192446762,-55.0694634564463));
#34531=CARTESIAN_POINT('Ctrl Pts',(-2.81900706367222,6.1547646582062,-55.0606047417697));
#34532=CARTESIAN_POINT('Ctrl Pts',(-2.98838626350261,6.07139494186541,-55.0517460270931));
#34533=CARTESIAN_POINT('Ctrl Pts',(-3.1580823424592,5.98786925523493,-55.0428707392967));
#34534=CARTESIAN_POINT('Ctrl Pts',(-3.32411798127155,5.89730232566225,-55.0339954515003));
#34535=CARTESIAN_POINT('Ctrl Pts',(-3.48594122879942,5.80004334029983,-55.0251201637039));
#34536=CARTESIAN_POINT('Ctrl Pts',(-3.64822408849316,5.70250811889843,-55.0162196682176));
#34537=CARTESIAN_POINT('Ctrl Pts',(-3.80627039163525,5.59824294110568,-55.0073191727313));
#34538=CARTESIAN_POINT('Ctrl Pts',(-3.95955618398132,5.48764100738152,-54.998418677245));
#34539=CARTESIAN_POINT('Ctrl Pts',(-4.11304947856779,5.37688935235125,-54.9895061332007));
#34540=CARTESIAN_POINT('Ctrl Pts',(-4.26176918308157,5.2597839632968,-54.9805935891564));
#34541=CARTESIAN_POINT('Ctrl Pts',(-4.40522485176231,5.13675802480667,-54.9716810451121));
#34542=CARTESIAN_POINT('Ctrl Pts',(-4.54899728398812,5.01346043352812,-54.9627488213363));
#34543=CARTESIAN_POINT('Ctrl Pts',(-4.6874822338197,4.8842163139173,-54.9538165975605));
#34544=CARTESIAN_POINT('Ctrl Pts',(-4.82022445603094,4.74949736219332,-54.9448843737847));
#34545=CARTESIAN_POINT('Ctrl Pts',(-4.94568145610411,4.62217212042211,-54.9364423725869));
#34546=CARTESIAN_POINT('Ctrl Pts',(-5.06600898626905,4.48995693809524,-54.9280003713892));
#34547=CARTESIAN_POINT('Ctrl Pts',(-5.18085617329275,4.35327673272151,-54.9195583701915));
#34548=CARTESIAN_POINT('Ctrl Pts',(-5.2907928346339,4.22244056825272,-54.9114773239702));
#34549=CARTESIAN_POINT('Ctrl Pts',(-5.39594419765033,4.08722990267799,-54.903396277749));
#34550=CARTESIAN_POINT('Ctrl Pts',(-5.49593488230195,3.94803606486779,-54.8953152315278));
#34551=CARTESIAN_POINT('Ctrl Pts',(-5.59808594525775,3.80583483343557,-54.8870595878729));
#34552=CARTESIAN_POINT('Ctrl Pts',(-5.69485048431008,3.65947658957157,-54.878803944218));
#34553=CARTESIAN_POINT('Ctrl Pts',(-5.7858686313026,3.50941778380811,-54.8705483005631));
#34554=CARTESIAN_POINT('Ctrl Pts',(-5.87476860139071,3.36285115083847,-54.862484782482));
#34555=CARTESIAN_POINT('Ctrl Pts',(-5.95818644517708,3.21275461464334,-54.854421264401));
#34556=CARTESIAN_POINT('Ctrl Pts',(-6.03582831224443,3.05958585189378,-54.8463577463199));
#34557=CARTESIAN_POINT('Ctrl Pts',(-6.11342479917093,2.90650661326683,-54.8382989412062));
#34558=CARTESIAN_POINT('Ctrl Pts',(-6.18525185970134,2.75035905233115,-54.8302401360925));
#34559=CARTESIAN_POINT('Ctrl Pts',(-6.25106040147808,2.59162745337225,-54.8221813309788));
#34560=CARTESIAN_POINT('Ctrl Pts',(-6.31684345972862,2.43295732121918,-54.8141256465356));
#34561=CARTESIAN_POINT('Ctrl Pts',(-6.37661249610298,2.2717054863293,-54.8060699620924));
#34562=CARTESIAN_POINT('Ctrl Pts',(-6.43016565495611,2.10837820369659,-54.7980142776491));
#34563=CARTESIAN_POINT('Ctrl Pts',(-6.48602688876846,1.93801171704167,-54.7896114031625));
#34564=CARTESIAN_POINT('Ctrl Pts',(-6.53512436688111,1.76538729719315,-54.7812085286759));
#34565=CARTESIAN_POINT('Ctrl Pts',(-6.5772859921995,1.59109961247443,-54.7728056541894));
#34566=CARTESIAN_POINT('Ctrl Pts',(-6.61770753693504,1.42400507113478,-54.7647495803449));
#34567=CARTESIAN_POINT('Ctrl Pts',(-6.6517542056154,1.2553821973894,-54.7566935065005));
#34568=CARTESIAN_POINT('Ctrl Pts',(-6.6793262126381,1.08576716894813,-54.748637432656));
#34569=CARTESIAN_POINT('Ctrl Pts',(-6.7069026960708,0.9161246029246,-54.7405800508804));
#34570=CARTESIAN_POINT('Ctrl Pts',(-6.72800237314028,0.7454899302217,-54.7325226691047));
#34571=CARTESIAN_POINT('Ctrl Pts',(-6.7425771674299,0.574405902870916,-54.724465287329));
#34572=CARTESIAN_POINT('Ctrl Pts',(-6.75716071565542,0.403219118762315,
-54.716403066116));
#34573=CARTESIAN_POINT('Ctrl Pts',(-6.76521153804951,0.231582812735872,
-54.7083408449029));
#34574=CARTESIAN_POINT('Ctrl Pts',(-6.76673363030631,0.0600414563578614,
-54.7002786236899));
#34575=CARTESIAN_POINT('Ctrl Pts',(-6.76692864356885,0.038063261923281,
-54.6992456770633));
#34576=CARTESIAN_POINT('Ctrl Pts',(-6.76701655643823,0.0160866226493078,
-54.6982127304367));
#34577=CARTESIAN_POINT('Ctrl Pts',(-6.76699743900194,-0.00588732037279986,
-54.6971797838101));
#34578=CARTESIAN_POINT('Ctrl Pts',(-6.76699743900148,-0.00588732090315215,
-54.6971797837852));
#34579=CARTESIAN_POINT('Ctrl Pts',(-6.76680418587059,-0.228016106365009,
-54.6867379991958));
#34580=CARTESIAN_POINT('Ctrl Pts',(-6.75567034531407,-0.449632090273862,
-54.6762962146064));
#34581=CARTESIAN_POINT('Ctrl Pts',(-6.73376803723041,-0.669818647675761,
-54.6658544300171));
#34582=CARTESIAN_POINT('Ctrl Pts',(-6.71136652631499,-0.895023751641342,
-54.6551746536866));
#34583=CARTESIAN_POINT('Ctrl Pts',(-6.67770007774188,-1.11873373341628,
-54.6444948773561));
#34584=CARTESIAN_POINT('Ctrl Pts',(-6.63300103649544,-1.33999486933738,
-54.6338151010255));
#34585=CARTESIAN_POINT('Ctrl Pts',(-6.58865774832616,-1.55949502050875,
-54.6232203234598));
#34586=CARTESIAN_POINT('Ctrl Pts',(-6.53345690463797,-1.77658548395082,
-54.6126255458941));
#34587=CARTESIAN_POINT('Ctrl Pts',(-6.46767094968983,-1.9903571253768,-54.6020307683284));
#34588=CARTESIAN_POINT('Ctrl Pts',(-6.41755664466207,-2.15320369731077,
-54.5939598979572));
#34589=CARTESIAN_POINT('Ctrl Pts',(-6.36119638138062,-2.31445365969866,
-54.5858890275861));
#34590=CARTESIAN_POINT('Ctrl Pts',(-6.29870566844256,-2.47357957266986,
-54.5778181572149));
#34591=CARTESIAN_POINT('Ctrl Pts',(-6.23629272032192,-2.6325074658556,-54.5697573304123));
#34592=CARTESIAN_POINT('Ctrl Pts',(-6.16776463673065,-2.78931622614659,
-54.5616965036098));
#34593=CARTESIAN_POINT('Ctrl Pts',(-6.093287415256,-2.94349069559984,-54.5536356768072));
#34594=CARTESIAN_POINT('Ctrl Pts',(-6.01888654315695,-3.09750711505818,
-54.5455831134586));
#34595=CARTESIAN_POINT('Ctrl Pts',(-5.93854883066954,-3.24889428475438,
-54.53753055011));
#34596=CARTESIAN_POINT('Ctrl Pts',(-5.85248932311385,-3.39715435664003,
-54.5294779867614));
#34597=CARTESIAN_POINT('Ctrl Pts',(-5.76649919452756,-3.54529490505545,
-54.521431915183));
#34598=CARTESIAN_POINT('Ctrl Pts',(-5.67479663819831,-3.69031305234391,
-54.5133858436046));
#34599=CARTESIAN_POINT('Ctrl Pts',(-5.5776437966822,-3.83173311666308,-54.5053397720262));
#34600=CARTESIAN_POINT('Ctrl Pts',(-5.48054802622102,-3.97307010577691,
-54.4972984269981));
#34601=CARTESIAN_POINT('Ctrl Pts',(-5.3780085549301,-4.11081291292901,-54.48925708197));
#34602=CARTESIAN_POINT('Ctrl Pts',(-5.27033218331351,-4.244512654891,-54.4812157369419));
#34603=CARTESIAN_POINT('Ctrl Pts',(-5.1605801467745,-4.38078971126618,-54.4730193798388));
#34604=CARTESIAN_POINT('Ctrl Pts',(-5.04549134299811,-4.51286589513378,
-54.4648230227356));
#34605=CARTESIAN_POINT('Ctrl Pts',(-4.92543570251534,-4.64029871240929,
-54.4566266656324));
#34606=CARTESIAN_POINT('Ctrl Pts',(-4.80768803261037,-4.76528173897328,
-54.4485878767281));
#34607=CARTESIAN_POINT('Ctrl Pts',(-4.68516304162269,-4.88579804282406,
-54.4405490878238));
#34608=CARTESIAN_POINT('Ctrl Pts',(-4.55824866500417,-5.00146559600161,
-54.4325102989195));
#34609=CARTESIAN_POINT('Ctrl Pts',(-4.43132070737851,-5.11714552667261,
-54.4244706497908));
#34610=CARTESIAN_POINT('Ctrl Pts',(-4.30000270485133,-5.22797542187798,
-54.4164310006621));
#34611=CARTESIAN_POINT('Ctrl Pts',(-4.16471727806585,-5.33361219004342,
-54.4083913515333));
#34612=CARTESIAN_POINT('Ctrl Pts',(-4.02939058746502,-5.43928117879758,
-54.400349250207));
#34613=CARTESIAN_POINT('Ctrl Pts',(-3.89009435806851,-5.53975365790169,
-54.3923071488807));
#34614=CARTESIAN_POINT('Ctrl Pts',(-3.7472817766384,-5.63472876778233,-54.3842650475544));
#34615=CARTESIAN_POINT('Ctrl Pts',(-3.5996498416032,-5.73290890787539,-54.3759515574636));
#34616=CARTESIAN_POINT('Ctrl Pts',(-3.44826044016032,-5.82521391636151,
-54.3676380673729));
#34617=CARTESIAN_POINT('Ctrl Pts',(-3.2936426797554,-5.91136252467176,-54.3593245772821));
#34618=CARTESIAN_POINT('Ctrl Pts',(-3.14380883632135,-5.99484567082402,
-54.3512683089117));
#34619=CARTESIAN_POINT('Ctrl Pts',(-2.99094379298023,-6.07254760376807,
-54.3432120405414));
#34620=CARTESIAN_POINT('Ctrl Pts',(-2.83554971402137,-6.14426129158855,
-54.335155772171));
#34621=CARTESIAN_POINT('Ctrl Pts',(-2.67271346758084,-6.21940950715334,
-54.3267136712201));
#34622=CARTESIAN_POINT('Ctrl Pts',(-2.50710043562913,-6.28798160598858,
-54.3182715702691));
#34623=CARTESIAN_POINT('Ctrl Pts',(-2.33930596094258,-6.34979815593366,
-54.3098294693182));
#34624=CARTESIAN_POINT('Ctrl Pts',(-2.17151148625601,-6.41161470587875,
-54.3013873683672));
#34625=CARTESIAN_POINT('Ctrl Pts',(-2.00153603392613,-6.46667564716504,
-54.2929452674163));
#34626=CARTESIAN_POINT('Ctrl Pts',(-1.82998604543771,-6.51486301264296,
-54.2845031664654));
#34627=CARTESIAN_POINT('Ctrl Pts',(-1.66063595065124,-6.56243244114074,
-54.2761693238995));
#34628=CARTESIAN_POINT('Ctrl Pts',(-1.48921323568788,-6.60345534162941,
-54.2678354813336));
#34629=CARTESIAN_POINT('Ctrl Pts',(-1.31625876710413,-6.6377520184187,-54.2595016387678));
#34630=CARTESIAN_POINT('Ctrl Pts',(-1.14350814726892,-6.6720082722302,-54.251177618691));
#34631=CARTESIAN_POINT('Ctrl Pts',(-0.969229708560848,-6.69955402796864,
-54.2428535986142));
#34632=CARTESIAN_POINT('Ctrl Pts',(-0.793979341825377,-6.72025935546795,
-54.2345295785374));
#34633=CARTESIAN_POINT('Ctrl Pts',(-0.618903397940909,-6.74094407540837,
-54.2262138431754));
#34634=CARTESIAN_POINT('Ctrl Pts',(-0.442857796587523,-6.75480189061367,
-54.2178981078135));
#34635=CARTESIAN_POINT('Ctrl Pts',(-0.266408712091897,-6.76175386997498,
-54.2095823724515));
#34636=CARTESIAN_POINT('Ctrl Pts',(-0.0901029134722441,-6.7687002039658,
-54.2012733899012));
#34637=CARTESIAN_POINT('Ctrl Pts',(0.0866053693430223,-6.7687518627516,
-54.1929644073508));
#34638=CARTESIAN_POINT('Ctrl Pts',(0.263144515717021,-6.76188168809896,
-54.1846554248005));
#34639=CARTESIAN_POINT('Ctrl Pts',(0.439572631856113,-6.75501583428463,
-54.1763516679936));
#34640=CARTESIAN_POINT('Ctrl Pts',(0.615831476951372,-6.74123683624038,
-54.1680479111866));
#34641=CARTESIAN_POINT('Ctrl Pts',(0.791348872924406,-6.72056961583773,
-54.1597441543797));
#34642=CARTESIAN_POINT('Ctrl Pts',(0.966795013057527,-6.69991078582932,
-54.1514437686983));
#34643=CARTESIAN_POINT('Ctrl Pts',(1.14149995897005,-6.67236934622123,-54.1431433830168));
#34644=CARTESIAN_POINT('Ctrl Pts',(1.31489580276888,-6.6380221472861,-54.1348429973354));
#34645=CARTESIAN_POINT('Ctrl Pts',(1.48825508189294,-6.60368219128212,-54.1265443619895));
#34646=CARTESIAN_POINT('Ctrl Pts',(1.66030546790751,-6.56253940267501,-54.1182457266435));
#34647=CARTESIAN_POINT('Ctrl Pts',(1.83048816281293,-6.51472194999923,-54.1099470912976));
#34648=CARTESIAN_POINT('Ctrl Pts',(2.00066321899095,-6.46690664363148,-54.1016488284397));
#34649=CARTESIAN_POINT('Ctrl Pts',(2.16897041636322,-6.41241736445312,-54.0933505655818));
#34650=CARTESIAN_POINT('Ctrl Pts',(2.33486487486542,-6.35143251685159,-54.0850523027239));
#34651=CARTESIAN_POINT('Ctrl Pts',(2.50077942248289,-6.29044028424368,-54.0767530349815));
#34652=CARTESIAN_POINT('Ctrl Pts',(2.66428032284196,-6.22295103640304,-54.0684537672391));
#34653=CARTESIAN_POINT('Ctrl Pts',(2.82484129446398,-6.14919187057056,-54.0601544994968));
#34654=CARTESIAN_POINT('Ctrl Pts',(2.98551500578896,-6.07538091390522,-54.0518494043297));
#34655=CARTESIAN_POINT('Ctrl Pts',(3.14324434711673,-5.99529138764948,-54.0435443091626));
#34656=CARTESIAN_POINT('Ctrl Pts',(3.29752552309412,-5.90919744335412,-54.0352392139955));
#34657=CARTESIAN_POINT('Ctrl Pts',(3.45186295802048,-5.82307210472443,-54.0269310903583));
#34658=CARTESIAN_POINT('Ctrl Pts',(3.60274942141719,-5.73093815994321,-54.0186229667211));
#34659=CARTESIAN_POINT('Ctrl Pts',(3.74970869170949,-5.63311403464534,-54.0103148430839));
#34660=CARTESIAN_POINT('Ctrl Pts',(3.89682417889221,-5.53518592284406,-54.0019978879573));
#34661=CARTESIAN_POINT('Ctrl Pts',(4.04000384669348,-5.43155574446703,-53.9936809328307));
#34662=CARTESIAN_POINT('Ctrl Pts',(4.17880237305546,-5.32258393329275,-53.9853639777042));
#34663=CARTESIAN_POINT('Ctrl Pts',(4.2810948026693,-5.2422733448693,-53.9792345066702));
#34664=CARTESIAN_POINT('Ctrl Pts',(4.38100828633158,-5.1590623345053,-53.9731050356363));
#34665=CARTESIAN_POINT('Ctrl Pts',(4.47837707016747,-5.07310829939577,-53.9669755646024));
#34666=CARTESIAN_POINT('Ctrl Pts',(4.61262452482687,-4.9545989581411,-53.9585245410577));
#34667=CARTESIAN_POINT('Ctrl Pts',(4.74227860219775,-4.83065731156955,-53.950073517513));
#34668=CARTESIAN_POINT('Ctrl Pts',(4.86689164827471,-4.70166509695809,-53.9416224939683));
#34669=CARTESIAN_POINT('Ctrl Pts',(4.9913949762588,-4.57278645616757,-53.9331789112993));
#34670=CARTESIAN_POINT('Ctrl Pts',(5.1108658904331,-4.43886634810276,-53.9247353286303));
#34671=CARTESIAN_POINT('Ctrl Pts',(5.22489176344625,-4.30032499472674,-53.9162917459613));
#34672=CARTESIAN_POINT('Ctrl Pts',(5.33883274063569,-4.16188678971523,-53.9078544498034));
#34673=CARTESIAN_POINT('Ctrl Pts',(5.4473365481612,-4.018834453297,-53.8994171536454));
#34674=CARTESIAN_POINT('Ctrl Pts',(5.55002895738425,-3.87162337685321,-53.8909798574874));
#34675=CARTESIAN_POINT('Ctrl Pts',(5.65264810339016,-3.72451732430692,-53.882548580698));
#34676=CARTESIAN_POINT('Ctrl Pts',(5.74946393177135,-3.57325872101615,-53.8741173039086));
#34677=CARTESIAN_POINT('Ctrl Pts',(5.84014376584591,-3.41833435963353,-53.8656860271192));
#34678=CARTESIAN_POINT('Ctrl Pts',(5.93078473125402,-3.26347640445234,-53.8572583642809));
#34679=CARTESIAN_POINT('Ctrl Pts',(6.01529477845574,-3.1049561091485,-53.8488307014425));
#34680=CARTESIAN_POINT('Ctrl Pts',(6.09338532758643,-2.94328799976394,-53.8404030386042));
#34681=CARTESIAN_POINT('Ctrl Pts',(6.17145183734821,-2.7816696582369,-53.8319779701349));
#34682=CARTESIAN_POINT('Ctrl Pts',(6.24310264602628,-2.61690573324335,-53.8235529016655));
#34683=CARTESIAN_POINT('Ctrl Pts',(6.30809562696466,-2.44953435596836,-53.8151278331961));
#34684=CARTESIAN_POINT('Ctrl Pts',(6.3258796950885,-2.40373642621558,-53.8128224766877));
#34685=CARTESIAN_POINT('Ctrl Pts',(6.34316554090043,-2.35774339158578,-53.8105171201793));
#34686=CARTESIAN_POINT('Ctrl Pts',(6.35994882873505,-2.3115665458454,-53.8082117636709));
#34687=CARTESIAN_POINT('Ctrl Pts',(6.42269615910115,-2.13892612976682,-53.7995927750752));
#34688=CARTESIAN_POINT('Ctrl Pts',(6.47838710060114,-1.96379218154052,-53.7909737864795));
#34689=CARTESIAN_POINT('Ctrl Pts',(6.5268512827126,-1.7867572116415,-53.7823547978838));
#34690=CARTESIAN_POINT('Ctrl Pts',(6.57534449920554,-1.6096161819551,-53.7737306457427));
#34691=CARTESIAN_POINT('Ctrl Pts',(6.61660223568956,-1.43057215109361,-53.7651064936017));
#34692=CARTESIAN_POINT('Ctrl Pts',(6.65050486452753,-1.25022959767221,-53.7564823414606));
#34693=CARTESIAN_POINT('Ctrl Pts',(6.685568667084,-1.06371026561931,-53.7475628099005));
#34694=CARTESIAN_POINT('Ctrl Pts',(6.71276455494065,-0.875802239944836,
-53.7386432783404));
#34695=CARTESIAN_POINT('Ctrl Pts',(6.73201832590055,-0.687181387800304,
-53.7297237467803));
#34696=CARTESIAN_POINT('Ctrl Pts',(6.7506691682756,-0.504467165774861,-53.7210835288441));
#34697=CARTESIAN_POINT('Ctrl Pts',(6.76186780567942,-0.321084392675276,
-53.7124433109079));
#34698=CARTESIAN_POINT('Ctrl Pts',(6.7655998777319,-0.137649171570764,-53.7038030929718));
#34699=CARTESIAN_POINT('Ctrl Pts',(6.76951292066569,0.0546809564807878,
-53.6947439045997));
#34700=CARTESIAN_POINT('Ctrl Pts',(6.7652172860921,0.247068357662824,-53.6856847162276));
#34701=CARTESIAN_POINT('Ctrl Pts',(6.75275780520025,0.438806363111455,-53.6766255278555));
#34702=CARTESIAN_POINT('Ctrl Pts',(6.74029832430841,0.630544368560078,-53.6675663394835));
#34703=CARTESIAN_POINT('Ctrl Pts',(6.71967507109066,0.821632601412444,-53.6585071511114));
#34704=CARTESIAN_POINT('Ctrl Pts',(6.69099487965136,1.01137358106649,-53.6494479627393));
#34705=CARTESIAN_POINT('Ctrl Pts',(6.66236437472461,1.20078584716971,-53.6404044688049));
#34706=CARTESIAN_POINT('Ctrl Pts',(6.6256792856349,1.38903014656108,-53.6313609748705));
#34707=CARTESIAN_POINT('Ctrl Pts',(6.58105340602497,1.57544440303274,-53.6223174809361));
#34708=CARTESIAN_POINT('Ctrl Pts',(6.53646834555174,1.76168814703307,-53.6132822590541));
#34709=CARTESIAN_POINT('Ctrl Pts',(6.48395705137221,1.94610495878242,-53.6042470371721));
#34710=CARTESIAN_POINT('Ctrl Pts',(6.42368419507574,2.12804378759793,-53.5952118152901));
#34711=CARTESIAN_POINT('Ctrl Pts',(6.363517526431,2.30966207980415,-53.5861925115021));
#34712=CARTESIAN_POINT('Ctrl Pts',(6.29561667608616,2.48881088105503,-53.5771732077142));
#34713=CARTESIAN_POINT('Ctrl Pts',(6.22019577440718,2.66485525461462,-53.5681539039262));
#34714=CARTESIAN_POINT('Ctrl Pts',(6.1448694935097,2.84067876822908,-53.5591459154839));
#34715=CARTESIAN_POINT('Ctrl Pts',(6.06204208263578,3.01340540847851,-53.5501379270417));
#34716=CARTESIAN_POINT('Ctrl Pts',(5.97197621739012,3.18241874349162,-53.5411299385994));
#34717=CARTESIAN_POINT('Ctrl Pts',(5.88211376902373,3.35105035602785,-53.5321422950113));
#34718=CARTESIAN_POINT('Ctrl Pts',(5.78504561075211,3.51598519407826,-53.5231546514232));
#34719=CARTESIAN_POINT('Ctrl Pts',(5.68108067246096,3.67663044008921,-53.5141670078351));
#34720=CARTESIAN_POINT('Ctrl Pts',(5.59053440879704,3.81654132774757,-53.5063393924927));
#34721=CARTESIAN_POINT('Ctrl Pts',(5.49475756233667,3.95319867699258,-53.4985117771502));
#34722=CARTESIAN_POINT('Ctrl Pts',(5.39398321700737,4.086224914838,-53.4906841618078));
#34723=CARTESIAN_POINT('Ctrl Pts',(5.2894070098332,4.2242697650731,-53.4825612380512));
#34724=CARTESIAN_POINT('Ctrl Pts',(5.17949452655395,4.35834164200837,-53.4744383142946));
#34725=CARTESIAN_POINT('Ctrl Pts',(5.06459006469176,4.4880080744831,-53.466315390538));
#34726=CARTESIAN_POINT('Ctrl Pts',(4.94969501309805,4.61766388773624,-53.4581931320201));
#34727=CARTESIAN_POINT('Ctrl Pts',(4.82980904049795,4.74291470176019,-53.4500708735022));
#34728=CARTESIAN_POINT('Ctrl Pts',(4.705315673836,4.8633623563902,-53.4419486149843));
#34729=CARTESIAN_POINT('Ctrl Pts',(4.58076338501893,4.98386701835788,-53.4338225122376));
#34730=CARTESIAN_POINT('Ctrl Pts',(4.45159960678405,5.09956372221323,-53.425696409491));
#34731=CARTESIAN_POINT('Ctrl Pts',(4.31824396242724,5.21009194553808,-53.4175703067444));
#34732=CARTESIAN_POINT('Ctrl Pts',(4.18485735873682,5.32064582867023,-53.409442317473));
#34733=CARTESIAN_POINT('Ctrl Pts',(4.04727723757417,5.42602861391727,-53.4013143282016));
#34734=CARTESIAN_POINT('Ctrl Pts',(3.90595485003789,5.52592125436705,-53.3931863389302));
#34735=CARTESIAN_POINT('Ctrl Pts',(3.76449776475138,5.62590910488345,-53.3850506026776));
#34736=CARTESIAN_POINT('Ctrl Pts',(3.61929159131145,5.72039615221774,-53.3769148664251));
#34737=CARTESIAN_POINT('Ctrl Pts',(3.47081568271612,5.80910728912901,-53.3687791301726));
#34738=CARTESIAN_POINT('Ctrl Pts',(3.34901356465853,5.88188141439495,-53.3621049840644));
#34739=CARTESIAN_POINT('Ctrl Pts',(3.22501158011935,5.9507692992674,-53.3554308379562));
#34740=CARTESIAN_POINT('Ctrl Pts',(3.0990855038472,6.01564277861013,-53.3487566918479));
#34741=CARTESIAN_POINT('Origin',(0.,0.,-63.6971797838103));
#34742=CARTESIAN_POINT('',(3.0990855038472,6.01564277861013,-50.9542788176482));
#34743=CARTESIAN_POINT('',(3.09908550384718,6.01564277861014,-51.3484212393497));
#34744=CARTESIAN_POINT('',(3.09908550384721,6.01564277861012,-63.6971797838103));
#34745=CARTESIAN_POINT('',(-6.76699979006582,0.00168560055385441,-52.3028202161503));
#34746=CARTESIAN_POINT('Ctrl Pts',(-6.76699979006581,0.00168560055384907,
-52.3028202161503));
#34747=CARTESIAN_POINT('Ctrl Pts',(-6.76704222219873,-0.16866213331645,
-52.2948235459384));
#34748=CARTESIAN_POINT('Ctrl Pts',(-6.76064800700029,-0.339088473983994,
-52.2868268757265));
#34749=CARTESIAN_POINT('Ctrl Pts',(-6.74782562800835,-0.509056277825701,
-52.2788302055146));
#34750=CARTESIAN_POINT('Ctrl Pts',(-6.73500408146496,-0.67901304709633,
-52.2708340544588));
#34751=CARTESIAN_POINT('Ctrl Pts',(-6.7157552265512,-0.848510960915059,
-52.262837903403));
#34752=CARTESIAN_POINT('Ctrl Pts',(-6.69013956762023,-1.01701601057322,
-52.2548417523472));
#34753=CARTESIAN_POINT('Ctrl Pts',(-6.68070580473756,-1.07907323452712,
-52.2518969210924));
#34754=CARTESIAN_POINT('Ctrl Pts',(-6.67040901238627,-1.14099585344223,
-52.2489520898375));
#34755=CARTESIAN_POINT('Ctrl Pts',(-6.65925397533337,-1.20275745352367,
-52.2460072585826));
#34756=CARTESIAN_POINT('Ctrl Pts',(-6.62660519921238,-1.38352248768456,
-52.2373882700576));
#34757=CARTESIAN_POINT('Ctrl Pts',(-6.58660376208147,-1.56289156319099,
-52.2287692815326));
#34758=CARTESIAN_POINT('Ctrl Pts',(-6.53940058769381,-1.74026692023662,
-52.2201502930077));
#34759=CARTESIAN_POINT('Ctrl Pts',(-6.49216913439221,-1.91774854095037,
-52.2115261409394));
#34760=CARTESIAN_POINT('Ctrl Pts',(-6.4377274116605,-2.09323376559209,-52.2029019888711));
#34761=CARTESIAN_POINT('Ctrl Pts',(-6.37627621605827,-2.2661400257993,-52.1942778368028));
#34762=CARTESIAN_POINT('Ctrl Pts',(-6.31272030048007,-2.44496837191978,
-52.1853583052069));
#34763=CARTESIAN_POINT('Ctrl Pts',(-6.24166638578727,-2.62103763086395,
-52.1764387736109));
#34764=CARTESIAN_POINT('Ctrl Pts',(-6.16339044666578,-2.79372640069656,
-52.1675192420149));
#34765=CARTESIAN_POINT('Ctrl Pts',(-6.08756570632921,-2.96100744872433,
-52.1588790241551));
#34766=CARTESIAN_POINT('Ctrl Pts',(-6.00496458775122,-3.12511627111526,
-52.1502388062953));
#34767=CARTESIAN_POINT('Ctrl Pts',(-5.91588470560768,-3.28551322474239,
-52.1415985884355));
#34768=CARTESIAN_POINT('Ctrl Pts',(-5.82248527358039,-3.45368794620801,
-52.1325393999714));
#34769=CARTESIAN_POINT('Ctrl Pts',(-5.7219633396515,-3.61778153595023,-52.1234802115074));
#34770=CARTESIAN_POINT('Ctrl Pts',(-5.61471324293254,-3.77720587202206,
-52.1144210230433));
#34771=CARTESIAN_POINT('Ctrl Pts',(-5.5074631462136,-3.93663020809387,-52.1053618345792));
#34772=CARTESIAN_POINT('Ctrl Pts',(-5.39348514028475,-4.09138500205531,
-52.0963026461151));
#34773=CARTESIAN_POINT('Ctrl Pts',(-5.27322252168265,-4.24092127217883,
-52.0872434576511));
#34774=CARTESIAN_POINT('Ctrl Pts',(-5.15316824962704,-4.39019848120908,
-52.0781999635952));
#34775=CARTESIAN_POINT('Ctrl Pts',(-5.02674118180533,-4.53441328467973,
-52.0691564695394));
#34776=CARTESIAN_POINT('Ctrl Pts',(-4.89437281339686,-4.67305079829887,
-52.0601129754835));
#34777=CARTESIAN_POINT('Ctrl Pts',(-4.76212552185087,-4.81156150069134,
-52.0510777534786));
#34778=CARTESIAN_POINT('Ctrl Pts',(-4.6239479439629,-4.94450492639516,-52.0420425314737));
#34779=CARTESIAN_POINT('Ctrl Pts',(-4.48030999396894,-5.07140132093113,
-52.0330073094688));
#34780=CARTESIAN_POINT('Ctrl Pts',(-4.33692510277304,-5.19807415164515,
-52.023988005558));
#34781=CARTESIAN_POINT('Ctrl Pts',(-4.18809922758639,-5.31872106758195,
-52.0149687016473));
#34782=CARTESIAN_POINT('Ctrl Pts',(-4.03433691479374,-5.43290112720014,
-52.0059493977366));
#34783=CARTESIAN_POINT('Ctrl Pts',(-3.88076750756243,-5.54693793995833,
-51.9969414091727));
#34784=CARTESIAN_POINT('Ctrl Pts',(-3.72227421261627,-5.65452394588214,
-51.9879334206087));
#34785=CARTESIAN_POINT('Ctrl Pts',(-3.55939421592283,-5.75525862282966,
-51.9789254320447));
#34786=CARTESIAN_POINT('Ctrl Pts',(-3.39688208940721,-5.8557657869808,-51.9699377883385));
#34787=CARTESIAN_POINT('Ctrl Pts',(-3.23000323957779,-5.94945238460827,
-51.9609501446322));
#34788=CARTESIAN_POINT('Ctrl Pts',(-3.0593229411224,-6.03596157558364,-51.9519625009259));
#34789=CARTESIAN_POINT('Ctrl Pts',(-2.9106722310024,-6.11130508497971,-51.9441348861905));
#34790=CARTESIAN_POINT('Ctrl Pts',(-2.75913860364769,-6.18120494807919,
-51.936307271455));
#34791=CARTESIAN_POINT('Ctrl Pts',(-2.60511347837555,-6.24545216655976,
-51.9284796567195));
#34792=CARTESIAN_POINT('Ctrl Pts',(-2.44527289609821,-6.31212513821611,
-51.9203564982741));
#34793=CARTESIAN_POINT('Ctrl Pts',(-2.28281992949351,-6.37267921076693,
-51.9122333398287));
#34794=CARTESIAN_POINT('Ctrl Pts',(-2.11826977509098,-6.42691389081385,
-51.9041101813833));
#34795=CARTESIAN_POINT('Ctrl Pts',(-1.95373122233573,-6.48114474703192,
-51.8959875956631));
#34796=CARTESIAN_POINT('Ctrl Pts',(-1.78709612394014,-6.52905698366225,
-51.8878650099429));
#34797=CARTESIAN_POINT('Ctrl Pts',(-1.61889633192939,-6.57049949900809,
-51.8797424242227));
#34798=CARTESIAN_POINT('Ctrl Pts',(-1.45067632898252,-6.61194699409868,
-51.8716188624902));
#34799=CARTESIAN_POINT('Ctrl Pts',(-1.28089161371526,-6.64692313351184,
-51.8634953007577));
#34800=CARTESIAN_POINT('Ctrl Pts',(-1.11008571625013,-6.67532761013101,
-51.8553717390253));
#34801=CARTESIAN_POINT('Ctrl Pts',(-0.939155406957264,-6.70375277604081,
-51.847242260242));
#34802=CARTESIAN_POINT('Ctrl Pts',(-0.767202791315418,-6.72559665880027,
-51.8391127814588));
#34803=CARTESIAN_POINT('Ctrl Pts',(-0.594778673665024,-6.74081058399903,
-51.8309833026756));
#34804=CARTESIAN_POINT('Ctrl Pts',(-0.422284261736473,-6.75603071164733,
-51.8228505096469));
#34805=CARTESIAN_POINT('Ctrl Pts',(-0.249318329956004,-6.76461547588664,
-51.8147177166183));
#34806=CARTESIAN_POINT('Ctrl Pts',(-0.0764329557722841,-6.7665683328606,
-51.8065849235896));
#34807=CARTESIAN_POINT('Ctrl Pts',(0.0966404050276211,-6.76852331327026,
-51.7984432873824));
#34808=CARTESIAN_POINT('Ctrl Pts',(0.269632667839708,-6.76383199327735,
-51.7903016511751));
#34809=CARTESIAN_POINT('Ctrl Pts',(0.441994851095807,-6.75254985554382,
-51.7821600149679));
#34810=CARTESIAN_POINT('Ctrl Pts',(0.529811042273336,-6.74680175961359,
-51.7780119619079));
#34811=CARTESIAN_POINT('Ctrl Pts',(0.617463792326182,-6.7393436725938,-51.773863908848));
#34812=CARTESIAN_POINT('Ctrl Pts',(0.704881448879159,-6.73018804663183,
-51.769715855788));
#34813=CARTESIAN_POINT('Ctrl Pts',(0.882764304366164,-6.71155761252841,
-51.76127514081));
#34814=CARTESIAN_POINT('Ctrl Pts',(1.06003951795542,-6.68585678030588,-51.7528344258319));
#34815=CARTESIAN_POINT('Ctrl Pts',(1.2361229175544,-6.65314129811601,-51.7443937108538));
#34816=CARTESIAN_POINT('Ctrl Pts',(1.41207322502415,-6.62045054382891,-51.7359593757658));
#34817=CARTESIAN_POINT('Ctrl Pts',(1.58683318762128,-6.58075576948503,-51.7275250406778));
#34818=CARTESIAN_POINT('Ctrl Pts',(1.75982538832982,-6.53416433850495,-51.7190907055898));
#34819=CARTESIAN_POINT('Ctrl Pts',(1.93271339830978,-6.48760096887746,-51.7106614503811));
#34820=CARTESIAN_POINT('Ctrl Pts',(2.10383544789739,-6.43414931024615,-51.7022321951725));
#34821=CARTESIAN_POINT('Ctrl Pts',(2.27262553283553,-6.37396753894339,-51.6938029399639));
#34822=CARTESIAN_POINT('Ctrl Pts',(2.44133984904713,-6.31381278283038,-51.6853774685909));
#34823=CARTESIAN_POINT('Ctrl Pts',(2.60772397429615,-6.24693404959369,-51.6769519972179));
#34824=CARTESIAN_POINT('Ctrl Pts',(2.77122788126819,-6.17353910087899,-51.6685265258449));
#34825=CARTESIAN_POINT('Ctrl Pts',(2.93468345174203,-6.10016584984035,-51.6601035452856));
#34826=CARTESIAN_POINT('Ctrl Pts',(3.09526019812638,-6.02028036136421,-51.6516805647264));
#34827=CARTESIAN_POINT('Ctrl Pts',(3.25242850190691,-5.9341383401454,-51.6432575841671));
#34828=CARTESIAN_POINT('Ctrl Pts',(3.40959940806831,-5.84799489259352,-51.6348344641408));
#34829=CARTESIAN_POINT('Ctrl Pts',(3.5633614633841,-5.75559485972933,-51.6264113441145));
#34830=CARTESIAN_POINT('Ctrl Pts',(3.71320948120089,-5.65723999391221,-51.6179882240881));
#34831=CARTESIAN_POINT('Ctrl Pts',(3.86306268101168,-5.55888172682004,-51.6095648127763));
#34832=CARTESIAN_POINT('Ctrl Pts',(4.00900129454074,-5.45456839904279,-51.6011414014645));
#34833=CARTESIAN_POINT('Ctrl Pts',(4.15054884657595,-5.34464528965086,-51.5927179901526));
#34834=CARTESIAN_POINT('Ctrl Pts',(4.29212103445023,-5.23470304853962,-51.5842931127765));
#34835=CARTESIAN_POINT('Ctrl Pts',(4.42930037375532,-5.11914928378067,-51.5758682354004));
#34836=CARTESIAN_POINT('Ctrl Pts',(4.56164294226869,-4.99837000103537,-51.5674433580243));
#34837=CARTESIAN_POINT('Ctrl Pts',(4.6940270073443,-4.87755284744411,-51.5590158389929));
#34838=CARTESIAN_POINT('Ctrl Pts',(4.82157103172609,-4.7515071338917,-51.5505883199615));
#34839=CARTESIAN_POINT('Ctrl Pts',(4.94386721032279,-4.62065644759434,-51.5421608009301));
#34840=CARTESIAN_POINT('Ctrl Pts',(5.06627305940608,-4.4896884194585,-51.5337257244254));
#34841=CARTESIAN_POINT('Ctrl Pts',(5.18342143138052,-4.35390705262337,-51.5252906479206));
#34842=CARTESIAN_POINT('Ctrl Pts',(5.29494341274326,-4.21377066958404,-51.5168555714158));
#34843=CARTESIAN_POINT('Ctrl Pts',(5.40651929341353,-4.07356655770854,-51.5084164181831));
#34844=CARTESIAN_POINT('Ctrl Pts',(5.51246315903988,-3.9290034976198,-51.4999772649503));
#34845=CARTESIAN_POINT('Ctrl Pts',(5.61244856850397,-3.78057007154976,-51.4915381117176));
#34846=CARTESIAN_POINT('Ctrl Pts',(5.71254508979103,-3.63197169432685,-51.4830895802195));
#34847=CARTESIAN_POINT('Ctrl Pts',(5.80666974468458,-3.47949463808175,-51.4746410487214));
#34848=CARTESIAN_POINT('Ctrl Pts',(5.89454069013699,-3.32365447246241,-51.4661925172233));
#34849=CARTESIAN_POINT('Ctrl Pts',(5.94309223848076,-3.23754772470849,-51.4615244294572));
#34850=CARTESIAN_POINT('Ctrl Pts',(5.98973540072815,-3.15041466906316,-51.4568563416911));
#34851=CARTESIAN_POINT('Ctrl Pts',(6.03442885626921,-3.06234507830608,-51.452188253925));
#34852=CARTESIAN_POINT('Ctrl Pts',(6.11332813070659,-2.90687205151481,-51.4439474783282));
#34853=CARTESIAN_POINT('Ctrl Pts',(6.18632401263804,-2.74813324297844,-51.4357067027315));
#34854=CARTESIAN_POINT('Ctrl Pts',(6.25313627486011,-2.58661472353897,-51.4274659271348));
#34855=CARTESIAN_POINT('Ctrl Pts',(6.31987453525838,-2.42527510337069,-51.4192342790904));
#34856=CARTESIAN_POINT('Ctrl Pts',(6.38044267881536,-2.26116222869414,-51.4110026310461));
#34857=CARTESIAN_POINT('Ctrl Pts',(6.43460616171242,-2.09478699242967,-51.4027709830017));
#34858=CARTESIAN_POINT('Ctrl Pts',(6.48871930511851,-1.9285663851561,-51.3945469854435));
#34859=CARTESIAN_POINT('Ctrl Pts',(6.53643953293929,-1.76008794008611,-51.3863229878852));
#34860=CARTESIAN_POINT('Ctrl Pts',(6.57758021521458,-1.58988286122523,-51.378098990327));
#34861=CARTESIAN_POINT('Ctrl Pts',(6.61868454953738,-1.41982815921224,-51.3698822587025));
#34862=CARTESIAN_POINT('Ctrl Pts',(6.65322084107363,-1.2480502083729,-51.361665527078));
#34863=CARTESIAN_POINT('Ctrl Pts',(6.68105219721329,-1.07509559487122,-51.3534487954535));
#34864=CARTESIAN_POINT('Ctrl Pts',(6.70886929431887,-0.902229592420915,
-51.3452362735648));
#34865=CARTESIAN_POINT('Ctrl Pts',(6.7299882411787,-0.72818847834672,-51.3370237516761));
#34866=CARTESIAN_POINT('Ctrl Pts',(6.74432308701853,-0.553529672112451,
-51.3288112297874));
#34867=CARTESIAN_POINT('Ctrl Pts',(6.7586531392169,-0.378929272623817,-51.3206014542056));
#34868=CARTESIAN_POINT('Ctrl Pts',(6.76620358071624,-0.203711946670291,
-51.3123916786238));
#34869=CARTESIAN_POINT('Ctrl Pts',(6.76694023251375,-0.0284409842788165,
-51.3041819030419));
#34870=CARTESIAN_POINT('Ctrl Pts',(6.76726198288057,0.0481128185252991,
-51.3005960863591));
#34871=CARTESIAN_POINT('Ctrl Pts',(6.76628452514981,0.124676802548317,-51.2970102696763));
#34872=CARTESIAN_POINT('Ctrl Pts',(6.76400813024382,0.201203911481814,-51.2934244529935));
#34873=CARTESIAN_POINT('Ctrl Pts',(6.75838432366806,0.390263225096315,-51.2845657354717));
#34874=CARTESIAN_POINT('Ctrl Pts',(6.74483520472732,0.578901465519504,-51.2757070179499));
#34875=CARTESIAN_POINT('Ctrl Pts',(6.72345224154194,0.766471757930234,-51.2668483004281));
#34876=CARTESIAN_POINT('Ctrl Pts',(6.70202927426651,0.954392964234585,-51.2579730096685));
#34877=CARTESIAN_POINT('Ctrl Pts',(6.67274320337633,1.1412419720629,-51.2490977189089));
#34878=CARTESIAN_POINT('Ctrl Pts',(6.63573668356482,1.3263814181419,-51.2402224281493));
#34879=CARTESIAN_POINT('Ctrl Pts',(6.5986250569168,1.51204670187304,-51.2313219295685));
#34880=CARTESIAN_POINT('Ctrl Pts',(6.55374915226288,1.69599245141979,-51.2224214309877));
#34881=CARTESIAN_POINT('Ctrl Pts',(6.50130249978103,1.87759282229693,-51.2135209324069));
#34882=CARTESIAN_POINT('Ctrl Pts',(6.4487848501955,2.05943902583927,-51.2046083852093));
#34883=CARTESIAN_POINT('Ctrl Pts',(6.38867605897881,2.23893326127338,-51.1956958380116));
#34884=CARTESIAN_POINT('Ctrl Pts',(6.32121859672582,2.41546775023134,-51.186783290814));
#34885=CARTESIAN_POINT('Ctrl Pts',(6.25361218180803,2.59239204458193,-51.1778510638417));
#34886=CARTESIAN_POINT('Ctrl Pts',(6.17862473295434,2.76634327730635,-51.1689188368694));
#34887=CARTESIAN_POINT('Ctrl Pts',(6.09654684536151,2.93673382558118,-51.1599866098971));
#34888=CARTESIAN_POINT('Ctrl Pts',(6.01897376357476,3.09777256968948,-51.151544623952));
#34889=CARTESIAN_POINT('Ctrl Pts',(5.93506767619839,3.25563080195445,-51.143102638007));
#34890=CARTESIAN_POINT('Ctrl Pts',(5.84511032528628,3.40983493518847,-51.1346606520619));
#34891=CARTESIAN_POINT('Ctrl Pts',(5.75748275492568,3.56004537822453,-51.126437302776));
#34892=CARTESIAN_POINT('Ctrl Pts',(5.66394502973031,3.70707493802655,-51.1182139534901));
#34893=CARTESIAN_POINT('Ctrl Pts',(5.56475447860908,3.85042810513327,-51.1099906042042));
#34894=CARTESIAN_POINT('Ctrl Pts',(5.46566367724758,3.99363711088779,-51.1017755246286));
#34895=CARTESIAN_POINT('Ctrl Pts',(5.3609315701396,4.13317679234455,-51.0935604450529));
#34896=CARTESIAN_POINT('Ctrl Pts',(5.25086098479114,4.26857680244812,-51.0853453654773));
#34897=CARTESIAN_POINT('Ctrl Pts',(5.14088108712865,4.40386525583054,-51.0771370543453));
#34898=CARTESIAN_POINT('Ctrl Pts',(5.02557169463353,4.53502055289682,-51.0689287432133));
#34899=CARTESIAN_POINT('Ctrl Pts',(4.90527851016717,4.66160184246705,-51.0607204320813));
#34900=CARTESIAN_POINT('Ctrl Pts',(4.78506257820663,4.78810184129871,-51.0525173923419));
#34901=CARTESIAN_POINT('Ctrl Pts',(4.65986947517496,4.91003342419929,-51.0443143526025));
#34902=CARTESIAN_POINT('Ctrl Pts',(4.53008473553831,5.02698928672449,-51.0361113128631));
#34903=CARTESIAN_POINT('Ctrl Pts',(4.40035875462369,5.14389219867141,-51.0279119869666));
#34904=CARTESIAN_POINT('Ctrl Pts',(4.26604554444756,5.25582363856319,-51.0197126610701));
#34905=CARTESIAN_POINT('Ctrl Pts',(4.12756704767444,5.36241356731763,-51.0115133351736));
#34906=CARTESIAN_POINT('Ctrl Pts',(3.98912446940028,5.46897584881755,-51.0033161360151));
#34907=CARTESIAN_POINT('Ctrl Pts',(3.84651904166094,5.57019916198439,-50.9951189368566));
#34908=CARTESIAN_POINT('Ctrl Pts',(3.70020534501819,5.66575408967763,-50.9869217376981));
#34909=CARTESIAN_POINT('Ctrl Pts',(3.55388787310107,5.76131148293684,-50.9787243270305));
#34910=CARTESIAN_POINT('Ctrl Pts',(3.40386223999461,5.85120000058006,-50.9705269163629));
#34911=CARTESIAN_POINT('Ctrl Pts',(3.25061171475611,5.93513373732137,-50.9623295056953));
#34912=CARTESIAN_POINT('Ctrl Pts',(3.20044253240569,5.96261088258645,-50.9596459430129));
#34913=CARTESIAN_POINT('Ctrl Pts',(3.14992794992446,5.98945021807804,-50.9569623803306));
#34914=CARTESIAN_POINT('Ctrl Pts',(3.0990855038472,6.01564277861013,-50.9542788176482));
#34915=CARTESIAN_POINT('Ctrl Pts',(3.09908550384721,6.01564277861012,-52.953975806663));
#34916=CARTESIAN_POINT('Ctrl Pts',(2.94671772071282,6.09413826202614,-52.9459325567485));
#34917=CARTESIAN_POINT('Ctrl Pts',(2.79124015761376,6.16690566284332,-52.9378893068339));
#34918=CARTESIAN_POINT('Ctrl Pts',(2.63313311030458,6.23369064226143,-52.9298460569193));
#34919=CARTESIAN_POINT('Ctrl Pts',(2.47509990216388,6.30044443175201,-52.9218065633641));
#34920=CARTESIAN_POINT('Ctrl Pts',(2.31443999788565,6.36122121755229,-52.9137670698089));
#34921=CARTESIAN_POINT('Ctrl Pts',(2.15165623983891,6.41581362147953,-52.9057275762537));
#34922=CARTESIAN_POINT('Ctrl Pts',(1.98888382565985,6.4704022210407,-52.8976886429445));
#34923=CARTESIAN_POINT('Ctrl Pts',(1.8239882027693,6.51880716831367,-52.8896497096353));
#34924=CARTESIAN_POINT('Ctrl Pts',(1.65749021622967,6.56087000199691,-52.8816107763261));
#34925=CARTESIAN_POINT('Ctrl Pts',(1.49098986403336,6.60293343332236,-52.8735717287971));
#34926=CARTESIAN_POINT('Ctrl Pts',(1.32288746473816,6.63865447925112,-52.8655326812682));
#34927=CARTESIAN_POINT('Ctrl Pts',(1.15371665645136,6.66792523028166,-52.8574936337392));
#34928=CARTESIAN_POINT('Ctrl Pts',(0.98450995214953,6.69720219221424,-52.8494528804209));
#34929=CARTESIAN_POINT('Ctrl Pts',(0.814234755517338,6.72002607104307,-52.8414121271026));
#34930=CARTESIAN_POINT('Ctrl Pts',(0.643432323578413,6.7363405380796,-52.8333713737842));
#34931=CARTESIAN_POINT('Ctrl Pts',(0.472559823838546,6.75266169775402,-52.8253273219303));
#34932=CARTESIAN_POINT('Ctrl Pts',(0.301160029581996,6.7624680949701,-52.8172832700763));
#34933=CARTESIAN_POINT('Ctrl Pts',(0.129776564540633,6.76575546729972,-52.8092392182224));
#34934=CARTESIAN_POINT('Ctrl Pts',(-0.04181352272107,6.76904680292982,-52.8011854683509));
#34935=CARTESIAN_POINT('Ctrl Pts',(-0.21338686816161,6.7658034131288,-52.7931317184794));
#34936=CARTESIAN_POINT('Ctrl Pts',(-0.384401786763039,6.75607313950444,
-52.7850779686079));
#34937=CARTESIAN_POINT('Ctrl Pts',(-0.555530896877247,6.74633636870034,
-52.7770188410191));
#34938=CARTESIAN_POINT('Ctrl Pts',(-0.726100467547313,6.73010412384681,
-52.7689597134303));
#34939=CARTESIAN_POINT('Ctrl Pts',(-0.895577197395139,6.70747571620695,
-52.7609005858415));
#34940=CARTESIAN_POINT('Ctrl Pts',(-1.06531579411278,6.68481234429628,-52.7528290056965));
#34941=CARTESIAN_POINT('Ctrl Pts',(-1.23395781225078,6.65573313888357,-52.7447574255514));
#34942=CARTESIAN_POINT('Ctrl Pts',(-1.40098241985301,6.620387999148,-52.7366858454064));
#34943=CARTESIAN_POINT('Ctrl Pts',(-1.5002200628672,6.59938769021317,-52.7318901173966));
#34944=CARTESIAN_POINT('Ctrl Pts',(-1.59888704844799,6.57617636648305,-52.7270943893869));
#34945=CARTESIAN_POINT('Ctrl Pts',(-1.69687740114419,6.55079354624203,-52.7222986613771));
#34946=CARTESIAN_POINT('Ctrl Pts',(-1.8671614921318,6.50668419922451,-52.7139648186845));
#34947=CARTESIAN_POINT('Ctrl Pts',(-2.03594244851621,6.45587460051241,-52.7056309759919));
#34948=CARTESIAN_POINT('Ctrl Pts',(-2.20266244707944,6.39848162802911,-52.6972971332993));
#34949=CARTESIAN_POINT('Ctrl Pts',(-2.36918594503202,6.34115630042487,-52.6889731130946));
#34950=CARTESIAN_POINT('Ctrl Pts',(-2.53365299804881,6.27726316861511,-52.68064909289));
#34951=CARTESIAN_POINT('Ctrl Pts',(-2.6955178415194,6.20696967658539,-52.6723250726853));
#34952=CARTESIAN_POINT('Ctrl Pts',(-2.85722158447954,6.1367461461187,-52.6640093371945));
#34953=CARTESIAN_POINT('Ctrl Pts',(-3.01632796080577,6.06013508456906,-52.6556936017037));
#34954=CARTESIAN_POINT('Ctrl Pts',(-3.17230798206915,5.97735318237933,-52.6473778662128));
#34955=CARTESIAN_POINT('Ctrl Pts',(-3.32816133942105,5.89463850341119,-52.6390688835329));
#34956=CARTESIAN_POINT('Ctrl Pts',(-3.48089309451044,5.80576313114855,-52.6307599008529));
#34957=CARTESIAN_POINT('Ctrl Pts',(-3.62999560460828,5.71099123712553,-52.6224509181729));
#34958=CARTESIAN_POINT('Ctrl Pts',(-3.77900434012526,5.61627894769692,-52.6141471612358));
#34959=CARTESIAN_POINT('Ctrl Pts',(-3.92438808676057,5.51567771318103,-52.6058434042986));
#34960=CARTESIAN_POINT('Ctrl Pts',(-4.06566492689051,5.40949699161136,-52.5975396473614));
#34961=CARTESIAN_POINT('Ctrl Pts',(-4.20688441202795,5.30335937685584,-52.5892392615495));
#34962=CARTESIAN_POINT('Ctrl Pts',(-4.34400003529086,5.19164699714928,-52.5809388757375));
#34963=CARTESIAN_POINT('Ctrl Pts',(-4.47655969970676,5.07471203665403,-52.5726384899255));
#34964=CARTESIAN_POINT('Ctrl Pts',(-4.60909141073858,4.95780173469936,-52.564339854449));
#34965=CARTESIAN_POINT('Ctrl Pts',(-4.73706881627237,4.83567127596755,-52.5560412189724));
#34966=CARTESIAN_POINT('Ctrl Pts',(-4.86007351528718,4.70871260813443,-52.5477425834958));
#34967=CARTESIAN_POINT('Ctrl Pts',(-4.98307269317888,4.58175963890015,-52.5394443205074));
#34968=CARTESIAN_POINT('Ctrl Pts',(-5.10109936747627,4.44997914231351,-52.5311460575189));
#34969=CARTESIAN_POINT('Ctrl Pts',(-5.21377244339826,4.31379947476247,-52.5228477945305));
#34970=CARTESIAN_POINT('Ctrl Pts',(-5.32645916355048,4.17760331643294,-52.5145485266577));
#34971=CARTESIAN_POINT('Ctrl Pts',(-5.43379077228881,4.03700719395469,-52.5062492587849));
#34972=CARTESIAN_POINT('Ctrl Pts',(-5.53542674950234,3.89247218370202,-52.4979499909121));
#34973=CARTESIAN_POINT('Ctrl Pts',(-5.63713409155239,3.74783568657767,-52.4896448956156));
#34974=CARTESIAN_POINT('Ctrl Pts',(-5.73313761057706,3.59925506009198,-52.4813398003192));
#34975=CARTESIAN_POINT('Ctrl Pts',(-5.82313989610666,3.44722072840875,-52.4730347050228));
#34976=CARTESIAN_POINT('Ctrl Pts',(-5.91317500114936,3.29513095710296,-52.4647265812568));
#34977=CARTESIAN_POINT('Ctrl Pts',(-5.99720434021798,3.13958527344085,-52.4564184574908));
#34978=CARTESIAN_POINT('Ctrl Pts',(-6.07497661005813,2.98109848667344,-52.4481103337248));
#34979=CARTESIAN_POINT('Ctrl Pts',(-6.15283155137186,2.82244322936722,-52.4397933784712));
#34980=CARTESIAN_POINT('Ctrl Pts',(-6.22441598780934,2.66084093815967,-52.4314764232176));
#34981=CARTESIAN_POINT('Ctrl Pts',(-6.28952645710395,2.4968271757151,-52.423159467964));
#34982=CARTESIAN_POINT('Ctrl Pts',(-6.33751188234869,2.37595152818625,-52.4170299984807));
#34983=CARTESIAN_POINT('Ctrl Pts',(-6.38198199989548,2.25376651867671,-52.4109005289974));
#34984=CARTESIAN_POINT('Ctrl Pts',(-6.42287277311734,2.13049157246586,-52.4047710595141));
#34985=CARTESIAN_POINT('Ctrl Pts',(-6.48252027860105,1.95067000268968,-52.3958299822047));
#34986=CARTESIAN_POINT('Ctrl Pts',(-6.53464595542439,1.7682396727302,-52.3868889048954));
#34987=CARTESIAN_POINT('Ctrl Pts',(-6.57904187216683,1.58382355212808,-52.377947827586));
#34988=CARTESIAN_POINT('Ctrl Pts',(-6.6233814392243,1.3996415023834,-52.3690180987727));
#34989=CARTESIAN_POINT('Ctrl Pts',(-6.66001076183165,1.21347893703743,-52.3600883699595));
#34990=CARTESIAN_POINT('Ctrl Pts',(-6.68877173731219,1.0259735114191,-52.3511586411462));
#34991=CARTESIAN_POINT('Ctrl Pts',(-6.71747212389303,0.838863091437286,
-52.3422477240191));
#34992=CARTESIAN_POINT('Ctrl Pts',(-6.7383372084734,0.650415708016407,-52.333336806892));
#34993=CARTESIAN_POINT('Ctrl Pts',(-6.75125997573567,0.461278375852977,
-52.3244258897648));
#34994=CARTESIAN_POINT('Ctrl Pts',(-6.76170428381188,0.308415716815962,
-52.3172239985732));
#34995=CARTESIAN_POINT('Ctrl Pts',(-6.76696157518998,0.155102687705959,
-52.3100221073816));
#34996=CARTESIAN_POINT('Ctrl Pts',(-6.7669997900656,0.00168560139907666,
-52.30282021619));
#34997=CARTESIAN_POINT('',(-6.76699988382611,0.00125391286841605,-52.6971797837818));
#34998=CARTESIAN_POINT('Ctrl Pts',(3.0990855038472,6.01564277861013,-53.3487566918479));
#34999=CARTESIAN_POINT('Ctrl Pts',(2.99319764624946,6.07019314614216,-53.3431445815241));
#35000=CARTESIAN_POINT('Ctrl Pts',(2.88594953658319,6.12190541594522,-53.3375324712002));
#35001=CARTESIAN_POINT('Ctrl Pts',(2.77750956863615,6.17071548494457,-53.3319203608763));
#35002=CARTESIAN_POINT('Ctrl Pts',(2.61441390448676,6.24412670749781,-53.3234796459085));
#35003=CARTESIAN_POINT('Ctrl Pts',(2.44828550491286,6.31112214687189,-53.3150389309408));
#35004=CARTESIAN_POINT('Ctrl Pts',(2.27965724571934,6.37145602213806,-53.306598215973));
#35005=CARTESIAN_POINT('Ctrl Pts',(2.11115644371377,6.43174429421697,-53.2981638808955));
#35006=CARTESIAN_POINT('Ctrl Pts',(1.94015986151861,6.48538092748719,-53.2897295458181));
#35007=CARTESIAN_POINT('Ctrl Pts',(1.7672205103348,6.5321681444871,-53.2812952107406));
#35008=CARTESIAN_POINT('Ctrl Pts',(1.59438531805329,6.57892718221416,-53.2728659555427));
#35009=CARTESIAN_POINT('Ctrl Pts',(1.41961001059839,6.61884494123383,-53.2644367003449));
#35010=CARTESIAN_POINT('Ctrl Pts',(1.24346330579621,6.6517732979363,-53.256007445147));
#35011=CARTESIAN_POINT('Ctrl Pts',(1.06739567206154,6.68468687332158,-53.247581973785));
#35012=CARTESIAN_POINT('Ctrl Pts',(0.889958195636715,6.71061724106131,-53.2391565024229));
#35013=CARTESIAN_POINT('Ctrl Pts',(0.711730739017968,6.72946716725306,-53.2307310310608));
#35014=CARTESIAN_POINT('Ctrl Pts',(0.533555971609326,6.74831152085942,-53.2223080505127));
#35015=CARTESIAN_POINT('Ctrl Pts',(0.354592020952775,6.76007957217432,-53.2138850699646));
#35016=CARTESIAN_POINT('Ctrl Pts',(0.175425237951395,6.76472578793034,-53.2054620894164));
#35017=CARTESIAN_POINT('Ctrl Pts',(-0.00374451167684181,6.76937208061796,
-53.1970389694014));
#35018=CARTESIAN_POINT('Ctrl Pts',(-0.183116767313299,6.7668962868897,-53.1886158493863));
#35019=CARTESIAN_POINT('Ctrl Pts',(-0.362103120012962,6.75730496059464,
-53.1801927293712));
#35020=CARTESIAN_POINT('Ctrl Pts',(-0.541095662357151,6.74771330261563,
-53.1717693180707));
#35021=CARTESIAN_POINT('Ctrl Pts',(-0.71970194211908,6.73100563912223,-53.1633459067702));
#35022=CARTESIAN_POINT('Ctrl Pts',(-0.897336459140573,6.70724058604558,
-53.1549224954697));
#35023=CARTESIAN_POINT('Ctrl Pts',(-1.07500189280553,6.68347139674764,-53.146497618105));
#35024=CARTESIAN_POINT('Ctrl Pts',(-1.25169489599059,6.65264241319582,-53.1380727407404));
#35025=CARTESIAN_POINT('Ctrl Pts',(-1.42683760609694,6.61486382670328,-53.1296478633757));
#35026=CARTESIAN_POINT('Ctrl Pts',(-1.60203523292746,6.57707339457804,-53.1212203443557));
#35027=CARTESIAN_POINT('Ctrl Pts',(-1.77568127166105,6.53232908531064,-53.1127928253357));
#35028=CARTESIAN_POINT('Ctrl Pts',(-1.9472101598671,6.4807917412389,-53.1043653063157));
#35029=CARTESIAN_POINT('Ctrl Pts',(-2.11889286855081,6.42920818046882,-53.0959302298224));
#35030=CARTESIAN_POINT('Ctrl Pts',(-2.2884543133863,6.37081950879481,-53.0874951533291));
#35031=CARTESIAN_POINT('Ctrl Pts',(-2.45534506196263,6.30583615603004,-53.0790600768357));
#35032=CARTESIAN_POINT('Ctrl Pts',(-2.6223164699364,6.24082139638309,-53.0706209236144));
#35033=CARTESIAN_POINT('Ctrl Pts',(-2.78661429978894,6.16920572749927,-53.0621817703931));
#35034=CARTESIAN_POINT('Ctrl Pts',(-2.94771059564376,6.09124710090877,-53.0537426171718));
#35035=CARTESIAN_POINT('Ctrl Pts',(-3.10898591465231,6.01320184042568,-53.045294085685));
#35036=CARTESIAN_POINT('Ctrl Pts',(-3.26705229410281,5.92879969030739,-53.0368455541982));
#35037=CARTESIAN_POINT('Ctrl Pts',(-3.42140673824391,5.83834436561421,-53.0283970227115));
#35038=CARTESIAN_POINT('Ctrl Pts',(-3.50669257922616,5.78836486239545,-53.023728934812));
#35039=CARTESIAN_POINT('Ctrl Pts',(-3.59084569318444,5.73653815171483,-53.0190608469127));
#35040=CARTESIAN_POINT('Ctrl Pts',(-3.67378519826791,5.68292101977387,-53.0143927590132));
#35041=CARTESIAN_POINT('Ctrl Pts',(-3.8202018606275,5.58826839921398,-53.0061519834125));
#35042=CARTESIAN_POINT('Ctrl Pts',(-3.96316034508716,5.48782299183043,-52.9979112078117));
#35043=CARTESIAN_POINT('Ctrl Pts',(-4.10217389612254,5.38186383383776,-52.9896704322109));
#35044=CARTESIAN_POINT('Ctrl Pts',(-4.2410334745788,5.27602203710028,-52.9814387841626));
#35045=CARTESIAN_POINT('Ctrl Pts',(-4.37595653949345,5.16467886384185,-52.9732071361142));
#35046=CARTESIAN_POINT('Ctrl Pts',(-4.5064833229646,5.04815778872273,-52.9649754880659));
#35047=CARTESIAN_POINT('Ctrl Pts',(-4.63688879496296,4.93174500818391,-52.9567514905037));
#35048=CARTESIAN_POINT('Ctrl Pts',(-4.76290585886092,4.81016414525168,-52.9485274929414));
#35049=CARTESIAN_POINT('Ctrl Pts',(-4.88410593182653,4.68378033715255,-52.9403034953792));
#35050=CARTESIAN_POINT('Ctrl Pts',(-5.00519892405635,4.55750818963937,-52.9320867637508));
#35051=CARTESIAN_POINT('Ctrl Pts',(-5.12148316235565,4.42644181035422,-52.9238700321225));
#35052=CARTESIAN_POINT('Ctrl Pts',(-5.23256530501393,4.29098465725112,-52.9156533004941));
#35053=CARTESIAN_POINT('Ctrl Pts',(-5.34359053617773,4.15559690386283,-52.9074407786015));
#35054=CARTESIAN_POINT('Ctrl Pts',(-5.44941875472911,4.01582313131885,-52.899228256709));
#35055=CARTESIAN_POINT('Ctrl Pts',(-5.54969518995384,3.8721017934196,-52.8910157348164));
#35056=CARTESIAN_POINT('Ctrl Pts',(-5.64993809225506,3.7284285166288,-52.8828059592308));
#35057=CARTESIAN_POINT('Ctrl Pts',(-5.74463270632478,3.58081059571235,-52.8745961836452));
#35058=CARTESIAN_POINT('Ctrl Pts',(-5.83346604690986,3.42971760930108,-52.8663864080595));
#35059=CARTESIAN_POINT('Ctrl Pts',(-5.8722661418999,3.36372411872112,-52.8628005914003));
#35060=CARTESIAN_POINT('Ctrl Pts',(-5.90994862520771,3.29706806537326,-52.859214774741));
#35061=CARTESIAN_POINT('Ctrl Pts',(-5.9464900521143,3.22979025017194,-52.8556289580817));
#35062=CARTESIAN_POINT('Ctrl Pts',(-6.03671973994501,3.06366492947592,-52.8467747029205));
#35063=CARTESIAN_POINT('Ctrl Pts',(-6.11989614724476,2.8939185407244,-52.8379204477593));
#35064=CARTESIAN_POINT('Ctrl Pts',(-6.19577291945262,2.72115544035573,-52.8290661925981));
#35065=CARTESIAN_POINT('Ctrl Pts',(-6.27179059181142,2.5480715257746,-52.8201954954369));
#35066=CARTESIAN_POINT('Ctrl Pts',(-6.34048143590617,2.37195994293093,-52.8113247982758));
#35067=CARTESIAN_POINT('Ctrl Pts',(-6.40164811785171,2.19344258534517,-52.8024541011146));
#35068=CARTESIAN_POINT('Ctrl Pts',(-6.46298755491246,2.01442103518764,-52.7935583501453));
#35069=CARTESIAN_POINT('Ctrl Pts',(-6.51676022021659,1.83298036107809,-52.784662599176));
#35070=CARTESIAN_POINT('Ctrl Pts',(-6.56281854556193,1.6497580846986,-52.7757668482068));
#35071=CARTESIAN_POINT('Ctrl Pts',(-6.60893902019319,1.46628857541269,-52.7668590936623));
#35072=CARTESIAN_POINT('Ctrl Pts',(-6.64732430461649,1.28103291561712,-52.7579513391179));
#35073=CARTESIAN_POINT('Ctrl Pts',(-6.67787821435154,1.0946376360646,-52.7490435845735));
#35074=CARTESIAN_POINT('Ctrl Pts',(-6.70849946755582,0.907831525136283,
-52.7401161965648));
#35075=CARTESIAN_POINT('Ctrl Pts',(-6.731254779247,0.71988102823706,-52.7311888085561));
#35076=CARTESIAN_POINT('Ctrl Pts',(-6.74609969577474,0.531439455317279,
-52.7222614205475));
#35077=CARTESIAN_POINT('Ctrl Pts',(-6.76000203777315,0.354962936331661,
-52.7139008749683));
#35078=CARTESIAN_POINT('Ctrl Pts',(-6.76696712271792,0.178055918259438,
-52.7055403293892));
#35079=CARTESIAN_POINT('Ctrl Pts',(-6.766999883826,0.0012539134656088,-52.69717978381));
#35080=CARTESIAN_POINT('Ctrl Pts',(-6.76699988382611,0.00125391286840704,
-52.6971797837818));
#35081=CARTESIAN_POINT('Ctrl Pts',(-6.76700029478462,-0.000963909669029427,
-52.697074908238));
#35082=CARTESIAN_POINT('Ctrl Pts',(-6.76699961543752,-0.0031817380629446,
-52.6969700326941));
#35083=CARTESIAN_POINT('Ctrl Pts',(-6.76699784576786,-0.00539957157367193,
-52.6968651571502));
#35084=CARTESIAN_POINT('Ctrl Pts',(-6.76685907444447,-0.179314341218538,
-52.6886411827333));
#35085=CARTESIAN_POINT('Ctrl Pts',(-6.76001128430234,-0.353454329022078,
-52.6804172083163));
#35086=CARTESIAN_POINT('Ctrl Pts',(-6.74642750524413,-0.527261715361,-52.6721932338993));
#35087=CARTESIAN_POINT('Ctrl Pts',(-6.73285807197459,-0.700885544236132,
-52.6639779447973));
#35088=CARTESIAN_POINT('Ctrl Pts',(-6.71256684358021,-0.874177116575075,
-52.6557626556952));
#35089=CARTESIAN_POINT('Ctrl Pts',(-6.68557884092691,-1.04657754693592,
-52.6475473665932));
#35090=CARTESIAN_POINT('Ctrl Pts',(-6.65861392700485,-1.21883048556674,
-52.6393391058216));
#35091=CARTESIAN_POINT('Ctrl Pts',(-6.62496370427886,-1.39019344831153,
-52.6311308450501));
#35092=CARTESIAN_POINT('Ctrl Pts',(-6.58470508469999,-1.56011151765705,
-52.6229225842785));
#35093=CARTESIAN_POINT('Ctrl Pts',(-6.54447283438675,-1.72991829121661,
-52.6147196998912));
#35094=CARTESIAN_POINT('Ctrl Pts',(-6.49764089147426,-1.89828170881955,
-52.606516815504));
#35095=CARTESIAN_POINT('Ctrl Pts',(-6.44433746334812,-2.06465582083017,
-52.5983139311167));
#35096=CARTESIAN_POINT('Ctrl Pts',(-6.39105826249282,-2.23095431311399,
-52.5901147750731));
#35097=CARTESIAN_POINT('Ctrl Pts',(-6.33131354563359,-2.39526496035845,
-52.5819156190296));
#35098=CARTESIAN_POINT('Ctrl Pts',(-6.26528173009178,-2.5570556979812,-52.573716462986));
#35099=CARTESIAN_POINT('Ctrl Pts',(-6.19925565771237,-2.71883236374372,
-52.5655180200697));
#35100=CARTESIAN_POINT('Ctrl Pts',(-6.12694370334506,-2.87808922146103,
-52.5573195771533));
#35101=CARTESIAN_POINT('Ctrl Pts',(-6.04857304747007,-3.03431262222907,
-52.549121134237));
#35102=CARTESIAN_POINT('Ctrl Pts',(-5.9702031720742,-3.19053446719664,-52.5409227729674));
#35103=CARTESIAN_POINT('Ctrl Pts',(-5.88577487524587,-3.34372259429593,
-52.5327244116979));
#35104=CARTESIAN_POINT('Ctrl Pts',(-5.79556202206993,-3.49338658730189,
-52.5245260504283));
#35105=CARTESIAN_POINT('Ctrl Pts',(-5.70533367949665,-3.64307627736733,
-52.5163262815138));
#35106=CARTESIAN_POINT('Ctrl Pts',(-5.60931898701095,-3.78924032061379,
-52.5081265125992));
#35107=CARTESIAN_POINT('Ctrl Pts',(-5.50783601493496,-3.93141595771618,
-52.4999267436846));
#35108=CARTESIAN_POINT('Ctrl Pts',(-5.40631718309977,-4.07364183363209,
-52.491724077321));
#35109=CARTESIAN_POINT('Ctrl Pts',(-5.29932643084953,-4.21187620421581,
-52.4835214109574));
#35110=CARTESIAN_POINT('Ctrl Pts',(-5.18722312521175,-4.34568812149106,
-52.4753187445938));
#35111=CARTESIAN_POINT('Ctrl Pts',(-5.07499249823927,-4.4796520156577,-52.4671067620515));
#35112=CARTESIAN_POINT('Ctrl Pts',(-4.95763794804585,-4.60918314670217,
-52.4588947795091));
#35113=CARTESIAN_POINT('Ctrl Pts',(-4.83555755688677,-4.7338855197433,-52.4506827969668));
#35114=CARTESIAN_POINT('Ctrl Pts',(-4.71340516106317,-4.85866144392928,
-52.4424659708862));
#35115=CARTESIAN_POINT('Ctrl Pts',(-4.58652162829243,-4.97860268690591,
-52.4342491448056));
#35116=CARTESIAN_POINT('Ctrl Pts',(-4.45533926818216,-5.09335262920152,
-52.426032318725));
#35117=CARTESIAN_POINT('Ctrl Pts',(-4.32395460592637,-5.20827953248111,
-52.4178028211119));
#35118=CARTESIAN_POINT('Ctrl Pts',(-4.18825814709303,-5.3179989113675,-52.4095733234987));
#35119=CARTESIAN_POINT('Ctrl Pts',(-4.04871346690596,-5.42219588938783,
-52.4013438258856));
#35120=CARTESIAN_POINT('Ctrl Pts',(-3.92432928465839,-5.51507263600657,
-52.3940084023528));
#35121=CARTESIAN_POINT('Ctrl Pts',(-3.79688817561486,-5.60356225692823,
-52.38667297882));
#35122=CARTESIAN_POINT('Ctrl Pts',(-3.66673498003497,-5.68747251300505,
-52.3793375552872));
#35123=CARTESIAN_POINT('Ctrl Pts',(-3.52353267668539,-5.77979557807707,
-52.3712666851003));
#35124=CARTESIAN_POINT('Ctrl Pts',(-3.37657972706634,-5.86687518962925,
-52.3631958149133));
#35125=CARTESIAN_POINT('Ctrl Pts',(-3.22630413519261,-5.94838218570723,
-52.3551249447264));
#35126=CARTESIAN_POINT('Ctrl Pts',(-3.07621554961226,-6.029787752664,-52.3470641181101));
#35127=CARTESIAN_POINT('Ctrl Pts',(-2.92281287269902,-6.10563432685951,
-52.3390032914938));
#35128=CARTESIAN_POINT('Ctrl Pts',(-2.76655482863393,-6.17563465403859,
-52.3309424648774));
#35129=CARTESIAN_POINT('Ctrl Pts',(-2.6104569705547,-6.24556322125493,-52.322889901717));
#35130=CARTESIAN_POINT('Ctrl Pts',(-2.45150990799485,-6.30965731695414,
-52.3148373385566));
#35131=CARTESIAN_POINT('Ctrl Pts',(-2.29019874499602,-6.36767451338546,
-52.3067847753962));
#35132=CARTESIAN_POINT('Ctrl Pts',(-2.12901762696162,-6.42564493782588,
-52.2987387040078));
#35133=CARTESIAN_POINT('Ctrl Pts',(-1.96547655106936,-6.47754808820998,
-52.2906926326193));
#35134=CARTESIAN_POINT('Ctrl Pts',(-1.80008238183293,-6.52318882285456,
-52.2826465612309));
#35135=CARTESIAN_POINT('Ctrl Pts',(-1.63478537108558,-6.56880274648858,
-52.2746052163945));
#35136=CARTESIAN_POINT('Ctrl Pts',(-1.46763779269884,-6.6081614788189,-52.2665638715581));
#35137=CARTESIAN_POINT('Ctrl Pts',(-1.29916342247539,-6.64111913774343,
-52.2585225267216));
#35138=CARTESIAN_POINT('Ctrl Pts',(-1.12744138480924,-6.67471211891748,
-52.2503261695009));
#35139=CARTESIAN_POINT('Ctrl Pts',(-0.954341253873892,-6.70165459061485,
-52.2421298122802));
#35140=CARTESIAN_POINT('Ctrl Pts',(-0.780430991748114,-6.7218462097194,
-52.2339334550594));
#35141=CARTESIAN_POINT('Ctrl Pts',(-0.609864017430613,-6.74164966085067,
-52.2258946663504));
#35142=CARTESIAN_POINT('Ctrl Pts',(-0.438518164373885,-6.75495944178028,
-52.2178558776413));
#35143=CARTESIAN_POINT('Ctrl Pts',(-0.266936234653601,-6.76173306531905,
-52.2098170889323));
#35144=CARTESIAN_POINT('Ctrl Pts',(-0.0953359441126302,-6.7685074136969,
-52.20177744));
#35145=CARTESIAN_POINT('Ctrl Pts',(0.0765001001908305,-6.76874419718307,
-52.1937377910677));
#35146=CARTESIAN_POINT('Ctrl Pts',(0.248027630732855,-6.76245305302692,
-52.1856981421355));
#35147=CARTESIAN_POINT('Ctrl Pts',(0.419607479380795,-6.75615998999077,
-52.1776560410067));
#35148=CARTESIAN_POINT('Ctrl Pts',(0.590878253952469,-6.74333504971082,
-52.169613939878));
#35149=CARTESIAN_POINT('Ctrl Pts',(0.761299495061186,-6.72403986297074,
-52.1615718387493));
#35150=CARTESIAN_POINT('Ctrl Pts',(0.937471783458669,-6.70409353949051,
-52.1532583483055));
#35151=CARTESIAN_POINT('Ctrl Pts',(1.11273576417626,-6.67723268701323,-52.1449448578618));
#35152=CARTESIAN_POINT('Ctrl Pts',(1.28650550641272,-6.64358281215563,-52.136631367418));
#35153=CARTESIAN_POINT('Ctrl Pts',(1.45489875266539,-6.6109740760757,-52.1285750992467));
#35154=CARTESIAN_POINT('Ctrl Pts',(1.62188850625641,-6.57199032598076,-52.1205188310754));
#35155=CARTESIAN_POINT('Ctrl Pts',(1.78695725300251,-6.52679651712398,-52.1124625629041));
#35156=CARTESIAN_POINT('Ctrl Pts',(1.95993152571549,-6.47943827171273,-52.1040204613241));
#35157=CARTESIAN_POINT('Ctrl Pts',(2.13079580024639,-6.42526065884737,-52.0955783597441));
#35158=CARTESIAN_POINT('Ctrl Pts',(2.29897904412963,-6.36450974974921,-52.0871362581641));
#35159=CARTESIAN_POINT('Ctrl Pts',(2.46716228801287,-6.30375884065107,-52.0786941565841));
#35160=CARTESIAN_POINT('Ctrl Pts',(2.63266410692396,-6.23643488907362,-52.0702520550041));
#35161=CARTESIAN_POINT('Ctrl Pts',(2.79494455544576,-6.16283813936275,-52.0618099534241));
#35162=CARTESIAN_POINT('Ctrl Pts',(2.95514396992221,-6.09018517150096,-52.0534761107315));
#35163=CARTESIAN_POINT('Ctrl Pts',(3.11271368751341,-6.01118890160491,-52.0451422680389));
#35164=CARTESIAN_POINT('Ctrl Pts',(3.26712418554607,-5.92606012087457,-52.0368084253463));
#35165=CARTESIAN_POINT('Ctrl Pts',(3.42135269127273,-5.84103167518175,-52.0284844051416));
#35166=CARTESIAN_POINT('Ctrl Pts',(3.57242909304589,-5.74988528387595,-52.0201603849369));
#35167=CARTESIAN_POINT('Ctrl Pts',(3.71984441825884,-5.65287948783172,-52.0118363647322));
#35168=CARTESIAN_POINT('Ctrl Pts',(3.86711302424635,-5.55597023951913,-52.0035206292415));
#35169=CARTESIAN_POINT('Ctrl Pts',(4.01072752454583,-5.45321339525729,-51.9952048937507));
#35170=CARTESIAN_POINT('Ctrl Pts',(4.15020391807029,-5.34491313665938,-51.9868891582599));
#35171=CARTESIAN_POINT('Ctrl Pts',(4.28956704949117,-5.23670082351804,-51.9785801755799));
#35172=CARTESIAN_POINT('Ctrl Pts',(4.42479849641288,-5.12295427820283,-51.9702711928999));
#35173=CARTESIAN_POINT('Ctrl Pts',(4.55544342842863,-5.00402080035509,-51.96196221022));
#35174=CARTESIAN_POINT('Ctrl Pts',(4.68600619432943,-4.88516212297349,-51.9536584532829));
#35175=CARTESIAN_POINT('Ctrl Pts',(4.81198793749897,-4.76112324778029,-51.9453546963458));
#35176=CARTESIAN_POINT('Ctrl Pts',(4.93296693647855,-4.63229167946163,-51.9370509394087));
#35177=CARTESIAN_POINT('Ctrl Pts',(5.05389682090104,-4.50351241365391,-51.9287505535967));
#35178=CARTESIAN_POINT('Ctrl Pts',(5.16982777032636,-4.36994458486356,-51.9204501677848));
#35179=CARTESIAN_POINT('Ctrl Pts',(5.28037476813952,-4.23201267814683,-51.9121497819729));
#35180=CARTESIAN_POINT('Ctrl Pts',(5.39089845446724,-4.09410985768027,-51.9038511464963));
#35181=CARTESIAN_POINT('Ctrl Pts',(5.49604023366747,-3.95184506391964,-51.8955525110197));
#35182=CARTESIAN_POINT('Ctrl Pts',(5.59545510391203,-3.80567617909155,-51.8872538755432));
#35183=CARTESIAN_POINT('Ctrl Pts',(5.69486551187465,-3.65951385512073,-51.8789556125547));
#35184=CARTESIAN_POINT('Ctrl Pts',(5.78854932769342,-3.50944807694209,-51.8706573495662));
#35185=CARTESIAN_POINT('Ctrl Pts',(5.87620454593848,-3.35596619981369,-51.8623590865777));
#35186=CARTESIAN_POINT('Ctrl Pts',(5.96387037885675,-3.20246573668435,-51.8540598187049));
#35187=CARTESIAN_POINT('Ctrl Pts',(6.04550598757024,-3.04554865259202,-51.8457605508321));
#35188=CARTESIAN_POINT('Ctrl Pts',(6.1208549506089,-2.88572758132269,-51.8374612829594));
#35189=CARTESIAN_POINT('Ctrl Pts',(6.19625682076367,-2.72579428990284,-51.8291561876629));
#35190=CARTESIAN_POINT('Ctrl Pts',(6.26536307632958,-2.56295325185163,-51.8208510923665));
#35191=CARTESIAN_POINT('Ctrl Pts',(6.32796479903219,-2.39773862257953,-51.8125459970701));
#35192=CARTESIAN_POINT('Ctrl Pts',(6.39058934957813,-2.23246374746257,-51.8042378733041));
#35193=CARTESIAN_POINT('Ctrl Pts',(6.44670452346408,-2.06481388378804,-51.795929749538));
#35194=CARTESIAN_POINT('Ctrl Pts',(6.49615100789215,-1.89533930541784,-51.787621625772));
#35195=CARTESIAN_POINT('Ctrl Pts',(6.54565005364756,-1.72568457654975,-51.7793046705184));
#35196=CARTESIAN_POINT('Ctrl Pts',(6.58846615637215,-1.55420159368787,-51.7709877152648));
#35197=CARTESIAN_POINT('Ctrl Pts',(6.62449069415686,-1.38145287398055,-51.7626707600112));
#35198=CARTESIAN_POINT('Ctrl Pts',(6.65104023040786,-1.25413969584648,-51.7565412905279));
#35199=CARTESIAN_POINT('Ctrl Pts',(6.67390201399178,-1.12613927883489,-51.7504118210445));
#35200=CARTESIAN_POINT('Ctrl Pts',(6.69305057914302,-0.997678778481976,
-51.7442823515612));
#35201=CARTESIAN_POINT('Ctrl Pts',(6.71945171793614,-0.820563497391044,
-51.7358313280364));
#35202=CARTESIAN_POINT('Ctrl Pts',(6.73884052608722,-0.642249769575589,
-51.7273803045117));
#35203=CARTESIAN_POINT('Ctrl Pts',(6.7511203152946,-0.463317912902791,-51.7189292809869));
#35204=CARTESIAN_POINT('Ctrl Pts',(6.76338929251252,-0.284543600412125,
-51.7104856983372));
#35205=CARTESIAN_POINT('Ctrl Pts',(6.76856170412666,-0.105152573017721,
-51.7020421156875));
#35206=CARTESIAN_POINT('Ctrl Pts',(6.76659244153974,0.0742679614456169,
-51.6935985330379));
#35207=CARTESIAN_POINT('Ctrl Pts',(6.76462464513015,0.253554911732638,-51.6851612368984));
#35208=CARTESIAN_POINT('Ctrl Pts',(6.75552577772988,0.432870994911237,-51.676723940759));
#35209=CARTESIAN_POINT('Ctrl Pts',(6.73930275561423,0.611626821003214,-51.6682866446196));
#35210=CARTESIAN_POINT('Ctrl Pts',(6.72309130738794,0.790255118442305,-51.6598553678477));
#35211=CARTESIAN_POINT('Ctrl Pts',(6.69976587231466,0.968323626735281,-51.6514240910758));
#35212=CARTESIAN_POINT('Ctrl Pts',(6.66938537767895,1.14524568717907,-51.6429928143039));
#35213=CARTESIAN_POINT('Ctrl Pts',(6.63901790522285,1.3220919124241,-51.6345651514823));
#35214=CARTESIAN_POINT('Ctrl Pts',(6.60160145778941,1.49779234336162,-51.6261374886608));
#35215=CARTESIAN_POINT('Ctrl Pts',(6.55724655890211,1.67176749752065,-51.6177098258393));
#35216=CARTESIAN_POINT('Ctrl Pts',(6.51290531420719,1.84568909524546,-51.6092847573858));
#35217=CARTESIAN_POINT('Ctrl Pts',(6.46162995944129,2.01788615452275,-51.6008596889322));
#35218=CARTESIAN_POINT('Ctrl Pts',(6.40358175896227,2.18779104493223,-51.5924346204787));
#35219=CARTESIAN_POINT('Ctrl Pts',(6.38769799448225,2.23428222365952,-51.5901292638623));
#35220=CARTESIAN_POINT('Ctrl Pts',(6.37130741179366,2.2806018601415,-51.5878239072459));
#35221=CARTESIAN_POINT('Ctrl Pts',(6.35441396599858,2.32673852177725,-51.5855185506295));
#35222=CARTESIAN_POINT('Ctrl Pts',(6.29125479382549,2.49922869288211,-51.5768995621046));
#35223=CARTESIAN_POINT('Ctrl Pts',(6.22109119538753,2.66908289411008,-51.5682805735796));
#35224=CARTESIAN_POINT('Ctrl Pts',(6.14417435104374,2.83573809509558,-51.5596615850546));
#35225=CARTESIAN_POINT('Ctrl Pts',(6.06721142664618,3.00249313741863,-51.5510374329864));
#35226=CARTESIAN_POINT('Ctrl Pts',(5.98348730962295,3.16604507861792,-51.5424132809181));
#35227=CARTESIAN_POINT('Ctrl Pts',(5.89329970986362,3.3258544059717,-51.5337891288499));
#35228=CARTESIAN_POINT('Ctrl Pts',(5.80002316055734,3.49113724576673,-51.5248695972539));
#35229=CARTESIAN_POINT('Ctrl Pts',(5.69983272053446,3.65241625390595,-51.5159500656579));
#35230=CARTESIAN_POINT('Ctrl Pts',(5.59310682289629,3.8091265491804,-51.5070305340619));
#35231=CARTESIAN_POINT('Ctrl Pts',(5.4897230300421,3.96092948608048,-51.4983903162021));
#35232=CARTESIAN_POINT('Ctrl Pts',(5.38020711750334,4.10844529973347,-51.4897500983423));
#35233=CARTESIAN_POINT('Ctrl Pts',(5.26494481958201,4.25119336736835,-51.4811098804825));
#35234=CARTESIAN_POINT('Ctrl Pts',(5.14409336691997,4.40086339520475,-51.4720506920185));
#35235=CARTESIAN_POINT('Ctrl Pts',(5.01692463720449,4.54529150735008,-51.4629915035544));
#35236=CARTESIAN_POINT('Ctrl Pts',(4.88392796895243,4.68396590445364,-51.4539323150903));
#35237=CARTESIAN_POINT('Ctrl Pts',(4.75093130070036,4.8226403015572,-51.4448731266262));
#35238=CARTESIAN_POINT('Ctrl Pts',(4.61210699319241,4.95556074292922,-51.4358139381622));
#35239=CARTESIAN_POINT('Ctrl Pts',(4.46798590640481,5.0822623840341,-51.4267547496981));
#35240=CARTESIAN_POINT('Ctrl Pts',(4.32411342256124,5.20874547002193,-51.4177111879613));
#35241=CARTESIAN_POINT('Ctrl Pts',(4.17483043324289,5.32914835120471,-51.4086676262245));
#35242=CARTESIAN_POINT('Ctrl Pts',(4.02065033715821,5.44303774250276,-51.3996240644878));
#35243=CARTESIAN_POINT('Ctrl Pts',(3.86666731860615,5.55678155703184,-51.3905920624975));
#35244=CARTESIAN_POINT('Ctrl Pts',(3.70779988610797,5.66402836840122,-51.3815600605073));
#35245=CARTESIAN_POINT('Ctrl Pts',(3.54459266539005,5.76438650998205,-51.3725280585171));
#35246=CARTESIAN_POINT('Ctrl Pts',(3.39939019677095,5.853673306482,-51.364492452128));
#35247=CARTESIAN_POINT('Ctrl Pts',(3.25075318376519,5.93750796816106,-51.3564568457388));
#35248=CARTESIAN_POINT('Ctrl Pts',(3.09908550384718,6.01564277861014,-51.3484212393497));
#35249=CARTESIAN_POINT('Origin',(0.,0.,-63.6971797838103));
#35250=CARTESIAN_POINT('',(3.09908550384721,6.01564277861012,-48.954361679463));
#35251=CARTESIAN_POINT('',(3.0990855038472,6.01564277861013,-49.3486032095739));
#35252=CARTESIAN_POINT('',(3.09908550384721,6.01564277861012,-63.6971797838103));
#35253=CARTESIAN_POINT('',(-6.76699999643594,-0.000219627007310033,-50.3028202161602));
#35254=CARTESIAN_POINT('Ctrl Pts',(-6.76699999643594,-0.000219627007290654,
-50.3028202161602));
#35255=CARTESIAN_POINT('Ctrl Pts',(-6.76699376355498,-0.192262973378822,
-50.2938218191915));
#35256=CARTESIAN_POINT('Ctrl Pts',(-6.75880815810201,-0.384103022895448,
-50.2848234222228));
#35257=CARTESIAN_POINT('Ctrl Pts',(-6.74252052002201,-0.575070462710529,
-50.2758250252541));
#35258=CARTESIAN_POINT('Ctrl Pts',(-6.72617712925943,-0.766691585214444,
-50.2667958267188));
#35259=CARTESIAN_POINT('Ctrl Pts',(-6.70167620673784,-0.957433885510391,
-50.2577666281834));
#35260=CARTESIAN_POINT('Ctrl Pts',(-6.6691469286502,-1.14663343928025,-50.2487374296481));
#35261=CARTESIAN_POINT('Ctrl Pts',(-6.63656304962023,-1.33615056769457,
-50.2396930754506));
#35262=CARTESIAN_POINT('Ctrl Pts',(-6.5959239287075,-1.52411954709816,-50.2306487212531));
#35263=CARTESIAN_POINT('Ctrl Pts',(-6.5474093650472,-1.70988877021058,-50.2216043670556));
#35264=CARTESIAN_POINT('Ctrl Pts',(-6.49878671787905,-1.89607186057788,
-50.2125398633308));
#35265=CARTESIAN_POINT('Ctrl Pts',(-6.44225359159685,-2.08004516723249,
-50.2034753596059));
#35266=CARTESIAN_POINT('Ctrl Pts',(-6.37803978603545,-2.26117170682567,
-50.1944108558811));
#35267=CARTESIAN_POINT('Ctrl Pts',(-6.34891704925298,-2.34331760194549,
-50.190299852745));
#35268=CARTESIAN_POINT('Ctrl Pts',(-6.31821514885094,-2.42487823106995,
-50.1861888496089));
#35269=CARTESIAN_POINT('Ctrl Pts',(-6.2859587357902,-2.50579563650807,-50.1820778464728));
#35270=CARTESIAN_POINT('Ctrl Pts',(-6.21964895771645,-2.67213822354038,
-50.1736268229477));
#35271=CARTESIAN_POINT('Ctrl Pts',(-6.14667628219524,-2.83598784984301,
-50.1651757994225));
#35272=CARTESIAN_POINT('Ctrl Pts',(-6.06724917150553,-2.99679436913271,
-50.1567247758973));
#35273=CARTESIAN_POINT('Ctrl Pts',(-5.98789199402615,-3.15745930306146,
-50.1482811932472));
#35274=CARTESIAN_POINT('Ctrl Pts',(-5.90209185466891,-3.31508617463203,
-50.1398376105971));
#35275=CARTESIAN_POINT('Ctrl Pts',(-5.81010525632382,-3.46914483849238,
-50.131394027947));
#35276=CARTESIAN_POINT('Ctrl Pts',(-5.71818714486636,-3.62308880087893,
-50.1229567318071));
#35277=CARTESIAN_POINT('Ctrl Pts',(-5.62009192566996,-3.77346956776266,
-50.1145194356673));
#35278=CARTESIAN_POINT('Ctrl Pts',(-5.51612215794817,-3.91978128708647,
-50.1060821395274));
#35279=CARTESIAN_POINT('Ctrl Pts',(-5.41222656472862,-4.06598862415387,
-50.0976508627551));
#35280=CARTESIAN_POINT('Ctrl Pts',(-5.30246497426804,-4.20813243453552,
-50.0892195859827));
#35281=CARTESIAN_POINT('Ctrl Pts',(-5.18718351767982,-4.34573539851552,
-50.0807883092104));
#35282=CARTESIAN_POINT('Ctrl Pts',(-5.07195147489672,-4.48327938088436,
-50.0723606463885));
#35283=CARTESIAN_POINT('Ctrl Pts',(-4.95120449523002,-4.61628614339895,
-50.0639329835665));
#35284=CARTESIAN_POINT('Ctrl Pts',(-4.82532968654888,-4.74431053116363,
-50.0555053207446));
#35285=CARTESIAN_POINT('Ctrl Pts',(-4.69949362711262,-4.87229550795797,
-50.0470802522906));
#35286=CARTESIAN_POINT('Ctrl Pts',(-4.56853311881905,-4.99530093263866,
-50.0386551838367));
#35287=CARTESIAN_POINT('Ctrl Pts',(-4.43287315419674,-5.11291742538464,
-50.0302301153827));
#35288=CARTESIAN_POINT('Ctrl Pts',(-4.39575243543028,-5.14510089794912,
-50.0279247587689));
#35289=CARTESIAN_POINT('Ctrl Pts',(-4.35828006070707,-5.17688109700189,
-50.0256194021551));
#35290=CARTESIAN_POINT('Ctrl Pts',(-4.32046520081324,-5.20825013306407,
-50.0233140455413));
#35291=CARTESIAN_POINT('Ctrl Pts',(-4.17908757553354,-5.32552889168528,
-50.0146950570169));
#35292=CARTESIAN_POINT('Ctrl Pts',(-4.03298337072702,-5.43700508445549,
-50.0060760684924));
#35293=CARTESIAN_POINT('Ctrl Pts',(-3.88265296675354,-5.5423185527142,-49.9974570799679));
#35294=CARTESIAN_POINT('Ctrl Pts',(-3.73223250145224,-5.6476951131388,-49.9888329279001));
#35295=CARTESIAN_POINT('Ctrl Pts',(-3.57758103325063,-5.74690140639123,
-49.9802087758323));
#35296=CARTESIAN_POINT('Ctrl Pts',(-3.41922731773806,-5.83962101078775,
-49.9715846237645));
#35297=CARTESIAN_POINT('Ctrl Pts',(-3.2554499448681,-5.93551628657874,-49.9626650921683));
#35298=CARTESIAN_POINT('Ctrl Pts',(-3.08771254162915,-6.0244724909439,-49.953745560572));
#35299=CARTESIAN_POINT('Ctrl Pts',(-2.91662638756051,-6.10619189965282,
-49.9448260289758));
#35300=CARTESIAN_POINT('Ctrl Pts',(-2.75089776964948,-6.18535227785855,
-49.9361858111165));
#35301=CARTESIAN_POINT('Ctrl Pts',(-2.58202725636523,-6.25772216189874,
-49.9275455932573));
#35302=CARTESIAN_POINT('Ctrl Pts',(-2.410590037677,-6.32308031502466,-49.918905375398));
#35303=CARTESIAN_POINT('Ctrl Pts',(-2.2308397004448,-6.39160773372144,-49.9098461869333));
#35304=CARTESIAN_POINT('Ctrl Pts',(-2.04826791438665,-6.4524263849406,-49.9007869984686));
#35305=CARTESIAN_POINT('Ctrl Pts',(-1.86355508911284,-6.50534022398842,
-49.8917278100039));
#35306=CARTESIAN_POINT('Ctrl Pts',(-1.67884226383904,-6.55825406303623,
-49.8826686215392));
#35307=CARTESIAN_POINT('Ctrl Pts',(-1.49198877909424,-6.60326303251488,
-49.8736094330745));
#35308=CARTESIAN_POINT('Ctrl Pts',(-1.30368729826192,-6.64023255830325,
-49.8645502446098));
#35309=CARTESIAN_POINT('Ctrl Pts',(-1.11571203653408,-6.67713803698195,
-49.8555067505535));
#35310=CARTESIAN_POINT('Ctrl Pts',(-0.926120782753142,-6.70606673400241,
-49.8464632564972));
#35311=CARTESIAN_POINT('Ctrl Pts',(-0.735575215138369,-6.72690256380113,
-49.8374197624409));
#35312=CARTESIAN_POINT('Ctrl Pts',(-0.545203938857249,-6.74771933514254,
-49.8283845404356));
#35313=CARTESIAN_POINT('Ctrl Pts',(-0.353880327978583,-6.76045799255479,
-49.8193493184303));
#35314=CARTESIAN_POINT('Ctrl Pts',(-0.162272834050877,-6.76505406684449,
-49.8103140964249));
#35315=CARTESIAN_POINT('Ctrl Pts',(0.0289970891847575,-6.76964204385183,
-49.8012947925138));
#35316=CARTESIAN_POINT('Ctrl Pts',(0.220549659042468,-6.76611607813147,
-49.7922754886027));
#35317=CARTESIAN_POINT('Ctrl Pts',(0.411714919618717,-6.75446369632433,
-49.7832561846916));
#35318=CARTESIAN_POINT('Ctrl Pts',(0.602640350023257,-6.74282593324405,
-49.7742481961272));
#35319=CARTESIAN_POINT('Ctrl Pts',(0.793179203908962,-6.72308211454778,
-49.7652402075629));
#35320=CARTESIAN_POINT('Ctrl Pts',(0.982662579947927,-6.69527170874865,
-49.7562322189985));
#35321=CARTESIAN_POINT('Ctrl Pts',(1.17171800114492,-6.66752411372516,-49.7472445752918));
#35322=CARTESIAN_POINT('Ctrl Pts',(1.35972246771617,-6.63174633224124,-49.7382569315852));
#35323=CARTESIAN_POINT('Ctrl Pts',(1.54601371560388,-6.58802934049058,-49.7292692878785));
#35324=CARTESIAN_POINT('Ctrl Pts',(1.70826048063626,-6.54995487070782,-49.7214416731451));
#35325=CARTESIAN_POINT('Ctrl Pts',(1.86920766915795,-6.50585913879513,-49.7136140584117));
#35326=CARTESIAN_POINT('Ctrl Pts',(2.02842123090489,-6.45583428458432,-49.7057864436783));
#35327=CARTESIAN_POINT('Ctrl Pts',(2.19364614714791,-6.40392066456125,-49.697663285233));
#35328=CARTESIAN_POINT('Ctrl Pts',(2.35692969512879,-6.34564335320328,-49.6895401267877));
#35329=CARTESIAN_POINT('Ctrl Pts',(2.51774860006068,-6.28118070006687,-49.6814169683424));
#35330=CARTESIAN_POINT('Ctrl Pts',(2.67855616641804,-6.2167225918849,-49.6732943826223));
#35331=CARTESIAN_POINT('Ctrl Pts',(2.836899096113,-6.14608014677511,-49.6651717969022));
#35332=CARTESIAN_POINT('Ctrl Pts',(2.99227317568785,-6.06948022832754,-49.6570492111821));
#35333=CARTESIAN_POINT('Ctrl Pts',(3.1476659250574,-5.99287110561144,-49.6489256494497));
#35334=CARTESIAN_POINT('Ctrl Pts',(3.30008878619914,-5.91030324705111,-49.6408020877173));
#35335=CARTESIAN_POINT('Ctrl Pts',(3.44906131849665,-5.82204989855379,-49.6326785259849));
#35336=CARTESIAN_POINT('Ctrl Pts',(3.59814235960617,-5.73373226796464,-49.6245490472018));
#35337=CARTESIAN_POINT('Ctrl Pts',(3.74376773720741,-5.63972106311222,-49.6164195684187));
#35338=CARTESIAN_POINT('Ctrl Pts',(3.88548469258686,-5.54033371771712,-49.6082900896356));
#35339=CARTESIAN_POINT('Ctrl Pts',(4.02725942347458,-5.44090585385068,-49.600157296607));
#35340=CARTESIAN_POINT('Ctrl Pts',(4.16512226485639,-5.33609770197789,-49.5920245035785));
#35341=CARTESIAN_POINT('Ctrl Pts',(4.29865305189998,-5.22626740029546,-49.58389171055));
#35342=CARTESIAN_POINT('Ctrl Pts',(4.43232903341692,-5.11631767482196,-49.5757500743428));
#35343=CARTESIAN_POINT('Ctrl Pts',(4.5616632791119,-5.00133513542633,-49.5676084381357));
#35344=CARTESIAN_POINT('Ctrl Pts',(4.6862714937236,-4.88171573190345,-49.5594668019286));
#35345=CARTESIAN_POINT('Ctrl Pts',(4.74975768652857,-4.82077127058576,-49.555318748868));
#35346=CARTESIAN_POINT('Ctrl Pts',(4.81201773362238,-4.75862375098831,-49.5511706958074));
#35347=CARTESIAN_POINT('Ctrl Pts',(4.87300483250201,-4.69532883858118,-49.5470226427468));
#35348=CARTESIAN_POINT('Ctrl Pts',(4.99710515413813,-4.56653243521136,-49.5385819277687));
#35349=CARTESIAN_POINT('Ctrl Pts',(5.1161877999895,-4.43271779629924,-49.5301412127906));
#35350=CARTESIAN_POINT('Ctrl Pts',(5.22984172174294,-4.29430373466024,-49.5217004978125));
#35351=CARTESIAN_POINT('Ctrl Pts',(5.34340973850756,-4.15599429289035,-49.5132661627245));
#35352=CARTESIAN_POINT('Ctrl Pts',(5.45155700000134,-4.01309261526358,-49.5048318276365));
#35353=CARTESIAN_POINT('Ctrl Pts',(5.55391086229364,-3.8660526553187,-49.4963974925485));
#35354=CARTESIAN_POINT('Ctrl Pts',(5.65620307831851,-3.71910125543876,-49.4879682373399));
#35355=CARTESIAN_POINT('Ctrl Pts',(5.75270866154225,-3.56801681523327,-49.4795389821312));
#35356=CARTESIAN_POINT('Ctrl Pts',(5.84309641932045,-3.41328481591042,-49.4711097269226));
#35357=CARTESIAN_POINT('Ctrl Pts',(5.93344360264594,-3.25862227473479,-49.4626842555496));
#35358=CARTESIAN_POINT('Ctrl Pts',(6.01767826836475,-3.10031572659021,-49.4542587841766));
#35359=CARTESIAN_POINT('Ctrl Pts',(6.09551337666583,-2.93887830215679,-49.4458333128036));
#35360=CARTESIAN_POINT('Ctrl Pts',(6.17332547465082,-2.77748860330949,-49.4374103322443));
#35361=CARTESIAN_POINT('Ctrl Pts',(6.24474164344188,-2.61297017399657,-49.4289873516851));
#35362=CARTESIAN_POINT('Ctrl Pts',(6.30952132935479,-2.44585968412274,-49.4205643711259));
#35363=CARTESIAN_POINT('Ctrl Pts',(6.3743020878849,-2.27874642724589,-49.4121412510995));
#35364=CARTESIAN_POINT('Ctrl Pts',(6.43244601734344,-2.10904133246272,-49.4037181310732));
#35365=CARTESIAN_POINT('Ctrl Pts',(6.48376090770987,-1.93730056822717,-49.3952950110469));
#35366=CARTESIAN_POINT('Ctrl Pts',(6.53507757263076,-1.76555386490967,-49.386871599735));
#35367=CARTESIAN_POINT('Ctrl Pts',(6.5795646319486,-1.591771671276,-49.3784481884232));
#35368=CARTESIAN_POINT('Ctrl Pts',(6.61707987028794,-1.41652496985763,-49.3700247771113));
#35369=CARTESIAN_POINT('Ctrl Pts',(6.65460163801874,-1.24124776738511,-49.3615998997352));
#35370=CARTESIAN_POINT('Ctrl Pts',(6.68514909576253,-1.06450587504572,-49.3531750223591));
#35371=CARTESIAN_POINT('Ctrl Pts',(6.70863115887434,-0.886880473446274,
-49.344750144983));
#35372=CARTESIAN_POINT('Ctrl Pts',(6.73212058488464,-0.709199376663938,
-49.3363226259515));
#35373=CARTESIAN_POINT('Ctrl Pts',(6.7485401556958,-0.530634548786091,-49.3278951069201));
#35374=CARTESIAN_POINT('Ctrl Pts',(6.75785061913856,-0.35177266722784,-49.3194675878887));
#35375=CARTESIAN_POINT('Ctrl Pts',(6.7671694318451,-0.172750389246998,-49.3110325113839));
#35376=CARTESIAN_POINT('Ctrl Pts',(6.76936638132112,0.0065691413373811,
-49.3025974348791));
#35377=CARTESIAN_POINT('Ctrl Pts',(6.76445433781425,0.18559771449576,-49.2941623583743));
#35378=CARTESIAN_POINT('Ctrl Pts',(6.75953992028441,0.364712813341815,-49.2857232051416));
#35379=CARTESIAN_POINT('Ctrl Pts',(6.74750967465999,0.543536341425885,-49.2772840519088));
#35380=CARTESIAN_POINT('Ctrl Pts',(6.7284284513529,0.721484286055326,-49.268844898676));
#35381=CARTESIAN_POINT('Ctrl Pts',(6.70932602345691,0.899629980742703,-49.2603963671779));
#35382=CARTESIAN_POINT('Ctrl Pts',(6.68315700487441,1.0768978170993,-49.2519478356798));
#35383=CARTESIAN_POINT('Ctrl Pts',(6.65003774541412,1.25271185217012,-49.2434993041817));
#35384=CARTESIAN_POINT('Ctrl Pts',(6.63173828000527,1.34985481084729,-49.2388312164157));
#35385=CARTESIAN_POINT('Ctrl Pts',(6.61131786213327,1.44655414126861,-49.2341631286497));
#35386=CARTESIAN_POINT('Ctrl Pts',(6.58880268423295,1.54271455177059,-49.2294950408837));
#35387=CARTESIAN_POINT('Ctrl Pts',(6.54905567477237,1.71247064976259,-49.221254265287));
#35388=CARTESIAN_POINT('Ctrl Pts',(6.5026891205378,1.88092405804825,-49.2130134896902));
#35389=CARTESIAN_POINT('Ctrl Pts',(6.44980161272551,2.04752244346269,-49.2047727140935));
#35390=CARTESIAN_POINT('Ctrl Pts',(6.39697268356182,2.21393630310386,-49.1965410660491));
#35391=CARTESIAN_POINT('Ctrl Pts',(6.33763728916775,2.37849889490668,-49.1883094180047));
#35392=CARTESIAN_POINT('Ctrl Pts',(6.27194495619697,2.54066831098343,-49.1800777699603));
#35393=CARTESIAN_POINT('Ctrl Pts',(6.20631367761972,2.70268700695481,-49.171853772402));
#35394=CARTESIAN_POINT('Ctrl Pts',(6.13433735949582,2.86231662897421,-49.1636297748437));
#35395=CARTESIAN_POINT('Ctrl Pts',(6.05621526573445,3.01903058200558,-49.1554057772855));
#35396=CARTESIAN_POINT('Ctrl Pts',(5.97816219314641,3.17560607765067,-49.147189045661));
#35397=CARTESIAN_POINT('Ctrl Pts',(5.89397432524319,3.32927072135779,-49.1389723140365));
#35398=CARTESIAN_POINT('Ctrl Pts',(5.80389888449294,3.47951817621085,-49.130755582412));
#35399=CARTESIAN_POINT('Ctrl Pts',(5.71386959272571,3.62968865373038,-49.1225430605233));
#35400=CARTESIAN_POINT('Ctrl Pts',(5.61795891812474,3.77644512480496,-49.1143305386346));
#35401=CARTESIAN_POINT('Ctrl Pts',(5.51646003415715,3.91930576652893,-49.1061180167459));
#35402=CARTESIAN_POINT('Ctrl Pts',(5.41499509190489,4.06211863496669,-49.097908241164));
#35403=CARTESIAN_POINT('Ctrl Pts',(5.30794586884362,4.20103797963546,-49.0896984655822));
#35404=CARTESIAN_POINT('Ctrl Pts',(5.19564892880966,4.33561082300511,-49.0814886900003));
#35405=CARTESIAN_POINT('Ctrl Pts',(5.14660054289747,4.39438874476237,-49.0779028733176));
#35406=CARTESIAN_POINT('Ctrl Pts',(5.09655158672348,4.45233786950648,-49.0743170566349));
#35407=CARTESIAN_POINT('Ctrl Pts',(5.04553256808488,4.50942236926136,-49.0707312399522));
#35408=CARTESIAN_POINT('Ctrl Pts',(4.91955089499462,4.65038158365912,-49.0618767539755));
#35409=CARTESIAN_POINT('Ctrl Pts',(4.7877822974446,4.78592055307892,-49.0530222679987));
#35410=CARTESIAN_POINT('Ctrl Pts',(4.65071258853474,4.9156038712293,-49.044167782022));
#35411=CARTESIAN_POINT('Ctrl Pts',(4.51325128960666,5.04565767745704,-49.0352879999506));
#35412=CARTESIAN_POINT('Ctrl Pts',(4.37045876470817,5.1698221793112,-49.0264082178793));
#35413=CARTESIAN_POINT('Ctrl Pts',(4.22285535174613,5.28770098230121,-49.0175284358079));
#35414=CARTESIAN_POINT('Ctrl Pts',(4.07503400119427,5.4057538342627,-49.0086355426691));
#35415=CARTESIAN_POINT('Ctrl Pts',(3.92238777843376,5.51750229011527,-48.9997426495303));
#35416=CARTESIAN_POINT('Ctrl Pts',(3.76546632465436,5.62259302794485,-48.9908497563915));
#35417=CARTESIAN_POINT('Ctrl Pts',(3.60821568568681,5.72790422201843,-48.9819382080043));
#35418=CARTESIAN_POINT('Ctrl Pts',(3.44667209776304,5.82652962585396,-48.9730266596171));
#35419=CARTESIAN_POINT('Ctrl Pts',(3.28141222117305,5.91816042657988,-48.9641151112299));
#35420=CARTESIAN_POINT('Ctrl Pts',(3.22112150400139,5.95158951296656,-48.9608639673076));
#35421=CARTESIAN_POINT('Ctrl Pts',(3.16033637079744,5.98408810010785,-48.9576128233853));
#35422=CARTESIAN_POINT('Ctrl Pts',(3.09908550384721,6.01564277861012,-48.954361679463));
#35423=CARTESIAN_POINT('Ctrl Pts',(3.0990855038472,6.01564277861013,-50.9542788176482));
#35424=CARTESIAN_POINT('Ctrl Pts',(2.94371885527148,6.09568319093221,-50.9460782653071));
#35425=CARTESIAN_POINT('Ctrl Pts',(2.78528905180417,6.16968031566986,-50.9378777129661));
#35426=CARTESIAN_POINT('Ctrl Pts',(2.62431077295935,6.2374098764575,-50.9296771606251));
#35427=CARTESIAN_POINT('Ctrl Pts',(2.46326604928346,6.30516739306164,-50.9214732234527));
#35428=CARTESIAN_POINT('Ctrl Pts',(2.29967108513821,6.3666520534542,-50.9132692862804));
#35429=CARTESIAN_POINT('Ctrl Pts',(2.13405869120049,6.421688446391,-50.9050653491081));
#35430=CARTESIAN_POINT('Ctrl Pts',(1.96825491490221,6.47678843960884,-50.8968519314324));
#35431=CARTESIAN_POINT('Ctrl Pts',(1.8004293927172,6.5254251684168,-50.8886385137566));
#35432=CARTESIAN_POINT('Ctrl Pts',(1.63112914484802,6.5674733888176,-50.8804250960809));
#35433=CARTESIAN_POINT('Ctrl Pts',(1.4617200186328,6.60954865076589,-50.8722063962905));
#35434=CARTESIAN_POINT('Ctrl Pts',(1.29083462661431,6.64502688625558,-50.8639876965));
#35435=CARTESIAN_POINT('Ctrl Pts',(1.1190281028488,6.6738343630206,-50.8557689967096));
#35436=CARTESIAN_POINT('Ctrl Pts',(0.946972562451434,6.70268359338543,-50.8475383847234));
#35437=CARTESIAN_POINT('Ctrl Pts',(0.773993578147219,6.72484270590575,-50.8393077727373));
#35438=CARTESIAN_POINT('Ctrl Pts',(0.600650386828964,6.74028991311221,-50.8310771607511));
#35439=CARTESIAN_POINT('Ctrl Pts',(0.502759058404987,6.74901334564153,-50.8264291239004));
#35440=CARTESIAN_POINT('Ctrl Pts',(0.404751579198324,6.75559719899961,-50.8217810870496));
#35441=CARTESIAN_POINT('Ctrl Pts',(0.306728244600427,6.76004488032175,-50.8171330501989));
#35442=CARTESIAN_POINT('Ctrl Pts',(0.13652012573504,6.76776785234939,-50.8090621800125));
#35443=CARTESIAN_POINT('Ctrl Pts',(-0.0342906662540302,6.7690722624394,
-50.8009913098261));
#35444=CARTESIAN_POINT('Ctrl Pts',(-0.205168628666277,6.76388903174876,
-50.7929204396397));
#35445=CARTESIAN_POINT('Ctrl Pts',(-0.375833946736591,6.75871225118583,
-50.7848596130239));
#35446=CARTESIAN_POINT('Ctrl Pts',(-0.546565900771842,6.74706390500711,
-50.7767987864081));
#35447=CARTESIAN_POINT('Ctrl Pts',(-0.716823528716951,6.72892658814746,
-50.7687379597922));
#35448=CARTESIAN_POINT('Ctrl Pts',(-0.886906619177028,6.7108078645321,-50.7606853966324));
#35449=CARTESIAN_POINT('Ctrl Pts',(-1.05651598341785,6.68621344732343,-50.7526328334725));
#35450=CARTESIAN_POINT('Ctrl Pts',(-1.22511041953536,6.65517794352232,-50.7445802703126));
#35451=CARTESIAN_POINT('Ctrl Pts',(-1.39356893909867,6.62416745975646,-50.7365341989247));
#35452=CARTESIAN_POINT('Ctrl Pts',(-1.56101379407839,6.58672629176055,-50.7284881275368));
#35453=CARTESIAN_POINT('Ctrl Pts',(-1.72690877231002,6.54294085959202,-50.7204420561489));
#35454=CARTESIAN_POINT('Ctrl Pts',(-1.89270629785877,6.49918114856274,-50.712400711313));
#35455=CARTESIAN_POINT('Ctrl Pts',(-2.05695539937716,6.44908468743227,-50.7043593664771));
#35456=CARTESIAN_POINT('Ctrl Pts',(-2.21913003802878,6.3927889746431,-50.6963180216413));
#35457=CARTESIAN_POINT('Ctrl Pts',(-2.38443090470133,6.33540805373358,-50.6881216644202));
#35458=CARTESIAN_POINT('Ctrl Pts',(-2.54757612479494,6.27158651133287,-50.6799253071992));
#35459=CARTESIAN_POINT('Ctrl Pts',(-2.70802439040033,6.20152343388275,-50.6717289499781));
#35460=CARTESIAN_POINT('Ctrl Pts',(-2.86538816445975,6.13280726391876,-50.6636901612696));
#35461=CARTESIAN_POINT('Ctrl Pts',(-3.02015739141042,6.05808753417179,-50.6556513725611));
#35462=CARTESIAN_POINT('Ctrl Pts',(-3.17184161906389,5.9776006677909,-50.6476125838526));
#35463=CARTESIAN_POINT('Ctrl Pts',(-3.32354207830387,5.89710518858615,-50.6395729349209));
#35464=CARTESIAN_POINT('Ctrl Pts',(-3.47215655094803,5.81084151891391,-50.6315332859892));
#35465=CARTESIAN_POINT('Ctrl Pts',(-3.61721954755021,5.71909186364589,-50.6234936370575));
#35466=CARTESIAN_POINT('Ctrl Pts',(-3.76232679023396,5.6273142235518,-50.6154515359294));
#35467=CARTESIAN_POINT('Ctrl Pts',(-3.90388008522075,5.53004746669188,-50.6074094348013));
#35468=CARTESIAN_POINT('Ctrl Pts',(-4.04144339720263,5.42761681285694,-50.5993673336731));
#35469=CARTESIAN_POINT('Ctrl Pts',(-4.18364893049433,5.32172952689267,-50.5910538432284));
#35470=CARTESIAN_POINT('Ctrl Pts',(-4.32159012595492,5.21032398423091,-50.5827403527836));
#35471=CARTESIAN_POINT('Ctrl Pts',(-4.45482379577049,5.09380348547498,-50.5744268623388));
#35472=CARTESIAN_POINT('Ctrl Pts',(-4.58393516969235,4.98088817131105,-50.566370594168));
#35473=CARTESIAN_POINT('Ctrl Pts',(-4.70862576761979,4.86317001060159,-50.5583143259973));
#35474=CARTESIAN_POINT('Ctrl Pts',(-4.82853137587974,4.74105196682603,-50.5502580578265));
#35475=CARTESIAN_POINT('Ctrl Pts',(-4.95417954246217,4.61308540604791,-50.5418159562447));
#35476=CARTESIAN_POINT('Ctrl Pts',(-5.07457279345764,4.48028751760336,-50.533373854663));
#35477=CARTESIAN_POINT('Ctrl Pts',(-5.18934148411168,4.34315829337104,-50.5249317530812));
#35478=CARTESIAN_POINT('Ctrl Pts',(-5.30411017476572,4.2060290691387,-50.5164896514994));
#35479=CARTESIAN_POINT('Ctrl Pts',(-5.4132540920048,4.0645689268294,-50.5080475499177));
#35480=CARTESIAN_POINT('Ctrl Pts',(-5.5164577155674,3.91930902996394,-50.4996054483359));
#35481=CARTESIAN_POINT('Ctrl Pts',(-5.62099658766643,3.77216976047574,-50.4910541228394));
#35482=CARTESIAN_POINT('Ctrl Pts',(-5.71975709886979,3.62068774169861,-50.4825027973429));
#35483=CARTESIAN_POINT('Ctrl Pts',(-5.81237669910402,3.46533780571429,-50.4739514718463));
#35484=CARTESIAN_POINT('Ctrl Pts',(-5.9048762937362,3.31018915393491,-50.4654112261533));
#35485=CARTESIAN_POINT('Ctrl Pts',(-5.99125067460389,3.15118284725474,-50.4568709804602));
#35486=CARTESIAN_POINT('Ctrl Pts',(-6.0711794357131,2.98882405962184,-50.4483307347671));
#35487=CARTESIAN_POINT('Ctrl Pts',(-6.15101355609578,2.82665751509901,-50.439800601267));
#35488=CARTESIAN_POINT('Ctrl Pts',(-6.22441713018384,2.6611466881456,-50.4312704677669));
#35489=CARTESIAN_POINT('Ctrl Pts',(-6.29111445915045,2.49282327128663,-50.4227403342668));
#35490=CARTESIAN_POINT('Ctrl Pts',(-6.35774023414615,2.32468043450573,-50.4142193520316));
#35491=CARTESIAN_POINT('Ctrl Pts',(-6.41767398982197,2.15373131958206,-50.4056983697963));
#35492=CARTESIAN_POINT('Ctrl Pts',(-6.47068694435408,1.9805300977682,-50.3971773875611));
#35493=CARTESIAN_POINT('Ctrl Pts',(-6.52363271889448,1.8075483629976,-50.3886672034321));
#35494=CARTESIAN_POINT('Ctrl Pts',(-6.56967509607546,1.63232052007738,-50.3801570193032));
#35495=CARTESIAN_POINT('Ctrl Pts',(-6.60863420702198,1.45541846826916,-50.3716468351742));
#35496=CARTESIAN_POINT('Ctrl Pts',(-6.64756370104846,1.27865089832662,-50.3631431205318));
#35497=CARTESIAN_POINT('Ctrl Pts',(-6.67942059378738,1.10021196802362,-50.3546394058893));
#35498=CARTESIAN_POINT('Ctrl Pts',(-6.70407512900704,0.920687604255242,
-50.3461356912469));
#35499=CARTESIAN_POINT('Ctrl Pts',(-6.72870903519254,0.741313452778424,
-50.3376390918641));
#35500=CARTESIAN_POINT('Ctrl Pts',(-6.74615256207308,0.560855995920925,
-50.3291424924813));
#35501=CARTESIAN_POINT('Ctrl Pts',(-6.75632719034912,0.379910380154642,
-50.3206458930985));
#35502=CARTESIAN_POINT('Ctrl Pts',(-6.76344257177574,0.253370418327687,
-50.3147040007956));
#35503=CARTESIAN_POINT('Ctrl Pts',(-6.76700411216908,0.126591947465235,
-50.3087621084928));
#35504=CARTESIAN_POINT('Ctrl Pts',(-6.76699999643596,-0.000219626373065103,
-50.3028202161899));
#35505=CARTESIAN_POINT('',(-6.76699981440648,0.000570866902357549,-50.6971797838101));
#35506=CARTESIAN_POINT('Ctrl Pts',(3.09908550384718,6.01564277861014,-51.3484212393497));
#35507=CARTESIAN_POINT('Ctrl Pts',(2.92904011259127,6.10324525542459,-51.3394119511931));
#35508=CARTESIAN_POINT('Ctrl Pts',(2.75518479088681,6.18368201021633,-51.3304026630366));
#35509=CARTESIAN_POINT('Ctrl Pts',(2.57811484594898,6.25664549428026,-51.32139337488));
#35510=CARTESIAN_POINT('Ctrl Pts',(2.40144887074735,6.32944251847761,-51.3124046406337));
#35511=CARTESIAN_POINT('Ctrl Pts',(2.2215831314487,6.3948002148617,-51.3034159063874));
#35512=CARTESIAN_POINT('Ctrl Pts',(2.03913343426668,6.45245874355317,-51.2944271721411));
#35513=CARTESIAN_POINT('Ctrl Pts',(1.86026950611045,6.50898408227805,-51.2856150976829));
#35514=CARTESIAN_POINT('Ctrl Pts',(1.67892245044474,6.55810994139659,-51.2768030232247));
#35515=CARTESIAN_POINT('Ctrl Pts',(1.49569253948088,6.59963581020508,-51.2679909487665));
#35516=CARTESIAN_POINT('Ctrl Pts',(1.32678729409768,6.63791524298957,-51.2598677903211));
#35517=CARTESIAN_POINT('Ctrl Pts',(1.15635749427144,6.66971847226523,-51.2517446318757));
#35518=CARTESIAN_POINT('Ctrl Pts',(0.984945083573756,6.69493630905805,-51.2436214734303));
#35519=CARTESIAN_POINT('Ctrl Pts',(0.81354475834823,6.7201523678614,-51.2354988877101));
#35520=CARTESIAN_POINT('Ctrl Pts',(0.641162322375299,6.73878390575607,-51.2273763019899));
#35521=CARTESIAN_POINT('Ctrl Pts',(0.468347659396175,6.75077324977948,-51.2192537162697));
#35522=CARTESIAN_POINT('Ctrl Pts',(0.295512230956435,6.76276403444598,-51.2111301545372));
#35523=CARTESIAN_POINT('Ctrl Pts',(0.122244837314489,6.76811101184451,-51.2030065928047));
#35524=CARTESIAN_POINT('Ctrl Pts',(-0.0509018418445705,6.76680855370512,
-51.1948830310722));
#35525=CARTESIAN_POINT('Ctrl Pts',(-0.224174637812543,6.76550514687954,
-51.186753552289));
#35526=CARTESIAN_POINT('Ctrl Pts',(-0.397326177299663,6.75754263387956,
-51.1786240735057));
#35527=CARTESIAN_POINT('Ctrl Pts',(-0.569805467044783,6.74296750175514,
-51.1704945947225));
#35528=CARTESIAN_POINT('Ctrl Pts',(-0.742355073561008,6.72838642760584,
-51.1623618016939));
#35529=CARTESIAN_POINT('Ctrl Pts',(-0.914231521030211,6.70718740547868,
-51.1542290086652));
#35530=CARTESIAN_POINT('Ctrl Pts',(-1.08489150021608,6.6794684992714,-51.1460962156366));
#35531=CARTESIAN_POINT('Ctrl Pts',(-1.25573704623894,6.65171945295878,-51.1379545794293));
#35532=CARTESIAN_POINT('Ctrl Pts',(-1.42536312374954,6.61743643522956,-51.129812943222));
#35533=CARTESIAN_POINT('Ctrl Pts',(-1.5932383939877,6.57676823522948,-51.1216713070148));
#35534=CARTESIAN_POINT('Ctrl Pts',(-1.67876856392686,6.55604833972497,-51.1175232539549));
#35535=CARTESIAN_POINT('Ctrl Pts',(-1.76384451885883,6.5336717996434,-51.113375200895));
#35536=CARTESIAN_POINT('Ctrl Pts',(-1.84839780253586,6.50966316821236,-51.1092271478351));
#35537=CARTESIAN_POINT('Ctrl Pts',(-2.02045205489797,6.46080891972589,-51.100786432857));
#35538=CARTESIAN_POINT('Ctrl Pts',(-2.19069537674778,6.40509316346649,-51.092345717879));
#35539=CARTESIAN_POINT('Ctrl Pts',(-2.35856180545217,6.34267098388859,-51.0839050029009));
#35540=CARTESIAN_POINT('Ctrl Pts',(-2.52630135280056,6.28029598593509,-51.0754706678129));
#35541=CARTESIAN_POINT('Ctrl Pts',(-2.69166727696468,6.2112247852629,-51.0670363327249));
#35542=CARTESIAN_POINT('Ctrl Pts',(-2.85410912028243,6.13566215901109,-51.0586019976369));
#35543=CARTESIAN_POINT('Ctrl Pts',(-3.01645312720168,6.06014504304816,-51.0501727424283));
#35544=CARTESIAN_POINT('Ctrl Pts',(-3.175876262803,5.97814443633935,-51.0417434872197));
#35545=CARTESIAN_POINT('Ctrl Pts',(-3.33184802553106,5.88991321962937,-51.0333142320111));
#35546=CARTESIAN_POINT('Ctrl Pts',(-3.48774977359163,5.80172160931475,-51.024888760638));
#35547=CARTESIAN_POINT('Ctrl Pts',(-3.64020294819763,5.70730512957085,-51.0164632892649));
#35548=CARTESIAN_POINT('Ctrl Pts',(-3.78870129001075,5.60696277275594,-51.0080378178918));
#35549=CARTESIAN_POINT('Ctrl Pts',(-3.93715573140377,5.50665008005419,-50.9996148373327));
#35550=CARTESIAN_POINT('Ctrl Pts',(-4.08165739561812,5.4004151903653,-50.9911918567735));
#35551=CARTESIAN_POINT('Ctrl Pts',(-4.2217283501773,5.2886008298329,-50.9827688762143));
#35552=CARTESIAN_POINT('Ctrl Pts',(-4.3618016240215,5.17678461788618,-50.974345756188));
#35553=CARTESIAN_POINT('Ctrl Pts',(-4.49744377700071,5.05938895330167,-50.9659226361617));
#35554=CARTESIAN_POINT('Ctrl Pts',(-4.62820884200249,4.93679773890018,-50.9574995161354));
#35555=CARTESIAN_POINT('Ctrl Pts',(-4.75897842907795,4.81420228509039,-50.9490761048236));
#35556=CARTESIAN_POINT('Ctrl Pts',(-4.88487034847325,4.68641115119791,-50.9406526935117));
#35557=CARTESIAN_POINT('Ctrl Pts',(-5.00547438240334,4.55384619932469,-50.9322292821999));
#35558=CARTESIAN_POINT('Ctrl Pts',(-5.12609940702924,4.42125817500115,-50.9238044048238));
#35559=CARTESIAN_POINT('Ctrl Pts',(-5.24143448689091,4.28389492287238,-50.9153795274477));
#35560=CARTESIAN_POINT('Ctrl Pts',(-5.35110845808286,4.14221284699785,-50.9069546500717));
#35561=CARTESIAN_POINT('Ctrl Pts',(-5.46081681800385,4.00048634612017,-50.8985271310403));
#35562=CARTESIAN_POINT('Ctrl Pts',(-5.56486032620094,3.85443858522592,-50.8900996120089));
#35563=CARTESIAN_POINT('Ctrl Pts',(-5.66290984476275,3.70455680076432,-50.8816720929776));
#35564=CARTESIAN_POINT('Ctrl Pts',(-5.76104729034368,3.55454060811059,-50.8732370164728));
#35565=CARTESIAN_POINT('Ctrl Pts',(-5.8531798231717,3.40068380120735,-50.8648019399681));
#35566=CARTESIAN_POINT('Ctrl Pts',(-5.93902257667899,3.24350116906057,-50.8563668634633));
#35567=CARTESIAN_POINT('Ctrl Pts',(-6.0249068185538,3.08624256951358,-50.8479277102306));
#35568=CARTESIAN_POINT('Ctrl Pts',(-6.10449506578661,2.92565523530496,-50.8394885569979));
#35569=CARTESIAN_POINT('Ctrl Pts',(-6.17754948354762,2.7622764847713,-50.8310494037651));
#35570=CARTESIAN_POINT('Ctrl Pts',(-6.25068508524938,2.59871617463853,-50.8226008722671));
#35571=CARTESIAN_POINT('Ctrl Pts',(-6.31727222048796,2.4323585575581,-50.814152340769));
#35572=CARTESIAN_POINT('Ctrl Pts',(-6.37712161930826,2.26375989286657,-50.8057038092709));
#35573=CARTESIAN_POINT('Ctrl Pts',(-6.41019035397727,2.17060366042096,-50.8010357215046));
#35574=CARTESIAN_POINT('Ctrl Pts',(-6.44120299326327,2.07676352947594,-50.7963676337383));
#35575=CARTESIAN_POINT('Ctrl Pts',(-6.4701342208643,1.98233502819294,-50.791699545972));
#35576=CARTESIAN_POINT('Ctrl Pts',(-6.52561322009058,1.80125737667182,-50.7827479438781));
#35577=CARTESIAN_POINT('Ctrl Pts',(-6.57354245803368,1.61766672833935,-50.7737963417841));
#35578=CARTESIAN_POINT('Ctrl Pts',(-6.61370831146901,1.43218412601375,-50.7648447396901));
#35579=CARTESIAN_POINT('Ctrl Pts',(-6.65378960644619,1.24709200768197,-50.7559119827994));
#35580=CARTESIAN_POINT('Ctrl Pts',(-6.68614005816093,1.06011612052976,-50.7469792259087));
#35581=CARTESIAN_POINT('Ctrl Pts',(-6.71059549156741,0.871892853827292,
-50.7380464690179));
#35582=CARTESIAN_POINT('Ctrl Pts',(-6.73497102105433,0.684284574253256,
-50.7291428983729));
#35583=CARTESIAN_POINT('Ctrl Pts',(-6.75150295156409,0.495437290930622,
-50.7202393277279));
#35584=CARTESIAN_POINT('Ctrl Pts',(-6.76007802694969,0.305996845657041,
-50.7113357570829));
#35585=CARTESIAN_POINT('Ctrl Pts',(-6.7646225908784,0.205598403017538,-50.7066170993253));
#35586=CARTESIAN_POINT('Ctrl Pts',(-6.76693313590177,0.105033600446035,
-50.7018984415677));
#35587=CARTESIAN_POINT('Ctrl Pts',(-6.76699856951929,0.0044000140721489,
-50.6971797838101));
#35588=CARTESIAN_POINT('Ctrl Pts',(-6.767,7.54030492757439E-13,-50.6971797838101));
#35589=CARTESIAN_POINT('Ctrl Pts',(-6.76700000000002,-0.186007249559271,
-50.6884302719974));
#35590=CARTESIAN_POINT('Ctrl Pts',(-6.75932637294251,-0.372014355815471,
-50.6796807601846));
#35591=CARTESIAN_POINT('Ctrl Pts',(-6.74400518263367,-0.557389537585863,
-50.6709312483719));
#35592=CARTESIAN_POINT('Ctrl Pts',(-6.72868405703733,-0.742763936382495,
-50.6621817735147));
#35593=CARTESIAN_POINT('Ctrl Pts',(-6.70571545643565,-0.927506130404962,
-50.6534322986575));
#35594=CARTESIAN_POINT('Ctrl Pts',(-6.67517739401572,-1.11098864009564,
-50.6446828238003));
#35595=CARTESIAN_POINT('Ctrl Pts',(-6.64463945804386,-1.29447039004558,
-50.6359333851717));
#35596=CARTESIAN_POINT('Ctrl Pts',(-6.6065321700272,-1.47669218339293,-50.6271839465432));
#35597=CARTESIAN_POINT('Ctrl Pts',(-6.56098496085476,-1.65703510627797,
-50.6184345079147));
#35598=CARTESIAN_POINT('Ctrl Pts',(-6.5154379364955,-1.83737729740029,-50.6096851047881));
#35599=CARTESIAN_POINT('Ctrl Pts',(-6.46245112156888,-2.01584035544979,
-50.6009357016615));
#35600=CARTESIAN_POINT('Ctrl Pts',(-6.40220448361706,-2.19181813797441,
-50.5921862985348));
#35601=CARTESIAN_POINT('Ctrl Pts',(-6.34195808511951,-2.36779522106362,
-50.5834369301833));
#35602=CARTESIAN_POINT('Ctrl Pts',(-6.2744520141632,-2.54128677725829,-50.5746875618317));
#35603=CARTESIAN_POINT('Ctrl Pts',(-6.19991555052676,-2.71170355428768,
-50.5659381934802));
#35604=CARTESIAN_POINT('Ctrl Pts',(-6.12537937695062,-2.8821196681364,-50.557188859177));
#35605=CARTESIAN_POINT('Ctrl Pts',(-6.04381298028282,-3.04946076420006,
-50.5484395248738));
#35606=CARTESIAN_POINT('Ctrl Pts',(-5.95549339308799,-3.21315848424651,
-50.5396901905706));
#35607=CARTESIAN_POINT('Ctrl Pts',(-5.86717414225612,-3.37685558085424,
-50.5309408895891));
#35608=CARTESIAN_POINT('Ctrl Pts',(-5.77210188843856,-3.53690907700344,
-50.5221915886075));
#35609=CARTESIAN_POINT('Ctrl Pts',(-5.67059953311147,-3.69277537024336,
-50.513442287626));
#35610=CARTESIAN_POINT('Ctrl Pts',(-5.56909755592466,-3.84864108281377,
-50.5046930192393));
#35611=CARTESIAN_POINT('Ctrl Pts',(-5.46116568154707,-4.00031938355183,
-50.4959437508527));
#35612=CARTESIAN_POINT('Ctrl Pts',(-5.347170484881,-4.14729511918522,-50.4871944824661));
#35613=CARTESIAN_POINT('Ctrl Pts',(-5.23317570343005,-4.29427031947545,
-50.4784452459477));
#35614=CARTESIAN_POINT('Ctrl Pts',(-5.11311781951224,-4.43654276249929,
-50.4696960094294));
#35615=CARTESIAN_POINT('Ctrl Pts',(-4.98740458928897,-4.57362924412761,
-50.460946772911));
#35616=CARTESIAN_POINT('Ctrl Pts',(-4.86169180652367,-4.71071523781654,
-50.4521975675343));
#35617=CARTESIAN_POINT('Ctrl Pts',(-4.73032391141173,-4.84261509584881,
-50.4434483621576));
#35618=CARTESIAN_POINT('Ctrl Pts',(-4.593747069469,-4.96888084599993,-50.4346991567808));
#35619=CARTESIAN_POINT('Ctrl Pts',(-4.45717070231126,-5.09514615721074,
-50.4259499818192));
#35620=CARTESIAN_POINT('Ctrl Pts',(-4.31538563497031,-5.21577720520855,
-50.4172008068575));
#35621=CARTESIAN_POINT('Ctrl Pts',(-4.16887340951763,-5.33036429293692,
-50.4084516318958));
#35622=CARTESIAN_POINT('Ctrl Pts',(-4.02236168122246,-5.44495099183882,
-50.3997024866226));
#35623=CARTESIAN_POINT('Ctrl Pts',(-3.87112305262948,-5.5534935949809,-50.3909533413493));
#35624=CARTESIAN_POINT('Ctrl Pts',(-3.71567116928769,-5.6556234635736,-50.3822041960761));
#35625=CARTESIAN_POINT('Ctrl Pts',(-3.56021980053097,-5.75775299409059,
-50.3734550797647));
#35626=CARTESIAN_POINT('Ctrl Pts',(-3.40055544441883,-5.85346967519995,
-50.3647059634533));
#35627=CARTESIAN_POINT('Ctrl Pts',(-3.23722035886657,-5.94244843041484,
-50.355956847142));
#35628=CARTESIAN_POINT('Ctrl Pts',(-3.07388580043289,-6.03142689847554,
-50.347207759066));
#35629=CARTESIAN_POINT('Ctrl Pts',(-2.90688078789007,-6.11366734708005,
-50.3384586709899));
#35630=CARTESIAN_POINT('Ctrl Pts',(-2.73677250610162,-6.18889047001531,
-50.3297095829139));
#35631=CARTESIAN_POINT('Ctrl Pts',(-2.56666475916715,-6.26411335643424,
-50.3209605223468));
#35632=CARTESIAN_POINT('Ctrl Pts',(-2.39345402456885,-6.33231884545334,
-50.3122114617796));
#35633=CARTESIAN_POINT('Ctrl Pts',(-2.2177285594387,-6.39327529804951,-50.3034624012124));
#35634=CARTESIAN_POINT('Ctrl Pts',(-2.04200363223416,-6.45423156404757,
-50.2947133674276));
#35635=CARTESIAN_POINT('Ctrl Pts',(-1.86376426060879,-6.50793874412497,
-50.2859643336429));
#35636=CARTESIAN_POINT('Ctrl Pts',(-1.68361577621555,-6.55421443943346,
-50.2772152998581));
#35637=CARTESIAN_POINT('Ctrl Pts',(-1.50346782833097,-6.60048999692614,
-50.2684662921292));
#35638=CARTESIAN_POINT('Ctrl Pts',(-1.32141105657284,-6.63933404265182,
-50.2597172844003));
#35639=CARTESIAN_POINT('Ctrl Pts',(-1.13806375346447,-6.67061465631544,
-50.2509682766714));
#35640=CARTESIAN_POINT('Ctrl Pts',(-0.954716981169393,-6.70189517941779,
-50.242219294272));
#35641=CARTESIAN_POINT('Ctrl Pts',(-0.77007996744194,-6.72561226609007,
-50.2334703118726));
#35642=CARTESIAN_POINT('Ctrl Pts',(-0.584779764073002,-6.74168536995985,
-50.2247213294731));
#35643=CARTESIAN_POINT('Ctrl Pts',(-0.391489587592836,-6.75845153117873,
-50.2155950990575));
#35644=CARTESIAN_POINT('Ctrl Pts',(-0.197478091805063,-6.76689985146395,
-50.2064688686419));
#35645=CARTESIAN_POINT('Ctrl Pts',(-0.00346214753080522,-6.76699911434415,
-50.1973426382263));
#35646=CARTESIAN_POINT('Ctrl Pts',(0.184490798484886,-6.76709527525934,
-50.1885016025112));
#35647=CARTESIAN_POINT('Ctrl Pts',(0.372447602155044,-6.75935633790762,
-50.179660566796));
#35648=CARTESIAN_POINT('Ctrl Pts',(0.559756448194499,-6.74380914014511,
-50.1708195310809));
#35649=CARTESIAN_POINT('Ctrl Pts',(0.745136131043656,-6.72842206873151,
-50.1620695524676));
#35650=CARTESIAN_POINT('Ctrl Pts',(0.929880851945357,-6.70538686355719,
-50.1533195738543));
#35651=CARTESIAN_POINT('Ctrl Pts',(1.11336305057495,-6.67478177303307,-50.144569595241));
#35652=CARTESIAN_POINT('Ctrl Pts',(1.29684337090154,-6.64417699581255,-50.135819706201));
#35653=CARTESIAN_POINT('Ctrl Pts',(1.47906091205219,-6.60600253548053,-50.127069817161));
#35654=CARTESIAN_POINT('Ctrl Pts',(1.65939671095249,-6.56038806441205,-50.118319928121));
#35655=CARTESIAN_POINT('Ctrl Pts',(1.83973072369188,-6.51477404513842,-50.1095701257455));
#35656=CARTESIAN_POINT('Ctrl Pts',(2.01818275357064,-6.46172023288652,-50.1008203233701));
#35657=CARTESIAN_POINT('Ctrl Pts',(2.19414664033354,-6.40140683918098,-50.0920705209946));
#35658=CARTESIAN_POINT('Ctrl Pts',(2.37010884271288,-6.34109402281487,-50.083320802375));
#35659=CARTESIAN_POINT('Ctrl Pts',(2.54358267847834,-6.2735218569978,-50.0745710837555));
#35660=CARTESIAN_POINT('Ctrl Pts',(2.71397890841771,-6.19891986435249,-50.0658213651359));
#35661=CARTESIAN_POINT('Ctrl Pts',(2.88437356388977,-6.12431856103227,-50.0570717273641));
#35662=CARTESIAN_POINT('Ctrl Pts',(3.05169040787213,-6.04268767582537,-50.0483220895923));
#35663=CARTESIAN_POINT('Ctrl Pts',(3.215361125121,-5.95430447953921,-50.0395724518205));
#35664=CARTESIAN_POINT('Ctrl Pts',(3.3790303844288,-5.86592207055021,-50.0308228919884));
#35665=CARTESIAN_POINT('Ctrl Pts',(3.53905332980003,-5.77078760703359,-50.0220733321563));
#35666=CARTESIAN_POINT('Ctrl Pts',(3.69488643041914,-5.66922422085284,-50.0133237723243));
#35667=CARTESIAN_POINT('Ctrl Pts',(3.85071819468771,-5.56766170563139,-50.0045742875243));
#35668=CARTESIAN_POINT('Ctrl Pts',(4.0023599459926,-5.45967053456226,-49.9958248027243));
#35669=CARTESIAN_POINT('Ctrl Pts',(4.14929662974342,-5.34561750206652,-49.9870753179243));
#35670=CARTESIAN_POINT('Ctrl Pts',(4.29623210225083,-5.23156540974434,-49.9783259052489));
#35671=CARTESIAN_POINT('Ctrl Pts',(4.43846235842153,-5.11145173172155,-49.9695764925736));
#35672=CARTESIAN_POINT('Ctrl Pts',(4.57550431797461,-4.98568443006531,-49.9608270798982));
#35673=CARTESIAN_POINT('Ctrl Pts',(4.71254519337526,-4.85991812336658,-49.9520777364403));
#35674=CARTESIAN_POINT('Ctrl Pts',(4.84439764315016,-4.72849847631068,-49.9433283929824));
#35675=CARTESIAN_POINT('Ctrl Pts',(4.97061384196717,-4.5918718442531,-49.9345790495245));
#35676=CARTESIAN_POINT('Ctrl Pts',(5.09682908420235,-4.45524624767715,-49.9258297723772));
#35677=CARTESIAN_POINT('Ctrl Pts',(5.21740796650197,-4.31341395556861,-49.9170804952298));
#35678=CARTESIAN_POINT('Ctrl Pts',(5.33194095942275,-4.16685668162826,-49.9083312180825));
#35679=CARTESIAN_POINT('Ctrl Pts',(5.44647312235168,-4.02030046975168,-49.8995820043389));
#35680=CARTESIAN_POINT('Ctrl Pts',(5.55495930712333,-3.86901957035484,-49.8908327905954));
#35681=CARTESIAN_POINT('Ctrl Pts',(5.65703106079848,-3.71352778058294,-49.8820835768518));
#35682=CARTESIAN_POINT('Ctrl Pts',(5.75910210868779,-3.55803706597532,-49.8733344236056));
#35683=CARTESIAN_POINT('Ctrl Pts',(5.85475865698584,-3.39833575880839,-49.8645852703594));
#35684=CARTESIAN_POINT('Ctrl Pts',(5.9436758306909,-3.23496624706672,-49.8558361171132));
#35685=CARTESIAN_POINT('Ctrl Pts',(6.03259241910112,-3.07159781070032,-49.8470870214581));
#35686=CARTESIAN_POINT('Ctrl Pts',(6.11476958471009,-2.90456146975747,-49.838337925803));
#35687=CARTESIAN_POINT('Ctrl Pts',(6.18992823574433,-2.73442451648151,-49.8295888301478));
#35688=CARTESIAN_POINT('Ctrl Pts',(6.26508641700982,-2.56428862662302,-49.8208397891777));
#35689=CARTESIAN_POINT('Ctrl Pts',(6.33322605570343,-2.39105242531156,-49.8120907482076));
#35690=CARTESIAN_POINT('Ctrl Pts',(6.39411573747812,-2.215304253536,-49.8033417072375));
#35691=CARTESIAN_POINT('Ctrl Pts',(6.45500505889165,-2.03955712188435,-49.7945927180465));
#35692=CARTESIAN_POINT('Ctrl Pts',(6.50864441544964,-1.86129832025448,-49.7858437288555));
#35693=CARTESIAN_POINT('Ctrl Pts',(6.55485164049937,-1.68113324012188,-49.7770947396645));
#35694=CARTESIAN_POINT('Ctrl Pts',(6.60199852639138,-1.49730435912772,-49.7681678327876));
#35695=CARTESIAN_POINT('Ctrl Pts',(6.64140767441036,-1.3114911317352,-49.7592409259107));
#35696=CARTESIAN_POINT('Ctrl Pts',(6.67293975269625,-1.12435050446295,-49.7503140190338));
#35697=CARTESIAN_POINT('Ctrl Pts',(6.70384664831526,-0.940920291562351,
-49.7415641048498));
#35698=CARTESIAN_POINT('Ctrl Pts',(6.72718585889682,-0.756215114276515,
-49.7328141906658));
#35699=CARTESIAN_POINT('Ctrl Pts',(6.74287810451877,-0.570862389373684,
-49.7240642764819));
#35700=CARTESIAN_POINT('Ctrl Pts',(6.75857004154131,-0.385513309566699,
-49.7153145343713));
#35701=CARTESIAN_POINT('Ctrl Pts',(6.7666152903556,-0.199516993257867,-49.7065647922607));
#35702=CARTESIAN_POINT('Ctrl Pts',(6.76698652348897,-0.0135052182037693,
-49.6978150501501));
#35703=CARTESIAN_POINT('Ctrl Pts',(6.76735774981521,0.172503146039211,-49.6890654684795));
#35704=CARTESIAN_POINT('Ctrl Pts',(6.76005524147477,0.358526681833818,-49.6803158868088));
#35705=CARTESIAN_POINT('Ctrl Pts',(6.74510380214878,0.543933542115243,-49.6715663051382));
#35706=CARTESIAN_POINT('Ctrl Pts',(6.73015261710975,0.729337249085073,-49.6628168722762));
#35707=CARTESIAN_POINT('Ctrl Pts',(6.70755278444601,0.914124015854987,-49.6540674394143));
#35708=CARTESIAN_POINT('Ctrl Pts',(6.67738106408284,1.09766621749415,-49.6453180065524));
#35709=CARTESIAN_POINT('Ctrl Pts',(6.64720981677249,1.28120554143349,-49.63656871087));
#35710=CARTESIAN_POINT('Ctrl Pts',(6.60946696581517,1.46350005650645,-49.6278194151877));
#35711=CARTESIAN_POINT('Ctrl Pts',(6.56428070010989,1.64393062206556,-49.6190701195054));
#35712=CARTESIAN_POINT('Ctrl Pts',(6.51909508282734,1.82435859844675,-49.6103209493754));
#35713=CARTESIAN_POINT('Ctrl Pts',(6.46646633415654,2.00292240086586,-49.6015717792454));
#35714=CARTESIAN_POINT('Ctrl Pts',(6.40657319597184,2.17901557696477,-49.5928226091154));
#35715=CARTESIAN_POINT('Ctrl Pts',(6.34668083768285,2.35510646007461,-49.5840735529123));
#35716=CARTESIAN_POINT('Ctrl Pts',(6.27952437143873,2.5287265099656,-49.5753244967092));
#35717=CARTESIAN_POINT('Ctrl Pts',(6.20533187335121,2.69928607997958,-49.5665754405061));
#35718=CARTESIAN_POINT('Ctrl Pts',(6.12831449784238,2.87633970115428,-49.5574932642173));
#35719=CARTESIAN_POINT('Ctrl Pts',(6.04371489463139,3.05009490562377,-49.5484110879285));
#35720=CARTESIAN_POINT('Ctrl Pts',(5.95184265120477,3.21991584599657,-49.5393289116396));
#35721=CARTESIAN_POINT('Ctrl Pts',(5.86333281335475,3.38352155905331,-49.5305791312852));
#35722=CARTESIAN_POINT('Ctrl Pts',(5.76807337235663,3.5434756090386,-49.5218293509308));
#35723=CARTESIAN_POINT('Ctrl Pts',(5.66638790086329,3.69923467178687,-49.5130795705764));
#35724=CARTESIAN_POINT('Ctrl Pts',(5.56470608502714,3.85498813489805,-49.5043301047821));
#35725=CARTESIAN_POINT('Ctrl Pts',(5.45659885766922,4.00654667256303,-49.4955806389878));
#35726=CARTESIAN_POINT('Ctrl Pts',(5.34243340580475,4.15339551506252,-49.4868311731936));
#35727=CARTESIAN_POINT('Ctrl Pts',(5.22827145140558,4.30023985883914,-49.4780819754397));
#35728=CARTESIAN_POINT('Ctrl Pts',(5.10805181978051,4.44237456993087,-49.4693327776858));
#35729=CARTESIAN_POINT('Ctrl Pts',(4.9821828128251,4.57931691626494,-49.4605835799319));
#35730=CARTESIAN_POINT('Ctrl Pts',(4.85631699296187,4.71625579512204,-49.4518346037139));
#35731=CARTESIAN_POINT('Ctrl Pts',(4.72480227791797,4.8480023613581,-49.4430856274959));
#35732=CARTESIAN_POINT('Ctrl Pts',(4.58808530848072,4.97410918678947,-49.4343366512779));
#35733=CARTESIAN_POINT('Ctrl Pts',(4.45135945056923,5.1002242108905,-49.4255871062567));
#35734=CARTESIAN_POINT('Ctrl Pts',(4.30943087207987,5.22069856612031,-49.4168375612355));
#35735=CARTESIAN_POINT('Ctrl Pts',(4.16278164322408,5.3351230530173,-49.4080880162143));
#35736=CARTESIAN_POINT('Ctrl Pts',(4.01614103534339,5.44954081331465,-49.3993389855471));
#35737=CARTESIAN_POINT('Ctrl Pts',(3.8647805583337,5.55790924068367,-49.3905899548798));
#35738=CARTESIAN_POINT('Ctrl Pts',(3.70921425811917,5.65986029751313,-49.3818409242126));
#35739=CARTESIAN_POINT('Ctrl Pts',(3.55364584530093,5.7618127388467,-49.3730917747327));
#35740=CARTESIAN_POINT('Ctrl Pts',(3.39387173464324,5.85734747818075,-49.3643426252529));
#35741=CARTESIAN_POINT('Ctrl Pts',(3.23043456092393,5.94614005448814,-49.355593475773));
#35742=CARTESIAN_POINT('Ctrl Pts',(3.18690768806384,5.96978744811286,-49.35326338704));
#35743=CARTESIAN_POINT('Ctrl Pts',(3.14312114982877,5.99295688499302,-49.350933298307));
#35744=CARTESIAN_POINT('Ctrl Pts',(3.0990855038472,6.01564277861013,-49.3486032095739));
#35745=CARTESIAN_POINT('Origin',(0.,0.,-63.6971797838103));
#35746=CARTESIAN_POINT('',(3.0990855038472,6.01564277861013,-46.9540128207846));
#35747=CARTESIAN_POINT('',(3.0990855038472,6.01564277861012,-47.3486841594369));
#35748=CARTESIAN_POINT('',(3.09908550384721,6.01564277861012,-63.6971797838103));
#35749=CARTESIAN_POINT('',(-6.76699650576387,-0.00687684372451031,-48.3028202162139));
#35750=CARTESIAN_POINT('Ctrl Pts',(-6.76699650576336,-0.00687684422915549,
-48.30282021619));
#35751=CARTESIAN_POINT('Ctrl Pts',(-6.76681092372738,-0.189494473350243,
-48.2941842225582));
#35752=CARTESIAN_POINT('Ctrl Pts',(-6.75923366544663,-0.37185469943169,
-48.2855482289264));
#35753=CARTESIAN_POINT('Ctrl Pts',(-6.74432341447577,-0.553525682289361,
-48.2769122352947));
#35754=CARTESIAN_POINT('Ctrl Pts',(-6.72993483437743,-0.728840470316843,
-48.268578392602));
#35755=CARTESIAN_POINT('Ctrl Pts',(-6.70868774546245,-0.903818148243271,
-48.2602445499093));
#35756=CARTESIAN_POINT('Ctrl Pts',(-6.68060207070955,-1.07788912826471,
-48.2519107072166));
#35757=CARTESIAN_POINT('Ctrl Pts',(-6.65254949847752,-1.25175494361415,
-48.2435866870119));
#35758=CARTESIAN_POINT('Ctrl Pts',(-6.617674451869,-1.42471584944315,-48.2352626668071));
#35759=CARTESIAN_POINT('Ctrl Pts',(-6.57604873628253,-1.5962055062043,-48.2269386466024));
#35760=CARTESIAN_POINT('Ctrl Pts',(-6.53446444985352,-1.76752448308903,
-48.2186229111115));
#35761=CARTESIAN_POINT('Ctrl Pts',(-6.48614296206281,-1.93737479235349,
-48.2103071756207));
#35762=CARTESIAN_POINT('Ctrl Pts',(-6.43120746594508,-2.10519821631414,
-48.2019914401298));
#35763=CARTESIAN_POINT('Ctrl Pts',(-6.37631658031481,-2.27288535890342,
-48.1936824574498));
#35764=CARTESIAN_POINT('Ctrl Pts',(-6.31482249617295,-2.43854856671804,
-48.1853734747698));
#35765=CARTESIAN_POINT('Ctrl Pts',(-6.24689883491245,-2.60164254777044,
-48.1770644920897));
#35766=CARTESIAN_POINT('Ctrl Pts',(-6.17901789267081,-2.76463395462818,
-48.1687607351526));
#35767=CARTESIAN_POINT('Ctrl Pts',(-6.10471556539651,-2.92505903475394,
-48.1604569782154));
#35768=CARTESIAN_POINT('Ctrl Pts',(-6.02421448818061,-3.08239011164954,
-48.1521532212782));
#35769=CARTESIAN_POINT('Ctrl Pts',(-5.94374609246139,-3.23965731592076,
-48.1438528354662));
#35770=CARTESIAN_POINT('Ctrl Pts',(-5.8570841193892,-3.39383271067024,-48.1355524496542));
#35771=CARTESIAN_POINT('Ctrl Pts',(-5.76449839422093,-3.54441070744128,
-48.1272520638422));
#35772=CARTESIAN_POINT('Ctrl Pts',(-5.67193219297302,-3.69495695123081,
-48.1189534283655));
#35773=CARTESIAN_POINT('Ctrl Pts',(-5.57344491033089,-3.84190701225639,
-48.1106547928889));
#35774=CARTESIAN_POINT('Ctrl Pts',(-5.4693513042428,-3.98478171431981,-48.1023561574123));
#35775=CARTESIAN_POINT('Ctrl Pts',(-5.36526237044381,-4.12765000338693,
-48.0940578944237));
#35776=CARTESIAN_POINT('Ctrl Pts',(-5.25556781958377,-4.2664430170399,-48.0857596314351));
#35777=CARTESIAN_POINT('Ctrl Pts',(-5.14062465315402,-4.40071212139412,
-48.0774613684465));
#35778=CARTESIAN_POINT('Ctrl Pts',(-5.02566756759752,-4.53499748516367,
-48.0691621005737));
#35779=CARTESIAN_POINT('Ctrl Pts',(-4.90546082660754,-4.66475758423433,
-48.0608628327009));
#35780=CARTESIAN_POINT('Ctrl Pts',(-4.78040059868223,-4.78957817726348,
-48.0525635648281));
#35781=CARTESIAN_POINT('Ctrl Pts',(-4.65525255832012,-4.91448641446711,
-48.0442584695316));
#35782=CARTESIAN_POINT('Ctrl Pts',(-4.52524446783627,-5.03444796931389,
-48.035953374235));
#35783=CARTESIAN_POINT('Ctrl Pts',(-4.39080877285501,-5.14908606649952,
-48.0276482789385));
#35784=CARTESIAN_POINT('Ctrl Pts',(-4.25632405562877,-5.26376596669652,
-48.0193401551724));
#35785=CARTESIAN_POINT('Ctrl Pts',(-4.11740878530932,-5.37311832013723,
-48.0110320314063));
#35786=CARTESIAN_POINT('Ctrl Pts',(-3.97452730659566,-5.47680761841471,
-48.0027239076402));
#35787=CARTESIAN_POINT('Ctrl Pts',(-3.83149394569557,-5.58060713781724,
-47.9944069523865));
#35788=CARTESIAN_POINT('Ctrl Pts',(-3.68448623877602,-5.678731376263,-47.9860899971329));
#35789=CARTESIAN_POINT('Ctrl Pts',(-3.53399714727165,-5.77088842060526,
-47.9777730418792));
#35790=CARTESIAN_POINT('Ctrl Pts',(-3.42308897646928,-5.83880676014987,
-47.9716435723967));
#35791=CARTESIAN_POINT('Ctrl Pts',(-3.31029048939629,-5.90348495750656,
-47.9655141029141));
#35792=CARTESIAN_POINT('Ctrl Pts',(-3.19580695641193,-5.96482245312877,
-47.9593846334316));
#35793=CARTESIAN_POINT('Ctrl Pts',(-3.03796245889818,-6.04939170010127,
-47.9509336099064));
#35794=CARTESIAN_POINT('Ctrl Pts',(-2.87662549678967,-6.1277632259886,-47.9424825863812));
#35795=CARTESIAN_POINT('Ctrl Pts',(-2.71230981342227,-6.19965035110959,
-47.9340315628561));
#35796=CARTESIAN_POINT('Ctrl Pts',(-2.54813880513028,-6.27147418175354,
-47.9255879802059));
#35797=CARTESIAN_POINT('Ctrl Pts',(-2.38099460535192,-6.33682485914442,
-47.9171443975558));
#35798=CARTESIAN_POINT('Ctrl Pts',(-2.21141483392661,-6.3954619404926,-47.9087008149056));
#35799=CARTESIAN_POINT('Ctrl Pts',(-2.04196131992396,-6.45405536470702,
-47.9002635187658));
#35800=CARTESIAN_POINT('Ctrl Pts',(-1.87007616138224,-6.50594504914093,
-47.891826222626));
#35801=CARTESIAN_POINT('Ctrl Pts',(-1.69631657254045,-6.55093879422825,
-47.8833889264862));
#35802=CARTESIAN_POINT('Ctrl Pts',(-1.52268094791664,-6.59590043970909,
-47.8749576497138));
#35803=CARTESIAN_POINT('Ctrl Pts',(-1.34717388051281,-6.63397587616908,
-47.8665263729415));
#35804=CARTESIAN_POINT('Ctrl Pts',(-1.1703675485453,-6.66502279075714,-47.8580950961691));
#35805=CARTESIAN_POINT('Ctrl Pts',(-0.99363700217148,-6.69605639751381,
-47.8496674333472));
#35806=CARTESIAN_POINT('Ctrl Pts',(-0.815608627353799,-6.7200674310835,
-47.8412397705252));
#35807=CARTESIAN_POINT('Ctrl Pts',(-0.636865241733313,-6.73696457344641,
-47.8328121077033));
#35808=CARTESIAN_POINT('Ctrl Pts',(-0.458176880396861,-6.75385651420056,
-47.8243870392493));
#35809=CARTESIAN_POINT('Ctrl Pts',(-0.278774276837421,-6.76363889987786,
-47.8159619707953));
#35810=CARTESIAN_POINT('Ctrl Pts',(-0.0992461976646876,-6.76627217840438,
-47.8075369023414));
#35811=CARTESIAN_POINT('Ctrl Pts',(-0.0501218199894398,-6.76699272401182,
-47.8052315457276));
#35812=CARTESIAN_POINT('Ctrl Pts',(-0.000988069017895526,-6.76717828963977,
-47.8029261891139));
#35813=CARTESIAN_POINT('Ctrl Pts',(0.0481429585539462,-6.76682874436332,
-47.8006208325001));
#35814=CARTESIAN_POINT('Ctrl Pts',(0.231828103105414,-6.76552190675368,
-47.7920018439757));
#35815=CARTESIAN_POINT('Ctrl Pts',(0.415393127712019,-6.75673202860711,
-47.7833828554512));
#35816=CARTESIAN_POINT('Ctrl Pts',(0.598223281609024,-6.74050576035218,
-47.7747638669267));
#35817=CARTESIAN_POINT('Ctrl Pts',(0.781162967084149,-6.72426977111452,
-47.7661397148589));
#35818=CARTESIAN_POINT('Ctrl Pts',(0.963366600276988,-6.70058852771357,
-47.7575155627911));
#35819=CARTESIAN_POINT('Ctrl Pts',(1.14422588387882,-6.6695604147996,-47.7488914107233));
#35820=CARTESIAN_POINT('Ctrl Pts',(1.33127964660014,-6.6374695806709,-47.7399718791271));
#35821=CARTESIAN_POINT('Ctrl Pts',(1.51689498925224,-6.59751977075137,-47.7310523475308));
#35822=CARTESIAN_POINT('Ctrl Pts',(1.70041251574297,-6.54987681382671,-47.7221328159346));
#35823=CARTESIAN_POINT('Ctrl Pts',(1.87818321959255,-6.50372578864709,-47.7134925980753));
#35824=CARTESIAN_POINT('Ctrl Pts',(2.05398522635387,-6.45035627683088,-47.7048523802161));
#35825=CARTESIAN_POINT('Ctrl Pts',(2.2272360036432,-6.38996938835199,-47.6962121623568));
#35826=CARTESIAN_POINT('Ctrl Pts',(2.40888784028563,-6.32665429463097,-47.6871529738921));
#35827=CARTESIAN_POINT('Ctrl Pts',(2.58773451367977,-6.25562449231842,-47.6780937854274));
#35828=CARTESIAN_POINT('Ctrl Pts',(2.76312921036194,-6.17716811871302,-47.6690345969626));
#35829=CARTESIAN_POINT('Ctrl Pts',(2.93852390704411,-6.09871174510763,-47.6599754084979));
#35830=CARTESIAN_POINT('Ctrl Pts',(3.11046629951489,-6.01282900082008,-47.6509162200332));
#35831=CARTESIAN_POINT('Ctrl Pts',(3.27833978119587,-5.9198629442774,-47.6418570315685));
#35832=CARTESIAN_POINT('Ctrl Pts',(3.44592243384757,-5.82705794490533,-47.6328135375122));
#35833=CARTESIAN_POINT('Ctrl Pts',(3.60960505752249,-5.72710939950069,-47.6237700434559));
#35834=CARTESIAN_POINT('Ctrl Pts',(3.76880665731814,-5.62035455996813,-47.6147265493996));
#35835=CARTESIAN_POINT('Ctrl Pts',(3.9278626359926,-5.51369736869691,-47.6056913273943));
#35836=CARTESIAN_POINT('Ctrl Pts',(4.0824455764349,-5.40024644540185,-47.596656105389));
#35837=CARTESIAN_POINT('Ctrl Pts',(4.23200253835245,-5.28038289476989,-47.5876208833837));
#35838=CARTESIAN_POINT('Ctrl Pts',(4.38129601346128,-5.16073051762015,-47.5786015794725));
#35839=CARTESIAN_POINT('Ctrl Pts',(4.52558100619863,-5.03468822184525,-47.5695822755614));
#35840=CARTESIAN_POINT('Ctrl Pts',(4.66433690647915,-4.90267786243972,-47.5605629716503));
#35841=CARTESIAN_POINT('Ctrl Pts',(4.80291872779106,-4.77083311925062,-47.551554983086));
#35842=CARTESIAN_POINT('Ctrl Pts',(4.93598512779966,-4.63303541823355,-47.5425469945216));
#35843=CARTESIAN_POINT('Ctrl Pts',(5.06304974969824,-4.48974567565698,-47.5335390059572));
#35844=CARTESIAN_POINT('Ctrl Pts',(5.18982739169751,-4.34677955798311,-47.5245513622505));
#35845=CARTESIAN_POINT('Ctrl Pts',(5.31063015538514,-4.1983463360139,-47.5155637185439));
#35846=CARTESIAN_POINT('Ctrl Pts',(5.42500992892582,-4.04494206028422,-47.5065760748372));
#35847=CARTESIAN_POINT('Ctrl Pts',(5.52462678399769,-3.91133756860077,-47.4987484601039));
#35848=CARTESIAN_POINT('Ctrl Pts',(5.61937212936148,-3.77396307825581,-47.4909208453705));
#35849=CARTESIAN_POINT('Ctrl Pts',(5.7089732071335,-3.63316857855946,-47.4830932306371));
#35850=CARTESIAN_POINT('Ctrl Pts',(5.80195731230526,-3.4870581645678,-47.4749700721918));
#35851=CARTESIAN_POINT('Ctrl Pts',(5.88935838056739,-3.33732902469527,-47.4668469137465));
#35852=CARTESIAN_POINT('Ctrl Pts',(5.97089090122295,-3.18445456015517,-47.4587237553012));
#35853=CARTESIAN_POINT('Ctrl Pts',(6.05241767340907,-3.03159087406493,-47.4506011695811));
#35854=CARTESIAN_POINT('Ctrl Pts',(6.12807654991875,-2.87558262799833,-47.442478583861));
#35855=CARTESIAN_POINT('Ctrl Pts',(6.19762784291046,-2.71692806691327,-47.4343559981409));
#35856=CARTESIAN_POINT('Ctrl Pts',(6.26718749320598,-2.55825444184951,-47.4262324364085));
#35857=CARTESIAN_POINT('Ctrl Pts',(6.33063795278142,-2.39693420429176,-47.4181088746761));
#35858=CARTESIAN_POINT('Ctrl Pts',(6.38778758873765,-2.2334857781435,-47.4099853129437));
#35859=CARTESIAN_POINT('Ctrl Pts',(6.44497885142188,-2.06991829921278,-47.4018558341606));
#35860=CARTESIAN_POINT('Ctrl Pts',(6.49586000331293,-1.90421988153315,-47.3937263553775));
#35861=CARTESIAN_POINT('Ctrl Pts',(6.54028904416195,-1.73692493183075,-47.3855968765943));
#35862=CARTESIAN_POINT('Ctrl Pts',(6.58473619794893,-1.56956177892189,-47.3774640835658));
#35863=CARTESIAN_POINT('Ctrl Pts',(6.62272591726439,-1.40060115345188,-47.3693312905373));
#35864=CARTESIAN_POINT('Ctrl Pts',(6.65416734963562,-1.23058761697138,-47.3611984975087));
#35865=CARTESIAN_POINT('Ctrl Pts',(6.68564296979464,-1.06038921656236,-47.3530568613016));
#35866=CARTESIAN_POINT('Ctrl Pts',(6.71055602893938,-0.889135980215188,
-47.3449152250944));
#35867=CARTESIAN_POINT('Ctrl Pts',(6.72886746579591,-0.717378301702387,
-47.3367735888873));
#35868=CARTESIAN_POINT('Ctrl Pts',(6.73819689415205,-0.629870097465948,
-47.3326255358267));
#35869=CARTESIAN_POINT('Ctrl Pts',(6.74581353386546,-0.542230982593186,
-47.3284774827661));
#35870=CARTESIAN_POINT('Ctrl Pts',(6.7517174208235,-0.454533683403681,-47.3243294297055));
#35871=CARTESIAN_POINT('Ctrl Pts',(6.76373101523702,-0.276081793807462,
-47.3158887147275));
#35872=CARTESIAN_POINT('Ctrl Pts',(6.76867427935843,-0.0970214736078914,
-47.3074479997494));
#35873=CARTESIAN_POINT('Ctrl Pts',(6.76650240531966,0.0820621642614203,
-47.2990072847713));
#35874=CARTESIAN_POINT('Ctrl Pts',(6.76433217288562,0.261010442279826,-47.2905729496833));
#35875=CARTESIAN_POINT('Ctrl Pts',(6.75505752695338,0.439981670637915,-47.2821386145952));
#35876=CARTESIAN_POINT('Ctrl Pts',(6.73868567038815,0.618388579863343,-47.2737042795072));
#35877=CARTESIAN_POINT('Ctrl Pts',(6.72232367435799,0.796688037158855,-47.2652750242986));
#35878=CARTESIAN_POINT('Ctrl Pts',(6.69887302004291,0.974423521735699,-47.25684576909));
#35879=CARTESIAN_POINT('Ctrl Pts',(6.66839292568548,1.15101033386669,-47.2484165138813));
#35880=CARTESIAN_POINT('Ctrl Pts',(6.63792651363609,1.32751787737294,-47.2399910425083));
#35881=CARTESIAN_POINT('Ctrl Pts',(6.60043700983284,1.50287744853693,-47.2315655711353));
#35882=CARTESIAN_POINT('Ctrl Pts',(6.55603521757861,1.67651162413774,-47.2231400997623));
#35883=CARTESIAN_POINT('Ctrl Pts',(6.51164655178232,1.85009446843894,-47.2147171192031));
#35884=CARTESIAN_POINT('Ctrl Pts',(6.46034975520118,2.021952611711,-47.2062941386438));
#35885=CARTESIAN_POINT('Ctrl Pts',(6.40230635471168,2.19152055441387,-47.1978711580846));
#35886=CARTESIAN_POINT('Ctrl Pts',(6.34426199314389,2.36109130481006,-47.1894480380582));
#35887=CARTESIAN_POINT('Ctrl Pts',(6.27947090616957,2.5283714613647,-47.1810249180319));
#35888=CARTESIAN_POINT('Ctrl Pts',(6.20814416355303,2.6928117358149,-47.1726017980056));
#35889=CARTESIAN_POINT('Ctrl Pts',(6.13681495433881,2.85725769688395,-47.1641783866937));
#35890=CARTESIAN_POINT('Ctrl Pts',(6.05894977139855,3.01886327400483,-47.1557549753819));
#35891=CARTESIAN_POINT('Ctrl Pts',(5.97480747411099,3.17710003734655,-47.14733156407));
#35892=CARTESIAN_POINT('Ctrl Pts',(5.89065053216109,3.33536434122428,-47.1389066866939));
#35893=CARTESIAN_POINT('Ctrl Pts',(5.80021445429574,3.4902583679092,-47.1304818093178));
#35894=CARTESIAN_POINT('Ctrl Pts',(5.7038037863806,3.64127880921941,-47.1220569319417));
#35895=CARTESIAN_POINT('Ctrl Pts',(5.60736288849981,3.79234660361671,-47.1136294129102));
#35896=CARTESIAN_POINT('Ctrl Pts',(5.50494384497838,3.93953811011377,-47.1052018938788));
#35897=CARTESIAN_POINT('Ctrl Pts',(5.39689439782721,4.08237919094997,-47.0967743748474));
#35898=CARTESIAN_POINT('Ctrl Pts',(5.28874805610789,4.22534836614671,-47.0883392983426));
#35899=CARTESIAN_POINT('Ctrl Pts',(5.17496142325378,4.36395905411746,-47.0799042218378));
#35900=CARTESIAN_POINT('Ctrl Pts',(5.0559231066275,4.49776950719689,-47.071469145333));
#35901=CARTESIAN_POINT('Ctrl Pts',(4.93682725799934,4.63164463174897,-47.0630299921003));
#35902=CARTESIAN_POINT('Ctrl Pts',(4.81247489104588,4.76071465088317,-47.0545908388675));
#35903=CARTESIAN_POINT('Ctrl Pts',(4.68329168001268,4.8845744993729,-47.0461516856347));
#35904=CARTESIAN_POINT('Ctrl Pts',(4.55396491021281,5.008571990881,-47.0377031541366));
#35905=CARTESIAN_POINT('Ctrl Pts',(4.41979681578023,5.1273475177224,-47.0292546226385));
#35906=CARTESIAN_POINT('Ctrl Pts',(4.28124727649392,5.240535350278,-47.0208060911404));
#35907=CARTESIAN_POINT('Ctrl Pts',(4.20469416078772,5.30307530015296,-47.0161380033744));
#35908=CARTESIAN_POINT('Ctrl Pts',(4.126803981546,5.36391010883663,-47.0114699156085));
#35909=CARTESIAN_POINT('Ctrl Pts',(4.04765813864944,5.42298373523515,-47.0068018278425));
#35910=CARTESIAN_POINT('Ctrl Pts',(3.90790280804022,5.5272956470863,-46.9985589419856));
#35911=CARTESIAN_POINT('Ctrl Pts',(3.76391957585603,5.62634572550133,-46.9903160561287));
#35912=CARTESIAN_POINT('Ctrl Pts',(3.61613986786052,5.71977459836222,-46.9820731702718));
#35913=CARTESIAN_POINT('Ctrl Pts',(3.46854919040335,5.81308396286589,-46.9738408281978));
#35914=CARTESIAN_POINT('Ctrl Pts',(3.31717201017708,5.90078625774799,-46.9656084861237));
#35915=CARTESIAN_POINT('Ctrl Pts',(3.16247180109459,5.98256308844976,-46.9573761440496));
#35916=CARTESIAN_POINT('Ctrl Pts',(3.14140421151363,5.99369972954853,-46.9562550362946));
#35917=CARTESIAN_POINT('Ctrl Pts',(3.12027504089109,6.00472654081099,-46.9551339285396));
#35918=CARTESIAN_POINT('Ctrl Pts',(3.0990855038472,6.01564277861013,-46.9540128207846));
#35919=CARTESIAN_POINT('Ctrl Pts',(3.09908550384721,6.01564277861012,-48.954361679463));
#35920=CARTESIAN_POINT('Ctrl Pts',(2.93076068015984,6.10235886868149,-48.9454271409862));
#35921=CARTESIAN_POINT('Ctrl Pts',(2.75891733807477,6.18194282230756,-48.9364926025095));
#35922=CARTESIAN_POINT('Ctrl Pts',(2.5841629993212,6.25414986972164,-48.9275580640327));
#35923=CARTESIAN_POINT('Ctrl Pts',(2.48251516857192,6.29614991267796,-48.9223611890287));
#35924=CARTESIAN_POINT('Ctrl Pts',(2.37988278964582,6.33565504789918,-48.9171643140247));
#35925=CARTESIAN_POINT('Ctrl Pts',(2.2763878057268,6.3726248562063,-48.9119674390207));
#35926=CARTESIAN_POINT('Ctrl Pts',(2.11260859236491,6.43112900677864,-48.9037434646031));
#35927=CARTESIAN_POINT('Ctrl Pts',(1.94635542308809,6.48339286898614,-48.8955194901855));
#35928=CARTESIAN_POINT('Ctrl Pts',(1.77814436547817,6.52920298470788,-48.887295515768));
#35929=CARTESIAN_POINT('Ctrl Pts',(1.61011095506566,6.57496472050272,-48.8790802266653));
#35930=CARTESIAN_POINT('Ctrl Pts',(1.44012411697685,6.61428618887802,-48.8708649375627));
#35931=CARTESIAN_POINT('Ctrl Pts',(1.26871845079435,6.64700251937774,-48.86264964846));
#35932=CARTESIAN_POINT('Ctrl Pts',(1.09745942530239,6.67969086045679,-48.8544413876878));
#35933=CARTESIAN_POINT('Ctrl Pts',(0.924784339437631,6.70578525098115,-48.8462331269156));
#35934=CARTESIAN_POINT('Ctrl Pts',(0.751241552077881,6.72517101124065,-48.8380248661435));
#35935=CARTESIAN_POINT('Ctrl Pts',(0.577812434683422,6.74454407388979,-48.8298219817556));
#35936=CARTESIAN_POINT('Ctrl Pts',(0.403517102976043,6.75721721925584,-48.8216190973677));
#35937=CARTESIAN_POINT('Ctrl Pts',(0.228912767094718,6.76312708331442,-48.8134162129798));
#35938=CARTESIAN_POINT('Ctrl Pts',(0.0543877917091412,6.76903426124417,
-48.8052170569356));
#35939=CARTESIAN_POINT('Ctrl Pts',(-0.120445550391488,6.76818427001214,
-48.7970179008914));
#35940=CARTESIAN_POINT('Ctrl Pts',(-0.295026193065019,6.7605656971444,-48.7888187448472));
#35941=CARTESIAN_POINT('Ctrl Pts',(-0.469591651468012,6.75294778690724,
-48.7806203019302));
#35942=CARTESIAN_POINT('Ctrl Pts',(-0.643904095868667,6.73856247474029,
-48.7724218590132));
#35943=CARTESIAN_POINT('Ctrl Pts',(-0.817403357264144,6.71745046513432,
-48.7642234160962));
#35944=CARTESIAN_POINT('Ctrl Pts',(-0.990900890812345,6.69633866577898,
-48.7560250548259));
#35945=CARTESIAN_POINT('Ctrl Pts',(-1.16358490128616,6.66850034469401,-48.7478266935557));
#35946=CARTESIAN_POINT('Ctrl Pts',(-1.33490135257533,6.63402799051169,-48.7396283322855));
#35947=CARTESIAN_POINT('Ctrl Pts',(-1.50624721861559,6.59954971748322,-48.7314285633702));
#35948=CARTESIAN_POINT('Ctrl Pts',(-1.67622470600697,6.55843521279149,-48.7232287944549));
#35949=CARTESIAN_POINT('Ctrl Pts',(-1.84429091263455,6.5108279066163,-48.7150290255396));
#35950=CARTESIAN_POINT('Ctrl Pts',(-2.01241650669963,6.46320377804728,-48.7068263591753));
#35951=CARTESIAN_POINT('Ctrl Pts',(-2.1786291297559,6.40908237545152,-48.698623692811));
#35952=CARTESIAN_POINT('Ctrl Pts',(-2.34240190550047,6.34865673297177,-48.6904210264467));
#35953=CARTESIAN_POINT('Ctrl Pts',(-2.50636068618298,6.28816246206567,-48.6822090439037));
#35954=CARTESIAN_POINT('Ctrl Pts',(-2.66787374666015,6.22134977120187,-48.6739970613607));
#35955=CARTESIAN_POINT('Ctrl Pts',(-2.82643406458156,6.14845992737799,-48.6657850788177));
#35956=CARTESIAN_POINT('Ctrl Pts',(-2.98508790352148,6.07552709213909,-48.6575682527364));
#35957=CARTESIAN_POINT('Ctrl Pts',(-3.1407852090137,5.99651012103758,-48.6493514266551));
#35958=CARTESIAN_POINT('Ctrl Pts',(-3.29304448913009,5.91169577977504,-48.6411346005738));
#35959=CARTESIAN_POINT('Ctrl Pts',(-3.44553857504676,5.82675064254879,-48.6329051029599));
#35960=CARTESIAN_POINT('Ctrl Pts',(-3.59458373427576,5.73599045547337,-48.6246756053461));
#35961=CARTESIAN_POINT('Ctrl Pts',(-3.73972723282283,5.63974549284658,-48.6164461077323));
#35962=CARTESIAN_POINT('Ctrl Pts',(-3.86910196305317,5.55395683403295,-48.6091106842074));
#35963=CARTESIAN_POINT('Ctrl Pts',(-3.99537705743535,5.46381111992917,-48.6017752606825));
#35964=CARTESIAN_POINT('Ctrl Pts',(-4.11825527025049,5.36956818832335,-48.5944398371577));
#35965=CARTESIAN_POINT('Ctrl Pts',(-4.25206793835219,5.26693894397657,-48.586451662761));
#35966=CARTESIAN_POINT('Ctrl Pts',(-4.38230611285813,5.15910143668588,-48.5784634883643));
#35967=CARTESIAN_POINT('Ctrl Pts',(-4.50852037101767,5.04633858001212,-48.5704753139677));
#35968=CARTESIAN_POINT('Ctrl Pts',(-4.63457795032364,4.93371570399797,-48.5624970558675));
#35969=CARTESIAN_POINT('Ctrl Pts',(-4.7566212692965,4.81617988999997,-48.5545187977673));
#35970=CARTESIAN_POINT('Ctrl Pts',(-4.87422961755164,4.69405737453031,-48.5465405396672));
#35971=CARTESIAN_POINT('Ctrl Pts',(-4.99171865488284,4.57205874950186,-48.5385703753236));
#35972=CARTESIAN_POINT('Ctrl Pts',(-5.10478141064177,4.44548295121236,-48.53060021098));
#35973=CARTESIAN_POINT('Ctrl Pts',(-5.21303020169676,4.31469641066408,-48.5226300466365));
#35974=CARTESIAN_POINT('Ctrl Pts',(-5.32119366389288,4.18401296471992,-48.5146661649038));
#35975=CARTESIAN_POINT('Ctrl Pts',(-5.42455047063288,4.0491256722081,-48.5067022831711));
#35976=CARTESIAN_POINT('Ctrl Pts',(-5.52274993362333,3.91043759324497,-48.4987384014383));
#35977=CARTESIAN_POINT('Ctrl Pts',(-5.62340782270726,3.76827745464124,-48.4905751437207));
#35978=CARTESIAN_POINT('Ctrl Pts',(-5.71864645666591,3.6221240072378,-48.482411886003));
#35979=CARTESIAN_POINT('Ctrl Pts',(-5.80813185606154,3.47244774512204,-48.4742486282853));
#35980=CARTESIAN_POINT('Ctrl Pts',(-5.89536366442474,3.32654091449287,-48.4662909532047));
#35981=CARTESIAN_POINT('Ctrl Pts',(-5.97712833485484,3.17728692360154,-48.4583332781241));
#35982=CARTESIAN_POINT('Ctrl Pts',(-6.05316052074016,3.02515069213961,-48.4503756030435));
#35983=CARTESIAN_POINT('Ctrl Pts',(-6.12918825432945,2.87302336947769,-48.4424183939488));
#35984=CARTESIAN_POINT('Ctrl Pts',(-6.19948400072992,2.71801448226019,-48.434461184854));
#35985=CARTESIAN_POINT('Ctrl Pts',(-6.26382885480873,2.56061263717603,-48.4265039757593));
#35986=CARTESIAN_POINT('Ctrl Pts',(-6.3281830729576,2.40318788549077,-48.4185456086565));
#35987=CARTESIAN_POINT('Ctrl Pts',(-6.38658453224515,2.24336983552793,-48.4105872415536));
#35988=CARTESIAN_POINT('Ctrl Pts',(-6.43886295915178,2.08166586974548,-48.4026288744508));
#35989=CARTESIAN_POINT('Ctrl Pts',(-6.49349979164998,1.91266704909369,-48.3943114862644));
#35990=CARTESIAN_POINT('Ctrl Pts',(-6.5414481535414,1.74160864021316,-48.385994098078));
#35991=CARTESIAN_POINT('Ctrl Pts',(-6.58257252794975,1.56908505642021,-48.3776767098916));
#35992=CARTESIAN_POINT('Ctrl Pts',(-6.62197743791774,1.40377491165765,-48.3697070826968));
#35993=CARTESIAN_POINT('Ctrl Pts',(-6.65511740779374,1.23712001178683,-48.3617374555019));
#35994=CARTESIAN_POINT('Ctrl Pts',(-6.68192607887337,1.06965081988094,-48.3537678283071));
#35995=CARTESIAN_POINT('Ctrl Pts',(-6.70875183033336,0.902074929754604,
-48.3457931234916));
#35996=CARTESIAN_POINT('Ctrl Pts',(-6.72923820885137,0.733684090666321,
-48.3378184186761));
#35997=CARTESIAN_POINT('Ctrl Pts',(-6.74337090337002,0.565011380047041,
-48.3298437138605));
#35998=CARTESIAN_POINT('Ctrl Pts',(-6.7575215467703,0.396124450793563,-48.321858880967));
#35999=CARTESIAN_POINT('Ctrl Pts',(-6.76530239298436,0.226955312878489,
-48.3138740480734));
#36000=CARTESIAN_POINT('Ctrl Pts',(-6.76675113645843,0.0580349656550752,
-48.3058892151799));
#36001=CARTESIAN_POINT('Ctrl Pts',(-6.76693674636341,0.0363932532619834,
-48.3048662155245));
#36002=CARTESIAN_POINT('Ctrl Pts',(-6.76701848937722,0.0147556145212476,
-48.3038432158692));
#36003=CARTESIAN_POINT('Ctrl Pts',(-6.76699650576387,-0.00687684372454104,
-48.3028202162139));
#36004=CARTESIAN_POINT('',(-6.76728246533827,-0.0010053267103838,-48.6966910258876));
#36005=CARTESIAN_POINT('Ctrl Pts',(3.0990855038472,6.01564277861013,-49.3486032095739));
#36006=CARTESIAN_POINT('Ctrl Pts',(2.93373232018331,6.10082796552479,-49.3398537616746));
#36007=CARTESIAN_POINT('Ctrl Pts',(2.7648650214443,6.17919158180189,-49.3311043137754));
#36008=CARTESIAN_POINT('Ctrl Pts',(2.59305716434358,6.25046746591377,-49.3223548658761));
#36009=CARTESIAN_POINT('Ctrl Pts',(2.42125069459287,6.32174277447223,-49.3136054886286));
#36010=CARTESIAN_POINT('Ctrl Pts',(2.24650397871061,6.38593035557825,-49.3048561113812));
#36011=CARTESIAN_POINT('Ctrl Pts',(2.06941053323773,6.44281220003538,-49.2961067341338));
#36012=CARTESIAN_POINT('Ctrl Pts',(1.89231845896684,6.49969360406685,-49.2873574246312));
#36013=CARTESIAN_POINT('Ctrl Pts',(1.71287996431505,6.54926929700881,-49.2786081151286));
#36014=CARTESIAN_POINT('Ctrl Pts',(1.53170449173504,6.59137090065479,-49.269858805626));
#36015=CARTESIAN_POINT('Ctrl Pts',(1.35053036178169,6.63347219230084,-49.2611095609614));
#36016=CARTESIAN_POINT('Ctrl Pts',(1.16761955878841,6.66809944062455,-49.2523603162968));
#36017=CARTESIAN_POINT('Ctrl Pts',(0.983593309310438,6.69513503985392,-49.2436110716323));
#36018=CARTESIAN_POINT('Ctrl Pts',(0.799568362459991,6.72217044771214,-49.2348618888991));
#36019=CARTESIAN_POINT('Ctrl Pts',(0.614428268438663,6.74161427235976,-49.2261127061659));
#36020=CARTESIAN_POINT('Ctrl Pts',(0.428801816330396,6.75340047696801,-49.2173635234327));
#36021=CARTESIAN_POINT('Ctrl Pts',(0.243176616522864,6.76518660206242,-49.2086143997246));
#36022=CARTESIAN_POINT('Ctrl Pts',(0.0570653511654939,6.76931519233997,
-49.1998652760165));
#36023=CARTESIAN_POINT('Ctrl Pts',(-0.128899900800044,6.76577222610795,
-49.1911161523083));
#36024=CARTESIAN_POINT('Ctrl Pts',(-0.314863959941968,6.76222928260133,
-49.1823670847191));
#36025=CARTESIAN_POINT('Ctrl Pts',(-0.500681721080561,6.75101488651277,
-49.1736180171298));
#36026=CARTESIAN_POINT('Ctrl Pts',(-0.685722110173113,6.73216712415993,
-49.1648689495406));
#36027=CARTESIAN_POINT('Ctrl Pts',(-0.870761373827375,6.71331947644148,
-49.1561199351642));
#36028=CARTESIAN_POINT('Ctrl Pts',(-1.05502298984314,6.68683858440001,-49.1473709207878));
#36029=CARTESIAN_POINT('Ctrl Pts',(-1.23788117676026,6.65281438131432,-49.1386219064115));
#36030=CARTESIAN_POINT('Ctrl Pts',(-1.43009641451763,6.61704912302384,-49.1294251955239));
#36031=CARTESIAN_POINT('Ctrl Pts',(-1.62076048992669,6.57294837083172,-49.1202284846364));
#36032=CARTESIAN_POINT('Ctrl Pts',(-1.80915798961109,6.52067760042056,-49.1110317737489));
#36033=CARTESIAN_POINT('Ctrl Pts',(-1.98840443002984,6.47094578577417,-49.1022817760424));
#36034=CARTESIAN_POINT('Ctrl Pts',(-2.16559895952159,6.41381888474486,-49.0935317783359));
#36035=CARTESIAN_POINT('Ctrl Pts',(-2.34013966242285,6.34949095285248,-49.0847817806294));
#36036=CARTESIAN_POINT('Ctrl Pts',(-2.51467682553977,6.285164325567,-49.0760319603778));
#36037=CARTESIAN_POINT('Ctrl Pts',(-2.68656000078803,6.21363705879677,-49.0672821401262));
#36038=CARTESIAN_POINT('Ctrl Pts',(-2.85520533840849,6.13515211510877,-49.0585323198746));
#36039=CARTESIAN_POINT('Ctrl Pts',(-3.02384747998281,6.05666865881144,-49.0497826654434));
#36040=CARTESIAN_POINT('Ctrl Pts',(-3.18925164684485,5.97122791039871,-49.0410330110121));
#36041=CARTESIAN_POINT('Ctrl Pts',(-3.350856018291,5.87912008251941,-49.0322833565809));
#36042=CARTESIAN_POINT('Ctrl Pts',(-3.5124575419136,5.78701387778209,-49.0235338563377));
#36043=CARTESIAN_POINT('Ctrl Pts',(-3.67025915510879,5.68824097061019,-49.0147843560946));
#36044=CARTESIAN_POINT('Ctrl Pts',(-3.82372487928777,5.58313684656894,-49.0060348558514));
#36045=CARTESIAN_POINT('Ctrl Pts',(-3.97718810300748,5.4780344350181,-48.9972854981663));
#36046=CARTESIAN_POINT('Ctrl Pts',(-4.12631534262981,5.3666011749641,-48.9885361404812));
#36047=CARTESIAN_POINT('Ctrl Pts',(-4.27060009886187,5.24921554097382,-48.9797867827961));
#36048=CARTESIAN_POINT('Ctrl Pts',(-4.41488269594177,5.13183166360322,-48.9710375560409));
#36049=CARTESIAN_POINT('Ctrl Pts',(-4.55432273235054,5.00849577139502,-48.9622883292857));
#36050=CARTESIAN_POINT('Ctrl Pts',(-4.68844662480174,4.87962675277374,-48.9535391025305));
#36051=CARTESIAN_POINT('Ctrl Pts',(-4.8225686883511,4.75075949139929,-48.9447899950791));
#36052=CARTESIAN_POINT('Ctrl Pts',(-4.951374546378,4.61635945312591,-48.9360408876276));
#36053=CARTESIAN_POINT('Ctrl Pts',(-5.07442674461004,4.47688309134675,-48.9272917801761));
#36054=CARTESIAN_POINT('Ctrl Pts',(-5.19747742838482,4.3374084461642,-48.9185427804037));
#36055=CARTESIAN_POINT('Ctrl Pts',(-5.31477440450887,4.19285781736081,-48.9097937806313));
#36056=CARTESIAN_POINT('Ctrl Pts',(-5.42591931531128,4.0437221199944,-48.9010447808589));
#36057=CARTESIAN_POINT('Ctrl Pts',(-5.53707636462958,3.89457013500834,-48.8922948255784));
#36058=CARTESIAN_POINT('Ctrl Pts',(-5.64207983273449,3.74083230916453,-48.8835448702978));
#36059=CARTESIAN_POINT('Ctrl Pts',(-5.74057303468728,3.58303087251859,-48.8747949150172));
#36060=CARTESIAN_POINT('Ctrl Pts',(-5.83906243363747,3.42523552887462,-48.8660452975884));
#36061=CARTESIAN_POINT('Ctrl Pts',(-5.93104191768408,3.26337713157024,-48.8572956801596));
#36062=CARTESIAN_POINT('Ctrl Pts',(-6.0161990669964,3.09800545291187,-48.8485460627308));
#36063=CARTESIAN_POINT('Ctrl Pts',(-6.10135338095371,2.9326392803962,-48.8397967366254));
#36064=CARTESIAN_POINT('Ctrl Pts',(-6.17968568352831,2.76376031540242,-48.83104741052));
#36065=CARTESIAN_POINT('Ctrl Pts',(-6.25092992694882,2.59194213831553,-48.8222980844146));
#36066=CARTESIAN_POINT('Ctrl Pts',(-6.32217217691094,2.42012876880843,-48.8135490031208));
#36067=CARTESIAN_POINT('Ctrl Pts',(-6.38632665483837,2.24537661647707,-48.804799921827));
#36068=CARTESIAN_POINT('Ctrl Pts',(-6.44317547869334,2.06827917621507,-48.7960508405332));
#36069=CARTESIAN_POINT('Ctrl Pts',(-6.50002944235921,1.89116572423475,-48.7873009682183));
#36070=CARTESIAN_POINT('Ctrl Pts',(-6.54957634250384,1.71170683289251,-48.7785510959033));
#36071=CARTESIAN_POINT('Ctrl Pts',(-6.59164787708383,1.53051209225419,-48.7698012235883));
#36072=CARTESIAN_POINT('Ctrl Pts',(-6.63371649074997,1.3493299314809,-48.7610519587536));
#36073=CARTESIAN_POINT('Ctrl Pts',(-6.66831071257112,1.16641244174069,-48.7523026939188));
#36074=CARTESIAN_POINT('Ctrl Pts',(-6.69531304840323,0.982380875160711,
-48.743553429084));
#36075=CARTESIAN_POINT('Ctrl Pts',(-6.72231677033035,0.798339861796561,
-48.7348037151283));
#36076=CARTESIAN_POINT('Ctrl Pts',(-6.74172778477883,0.613184940730893,
-48.7260540011727));
#36077=CARTESIAN_POINT('Ctrl Pts',(-6.75348015835513,0.42754502769131,-48.717304287217));
#36078=CARTESIAN_POINT('Ctrl Pts',(-6.76249038365218,0.285219953547609,
-48.7105961194147));
#36079=CARTESIAN_POINT('Ctrl Pts',(-6.76699999999999,0.142609995758117,
-48.7038879516124));
#36080=CARTESIAN_POINT('Ctrl Pts',(-6.767,7.58693081418461E-13,-48.6971797838101));
#36081=CARTESIAN_POINT('Ctrl Pts',(-6.76699917014542,-0.0033513059037753,
-48.6971797838101));
#36082=CARTESIAN_POINT('Ctrl Pts',(-6.76690054123612,-0.202504044116444,
-48.6878331625662));
#36083=CARTESIAN_POINT('Ctrl Pts',(-6.7580062315747,-0.401386650076133,
-48.6784865413224));
#36084=CARTESIAN_POINT('Ctrl Pts',(-6.74041208644594,-0.599277819457265,
-48.6691399200785));
#36085=CARTESIAN_POINT('Ctrl Pts',(-6.72271805758446,-0.798292436924462,
-48.6597402371252));
#36086=CARTESIAN_POINT('Ctrl Pts',(-6.69622519243849,-0.996304175997024,
-48.6503405541718));
#36087=CARTESIAN_POINT('Ctrl Pts',(-6.66108160237869,-1.19259418347239,
-48.6409408712184));
#36088=CARTESIAN_POINT('Ctrl Pts',(-6.6258495783146,-1.38937812771784,-48.6315175352574));
#36089=CARTESIAN_POINT('Ctrl Pts',(-6.58192331598605,-1.58443152368695,
-48.6220941992965));
#36090=CARTESIAN_POINT('Ctrl Pts',(-6.52950170788515,-1.77704711437963,
-48.6126708633355));
#36091=CARTESIAN_POINT('Ctrl Pts',(-6.47693929460969,-1.97018007325028,
-48.603222216162));
#36092=CARTESIAN_POINT('Ctrl Pts',(-6.41583590556948,-2.16086197399059,
-48.5937735689885));
#36093=CARTESIAN_POINT('Ctrl Pts',(-6.34644080315507,-2.34839905724058,
-48.584324921815));
#36094=CARTESIAN_POINT('Ctrl Pts',(-6.30893860751651,-2.44974702187829,
-48.5792187255202));
#36095=CARTESIAN_POINT('Ctrl Pts',(-6.26901565813335,-2.55017688884191,
-48.5741125292255));
#36096=CARTESIAN_POINT('Ctrl Pts',(-6.22671709480138,-2.64958170685644,
-48.5690063329308));
#36097=CARTESIAN_POINT('Ctrl Pts',(-6.15845239278756,-2.81000891161144,
-48.560765557334));
#36098=CARTESIAN_POINT('Ctrl Pts',(-6.0838895322984,-2.96801773399273,-48.5525247817373));
#36099=CARTESIAN_POINT('Ctrl Pts',(-6.00322034728997,-3.12308092464537,
-48.5442840061405));
#36100=CARTESIAN_POINT('Ctrl Pts',(-5.92264051214965,-3.27797236600324,
-48.5360523580961));
#36101=CARTESIAN_POINT('Ctrl Pts',(-5.83596798244575,-3.42992435922279,
-48.5278207100518));
#36102=CARTESIAN_POINT('Ctrl Pts',(-5.7434429857839,-3.57842865920919,-48.5195890620074));
#36103=CARTESIAN_POINT('Ctrl Pts',(-5.65100398176838,-3.72679493943654,
-48.5113650644491));
#36104=CARTESIAN_POINT('Ctrl Pts',(-5.55272353032596,-3.87171960766436,
-48.5031410668909));
#36105=CARTESIAN_POINT('Ctrl Pts',(-5.44888823423283,-4.01271803281006,
-48.4949170693326));
#36106=CARTESIAN_POINT('Ctrl Pts',(-5.34514467702711,-4.15359188529947,
-48.4867003377081));
#36107=CARTESIAN_POINT('Ctrl Pts',(-5.23585626695808,-4.29054612310275,
-48.4784836060836));
#36108=CARTESIAN_POINT('Ctrl Pts',(-5.12135338170287,-4.4231242962097,-48.4702668744591));
#36109=CARTESIAN_POINT('Ctrl Pts',(-5.00690916051487,-4.55563454461031,
-48.4620543525704));
#36110=CARTESIAN_POINT('Ctrl Pts',(-4.88725601683277,-4.68377292493266,
-48.4538418306817));
#36111=CARTESIAN_POINT('Ctrl Pts',(-4.76276539569147,-4.80711501688943,
-48.445629308793));
#36112=CARTESIAN_POINT('Ctrl Pts',(-4.63831640481326,-4.9304158626568,-48.4374195332112));
#36113=CARTESIAN_POINT('Ctrl Pts',(-4.50903341154218,-5.04892336508585,
-48.4292097576294));
#36114=CARTESIAN_POINT('Ctrl Pts',(-4.37532566290722,-5.16224896179035,
-48.4209999820476));
#36115=CARTESIAN_POINT('Ctrl Pts',(-4.31692559205371,-5.21174663821244,
-48.4174141653648));
#36116=CARTESIAN_POINT('Ctrl Pts',(-4.25768187335778,-5.26025623384032,
-48.413828348682));
#36117=CARTESIAN_POINT('Ctrl Pts',(-4.19763070587936,-5.3077476821208,-48.4102425319993));
#36118=CARTESIAN_POINT('Ctrl Pts',(-4.04927500992292,-5.42507474098545,
-48.4013838144775));
#36119=CARTESIAN_POINT('Ctrl Pts',(-3.89614287579507,-5.53606354164227,
-48.3925250969557));
#36120=CARTESIAN_POINT('Ctrl Pts',(-3.73878837613257,-5.64036793821963,
-48.3836663794339));
#36121=CARTESIAN_POINT('Ctrl Pts',(-3.58113949147413,-5.74486747157052,
-48.3747910886745));
#36122=CARTESIAN_POINT('Ctrl Pts',(-3.41925267110229,-5.84265746627009,
-48.3659157979151));
#36123=CARTESIAN_POINT('Ctrl Pts',(-3.25370763711922,-5.93343708251398,
-48.3570405071556));
#36124=CARTESIAN_POINT('Ctrl Pts',(-3.08769241801749,-6.02447453327945,
-48.3481400085748));
#36125=CARTESIAN_POINT('Ctrl Pts',(-2.91799842216406,-6.10846163565813,
-48.3392395099941));
#36126=CARTESIAN_POINT('Ctrl Pts',(-2.74522928430887,-6.18514390912394,
-48.3303390114133));
#36127=CARTESIAN_POINT('Ctrl Pts',(-2.57222626864046,-6.26192998748601,
-48.3214264642156));
#36128=CARTESIAN_POINT('Ctrl Pts',(-2.39614003515011,-6.33139138475548,
-48.312513917018));
#36129=CARTESIAN_POINT('Ctrl Pts',(-2.21759187387818,-6.39332271052459,
-48.3036013698204));
#36130=CARTESIAN_POINT('Ctrl Pts',(-2.03864946082848,-6.45539078670944,
-48.2946691428481));
#36131=CARTESIAN_POINT('Ctrl Pts',(-1.85723449276926,-6.50989544904072,
-48.2857369158759));
#36132=CARTESIAN_POINT('Ctrl Pts',(-1.67398379057515,-6.55668111691362,
-48.2768046889036));
#36133=CARTESIAN_POINT('Ctrl Pts',(-1.50079071597112,-6.60089897566828,
-48.2683627029583));
#36134=CARTESIAN_POINT('Ctrl Pts',(-1.32595815882831,-6.63822229220504,
-48.259920717013));
#36135=CARTESIAN_POINT('Ctrl Pts',(-1.15002994236985,-6.66856207376469,
-48.2514787310677));
#36136=CARTESIAN_POINT('Ctrl Pts',(-0.978645014598349,-6.69811834038228,
-48.2432547566502));
#36137=CARTESIAN_POINT('Ctrl Pts',(-0.805892724177182,-6.72110254673465,
-48.2350307822326));
#36138=CARTESIAN_POINT('Ctrl Pts',(-0.632318095756071,-6.73739288046789,
-48.226806807815));
#36139=CARTESIAN_POINT('Ctrl Pts',(-0.45892677898349,-6.75366601002816,
-48.2185915187124));
#36140=CARTESIAN_POINT('Ctrl Pts',(-0.284715207696388,-6.76325931124833,
-48.2103762296097));
#36141=CARTESIAN_POINT('Ctrl Pts',(-0.110238333290158,-6.76610201740067,
-48.2021609405071));
#36142=CARTESIAN_POINT('Ctrl Pts',(0.0640892729504751,-6.76894229156577,
-48.1939526797349));
#36143=CARTESIAN_POINT('Ctrl Pts',(0.238681373748767,-6.76504346686485,
-48.1857444189627));
#36144=CARTESIAN_POINT('Ctrl Pts',(0.412978067854543,-6.75438658321177,
-48.1775361581905));
#36145=CARTESIAN_POINT('Ctrl Pts',(0.587160598188498,-6.74373667978307,
-48.1693332738027));
#36146=CARTESIAN_POINT('Ctrl Pts',(0.761047750594994,-6.7263375563464,-48.1611303894148));
#36147=CARTESIAN_POINT('Ctrl Pts',(0.934079702202542,-6.70222232620891,
-48.1529275050269));
#36148=CARTESIAN_POINT('Ctrl Pts',(1.10703300798866,-6.67811805683368,-48.1447283489827));
#36149=CARTESIAN_POINT('Ctrl Pts',(1.27913153294253,-6.64730381168794,-48.1365291929385));
#36150=CARTESIAN_POINT('Ctrl Pts',(1.44982056288041,-6.60986454743584,-48.1283300368943));
#36151=CARTESIAN_POINT('Ctrl Pts',(1.62049474702332,-6.57242853948932,-48.1201315939773));
#36152=CARTESIAN_POINT('Ctrl Pts',(1.78975932850531,-6.52836872860921,-48.1119331510603));
#36153=CARTESIAN_POINT('Ctrl Pts',(1.95706941294622,-6.47782126280977,-48.1037347081433));
#36154=CARTESIAN_POINT('Ctrl Pts',(2.12437783117674,-6.42727430040325,-48.095536346873));
#36155=CARTESIAN_POINT('Ctrl Pts',(2.28973144746005,-6.37023991449283,-48.0873379856028));
#36156=CARTESIAN_POINT('Ctrl Pts',(2.45260028837174,-6.30690421882867,-48.0791396243326));
#36157=CARTESIAN_POINT('Ctrl Pts',(2.61549709359384,-6.24355764853039,-48.0709398554173));
#36158=CARTESIAN_POINT('Ctrl Pts',(2.77590793915033,-6.17390774297557,-48.062740086502));
#36159=CARTESIAN_POINT('Ctrl Pts',(2.93332255514403,-6.09818889404742,-48.0545403175867));
#36160=CARTESIAN_POINT('Ctrl Pts',(3.09079279475686,-6.02244328930384,-48.0463376512225));
#36161=CARTESIAN_POINT('Ctrl Pts',(3.24526437273231,-5.9406246246854,-48.0381349848582));
#36162=CARTESIAN_POINT('Ctrl Pts',(3.39625131273346,-5.85301341368327,-48.0299323184939));
#36163=CARTESIAN_POINT('Ctrl Pts',(3.54740973615904,-5.76530269824399,-48.0217203359508));
#36164=CARTESIAN_POINT('Ctrl Pts',(3.6950753043787,-5.67178647330122,-48.0135083534078));
#36165=CARTESIAN_POINT('Ctrl Pts',(3.83878987097631,-5.57278936677942,-48.0052963708648));
#36166=CARTESIAN_POINT('Ctrl Pts',(3.98258920236766,-5.4737338704262,-47.9970795447835));
#36167=CARTESIAN_POINT('Ctrl Pts',(4.12243260009857,-5.36919126298458,-47.9888627187022));
#36168=CARTESIAN_POINT('Ctrl Pts',(4.25789487128543,-5.2595266198662,-47.9806458926209));
#36169=CARTESIAN_POINT('Ctrl Pts',(4.39356604485876,-5.1496928580297,-47.9724163950071));
#36170=CARTESIAN_POINT('Ctrl Pts',(4.52484232066105,-5.03472151177761,-47.9641868973932));
#36171=CARTESIAN_POINT('Ctrl Pts',(4.65133429783418,-4.91501558998457,-47.9559573997794));
#36172=CARTESIAN_POINT('Ctrl Pts',(4.76408385662894,-4.80831483181071,-47.9486219762545));
#36173=CARTESIAN_POINT('Ctrl Pts',(4.87303262295225,-4.69785300333945,-47.9412865527296));
#36174=CARTESIAN_POINT('Ctrl Pts',(4.97793230461094,-4.58393706007301,-47.9339511292047));
#36175=CARTESIAN_POINT('Ctrl Pts',(5.09334918686618,-4.45859994938706,-47.9258802590183));
#36176=CARTESIAN_POINT('Ctrl Pts',(5.20423996285354,-4.32867203111494,-47.9178093888319));
#36177=CARTESIAN_POINT('Ctrl Pts',(5.31020722916382,-4.19451882619881,-47.9097385186455));
#36178=CARTESIAN_POINT('Ctrl Pts',(5.41604262744776,-4.06053256451881,-47.9016776920297));
#36179=CARTESIAN_POINT('Ctrl Pts',(5.51696647882461,-3.92233176741359,-47.8936168654139));
#36180=CARTESIAN_POINT('Ctrl Pts',(5.61261742731917,-3.78031937996687,-47.8855560387981));
#36181=CARTESIAN_POINT('Ctrl Pts',(5.70817032043641,-3.63845257474862,-47.8775034756382));
#36182=CARTESIAN_POINT('Ctrl Pts',(5.79846086110304,-3.49278226184258,-47.8694509124784));
#36183=CARTESIAN_POINT('Ctrl Pts',(5.88316735776083,-3.34374503223219,-47.8613983493185));
#36184=CARTESIAN_POINT('Ctrl Pts',(5.96780556619126,-3.19482795265305,-47.8533522779306));
#36185=CARTESIAN_POINT('Ctrl Pts',(6.04686850722501,-3.04254968146831,-47.8453062065427));
#36186=CARTESIAN_POINT('Ctrl Pts',(6.12007736585327,-2.88737632392635,-47.8372601351548));
#36187=CARTESIAN_POINT('Ctrl Pts',(6.19324321896246,-2.73229412080086,-47.829218790319));
#36188=CARTESIAN_POINT('Ctrl Pts',(6.26056167680664,-2.57432055338884,-47.8211774454831));
#36189=CARTESIAN_POINT('Ctrl Pts',(6.32179957337942,-2.41394680016355,-47.8131361006472));
#36190=CARTESIAN_POINT('Ctrl Pts',(6.3842179481688,-2.25048153444691,-47.8049397434261));
#36191=CARTESIAN_POINT('Ctrl Pts',(6.44031874685477,-2.08452294774335,-47.7967433862051));
#36192=CARTESIAN_POINT('Ctrl Pts',(6.48990612972447,-1.91661353103979,-47.788547028984));
#36193=CARTESIAN_POINT('Ctrl Pts',(6.53854023421086,-1.7519320406359,-47.7805082402755));
#36194=CARTESIAN_POINT('Ctrl Pts',(6.5809089933205,-1.58537442334995,-47.772469451567));
#36195=CARTESIAN_POINT('Ctrl Pts',(6.61687786943182,-1.41746825750119,-47.7644306628585));
#36196=CARTESIAN_POINT('Ctrl Pts',(6.65285059453878,-1.24954412417139,-47.7563910139268));
#36197=CARTESIAN_POINT('Ctrl Pts',(6.68242199468255,-1.08027152013186,-47.748351364995));
#36198=CARTESIAN_POINT('Ctrl Pts',(6.70550864115327,-0.910188366998158,
-47.7403117160633));
#36199=CARTESIAN_POINT('Ctrl Pts',(6.72860232934845,-0.740053336312645,
-47.7322696149351));
#36200=CARTESIAN_POINT('Ctrl Pts',(6.74520727659557,-0.56910763429333,-47.724227513807));
#36201=CARTESIAN_POINT('Ctrl Pts',(6.75529193448963,-0.397894307347293,
-47.7161854126788));
#36202=CARTESIAN_POINT('Ctrl Pts',(6.76571690996615,-0.2209032032943,-47.707871922234));
#36203=CARTESIAN_POINT('Ctrl Pts',(6.76917380210623,-0.0436265318524084,
-47.6995584317893));
#36204=CARTESIAN_POINT('Ctrl Pts',(6.76568623699593,0.133336951082305,-47.6912449413445));
#36205=CARTESIAN_POINT('Ctrl Pts',(6.76230657835816,0.304825122558117,-47.6831886731737));
#36206=CARTESIAN_POINT('Ctrl Pts',(6.75240588539718,0.476018834040483,-47.675132405003));
#36207=CARTESIAN_POINT('Ctrl Pts',(6.73605833460217,0.646380006526059,-47.6670761368322));
#36208=CARTESIAN_POINT('Ctrl Pts',(6.71892786159665,0.824900171598416,-47.6586340352505));
#36209=CARTESIAN_POINT('Ctrl Pts',(6.69471790127608,1.00250561037161,-47.6501919336687));
#36210=CARTESIAN_POINT('Ctrl Pts',(6.66357341775822,1.17859166217401,-47.6417498320869));
#36211=CARTESIAN_POINT('Ctrl Pts',(6.63242893424036,1.35467771397639,-47.6333077305052));
#36212=CARTESIAN_POINT('Ctrl Pts',(6.5943501102287,1.52924394694912,-47.6248656289234));
#36213=CARTESIAN_POINT('Ctrl Pts',(6.54954059514586,1.70170708188466,-47.6164235273417));
#36214=CARTESIAN_POINT('Ctrl Pts',(6.50530051555239,1.87197857003586,-47.6080887072656));
#36215=CARTESIAN_POINT('Ctrl Pts',(6.45435972196866,2.0407416297399,-47.5997538871894));
#36216=CARTESIAN_POINT('Ctrl Pts',(6.39683554788043,2.2074383283284,-47.5914190671133));
#36217=CARTESIAN_POINT('Ctrl Pts',(6.33938031656763,2.37393524077068,-47.5830942363267));
#36218=CARTESIAN_POINT('Ctrl Pts',(6.27535753615828,2.53837039965132,-47.5747694055401));
#36219=CARTESIAN_POINT('Ctrl Pts',(6.20493511043231,2.70019800668846,-47.5664445747535));
#36220=CARTESIAN_POINT('Ctrl Pts',(6.13458417270687,2.861861337475,-47.5581281947623));
#36221=CARTESIAN_POINT('Ctrl Pts',(6.05784667168943,3.02092207337447,-47.549811814771));
#36222=CARTESIAN_POINT('Ctrl Pts',(5.97493975071795,3.17685126741723,-47.5414954347798));
#36223=CARTESIAN_POINT('Ctrl Pts',(5.89211498600623,3.33262594409017,-47.5331872958698));
#36224=CARTESIAN_POINT('Ctrl Pts',(5.80313315337678,3.485274960318,-47.5248791569598));
#36225=CARTESIAN_POINT('Ctrl Pts',(5.70825872939257,3.6342910282906,-47.5165710180499));
#36226=CARTESIAN_POINT('Ctrl Pts',(5.61343847697899,3.78322201079851,-47.5082676229361));
#36227=CARTESIAN_POINT('Ctrl Pts',(5.5127325222,3.92852388502452,-47.4999642278224));
#36228=CARTESIAN_POINT('Ctrl Pts',(5.40645064539748,4.06971502919813,-47.4916608327086));
#36229=CARTESIAN_POINT('Ctrl Pts',(5.30021180577,4.21084900023774,-47.4833607999242));
#36230=CARTESIAN_POINT('Ctrl Pts',(5.18840175188563,4.34787528060164,-47.4750607671397));
#36231=CARTESIAN_POINT('Ctrl Pts',(5.0713729614526,4.48034209473423,-47.4667607343553));
#36232=CARTESIAN_POINT('Ctrl Pts',(4.95437213213938,4.61277725921508,-47.4584626846573));
#36233=CARTESIAN_POINT('Ctrl Pts',(4.83215528170351,4.74065486843714,-47.4501646349593));
#36234=CARTESIAN_POINT('Ctrl Pts',(4.70511458584861,4.86355690149038,-47.4418665852614));
#36235=CARTESIAN_POINT('Ctrl Pts',(4.57805486031474,4.98647734428403,-47.433567292582));
#36236=CARTESIAN_POINT('Ctrl Pts',(4.44617009151387,5.10442047562056,-47.4252679999026));
#36237=CARTESIAN_POINT('Ctrl Pts',(4.3098890796138,5.21700537870393,-47.4169687072233));
#36238=CARTESIAN_POINT('Ctrl Pts',(4.17360043473173,5.32959658757068,-47.4086689497077));
#36239=CARTESIAN_POINT('Ctrl Pts',(4.03291532722172,5.43682875214606,-47.4003691921921));
#36240=CARTESIAN_POINT('Ctrl Pts',(3.88829517179141,5.53836164014446,-47.3920694346765));
#36241=CARTESIAN_POINT('Ctrl Pts',(3.74359164961655,5.63995305709625,-47.3837648927395));
#36242=CARTESIAN_POINT('Ctrl Pts',(3.59494883398991,5.73583843582138,-47.3754603508025));
#36243=CARTESIAN_POINT('Ctrl Pts',(3.44285727499436,5.82572079523371,-47.3671558088655));
#36244=CARTESIAN_POINT('Ctrl Pts',(3.33009239764871,5.89236205594276,-47.3609985923893));
#36245=CARTESIAN_POINT('Ctrl Pts',(3.21543230600807,5.95570426476123,-47.3548413759131));
#36246=CARTESIAN_POINT('Ctrl Pts',(3.0990855038472,6.01564277861013,-47.3486841594369));
#36247=CARTESIAN_POINT('Origin',(0.,0.,-63.6971797838103));
#36248=CARTESIAN_POINT('',(3.0990855038472,6.01564277861013,-44.9542932404068));
#36249=CARTESIAN_POINT('',(3.09908550384718,6.01564277861013,-45.3486032095739));
#36250=CARTESIAN_POINT('',(3.09908550384721,6.01564277861012,-63.6971797838103));
#36251=CARTESIAN_POINT('',(-6.76699445554588,0.00866248297634946,-46.3028202161574));
#36252=CARTESIAN_POINT('Ctrl Pts',(-6.76699445554588,0.00866248297634946,
-46.3028202161574));
#36253=CARTESIAN_POINT('Ctrl Pts',(-6.76721031445594,-0.159963077559033,
-46.2948874461289));
#36254=CARTESIAN_POINT('Ctrl Pts',(-6.76111922286706,-0.328826249995859,
-46.2869546761004));
#36255=CARTESIAN_POINT('Ctrl Pts',(-6.74869499058743,-0.497398154419779,
-46.2790219060718));
#36256=CARTESIAN_POINT('Ctrl Pts',(-6.73628023855867,-0.665841430860132,
-46.2710951891054));
#36257=CARTESIAN_POINT('Ctrl Pts',(-6.71754198738097,-0.833993501133486,
-46.263168472139));
#36258=CARTESIAN_POINT('Ctrl Pts',(-6.69250610205252,-1.00132465963334,
-46.2552417551727));
#36259=CARTESIAN_POINT('Ctrl Pts',(-6.66748360251499,-1.16856635215775,
-46.2473192763378));
#36260=CARTESIAN_POINT('Ctrl Pts',(-6.63617022537958,-1.33498762807606,
-46.239396797503));
#36261=CARTESIAN_POINT('Ctrl Pts',(-6.59864372361297,-1.50006333493727,
-46.2314743186682));
#36262=CARTESIAN_POINT('Ctrl Pts',(-6.56112284707921,-1.66511429690502,
-46.2235530274151));
#36263=CARTESIAN_POINT('Ctrl Pts',(-6.51739077483453,-1.82881971544845,
-46.2156317361621));
#36264=CARTESIAN_POINT('Ctrl Pts',(-6.46757647866796,-1.99066408331014,
-46.207710444909));
#36265=CARTESIAN_POINT('Ctrl Pts',(-6.41776374034483,-2.15250338980982,
-46.1997894013786));
#36266=CARTESIAN_POINT('Ctrl Pts',(-6.36186926856301,-2.31248139441357,
-46.1918683578482));
#36267=CARTESIAN_POINT('Ctrl Pts',(-6.30007195470136,-2.47009764292536,
-46.1839473143178));
#36268=CARTESIAN_POINT('Ctrl Pts',(-6.2382638160406,-2.62774150047253,-46.1760248832886));
#36269=CARTESIAN_POINT('Ctrl Pts',(-6.17055091868677,-2.78302242183815,
-46.1681024522593));
#36270=CARTESIAN_POINT('Ctrl Pts',(-6.09716023660602,-2.93546010859464,
-46.16018002123));
#36271=CARTESIAN_POINT('Ctrl Pts',(-6.02374153513716,-3.08795599362083,
-46.1522545655433));
#36272=CARTESIAN_POINT('Ctrl Pts',(-5.94464090369827,-3.23760613974861,
-46.1443291098566));
#36273=CARTESIAN_POINT('Ctrl Pts',(-5.86013102767455,-3.38395528021368,
-46.13640365417));
#36274=CARTESIAN_POINT('Ctrl Pts',(-5.77552340599045,-3.53047369075763,
-46.128469031757));
#36275=CARTESIAN_POINT('Ctrl Pts',(-5.68549424387489,-3.67368314307318,
-46.1205344093441));
#36276=CARTESIAN_POINT('Ctrl Pts',(-5.59035961032058,-3.81315727806975,
-46.1125997869311));
#36277=CARTESIAN_POINT('Ctrl Pts',(-5.49516237281654,-3.95272319490654,
-46.1046599430895));
#36278=CARTESIAN_POINT('Ctrl Pts',(-5.39485320534837,-4.08854859656338,
-46.0967200992479));
#36279=CARTESIAN_POINT('Ctrl Pts',(-5.28978760141626,-4.22024124096039,
-46.0887802554063));
#36280=CARTESIAN_POINT('Ctrl Pts',(-5.1845670780937,-4.35212806635891,-46.080828704253));
#36281=CARTESIAN_POINT('Ctrl Pts',(-5.07457637133191,-4.47986968581321,
-46.0728771530998));
#36282=CARTESIAN_POINT('Ctrl Pts',(-4.96020730033993,-4.60311118024043,
-46.0649256019465));
#36283=CARTESIAN_POINT('Ctrl Pts',(-4.90887553083546,-4.658425120718,-46.0613567420488));
#36284=CARTESIAN_POINT('Ctrl Pts',(-4.85666220303607,-4.71283308217111,
-46.0577878821511));
#36285=CARTESIAN_POINT('Ctrl Pts',(-4.80360476700314,-4.76630572271909,
-46.0542190222534));
#36286=CARTESIAN_POINT('Ctrl Pts',(-4.67970740531085,-4.89117265150364,
-46.0458851795607));
#36287=CARTESIAN_POINT('Ctrl Pts',(-4.55077972205122,-5.01136532619399,
-46.037551336868));
#36288=CARTESIAN_POINT('Ctrl Pts',(-4.41720372934772,-5.12646078824725,
-46.0292174941753));
#36289=CARTESIAN_POINT('Ctrl Pts',(-4.28378517285028,-5.24142059573779,
-46.0208934739706));
#36290=CARTESIAN_POINT('Ctrl Pts',(-4.14572948208992,-5.35129493336938,
-46.0125694537658));
#36291=CARTESIAN_POINT('Ctrl Pts',(-4.00345627242166,-5.45569673596395,
-46.0042454335611));
#36292=CARTESIAN_POINT('Ctrl Pts',(-3.86132466414372,-5.55999462974509,
-45.9959296980702));
#36293=CARTESIAN_POINT('Ctrl Pts',(-3.71498417868327,-5.6588306356081,-45.9876139625793));
#36294=CARTESIAN_POINT('Ctrl Pts',(-3.56488851785638,-5.75185699189885,
-45.9792982270884));
#36295=CARTESIAN_POINT('Ctrl Pts',(-3.41491474253282,-5.84480780593744,
-45.9709892444083));
#36296=CARTESIAN_POINT('Ctrl Pts',(-3.26119216244563,-5.93195818849206,
-45.9626802617283));
#36297=CARTESIAN_POINT('Ctrl Pts',(-3.10420473865019,-6.01300273910978,
-45.9543712790482));
#36298=CARTESIAN_POINT('Ctrl Pts',(-2.94731604847152,-6.09399631862798,
-45.9460675221111));
#36299=CARTESIAN_POINT('Ctrl Pts',(-2.78716691489952,-6.16889156005191,
-45.9377637651739));
#36300=CARTESIAN_POINT('Ctrl Pts',(-2.62426745602946,-6.23742810132708,
-45.9294600082367));
#36301=CARTESIAN_POINT('Ctrl Pts',(-2.46143413041278,-6.30593681841866,
-45.9211596224247));
#36302=CARTESIAN_POINT('Ctrl Pts',(-2.2958530244332,-6.36809184448666,-45.9128592366127));
#36303=CARTESIAN_POINT('Ctrl Pts',(-2.12805613808744,-6.42368010358147,
-45.9045588508006));
#36304=CARTESIAN_POINT('Ctrl Pts',(-1.96029463573881,-6.47925664055888,
-45.896260215324));
#36305=CARTESIAN_POINT('Ctrl Pts',(-1.79031861385656,-6.52826906003398,
-45.8879615798474));
#36306=CARTESIAN_POINT('Ctrl Pts',(-1.6186774427106,-6.57055342695422,-45.8796629443707));
#36307=CARTESIAN_POINT('Ctrl Pts',(-1.44704397575741,-6.61283589592124,
-45.8713646813821));
#36308=CARTESIAN_POINT('Ctrl Pts',(-1.27374584619206,-6.64839083111104,
-45.8630664183936));
#36309=CARTESIAN_POINT('Ctrl Pts',(-1.09934507768376,-6.67710486664486,
-45.854768155405));
#36310=CARTESIAN_POINT('Ctrl Pts',(-0.924923189986577,-6.70582237932586,
-45.8464688875322));
#36311=CARTESIAN_POINT('Ctrl Pts',(-0.749398740524253,-6.72769728575488,
-45.8381696196593));
#36312=CARTESIAN_POINT('Ctrl Pts',(-0.573341573289961,-6.74266775396337,
-45.8298703517865));
#36313=CARTESIAN_POINT('Ctrl Pts',(-0.397160785548049,-6.75764873385342,
-45.82156525649));
#36314=CARTESIAN_POINT('Ctrl Pts',(-0.220446879565258,-6.76571555880835,
-45.8132601611935));
#36315=CARTESIAN_POINT('Ctrl Pts',(-0.0437733295457148,-6.76685842142574,
-45.804955065897));
#36316=CARTESIAN_POINT('Ctrl Pts',(0.132964644837099,-6.76800170079027,
-45.7966469421309));
#36317=CARTESIAN_POINT('Ctrl Pts',(0.309661886153458,-6.76221599062028,
-45.7883388183648));
#36318=CARTESIAN_POINT('Ctrl Pts',(0.485747087053247,-6.74954359697152,
-45.7800306945987));
#36319=CARTESIAN_POINT('Ctrl Pts',(0.662019465504322,-6.73685773264153,
-45.771713739345));
#36320=CARTESIAN_POINT('Ctrl Pts',(0.837678157137102,-6.71727059098702,
-45.7633967840913));
#36321=CARTESIAN_POINT('Ctrl Pts',(1.01215803202879,-6.69087625936989,-45.7550798288376));
#36322=CARTESIAN_POINT('Ctrl Pts',(1.14074704517418,-6.67142403854851,-45.7489503593552));
#36323=CARTESIAN_POINT('Ctrl Pts',(1.26869593148752,-6.64827559605648,-45.7428208898728));
#36324=CARTESIAN_POINT('Ctrl Pts',(1.39578288781446,-6.62148617230938,-45.7366914203904));
#36325=CARTESIAN_POINT('Ctrl Pts',(1.57100439119975,-6.58455017793623,-45.7282403968652));
#36326=CARTESIAN_POINT('Ctrl Pts',(1.74490711405204,-6.54062348449208,-45.71978937334));
#36327=CARTESIAN_POINT('Ctrl Pts',(1.91691339630708,-6.48981756531403,-45.7113383498148));
#36328=CARTESIAN_POINT('Ctrl Pts',(2.08876823214282,-6.4390563792378,-45.7028947671647));
#36329=CARTESIAN_POINT('Ctrl Pts',(2.25872963909701,-6.38142813354898,-45.6944511845145));
#36330=CARTESIAN_POINT('Ctrl Pts',(2.42623146224893,-6.31709505165099,-45.6860076018643));
#36331=CARTESIAN_POINT('Ctrl Pts',(2.59360857507555,-6.25280986773656,-45.6775703057245));
#36332=CARTESIAN_POINT('Ctrl Pts',(2.75852944614736,-6.18182991731004,-45.6691330095847));
#36333=CARTESIAN_POINT('Ctrl Pts',(2.92044399381099,-6.10436695153669,-45.6606957134449));
#36334=CARTESIAN_POINT('Ctrl Pts',(3.08224302779018,-6.02695924968318,-45.6522644366725));
#36335=CARTESIAN_POINT('Ctrl Pts',(3.24103971818719,-5.94307790080715,-45.6438331599002));
#36336=CARTESIAN_POINT('Ctrl Pts',(3.39630465759495,-5.85298245963533,-45.6354018831278));
#36337=CARTESIAN_POINT('Ctrl Pts',(3.55150304482962,-5.76292563663075,-45.6269742203059));
#36338=CARTESIAN_POINT('Ctrl Pts',(3.70317241279008,-5.66666019737143,-45.6185465574839));
#36339=CARTESIAN_POINT('Ctrl Pts',(3.85080805053698,-5.56449156328946,-45.610118894662));
#36340=CARTESIAN_POINT('Ctrl Pts',(3.99839824019555,-5.46235438075386,-45.601693826208));
#36341=CARTESIAN_POINT('Ctrl Pts',(4.14195690372836,-5.35431781584026,-45.593268757754));
#36342=CARTESIAN_POINT('Ctrl Pts',(4.28100811183295,-5.24073072637972,-45.5848436893));
#36343=CARTESIAN_POINT('Ctrl Pts',(4.31905677861794,-5.20964982189229,-45.5825383326863));
#36344=CARTESIAN_POINT('Ctrl Pts',(4.35676813232352,-5.17815357257993,-45.5802329760726));
#36345=CARTESIAN_POINT('Ctrl Pts',(4.39413283355317,-5.14624966758221,-45.5779276194589));
#36346=CARTESIAN_POINT('Ctrl Pts',(4.53382746006166,-5.02697120566097,-45.5693086309344));
#36347=CARTESIAN_POINT('Ctrl Pts',(4.6686117013062,-4.90204487325264,-45.5606896424098));
#36348=CARTESIAN_POINT('Ctrl Pts',(4.79804525525148,-4.77190221280348,-45.5520706538853));
#36349=CARTESIAN_POINT('Ctrl Pts',(4.92755635144531,-4.6416815852877,-45.5434465018176));
#36350=CARTESIAN_POINT('Ctrl Pts',(5.05171014858183,-4.50623860874799,-45.5348223497499));
#36351=CARTESIAN_POINT('Ctrl Pts',(5.1701045948368,-4.36604025158352,-45.5261981976821));
#36352=CARTESIAN_POINT('Ctrl Pts',(5.29255408272797,-4.22104006296822,-45.5172786660859));
#36353=CARTESIAN_POINT('Ctrl Pts',(5.40884249144538,-4.07095325895653,-45.5083591344897));
#36354=CARTESIAN_POINT('Ctrl Pts',(5.51857210252305,-3.91633131249826,-45.4994396028934));
#36355=CARTESIAN_POINT('Ctrl Pts',(5.62486554799119,-3.76655132811095,-45.4907993850342));
#36356=CARTESIAN_POINT('Ctrl Pts',(5.72500462734414,-3.61251621795943,-45.4821591671749));
#36357=CARTESIAN_POINT('Ctrl Pts',(5.81867314823915,-3.45475495425663,-45.4735189493156));
#36358=CARTESIAN_POINT('Ctrl Pts',(5.91688372554382,-3.28934372926319,-45.4644597608509));
#36359=CARTESIAN_POINT('Ctrl Pts',(6.00798043531471,-3.11983634042863,-45.4554005723862));
#36360=CARTESIAN_POINT('Ctrl Pts',(6.09165394290615,-2.94686973581731,-45.4463413839214));
#36361=CARTESIAN_POINT('Ctrl Pts',(6.17532745049759,-2.77390313120598,-45.4372821954567));
#36362=CARTESIAN_POINT('Ctrl Pts',(6.25157763451954,-2.59747767518718,-45.428223006992));
#36363=CARTESIAN_POINT('Ctrl Pts',(6.32015363622209,-2.41825288473906,-45.4191638185273));
#36364=CARTESIAN_POINT('Ctrl Pts',(6.38861083481286,-2.23933858866626,-45.4101203244711));
#36365=CARTESIAN_POINT('Ctrl Pts',(6.44948427553468,-2.05747012730974,-45.4010768304148));
#36366=CARTESIAN_POINT('Ctrl Pts',(6.50254660692547,-1.87327964403664,-45.3920333363585));
#36367=CARTESIAN_POINT('Ctrl Pts',(6.55556040239563,-1.68925763912556,-45.3829981143532));
#36368=CARTESIAN_POINT('Ctrl Pts',(6.6007772872885,-1.50291808134845,-45.3739628923479));
#36369=CARTESIAN_POINT('Ctrl Pts',(6.63801961221435,-1.31490860057179,-45.3649276703426));
#36370=CARTESIAN_POINT('Ctrl Pts',(6.67519632427136,-1.12723035157049,-45.3559083664315));
#36371=CARTESIAN_POINT('Ctrl Pts',(6.70442648513945,-0.937888287704712,
-45.3468890625204));
#36372=CARTESIAN_POINT('Ctrl Pts',(6.72558342098193,-0.747540398515744,
-45.3378697586093));
#36373=CARTESIAN_POINT('Ctrl Pts',(6.74671381397062,-0.557431314049226,
-45.3288617700449));
#36374=CARTESIAN_POINT('Ctrl Pts',(6.75979116856504,-0.366319158461256,
-45.3198537814806));
#36375=CARTESIAN_POINT('Ctrl Pts',(6.76474017020583,-0.174869750396155,
-45.3108457929162));
#36376=CARTESIAN_POINT('Ctrl Pts',(6.76967799435306,0.0161472624749014,
-45.3018581492096));
#36377=CARTESIAN_POINT('Ctrl Pts',(6.76652410399345,0.2074997698381,-45.2928705055029));
#36378=CARTESIAN_POINT('Ctrl Pts',(6.75525506917884,0.398519698802507,-45.2838828617962));
#36379=CARTESIAN_POINT('Ctrl Pts',(6.74544052091391,0.564884817308657,-45.2760552470628));
#36380=CARTESIAN_POINT('Ctrl Pts',(6.72947123810675,0.730997469063674,-45.2682276323293));
#36381=CARTESIAN_POINT('Ctrl Pts',(6.7073639010008,0.896414245508953,-45.2604000175958));
#36382=CARTESIAN_POINT('Ctrl Pts',(6.68442186715912,1.06807658842258,-45.2522768591505));
#36383=CARTESIAN_POINT('Ctrl Pts',(6.65487812228032,1.2389125600411,-45.2441537007052));
#36384=CARTESIAN_POINT('Ctrl Pts',(6.61881905696717,1.40837611848831,-45.2360305422599));
#36385=CARTESIAN_POINT('Ctrl Pts',(6.58276253400699,1.57782772886709,-45.2279079565399));
#36386=CARTESIAN_POINT('Ctrl Pts',(6.54019168179962,1.74590676080617,-45.2197853708198));
#36387=CARTESIAN_POINT('Ctrl Pts',(6.49124394706447,1.91207767093778,-45.2116627850997));
#36388=CARTESIAN_POINT('Ctrl Pts',(6.44229033075539,2.07826854821392,-45.2035392233674));
#36389=CARTESIAN_POINT('Ctrl Pts',(6.38695841070977,2.2425504963687,-45.1954156616351));
#36390=CARTESIAN_POINT('Ctrl Pts',(6.32543539375741,2.40440347683183,-45.1872920999027));
#36391=CARTESIAN_POINT('Ctrl Pts',(6.26386756458739,2.56637434798613,-45.1791626211196));
#36392=CARTESIAN_POINT('Ctrl Pts',(6.19609976208033,2.72591237537359,-45.1710331423365));
#36393=CARTESIAN_POINT('Ctrl Pts',(6.12236745829981,2.88251725156182,-45.1629036635534));
#36394=CARTESIAN_POINT('Ctrl Pts',(6.04860509515681,3.03918597280169,-45.1547708705249));
#36395=CARTESIAN_POINT('Ctrl Pts',(5.96887355219253,3.1929188345764,-45.1466380774963));
#36396=CARTESIAN_POINT('Ctrl Pts',(5.88345397314894,3.34324069516958,-45.1385052844678));
#36397=CARTESIAN_POINT('Ctrl Pts',(5.79794151327188,3.49372600798129,-45.1303636482606));
#36398=CARTESIAN_POINT('Ctrl Pts',(5.70672885683142,3.6407926009944,-45.1222220120535));
#36399=CARTESIAN_POINT('Ctrl Pts',(5.61014052811366,3.78399421971237,-45.1140803758463));
#36400=CARTESIAN_POINT('Ctrl Pts',(5.56093008657976,3.85695349935859,-45.1099323227857));
#36401=CARTESIAN_POINT('Ctrl Pts',(5.51032490727817,3.92891003821627,-45.105784269725));
#36402=CARTESIAN_POINT('Ctrl Pts',(5.45837184762625,3.99980821703257,-45.1016362166643));
#36403=CARTESIAN_POINT('Ctrl Pts',(5.35265160826175,4.14408022882907,-45.09319526698));
#36404=CARTESIAN_POINT('Ctrl Pts',(5.24112980853916,4.28426478902159,-45.0847543172956));
#36405=CARTESIAN_POINT('Ctrl Pts',(5.12414896161536,4.41988534004857,-45.0763133676113));
#36406=CARTESIAN_POINT('Ctrl Pts',(5.00725445971155,4.55540578785783,-45.067878648297));
#36407=CARTESIAN_POINT('Ctrl Pts',(4.88490915937136,4.68636868978522,-45.0594439289827));
#36408=CARTESIAN_POINT('Ctrl Pts',(4.75749678072063,4.81232930932962,-45.0510092096685));
#36409=CARTESIAN_POINT('Ctrl Pts',(4.63017123614944,4.93820408419729,-45.0425802387838));
#36410=CARTESIAN_POINT('Ctrl Pts',(4.49778573702322,5.059083142006,-45.0341512678991));
#36411=CARTESIAN_POINT('Ctrl Pts',(4.36076205027886,5.17455730868329,-45.0257222970144));
#36412=CARTESIAN_POINT('Ctrl Pts',(4.22379593538374,5.28998295775409,-45.0172968676447));
#36413=CARTESIAN_POINT('Ctrl Pts',(4.08219577218,5.40000802818307,-45.008871438275));
#36414=CARTESIAN_POINT('Ctrl Pts',(3.93641814444968,5.50426209332799,-45.0004460089053));
#36415=CARTESIAN_POINT('Ctrl Pts',(3.79067326559698,5.60849273784468,-44.9920224723045));
#36416=CARTESIAN_POINT('Ctrl Pts',(3.64075306277067,5.70695476607202,-44.9835989357037));
#36417=CARTESIAN_POINT('Ctrl Pts',(3.48714535424184,5.79931946683312,-44.9751753991029));
#36418=CARTESIAN_POINT('Ctrl Pts',(3.36021289904917,5.8756442707966,-44.9682146795375));
#36419=CARTESIAN_POINT('Ctrl Pts',(3.23076311096976,5.94780627660475,-44.9612539599721));
#36420=CARTESIAN_POINT('Ctrl Pts',(3.0990855038472,6.01564277861013,-44.9542932404068));
#36421=CARTESIAN_POINT('Ctrl Pts',(3.0990855038472,6.01564277861013,-46.9540128207846));
#36422=CARTESIAN_POINT('Ctrl Pts',(2.9436651366959,6.09571086519164,-46.945789753969));
#36423=CARTESIAN_POINT('Ctrl Pts',(2.78499491016231,6.16982658704594,-46.9375666871535));
#36424=CARTESIAN_POINT('Ctrl Pts',(2.62356988515337,6.23772154377833,-46.929343620338));
#36425=CARTESIAN_POINT('Ctrl Pts',(2.4622820399152,6.30555880304654,-46.9211275415246));
#36426=CARTESIAN_POINT('Ctrl Pts',(2.29824438899914,6.36718569630545,-46.9129114627112));
#36427=CARTESIAN_POINT('Ctrl Pts',(2.1319750432217,6.42238050998848,-46.9046953838978));
#36428=CARTESIAN_POINT('Ctrl Pts',(1.96578725261032,6.47754825059814,-46.8964833350737));
#36429=CARTESIAN_POINT('Ctrl Pts',(1.79737028426355,6.526290083495,-46.8882712862495));
#36430=CARTESIAN_POINT('Ctrl Pts',(1.62726097812719,6.56843289598551,-46.8800592374253));
#36431=CARTESIAN_POINT('Ctrl Pts',(1.45720570249951,6.61056232297908,-46.871849796931));
#36432=CARTESIAN_POINT('Ctrl Pts',(1.28545950506018,6.64609682019459,-46.8636403564367));
#36433=CARTESIAN_POINT('Ctrl Pts',(1.11257317584935,6.67491347722055,-46.8554309159423));
#36434=CARTESIAN_POINT('Ctrl Pts',(1.06067644192987,6.6835636139257,-46.8529666195985));
#36435=CARTESIAN_POINT('Ctrl Pts',(1.00867705365995,6.69160877317709,-46.8505023232548));
#36436=CARTESIAN_POINT('Ctrl Pts',(0.956590091472105,6.69904652893958,-46.848038026911));
#36437=CARTESIAN_POINT('Ctrl Pts',(0.769346505385178,6.72578396961396,-46.8391793093892));
#36438=CARTESIAN_POINT('Ctrl Pts',(0.581164697193612,6.74464057162761,-46.8303205918675));
#36439=CARTESIAN_POINT('Ctrl Pts',(0.392697660495038,6.75559601718766,-46.8214618743457));
#36440=CARTESIAN_POINT('Ctrl Pts',(0.203878032240445,6.76657195862679,-46.8125865835862));
#36441=CARTESIAN_POINT('Ctrl Pts',(0.0147723679925125,6.76961718815369,
-46.8037112928268));
#36442=CARTESIAN_POINT('Ctrl Pts',(-0.173966971303869,6.76476344692816,
-46.7948360020673));
#36443=CARTESIAN_POINT('Ctrl Pts',(-0.36324237276091,6.75989591998622,-46.7859355034866));
#36444=CARTESIAN_POINT('Ctrl Pts',(-0.552149106327011,6.74708453411111,
-46.7770350049058));
#36445=CARTESIAN_POINT('Ctrl Pts',(-0.740037474591596,6.72641312559674,
-46.768134506325));
#36446=CARTESIAN_POINT('Ctrl Pts',(-0.928180187591721,6.705713734169,-46.7592219591274));
#36447=CARTESIAN_POINT('Ctrl Pts',(-1.11530152449871,6.67713310069943,-46.7503094119298));
#36448=CARTESIAN_POINT('Ctrl Pts',(-1.30076123301329,6.64080636780578,-46.7413968647322));
#36449=CARTESIAN_POINT('Ctrl Pts',(-1.48663045467715,6.60439942193806,-46.7324646377599));
#36450=CARTESIAN_POINT('Ctrl Pts',(-1.67083045371743,6.56021221558444,-46.7235324107876));
#36451=CARTESIAN_POINT('Ctrl Pts',(-1.85273262098156,6.50843075058426,-46.7146001838154));
#36452=CARTESIAN_POINT('Ctrl Pts',(-2.02465117435366,6.45949128665037,-46.7061581978701));
#36453=CARTESIAN_POINT('Ctrl Pts',(-2.19451716772574,6.40376878410272,-46.6977162119248));
#36454=CARTESIAN_POINT('Ctrl Pts',(-2.36181586475644,6.34145999127841,-46.6892742259795));
#36455=CARTESIAN_POINT('Ctrl Pts',(-2.52479412761867,6.28076030266288,-46.6810502515619));
#36456=CARTESIAN_POINT('Ctrl Pts',(-2.6856469466595,6.21369318557838,-46.6728262771444));
#36457=CARTESIAN_POINT('Ctrl Pts',(-2.84384203240731,6.14042763125773,-46.6646023027268));
#36458=CARTESIAN_POINT('Ctrl Pts',(-3.00187004879588,6.06723945247096,-46.6563870136241));
#36459=CARTESIAN_POINT('Ctrl Pts',(-3.15724559852198,5.98786602148833,-46.6481717245215));
#36460=CARTESIAN_POINT('Ctrl Pts',(-3.30945350000741,5.90252543673373,-46.6399564354188));
#36461=CARTESIAN_POINT('Ctrl Pts',(-3.46153118484209,5.81725786241428,-46.6317481746466));
#36462=CARTESIAN_POINT('Ctrl Pts',(-3.61044630761767,5.72603347585005,-46.6235399138744));
#36463=CARTESIAN_POINT('Ctrl Pts',(-3.75570547846719,5.62911763591875,-46.6153316531022));
#36464=CARTESIAN_POINT('Ctrl Pts',(-3.90086950502898,5.53226527554958,-46.6071287687143));
#36465=CARTESIAN_POINT('Ctrl Pts',(-4.0423820522995,5.42972908567718,-46.5989258843265));
#36466=CARTESIAN_POINT('Ctrl Pts',(-4.17977600159479,5.321819385933,-46.5907229999386));
#36467=CARTESIAN_POINT('Ctrl Pts',(-4.317107503117,5.2139587328934,-46.5825238438944));
#36468=CARTESIAN_POINT('Ctrl Pts',(-4.45032385468422,5.10072965681161,-46.5743246878501));
#36469=CARTESIAN_POINT('Ctrl Pts',(-4.57898844007612,4.98248470801961,-46.5661255318059));
#36470=CARTESIAN_POINT('Ctrl Pts',(-4.70764183477774,4.86425004366288,-46.5579270888889));
#36471=CARTESIAN_POINT('Ctrl Pts',(-4.83174398226159,4.7410006117415,-46.5497286459719));
#36472=CARTESIAN_POINT('Ctrl Pts',(-4.95089251187824,4.61312825919983,-46.5415302030549));
#36473=CARTESIAN_POINT('Ctrl Pts',(-5.07003985491662,4.48525718011537,-46.5333318417847));
#36474=CARTESIAN_POINT('Ctrl Pts',(-5.18423343304624,4.35276353382202,-46.5251334805144));
#36475=CARTESIAN_POINT('Ctrl Pts',(-5.29310891271248,4.21607483782769,-46.5169351192442));
#36476=CARTESIAN_POINT('Ctrl Pts',(-5.40200308611845,4.07936267261039,-46.5087353503289));
#36477=CARTESIAN_POINT('Ctrl Pts',(-5.50557711839364,3.93845430325552,-46.5005355814136));
#36478=CARTESIAN_POINT('Ctrl Pts',(-5.60350799682097,3.79380905286012,-46.4923358124983));
#36479=CARTESIAN_POINT('Ctrl Pts',(-5.7014734798485,3.6491126909957,-46.484133146134));
#36480=CARTESIAN_POINT('Ctrl Pts',(-5.79379163587259,3.50067711456468,-46.4759304797698));
#36481=CARTESIAN_POINT('Ctrl Pts',(-5.88018365440796,3.34898927893677,-46.4677278134055));
#36482=CARTESIAN_POINT('Ctrl Pts',(-5.9666737926827,3.19712916384197,-46.4595158308625));
#36483=CARTESIAN_POINT('Ctrl Pts',(-6.0472241693232,3.04200972215826,-46.4513038483194));
#36484=CARTESIAN_POINT('Ctrl Pts',(-6.12160222207306,2.88414202748585,-46.4430918657764));
#36485=CARTESIAN_POINT('Ctrl Pts',(-6.19602414400368,2.72618122031349,-46.4348750396951));
#36486=CARTESIAN_POINT('Ctrl Pts',(-6.26426634522733,2.56546925861872,-46.4266582136138));
#36487=CARTESIAN_POINT('Ctrl Pts',(-6.32614509416542,2.40253558715929,-46.4184413875325));
#36488=CARTESIAN_POINT('Ctrl Pts',(-6.38811926907129,2.23935064844657,-46.4102118899186));
#36489=CARTESIAN_POINT('Ctrl Pts',(-6.44371026686801,2.07393749294943,-46.4019823923048));
#36490=CARTESIAN_POINT('Ctrl Pts',(-6.49278437452873,1.90684033570607,-46.3937528946909));
#36491=CARTESIAN_POINT('Ctrl Pts',(-6.53652694311385,1.75789704953099,-46.3864174711661));
#36492=CARTESIAN_POINT('Ctrl Pts',(-6.57509240681827,1.60761613177491,-46.3790820476413));
#36493=CARTESIAN_POINT('Ctrl Pts',(-6.6084206600231,1.45638778495972,-46.3717466241164));
#36494=CARTESIAN_POINT('Ctrl Pts',(-6.66061480096339,1.21955468124653,-46.360258889462));
#36495=CARTESIAN_POINT('Ctrl Pts',(-6.70011427082052,0.979728298518272,
-46.3487711548076));
#36496=CARTESIAN_POINT('Ctrl Pts',(-6.72663108996774,0.738053642684177,
-46.3372834201532));
#36497=CARTESIAN_POINT('Ctrl Pts',(-6.75169631263707,0.509608857192325,
-46.326424552599));
#36498=CARTESIAN_POINT('Ctrl Pts',(-6.76516160254484,0.279512294337435,
-46.3155656850448));
#36499=CARTESIAN_POINT('Ctrl Pts',(-6.76682433008413,0.0487594686342606,
-46.3047068174906));
#36500=CARTESIAN_POINT('Ctrl Pts',(-6.76692062324185,0.035395933289899,
-46.3040779503904));
#36501=CARTESIAN_POINT('Ctrl Pts',(-6.7669773434168,0.0220302060269217,
-46.3034490832902));
#36502=CARTESIAN_POINT('Ctrl Pts',(-6.766994455545,0.00866248366889811,
-46.30282021619));
#36503=CARTESIAN_POINT('',(-6.767,7.08953227612601E-13,-46.6971797838101));
#36504=CARTESIAN_POINT('Ctrl Pts',(3.0990855038472,6.01564277861013,-47.3486841594369));
#36505=CARTESIAN_POINT('Ctrl Pts',(2.94193708164431,6.09660110926984,-47.340367670832));
#36506=CARTESIAN_POINT('Ctrl Pts',(2.78171095141422,6.17134796408445,-47.332051182227));
#36507=CARTESIAN_POINT('Ctrl Pts',(2.61893827740273,6.23966756319236,-47.3237346936221));
#36508=CARTESIAN_POINT('Ctrl Pts',(2.45688780546686,6.30768403675059,-47.3154551042409));
#36509=CARTESIAN_POINT('Ctrl Pts',(2.29231367972388,6.36933010932947,-47.3071755148598));
#36510=CARTESIAN_POINT('Ctrl Pts',(2.12575517203363,6.42444191728529,-47.2988959254787));
#36511=CARTESIAN_POINT('Ctrl Pts',(1.95574796491077,6.48069485014348,-47.2904449019535));
#36512=CARTESIAN_POINT('Ctrl Pts',(1.78336267081961,6.53024302663276,-47.2819938784283));
#36513=CARTESIAN_POINT('Ctrl Pts',(1.60915457911702,6.57289209865085,-47.2735428549031));
#36514=CARTESIAN_POINT('Ctrl Pts',(1.43509987246143,6.61550361942862,-47.265099272253));
#36515=CARTESIAN_POINT('Ctrl Pts',(1.2592258875842,6.65122806481807,-47.2566556896028));
#36516=CARTESIAN_POINT('Ctrl Pts',(1.08210350900727,6.67992073274782,-47.2482121069527));
#36517=CARTESIAN_POINT('Ctrl Pts',(0.905113003558764,6.70859203809249,-47.2397748108129));
#36518=CARTESIAN_POINT('Ctrl Pts',(0.726876283412527,6.73024194961993,-47.231337514673));
#36519=CARTESIAN_POINT('Ctrl Pts',(0.547975265559801,6.74477665370283,-47.2229002185332));
#36520=CARTESIAN_POINT('Ctrl Pts',(0.369201879942919,6.75930098838256,-47.2144689417608));
#36521=CARTESIAN_POINT('Ctrl Pts',(0.189765471540904,6.76672021408748,-47.2060376649885));
#36522=CARTESIAN_POINT('Ctrl Pts',(0.0102541461709204,6.76699223085754,
-47.1976063882161));
#36523=CARTESIAN_POINT('Ctrl Pts',(-0.169180234146751,6.76726413103137,
-47.1891787253942));
#36524=CARTESIAN_POINT('Ctrl Pts',(-0.348689136538506,6.76039492909866,
-47.1807510625723));
#36525=CARTESIAN_POINT('Ctrl Pts',(-0.527682716869333,6.74639458898732,
-47.1723233997504));
#36526=CARTESIAN_POINT('Ctrl Pts',(-0.706621195896954,6.73239855873438,
-47.1638983312964));
#36527=CARTESIAN_POINT('Ctrl Pts',(-0.885044339136366,6.71127579399997,
-47.1554732628424));
#36528=CARTESIAN_POINT('Ctrl Pts',(-1.06236531734555,6.68308827807185,-47.1470481943884));
#36529=CARTESIAN_POINT('Ctrl Pts',(-1.11088576464008,6.67537531091609,-47.1447428377747));
#36530=CARTESIAN_POINT('Ctrl Pts',(-1.15932371901165,6.66713367906998,-47.1424374811609));
#36531=CARTESIAN_POINT('Ctrl Pts',(-1.20766724045393,6.65836532764119,-47.1401321245471));
#36532=CARTESIAN_POINT('Ctrl Pts',(-1.38840815231793,6.62558327566189,-47.1315131360226));
#36533=CARTESIAN_POINT('Ctrl Pts',(-1.56774768451873,6.58544959396408,-47.1228941474982));
#36534=CARTESIAN_POINT('Ctrl Pts',(-1.74508818869424,6.53811564701022,-47.1142751589737));
#36535=CARTESIAN_POINT('Ctrl Pts',(-1.92253493565814,6.49075334279792,-47.1056510069059));
#36536=CARTESIAN_POINT('Ctrl Pts',(-2.09797997069514,6.43618224313281,-47.0970268548381));
#36537=CARTESIAN_POINT('Ctrl Pts',(-2.2708408736559,6.37460357406904,-47.0884027027703));
#36538=CARTESIAN_POINT('Ctrl Pts',(-2.44962230904706,6.31091581902359,-47.0794831711741));
#36539=CARTESIAN_POINT('Ctrl Pts',(-2.62563912946027,6.23973210127814,-47.0705636395779));
#36540=CARTESIAN_POINT('Ctrl Pts',(-2.79827013661542,6.16132885362617,-47.0616441079816));
#36541=CARTESIAN_POINT('Ctrl Pts',(-2.96549523077994,6.08538079141263,-47.0530038901224));
#36542=CARTESIAN_POINT('Ctrl Pts',(-3.12954310369647,6.00265869179961,-47.0443636722631));
#36543=CARTESIAN_POINT('Ctrl Pts',(-3.28987433182708,5.91346056728083,-47.0357234544039));
#36544=CARTESIAN_POINT('Ctrl Pts',(-3.45798014074014,5.81993715920501,-47.0266642659392));
#36545=CARTESIAN_POINT('Ctrl Pts',(-3.62199956735499,5.71929426033176,-47.0176050774744));
#36546=CARTESIAN_POINT('Ctrl Pts',(-3.78134478064512,5.61192664330958,-47.0085458890097));
#36547=CARTESIAN_POINT('Ctrl Pts',(-3.94068999393526,5.50455902628739,-46.999486700545));
#36548=CARTESIAN_POINT('Ctrl Pts',(-4.09536070564776,5.39046694490904,-46.9904275120803));
#36549=CARTESIAN_POINT('Ctrl Pts',(-4.24480826106308,5.27009410037531,-46.9813683236156));
#36550=CARTESIAN_POINT('Ctrl Pts',(-4.39399690907377,5.14992979334946,-46.9723248295593));
#36551=CARTESIAN_POINT('Ctrl Pts',(-4.53811845400273,5.02339642498788,-46.963281335503));
#36552=CARTESIAN_POINT('Ctrl Pts',(-4.67665832985533,4.89092586999586,-46.9542378414467));
#36553=CARTESIAN_POINT('Ctrl Pts',(-4.81507148379015,4.75857648533602,-46.9452026194414));
#36554=CARTESIAN_POINT('Ctrl Pts',(-4.94791298992995,4.62030092090447,-46.936167397436));
#36555=CARTESIAN_POINT('Ctrl Pts',(-5.07470344041103,4.4765694445502,-46.9271321754307));
#36556=CARTESIAN_POINT('Ctrl Pts',(-5.20127051372017,4.33309119176746,-46.9181128715196));
#36557=CARTESIAN_POINT('Ctrl Pts',(-5.32180766205109,4.18417639960211,-46.9090935676085));
#36558=CARTESIAN_POINT('Ctrl Pts',(-5.43587431600292,4.0303299394243,-46.9000742636973));
#36559=CARTESIAN_POINT('Ctrl Pts',(-5.54979786537001,3.87667649037666,-46.891066275133));
#36560=CARTESIAN_POINT('Ctrl Pts',(-5.65726697909139,3.71810391137042,-46.8820582865686));
#36561=CARTESIAN_POINT('Ctrl Pts',(-5.75788153122102,3.55514968354694,-46.8730502980042));
#36562=CARTESIAN_POINT('Ctrl Pts',(-5.85826884186048,3.39256349355473,-46.8640626542976));
#36563=CARTESIAN_POINT('Ctrl Pts',(-5.9518323680833,3.22561561049101,-46.8550750105909));
#36564=CARTESIAN_POINT('Ctrl Pts',(-6.0382156866559,3.05487157200145,-46.8460873668842));
#36565=CARTESIAN_POINT('Ctrl Pts',(-6.11344956988983,2.90616534877599,-46.8382597521508));
#36566=CARTESIAN_POINT('Ctrl Pts',(-6.18323768262847,2.75458022290258,-46.8304321374175));
#36567=CARTESIAN_POINT('Ctrl Pts',(-6.24737131521439,2.60050776769393,-46.8226045226841));
#36568=CARTESIAN_POINT('Ctrl Pts',(-6.31208327184665,2.44504596648796,-46.8147063225551));
#36569=CARTESIAN_POINT('Ctrl Pts',(-6.37102274600033,2.28708443549865,-46.8068081224262));
#36570=CARTESIAN_POINT('Ctrl Pts',(-6.4239928389839,2.12711189284522,-46.7989099222972));
#36571=CARTESIAN_POINT('Ctrl Pts',(-6.47695463193929,1.96716441672535,-46.7910129597588));
#36572=CARTESIAN_POINT('Ctrl Pts',(-6.52394878452144,1.8052069232848,-46.7831159972203));
#36573=CARTESIAN_POINT('Ctrl Pts',(-6.56482759592059,1.64174530175647,-46.7752190346819));
#36574=CARTESIAN_POINT('Ctrl Pts',(-6.60572002569664,1.47822922458494,-46.7673194413475));
#36575=CARTESIAN_POINT('Ctrl Pts',(-6.64049294982191,1.31320839355458,-46.7594198480131));
#36576=CARTESIAN_POINT('Ctrl Pts',(-6.669049312613,1.14720105732872,-46.7515202546787));
#36577=CARTESIAN_POINT('Ctrl Pts',(-6.69761136836199,0.981160626104589,
-46.743619086492));
#36578=CARTESIAN_POINT('Ctrl Pts',(-6.7199543417302,0.814133680992182,-46.7357179183053));
#36579=CARTESIAN_POINT('Ctrl Pts',(-6.73603290875121,0.646644919736252,
-46.7278167501186));
#36580=CARTESIAN_POINT('Ctrl Pts',(-6.7521232703795,0.479033295282363,-46.7199097859443));
#36581=CARTESIAN_POINT('Ctrl Pts',(-6.76194003144293,0.310959563961669,
-46.71200282177));
#36582=CARTESIAN_POINT('Ctrl Pts',(-6.76548995400033,0.142949929418268,
-46.7040958575957));
#36583=CARTESIAN_POINT('Ctrl Pts',(-6.76649701697076,0.0952879652797101,
-46.7018527633592));
#36584=CARTESIAN_POINT('Ctrl Pts',(-6.76700006046205,0.0476311417937134,
-46.6996096691227));
#36585=CARTESIAN_POINT('Ctrl Pts',(-6.76699999999455,-8.58912449818477E-6,
-46.6973665748862));
#36586=CARTESIAN_POINT('Ctrl Pts',(-6.767,7.08953217511608E-13,-46.6971797838101));
#36587=CARTESIAN_POINT('Ctrl Pts',(-6.76700000000002,-0.186007249559383,
-46.6884302719974));
#36588=CARTESIAN_POINT('Ctrl Pts',(-6.7593263729425,-0.37201435581565,-46.6796807601846));
#36589=CARTESIAN_POINT('Ctrl Pts',(-6.74400518263365,-0.557389537586108,
-46.6709312483719));
#36590=CARTESIAN_POINT('Ctrl Pts',(-6.72868405703731,-0.742763936382679,
-46.6621817735147));
#36591=CARTESIAN_POINT('Ctrl Pts',(-6.70571545643563,-0.927506130405085,
-46.6534322986575));
#36592=CARTESIAN_POINT('Ctrl Pts',(-6.67517739401571,-1.1109886400957,-46.6446828238003));
#36593=CARTESIAN_POINT('Ctrl Pts',(-6.64463945804384,-1.29447039004569,
-46.6359333851717));
#36594=CARTESIAN_POINT('Ctrl Pts',(-6.60653217002717,-1.4766921833931,-46.6271839465432));
#36595=CARTESIAN_POINT('Ctrl Pts',(-6.56098496085471,-1.65703510627818,
-46.6184345079147));
#36596=CARTESIAN_POINT('Ctrl Pts',(-6.51543793649543,-1.83737729740056,
-46.6096851047881));
#36597=CARTESIAN_POINT('Ctrl Pts',(-6.46245112156878,-2.01584035545012,
-46.6009357016614));
#36598=CARTESIAN_POINT('Ctrl Pts',(-6.40220448361693,-2.1918181379748,-46.5921862985348));
#36599=CARTESIAN_POINT('Ctrl Pts',(-6.34195808511946,-2.36779522106376,
-46.5834369301833));
#36600=CARTESIAN_POINT('Ctrl Pts',(-6.27445201416324,-2.54128677725818,
-46.5746875618317));
#36601=CARTESIAN_POINT('Ctrl Pts',(-6.19991555052692,-2.71170355428733,
-46.5659381934802));
#36602=CARTESIAN_POINT('Ctrl Pts',(-6.12537937695079,-2.88211966813605,
-46.557188859177));
#36603=CARTESIAN_POINT('Ctrl Pts',(-6.04381298028299,-3.04946076419972,
-46.5484395248738));
#36604=CARTESIAN_POINT('Ctrl Pts',(-5.95549339308817,-3.21315848424618,
-46.5396901905707));
#36605=CARTESIAN_POINT('Ctrl Pts',(-5.86717414225637,-3.37685558085381,
-46.5309408895891));
#36606=CARTESIAN_POINT('Ctrl Pts',(-5.77210188843887,-3.53690907700293,
-46.5221915886075));
#36607=CARTESIAN_POINT('Ctrl Pts',(-5.67059953311186,-3.69277537024277,
-46.513442287626));
#36608=CARTESIAN_POINT('Ctrl Pts',(-5.56909755592504,-3.84864108281321,
-46.5046930192394));
#36609=CARTESIAN_POINT('Ctrl Pts',(-5.46116568154745,-4.00031938355131,
-46.4959437508527));
#36610=CARTESIAN_POINT('Ctrl Pts',(-5.34717048488137,-4.14729511918474,
-46.4871944824661));
#36611=CARTESIAN_POINT('Ctrl Pts',(-5.23317570343069,-4.29427031947465,
-46.4784452459478));
#36612=CARTESIAN_POINT('Ctrl Pts',(-5.11311781951318,-4.43654276249819,
-46.4696960094294));
#36613=CARTESIAN_POINT('Ctrl Pts',(-4.98740458929022,-4.57362924412625,
-46.4609467729111));
#36614=CARTESIAN_POINT('Ctrl Pts',(-4.86169180652513,-4.71071523781502,
-46.4521975675344));
#36615=CARTESIAN_POINT('Ctrl Pts',(-4.7303239114134,-4.84261509584716,-46.4434483621577));
#36616=CARTESIAN_POINT('Ctrl Pts',(-4.59374706947091,-4.96888084599817,
-46.434699156781));
#36617=CARTESIAN_POINT('Ctrl Pts',(-4.45717070231289,-5.09514615720933,
-46.4259499818193));
#36618=CARTESIAN_POINT('Ctrl Pts',(-4.31538563497163,-5.21577720520747,
-46.4172008068576));
#36619=CARTESIAN_POINT('Ctrl Pts',(-4.16887340951861,-5.33036429293615,
-46.4084516318959));
#36620=CARTESIAN_POINT('Ctrl Pts',(-4.02236168122368,-5.44495099183791,
-46.3997024866226));
#36621=CARTESIAN_POINT('Ctrl Pts',(-3.87112305263094,-5.55349359497987,
-46.3909533413494));
#36622=CARTESIAN_POINT('Ctrl Pts',(-3.71567116928941,-5.65562346357247,
-46.3822041960762));
#36623=CARTESIAN_POINT('Ctrl Pts',(-3.56021980053267,-5.75775299408954,
-46.3734550797648));
#36624=CARTESIAN_POINT('Ctrl Pts',(-3.4005554444205,-5.85346967519898,-46.3647059634534));
#36625=CARTESIAN_POINT('Ctrl Pts',(-3.2372203588682,-5.94244843041395,-46.3559568471421));
#36626=CARTESIAN_POINT('Ctrl Pts',(-3.0738858004348,-6.03142689847455,-46.3472077590661));
#36627=CARTESIAN_POINT('Ctrl Pts',(-2.90688078789226,-6.113667347079,-46.3384586709901));
#36628=CARTESIAN_POINT('Ctrl Pts',(-2.7367725061041,-6.18889047001421,-46.3297095829141));
#36629=CARTESIAN_POINT('Ctrl Pts',(-2.56666475916939,-6.26411335643332,
-46.3209605223469));
#36630=CARTESIAN_POINT('Ctrl Pts',(-2.39345402457085,-6.33231884545259,
-46.3122114617797));
#36631=CARTESIAN_POINT('Ctrl Pts',(-2.21772855944043,-6.3932752980489,-46.3034624012125));
#36632=CARTESIAN_POINT('Ctrl Pts',(-2.04200363223579,-6.45423156404706,
-46.2947133674277));
#36633=CARTESIAN_POINT('Ctrl Pts',(-1.86376426061031,-6.50793874412453,
-46.2859643336429));
#36634=CARTESIAN_POINT('Ctrl Pts',(-1.68361577621695,-6.5542144394331,-46.2772152998581));
#36635=CARTESIAN_POINT('Ctrl Pts',(-1.5034678283323,-6.60048999692584,-46.2684662921292));
#36636=CARTESIAN_POINT('Ctrl Pts',(-1.32141105657409,-6.63933404265157,
-46.2597172844003));
#36637=CARTESIAN_POINT('Ctrl Pts',(-1.13806375346565,-6.67061465631524,
-46.2509682766715));
#36638=CARTESIAN_POINT('Ctrl Pts',(-0.954716981170515,-6.70189517941763,
-46.242219294272));
#36639=CARTESIAN_POINT('Ctrl Pts',(-0.770079967442999,-6.72561226608995,
-46.2334703118726));
#36640=CARTESIAN_POINT('Ctrl Pts',(-0.584779764073998,-6.74168536995977,
-46.2247213294732));
#36641=CARTESIAN_POINT('Ctrl Pts',(-0.391489587593831,-6.75845153117868,
-46.2155950990576));
#36642=CARTESIAN_POINT('Ctrl Pts',(-0.197478091806054,-6.76689985146392,
-46.2064688686419));
#36643=CARTESIAN_POINT('Ctrl Pts',(-0.00346214753179392,-6.76699911434415,
-46.1973426382263));
#36644=CARTESIAN_POINT('Ctrl Pts',(0.1844907984839,-6.76709527525937,-46.1885016025112));
#36645=CARTESIAN_POINT('Ctrl Pts',(0.372447602154062,-6.75935633790767,
-46.1796605667961));
#36646=CARTESIAN_POINT('Ctrl Pts',(0.559756448193523,-6.74380914014519,
-46.170819531081));
#36647=CARTESIAN_POINT('Ctrl Pts',(0.745136131042637,-6.72842206873162,
-46.1620695524676));
#36648=CARTESIAN_POINT('Ctrl Pts',(0.929880851944298,-6.70538686355734,
-46.1533195738543));
#36649=CARTESIAN_POINT('Ctrl Pts',(1.11336305057386,-6.67478177303325,-46.144569595241));
#36650=CARTESIAN_POINT('Ctrl Pts',(1.29684337090055,-6.64417699581274,-46.1358197062011));
#36651=CARTESIAN_POINT('Ctrl Pts',(1.4790609120513,-6.60600253548073,-46.1270698171611));
#36652=CARTESIAN_POINT('Ctrl Pts',(1.6593967109517,-6.56038806441225,-46.1183199281211));
#36653=CARTESIAN_POINT('Ctrl Pts',(1.83973072369116,-6.51477404513862,-46.1095701257456));
#36654=CARTESIAN_POINT('Ctrl Pts',(2.01818275356999,-6.46172023288673,-46.1008203233701));
#36655=CARTESIAN_POINT('Ctrl Pts',(2.19414664033296,-6.40140683918118,-46.0920705209946));
#36656=CARTESIAN_POINT('Ctrl Pts',(2.37010884271224,-6.3410940228151,-46.0833208023751));
#36657=CARTESIAN_POINT('Ctrl Pts',(2.54358267847766,-6.27352185699808,-46.0745710837555));
#36658=CARTESIAN_POINT('Ctrl Pts',(2.71397890841697,-6.19891986435281,-46.065821365136));
#36659=CARTESIAN_POINT('Ctrl Pts',(2.88437356388903,-6.12431856103262,-46.0570717273642));
#36660=CARTESIAN_POINT('Ctrl Pts',(3.05169040787139,-6.04268767582574,-46.0483220895923));
#36661=CARTESIAN_POINT('Ctrl Pts',(3.21536112512026,-5.9543044795396,-46.0395724518205));
#36662=CARTESIAN_POINT('Ctrl Pts',(3.37903038442812,-5.8659220705506,-46.0308228919884));
#36663=CARTESIAN_POINT('Ctrl Pts',(3.5390533297994,-5.77078760703397,-46.0220733321564));
#36664=CARTESIAN_POINT('Ctrl Pts',(3.69488643041856,-5.66922422085322,-46.0133237723243));
#36665=CARTESIAN_POINT('Ctrl Pts',(3.85071819468712,-5.56766170563179,-46.0045742875243));
#36666=CARTESIAN_POINT('Ctrl Pts',(4.00235994599199,-5.4596705345627,-45.9958248027243));
#36667=CARTESIAN_POINT('Ctrl Pts',(4.14929662974281,-5.34561750206699,-45.9870753179243));
#36668=CARTESIAN_POINT('Ctrl Pts',(4.29623210225016,-5.23156540974489,-45.978325905249));
#36669=CARTESIAN_POINT('Ctrl Pts',(4.4384623584208,-5.11145173172218,-45.9695764925736));
#36670=CARTESIAN_POINT('Ctrl Pts',(4.57550431797384,-4.98568443006602,-45.9608270798983));
#36671=CARTESIAN_POINT('Ctrl Pts',(4.71254519337452,-4.8599181233673,-45.9520777364404));
#36672=CARTESIAN_POINT('Ctrl Pts',(4.84439764314945,-4.72849847631141,-45.9433283929825));
#36673=CARTESIAN_POINT('Ctrl Pts',(4.9706138419665,-4.59187184425383,-45.9345790495246));
#36674=CARTESIAN_POINT('Ctrl Pts',(5.09682908420175,-4.45524624767783,-45.9258297723772));
#36675=CARTESIAN_POINT('Ctrl Pts',(5.21740796650144,-4.31341395556925,-45.9170804952299));
#36676=CARTESIAN_POINT('Ctrl Pts',(5.33194095942229,-4.16685668162884,-45.9083312180825));
#36677=CARTESIAN_POINT('Ctrl Pts',(5.44647312235122,-4.0203004697523,-45.8995820043389));
#36678=CARTESIAN_POINT('Ctrl Pts',(5.55495930712287,-3.8690195703555,-45.8908327905954));
#36679=CARTESIAN_POINT('Ctrl Pts',(5.65703106079802,-3.71352778058364,-45.8820835768519));
#36680=CARTESIAN_POINT('Ctrl Pts',(5.75910210868741,-3.55803706597595,-45.8733344236057));
#36681=CARTESIAN_POINT('Ctrl Pts',(5.85475865698552,-3.39833575880895,-45.8645852703595));
#36682=CARTESIAN_POINT('Ctrl Pts',(5.94367583069064,-3.23496624706719,-45.8558361171133));
#36683=CARTESIAN_POINT('Ctrl Pts',(6.03259241910078,-3.07159781070098,-45.8470870214582));
#36684=CARTESIAN_POINT('Ctrl Pts',(6.11476958470968,-2.90456146975833,-45.838337925803));
#36685=CARTESIAN_POINT('Ctrl Pts',(6.18992823574386,-2.73442451648256,-45.8295888301479));
#36686=CARTESIAN_POINT('Ctrl Pts',(6.26508641700941,-2.56428862662402,-45.8208397891778));
#36687=CARTESIAN_POINT('Ctrl Pts',(6.33322605570308,-2.39105242531249,-45.8120907482077));
#36688=CARTESIAN_POINT('Ctrl Pts',(6.39411573747782,-2.21530425353686,-45.8033417072375));
#36689=CARTESIAN_POINT('Ctrl Pts',(6.45500505889142,-2.03955712188509,-45.7945927180465));
#36690=CARTESIAN_POINT('Ctrl Pts',(6.50864441544947,-1.8612983202551,-45.7858437288555));
#36691=CARTESIAN_POINT('Ctrl Pts',(6.55485164049925,-1.68113324012237,-45.7770947396645));
#36692=CARTESIAN_POINT('Ctrl Pts',(6.60199852639128,-1.4973043591282,-45.7681678327876));
#36693=CARTESIAN_POINT('Ctrl Pts',(6.64140767441027,-1.31149113173566,-45.7592409259108));
#36694=CARTESIAN_POINT('Ctrl Pts',(6.67293975269618,-1.1243505044634,-45.7503140190339));
#36695=CARTESIAN_POINT('Ctrl Pts',(6.70384664831519,-0.940920291562845,
-45.7415641048499));
#36696=CARTESIAN_POINT('Ctrl Pts',(6.72718585889676,-0.756215114277056,
-45.7328141906659));
#36697=CARTESIAN_POINT('Ctrl Pts',(6.74287810451872,-0.570862389374271,
-45.7240642764819));
#36698=CARTESIAN_POINT('Ctrl Pts',(6.75857004154128,-0.385513309567318,
-45.7153145343713));
#36699=CARTESIAN_POINT('Ctrl Pts',(6.76661529035558,-0.199516993258512,
-45.7065647922607));
#36700=CARTESIAN_POINT('Ctrl Pts',(6.76698652348896,-0.013505218204444,
-45.6978150501501));
#36701=CARTESIAN_POINT('Ctrl Pts',(6.76735774981522,0.172503146038539,-45.6890654684795));
#36702=CARTESIAN_POINT('Ctrl Pts',(6.76005524147481,0.358526681833149,-45.6803158868089));
#36703=CARTESIAN_POINT('Ctrl Pts',(6.74510380214884,0.543933542114578,-45.6715663051382));
#36704=CARTESIAN_POINT('Ctrl Pts',(6.73015261710983,0.729337249084396,-45.6628168722763));
#36705=CARTESIAN_POINT('Ctrl Pts',(6.7075527844461,0.914124015854301,-45.6540674394144));
#36706=CARTESIAN_POINT('Ctrl Pts',(6.67738106408296,1.09766621749346,-45.6453180065524));
#36707=CARTESIAN_POINT('Ctrl Pts',(6.64720981677262,1.28120554143281,-45.6365687108701));
#36708=CARTESIAN_POINT('Ctrl Pts',(6.60946696581532,1.46350005650579,-45.6278194151877));
#36709=CARTESIAN_POINT('Ctrl Pts',(6.56428070011004,1.64393062206493,-45.6190701195054));
#36710=CARTESIAN_POINT('Ctrl Pts',(6.51909508282753,1.82435859844609,-45.6103209493754));
#36711=CARTESIAN_POINT('Ctrl Pts',(6.46646633415675,2.00292240086518,-45.6015717792454));
#36712=CARTESIAN_POINT('Ctrl Pts',(6.40657319597208,2.17901557696408,-45.5928226091154));
#36713=CARTESIAN_POINT('Ctrl Pts',(6.34668083768312,2.35510646007389,-45.5840735529124));
#36714=CARTESIAN_POINT('Ctrl Pts',(6.27952437143903,2.52872650996487,-45.5753244967093));
#36715=CARTESIAN_POINT('Ctrl Pts',(6.20533187335154,2.69928607997882,-45.5665754405062));
#36716=CARTESIAN_POINT('Ctrl Pts',(6.12831449784272,2.87633970115356,-45.5574932642173));
#36717=CARTESIAN_POINT('Ctrl Pts',(6.04371489463173,3.0500949056231,-45.5484110879285));
#36718=CARTESIAN_POINT('Ctrl Pts',(5.95184265120511,3.21991584599594,-45.5393289116397));
#36719=CARTESIAN_POINT('Ctrl Pts',(5.86333281335513,3.38352155905265,-45.5305791312852));
#36720=CARTESIAN_POINT('Ctrl Pts',(5.76807337235705,3.54347560903791,-45.5218293509308));
#36721=CARTESIAN_POINT('Ctrl Pts',(5.66638790086376,3.69923467178616,-45.5130795705764));
#36722=CARTESIAN_POINT('Ctrl Pts',(5.56470608502762,3.85498813489736,-45.5043301047821));
#36723=CARTESIAN_POINT('Ctrl Pts',(5.4565988576697,4.00654667256237,-45.4955806389879));
#36724=CARTESIAN_POINT('Ctrl Pts',(5.34243340580524,4.1533955150619,-45.4868311731936));
#36725=CARTESIAN_POINT('Ctrl Pts',(5.22827145140602,4.30023985883861,-45.4780819754397));
#36726=CARTESIAN_POINT('Ctrl Pts',(5.10805181978088,4.44237456993045,-45.4693327776858));
#36727=CARTESIAN_POINT('Ctrl Pts',(4.9821828128254,4.57931691626461,-45.460583579932));
#36728=CARTESIAN_POINT('Ctrl Pts',(4.85631699296224,4.71625579512166,-45.451834603714));
#36729=CARTESIAN_POINT('Ctrl Pts',(4.7248022779184,4.84800236135767,-45.443085627496));
#36730=CARTESIAN_POINT('Ctrl Pts',(4.58808530848123,4.974109186789,-45.434336651278));
#36731=CARTESIAN_POINT('Ctrl Pts',(4.45135945056974,5.10022421089005,-45.4255871062568));
#36732=CARTESIAN_POINT('Ctrl Pts',(4.30943087208039,5.22069856611988,-45.4168375612356));
#36733=CARTESIAN_POINT('Ctrl Pts',(4.16278164322461,5.33512305301689,-45.4080880162144));
#36734=CARTESIAN_POINT('Ctrl Pts',(4.01614103534387,5.44954081331429,-45.3993389855471));
#36735=CARTESIAN_POINT('Ctrl Pts',(3.86478055833414,5.55790924068337,-45.3905899548799));
#36736=CARTESIAN_POINT('Ctrl Pts',(3.70921425811957,5.65986029751287,-45.3818409242126));
#36737=CARTESIAN_POINT('Ctrl Pts',(3.55364584530133,5.76181273884646,-45.3730917747328));
#36738=CARTESIAN_POINT('Ctrl Pts',(3.39387173464365,5.85734747818051,-45.3643426252529));
#36739=CARTESIAN_POINT('Ctrl Pts',(3.23043456092434,5.94614005448792,-45.3555934757731));
#36740=CARTESIAN_POINT('Ctrl Pts',(3.1869076880641,5.96978744811272,-45.35326338704));
#36741=CARTESIAN_POINT('Ctrl Pts',(3.1431211498289,5.99295688499296,-45.350933298307));
#36742=CARTESIAN_POINT('Ctrl Pts',(3.09908550384718,6.01564277861014,-45.3486032095739));
#36743=CARTESIAN_POINT('Origin',(0.,0.,-63.6971797838103));
#36744=CARTESIAN_POINT('',(3.09908550384721,6.01564277861012,-42.9543661083715));
#36745=CARTESIAN_POINT('',(3.09908550384722,6.01564277861012,-43.3486032095739));
#36746=CARTESIAN_POINT('',(3.09908550384721,6.01564277861012,-63.6971797838103));
#36747=CARTESIAN_POINT('',(-6.76699974817481,-0.00184613164357677,-44.3028202161442));
#36748=CARTESIAN_POINT('Ctrl Pts',(-6.76699974817481,-0.00184613164357843,
-44.3028202161442));
#36749=CARTESIAN_POINT('Ctrl Pts',(-6.76694808985158,-0.191199833202375,
-44.2939578052881));
#36750=CARTESIAN_POINT('Ctrl Pts',(-6.75894451409944,-0.380318812548052,
-44.2850953944321));
#36751=CARTESIAN_POINT('Ctrl Pts',(-6.74307314779978,-0.568553887878346,
-44.276232983576));
#36752=CARTESIAN_POINT('Ctrl Pts',(-6.72716340080505,-0.75724415987488,
-44.2673491413269));
#36753=CARTESIAN_POINT('Ctrl Pts',(-6.70334785009519,-0.945046000564817,
-44.2584652990779));
#36754=CARTESIAN_POINT('Ctrl Pts',(-6.67176184369028,-1.13131909781393,
-44.2495814568288));
#36755=CARTESIAN_POINT('Ctrl Pts',(-6.64006191419913,-1.31826403707587,
-44.2406655727092));
#36756=CARTESIAN_POINT('Ctrl Pts',(-6.60053546746428,-1.50366894112442,
-44.2317496885897));
#36757=CARTESIAN_POINT('Ctrl Pts',(-6.55336891665049,-1.68690392206526,
-44.2228338044701));
#36758=CARTESIAN_POINT('Ctrl Pts',(-6.5061169547119,-1.87047071242522,-44.2139017751019));
#36759=CARTESIAN_POINT('Ctrl Pts',(-6.45119731553769,-2.05185948326789,
-44.2049697457337));
#36760=CARTESIAN_POINT('Ctrl Pts',(-6.38884548165277,-2.23045789280251,
-44.1960377163655));
#36761=CARTESIAN_POINT('Ctrl Pts',(-6.32631832791001,-2.40955848239852,
-44.1870805720645));
#36762=CARTESIAN_POINT('Ctrl Pts',(-6.25631725423912,-2.58585277136457,
-44.1781234277634));
#36763=CARTESIAN_POINT('Ctrl Pts',(-6.17912614081321,-2.75874774778681,
-44.1691662834624));
#36764=CARTESIAN_POINT('Ctrl Pts',(-6.12134972749879,-2.88815709524164,
-44.1624619926666));
#36765=CARTESIAN_POINT('Ctrl Pts',(-6.05954620669863,-3.01566253252796,
-44.1557577018709));
#36766=CARTESIAN_POINT('Ctrl Pts',(-5.99385085683238,-3.14102545453707,
-44.1490534110752));
#36767=CARTESIAN_POINT('Ctrl Pts',(-5.91476439462841,-3.29194191990997,
-44.1409825408888));
#36768=CARTESIAN_POINT('Ctrl Pts',(-5.82982994497036,-3.44014504877998,
-44.1329116707024));
#36769=CARTESIAN_POINT('Ctrl Pts',(-5.73925764505817,-3.58513747067549,
-44.124840800516));
#36770=CARTESIAN_POINT('Ctrl Pts',(-5.64879805533318,-3.72994946077196,
-44.1167799739002));
#36771=CARTESIAN_POINT('Ctrl Pts',(-5.55271477032055,-3.87155838153066,
-44.1087191472844));
#36772=CARTESIAN_POINT('Ctrl Pts',(-5.45126531353203,-4.00948818198565,
-44.1006583206686));
#36773=CARTESIAN_POINT('Ctrl Pts',(-5.34991985638948,-4.14727658542512,
-44.0926057575087));
#36774=CARTESIAN_POINT('Ctrl Pts',(-5.24321939394609,-4.28139307624674,
-44.0845531943488));
#36775=CARTESIAN_POINT('Ctrl Pts',(-5.13146649844571,-4.41138760202834,
-44.076500631189));
#36776=CARTESIAN_POINT('Ctrl Pts',(-5.01980369529258,-4.54127732952346,
-44.0684545598011));
#36777=CARTESIAN_POINT('Ctrl Pts',(-4.90309680799491,-4.6670514245402,-44.0604084884132));
#36778=CARTESIAN_POINT('Ctrl Pts',(-4.78169065075232,-4.78829025023628,
-44.0523624170253));
#36779=CARTESIAN_POINT('Ctrl Pts',(-4.66035581185737,-4.9094578558813,-44.0443210721894));
#36780=CARTESIAN_POINT('Ctrl Pts',(-4.53432746171645,-5.02609523294419,
-44.0362797273536));
#36781=CARTESIAN_POINT('Ctrl Pts',(-4.40398941018188,-5.13781726757636,
-44.0282383825177));
#36782=CARTESIAN_POINT('Ctrl Pts',(-4.27113884206445,-5.25169295926709,
-44.0200420252966));
#36783=CARTESIAN_POINT('Ctrl Pts',(-4.13381098147026,-5.36046157063303,
-44.0118456680756));
#36784=CARTESIAN_POINT('Ctrl Pts',(-3.99245053096405,-5.4637558288969,-44.0036493108545));
#36785=CARTESIAN_POINT('Ctrl Pts',(-3.85380762379097,-5.56506433639463,
-43.995610522146));
#36786=CARTESIAN_POINT('Ctrl Pts',(-3.71128609225324,-5.66110685131684,
-43.9875717334375));
#36787=CARTESIAN_POINT('Ctrl Pts',(-3.5653372671532,-5.75157884162676,-43.979532944729));
#36788=CARTESIAN_POINT('Ctrl Pts',(-3.41937282420635,-5.84206051325946,
-43.9714932957973));
#36789=CARTESIAN_POINT('Ctrl Pts',(-3.26998067483839,-5.92697027649108,
-43.9634536468655));
#36790=CARTESIAN_POINT('Ctrl Pts',(-3.11763911877259,-6.00604822866907,
-43.9554139979338));
#36791=CARTESIAN_POINT('Ctrl Pts',(-2.96525109657065,-6.08515030064068,
-43.9473718968056));
#36792=CARTESIAN_POINT('Ctrl Pts',(-2.80991220829138,-6.15841684894291,
-43.9393297956774));
#36793=CARTESIAN_POINT('Ctrl Pts',(-2.65212306967938,-6.22563508593898,
-43.9312876945493));
#36794=CARTESIAN_POINT('Ctrl Pts',(-2.48900916757461,-6.29512167434095,
-43.9229742041045));
#36795=CARTESIAN_POINT('Ctrl Pts',(-2.32327715088782,-6.35814442408832,
-43.9146607136597));
#36796=CARTESIAN_POINT('Ctrl Pts',(-2.15549868507928,-6.414523709413,-43.906347223215));
#36797=CARTESIAN_POINT('Ctrl Pts',(-1.99291134311829,-6.46915860012097,
-43.8982909550442));
#36798=CARTESIAN_POINT('Ctrl Pts',(-1.82840267569508,-6.51755497307224,
-43.8902346868735));
#36799=CARTESIAN_POINT('Ctrl Pts',(-1.66250426678463,-6.5596012502989,-43.8821784187027));
#36800=CARTESIAN_POINT('Ctrl Pts',(-1.48866059740945,-6.60366122148641,
-43.8737363171209));
#36801=CARTESIAN_POINT('Ctrl Pts',(-1.31329127299102,-6.64074779740795,
-43.8652942155392));
#36802=CARTESIAN_POINT('Ctrl Pts',(-1.13701442677451,-6.67079359546573,
-43.8568521139574));
#36803=CARTESIAN_POINT('Ctrl Pts',(-0.960737580557974,-6.70083939352352,
-43.8484100123757));
#36804=CARTESIAN_POINT('Ctrl Pts',(-0.783553680715682,-6.72384444012432,
-43.8399679107939));
#36805=CARTESIAN_POINT('Ctrl Pts',(-0.606080516427321,-6.73980381076536,
-43.8315258092121));
#36806=CARTESIAN_POINT('Ctrl Pts',(-0.430883212885349,-6.75555852339331,
-43.8231919665194));
#36807=CARTESIAN_POINT('Ctrl Pts',(-0.254847095583368,-6.76449787264988,
-43.8148581238268));
#36808=CARTESIAN_POINT('Ctrl Pts',(-0.0785367907614893,-6.76654424152365,
-43.8065242811341));
#36809=CARTESIAN_POINT('Ctrl Pts',(0.0975657100611083,-6.76858819849283,
-43.7982002609293));
#36810=CARTESIAN_POINT('Ctrl Pts',(0.273941409770814,-6.76375535531757,
-43.7898762407246));
#36811=CARTESIAN_POINT('Ctrl Pts',(0.450020024646737,-6.75201977021817,
-43.7815522205198));
#36812=CARTESIAN_POINT('Ctrl Pts',(0.625923392357247,-6.74029586528802,
-43.7732364850289));
#36813=CARTESIAN_POINT('Ctrl Pts',(0.801529919411688,-6.72168292904772,
-43.7649207495381));
#36814=CARTESIAN_POINT('Ctrl Pts',(0.976268551134108,-6.69620703951622,
-43.7566050140472));
#36815=CARTESIAN_POINT('Ctrl Pts',(1.15086528597577,-6.67075183773546,-43.7482960313672));
#36816=CARTESIAN_POINT('Ctrl Pts',(1.32459518710004,-6.63844483751473,-43.7399870486871));
#36817=CARTESIAN_POINT('Ctrl Pts',(1.49689132595528,-6.59936401165141,-43.7316780660071));
#36818=CARTESIAN_POINT('Ctrl Pts',(1.669079103131,-6.56030776477144,-43.72337430907));
#36819=CARTESIAN_POINT('Ctrl Pts',(1.83983457682786,-6.51448625918412,-43.7150705521328));
#36820=CARTESIAN_POINT('Ctrl Pts',(2.00859980708244,-6.46202876927892,-43.7067667951956));
#36821=CARTESIAN_POINT('Ctrl Pts',(2.17729652272206,-6.40959257584999,-43.6984664093836));
#36822=CARTESIAN_POINT('Ctrl Pts',(2.34400427328645,-6.3505258692829,-43.6901660235716));
#36823=CARTESIAN_POINT('Ctrl Pts',(2.50817882562078,-6.28500819241372,-43.6818656377596));
#36824=CARTESIAN_POINT('Ctrl Pts',(2.67231875781387,-6.21950433151781,-43.6735670022829));
#36825=CARTESIAN_POINT('Ctrl Pts',(2.83392623317169,-6.1475523392859,-43.6652683668063));
#36826=CARTESIAN_POINT('Ctrl Pts',(2.9924753714994,-6.06938054095882,-43.6569697313297));
#36827=CARTESIAN_POINT('Ctrl Pts',(3.15101739327636,-5.99121225140874,-43.6486714683411));
#36828=CARTESIAN_POINT('Ctrl Pts',(3.30650103974126,-5.90682486604122,-43.6403732053525));
#36829=CARTESIAN_POINT('Ctrl Pts',(3.45842331220062,-5.81649354797436,-43.6320749423639));
#36830=CARTESIAN_POINT('Ctrl Pts',(3.61036398179866,-5.72615129117047,-43.6237756744911));
#36831=CARTESIAN_POINT('Ctrl Pts',(3.75874211943104,-5.62986384565985,-43.6154764066183));
#36832=CARTESIAN_POINT('Ctrl Pts',(3.90308192686874,-5.52795083843467,-43.6071771387455));
#36833=CARTESIAN_POINT('Ctrl Pts',(4.0475230841156,-5.42596627185234,-43.598872043449));
#36834=CARTESIAN_POINT('Ctrl Pts',(4.18791996077287,-5.31834845149992,-43.5905669481525));
#36835=CARTESIAN_POINT('Ctrl Pts',(4.32382748084337,-5.2054591455417,-43.582261852856));
#36836=CARTESIAN_POINT('Ctrl Pts',(4.45978455986293,-5.09252867427223,-43.5739537290899));
#36837=CARTESIAN_POINT('Ctrl Pts',(4.59124875666223,-4.97432311395071,-43.5656456053238));
#36838=CARTESIAN_POINT('Ctrl Pts',(4.71781021000627,-4.85124270907575,-43.5573374815577));
#36839=CARTESIAN_POINT('Ctrl Pts',(4.84450619744388,-4.72803147044162,-43.549020526304));
#36840=CARTESIAN_POINT('Ctrl Pts',(4.96628878450176,-4.59993528176384,-43.5407035710503));
#36841=CARTESIAN_POINT('Ctrl Pts',(5.08278617928712,-4.46739002725841,-43.5323866157967));
#36842=CARTESIAN_POINT('Ctrl Pts',(5.16864298677856,-4.36970619131561,-43.5262571463141));
#36843=CARTESIAN_POINT('Ctrl Pts',(5.2516299655268,-4.2696065946261,-43.5201276768316));
#36844=CARTESIAN_POINT('Ctrl Pts',(5.33161298603271,-4.16727632479145,-43.5139982073491));
#36845=CARTESIAN_POINT('Ctrl Pts',(5.44188980360044,-4.02618817349592,-43.5055471838239));
#36846=CARTESIAN_POINT('Ctrl Pts',(5.54665617839165,-3.88060068047054,-43.4970961602988));
#36847=CARTESIAN_POINT('Ctrl Pts',(5.64554192698029,-3.73097110022413,-43.4886451367736));
#36848=CARTESIAN_POINT('Ctrl Pts',(5.74434060960638,-3.58147326437585,-43.4802015541234));
#36849=CARTESIAN_POINT('Ctrl Pts',(5.83726880428459,-3.42794071020951,-43.4717579714733));
#36850=CARTESIAN_POINT('Ctrl Pts',(5.9239978090905,-3.27086211233231,-43.4633143888231));
#36851=CARTESIAN_POINT('Ctrl Pts',(6.01066224145046,-3.1139004643647,-43.4548770926833));
#36852=CARTESIAN_POINT('Ctrl Pts',(6.09113652499687,-2.95339832492342,-43.4464397965435));
#36853=CARTESIAN_POINT('Ctrl Pts',(6.16513614727734,-2.78987191203006,-43.4380025004037));
#36854=CARTESIAN_POINT('Ctrl Pts',(6.23908297646957,-2.62646216276389,-43.4295712236313));
#36855=CARTESIAN_POINT('Ctrl Pts',(6.30656422178593,-2.46003274498916,-43.421139946859));
#36856=CARTESIAN_POINT('Ctrl Pts',(6.3673419701728,-2.29112313830488,-43.4127086700866));
#36857=CARTESIAN_POINT('Ctrl Pts',(6.42809366701662,-2.12228593239238,-43.4042810072647));
#36858=CARTESIAN_POINT('Ctrl Pts',(6.48214748308018,-1.95097096824125,-43.3958533444428));
#36859=CARTESIAN_POINT('Ctrl Pts',(6.52931393489892,-1.77773691516344,-43.3874256816209));
#36860=CARTESIAN_POINT('Ctrl Pts',(6.57646586701831,-1.60455619037872,-43.3790006131669));
#36861=CARTESIAN_POINT('Ctrl Pts',(6.61673457613478,-1.42945787428303,-43.3705755447129));
#36862=CARTESIAN_POINT('Ctrl Pts',(6.64998056898124,-1.25301533596841,-43.3621504762589));
#36863=CARTESIAN_POINT('Ctrl Pts',(6.65907769025789,-1.20473525671728,-43.3598451196452));
#36864=CARTESIAN_POINT('Ctrl Pts',(6.6676492868259,-1.15635460302723,-43.3575397630314));
#36865=CARTESIAN_POINT('Ctrl Pts',(6.6756931643768,-1.10788527162916,-43.3552344064176));
#36866=CARTESIAN_POINT('Ctrl Pts',(6.70576664103086,-0.9266739967168,-43.3466154178931));
#36867=CARTESIAN_POINT('Ctrl Pts',(6.72844643978489,-0.74430347567481,-43.3379964293687));
#36868=CARTESIAN_POINT('Ctrl Pts',(6.74367356783639,-0.561387397850085,
-43.3293774408442));
#36869=CARTESIAN_POINT('Ctrl Pts',(6.75890981829649,-0.378361736970917,
-43.3207532887764));
#36870=CARTESIAN_POINT('Ctrl Pts',(6.76668446241367,-0.194790170145841,
-43.3121291367086));
#36871=CARTESIAN_POINT('Ctrl Pts',(6.76699058382844,-0.0112888607616132,
-43.3035049846408));
#36872=CARTESIAN_POINT('Ctrl Pts',(6.76730718998401,0.178497417835661,-43.2945854530446));
#36873=CARTESIAN_POINT('Ctrl Pts',(6.75963462531111,0.368208183191211,-43.2856659214484));
#36874=CARTESIAN_POINT('Ctrl Pts',(6.74402370307352,0.557165408458398,-43.2767463898521));
#36875=CARTESIAN_POINT('Ctrl Pts',(6.72890163442433,0.74020546776821,-43.2681061719929));
#36876=CARTESIAN_POINT('Ctrl Pts',(6.70633094418731,0.922538170032766,-43.2594659541336));
#36877=CARTESIAN_POINT('Ctrl Pts',(6.67641033196807,1.10355519988358,-43.2508257362744));
#36878=CARTESIAN_POINT('Ctrl Pts',(6.64503884695588,1.29334988046378,-43.2417665478096));
#36879=CARTESIAN_POINT('Ctrl Pts',(6.60558699184346,1.48169774089452,-43.2327073593449));
#36880=CARTESIAN_POINT('Ctrl Pts',(6.5582282408616,1.66791227010457,-43.2236481708802));
#36881=CARTESIAN_POINT('Ctrl Pts',(6.51086948987974,1.85412679931461,-43.2145889824155));
#36882=CARTESIAN_POINT('Ctrl Pts',(6.45560398477864,2.03820764036222,-43.2055297939508));
#36883=CARTESIAN_POINT('Ctrl Pts',(6.39266447184202,2.21948866869125,-43.1964706054861));
#36884=CARTESIAN_POINT('Ctrl Pts',(6.32983399719578,2.4004556403572,-43.1874271114298));
#36885=CARTESIAN_POINT('Ctrl Pts',(6.25929899903813,2.57879948537713,-43.1783836173735));
#36886=CARTESIAN_POINT('Ctrl Pts',(6.18129258247601,2.75389015936132,-43.1693401233172));
#36887=CARTESIAN_POINT('Ctrl Pts',(6.10335751809788,2.92882067854624,-43.1603049013119));
#36888=CARTESIAN_POINT('Ctrl Pts',(6.01796477638797,3.10050375032539,-43.1512696793065));
#36889=CARTESIAN_POINT('Ctrl Pts',(5.92539546120855,3.26832948588252,-43.1422344573012));
#36890=CARTESIAN_POINT('Ctrl Pts',(5.83298923301035,3.43585954902888,-43.1332151533901));
#36891=CARTESIAN_POINT('Ctrl Pts',(5.73343179380139,3.59954563808829,-43.124195849479));
#36892=CARTESIAN_POINT('Ctrl Pts',(5.62704991926297,3.75880276233305,-43.1151765455679));
#36893=CARTESIAN_POINT('Ctrl Pts',(5.52080150821676,3.91786008739161,-43.1061685570035));
#36894=CARTESIAN_POINT('Ctrl Pts',(5.40774587996794,4.07249933900003,-43.0971605684391));
#36895=CARTESIAN_POINT('Ctrl Pts',(5.28825414611462,4.2221626077286,-43.0881525798747));
#36896=CARTESIAN_POINT('Ctrl Pts',(5.16903228852759,4.37148785672257,-43.0791649361681));
#36897=CARTESIAN_POINT('Ctrl Pts',(5.04340348913918,4.5158593700586,-43.0701772924614));
#36898=CARTESIAN_POINT('Ctrl Pts',(4.91178000762963,4.65475092315903,-43.0611896487547));
#36899=CARTESIAN_POINT('Ctrl Pts',(4.7971450780809,4.77571583931213,-43.0533620340213));
#36900=CARTESIAN_POINT('Ctrl Pts',(4.67796377580275,4.89252443596965,-43.0455344192879));
#36901=CARTESIAN_POINT('Ctrl Pts',(4.55453438253712,5.00484820531924,-43.0377068045545));
#36902=CARTESIAN_POINT('Ctrl Pts',(4.42644270366481,5.12141476870089,-43.0295835181457));
#36903=CARTESIAN_POINT('Ctrl Pts',(4.2938320800799,5.23309795129149,-43.0214602317368));
#36904=CARTESIAN_POINT('Ctrl Pts',(4.15712023609244,5.33953559241538,-43.013336945328));
#36905=CARTESIAN_POINT('Ctrl Pts',(4.02042557568307,5.44595985518475,-43.0052146799509));
#36906=CARTESIAN_POINT('Ctrl Pts',(3.8796310125444,5.54713966762463,-42.9970924145737));
#36907=CARTESIAN_POINT('Ctrl Pts',(3.73518650007377,5.64275383209889,-42.9889701491966));
#36908=CARTESIAN_POINT('Ctrl Pts',(3.59070430238548,5.73839294207324,-42.9808457647404));
#36909=CARTESIAN_POINT('Ctrl Pts',(3.44257055979513,5.82846330339839,-42.9727213802842));
#36910=CARTESIAN_POINT('Ctrl Pts',(3.29126351222216,5.91268750173008,-42.9645969958281));
#36911=CARTESIAN_POINT('Ctrl Pts',(3.22775078772149,5.94804149475773,-42.9611867000092));
#36912=CARTESIAN_POINT('Ctrl Pts',(3.16367924124438,5.98236594975342,-42.9577764041903));
#36913=CARTESIAN_POINT('Ctrl Pts',(3.09908550384721,6.01564277861012,-42.9543661083715));
#36914=CARTESIAN_POINT('Ctrl Pts',(3.0990855038472,6.01564277861013,-44.9542932404068));
#36915=CARTESIAN_POINT('Ctrl Pts',(2.93974035442061,6.09773279972179,-44.9458699638642));
#36916=CARTESIAN_POINT('Ctrl Pts',(2.77713243321382,6.17348729536887,-44.9374466873216));
#36917=CARTESIAN_POINT('Ctrl Pts',(2.61179635165935,6.24266039581354,-44.929023410779));
#36918=CARTESIAN_POINT('Ctrl Pts',(2.44643549540071,6.31184386146758,-44.9205988720547));
#36919=CARTESIAN_POINT('Ctrl Pts',(2.27834597141802,6.37444383702415,-44.9121743333303));
#36920=CARTESIAN_POINT('Ctrl Pts',(2.10808193716495,6.43026278982429,-44.903749794606));
#36921=CARTESIAN_POINT('Ctrl Pts',(1.93776863827557,6.4860978934247,-44.8953228183038));
#36922=CARTESIAN_POINT('Ctrl Pts',(1.76527989151013,6.53514795865822,-44.8868958420016));
#36923=CARTESIAN_POINT('Ctrl Pts',(1.59118491255707,6.57726535682199,-44.8784688656995));
#36924=CARTESIAN_POINT('Ctrl Pts',(1.41693492337219,6.61942025536454,-44.8700343862082));
#36925=CARTESIAN_POINT('Ctrl Pts',(1.24107616860051,6.65463007328726,-44.8615999067169));
#36926=CARTESIAN_POINT('Ctrl Pts',(1.06418911290291,6.68279810648047,-44.8531654272256));
#36927=CARTESIAN_POINT('Ctrl Pts',(0.887220494001733,6.71097912804649,-44.8447270585681));
#36928=CARTESIAN_POINT('Ctrl Pts',(0.709222958974084,6.73211184457387,-44.8362886899105));
#36929=CARTESIAN_POINT('Ctrl Pts',(0.53078253786795,6.74615141376878,-44.827850321253));
#36930=CARTESIAN_POINT('Ctrl Pts',(0.352136780759709,6.76020713865864,-44.8194022423467));
#36931=CARTESIAN_POINT('Ctrl Pts',(0.173047452317599,6.76715338594818,-44.8109541634403));
#36932=CARTESIAN_POINT('Ctrl Pts',(-0.00589763809075682,6.76699743001761,
-44.802506084534));
#36933=CARTESIAN_POINT('Ctrl Pts',(-0.135794502656443,6.76688422106427,
-44.7963735946231));
#36934=CARTESIAN_POINT('Ctrl Pts',(-0.265615351294428,6.76302969989654,
-44.7902411047122));
#36935=CARTESIAN_POINT('Ctrl Pts',(-0.395136940195535,6.75545378183383,
-44.7841086148013));
#36936=CARTESIAN_POINT('Ctrl Pts',(-0.569186692347734,6.74527334263192,
-44.7758678392045));
#36937=CARTESIAN_POINT('Ctrl Pts',(-0.743083056888376,6.72834813911043,
-44.7676270636077));
#36938=CARTESIAN_POINT('Ctrl Pts',(-0.916264977606776,6.70468101335263,
-44.759386288011));
#36939=CARTESIAN_POINT('Ctrl Pts',(-1.08925508057305,6.6810401015024,-44.7511546399666));
#36940=CARTESIAN_POINT('Ctrl Pts',(-1.26153196597617,6.65067218414367,-44.7429229919222));
#36941=CARTESIAN_POINT('Ctrl Pts',(-1.43253615344517,6.61363207088756,-44.7346913438778));
#36942=CARTESIAN_POINT('Ctrl Pts',(-1.6033814097802,6.57662638267853,-44.7264673463195));
#36943=CARTESIAN_POINT('Ctrl Pts',(-1.77295597817241,6.53296092320099,-44.7182433487612));
#36944=CARTESIAN_POINT('Ctrl Pts',(-1.94070697447512,6.48274212345545,-44.7100193512029));
#36945=CARTESIAN_POINT('Ctrl Pts',(-2.10830976212087,6.43256769221458,-44.7018026195784));
#36946=CARTESIAN_POINT('Ctrl Pts',(-2.274091849296,6.37585156223714,-44.6935858879539));
#36947=CARTESIAN_POINT('Ctrl Pts',(-2.4375121244189,6.31275087765317,-44.6853691563294));
#36948=CARTESIAN_POINT('Ctrl Pts',(-2.60084867328491,6.24968252188596,-44.6771566344407));
#36949=CARTESIAN_POINT('Ctrl Pts',(-2.76182548894159,6.18023625398197,-44.668944112552));
#36950=CARTESIAN_POINT('Ctrl Pts',(-2.91991776853191,6.10461867973845,-44.6607315906633));
#36951=CARTESIAN_POINT('Ctrl Pts',(-3.07795718130282,6.02902639237581,-44.6525218150815));
#36952=CARTESIAN_POINT('Ctrl Pts',(-3.2331136590022,5.94726706318852,-44.6443120394996));
#36953=CARTESIAN_POINT('Ctrl Pts',(-3.38488341245071,5.85959497611533,-44.6361022639178));
#36954=CARTESIAN_POINT('Ctrl Pts',(-3.45117249775066,5.82130208621886,-44.6325164472351));
#36955=CARTESIAN_POINT('Ctrl Pts',(-3.51681578541824,5.78188181406435,-44.6289306305525));
#36956=CARTESIAN_POINT('Ctrl Pts',(-3.58177276483859,5.74135810249287,-44.6253448138698));
#36957=CARTESIAN_POINT('Ctrl Pts',(-3.74224821092904,5.6412447544015,-44.6164860963481));
#36958=CARTESIAN_POINT('Ctrl Pts',(-3.89836685099313,5.53449769543603,-44.6076273788264));
#36959=CARTESIAN_POINT('Ctrl Pts',(-4.04961600148761,5.42152185649892,-44.5987686613047));
#36960=CARTESIAN_POINT('Ctrl Pts',(-4.20114811485178,5.30833465791128,-44.5898933705452));
#36961=CARTESIAN_POINT('Ctrl Pts',(-4.34779232508549,5.18889554673532,-44.5810180797858));
#36962=CARTESIAN_POINT('Ctrl Pts',(-4.48906995450461,5.06364887640958,-44.5721427890263));
#36963=CARTESIAN_POINT('Ctrl Pts',(-4.63074884415681,4.93804647737905,-44.5632422904455));
#36964=CARTESIAN_POINT('Ctrl Pts',(-4.76703045601414,4.8066036842549,-44.5543417918647));
#36965=CARTESIAN_POINT('Ctrl Pts',(-4.89747169536168,4.66980299296782,-44.545441293284));
#36966=CARTESIAN_POINT('Ctrl Pts',(-5.02808951319042,4.5328171144009,-44.5365287460863));
#36967=CARTESIAN_POINT('Ctrl Pts',(-5.15285099136919,4.3904590415754,-44.5276161988886));
#36968=CARTESIAN_POINT('Ctrl Pts',(-5.2713532987551,4.24324444260565,-44.5187036516909));
#36969=CARTESIAN_POINT('Ctrl Pts',(-5.39011727080803,4.09570477942518,-44.5097714247187));
#36970=CARTESIAN_POINT('Ctrl Pts',(-5.50259426477459,3.94328734380879,-44.5008391977464));
#36971=CARTESIAN_POINT('Ctrl Pts',(-5.60842310688594,3.78653921862007,-44.4919069707742));
#36972=CARTESIAN_POINT('Ctrl Pts',(-5.70844358335701,3.63839413969322,-44.4834649848289));
#36973=CARTESIAN_POINT('Ctrl Pts',(-5.80252592468991,3.48638109405627,-44.4750229988836));
#36974=CARTESIAN_POINT('Ctrl Pts',(-5.89040300023832,3.33098206161237,-44.4665810129382));
#36975=CARTESIAN_POINT('Ctrl Pts',(-5.97776970194635,3.17648555807587,-44.4581880564897));
#36976=CARTESIAN_POINT('Ctrl Pts',(-6.0591653667354,3.01835334963305,-44.4497951000411));
#36977=CARTESIAN_POINT('Ctrl Pts',(-6.13428132641641,2.85707570924869,-44.4414021435925));
#36978=CARTESIAN_POINT('Ctrl Pts',(-6.20930249335219,2.69600159352597,-44.4330197786532));
#36979=CARTESIAN_POINT('Ctrl Pts',(-6.27805960196019,2.53179025805266,-44.4246374137138));
#36980=CARTESIAN_POINT('Ctrl Pts',(-6.34028864572777,2.36495853850665,-44.4162550487745));
#36981=CARTESIAN_POINT('Ctrl Pts',(-6.40244851017053,2.1983122838982,-44.4078820024156));
#36982=CARTESIAN_POINT('Ctrl Pts',(-6.45809465261197,2.02905176457662,-44.3995089560566));
#36983=CARTESIAN_POINT('Ctrl Pts',(-6.50701004128297,1.85771615771696,-44.3911359096977));
#36984=CARTESIAN_POINT('Ctrl Pts',(-6.55586542985441,1.6865907128073,-44.3827731338002));
#36985=CARTESIAN_POINT('Ctrl Pts',(-6.59800643617382,1.51339557994791,-44.3744103579028));
#36986=CARTESIAN_POINT('Ctrl Pts',(-6.63326503441398,1.33868741057084,-44.3660475820053));
#36987=CARTESIAN_POINT('Ctrl Pts',(-6.66849827503971,1.16410488947872,-44.3576908205287));
#36988=CARTESIAN_POINT('Ctrl Pts',(-6.69685890240044,0.988011830130503,
-44.349334059052));
#36989=CARTESIAN_POINT('Ctrl Pts',(-6.71822916313347,0.810978366926595,
-44.3409772975753));
#36990=CARTESIAN_POINT('Ctrl Pts',(-6.7395845623884,0.634068017753489,-44.3326263476248));
#36991=CARTESIAN_POINT('Ctrl Pts',(-6.75395924728334,0.456218903690333,
-44.3242753976742));
#36992=CARTESIAN_POINT('Ctrl Pts',(-6.76128682932984,0.278009732798816,
-44.3159244477236));
#36993=CARTESIAN_POINT('Ctrl Pts',(-6.76511962010167,0.184795018679802,
-44.3115563705457));
#36994=CARTESIAN_POINT('Ctrl Pts',(-6.76702520935342,0.0914819259722868,
-44.3071882933678));
#36995=CARTESIAN_POINT('Ctrl Pts',(-6.76699974817508,-0.00184613066680469,
-44.3028202161899));
#36996=CARTESIAN_POINT('',(-6.767,6.6187019857333E-10,-44.6971797838412));
#36997=CARTESIAN_POINT('Ctrl Pts',(3.09908550384718,6.01564277861014,-45.3486032095739));
#36998=CARTESIAN_POINT('Ctrl Pts',(2.93373232018329,6.1008279655248,-45.3398537616746));
#36999=CARTESIAN_POINT('Ctrl Pts',(2.76486502144428,6.1791915818019,-45.3311043137754));
#37000=CARTESIAN_POINT('Ctrl Pts',(2.59305716434355,6.25046746591378,-45.3223548658761));
#37001=CARTESIAN_POINT('Ctrl Pts',(2.42125069459284,6.32174277447224,-45.3136054886287));
#37002=CARTESIAN_POINT('Ctrl Pts',(2.24650397871058,6.38593035557826,-45.3048561113812));
#37003=CARTESIAN_POINT('Ctrl Pts',(2.06941053323769,6.44281220003539,-45.2961067341338));
#37004=CARTESIAN_POINT('Ctrl Pts',(1.89231845896685,6.49969360406685,-45.2873574246312));
#37005=CARTESIAN_POINT('Ctrl Pts',(1.71287996431511,6.54926929700879,-45.2786081151286));
#37006=CARTESIAN_POINT('Ctrl Pts',(1.53170449173514,6.59137090065477,-45.269858805626));
#37007=CARTESIAN_POINT('Ctrl Pts',(1.35053036178178,6.63347219230082,-45.2611095609615));
#37008=CARTESIAN_POINT('Ctrl Pts',(1.1676195587885,6.66809944062453,-45.2523603162969));
#37009=CARTESIAN_POINT('Ctrl Pts',(0.983593309310526,6.69513503985391,-45.2436110716323));
#37010=CARTESIAN_POINT('Ctrl Pts',(0.799568362459917,6.72217044771215,-45.2348618888991));
#37011=CARTESIAN_POINT('Ctrl Pts',(0.614428268438427,6.74161427235979,-45.2261127061659));
#37012=CARTESIAN_POINT('Ctrl Pts',(0.428801816329997,6.75340047696804,-45.2173635234327));
#37013=CARTESIAN_POINT('Ctrl Pts',(0.243176616522541,6.76518660206243,-45.2086143997246));
#37014=CARTESIAN_POINT('Ctrl Pts',(0.0570653511652483,6.76931519233997,
-45.1998652760165));
#37015=CARTESIAN_POINT('Ctrl Pts',(-0.128899900800212,6.76577222610795,
-45.1911161523083));
#37016=CARTESIAN_POINT('Ctrl Pts',(-0.314863959942268,6.76222928260132,
-45.1823670847191));
#37017=CARTESIAN_POINT('Ctrl Pts',(-0.500681721080991,6.75101488651274,
-45.1736180171298));
#37018=CARTESIAN_POINT('Ctrl Pts',(-0.685722110173672,6.73216712415987,
-45.1648689495405));
#37019=CARTESIAN_POINT('Ctrl Pts',(-0.870761373827983,6.7133194764414,-45.1561199351642));
#37020=CARTESIAN_POINT('Ctrl Pts',(-1.0550229898438,6.6868385843999,-45.1473709207878));
#37021=CARTESIAN_POINT('Ctrl Pts',(-1.23788117676096,6.65281438131419,-45.1386219064115));
#37022=CARTESIAN_POINT('Ctrl Pts',(-1.43009641450478,6.61704912302621,-45.1294251955246));
#37023=CARTESIAN_POINT('Ctrl Pts',(-1.62076048990051,6.57294837083776,-45.1202284846377));
#37024=CARTESIAN_POINT('Ctrl Pts',(-1.80915798957194,6.52067760043142,-45.1110317737508));
#37025=CARTESIAN_POINT('Ctrl Pts',(-1.98840442999105,6.4709457857861,-45.1022817760443));
#37026=CARTESIAN_POINT('Ctrl Pts',(-2.16559895948318,6.41381888475783,-45.0935317783378));
#37027=CARTESIAN_POINT('Ctrl Pts',(-2.34013966238487,6.34949095286648,-45.0847817806313));
#37028=CARTESIAN_POINT('Ctrl Pts',(-2.51467682550215,6.28516432558205,-45.0760319603797));
#37029=CARTESIAN_POINT('Ctrl Pts',(-2.68656000075082,6.21363705881287,-45.0672821401281));
#37030=CARTESIAN_POINT('Ctrl Pts',(-2.85520533837172,6.13515211512589,-45.0585323198765));
#37031=CARTESIAN_POINT('Ctrl Pts',(-3.02384747994653,6.05666865882956,-45.0497826654453));
#37032=CARTESIAN_POINT('Ctrl Pts',(-3.18925164680909,5.97122791041781,-45.041033011014));
#37033=CARTESIAN_POINT('Ctrl Pts',(-3.35085601825581,5.87912008253947,-45.0322833565828));
#37034=CARTESIAN_POINT('Ctrl Pts',(-3.51245754187895,5.78701387780312,-45.0235338563396));
#37035=CARTESIAN_POINT('Ctrl Pts',(-3.67025915507472,5.68824097063218,-45.0147843560965));
#37036=CARTESIAN_POINT('Ctrl Pts',(-3.82372487925432,5.58313684659185,-45.0060348558534));
#37037=CARTESIAN_POINT('Ctrl Pts',(-3.97718810297457,5.47803443504199,-44.9972854981682));
#37038=CARTESIAN_POINT('Ctrl Pts',(-4.12631534259748,5.36660117498896,-44.9885361404831));
#37039=CARTESIAN_POINT('Ctrl Pts',(-4.27060009883016,5.24921554099961,-44.979786782798));
#37040=CARTESIAN_POINT('Ctrl Pts',(-4.41488269591073,5.13183166362993,-44.9710375560428));
#37041=CARTESIAN_POINT('Ctrl Pts',(-4.5543227323202,5.00849577142261,-44.9622883292877));
#37042=CARTESIAN_POINT('Ctrl Pts',(-4.68844662477214,4.87962675280218,-44.9535391025325));
#37043=CARTESIAN_POINT('Ctrl Pts',(-4.82256868832243,4.7507594914284,-44.944789995081));
#37044=CARTESIAN_POINT('Ctrl Pts',(-4.95137454635029,4.61635945315564,-44.9360408876295));
#37045=CARTESIAN_POINT('Ctrl Pts',(-5.07442674458329,4.47688309137706,-44.927291780178));
#37046=CARTESIAN_POINT('Ctrl Pts',(-5.19747742835866,4.33740844619554,-44.9185427804056));
#37047=CARTESIAN_POINT('Ctrl Pts',(-5.31477440448334,4.19285781739315,-44.9097937806333));
#37048=CARTESIAN_POINT('Ctrl Pts',(-5.42591931528644,4.04372212002773,-44.9010447808609));
#37049=CARTESIAN_POINT('Ctrl Pts',(-5.53707636460566,3.89457013504235,-44.8922948255803));
#37050=CARTESIAN_POINT('Ctrl Pts',(-5.64207983271152,3.74083230919918,-44.8835448702997));
#37051=CARTESIAN_POINT('Ctrl Pts',(-5.74057303466527,3.58303087255384,-44.8747949150192));
#37052=CARTESIAN_POINT('Ctrl Pts',(-5.83906243361643,3.42523552891048,-44.8660452975904));
#37053=CARTESIAN_POINT('Ctrl Pts',(-5.93104191766405,3.26337713160666,-44.8572956801615));
#37054=CARTESIAN_POINT('Ctrl Pts',(-6.01619906697738,3.09800545294881,-44.8485460627327));
#37055=CARTESIAN_POINT('Ctrl Pts',(-6.10135338093573,2.93263928043362,-44.8397967366273));
#37056=CARTESIAN_POINT('Ctrl Pts',(-6.17968568351138,2.76376031544027,-44.831047410522));
#37057=CARTESIAN_POINT('Ctrl Pts',(-6.25092992693296,2.59194213835376,-44.8222980844166));
#37058=CARTESIAN_POINT('Ctrl Pts',(-6.32217217689611,2.42012876884716,-44.8135490031228));
#37059=CARTESIAN_POINT('Ctrl Pts',(-6.38632665482459,2.24537661651625,-44.804799921829));
#37060=CARTESIAN_POINT('Ctrl Pts',(-6.44317547868063,2.06827917625466,-44.7960508405352));
#37061=CARTESIAN_POINT('Ctrl Pts',(-6.50002944234756,1.8911657242748,-44.7873009682202));
#37062=CARTESIAN_POINT('Ctrl Pts',(-6.54957634249327,1.71170683293297,-44.7785510959053));
#37063=CARTESIAN_POINT('Ctrl Pts',(-6.59164787707435,1.53051209229501,-44.7698012235903));
#37064=CARTESIAN_POINT('Ctrl Pts',(-6.63371649074161,1.34932993152199,-44.7610519587555));
#37065=CARTESIAN_POINT('Ctrl Pts',(-6.6683107125639,1.16641244178201,-44.7523026939207));
#37066=CARTESIAN_POINT('Ctrl Pts',(-6.69531304839714,0.982380875202212,
-44.7435534290859));
#37067=CARTESIAN_POINT('Ctrl Pts',(-6.72231677032539,0.798339861838338,
-44.7348037151303));
#37068=CARTESIAN_POINT('Ctrl Pts',(-6.74172778477501,0.613184940772896,
-44.7260540011747));
#37069=CARTESIAN_POINT('Ctrl Pts',(-6.75348015835246,0.427545027733496,
-44.717304287219));
#37070=CARTESIAN_POINT('Ctrl Pts',(-6.76249038363737,0.28521995379571,-44.7105961194264));
#37071=CARTESIAN_POINT('Ctrl Pts',(-6.76699999998605,0.142609996212931,
-44.7038879516338));
#37072=CARTESIAN_POINT('Ctrl Pts',(-6.767,6.61843980926672E-10,-44.6971797838412));
#37073=CARTESIAN_POINT('Ctrl Pts',(-6.767,6.63875942265778E-13,-44.6971797838101));
#37074=CARTESIAN_POINT('Ctrl Pts',(-6.76700000000002,-0.18600724955928,
-44.6884302719974));
#37075=CARTESIAN_POINT('Ctrl Pts',(-6.75932637294251,-0.372014355815401,
-44.6796807601846));
#37076=CARTESIAN_POINT('Ctrl Pts',(-6.74400518263369,-0.557389537585713,
-44.6709312483719));
#37077=CARTESIAN_POINT('Ctrl Pts',(-6.72868405703734,-0.742763936382393,
-44.6621817735147));
#37078=CARTESIAN_POINT('Ctrl Pts',(-6.70571545643566,-0.927506130404909,
-44.6534322986575));
#37079=CARTESIAN_POINT('Ctrl Pts',(-6.67517739401572,-1.11098864009563,
-44.6446828238003));
#37080=CARTESIAN_POINT('Ctrl Pts',(-6.64463945804385,-1.29447039004561,
-44.6359333851717));
#37081=CARTESIAN_POINT('Ctrl Pts',(-6.60653217002719,-1.47669218339299,
-44.6271839465432));
#37082=CARTESIAN_POINT('Ctrl Pts',(-6.56098496085474,-1.65703510627806,
-44.6184345079147));
#37083=CARTESIAN_POINT('Ctrl Pts',(-6.51543793649547,-1.83737729740041,
-44.6096851047881));
#37084=CARTESIAN_POINT('Ctrl Pts',(-6.46245112156884,-2.01584035544993,
-44.6009357016614));
#37085=CARTESIAN_POINT('Ctrl Pts',(-6.402204483617,-2.19181813797458,-44.5921862985348));
#37086=CARTESIAN_POINT('Ctrl Pts',(-6.34195808511952,-2.3677952210636,-44.5834369301833));
#37087=CARTESIAN_POINT('Ctrl Pts',(-6.27445201416329,-2.54128677725807,
-44.5746875618317));
#37088=CARTESIAN_POINT('Ctrl Pts',(-6.19991555052694,-2.71170355428728,
-44.5659381934802));
#37089=CARTESIAN_POINT('Ctrl Pts',(-6.12537937695079,-2.88211966813606,
-44.557188859177));
#37090=CARTESIAN_POINT('Ctrl Pts',(-6.04381298028296,-3.04946076419978,
-44.5484395248738));
#37091=CARTESIAN_POINT('Ctrl Pts',(-5.95549339308811,-3.21315848424629,
-44.5396901905706));
#37092=CARTESIAN_POINT('Ctrl Pts',(-5.86717414225626,-3.37685558085401,
-44.5309408895891));
#37093=CARTESIAN_POINT('Ctrl Pts',(-5.77210188843871,-3.5369090770032,-44.5221915886075));
#37094=CARTESIAN_POINT('Ctrl Pts',(-5.67059953311163,-3.69277537024311,
-44.513442287626));
#37095=CARTESIAN_POINT('Ctrl Pts',(-5.56909755592481,-3.84864108281355,
-44.5046930192393));
#37096=CARTESIAN_POINT('Ctrl Pts',(-5.46116568154721,-4.00031938355164,
-44.4959437508527));
#37097=CARTESIAN_POINT('Ctrl Pts',(-5.34717048488112,-4.14729511918505,
-44.4871944824661));
#37098=CARTESIAN_POINT('Ctrl Pts',(-5.2331757034303,-4.29427031947514,-44.4784452459477));
#37099=CARTESIAN_POINT('Ctrl Pts',(-5.11311781951263,-4.43654276249883,
-44.4696960094294));
#37100=CARTESIAN_POINT('Ctrl Pts',(-4.98740458928951,-4.57362924412703,
-44.460946772911));
#37101=CARTESIAN_POINT('Ctrl Pts',(-4.86169180652435,-4.71071523781583,
-44.4521975675343));
#37102=CARTESIAN_POINT('Ctrl Pts',(-4.73032391141256,-4.84261509584798,
-44.4434483621576));
#37103=CARTESIAN_POINT('Ctrl Pts',(-4.59374706947,-4.96888084599901,-44.4346991567809));
#37104=CARTESIAN_POINT('Ctrl Pts',(-4.45717070231214,-5.09514615720998,
-44.4259499818192));
#37105=CARTESIAN_POINT('Ctrl Pts',(-4.31538563497104,-5.21577720520795,
-44.4172008068575));
#37106=CARTESIAN_POINT('Ctrl Pts',(-4.16887340951821,-5.33036429293646,
-44.4084516318958));
#37107=CARTESIAN_POINT('Ctrl Pts',(-4.0223616812229,-5.4449509918385,-44.3997024866226));
#37108=CARTESIAN_POINT('Ctrl Pts',(-3.87112305262978,-5.5534935949807,-44.3909533413493));
#37109=CARTESIAN_POINT('Ctrl Pts',(-3.71567116928783,-5.65562346357351,
-44.3822041960761));
#37110=CARTESIAN_POINT('Ctrl Pts',(-3.56021980053102,-5.75775299409056,
-44.3734550797647));
#37111=CARTESIAN_POINT('Ctrl Pts',(-3.40055544441879,-5.85346967519998,
-44.3647059634533));
#37112=CARTESIAN_POINT('Ctrl Pts',(-3.23722035886642,-5.94244843041492,
-44.355956847142));
#37113=CARTESIAN_POINT('Ctrl Pts',(-3.07388580043271,-6.03142689847563,
-44.347207759066));
#37114=CARTESIAN_POINT('Ctrl Pts',(-2.90688078788986,-6.11366734708015,
-44.3384586709899));
#37115=CARTESIAN_POINT('Ctrl Pts',(-2.73677250610137,-6.18889047001541,
-44.3297095829139));
#37116=CARTESIAN_POINT('Ctrl Pts',(-2.56666475916652,-6.26411335643451,
-44.3209605223467));
#37117=CARTESIAN_POINT('Ctrl Pts',(-2.39345402456782,-6.33231884545374,
-44.3122114617796));
#37118=CARTESIAN_POINT('Ctrl Pts',(-2.21772855943726,-6.39327529805,-44.3034624012124));
#37119=CARTESIAN_POINT('Ctrl Pts',(-2.04200363223274,-6.45423156404802,
-44.2947133674276));
#37120=CARTESIAN_POINT('Ctrl Pts',(-1.8637642606074,-6.50793874412536,-44.2859643336428));
#37121=CARTESIAN_POINT('Ctrl Pts',(-1.68361577621418,-6.55421443943382,
-44.277215299858));
#37122=CARTESIAN_POINT('Ctrl Pts',(-1.50346782832924,-6.60048999692654,
-44.2684662921291));
#37123=CARTESIAN_POINT('Ctrl Pts',(-1.32141105657075,-6.63933404265224,
-44.2597172844002));
#37124=CARTESIAN_POINT('Ctrl Pts',(-1.13806375346203,-6.67061465631586,
-44.2509682766713));
#37125=CARTESIAN_POINT('Ctrl Pts',(-0.954716981166183,-6.70189517941827,
-44.2422192942718));
#37126=CARTESIAN_POINT('Ctrl Pts',(-0.770079967437952,-6.72561226609055,
-44.2334703118724));
#37127=CARTESIAN_POINT('Ctrl Pts',(-0.584779764068238,-6.74168536996027,
-44.2247213294729));
#37128=CARTESIAN_POINT('Ctrl Pts',(-0.391489587588108,-6.75845153117901,
-44.2155950990573));
#37129=CARTESIAN_POINT('Ctrl Pts',(-0.197478091800382,-6.76689985146408,
-44.2064688686417));
#37130=CARTESIAN_POINT('Ctrl Pts',(-0.00346214752617278,-6.76699911434415,
-44.1973426382261));
#37131=CARTESIAN_POINT('Ctrl Pts',(0.18449079848947,-6.76709527525922,-44.1885016025109));
#37132=CARTESIAN_POINT('Ctrl Pts',(0.372447602159575,-6.75935633790737,
-44.1796605667958));
#37133=CARTESIAN_POINT('Ctrl Pts',(0.559756448198972,-6.74380914014474,
-44.1708195310807));
#37134=CARTESIAN_POINT('Ctrl Pts',(0.74513613104807,-6.72842206873102,-44.1620695524674));
#37135=CARTESIAN_POINT('Ctrl Pts',(0.92988085194971,-6.70538686355659,-44.1533195738541));
#37136=CARTESIAN_POINT('Ctrl Pts',(1.11336305057924,-6.67478177303235,-44.1445695952408));
#37137=CARTESIAN_POINT('Ctrl Pts',(1.29684337090586,-6.6441769958117,-44.1358197062008));
#37138=CARTESIAN_POINT('Ctrl Pts',(1.47906091205653,-6.60600253547956,-44.1270698171608));
#37139=CARTESIAN_POINT('Ctrl Pts',(1.65939671095684,-6.56038806441095,-44.1183199281208));
#37140=CARTESIAN_POINT('Ctrl Pts',(1.83973072369626,-6.51477404513718,-44.1095701257453));
#37141=CARTESIAN_POINT('Ctrl Pts',(2.01818275357505,-6.46172023288515,-44.1008203233698));
#37142=CARTESIAN_POINT('Ctrl Pts',(2.19414664033797,-6.40140683917947,-44.0920705209943));
#37143=CARTESIAN_POINT('Ctrl Pts',(2.37010884271728,-6.34109402281323,-44.0833208023748));
#37144=CARTESIAN_POINT('Ctrl Pts',(2.54358267848271,-6.27352185699603,-44.0745710837553));
#37145=CARTESIAN_POINT('Ctrl Pts',(2.71397890842203,-6.19891986435059,-44.0658213651357));
#37146=CARTESIAN_POINT('Ctrl Pts',(2.88437356389396,-6.1243185610303,-44.0570717273639));
#37147=CARTESIAN_POINT('Ctrl Pts',(3.05169040787617,-6.04268767582332,-44.0483220895921));
#37148=CARTESIAN_POINT('Ctrl Pts',(3.2153611251249,-5.9543044795371,-44.0395724518203));
#37149=CARTESIAN_POINT('Ctrl Pts',(3.37903038443271,-5.86592207054796,-44.0308228919882));
#37150=CARTESIAN_POINT('Ctrl Pts',(3.53905332980392,-5.7707876070312,-44.0220733321561));
#37151=CARTESIAN_POINT('Ctrl Pts',(3.69488643042301,-5.66922422085032,-44.0133237723241));
#37152=CARTESIAN_POINT('Ctrl Pts',(3.8507181946915,-5.56766170562876,-44.0045742875241));
#37153=CARTESIAN_POINT('Ctrl Pts',(4.0023599459963,-5.45967053455954,-43.9958248027241));
#37154=CARTESIAN_POINT('Ctrl Pts',(4.14929662974704,-5.34561750206371,-43.9870753179241));
#37155=CARTESIAN_POINT('Ctrl Pts',(4.29623210225434,-5.23156540974145,-43.9783259052487));
#37156=CARTESIAN_POINT('Ctrl Pts',(4.43846235842494,-5.11145173171859,-43.9695764925734));
#37157=CARTESIAN_POINT('Ctrl Pts',(4.57550431797791,-4.98568443006228,-43.960827079898));
#37158=CARTESIAN_POINT('Ctrl Pts',(4.71254519337846,-4.85991812336348,-43.9520777364401));
#37159=CARTESIAN_POINT('Ctrl Pts',(4.84439764315324,-4.72849847630752,-43.9433283929822));
#37160=CARTESIAN_POINT('Ctrl Pts',(4.97061384197015,-4.59187184424988,-43.9345790495243));
#37161=CARTESIAN_POINT('Ctrl Pts',(5.09682908420519,-4.45524624767389,-43.925829772377));
#37162=CARTESIAN_POINT('Ctrl Pts',(5.21740796650468,-4.31341395556533,-43.9170804952296));
#37163=CARTESIAN_POINT('Ctrl Pts',(5.33194095942533,-4.16685668162496,-43.9083312180823));
#37164=CARTESIAN_POINT('Ctrl Pts',(5.44647312235404,-4.02030046974848,-43.8995820043387));
#37165=CARTESIAN_POINT('Ctrl Pts',(5.55495930712548,-3.86901957035174,-43.8908327905952));
#37166=CARTESIAN_POINT('Ctrl Pts',(5.65703106080043,-3.71352778057996,-43.8820835768516));
#37167=CARTESIAN_POINT('Ctrl Pts',(5.75910210868975,-3.55803706597215,-43.8733344236054));
#37168=CARTESIAN_POINT('Ctrl Pts',(5.85475865698779,-3.39833575880504,-43.8645852703592));
#37169=CARTESIAN_POINT('Ctrl Pts',(5.94367583069283,-3.23496624706317,-43.855836117113));
#37170=CARTESIAN_POINT('Ctrl Pts',(6.03259241910281,-3.07159781069699,-43.8470870214579));
#37171=CARTESIAN_POINT('Ctrl Pts',(6.11476958471156,-2.90456146975437,-43.8383379258028));
#37172=CARTESIAN_POINT('Ctrl Pts',(6.18992823574559,-2.73442451647865,-43.8295888301477));
#37173=CARTESIAN_POINT('Ctrl Pts',(6.26508641701097,-2.5642886266202,-43.8208397891776));
#37174=CARTESIAN_POINT('Ctrl Pts',(6.33322605570447,-2.39105242530879,-43.8120907482075));
#37175=CARTESIAN_POINT('Ctrl Pts',(6.39411573747906,-2.21530425353328,-43.8033417072373));
#37176=CARTESIAN_POINT('Ctrl Pts',(6.45500505889255,-2.03955712188152,-43.7945927180463));
#37177=CARTESIAN_POINT('Ctrl Pts',(6.50864441545048,-1.86129832025156,-43.7858437288553));
#37178=CARTESIAN_POINT('Ctrl Pts',(6.55485164050015,-1.68113324011885,-43.7770947396643));
#37179=CARTESIAN_POINT('Ctrl Pts',(6.60199852639206,-1.49730435912473,-43.7681678327875));
#37180=CARTESIAN_POINT('Ctrl Pts',(6.64140767441094,-1.31149113173226,-43.7592409259106));
#37181=CARTESIAN_POINT('Ctrl Pts',(6.67293975269674,-1.12435050446006,-43.7503140190337));
#37182=CARTESIAN_POINT('Ctrl Pts',(6.70384664831567,-0.940920291559479,
-43.7415641048497));
#37183=CARTESIAN_POINT('Ctrl Pts',(6.72718585889714,-0.756215114273666,
-43.7328141906657));
#37184=CARTESIAN_POINT('Ctrl Pts',(6.742878104519,-0.570862389370861,-43.7240642764817));
#37185=CARTESIAN_POINT('Ctrl Pts',(6.75857004154147,-0.38551330956387,-43.7153145343711));
#37186=CARTESIAN_POINT('Ctrl Pts',(6.76661529035568,-0.199516993255035,
-43.7065647922606));
#37187=CARTESIAN_POINT('Ctrl Pts',(6.76698652348897,-0.0135052182009377,
-43.69781505015));
#37188=CARTESIAN_POINT('Ctrl Pts',(6.76735774981513,0.172503146041962,-43.6890654684793));
#37189=CARTESIAN_POINT('Ctrl Pts',(6.76005524147463,0.358526681836487,-43.6803158868087));
#37190=CARTESIAN_POINT('Ctrl Pts',(6.74510380214858,0.543933542117825,-43.671566305138));
#37191=CARTESIAN_POINT('Ctrl Pts',(6.73015261710947,0.729337249087633,-43.6628168722761));
#37192=CARTESIAN_POINT('Ctrl Pts',(6.70755278444566,0.914124015857523,-43.6540674394142));
#37193=CARTESIAN_POINT('Ctrl Pts',(6.67738106408243,1.09766621749666,-43.6453180065523));
#37194=CARTESIAN_POINT('Ctrl Pts',(6.64720981677201,1.28120554143597,-43.6365687108699));
#37195=CARTESIAN_POINT('Ctrl Pts',(6.60946696581463,1.4635000565089,-43.6278194151876));
#37196=CARTESIAN_POINT('Ctrl Pts',(6.56428070010928,1.64393062206798,-43.6190701195052));
#37197=CARTESIAN_POINT('Ctrl Pts',(6.51909508282668,1.82435859844912,-43.6103209493752));
#37198=CARTESIAN_POINT('Ctrl Pts',(6.46646633415582,2.00292240086818,-43.6015717792452));
#37199=CARTESIAN_POINT('Ctrl Pts',(6.40657319597107,2.17901557696704,-43.5928226091153));
#37200=CARTESIAN_POINT('Ctrl Pts',(6.34668083768203,2.35510646007682,-43.5840735529122));
#37201=CARTESIAN_POINT('Ctrl Pts',(6.27952437143786,2.52872650996777,-43.5753244967091));
#37202=CARTESIAN_POINT('Ctrl Pts',(6.2053318733503,2.69928607998169,-43.566575440506));
#37203=CARTESIAN_POINT('Ctrl Pts',(6.12831449784144,2.87633970115627,-43.5574932642172));
#37204=CARTESIAN_POINT('Ctrl Pts',(6.04371489463044,3.05009490562565,-43.5484110879284));
#37205=CARTESIAN_POINT('Ctrl Pts',(5.95184265120381,3.21991584599834,-43.5393289116395));
#37206=CARTESIAN_POINT('Ctrl Pts',(5.86333281335374,3.38352155905506,-43.5305791312851));
#37207=CARTESIAN_POINT('Ctrl Pts',(5.76807337235558,3.54347560904031,-43.5218293509307));
#37208=CARTESIAN_POINT('Ctrl Pts',(5.66638790086219,3.69923467178856,-43.5130795705763));
#37209=CARTESIAN_POINT('Ctrl Pts',(5.56470608502597,3.85498813489974,-43.504330104782));
#37210=CARTESIAN_POINT('Ctrl Pts',(5.45659885766797,4.00654667256472,-43.4955806389877));
#37211=CARTESIAN_POINT('Ctrl Pts',(5.34243340580343,4.15339551506422,-43.4868311731935));
#37212=CARTESIAN_POINT('Ctrl Pts',(5.22827145140429,4.30023985884069,-43.4780819754396));
#37213=CARTESIAN_POINT('Ctrl Pts',(5.10805181977926,4.4423745699323,-43.4693327776857));
#37214=CARTESIAN_POINT('Ctrl Pts',(4.9821828128239,4.57931691626624,-43.4605835799319));
#37215=CARTESIAN_POINT('Ctrl Pts',(4.85631699296061,4.71625579512334,-43.4518346037139));
#37216=CARTESIAN_POINT('Ctrl Pts',(4.72480227791663,4.8480023613594,-43.4430856274958));
#37217=CARTESIAN_POINT('Ctrl Pts',(4.58808530847932,4.97410918679076,-43.4343366512778));
#37218=CARTESIAN_POINT('Ctrl Pts',(4.45135945056777,5.10022421089178,-43.4255871062566));
#37219=CARTESIAN_POINT('Ctrl Pts',(4.30943087207835,5.22069856612156,-43.4168375612354));
#37220=CARTESIAN_POINT('Ctrl Pts',(4.1627816432225,5.33512305301853,-43.4080880162142));
#37221=CARTESIAN_POINT('Ctrl Pts',(4.01614103534175,5.44954081331585,-43.399338985547));
#37222=CARTESIAN_POINT('Ctrl Pts',(3.864780558332,5.55790924068485,-43.3905899548797));
#37223=CARTESIAN_POINT('Ctrl Pts',(3.70921425811742,5.65986029751428,-43.3818409242125));
#37224=CARTESIAN_POINT('Ctrl Pts',(3.55364584529909,5.76181273884784,-43.3730917747326));
#37225=CARTESIAN_POINT('Ctrl Pts',(3.39387173464132,5.85734747818186,-43.3643426252528));
#37226=CARTESIAN_POINT('Ctrl Pts',(3.23043456092192,5.94614005448924,-43.3555934757729));
#37227=CARTESIAN_POINT('Ctrl Pts',(3.18690768806249,5.96978744811357,-43.3532633870399));
#37228=CARTESIAN_POINT('Ctrl Pts',(3.14312114982811,5.99295688499337,-43.3509332983069));
#37229=CARTESIAN_POINT('Ctrl Pts',(3.09908550384722,6.01564277861012,-43.3486032095739));
#37230=CARTESIAN_POINT('Origin',(0.,0.,-63.6971797838103));
#37231=CARTESIAN_POINT('',(3.09908550384721,6.01564277861012,-40.9541976313953));
#37232=CARTESIAN_POINT('',(3.09908550384719,6.01564277861013,-41.3487246499327));
#37233=CARTESIAN_POINT('',(3.09908550384721,6.01564277861012,-63.6971797838103));
#37234=CARTESIAN_POINT('',(-6.76699866356674,-0.00425291500162284,-42.3028202162243));
#37235=CARTESIAN_POINT('Ctrl Pts',(-6.76699866356628,-0.00425291572926541,
-42.30282021619));
#37236=CARTESIAN_POINT('Ctrl Pts',(-6.76684388596092,-0.250526276245932,
-42.2912054307044));
#37237=CARTESIAN_POINT('Ctrl Pts',(-6.75324119786962,-0.496385215031647,
-42.2795906452187));
#37238=CARTESIAN_POINT('Ctrl Pts',(-6.72634853459335,-0.740624325264789,
-42.2679758597331));
#37239=CARTESIAN_POINT('Ctrl Pts',(-6.70775751590284,-0.909467917163841,
-42.2599465064544));
#37240=CARTESIAN_POINT('Ctrl Pts',(-6.68281621829628,-1.07753799544482,
-42.2519171531757));
#37241=CARTESIAN_POINT('Ctrl Pts',(-6.65159041399686,-1.24444122578171,
-42.243887799897));
#37242=CARTESIAN_POINT('Ctrl Pts',(-6.61960773658645,-1.41538997456125,
-42.2356638254795));
#37243=CARTESIAN_POINT('Ctrl Pts',(-6.58098823809289,-1.58533161726112,
-42.2274398510619));
#37244=CARTESIAN_POINT('Ctrl Pts',(-6.5358075490959,-1.75371282745525,-42.2192158766443));
#37245=CARTESIAN_POINT('Ctrl Pts',(-6.49067457529011,-1.92191621075436,
-42.2110005875417));
#37246=CARTESIAN_POINT('Ctrl Pts',(-6.43899430161741,-2.08856209972778,
-42.202785298439));
#37247=CARTESIAN_POINT('Ctrl Pts',(-6.38089366570641,-2.2531056404323,-42.1945700093364));
#37248=CARTESIAN_POINT('Ctrl Pts',(-6.32284273595483,-2.41750841112046,
-42.1863617485642));
#37249=CARTESIAN_POINT('Ctrl Pts',(-6.25838250203016,-2.57981207940195,
-42.178153487792));
#37250=CARTESIAN_POINT('Ctrl Pts',(-6.18769018867022,-2.73948519416227,
-42.1699452270198));
#37251=CARTESIAN_POINT('Ctrl Pts',(-6.11704417854715,-2.89905372354829,
-42.1617423426319));
#37252=CARTESIAN_POINT('Ctrl Pts',(-6.04017436454052,-3.05599480473207,
-42.153539458244));
#37253=CARTESIAN_POINT('Ctrl Pts',(-5.957306757357,-3.20979519576384,-42.1453365738561));
#37254=CARTESIAN_POINT('Ctrl Pts',(-5.87447681484184,-3.36352568202923,
-42.1371374178119));
#37255=CARTESIAN_POINT('Ctrl Pts',(-5.78565467998213,-3.51411800704669,
-42.1289382617677));
#37256=CARTESIAN_POINT('Ctrl Pts',(-5.69111318190415,-3.66108177329554,
-42.1207391057235));
#37257=CARTESIAN_POINT('Ctrl Pts',(-5.59657990663755,-3.80803275727044,
-42.1125406628065));
#37258=CARTESIAN_POINT('Ctrl Pts',(-5.49632844567494,-3.95135550512971,
-42.1043422198895));
#37259=CARTESIAN_POINT('Ctrl Pts',(-5.39067619462646,-4.09058665287605,
-42.0961437769724));
#37260=CARTESIAN_POINT('Ctrl Pts',(-5.28502499574932,-4.22981641404497,
-42.0879454157022));
#37261=CARTESIAN_POINT('Ctrl Pts',(-5.17397332990384,-4.36495436987936,
-42.079747054432));
#37262=CARTESIAN_POINT('Ctrl Pts',(-5.05788023371376,-4.49556854484588,
-42.0715486931618));
#37263=CARTESIAN_POINT('Ctrl Pts',(-4.9417672045311,-4.62620514605017,-42.0633489242465));
#37264=CARTESIAN_POINT('Ctrl Pts',(-4.82061125876662,-4.75231615081152,
-42.0551491553312));
#37265=CARTESIAN_POINT('Ctrl Pts',(-4.69480982647489,-4.87350486746806,
-42.0469493864159));
#37266=CARTESIAN_POINT('Ctrl Pts',(-4.56896394131635,-4.9947364070542,-42.0387467200516));
#37267=CARTESIAN_POINT('Ctrl Pts',(-4.43846955787128,-5.11104194506308,
-42.0305440536873));
#37268=CARTESIAN_POINT('Ctrl Pts',(-4.3037588795333,-5.22206362531502,-42.0223413873229));
#37269=CARTESIAN_POINT('Ctrl Pts',(-4.168895203536,-5.33321139844559,-42.0141294047799));
#37270=CARTESIAN_POINT('Ctrl Pts',(-4.02980594293001,-5.43906309635014,
-42.0059174222369));
#37271=CARTESIAN_POINT('Ctrl Pts',(-3.88695496132079,-5.53930231425075,
-41.9977054396939));
#37272=CARTESIAN_POINT('Ctrl Pts',(-3.7440197242719,-5.63960065459687,-41.9894886136126));
#37273=CARTESIAN_POINT('Ctrl Pts',(-3.59731864440727,-5.73427972211552,
-41.9812717875313));
#37274=CARTESIAN_POINT('Ctrl Pts',(-3.44734202376301,-5.82306808917752,
-41.97305496145));
#37275=CARTESIAN_POINT('Ctrl Pts',(-3.29713411750919,-5.91199338072488,
-41.9648254638361));
#37276=CARTESIAN_POINT('Ctrl Pts',(-3.14364089131701,-5.99500964756865,
-41.9565959662223));
#37277=CARTESIAN_POINT('Ctrl Pts',(-2.98737574045601,-6.07189222444988,
-41.9483664686084));
#37278=CARTESIAN_POINT('Ctrl Pts',(-2.84808764323296,-6.1404220776154,-41.9410310450836));
#37279=CARTESIAN_POINT('Ctrl Pts',(-2.70659765149766,-6.20407921759945,
-41.9336956215588));
#37280=CARTESIAN_POINT('Ctrl Pts',(-2.56327997653755,-6.26273780082495,
-41.9263601980339));
#37281=CARTESIAN_POINT('Ctrl Pts',(-2.4055933281651,-6.32727747040638,-41.9182893278475));
#37282=CARTESIAN_POINT('Ctrl Pts',(-2.24517960117377,-6.38597554821436,
-41.9102184576611));
#37283=CARTESIAN_POINT('Ctrl Pts',(-2.08251983694756,-6.43858681146103,
-41.9021475874747));
#37284=CARTESIAN_POINT('Ctrl Pts',(-1.92006249015466,-6.49113260407997,
-41.8940867608589));
#37285=CARTESIAN_POINT('Ctrl Pts',(-1.75536501795551,-6.53760654030773,
-41.8860259342431));
#37286=CARTESIAN_POINT('Ctrl Pts',(-1.58893098858132,-6.57781022176271,
-41.8779651076273));
#37287=CARTESIAN_POINT('Ctrl Pts',(-1.42266757697749,-6.61797268891485,
-41.8699125444675));
#37288=CARTESIAN_POINT('Ctrl Pts',(-1.25467151040898,-6.65187760616159,
-41.8618599813076));
#37289=CARTESIAN_POINT('Ctrl Pts',(-1.08546408256142,-6.67937547420933,
-41.8538074181477));
#37290=CARTESIAN_POINT('Ctrl Pts',(-0.916393065446839,-6.70685117417389,
-41.8457613467598));
#37291=CARTESIAN_POINT('Ctrl Pts',(-0.746112997077899,-6.72793004596986,
-41.8377152753719));
#37292=CARTESIAN_POINT('Ctrl Pts',(-0.575157904931525,-6.74251306149234,
-41.8296692039841));
#37293=CARTESIAN_POINT('Ctrl Pts',(-0.404303237960745,-6.75708751042651,
-41.8216278591482));
#37294=CARTESIAN_POINT('Ctrl Pts',(-0.232774707315543,-6.76517366786207,
-41.8135865143123));
#37295=CARTESIAN_POINT('Ctrl Pts',(-0.0611139456945034,-6.76672402907357,
-41.8055451694764));
#37296=CARTESIAN_POINT('Ctrl Pts',(0.113855907209627,-6.76830427647876,
-41.7973488122554));
#37297=CARTESIAN_POINT('Ctrl Pts',(0.288962749829934,-6.76309411511982,
-41.7891524550343));
#37298=CARTESIAN_POINT('Ctrl Pts',(0.463629849140091,-6.75109890040032,
-41.7809560978132));
#37299=CARTESIAN_POINT('Ctrl Pts',(0.634939111024455,-6.73933428423701,
-41.7729173091047));
#37300=CARTESIAN_POINT('Ctrl Pts',(0.8058249993055,-6.72104317134424,-41.7648785203963));
#37301=CARTESIAN_POINT('Ctrl Pts',(0.975746109784252,-6.69628318765275,
-41.7568397316878));
#37302=CARTESIAN_POINT('Ctrl Pts',(1.14568540336148,-6.67152055441866,-41.748800082756));
#37303=CARTESIAN_POINT('Ctrl Pts',(1.31465934396178,-6.64028772581122,-41.7407604338243));
#37304=CARTESIAN_POINT('Ctrl Pts',(1.48213463143767,-6.60269383920632,-41.7327207848926));
#37305=CARTESIAN_POINT('Ctrl Pts',(1.64966100103271,-6.56508848598194,-41.7246786837644));
#37306=CARTESIAN_POINT('Ctrl Pts',(1.81568744343466,-6.5211182945414,-41.7166365826362));
#37307=CARTESIAN_POINT('Ctrl Pts',(1.97969392299502,-6.47094281934685,-41.708594481508));
#37308=CARTESIAN_POINT('Ctrl Pts',(2.14923497687789,-6.41907411899818,-41.7002809910633));
#37309=CARTESIAN_POINT('Ctrl Pts',(2.31661693306373,-6.36057412682575,-41.6919675006185));
#37310=CARTESIAN_POINT('Ctrl Pts',(2.48128674990314,-6.29567351954937,-41.6836540101738));
#37311=CARTESIAN_POINT('Ctrl Pts',(2.64086162557093,-6.2327809595425,-41.675597742003));
#37312=CARTESIAN_POINT('Ctrl Pts',(2.79788938413509,-6.16387817576336,-41.6675414738323));
#37313=CARTESIAN_POINT('Ctrl Pts',(2.95189146735603,-6.08922209850739,-41.6594852056615));
#37314=CARTESIAN_POINT('Ctrl Pts',(3.11326906834912,-6.01099056815958,-41.6510431040798));
#37315=CARTESIAN_POINT('Ctrl Pts',(3.27132362515598,-5.92644134502226,-41.642601002498));
#37316=CARTESIAN_POINT('Ctrl Pts',(3.42553881963984,-5.83592090377693,-41.6341589009162));
#37317=CARTESIAN_POINT('Ctrl Pts',(3.57975401412373,-5.74540046253157,-41.6257167993345));
#37318=CARTESIAN_POINT('Ctrl Pts',(3.73012950509335,-5.64890912484754,-41.6172746977527));
#37319=CARTESIAN_POINT('Ctrl Pts',(3.87618945569488,-5.54684093007541,-41.608832596171));
#37320=CARTESIAN_POINT('Ctrl Pts',(4.02037637884735,-5.44608162613678,-41.6004987534783));
#37321=CARTESIAN_POINT('Ctrl Pts',(4.16081652066068,-5.33956780953376,-41.5921649107856));
#37322=CARTESIAN_POINT('Ctrl Pts',(4.29702791065859,-5.2276036704231,-41.5838310680929));
#37323=CARTESIAN_POINT('Ctrl Pts',(4.43307875830125,-5.115771495215,-41.5755070478882));
#37324=CARTESIAN_POINT('Ctrl Pts',(4.56491051651839,-4.99850201347904,-41.5671830276834));
#37325=CARTESIAN_POINT('Ctrl Pts',(4.69207016107308,-4.87614259467129,-41.5588590074787));
#37326=CARTESIAN_POINT('Ctrl Pts',(4.81910324643551,-4.75390495749688,-41.5505432719878));
#37327=CARTESIAN_POINT('Ctrl Pts',(4.94147323349797,-4.62658771590757,-41.5422275364969));
#37328=CARTESIAN_POINT('Ctrl Pts',(5.05876000478071,-4.49457853575072,-41.5339118010061));
#37329=CARTESIAN_POINT('Ctrl Pts',(5.17595153308928,-4.36267655393176,-41.525602818326));
#37330=CARTESIAN_POINT('Ctrl Pts',(5.2880678406877,-4.22609048444294,-41.517293835646));
#37331=CARTESIAN_POINT('Ctrl Pts',(5.39472538306907,-4.08524504054166,-41.508984852966));
#37332=CARTESIAN_POINT('Ctrl Pts',(5.50131584565111,-3.94448817813124,-41.5006810960288));
#37333=CARTESIAN_POINT('Ctrl Pts',(5.6024541755498,-3.7994775564615,-41.4923773390917));
#37334=CARTESIAN_POINT('Ctrl Pts',(5.69779673950095,-3.65067135131778,-41.4840735821545));
#37335=CARTESIAN_POINT('Ctrl Pts',(5.79310059666959,-3.50192555790603,-41.4757731963425));
#37336=CARTESIAN_POINT('Ctrl Pts',(5.8826131889639,-3.34938754381223,-41.4674728105304));
#37337=CARTESIAN_POINT('Ctrl Pts',(5.96603373897391,-3.19354511873952,-41.4591724247184));
#37338=CARTESIAN_POINT('Ctrl Pts',(6.04943669776054,-3.0377355567792,-41.4508737892418));
#37339=CARTESIAN_POINT('Ctrl Pts',(6.12675000956663,-2.8786232785124,-41.4425751537651));
#37340=CARTESIAN_POINT('Ctrl Pts',(6.19771835067938,-2.7167215988489,-41.4342765182885));
#37341=CARTESIAN_POINT('Ctrl Pts',(6.26868350634561,-2.55482718621649,-41.4259782552999));
#37342=CARTESIAN_POINT('Ctrl Pts',(6.33330411939158,-2.39014394026607,-41.4176799923113));
#37343=CARTESIAN_POINT('Ctrl Pts',(6.39137253243378,-2.22320627735057,-41.4093817293228));
#37344=CARTESIAN_POINT('Ctrl Pts',(6.44944797731292,-2.05624839899674,-41.40108246145));
#37345=CARTESIAN_POINT('Ctrl Pts',(6.50096952747292,-1.88703588835013,-41.3927831935772));
#37346=CARTESIAN_POINT('Ctrl Pts',(6.5457789675968,-1.71611966580639,-41.3844839257044));
#37347=CARTESIAN_POINT('Ctrl Pts',(6.59061987116992,-1.54508343252655,-41.3761788304079));
#37348=CARTESIAN_POINT('Ctrl Pts',(6.628739159033,-1.37234143379624,-41.3678737351113));
#37349=CARTESIAN_POINT('Ctrl Pts',(6.66002925677816,-1.19845704923411,-41.3595686398148));
#37350=CARTESIAN_POINT('Ctrl Pts',(6.69133076452004,-1.02450925738344,-41.3512605160487));
#37351=CARTESIAN_POINT('Ctrl Pts',(6.71579806437575,-0.849418592958558,
-41.3429523922826));
#37352=CARTESIAN_POINT('Ctrl Pts',(6.73337530018403,-0.673755198029385,
-41.3346442685165));
#37353=CARTESIAN_POINT('Ctrl Pts',(6.75097122049243,-0.497905073926316,
-41.3263273132628));
#37354=CARTESIAN_POINT('Ctrl Pts',(6.7616624160892,-0.32148134989519,-41.3180103580091));
#37355=CARTESIAN_POINT('Ctrl Pts',(6.76544510652199,-0.14505692206052,-41.3096934027555));
#37356=CARTESIAN_POINT('Ctrl Pts',(6.7682328918187,-0.0150348029798014,
-41.303563933273));
#37357=CARTESIAN_POINT('Ctrl Pts',(6.76726943506968,0.114987655273514,-41.2974344637905));
#37358=CARTESIAN_POINT('Ctrl Pts',(6.7625712964825,0.244782474844537,-41.2913049943079));
#37359=CARTESIAN_POINT('Ctrl Pts',(6.75609372451022,0.423737452395306,-41.2828539707828));
#37360=CARTESIAN_POINT('Ctrl Pts',(6.74250293622476,0.602586556072336,-41.2744029472576));
#37361=CARTESIAN_POINT('Ctrl Pts',(6.7218101425669,0.780741575224981,-41.2659519237324));
#37362=CARTESIAN_POINT('Ctrl Pts',(6.70113556829883,0.958739734178298,-41.2575083410822));
#37363=CARTESIAN_POINT('Ctrl Pts',(6.67337149034784,1.13604469894378,-41.2490647584321));
#37364=CARTESIAN_POINT('Ctrl Pts',(6.63858108888244,1.31207093037401,-41.240621175782));
#37365=CARTESIAN_POINT('Ctrl Pts',(6.60381658995475,1.48796610479118,-41.2321838796421));
#37366=CARTESIAN_POINT('Ctrl Pts',(6.56203625995759,1.66258411962017,-41.2237465835023));
#37367=CARTESIAN_POINT('Ctrl Pts',(6.51335482385915,1.83534681695604,-41.2153092873625));
#37368=CARTESIAN_POINT('Ctrl Pts',(6.46470811825353,2.0079862612801,-41.2068780105902));
#37369=CARTESIAN_POINT('Ctrl Pts',(6.40917021680669,2.17877271001987,-41.1984467338178));
#37370=CARTESIAN_POINT('Ctrl Pts',(6.34690647594121,2.3471402143152,-41.1900154570455));
#37371=CARTESIAN_POINT('Ctrl Pts',(6.2846694235689,2.51543555020356,-41.1815877942236));
#37372=CARTESIAN_POINT('Ctrl Pts',(6.21571239381016,2.6813136983124,-41.1731601314016));
#37373=CARTESIAN_POINT('Ctrl Pts',(6.14025015285026,2.84422521267608,-41.1647324685797));
#37374=CARTESIAN_POINT('Ctrl Pts',(6.06481114215278,3.00708657643226,-41.1563074001257));
#37375=CARTESIAN_POINT('Ctrl Pts',(5.98287105303255,3.16698282725885,-41.1478823316718));
#37376=CARTESIAN_POINT('Ctrl Pts',(5.89469236428801,3.32338546220638,-41.1394572632178));
#37377=CARTESIAN_POINT('Ctrl Pts',(5.87056397596649,3.36618201049091,-41.137151906604));
#37378=CARTESIAN_POINT('Ctrl Pts',(5.8459687507013,3.40871711144768,-41.1348465499902));
#37379=CARTESIAN_POINT('Ctrl Pts',(5.82091267019111,3.45098025001718,-41.1325411933764));
#37380=CARTESIAN_POINT('Ctrl Pts',(5.72723602637226,3.60898856168555,-41.1239222048519));
#37381=CARTESIAN_POINT('Ctrl Pts',(5.62715607284524,3.76312286389861,-41.1153032163274));
#37382=CARTESIAN_POINT('Ctrl Pts',(5.52102284174427,3.9128756408731,-41.1066842278029));
#37383=CARTESIAN_POINT('Ctrl Pts',(5.41482602736629,4.06271813312529,-41.0980600757351));
#37384=CARTESIAN_POINT('Ctrl Pts',(5.30256887398964,4.20817361343996,-41.0894359236674));
#37385=CARTESIAN_POINT('Ctrl Pts',(5.18464285012906,4.34876620624811,-41.0808117715996));
#37386=CARTESIAN_POINT('Ctrl Pts',(5.06267782822622,4.49417413318286,-41.0718922400034));
#37387=CARTESIAN_POINT('Ctrl Pts',(4.93464897618203,4.63437989549188,-41.0629727084071));
#37388=CARTESIAN_POINT('Ctrl Pts',(4.80103176615619,4.76889745961885,-41.0540531768109));
#37389=CARTESIAN_POINT('Ctrl Pts',(4.67159875816515,4.89920262726316,-41.0454129589516));
#37390=CARTESIAN_POINT('Ctrl Pts',(4.53692234731059,5.02417028200731,-41.0367727410924));
#37391=CARTESIAN_POINT('Ctrl Pts',(4.39746975459071,5.14339856101585,-41.0281325232331));
#37392=CARTESIAN_POINT('Ctrl Pts',(4.25125500168537,5.26840830816039,-41.0190733347684));
#37393=CARTESIAN_POINT('Ctrl Pts',(4.09978965524161,5.38710798898233,-41.0100141463037));
#37394=CARTESIAN_POINT('Ctrl Pts',(3.9436484975699,5.49908406260667,-41.000954957839));
#37395=CARTESIAN_POINT('Ctrl Pts',(3.78750733989819,5.61106013623101,-40.9918957693743));
#37396=CARTESIAN_POINT('Ctrl Pts',(3.6266907092926,5.71631242084015,-40.9828365809096));
#37397=CARTESIAN_POINT('Ctrl Pts',(3.46180560937375,5.81448113961241,-40.9737773924449));
#37398=CARTESIAN_POINT('Ctrl Pts',(3.34301605592288,5.88520565184269,-40.9672508054284));
#37399=CARTESIAN_POINT('Ctrl Pts',(3.22203664576403,5.95230189956878,-40.9607242184118));
#37400=CARTESIAN_POINT('Ctrl Pts',(3.09908550384721,6.01564277861012,-40.9541976313953));
#37401=CARTESIAN_POINT('Ctrl Pts',(3.09908550384721,6.01564277861012,-42.9543661083715));
#37402=CARTESIAN_POINT('Ctrl Pts',(2.94508352360841,6.09498015319939,-42.9462354082376));
#37403=CARTESIAN_POINT('Ctrl Pts',(2.78811202322111,6.16835922330416,-42.9381047081037));
#37404=CARTESIAN_POINT('Ctrl Pts',(2.62868177603743,6.23556902939328,-42.9299740079697));
#37405=CARTESIAN_POINT('Ctrl Pts',(2.46190881464766,6.30587424809499,-42.9214688405786));
#37406=CARTESIAN_POINT('Ctrl Pts',(2.292445687093,6.36942830878534,-42.9129636731875));
#37407=CARTESIAN_POINT('Ctrl Pts',(2.12089558626553,6.42604784546142,-42.9044585057964));
#37408=CARTESIAN_POINT('Ctrl Pts',(1.94934548543806,6.48266738213751,-42.8959533384053));
#37409=CARTESIAN_POINT('Ctrl Pts',(1.77570886195601,6.5323523206861,-42.8874481710142));
#37410=CARTESIAN_POINT('Ctrl Pts',(1.60060127132296,6.57498019542564,-42.878943003623));
#37411=CARTESIAN_POINT('Ctrl Pts',(1.42682065125253,6.61728503485459,-42.870502288645));
#37412=CARTESIAN_POINT('Ctrl Pts',(1.25123339486017,6.65272723459906,-42.8620615736669));
#37413=CARTESIAN_POINT('Ctrl Pts',(1.07440837386975,6.68116274657028,-42.8536208586888));
#37414=CARTESIAN_POINT('Ctrl Pts',(0.897717005560992,6.70957676564187,-42.8451865236008));
#37415=CARTESIAN_POINT('Ctrl Pts',(0.71979006564518,6.73099460142001,-42.8367521885128));
#37416=CARTESIAN_POINT('Ctrl Pts',(0.541207430672698,6.74532308469985,-42.8283178534247));
#37417=CARTESIAN_POINT('Ctrl Pts',(0.362732353467413,6.75964293813911,-42.8198885982161));
#37418=CARTESIAN_POINT('Ctrl Pts',(0.183602700046286,6.76688192500108,-42.8114593430075));
#37419=CARTESIAN_POINT('Ctrl Pts',(0.00440469568970479,6.76699856647361,
-42.8030300877989));
#37420=CARTESIAN_POINT('Ctrl Pts',(-0.174712867895633,6.76711515558657,
-42.7946046164259));
#37421=CARTESIAN_POINT('Ctrl Pts',(-0.353898388377913,6.76011577391952,
-42.7861791450528));
#37422=CARTESIAN_POINT('Ctrl Pts',(-0.532564002869326,6.74601101265391,
-42.7777536736798));
#37423=CARTESIAN_POINT('Ctrl Pts',(-0.711176798621986,6.73191042116491,
-42.7693306931206));
#37424=CARTESIAN_POINT('Ctrl Pts',(-0.889269662869151,6.71070866527772,
-42.7609077125613));
#37425=CARTESIAN_POINT('Ctrl Pts',(-1.06625782114147,6.68246835075593,-42.7524847320021));
#37426=CARTESIAN_POINT('Ctrl Pts',(-1.24324890997032,6.65422756863314,-42.7440616119758));
#37427=CARTESIAN_POINT('Ctrl Pts',(-1.41913492607003,6.61894804101692,-42.7356384919494));
#37428=CARTESIAN_POINT('Ctrl Pts',(-1.59333860961469,6.57674395693729,-42.7272153719231));
#37429=CARTESIAN_POINT('Ctrl Pts',(-1.76754831741319,6.53453841337006,-42.7187919606113));
#37430=CARTESIAN_POINT('Ctrl Pts',(-1.94007525248876,6.48540791424459,-42.7103685492994));
#37431=CARTESIAN_POINT('Ctrl Pts',(-2.11035454792276,6.42951729774963,-42.7019451379875));
#37432=CARTESIAN_POINT('Ctrl Pts',(-2.28066347985192,6.37361695369513,-42.6935202606114));
#37433=CARTESIAN_POINT('Ctrl Pts',(-2.44872367536119,6.31095425053192,-42.6850953832353));
#37434=CARTESIAN_POINT('Ctrl Pts',(-2.61398722013432,6.24174333123162,-42.6766705058592));
#37435=CARTESIAN_POINT('Ctrl Pts',(-2.77930258397864,6.17251071055999,-42.6682429868278));
#37436=CARTESIAN_POINT('Ctrl Pts',(-2.9418192412985,6.09672590895556,-42.6598154677963));
#37437=CARTESIAN_POINT('Ctrl Pts',(-3.10101064488902,6.01465061165526,-42.6513879487649));
#37438=CARTESIAN_POINT('Ctrl Pts',(-3.26034480517789,5.93250171240037,-42.6429528722601));
#37439=CARTESIAN_POINT('Ctrl Pts',(-3.41634745666161,5.84405119874393,-42.6345177957553));
#37440=CARTESIAN_POINT('Ctrl Pts',(-3.56851698959077,5.74960655132176,-42.6260827192505));
#37441=CARTESIAN_POINT('Ctrl Pts',(-3.72076006705666,5.65511625817992,-42.6176435660178));
#37442=CARTESIAN_POINT('Ctrl Pts',(-3.86916605237184,5.55462623614353,-42.609204412785));
#37443=CARTESIAN_POINT('Ctrl Pts',(-4.01326315108692,5.4484867513951,-42.6007652595522));
#37444=CARTESIAN_POINT('Ctrl Pts',(-4.15752038207929,5.34222931592069,-42.5923167280541));
#37445=CARTESIAN_POINT('Ctrl Pts',(-4.29745889499402,5.2303100774344,-42.583868196556));
#37446=CARTESIAN_POINT('Ctrl Pts',(-4.43263981342177,5.11311972131185,-42.5754196650579));
#37447=CARTESIAN_POINT('Ctrl Pts',(-4.50733165680832,5.0483682473041,-42.5707515772919));
#37448=CARTESIAN_POINT('Ctrl Pts',(-4.58057167599017,4.98200821746615,-42.566083489526));
#37449=CARTESIAN_POINT('Ctrl Pts',(-4.65229075505635,4.91411026844303,-42.56141540176));
#37450=CARTESIAN_POINT('Ctrl Pts',(-4.77889952211963,4.79424710617333,-42.5531746261633));
#37451=CARTESIAN_POINT('Ctrl Pts',(-4.90104784218804,4.66932234474011,-42.5449338505665));
#37452=CARTESIAN_POINT('Ctrl Pts',(-5.01830828543984,4.53969943413503,-42.5366930749697));
#37453=CARTESIAN_POINT('Ctrl Pts',(-5.13543885003825,4.41022009495617,-42.5284614269253));
#37454=CARTESIAN_POINT('Ctrl Pts',(-5.24769208120687,4.27605322966876,-42.520229778881));
#37455=CARTESIAN_POINT('Ctrl Pts',(-5.354675217738,4.13760103351477,-42.5119981308366));
#37456=CARTESIAN_POINT('Ctrl Pts',(-5.4615589242409,3.99927751470395,-42.5037741332783));
#37457=CARTESIAN_POINT('Ctrl Pts',(-5.56318207440744,3.85667687674248,-42.49555013572));
#37458=CARTESIAN_POINT('Ctrl Pts',(-5.65919019381688,3.71023656256671,-42.4873261381617));
#37459=CARTESIAN_POINT('Ctrl Pts',(-5.75511348967983,3.56392562897745,-42.4791094065372));
#37460=CARTESIAN_POINT('Ctrl Pts',(-5.8454314480592,3.41378207692828,-42.4708926749127));
#37461=CARTESIAN_POINT('Ctrl Pts',(-5.92983125685374,3.26027456899575,-42.4626759432882));
#37462=CARTESIAN_POINT('Ctrl Pts',(-6.01418782450147,3.10684570864289,-42.4544634213995));
#37463=CARTESIAN_POINT('Ctrl Pts',(-6.09263211029324,2.9500566359011,-42.4462508995108));
#37464=CARTESIAN_POINT('Ctrl Pts',(-6.16489562918667,2.79040335457709,-42.4380383776221));
#37465=CARTESIAN_POINT('Ctrl Pts',(-6.23713498281156,2.6308034620788,-42.4298286020403));
#37466=CARTESIAN_POINT('Ctrl Pts',(-6.30319754045534,2.46834159283338,-42.4216188264584));
#37467=CARTESIAN_POINT('Ctrl Pts',(-6.36286159541037,2.30353669770027,-42.4134090508766));
#37468=CARTESIAN_POINT('Ctrl Pts',(-6.38892130453191,2.23155420116675,-42.4098232341939));
#37469=CARTESIAN_POINT('Ctrl Pts',(-6.41376097430492,2.15912499519095,-42.4062374175112));
#37470=CARTESIAN_POINT('Ctrl Pts',(-6.43736502764551,2.08629348387196,-42.4026516008285));
#37471=CARTESIAN_POINT('Ctrl Pts',(-6.49212766462547,1.9173205724184,-42.3943323187781));
#37472=CARTESIAN_POINT('Ctrl Pts',(-6.5402041605344,1.74627955095192,-42.3860130367278));
#37473=CARTESIAN_POINT('Ctrl Pts',(-6.5814623005094,1.57373536116259,-42.3776937546774));
#37474=CARTESIAN_POINT('Ctrl Pts',(-6.62263302592097,1.40155674468879,-42.36939209888));
#37475=CARTESIAN_POINT('Ctrl Pts',(-6.65701423575539,1.22788167181083,-42.3610904430825));
#37476=CARTESIAN_POINT('Ctrl Pts',(-6.6845263044129,1.05327920591459,-42.352788787285));
#37477=CARTESIAN_POINT('Ctrl Pts',(-6.71212599438798,0.878120660491798,
-42.3444606921082));
#37478=CARTESIAN_POINT('Ctrl Pts',(-6.73281268932431,0.702029154174227,
-42.3361325969314));
#37479=CARTESIAN_POINT('Ctrl Pts',(-6.74655859261206,0.525581731467544,
-42.3278045017547));
#37480=CARTESIAN_POINT('Ctrl Pts',(-6.76030449589981,0.349134308760862,
-42.3194764065779));
#37481=CARTESIAN_POINT('Ctrl Pts',(-6.76710964300839,0.172331317951537,
-42.3111483114011));
#37482=CARTESIAN_POINT('Ctrl Pts',(-6.76699866356674,-0.00425291500166258,
-42.3028202162243));
#37483=CARTESIAN_POINT('',(-6.767,7.13615364716924E-13,-42.6971797838101));
#37484=CARTESIAN_POINT('Ctrl Pts',(3.09908550384722,6.01564277861012,-43.3486032095739));
#37485=CARTESIAN_POINT('Ctrl Pts',(2.93373232018328,6.10082796552481,-43.3398537616746));
#37486=CARTESIAN_POINT('Ctrl Pts',(2.76486502144423,6.17919158180192,-43.3311043137753));
#37487=CARTESIAN_POINT('Ctrl Pts',(2.59305716434346,6.25046746591381,-43.3223548658761));
#37488=CARTESIAN_POINT('Ctrl Pts',(2.42125069459283,6.32174277447224,-43.3136054886286));
#37489=CARTESIAN_POINT('Ctrl Pts',(2.24650397871065,6.38593035557823,-43.3048561113812));
#37490=CARTESIAN_POINT('Ctrl Pts',(2.06941053323784,6.44281220003535,-43.2961067341338));
#37491=CARTESIAN_POINT('Ctrl Pts',(1.89231845896703,6.49969360406679,-43.2873574246312));
#37492=CARTESIAN_POINT('Ctrl Pts',(1.71287996431533,6.54926929700873,-43.2786081151286));
#37493=CARTESIAN_POINT('Ctrl Pts',(1.53170449173539,6.59137090065471,-43.269858805626));
#37494=CARTESIAN_POINT('Ctrl Pts',(1.35053036178204,6.63347219230076,-43.2611095609614));
#37495=CARTESIAN_POINT('Ctrl Pts',(1.16761955878877,6.66809944062448,-43.2523603162969));
#37496=CARTESIAN_POINT('Ctrl Pts',(0.983593309310796,6.69513503985387,-43.2436110716323));
#37497=CARTESIAN_POINT('Ctrl Pts',(0.799568362460319,6.7221704477121,-43.2348618888991));
#37498=CARTESIAN_POINT('Ctrl Pts',(0.614428268438959,6.74161427235974,-43.2261127061659));
#37499=CARTESIAN_POINT('Ctrl Pts',(0.428801816330661,6.75340047696799,-43.2173635234327));
#37500=CARTESIAN_POINT('Ctrl Pts',(0.243176616523146,6.76518660206241,-43.2086143997246));
#37501=CARTESIAN_POINT('Ctrl Pts',(0.0570653511657931,6.76931519233997,
-43.1998652760165));
#37502=CARTESIAN_POINT('Ctrl Pts',(-0.128899900799728,6.76577222610796,
-43.1911161523083));
#37503=CARTESIAN_POINT('Ctrl Pts',(-0.314863959941652,6.76222928260135,
-43.1823670847191));
#37504=CARTESIAN_POINT('Ctrl Pts',(-0.500681721080245,6.7510148865128,-43.1736180171298));
#37505=CARTESIAN_POINT('Ctrl Pts',(-0.685722110172797,6.73216712415996,
-43.1648689495406));
#37506=CARTESIAN_POINT('Ctrl Pts',(-0.870761373827028,6.71331947644152,
-43.1561199351642));
#37507=CARTESIAN_POINT('Ctrl Pts',(-1.05502298984277,6.68683858440007,-43.1473709207878));
#37508=CARTESIAN_POINT('Ctrl Pts',(-1.23788117675985,6.6528143813144,-43.1386219064115));
#37509=CARTESIAN_POINT('Ctrl Pts',(-1.43009641451724,6.61704912302392,-43.129425195524));
#37510=CARTESIAN_POINT('Ctrl Pts',(-1.62076048992632,6.57294837083181,-43.1202284846364));
#37511=CARTESIAN_POINT('Ctrl Pts',(-1.80915798961074,6.52067760042065,-43.1110317737489));
#37512=CARTESIAN_POINT('Ctrl Pts',(-1.98840443002955,6.47094578577426,-43.1022817760424));
#37513=CARTESIAN_POINT('Ctrl Pts',(-2.16559895952137,6.41381888474494,-43.0935317783359));
#37514=CARTESIAN_POINT('Ctrl Pts',(-2.34013966242268,6.34949095285254,-43.0847817806294));
#37515=CARTESIAN_POINT('Ctrl Pts',(-2.51467682553963,6.28516432556706,-43.0760319603778));
#37516=CARTESIAN_POINT('Ctrl Pts',(-2.68656000078793,6.21363705879682,-43.0672821401262));
#37517=CARTESIAN_POINT('Ctrl Pts',(-2.85520533840842,6.13515211510881,-43.0585323198746));
#37518=CARTESIAN_POINT('Ctrl Pts',(-3.02384747998287,6.05666865881142,-43.0497826654433));
#37519=CARTESIAN_POINT('Ctrl Pts',(-3.18925164684503,5.97122791039862,-43.0410330110121));
#37520=CARTESIAN_POINT('Ctrl Pts',(-3.3508560182913,5.87912008251924,-43.0322833565808));
#37521=CARTESIAN_POINT('Ctrl Pts',(-3.51245754191383,5.78701387778195,-43.0235338563377));
#37522=CARTESIAN_POINT('Ctrl Pts',(-3.67025915510894,5.68824097061009,-43.0147843560946));
#37523=CARTESIAN_POINT('Ctrl Pts',(-3.82372487928786,5.58313684656888,-43.0060348558514));
#37524=CARTESIAN_POINT('Ctrl Pts',(-3.97718810300738,5.47803443501816,-42.9972854981663));
#37525=CARTESIAN_POINT('Ctrl Pts',(-4.12631534262954,5.3666011749643,-42.9885361404812));
#37526=CARTESIAN_POINT('Ctrl Pts',(-4.27060009886143,5.24921554097417,-42.9797867827961));
#37527=CARTESIAN_POINT('Ctrl Pts',(-4.41488269594131,5.13183166360361,-42.9710375560409));
#37528=CARTESIAN_POINT('Ctrl Pts',(-4.55432273235007,5.00849577139544,-42.9622883292857));
#37529=CARTESIAN_POINT('Ctrl Pts',(-4.68844662480126,4.8796267527742,-42.9535391025306));
#37530=CARTESIAN_POINT('Ctrl Pts',(-4.82256868835087,4.75075949139953,-42.9447899950791));
#37531=CARTESIAN_POINT('Ctrl Pts',(-4.95137454637802,4.6163594531259,-42.9360408876276));
#37532=CARTESIAN_POINT('Ctrl Pts',(-5.07442674461026,4.47688309134649,-42.9272917801761));
#37533=CARTESIAN_POINT('Ctrl Pts',(-5.19747742838495,4.33740844616404,-42.9185427804037));
#37534=CARTESIAN_POINT('Ctrl Pts',(-5.3147744045089,4.19285781736076,-42.9097937806313));
#37535=CARTESIAN_POINT('Ctrl Pts',(-5.42591931531122,4.04372211999447,-42.9010447808589));
#37536=CARTESIAN_POINT('Ctrl Pts',(-5.53707636462956,3.89457013500838,-42.8922948255784));
#37537=CARTESIAN_POINT('Ctrl Pts',(-5.64207983273449,3.74083230916452,-42.8835448702978));
#37538=CARTESIAN_POINT('Ctrl Pts',(-5.7405730346873,3.58303087251854,-42.8747949150172));
#37539=CARTESIAN_POINT('Ctrl Pts',(-5.83906243363753,3.42523552887452,-42.8660452975884));
#37540=CARTESIAN_POINT('Ctrl Pts',(-5.93104191768417,3.26337713157008,-42.8572956801596));
#37541=CARTESIAN_POINT('Ctrl Pts',(-6.01619906699651,3.09800545291165,-42.8485460627308));
#37542=CARTESIAN_POINT('Ctrl Pts',(-6.10135338095378,2.93263928039605,-42.8397967366254));
#37543=CARTESIAN_POINT('Ctrl Pts',(-6.17968568352834,2.76376031540234,-42.83104741052));
#37544=CARTESIAN_POINT('Ctrl Pts',(-6.25092992694882,2.59194213831552,-42.8222980844146));
#37545=CARTESIAN_POINT('Ctrl Pts',(-6.32217217691111,2.42012876880803,-42.8135490031208));
#37546=CARTESIAN_POINT('Ctrl Pts',(-6.38632665483867,2.24537661647626,-42.804799921827));
#37547=CARTESIAN_POINT('Ctrl Pts',(-6.44317547869373,2.06827917621383,-42.7960508405332));
#37548=CARTESIAN_POINT('Ctrl Pts',(-6.50002944235956,1.89116572423353,-42.7873009682182));
#37549=CARTESIAN_POINT('Ctrl Pts',(-6.54957634250415,1.71170683289132,-42.7785510959033));
#37550=CARTESIAN_POINT('Ctrl Pts',(-6.5916478770841,1.53051209225302,-42.7698012235883));
#37551=CARTESIAN_POINT('Ctrl Pts',(-6.63371649075019,1.34932993147978,-42.7610519587535));
#37552=CARTESIAN_POINT('Ctrl Pts',(-6.66831071257131,1.16641244173963,-42.7523026939187));
#37553=CARTESIAN_POINT('Ctrl Pts',(-6.69531304840337,0.982380875159712,
-42.7435534290839));
#37554=CARTESIAN_POINT('Ctrl Pts',(-6.72231677033047,0.798339861795558,
-42.7348037151283));
#37555=CARTESIAN_POINT('Ctrl Pts',(-6.74172778477892,0.613184940729886,
-42.7260540011726));
#37556=CARTESIAN_POINT('Ctrl Pts',(-6.7534801583552,0.427545027690303,-42.717304287217));
#37557=CARTESIAN_POINT('Ctrl Pts',(-6.7624903836522,0.28521995354692,-42.7105961194147));
#37558=CARTESIAN_POINT('Ctrl Pts',(-6.76699999999999,0.142609995757751,
-42.7038879516124));
#37559=CARTESIAN_POINT('Ctrl Pts',(-6.767,7.1361580617263E-13,-42.6971797838101));
#37560=CARTESIAN_POINT('Ctrl Pts',(-6.76699988344647,-0.00125595997021738,
-42.6971797838101));
#37561=CARTESIAN_POINT('Ctrl Pts',(-6.76699667390786,-0.0185486666597619,
-42.6963684220283));
#37562=CARTESIAN_POINT('Ctrl Pts',(-6.76692717812646,-0.0358409891425261,
-42.6955570602465));
#37563=CARTESIAN_POINT('Ctrl Pts',(-6.76679140733531,-0.0531323781990722,
-42.6947456984647));
#37564=CARTESIAN_POINT('Ctrl Pts',(-6.76534913224035,-0.23681650923917,
-42.6861267099402));
#37565=CARTESIAN_POINT('Ctrl Pts',(-6.75642390721146,-0.420375002844922,
-42.6775077214157));
#37566=CARTESIAN_POINT('Ctrl Pts',(-6.740062835943,-0.603193142815786,-42.6688887328912));
#37567=CARTESIAN_POINT('Ctrl Pts',(-6.7236919629328,-0.786120807167066,
-42.6602645808235));
#37568=CARTESIAN_POINT('Ctrl Pts',(-6.69987638050173,-0.968306929775302,
-42.6516404287557));
#37569=CARTESIAN_POINT('Ctrl Pts',(-6.66871492179339,-1.14914328603976,
-42.6430162766879));
#37570=CARTESIAN_POINT('Ctrl Pts',(-6.63648617474091,-1.33617333615671,
-42.6340967450917));
#37571=CARTESIAN_POINT('Ctrl Pts',(-6.59639951463416,-1.52175917188238,
-42.6251772134955));
#37572=CARTESIAN_POINT('Ctrl Pts',(-6.54862125641083,-1.70524151957552,
-42.6162576818992));
#37573=CARTESIAN_POINT('Ctrl Pts',(-6.50233916687159,-1.88297814624599,
-42.60761746404));
#37574=CARTESIAN_POINT('Ctrl Pts',(-6.44884004425104,-2.05874075390657,
-42.5989772461807));
#37575=CARTESIAN_POINT('Ctrl Pts',(-6.38832542799106,-2.23194695861771,
-42.5903370283215));
#37576=CARTESIAN_POINT('Ctrl Pts',(-6.32487641287361,-2.41355206132448,
-42.5812778398568));
#37577=CARTESIAN_POINT('Ctrl Pts',(-6.25371475961217,-2.59234631320595,
-42.572218651392));
#37578=CARTESIAN_POINT('Ctrl Pts',(-6.17512908234659,-2.76768311342853,
-42.5631594629273));
#37579=CARTESIAN_POINT('Ctrl Pts',(-6.09654340508099,-2.94301991365113,
-42.5541002744626));
#37580=CARTESIAN_POINT('Ctrl Pts',(-6.01053390466334,-3.11489893486343,
-42.5450410859978));
#37581=CARTESIAN_POINT('Ctrl Pts',(-5.91744409407422,-3.28270382360427,
-42.5359818975331));
#37582=CARTESIAN_POINT('Ctrl Pts',(-5.82451555505095,-3.45021800214824,
-42.5269384034768));
#37583=CARTESIAN_POINT('Ctrl Pts',(-5.72444634757235,-3.61382688557528,
-42.5178949094205));
#37584=CARTESIAN_POINT('Ctrl Pts',(-5.61757415184038,-3.77294972780911,
-42.5088514153642));
#37585=CARTESIAN_POINT('Ctrl Pts',(-5.51079971171513,-3.93192702096089,
-42.4998161933589));
#37586=CARTESIAN_POINT('Ctrl Pts',(-5.39723483954908,-4.08642626782691,
-42.4907809713536));
#37587=CARTESIAN_POINT('Ctrl Pts',(-5.27726104762888,-4.23589480926745,
-42.4817457493482));
#37588=CARTESIAN_POINT('Ctrl Pts',(-5.15749862341199,-4.38510001967699,
-42.4727264454371));
#37589=CARTESIAN_POINT('Ctrl Pts',(-5.03134997524593,-4.52929203755353,
-42.463707141526));
#37590=CARTESIAN_POINT('Ctrl Pts',(-4.89923734187563,-4.66795056400252,
-42.4546878376149));
#37591=CARTESIAN_POINT('Ctrl Pts',(-4.76729045303197,-4.80643513364477,
-42.4456798490505));
#37592=CARTESIAN_POINT('Ctrl Pts',(-4.62939467470237,-4.93939989414737,
-42.4366718604862));
#37593=CARTESIAN_POINT('Ctrl Pts',(-4.48601128163889,-5.0663588286864,-42.4276638719218));
#37594=CARTESIAN_POINT('Ctrl Pts',(-4.34295172499068,-5.19303102202501,
-42.4186762282152));
#37595=CARTESIAN_POINT('Ctrl Pts',(-4.1944294710317,-5.31372430757826,-42.4096885845085));
#37596=CARTESIAN_POINT('Ctrl Pts',(-4.04094090057139,-5.42799093938902,
-42.4007009408018));
#37597=CARTESIAN_POINT('Ctrl Pts',(-3.90726299401948,-5.52750925585644,
-42.3928733260684));
#37598=CARTESIAN_POINT('Ctrl Pts',(-3.76981868177484,-5.62215328418074,
-42.385045711335));
#37599=CARTESIAN_POINT('Ctrl Pts',(-3.62895815416694,-5.71165052461242,
-42.3772180966016));
#37600=CARTESIAN_POINT('Ctrl Pts',(-3.48277921927813,-5.80452687190402,
-42.3690949381563));
#37601=CARTESIAN_POINT('Ctrl Pts',(-3.33298567607144,-5.89181751558342,
-42.360971779711));
#37602=CARTESIAN_POINT('Ctrl Pts',(-3.18005113614904,-5.97323729408745,
-42.3528486212657));
#37603=CARTESIAN_POINT('Ctrl Pts',(-3.02712737891212,-6.05465133207098,
-42.3447260355456));
#37604=CARTESIAN_POINT('Ctrl Pts',(-2.87106338916982,-6.13019515737294,
-42.3366034498255));
#37605=CARTESIAN_POINT('Ctrl Pts',(-2.71235758847528,-6.19962944959137,
-42.3284808641054));
#37606=CARTESIAN_POINT('Ctrl Pts',(-2.55363271764498,-6.2690720850548,-42.3203573023729));
#37607=CARTESIAN_POINT('Ctrl Pts',(-2.39226573957205,-6.33240358001369,
-42.3122337406405));
#37608=CARTESIAN_POINT('Ctrl Pts',(-2.22877521931706,-6.38943268387407,
-42.3041101789081));
#37609=CARTESIAN_POINT('Ctrl Pts',(-2.0651656156194,-6.446503326669,-42.295980700125));
#37610=CARTESIAN_POINT('Ctrl Pts',(-1.89942972642979,-6.49726228916622,
-42.2878512213419));
#37611=CARTESIAN_POINT('Ctrl Pts',(-1.73210206303117,-6.5415679651933,-42.2797217425588));
#37612=CARTESIAN_POINT('Ctrl Pts',(-1.56470618308922,-6.58589170386469,
-42.2715889495302));
#37613=CARTESIAN_POINT('Ctrl Pts',(-1.39571759232527,-6.62375683194439,
-42.2634561565017));
#37614=CARTESIAN_POINT('Ctrl Pts',(-1.22568091913084,-6.65507289850972,
-42.2553233634732));
#37615=CARTESIAN_POINT('Ctrl Pts',(-1.05545935685015,-6.68642301654657,
-42.247181727266));
#37616=CARTESIAN_POINT('Ctrl Pts',(-0.884187797736653,-6.71120979758355,
-42.2390400910589));
#37617=CARTESIAN_POINT('Ctrl Pts',(-0.712416664214558,-6.72939458618303,
-42.2308984548517));
#37618=CARTESIAN_POINT('Ctrl Pts',(-0.624901604834175,-6.7386594889724,
-42.2267504017912));
#37619=CARTESIAN_POINT('Ctrl Pts',(-0.537256897755374,-6.74621150705939,
-42.2226023487306));
#37620=CARTESIAN_POINT('Ctrl Pts',(-0.449555269251508,-6.75205072995518,
-42.2184542956701));
#37621=CARTESIAN_POINT('Ctrl Pts',(-0.271094570097564,-6.76393274193459,
-42.210013580692));
#37622=CARTESIAN_POINT('Ctrl Pts',(-0.0920306537212925,-6.76874397692548,
-42.2015728657139));
#37623=CARTESIAN_POINT('Ctrl Pts',(0.0870513340642555,-6.76644005849735,
-42.1931321507358));
#37624=CARTESIAN_POINT('Ctrl Pts',(0.265997963246156,-6.76413788147932,
-42.1846978156478));
#37625=CARTESIAN_POINT('Ctrl Pts',(0.444962304415066,-6.75473127597216,
-42.1762634805598));
#37626=CARTESIAN_POINT('Ctrl Pts',(0.623357093569214,-6.7382278778546,-42.1678291454718));
#37627=CARTESIAN_POINT('Ctrl Pts',(0.801644438093079,-6.72173441949772,
-42.1593998902631));
#37628=CARTESIAN_POINT('Ctrl Pts',(0.979362583322044,-6.69815272062077,
-42.1509706350545));
#37629=CARTESIAN_POINT('Ctrl Pts',(1.15592687335167,-6.66754243057091,-42.1425413798459));
#37630=CARTESIAN_POINT('Ctrl Pts',(1.33241190486665,-6.63694588127306,-42.1341159084729));
#37631=CARTESIAN_POINT('Ctrl Pts',(1.50774378596651,-6.59932708857285,-42.1256904370999));
#37632=CARTESIAN_POINT('Ctrl Pts',(1.68134517528666,-6.55479728149851,-42.1172649657268));
#37633=CARTESIAN_POINT('Ctrl Pts',(1.85489524299981,-6.51028063872699,-42.1088419851676));
#37634=CARTESIAN_POINT('Ctrl Pts',(2.02671551653271,-6.45885713873426,-42.1004190046083));
#37635=CARTESIAN_POINT('Ctrl Pts',(2.19624061559875,-6.40068872531655,-42.0919960240491));
#37636=CARTESIAN_POINT('Ctrl Pts',(2.36576852164858,-6.34251934875065,-42.0835729040228));
#37637=CARTESIAN_POINT('Ctrl Pts',(2.53300085986972,-6.27760493755164,-42.0751497839965));
#37638=CARTESIAN_POINT('Ctrl Pts',(2.69738849777813,-6.20615696643698,-42.0667266639701));
#37639=CARTESIAN_POINT('Ctrl Pts',(2.86178182048514,-6.13470652453235,-42.0583032526583));
#37640=CARTESIAN_POINT('Ctrl Pts',(3.0233299408013,-6.05672220499835,-42.0498798413464));
#37641=CARTESIAN_POINT('Ctrl Pts',(3.18150461990584,-5.97246325677419,-42.0414564300346));
#37642=CARTESIAN_POINT('Ctrl Pts',(3.33970682874089,-5.88818964358501,-42.0330315526585));
#37643=CARTESIAN_POINT('Ctrl Pts',(3.49453413146048,-5.79763938121708,-42.0246066752823));
#37644=CARTESIAN_POINT('Ctrl Pts',(3.64548344457245,-5.70111738656101,-42.0161817979062));
#37645=CARTESIAN_POINT('Ctrl Pts',(3.79648008846895,-5.60456512703233,-42.0077542788748));
#37646=CARTESIAN_POINT('Ctrl Pts',(3.94359603761136,-5.5020375816183,-41.9993267598434));
#37647=CARTESIAN_POINT('Ctrl Pts',(4.08635741077098,-5.39388284183455,-41.9908992408119));
#37648=CARTESIAN_POINT('Ctrl Pts',(4.22924680681245,-5.28563111306024,-41.9824641643072));
#37649=CARTESIAN_POINT('Ctrl Pts',(4.36777355801776,-5.17174230835793,-41.9740290878024));
#37650=CARTESIAN_POINT('Ctrl Pts',(4.50149620337621,-5.0526053607015,-41.9655940112976));
#37651=CARTESIAN_POINT('Ctrl Pts',(4.63528347776928,-4.93341083337415,-41.9571548580648));
#37652=CARTESIAN_POINT('Ctrl Pts',(4.76426177222556,-4.80896333213209,-41.948715704832));
#37653=CARTESIAN_POINT('Ctrl Pts',(4.88802633549392,-4.67968882977468,-41.9402765515993));
#37654=CARTESIAN_POINT('Ctrl Pts',(5.01192843589208,-4.55027066720032,-41.9318280201011));
#37655=CARTESIAN_POINT('Ctrl Pts',(5.13060500335559,-4.41601503165668,-41.923379488603));
#37656=CARTESIAN_POINT('Ctrl Pts',(5.24369064745112,-4.27738207246368,-41.9149309571049));
#37657=CARTESIAN_POINT('Ctrl Pts',(5.30617413488637,-4.20078286455247,-41.910262869339));
#37658=CARTESIAN_POINT('Ctrl Pts',(5.36695149572751,-4.12284785073278,-41.905594781573));
#37659=CARTESIAN_POINT('Ctrl Pts',(5.42596674891508,-4.04365847218431,-41.900926693807));
#37660=CARTESIAN_POINT('Ctrl Pts',(5.53014890715346,-3.90386206496541,-41.8926859182103));
#37661=CARTESIAN_POINT('Ctrl Pts',(5.62906881304512,-3.75984380107845,-41.8844451426135));
#37662=CARTESIAN_POINT('Ctrl Pts',(5.72236768346778,-3.61203503515728,-41.8762043670168));
#37663=CARTESIAN_POINT('Ctrl Pts',(5.8155632152766,-3.46438998346879,-41.8679727189724));
#37664=CARTESIAN_POINT('Ctrl Pts',(5.90314992029334,-3.31296308773015,-41.859741070928));
#37665=CARTESIAN_POINT('Ctrl Pts',(5.9848098138501,-3.15821792978945,-41.8515094228837));
#37666=CARTESIAN_POINT('Ctrl Pts',(6.06639381277728,-3.00361659185548,-41.8432854253254));
#37667=CARTESIAN_POINT('Ctrl Pts',(6.14206180527136,-2.84570344639689,-41.8350614277671));
#37668=CARTESIAN_POINT('Ctrl Pts',(6.21153957002151,-2.68497023634471,-41.8268374302088));
#37669=CARTESIAN_POINT('Ctrl Pts',(6.28095595089663,-2.52437903470798,-41.8186206985843));
#37670=CARTESIAN_POINT('Ctrl Pts',(6.34419286387446,-2.36097305971089,-41.8104039669598));
#37671=CARTESIAN_POINT('Ctrl Pts',(6.40102248589785,-2.19526766819678,-41.8021872353353));
#37672=CARTESIAN_POINT('Ctrl Pts',(6.45782299200198,-2.02964717368934,-41.7939747134466));
#37673=CARTESIAN_POINT('Ctrl Pts',(6.50822262984406,-1.86172994464453,-41.785762191558));
#37674=CARTESIAN_POINT('Ctrl Pts',(6.552041934908,-1.69205067394776,-41.7775496696693));
#37675=CARTESIAN_POINT('Ctrl Pts',(6.5958465865854,-1.52242814481584,-41.7693398940874));
#37676=CARTESIAN_POINT('Ctrl Pts',(6.63307520026661,-1.35104509196461,-41.7611301185056));
#37677=CARTESIAN_POINT('Ctrl Pts',(6.66359833152834,-1.17845079492218,-41.7529203429237));
#37678=CARTESIAN_POINT('Ctrl Pts',(6.67693004226706,-1.10306609000473,-41.749334526241));
#37679=CARTESIAN_POINT('Ctrl Pts',(6.68898318843072,-1.02745047825498,-41.7457487095583));
#37680=CARTESIAN_POINT('Ctrl Pts',(6.69975003711949,-0.951650377038417,
-41.7421628928756));
#37681=CARTESIAN_POINT('Ctrl Pts',(6.72634940891484,-0.764387127348094,
-41.7333041753538));
#37682=CARTESIAN_POINT('Ctrl Pts',(6.74506725240592,-0.576191466641557,
-41.7244454578321));
#37683=CARTESIAN_POINT('Ctrl Pts',(6.75588373128169,-0.387716403319989,
-41.7155867403103));
#37684=CARTESIAN_POINT('Ctrl Pts',(6.76672044605221,-0.198888733425766,
-41.7067114495509));
#37685=CARTESIAN_POINT('Ctrl Pts',(6.7696262401614,-0.00978087522273441,
-41.6978361587914));
#37686=CARTESIAN_POINT('Ctrl Pts',(6.76463333577029,0.178954833925484,-41.6889608680319));
#37687=CARTESIAN_POINT('Ctrl Pts',(6.75962625040808,0.368226594923957,-41.6800603694512));
#37688=CARTESIAN_POINT('Ctrl Pts',(6.74667558010456,0.55712383083115,-41.6711598708704));
#37689=CARTESIAN_POINT('Ctrl Pts',(6.72586564017671,0.744996906228688,-41.6622593722896));
#37690=CARTESIAN_POINT('Ctrl Pts',(6.70502752980533,0.933124305659871,-41.653346825092));
#37691=CARTESIAN_POINT('Ctrl Pts',(6.6763089326328,1.12022451814475,-41.6444342778944));
#37692=CARTESIAN_POINT('Ctrl Pts',(6.6398454633218,1.30565739120373,-41.6355217306967));
#37693=CARTESIAN_POINT('Ctrl Pts',(6.6033014791094,1.49149971815651,-41.6265895037245));
#37694=CARTESIAN_POINT('Ctrl Pts',(6.55897846730552,1.67566708626609,-41.6176572767522));
#37695=CARTESIAN_POINT('Ctrl Pts',(6.50706289319567,1.85753102369678,-41.6087250497799));
#37696=CARTESIAN_POINT('Ctrl Pts',(6.4579966806668,2.02941344546159,-41.6002830638347));
#37697=CARTESIAN_POINT('Ctrl Pts',(6.40214894479632,2.19923830639945,-41.5918410778894));
#37698=CARTESIAN_POINT('Ctrl Pts',(6.33971681340197,2.36649101537877,-41.5833990919441));
#37699=CARTESIAN_POINT('Ctrl Pts',(6.2788864724797,2.52945260390952,-41.5751736978778));
#37700=CARTESIAN_POINT('Ctrl Pts',(6.21168807255892,2.69028331838405,-41.5669483038116));
#37701=CARTESIAN_POINT('Ctrl Pts',(6.13829108938444,2.84845071959892,-41.5587229097454));
#37702=CARTESIAN_POINT('Ctrl Pts',(6.06497432842782,3.00644524531988,-41.5505065059581));
#37703=CARTESIAN_POINT('Ctrl Pts',(5.985472627089,3.16178193241649,-41.5422901021709));
#37704=CARTESIAN_POINT('Ctrl Pts',(5.90000456429368,3.31394555497126,-41.5340736983836));
#37705=CARTESIAN_POINT('Ctrl Pts',(5.81462748643463,3.46594719190184,-41.5258660413603));
#37706=CARTESIAN_POINT('Ctrl Pts',(5.72329688111432,3.61478218583412,-41.5176583843371));
#37707=CARTESIAN_POINT('Ctrl Pts',(5.62627842502757,3.75995745774727,-41.5094507273138));
#37708=CARTESIAN_POINT('Ctrl Pts',(5.52931891580423,3.90504452348535,-41.5012480571318));
#37709=CARTESIAN_POINT('Ctrl Pts',(5.42667863579515,4.04647599795403,-41.4930453869498));
#37710=CARTESIAN_POINT('Ctrl Pts',(5.31866823445393,4.18378503413007,-41.4848427167678));
#37711=CARTESIAN_POINT('Ctrl Pts',(5.21070383673897,4.32103558784976,-41.4766435402546));
#37712=CARTESIAN_POINT('Ctrl Pts',(5.09737409444621,4.45416691912772,-41.4684443637414));
#37713=CARTESIAN_POINT('Ctrl Pts',(4.97903189103809,4.58274267530107,-41.4602451872282));
#37714=CARTESIAN_POINT('Ctrl Pts',(4.8607185942922,4.7112870251304,-41.4520480134733));
#37715=CARTESIAN_POINT('Ctrl Pts',(4.73739551863087,4.83527775352706,-41.4438508397184));
#37716=CARTESIAN_POINT('Ctrl Pts',(4.60945463056433,4.95431297040962,-41.4356536659635));
#37717=CARTESIAN_POINT('Ctrl Pts',(4.48149343125921,5.07336708471214,-41.4274551908673));
#37718=CARTESIAN_POINT('Ctrl Pts',(4.3489132137002,5.18746386741849,-41.4192567157712));
#37719=CARTESIAN_POINT('Ctrl Pts',(4.21214178388496,5.29623928768805,-41.411058240675));
#37720=CARTESIAN_POINT('Ctrl Pts',(4.07535939164419,5.40502342646298,-41.4028591084594));
#37721=CARTESIAN_POINT('Ctrl Pts',(3.93438540207997,5.50848513434416,-41.3946599762438));
#37722=CARTESIAN_POINT('Ctrl Pts',(3.78967927024918,5.60630181390938,-41.3864608440281));
#37723=CARTESIAN_POINT('Ctrl Pts',(3.64488903257014,5.70417534631632,-41.378256946327));
#37724=CARTESIAN_POINT('Ctrl Pts',(3.49636262006873,5.79639710062467,-41.3700530486259));
#37725=CARTESIAN_POINT('Ctrl Pts',(3.34458741463909,5.88268850321329,-41.3618491509248));
#37726=CARTESIAN_POINT('Ctrl Pts',(3.26365133982806,5.92870450033015,-41.3574743172608));
#37727=CARTESIAN_POINT('Ctrl Pts',(3.18179184063274,5.97303486141136,-41.3530994835967));
#37728=CARTESIAN_POINT('Ctrl Pts',(3.09908550384719,6.01564277861013,-41.3487246499327));
#37729=CARTESIAN_POINT('Origin',(0.,0.,-63.6971797838103));
#37730=CARTESIAN_POINT('',(3.0990855038472,6.01564277861013,-38.9542099095282));
#37731=CARTESIAN_POINT('',(3.09908550384721,6.01564277861012,-39.3484860224351));
#37732=CARTESIAN_POINT('',(3.09908550384721,6.01564277861012,-63.6971797838103));
#37733=CARTESIAN_POINT('',(-6.76699799023945,0.00521537105487791,-40.3028202161432));
#37734=CARTESIAN_POINT('Ctrl Pts',(-6.76699799023945,0.00521537105492299,
-40.3028202161432));
#37735=CARTESIAN_POINT('Ctrl Pts',(-6.76712754022321,-0.162877075380806,
-40.2948963058703));
#37736=CARTESIAN_POINT('Ctrl Pts',(-6.76098983979437,-0.33122543153812,
-40.2869723955973));
#37737=CARTESIAN_POINT('Ctrl Pts',(-6.74855428627843,-0.499303560124519,
-40.2790484853244));
#37738=CARTESIAN_POINT('Ctrl Pts',(-6.73559519402501,-0.674457804070364,
-40.2707909771963));
#37739=CARTESIAN_POINT('Ctrl Pts',(-6.715796363107,-0.849318163805499,-40.2625334690682));
#37740=CARTESIAN_POINT('Ctrl Pts',(-6.6891833820932,-1.02328621642635,-40.2542759609401));
#37741=CARTESIAN_POINT('Ctrl Pts',(-6.66368313374093,-1.18998037762888,
-40.2463637128561));
#37742=CARTESIAN_POINT('Ctrl Pts',(-6.63192704679351,-1.35585490386659,
-40.238451464772));
#37743=CARTESIAN_POINT('Ctrl Pts',(-6.59399069768826,-1.52038668726107,
-40.230539216688));
#37744=CARTESIAN_POINT('Ctrl Pts',(-6.55606781177178,-1.68486008015379,
-40.2226297765729));
#37745=CARTESIAN_POINT('Ctrl Pts',(-6.51196911464742,-1.84799130365533,
-40.2147203364577));
#37746=CARTESIAN_POINT('Ctrl Pts',(-6.46182138259852,-2.00926688605388,
-40.2068108963426));
#37747=CARTESIAN_POINT('Ctrl Pts',(-6.41167809603406,-2.17052817173221,
-40.1989021573817));
#37748=CARTESIAN_POINT('Ctrl Pts',(-6.35548695491127,-2.32993377560291,
-40.1909934184208));
#37749=CARTESIAN_POINT('Ctrl Pts',(-6.29342468653699,-2.48698506527217,
-40.1830846794599));
#37750=CARTESIAN_POINT('Ctrl Pts',(-6.28524703420593,-2.50767897283795,
-40.1820425822357));
#37751=CARTESIAN_POINT('Ctrl Pts',(-6.27696751642473,-2.52833203012484,
-40.1810004850115));
#37752=CARTESIAN_POINT('Ctrl Pts',(-6.2685866004644,-2.5489431206832,-40.1799583877873));
#37753=CARTESIAN_POINT('Ctrl Pts',(-6.19734164812911,-2.72415501534487,
-40.1710996702656));
#37754=CARTESIAN_POINT('Ctrl Pts',(-6.11881653475247,-2.89620666730619,
-40.1622409527438));
#37755=CARTESIAN_POINT('Ctrl Pts',(-6.03332271373748,-3.06452378550069,
-40.1533822352221));
#37756=CARTESIAN_POINT('Ctrl Pts',(-5.94766894751403,-3.23315579799089,
-40.1445069444626));
#37757=CARTESIAN_POINT('Ctrl Pts',(-5.85502053688083,-3.39803908301622,
-40.1356316537032));
#37758=CARTESIAN_POINT('Ctrl Pts',(-5.75573358487283,-3.55862612534205,
-40.1267563629437));
#37759=CARTESIAN_POINT('Ctrl Pts',(-5.65616463559707,-3.71966927097509,
-40.1178558643629));
#37760=CARTESIAN_POINT('Ctrl Pts',(-5.54991955111832,-3.87639153365262,
-40.1089553657822));
#37761=CARTESIAN_POINT('Ctrl Pts',(-5.43739809211884,-4.02827394647166,
-40.1000548672014));
#37762=CARTESIAN_POINT('Ctrl Pts',(-5.32472431266944,-4.1803619627166,-40.0911423200038));
#37763=CARTESIAN_POINT('Ctrl Pts',(-5.20575734639003,-4.32759683721942,
-40.0822297728061));
#37764=CARTESIAN_POINT('Ctrl Pts',(-5.08093651341278,-4.46949361188365,
-40.0733172256085));
#37765=CARTESIAN_POINT('Ctrl Pts',(-4.95584006384608,-4.61170370848426,
-40.0643849986362));
#37766=CARTESIAN_POINT('Ctrl Pts',(-4.82486406561801,-4.74855193368263,
-40.0554527716639));
#37767=CARTESIAN_POINT('Ctrl Pts',(-4.68848590464814,-4.8795890115783,-40.0465205446917));
#37768=CARTESIAN_POINT('Ctrl Pts',(-4.55959279414736,-5.00343418180786,
-40.0380785587464));
#37769=CARTESIAN_POINT('Ctrl Pts',(-4.4258746730809,-5.12208879441507,-40.0296365728011));
#37770=CARTESIAN_POINT('Ctrl Pts',(-4.28776083656365,-5.23520735104456,
-40.0211945868558));
#37771=CARTESIAN_POINT('Ctrl Pts',(-4.15321374473151,-5.34540465792225,
-40.0129706124382));
#37772=CARTESIAN_POINT('Ctrl Pts',(-4.01423736702672,-5.45055785106176,
-40.0047466380206));
#37773=CARTESIAN_POINT('Ctrl Pts',(-3.87124586600751,-5.55029228463869,
-39.9965226636031));
#37774=CARTESIAN_POINT('Ctrl Pts',(-3.72840537788679,-5.64992138897727,
-39.9883073745004));
#37775=CARTESIAN_POINT('Ctrl Pts',(-3.58155850211936,-5.74414292619686,
-39.9800920853978));
#37776=CARTESIAN_POINT('Ctrl Pts',(-3.4311532002971,-5.83262177036116,-39.9718767962951));
#37777=CARTESIAN_POINT('Ctrl Pts',(-3.2808765729689,-5.92102491925163,-39.9636685355229));
#37778=CARTESIAN_POINT('Ctrl Pts',(-3.12704788995173,-6.00369497898534,
-39.9554602747507));
#37779=CARTESIAN_POINT('Ctrl Pts',(-2.97014495677272,-6.08033945892477,
-39.9472520139786));
#37780=CARTESIAN_POINT('Ctrl Pts',(-2.81334479450807,-6.15693373697744,
-39.9390491295907));
#37781=CARTESIAN_POINT('Ctrl Pts',(-2.65347471406588,-6.22751013988855,
-39.9308462452028));
#37782=CARTESIAN_POINT('Ctrl Pts',(-2.49103812149956,-6.29182152299602,
-39.9226433608149));
#37783=CARTESIAN_POINT('Ctrl Pts',(-2.32867535899208,-6.35610367553958,
-39.9144442047707));
#37784=CARTESIAN_POINT('Ctrl Pts',(-2.16374874110233,-6.41412634961514,
-39.9062450487264));
#37785=CARTESIAN_POINT('Ctrl Pts',(-1.99678278431146,-6.46569002599702,
-39.8980458926822));
#37786=CARTESIAN_POINT('Ctrl Pts',(-1.82983134949951,-6.51724921759269,
-39.8898474497652));
#37787=CARTESIAN_POINT('Ctrl Pts',(-1.66084126893709,-6.56235041658473,
-39.8816490068482));
#37788=CARTESIAN_POINT('Ctrl Pts',(-1.49035374915082,-6.60084348416111,
-39.8734505639312));
#37789=CARTESIAN_POINT('Ctrl Pts',(-1.3198679272181,-6.63933616839217,-39.865252202661));
#37790=CARTESIAN_POINT('Ctrl Pts',(-1.1478850454227,-6.67122077225602,-39.8570538413907));
#37791=CARTESIAN_POINT('Ctrl Pts',(-0.974957957846269,-6.69639798551671,
-39.8488554801205));
#37792=CARTESIAN_POINT('Ctrl Pts',(-0.802001178975093,-6.72157952166325,
-39.8406557112052));
#37793=CARTESIAN_POINT('Ctrl Pts',(-0.628100226299769,-6.74005132110533,
-39.8324559422899));
#37794=CARTESIAN_POINT('Ctrl Pts',(-0.453814608423492,-6.75176579134536,
-39.8242561733746));
#37795=CARTESIAN_POINT('Ctrl Pts',(-0.27946740543439,-6.76348440098014,
-39.8160535070103));
#37796=CARTESIAN_POINT('Ctrl Pts',(-0.104735624150543,-6.76844090092971,
-39.8078508406459));
#37797=CARTESIAN_POINT('Ctrl Pts',(0.06981962896297,-6.76663980269465,-39.7996481742816));
#37798=CARTESIAN_POINT('Ctrl Pts',(0.244573133213151,-6.76483665886219,
-39.7914361917386));
#37799=CARTESIAN_POINT('Ctrl Pts',(0.419149349707361,-6.75626058751377,
-39.7832242091956));
#37800=CARTESIAN_POINT('Ctrl Pts',(0.592989640392857,-6.74096820096244,
-39.7750122266526));
#37801=CARTESIAN_POINT('Ctrl Pts',(0.766932464431034,-6.72566679475486,
-39.7667954005713));
#37802=CARTESIAN_POINT('Ctrl Pts',(0.940138142190733,-6.70364122208695,
-39.75857857449));
#37803=CARTESIAN_POINT('Ctrl Pts',(1.11205676947754,-6.67499953119543,-39.7503617484087));
#37804=CARTESIAN_POINT('Ctrl Pts',(1.28424052011747,-6.64631367067989,-39.7421322507948));
#37805=CARTESIAN_POINT('Ctrl Pts',(1.4551329028892,-6.61099137519713,-39.733902753181));
#37806=CARTESIAN_POINT('Ctrl Pts',(1.62419645638245,-6.5691913407264,-39.7256732555671));
#37807=CARTESIAN_POINT('Ctrl Pts',(1.77489250438824,-6.53193257104429,-39.7183378320423));
#37808=CARTESIAN_POINT('Ctrl Pts',(1.9241355659828,-6.48952788029005,-39.7110024085175));
#37809=CARTESIAN_POINT('Ctrl Pts',(2.07155830167241,-6.44212194876596,-39.7036669849927));
#37810=CARTESIAN_POINT('Ctrl Pts',(2.23376158253994,-6.38996311729522,-39.6955961148063));
#37811=CARTESIAN_POINT('Ctrl Pts',(2.39428981073306,-6.3315789062554,-39.6875252446199));
#37812=CARTESIAN_POINT('Ctrl Pts',(2.55261704114451,-6.26709144988795,-39.6794543744335));
#37813=CARTESIAN_POINT('Ctrl Pts',(2.71074724562398,-6.20268424314755,-39.6713935478177));
#37814=CARTESIAN_POINT('Ctrl Pts',(2.86668156109682,-6.13218904221026,-39.663332721202));
#37815=CARTESIAN_POINT('Ctrl Pts',(3.01990695852402,-6.05577831181577,-39.6552718945862));
#37816=CARTESIAN_POINT('Ctrl Pts',(3.17297527884556,-5.97944591292879,-39.6472193314263));
#37817=CARTESIAN_POINT('Ctrl Pts',(3.32333987649275,-5.89721021769609,-39.6391667682664));
#37818=CARTESIAN_POINT('Ctrl Pts',(3.4705056479343,-5.80929251696419,-39.6311142051065));
#37819=CARTESIAN_POINT('Ctrl Pts',(3.61755277806687,-5.72144569325074,-39.6230681337186));
#37820=CARTESIAN_POINT('Ctrl Pts',(3.76140589614113,-5.62792617154377,-39.6150220623308));
#37821=CARTESIAN_POINT('Ctrl Pts',(3.90159265552522,-5.52900205736548,-39.6069759909429));
#37822=CARTESIAN_POINT('Ctrl Pts',(4.04169706415997,-5.43013605477323,-39.598934646107));
#37823=CARTESIAN_POINT('Ctrl Pts',(4.17813909763124,-5.32587199447616,-39.5908933012711));
#37824=CARTESIAN_POINT('Ctrl Pts',(4.31047376756382,-5.2165222993048,-39.5828519564352));
#37825=CARTESIAN_POINT('Ctrl Pts',(4.44535944273825,-5.10506467848009,-39.5746555992142));
#37826=CARTESIAN_POINT('Ctrl Pts',(4.57597744504392,-4.98832355638715,-39.5664592419931));
#37827=CARTESIAN_POINT('Ctrl Pts',(4.70188996882324,-4.86667440056137,-39.558262884772));
#37828=CARTESIAN_POINT('Ctrl Pts',(4.82538192349467,-4.74736385395217,-39.5502240960636));
#37829=CARTESIAN_POINT('Ctrl Pts',(4.94434741386688,-4.6233325525606,-39.5421853073551));
#37830=CARTESIAN_POINT('Ctrl Pts',(5.05840932216131,-4.49497320675792,-39.5341465186466));
#37831=CARTESIAN_POINT('Ctrl Pts',(5.17248343611352,-4.36660012534208,-39.5261068697149));
#37832=CARTESIAN_POINT('Ctrl Pts',(5.28165267500553,-4.23389835645969,-39.5180672207831));
#37833=CARTESIAN_POINT('Ctrl Pts',(5.38557929067777,-4.09729480313813,-39.5100275718514));
#37834=CARTESIAN_POINT('Ctrl Pts',(5.48953760530579,-3.9606495839741,-39.5019854707233));
#37835=CARTESIAN_POINT('Ctrl Pts',(5.58824988777376,-3.82010050855278,-39.4939433695951));
#37836=CARTESIAN_POINT('Ctrl Pts',(5.68142100308067,-3.6761045123546,-39.485901268467));
#37837=CARTESIAN_POINT('Ctrl Pts',(5.77773627747091,-3.52724921702795,-39.4775877780222));
#37838=CARTESIAN_POINT('Ctrl Pts',(5.86812961838286,-3.37471065711725,-39.4692742875774));
#37839=CARTESIAN_POINT('Ctrl Pts',(5.95232643524389,-3.21902143644568,-39.4609607971326));
#37840=CARTESIAN_POINT('Ctrl Pts',(6.03391817342702,-3.06814929418955,-39.4529045289619));
#37841=CARTESIAN_POINT('Ctrl Pts',(6.10969102577833,-2.91431891546404,-39.4448482607911));
#37842=CARTESIAN_POINT('Ctrl Pts',(6.17944429363589,-2.75803502911961,-39.4367919926203));
#37843=CARTESIAN_POINT('Ctrl Pts',(6.25253820764567,-2.59426634414703,-39.4283498910386));
#37844=CARTESIAN_POINT('Ctrl Pts',(6.31902159426447,-2.42780381573808,-39.4199077894568));
#37845=CARTESIAN_POINT('Ctrl Pts',(6.37872252447252,-2.25924499684892,-39.4114656878751));
#37846=CARTESIAN_POINT('Ctrl Pts',(6.43842345468058,-2.09068617795977,-39.4030235862933));
#37847=CARTESIAN_POINT('Ctrl Pts',(6.49134187456447,-1.92003153439721,-39.3945814847115));
#37848=CARTESIAN_POINT('Ctrl Pts',(6.53736745489061,-1.74788894376531,-39.3861393831297));
#37849=CARTESIAN_POINT('Ctrl Pts',(6.58280281746738,-1.57795385625877,-39.3778055404371));
#37850=CARTESIAN_POINT('Ctrl Pts',(6.62166609770372,-1.40602866319757,-39.3694716977444));
#37851=CARTESIAN_POINT('Ctrl Pts',(6.65378441784946,-1.23265644880628,-39.3611378550517));
#37852=CARTESIAN_POINT('Ctrl Pts',(6.68586488249151,-1.05948857550362,-39.352813834847));
#37853=CARTESIAN_POINT('Ctrl Pts',(6.71121616091981,-0.884877417489458,
-39.3444898146423));
#37854=CARTESIAN_POINT('Ctrl Pts',(6.72971532596606,-0.709380456072482,
-39.3361657944375));
#37855=CARTESIAN_POINT('Ctrl Pts',(6.74819607920109,-0.534058162912889,
-39.3278500589466));
#37856=CARTESIAN_POINT('Ctrl Pts',(6.75983827004864,-0.357852166613005,
-39.3195343234557));
#37857=CARTESIAN_POINT('Ctrl Pts',(6.76457009572151,-0.181329589616151,
-39.3112185879649));
#37858=CARTESIAN_POINT('Ctrl Pts',(6.76929807890517,-0.00495035815688297,
-39.3029096052848));
#37859=CARTESIAN_POINT('Ctrl Pts',(6.76712686923503,0.171744595524779,-39.2946006226048));
#37860=CARTESIAN_POINT('Ctrl Pts',(6.75803650121376,0.348183354373005,-39.2862916399247));
#37861=CARTESIAN_POINT('Ctrl Pts',(6.7489518503696,0.524511146137264,-39.2779878829875));
#37862=CARTESIAN_POINT('Ctrl Pts',(6.73295673138763,0.700582717780264,-39.2696841260503));
#37863=CARTESIAN_POINT('Ctrl Pts',(6.710083261767,0.875826249980194,-39.2613803691131));
#37864=CARTESIAN_POINT('Ctrl Pts',(6.68721907822373,1.05099863752983,-39.2530799833011));
#37865=CARTESIAN_POINT('Ctrl Pts',(6.65748215314951,1.22534331112235,-39.244779597489));
#37866=CARTESIAN_POINT('Ctrl Pts',(6.62095647461996,1.39829337450625,-39.236479211677));
#37867=CARTESIAN_POINT('Ctrl Pts',(6.58443849840557,1.57120696722212,-39.2281805762004));
#37868=CARTESIAN_POINT('Ctrl Pts',(6.5411346925989,1.74272619553313,-39.2198819407237));
#37869=CARTESIAN_POINT('Ctrl Pts',(6.49118024488089,1.91229391790805,-39.2115833052471));
#37870=CARTESIAN_POINT('Ctrl Pts',(6.44122803939115,2.08185402915806,-39.2032850422585));
#37871=CARTESIAN_POINT('Ctrl Pts',(6.38462588530303,2.24946247548421,-39.1949867792699));
#37872=CARTESIAN_POINT('Ctrl Pts',(6.3215590270979,2.41457666412088,-39.1866885162813));
#37873=CARTESIAN_POINT('Ctrl Pts',(6.25848453176547,2.57971084738092,-39.1783892484085));
#37874=CARTESIAN_POINT('Ctrl Pts',(6.18894389704812,2.74234984643531,-39.1700899805357));
#37875=CARTESIAN_POINT('Ctrl Pts',(6.11317082247102,2.90197027815397,-39.1617907126628));
#37876=CARTESIAN_POINT('Ctrl Pts',(6.03734454298267,3.06170278914287,-39.1534856173663));
#37877=CARTESIAN_POINT('Ctrl Pts',(5.95527722858991,3.21841218305704,-39.1451805220698));
#37878=CARTESIAN_POINT('Ctrl Pts',(5.86724934654525,3.37159815302245,-39.1368754267733));
#37879=CARTESIAN_POINT('Ctrl Pts',(5.77918936495744,3.52483998255801,-39.1285673030072));
#37880=CARTESIAN_POINT('Ctrl Pts',(5.68516466323755,3.67455552950446,-39.1202591792411));
#37881=CARTESIAN_POINT('Ctrl Pts',(5.58549963236082,3.82027261552067,-39.111951055475));
#37882=CARTESIAN_POINT('Ctrl Pts',(5.48572865813215,3.96614459795734,-39.1036341002213));
#37883=CARTESIAN_POINT('Ctrl Pts',(5.38030557814278,4.10800934435273,-39.0953171449676));
#37884=CARTESIAN_POINT('Ctrl Pts',(5.26959639949399,4.24542610187011,-39.0870001897139));
#37885=CARTESIAN_POINT('Ctrl Pts',(5.18800541923077,4.34670016141312,-39.0808707202315));
#37886=CARTESIAN_POINT('Ctrl Pts',(5.10354417342413,4.44555897920631,-39.0747412507491));
#37887=CARTESIAN_POINT('Ctrl Pts',(5.01637213175427,4.54183879455877,-39.0686117812667));
#37888=CARTESIAN_POINT('Ctrl Pts',(4.89616454163102,4.6746057271593,-39.0601594295596));
#37889=CARTESIAN_POINT('Ctrl Pts',(4.77058116702232,4.80270984526433,-39.0517070778525));
#37890=CARTESIAN_POINT('Ctrl Pts',(4.64000953199913,4.9257081260421,-39.0432547261455));
#37891=CARTESIAN_POINT('Ctrl Pts',(4.50958742826625,5.04856554857278,-39.0348120541139));
#37892=CARTESIAN_POINT('Ctrl Pts',(4.3741886985638,5.16632857020355,-39.0263693820823));
#37893=CARTESIAN_POINT('Ctrl Pts',(4.23423858843679,5.27859001781658,-39.0179267100508));
#37894=CARTESIAN_POINT('Ctrl Pts',(4.09438353268352,5.39077521724668,-39.0094897722977));
#37895=CARTESIAN_POINT('Ctrl Pts',(3.94998351461975,5.49746608262539,-39.0010528345446));
#37896=CARTESIAN_POINT('Ctrl Pts',(3.80149853946319,5.59829419148898,-38.9926158967915));
#37897=CARTESIAN_POINT('Ctrl Pts',(3.6531119608367,5.69905548459539,-38.9841845499434));
#37898=CARTESIAN_POINT('Ctrl Pts',(3.50064609711128,5.79396158332724,-38.9757532030954));
#37899=CARTESIAN_POINT('Ctrl Pts',(3.34459189983079,5.88268595316683,-38.9673218562474));
#37900=CARTESIAN_POINT('Ctrl Pts',(3.26369638942458,5.92867896911078,-38.962951207341));
#37901=CARTESIAN_POINT('Ctrl Pts',(3.18183712474675,5.97301153234306,-38.9585805584346));
#37902=CARTESIAN_POINT('Ctrl Pts',(3.0990855038472,6.01564277861013,-38.9542099095282));
#37903=CARTESIAN_POINT('Ctrl Pts',(3.09908550384721,6.01564277861012,-40.9541976313953));
#37904=CARTESIAN_POINT('Ctrl Pts',(2.92882846838773,6.10335428840864,-40.945159916578));
#37905=CARTESIAN_POINT('Ctrl Pts',(2.75478964636869,6.18386283890986,-40.9361222017608));
#37906=CARTESIAN_POINT('Ctrl Pts',(2.57757057627381,6.25686973848166,-40.9270844869435));
#37907=CARTESIAN_POINT('Ctrl Pts',(2.39443892302602,6.33231237684965,-40.9177452456576));
#37908=CARTESIAN_POINT('Ctrl Pts',(2.20791136910832,6.39974403881214,-40.9084060043718));
#37909=CARTESIAN_POINT('Ctrl Pts',(2.01867762557476,6.45888764757554,-40.8990667630859));
#37910=CARTESIAN_POINT('Ctrl Pts',(1.83609765572756,6.51595166852147,-40.8900559050829));
#37911=CARTESIAN_POINT('Ctrl Pts',(1.65099880494576,6.56530041468836,-40.8810450470798));
#37912=CARTESIAN_POINT('Ctrl Pts',(1.46402058189181,6.60673389321813,-40.8720341890768));
#37913=CARTESIAN_POINT('Ctrl Pts',(1.27729665572115,6.64811102077674,-40.8630355861539));
#37914=CARTESIAN_POINT('Ctrl Pts',(1.08869868941265,6.68159430937247,-40.854036983231));
#37915=CARTESIAN_POINT('Ctrl Pts',(0.898879886899542,6.70703391589214,-40.845038380308));
#37916=CARTESIAN_POINT('Ctrl Pts',(0.709452354237807,6.73242108423957,-40.8360583260325));
#37917=CARTESIAN_POINT('Ctrl Pts',(0.518809243438361,6.74979762800268,-40.8270782717569));
#37918=CARTESIAN_POINT('Ctrl Pts',(0.327612572950701,6.75906495027564,-40.8180982174814));
#37919=CARTESIAN_POINT('Ctrl Pts',(0.305720715110656,6.76012605087556,-40.8170700088253));
#37920=CARTESIAN_POINT('Ctrl Pts',(0.283821611724741,6.76108089412076,-40.8160418001693));
#37921=CARTESIAN_POINT('Ctrl Pts',(0.261916265177378,6.76192937481867,-40.8150135915133));
#37922=CARTESIAN_POINT('Ctrl Pts',(0.0888574217582246,6.76863262819677,
-40.806890433068));
#37923=CARTESIAN_POINT('Ctrl Pts',(-0.0845143140218471,6.76869001244394,
-40.7987672746227));
#37924=CARTESIAN_POINT('Ctrl Pts',(-0.257646167912469,6.76209342231827,
-40.7906441161774));
#37925=CARTESIAN_POINT('Ctrl Pts',(-0.430765815101109,6.75549729728674,
-40.7825215304573));
#37926=CARTESIAN_POINT('Ctrl Pts',(-0.603645248330071,6.74224814629945,
-40.7743989447372));
#37927=CARTESIAN_POINT('Ctrl Pts',(-0.77573332074428,6.72238996303302,-40.7662763590171));
#37928=CARTESIAN_POINT('Ctrl Pts',(-0.947842071311835,6.70252939360145,
-40.7581527972847));
#37929=CARTESIAN_POINT('Ctrl Pts',(-1.11915890825157,6.67605825371389,-40.7500292355523));
#37930=CARTESIAN_POINT('Ctrl Pts',(-1.28913946615814,6.64307221372713,-40.7419056738199));
#37931=CARTESIAN_POINT('Ctrl Pts',(-1.45924383473007,6.6100621473246,-40.7337761950368));
#37932=CARTESIAN_POINT('Ctrl Pts',(-1.62800962060493,6.57052777294826,-40.7256467162537));
#37933=CARTESIAN_POINT('Ctrl Pts',(-1.79490365933834,6.52461568628328,-40.7175172374706));
#37934=CARTESIAN_POINT('Ctrl Pts',(-1.96186573783402,6.47868488206861,-40.709384444442));
#37935=CARTESIAN_POINT('Ctrl Pts',(-2.1269541994697,6.42637129332055,-40.7012516514135));
#37936=CARTESIAN_POINT('Ctrl Pts',(-2.28965287835159,6.36787081343963,-40.693118858385));
#37937=CARTESIAN_POINT('Ctrl Pts',(-2.45252846736403,6.30930672316185,-40.6849772221778));
#37938=CARTESIAN_POINT('Ctrl Pts',(-2.61300874453222,6.24454244199253,-40.6768355859707));
#37939=CARTESIAN_POINT('Ctrl Pts',(-2.7705986005475,6.17382153893715,-40.6686939497635));
#37940=CARTESIAN_POINT('Ctrl Pts',(-2.85088849166117,6.13779019942487,-40.664545896703));
#37941=CARTESIAN_POINT('Ctrl Pts',(-2.93042849275127,6.10021339963102,-40.6603978436424));
#37942=CARTESIAN_POINT('Ctrl Pts',(-3.00915580109446,6.06112781293544,-40.6562497905818));
#37943=CARTESIAN_POINT('Ctrl Pts',(-3.16935499840773,5.98159404318106,-40.6478090756037));
#37944=CARTESIAN_POINT('Ctrl Pts',(-3.32651744598031,5.89564638932645,-40.6393683606257));
#37945=CARTESIAN_POINT('Ctrl Pts',(-3.48011514882274,5.80354094936311,-40.6309276456476));
#37946=CARTESIAN_POINT('Ctrl Pts',(-3.63359675528468,5.71150512703081,-40.6224933105596));
#37947=CARTESIAN_POINT('Ctrl Pts',(-3.78351870322428,5.61332096760009,-40.6140589754716));
#37948=CARTESIAN_POINT('Ctrl Pts',(-3.9293773398928,5.50929058234697,-40.6056246403836));
#37949=CARTESIAN_POINT('Ctrl Pts',(-4.07514812799051,5.40532285310705,-40.5971953851749));
#37950=CARTESIAN_POINT('Ctrl Pts',(-4.21686021305799,5.29551611100364,-40.5887661299663));
#37951=CARTESIAN_POINT('Ctrl Pts',(-4.35403836947873,5.18021610332107,-40.5803368747577));
#37952=CARTESIAN_POINT('Ctrl Pts',(-4.49115494755375,5.06496785303138,-40.5719114033847));
#37953=CARTESIAN_POINT('Ctrl Pts',(-4.62374140024711,4.9442314680578,-40.5634859320116));
#37954=CARTESIAN_POINT('Ctrl Pts',(-4.75135477795183,4.81839358853491,-40.5550604606386));
#37955=CARTESIAN_POINT('Ctrl Pts',(-4.8789304294401,4.69259291033971,-40.5466374800794));
#37956=CARTESIAN_POINT('Ctrl Pts',(-5.00153570067214,4.56169397904277,-40.5382144995201));
#37957=CARTESIAN_POINT('Ctrl Pts',(-5.1187634982169,4.42612124204956,-40.5297915189608));
#37958=CARTESIAN_POINT('Ctrl Pts',(-5.23599323681044,4.29054626025347,-40.5213683989345));
#37959=CARTESIAN_POINT('Ctrl Pts',(-5.34784510079353,4.15029756595743,-40.5129452789082));
#37960=CARTESIAN_POINT('Ctrl Pts',(-5.45395096164958,4.00583423370484,-40.5045221588818));
#37961=CARTESIAN_POINT('Ctrl Pts',(-5.56006049182318,3.86136590566939,-40.49609874757));
#37962=CARTESIAN_POINT('Ctrl Pts',(-5.66042342511529,3.71268291776603,-40.4876753362581));
#37963=CARTESIAN_POINT('Ctrl Pts',(-5.7547137287558,3.56027511578383,-40.4792519249463));
#37964=CARTESIAN_POINT('Ctrl Pts',(-5.84902044328238,3.40784078777531,-40.4708270475702));
#37965=CARTESIAN_POINT('Ctrl Pts',(-5.9372522455189,3.25168063678801,-40.462402170194));
#37966=CARTESIAN_POINT('Ctrl Pts',(-6.01912782135925,3.09231131520406,-40.4539772928179));
#37967=CARTESIAN_POINT('Ctrl Pts',(-6.10102906962677,2.9328920227068,-40.4455497737865));
#37968=CARTESIAN_POINT('Ctrl Pts',(-6.17656996561708,2.77026184994147,-40.4371222547551));
#37969=CARTESIAN_POINT('Ctrl Pts',(-6.24551615647476,2.6049600648019,-40.4286947357236));
#37970=CARTESIAN_POINT('Ctrl Pts',(-6.31452417561165,2.43951004341029,-40.4202596592188));
#37971=CARTESIAN_POINT('Ctrl Pts',(-6.37692554434306,2.27138393057703,-40.4118245827141));
#37972=CARTESIAN_POINT('Ctrl Pts',(-6.43253447786483,2.10113997417598,-40.4033895062093));
#37973=CARTESIAN_POINT('Ctrl Pts',(-6.48817028755014,1.93081373775044,-40.3949503529765));
#37974=CARTESIAN_POINT('Ctrl Pts',(-6.53700701903968,1.75836793564562,-40.3865111997438));
#37975=CARTESIAN_POINT('Ctrl Pts',(-6.57890924947765,1.58437435195645,-40.378072046511));
#37976=CARTESIAN_POINT('Ctrl Pts',(-6.62085804504184,1.41018741261292,-40.3696235150129));
#37977=CARTESIAN_POINT('Ctrl Pts',(-6.65585687139404,1.23444958090308,-40.3611749835148));
#37978=CARTESIAN_POINT('Ctrl Pts',(-6.68382151776658,1.05774236874601,-40.3527264520167));
#37979=CARTESIAN_POINT('Ctrl Pts',(-6.6992728922026,0.960105900749617,-40.3480583642507));
#37980=CARTESIAN_POINT('Ctrl Pts',(-6.7125777049321,0.862173597967542,-40.3433902764847));
#37981=CARTESIAN_POINT('Ctrl Pts',(-6.72372856026632,0.76404400911139,-40.3387221887187));
#37982=CARTESIAN_POINT('Ctrl Pts',(-6.74984068517333,0.534252481512515,
-40.327790857698));
#37983=CARTESIAN_POINT('Ctrl Pts',(-6.76418923897398,0.302940342222139,
-40.3168595266774));
#37984=CARTESIAN_POINT('Ctrl Pts',(-6.76662610837283,0.0711344465581041,
-40.3059281956566));
#37985=CARTESIAN_POINT('Ctrl Pts',(-6.76685705737744,0.0491655462588561,
-40.3048922025011));
#37986=CARTESIAN_POINT('Ctrl Pts',(-6.7669810525252,0.027192226654605,-40.3038562093455));
#37987=CARTESIAN_POINT('Ctrl Pts',(-6.76699799023869,0.00521537204463034,
-40.3028202161899));
#37988=CARTESIAN_POINT('',(-6.76699938789274,-0.00287823891704152,-40.6971797837711));
#37989=CARTESIAN_POINT('Ctrl Pts',(3.09908550384719,6.01564277861013,-41.3487246499327));
#37990=CARTESIAN_POINT('Ctrl Pts',(2.94379213113664,6.09564544132176,-41.3405102530541));
#37991=CARTESIAN_POINT('Ctrl Pts',(2.78551219358278,6.16957256320396,-41.3322958561754));
#37992=CARTESIAN_POINT('Ctrl Pts',(2.62476730733514,6.23721777576706,-41.3240814592968));
#37993=CARTESIAN_POINT('Ctrl Pts',(2.46391363966161,6.30490876610169,-41.3158615034618));
#37994=CARTESIAN_POINT('Ctrl Pts',(2.30059203317056,6.36630924838689,-41.3076415476268));
#37995=CARTESIAN_POINT('Ctrl Pts',(2.13533985033291,6.42126254903039,-41.2994215917918));
#37996=CARTESIAN_POINT('Ctrl Pts',(1.96985747544498,6.47629239821157,-41.2911901857692));
#37997=CARTESIAN_POINT('Ctrl Pts',(1.80243949674909,6.52485703144481,-41.2829587797467));
#37998=CARTESIAN_POINT('Ctrl Pts',(1.63363497364204,6.56685052158899,-41.2747273737242));
#37999=CARTESIAN_POINT('Ctrl Pts',(1.57309800053397,6.58191030041944,-41.2717754125098));
#38000=CARTESIAN_POINT('Ctrl Pts',(1.51238276679709,6.59612545097862,-41.2688234512953));
#38001=CARTESIAN_POINT('Ctrl Pts',(1.45151475646385,6.60949271213515,-41.2658714900809));
#38002=CARTESIAN_POINT('Ctrl Pts',(1.28509732268895,6.64603974704051,-41.2578006198945));
#38003=CARTESIAN_POINT('Ctrl Pts',(1.11699479168565,6.67636411374227,-41.2497297497081));
#38004=CARTESIAN_POINT('Ctrl Pts',(0.947723126957648,6.70030670004214,-41.2416588795217));
#38005=CARTESIAN_POINT('Ctrl Pts',(0.778662107659298,6.72421949165436,-41.2335980529059));
#38006=CARTESIAN_POINT('Ctrl Pts',(0.608435214196875,6.74176625316107,-41.2255372262901));
#38007=CARTESIAN_POINT('Ctrl Pts',(0.43757257483463,6.7528378657978,-41.2174763996744));
#38008=CARTESIAN_POINT('Ctrl Pts',(0.266885093176883,6.76389812850888,-41.2094238365145));
#38009=CARTESIAN_POINT('Ctrl Pts',(0.0955635316719927,6.76849642814417,
-41.2013712733546));
#38010=CARTESIAN_POINT('Ctrl Pts',(-0.0758529026689794,6.76657486008665,
-41.1933187101947));
#38011=CARTESIAN_POINT('Ctrl Pts',(-0.247131145431749,6.76465484114853,
-41.1852726388068));
#38012=CARTESIAN_POINT('Ctrl Pts',(-0.418503737707669,6.7562254202622,-41.177226567419));
#38013=CARTESIAN_POINT('Ctrl Pts',(-0.589427581032869,6.74128059990962,
-41.1691804960311));
#38014=CARTESIAN_POINT('Ctrl Pts',(-0.760251017539414,6.72634455868251,
-41.1611391511952));
#38015=CARTESIAN_POINT('Ctrl Pts',(-0.930625859224687,6.70490076964921,
-41.1530978063593));
#38016=CARTESIAN_POINT('Ctrl Pts',(-1.10001034920166,6.67699529965757,-41.1450564615235));
#38017=CARTESIAN_POINT('Ctrl Pts',(-1.27266005094853,6.64855189806975,-41.1368601043024));
#38018=CARTESIAN_POINT('Ctrl Pts',(-1.44428043351158,6.6133951575672,-41.1286637470813));
#38019=CARTESIAN_POINT('Ctrl Pts',(-1.61430422284346,6.57162924061528,-41.1204673898603));
#38020=CARTESIAN_POINT('Ctrl Pts',(-1.7810594387269,6.53066624052421,-41.1124286011518));
#38021=CARTESIAN_POINT('Ctrl Pts',(-1.94627852066613,6.48334598495039,-41.1043898124433));
#38022=CARTESIAN_POINT('Ctrl Pts',(-2.10943796254201,6.42981807535693,-41.0963510237348));
#38023=CARTESIAN_POINT('Ctrl Pts',(-2.27261486395664,6.37628443779209,-41.0883113748031));
#38024=CARTESIAN_POINT('Ctrl Pts',(-2.43373133154001,6.31654193986755,-41.0802717258714));
#38025=CARTESIAN_POINT('Ctrl Pts',(-2.59228067534066,6.25078954215029,-41.0722320769396));
#38026=CARTESIAN_POINT('Ctrl Pts',(-2.7508783787328,6.18501708910503,-41.0641899758115));
#38027=CARTESIAN_POINT('Ctrl Pts',(-2.90690705498651,6.1132312304802,-41.0561478746833));
#38028=CARTESIAN_POINT('Ctrl Pts',(-3.05988172670707,6.03567832298609,-41.0481057735551));
#38029=CARTESIAN_POINT('Ctrl Pts',(-3.21801869257826,5.95550830956053,-41.0397922831104));
#38030=CARTESIAN_POINT('Ctrl Pts',(-3.37289153634586,5.86917540387483,-41.0314787926656));
#38031=CARTESIAN_POINT('Ctrl Pts',(-3.52399495798297,5.77700169085233,-41.0231653022208));
#38032=CARTESIAN_POINT('Ctrl Pts',(-3.67042318741513,5.68767986443805,-41.0151090340501));
#38033=CARTESIAN_POINT('Ctrl Pts',(-3.81331150948368,5.59287354614307,-41.0070527658793));
#38034=CARTESIAN_POINT('Ctrl Pts',(-3.95223250598454,5.49291791479166,-40.9989964977086));
#38035=CARTESIAN_POINT('Ctrl Pts',(-4.09780675195578,5.38817517588919,-40.9905543961268));
#38036=CARTESIAN_POINT('Ctrl Pts',(-4.23902393556588,5.27777806943344,-40.982112294545));
#38037=CARTESIAN_POINT('Ctrl Pts',(-4.37543479113134,5.16215646688063,-40.9736701929633));
#38038=CARTESIAN_POINT('Ctrl Pts',(-4.51184564669678,5.04653486432783,-40.9652280913815));
#38039=CARTESIAN_POINT('Ctrl Pts',(-4.64344989323223,4.92568914108426,-40.9567859897997));
#38040=CARTESIAN_POINT('Ctrl Pts',(-4.76984630227191,4.80008908799649,-40.948343888218));
#38041=CARTESIAN_POINT('Ctrl Pts',(-4.89384004625725,4.67687656205977,-40.940062262259));
#38042=CARTESIAN_POINT('Ctrl Pts',(-5.01322680887011,4.54868741985101,-40.9317806363));
#38043=CARTESIAN_POINT('Ctrl Pts',(-5.12758617826025,4.41589730230612,-40.923499010341));
#38044=CARTESIAN_POINT('Ctrl Pts',(-5.24180727050531,4.28326774736704,-40.9152273980748));
#38045=CARTESIAN_POINT('Ctrl Pts',(-5.35101284864342,4.14604856369751,-40.9069557858086));
#38046=CARTESIAN_POINT('Ctrl Pts',(-5.45481820747363,4.00465320888267,-40.8986841735424));
#38047=CARTESIAN_POINT('Ctrl Pts',(-5.56018478539936,3.86113128632178,-40.8902881573035));
#38048=CARTESIAN_POINT('Ctrl Pts',(-5.6599871194426,3.71330679966699,-40.8818921410647));
#38049=CARTESIAN_POINT('Ctrl Pts',(-5.75386309753849,3.56164968164821,-40.8734961248258));
#38050=CARTESIAN_POINT('Ctrl Pts',(-5.84616337371679,3.41253811805693,-40.8652410351494));
#38051=CARTESIAN_POINT('Ctrl Pts',(-5.93273446191496,3.25972187539894,-40.856985945473));
#38052=CARTESIAN_POINT('Ctrl Pts',(-6.01327397138658,3.10367929159001,-40.8487308557966));
#38053=CARTESIAN_POINT('Ctrl Pts',(-6.09376909491767,2.94772270404419,-40.8404803155633));
#38054=CARTESIAN_POINT('Ctrl Pts',(-6.16823909902925,2.78854363023206,-40.83222977533));
#38055=CARTESIAN_POINT('Ctrl Pts',(-6.23642656767903,2.62664665799326,-40.8239792350968));
#38056=CARTESIAN_POINT('Ctrl Pts',(-6.30458838007217,2.46481060120347,-40.8157317992166));
#38057=CARTESIAN_POINT('Ctrl Pts',(-6.36647222962154,2.30025900876712,-40.8074843633364));
#38058=CARTESIAN_POINT('Ctrl Pts',(-6.42186800614757,2.13351829418411,-40.7992369274562));
#38059=CARTESIAN_POINT('Ctrl Pts',(-6.47899217181178,1.9615751461657,-40.7907321654857));
#38060=CARTESIAN_POINT('Ctrl Pts',(-6.52921667233642,1.78730441239828,-40.7822274035152));
#38061=CARTESIAN_POINT('Ctrl Pts',(-6.57236580696196,1.61130279571447,-40.7737226415447));
#38062=CARTESIAN_POINT('Ctrl Pts',(-6.61420760088614,1.44063370954358,-40.7654755584726));
#38063=CARTESIAN_POINT('Ctrl Pts',(-6.64939645595476,1.26833746207533,-40.7572284754005));
#38064=CARTESIAN_POINT('Ctrl Pts',(-6.67782361408341,1.09497067503655,-40.7489813923285));
#38065=CARTESIAN_POINT('Ctrl Pts',(-6.70758307577842,0.913478658327746,
-40.7403477909088));
#38066=CARTESIAN_POINT('Ctrl Pts',(-6.729931679293,0.730813754679236,-40.731714189489));
#38067=CARTESIAN_POINT('Ctrl Pts',(-6.7448052807437,0.547622794313622,-40.7230805880693));
#38068=CARTESIAN_POINT('Ctrl Pts',(-6.75967888219441,0.364431833948008,
-40.7144469866495));
#38069=CARTESIAN_POINT('Ctrl Pts',(-6.76707747653625,0.180715260589724,
-40.7058133852298));
#38070=CARTESIAN_POINT('Ctrl Pts',(-6.7669993878931,-0.0028782380871501,
-40.6971797838101));
#38071=CARTESIAN_POINT('Ctrl Pts',(-6.76699938789274,-0.00287823891708743,
-40.6971797837711));
#38072=CARTESIAN_POINT('Ctrl Pts',(-6.76689934781463,-0.238081488844765,
-40.6861192008684));
#38073=CARTESIAN_POINT('Ctrl Pts',(-6.75453223181383,-0.47288718151042,
-40.6750586179657));
#38074=CARTESIAN_POINT('Ctrl Pts',(-6.7300487737708,-0.706209956504527,
-40.663998035063));
#38075=CARTESIAN_POINT('Ctrl Pts',(-6.70556531572779,-0.939532731498602,
-40.6529374521603));
#38076=CARTESIAN_POINT('Ctrl Pts',(-6.66896560802827,-1.171372996591,-40.6418768692576));
#38077=CARTESIAN_POINT('Ctrl Pts',(-6.62045521010215,-1.40066477468068,
-40.6308162863549));
#38078=CARTESIAN_POINT('Ctrl Pts',(-6.58339002848412,-1.57585899616201,
-40.6223652628297));
#38079=CARTESIAN_POINT('Ctrl Pts',(-6.53933512208099,-1.74972928296825,
-40.6139142393046));
#38080=CARTESIAN_POINT('Ctrl Pts',(-6.48840239012968,-1.92169805738558,
-40.6054632157794));
#38081=CARTESIAN_POINT('Ctrl Pts',(-6.43751450293511,-2.09351541840799,
-40.5970196331292));
#38082=CARTESIAN_POINT('Ctrl Pts',(-6.37976095408972,-2.2634342877269,-40.5885760504791));
#38083=CARTESIAN_POINT('Ctrl Pts',(-6.31530438439976,-2.43088863018881,
-40.580132467829));
#38084=CARTESIAN_POINT('Ctrl Pts',(-6.25089580463375,-2.59821829767655,
-40.5716951716891));
#38085=CARTESIAN_POINT('Ctrl Pts',(-6.17979427125328,-2.76308678777859,
-40.5632578755493));
#38086=CARTESIAN_POINT('Ctrl Pts',(-6.10221194096156,-2.92494417512304,
-40.5548205794095));
#38087=CARTESIAN_POINT('Ctrl Pts',(-6.02468495974716,-3.08668608956259,
-40.5463893026372));
#38088=CARTESIAN_POINT('Ctrl Pts',(-5.9406865470088,-3.24542088797708,-40.5379580258648));
#38089=CARTESIAN_POINT('Ctrl Pts',(-5.85047664775428,-3.40061935448264,
-40.5295267490925));
#38090=CARTESIAN_POINT('Ctrl Pts',(-5.76030541572793,-3.5557512973077,-40.5210990862705));
#38091=CARTESIAN_POINT('Ctrl Pts',(-5.6639281712108,-3.70734964397582,-40.5126714234486));
#38092=CARTESIAN_POINT('Ctrl Pts',(-5.56165070769398,-3.85490990888336,
-40.5042437606267));
#38093=CARTESIAN_POINT('Ctrl Pts',(-5.45940472922576,-4.00242474890497,
-40.4958186921727));
#38094=CARTESIAN_POINT('Ctrl Pts',(-5.35126234257631,-4.14590371406427,
-40.4873936237187));
#38095=CARTESIAN_POINT('Ctrl Pts',(-5.23757275640213,-4.28487113241392,
-40.4789685552648));
#38096=CARTESIAN_POINT('Ctrl Pts',(-5.20646380567513,-4.32289687175891,
-40.476663198651));
#38097=CARTESIAN_POINT('Ctrl Pts',(-5.17493975894945,-4.36058499186709,
-40.4743578420372));
#38098=CARTESIAN_POINT('Ctrl Pts',(-5.14300831224887,-4.39792615901393,
-40.4720524854234));
#38099=CARTESIAN_POINT('Ctrl Pts',(-5.02362688074474,-4.53753279913351,
-40.4634334968989));
#38100=CARTESIAN_POINT('Ctrl Pts',(-4.89860120089721,-4.6722248909405,-40.4548145083744));
#38101=CARTESIAN_POINT('Ctrl Pts',(-4.7683631396862,-4.80156245071144,-40.4461955198499));
#38102=CARTESIAN_POINT('Ctrl Pts',(-4.63804705425388,-4.93097749522295,
-40.4375713677821));
#38103=CARTESIAN_POINT('Ctrl Pts',(-4.50251257135162,-5.05503139150259,
-40.4289472157144));
#38104=CARTESIAN_POINT('Ctrl Pts',(-4.36222695569932,-5.17332243214844,
-40.4203230636466));
#38105=CARTESIAN_POINT('Ctrl Pts',(-4.21713651997044,-5.29566497275978,
-40.4114035320504));
#38106=CARTESIAN_POINT('Ctrl Pts',(-4.06696401301909,-5.41184268532276,
-40.4024840004541));
#38107=CARTESIAN_POINT('Ctrl Pts',(-3.91226120089767,-5.52145825810091,
-40.3935644688579));
#38108=CARTESIAN_POINT('Ctrl Pts',(-3.76240288314324,-5.62764123636073,
-40.3849242509987));
#38109=CARTESIAN_POINT('Ctrl Pts',(-3.60829397862272,-5.72766671271702,
-40.3762840331394));
#38110=CARTESIAN_POINT('Ctrl Pts',(-3.45046369254555,-5.82121888494368,
-40.3676438152802));
#38111=CARTESIAN_POINT('Ctrl Pts',(-3.28498009823066,-5.91930747174675,
-40.3585846268154));
#38112=CARTESIAN_POINT('Ctrl Pts',(-3.11540558650537,-6.01027917269694,
-40.3495254383507));
#38113=CARTESIAN_POINT('Ctrl Pts',(-2.94237733334475,-6.093825122878,-40.340466249886));
#38114=CARTESIAN_POINT('Ctrl Pts',(-2.76934908018416,-6.17737107305904,
-40.3314070614213));
#38115=CARTESIAN_POINT('Ctrl Pts',(-2.59286745004693,-6.25349115134961,
-40.3223478729566));
#38116=CARTESIAN_POINT('Ctrl Pts',(-2.41359214469936,-6.32193498535421,
-40.3132886844919));
#38117=CARTESIAN_POINT('Ctrl Pts',(-2.23462742124062,-6.39026024521832,
-40.3042451904356));
#38118=CARTESIAN_POINT('Ctrl Pts',(-2.05271412508592,-6.45099957105981,
-40.2952016963793));
#38119=CARTESIAN_POINT('Ctrl Pts',(-1.86848456706522,-6.50392607758107,
-40.2861582023231));
#38120=CARTESIAN_POINT('Ctrl Pts',(-1.68442352314759,-6.55680417242035,
-40.2771229803177));
#38121=CARTESIAN_POINT('Ctrl Pts',(-1.49805067594403,-6.60188364998442,
-40.2680877583124));
#38122=CARTESIAN_POINT('Ctrl Pts',(-1.31001378613239,-6.63898733845329,
-40.2590525363071));
#38123=CARTESIAN_POINT('Ctrl Pts',(-1.1223081763854,-6.67602565830046,-40.2500332323959));
#38124=CARTESIAN_POINT('Ctrl Pts',(-0.932944611511852,-6.7051162023267,
-40.2410139284848));
#38125=CARTESIAN_POINT('Ctrl Pts',(-0.742581174275494,-6.72613278188973,
-40.2319946245737));
#38126=CARTESIAN_POINT('Ctrl Pts',(-0.552456561267698,-6.74712299468572,
-40.2229866360094));
#38127=CARTESIAN_POINT('Ctrl Pts',(-0.361334815213718,-6.76005943167516,
-40.213978647445));
#38128=CARTESIAN_POINT('Ctrl Pts',(-0.169881810109107,-6.76486726925178,
-40.2049706588806));
#38129=CARTESIAN_POINT('Ctrl Pts',(0.0211387916775638,-6.76966424815884,
-40.195983015174));
#38130=CARTESIAN_POINT('Ctrl Pts',(0.212488921545239,-6.76636926738616,
-40.1869953714673));
#38131=CARTESIAN_POINT('Ctrl Pts',(0.40350048950883,-6.75495938958675,-40.1780077277606));
#38132=CARTESIAN_POINT('Ctrl Pts',(0.569858326161454,-6.745022176844,-40.1701801130272));
#38133=CARTESIAN_POINT('Ctrl Pts',(0.735959158018499,-6.7289304173852,-40.1623524982937));
#38134=CARTESIAN_POINT('Ctrl Pts',(0.901359588940868,-6.7067011183908,-40.1545248835603));
#38135=CARTESIAN_POINT('Ctrl Pts',(1.0730049691823,-6.6836325178006,-40.146401725115));
#38136=CARTESIAN_POINT('Ctrl Pts',(1.24381911066791,-6.65396281728191,-40.1382785666697));
#38137=CARTESIAN_POINT('Ctrl Pts',(1.41325603536892,-6.61777881003085,-40.1301554082244));
#38138=CARTESIAN_POINT('Ctrl Pts',(1.58268101387985,-6.5815973539417,-40.1220328225043));
#38139=CARTESIAN_POINT('Ctrl Pts',(1.75072861106866,-6.53890258242891,-40.1139102367842));
#38140=CARTESIAN_POINT('Ctrl Pts',(1.91686338505769,-6.48983233705041,-40.1057876510641));
#38141=CARTESIAN_POINT('Ctrl Pts',(2.08301812184995,-6.44075619537681,-40.0976640893317));
#38142=CARTESIAN_POINT('Ctrl Pts',(2.24725922708082,-6.38530315922434,-40.0895405275993));
#38143=CARTESIAN_POINT('Ctrl Pts',(2.40906680035588,-6.32366081881556,-40.0814169658669));
#38144=CARTESIAN_POINT('Ctrl Pts',(2.57099223124696,-6.26197357927667,-40.0732874870838));
#38145=CARTESIAN_POINT('Ctrl Pts',(2.73048024756321,-6.19408816191164,-40.0651580083007));
#38146=CARTESIAN_POINT('Ctrl Pts',(2.88703071563051,-6.12024040761521,-40.0570285295176));
#38147=CARTESIAN_POINT('Ctrl Pts',(3.04364500656834,-6.04636254688909,-40.048895736489));
#38148=CARTESIAN_POINT('Ctrl Pts',(3.19731903754234,-5.96651767268191,-40.0407629434605));
#38149=CARTESIAN_POINT('Ctrl Pts',(3.34757787426296,-5.88098727899875,-40.032630150432));
#38150=CARTESIAN_POINT('Ctrl Pts',(3.49800009467293,-5.79536388398817,-40.0244885142248));
#38151=CARTESIAN_POINT('Ctrl Pts',(3.64499939324817,-5.70404281471206,-40.0163468780177));
#38152=CARTESIAN_POINT('Ctrl Pts',(3.78812975489722,-5.60734892440825,-40.0082052418105));
#38153=CARTESIAN_POINT('Ctrl Pts',(3.86105273003296,-5.55808470068126,-40.00405718875));
#38154=CARTESIAN_POINT('Ctrl Pts',(3.93297193626112,-5.50742647892359,-39.9999091356894));
#38155=CARTESIAN_POINT('Ctrl Pts',(4.0038317888937,-5.45542115755001,-39.9957610826288));
#38156=CARTESIAN_POINT('Ctrl Pts',(4.14802180062394,-5.34959751242089,-39.9873203676508));
#38157=CARTESIAN_POINT('Ctrl Pts',(4.28812031183531,-5.23797564500015,-39.9788796526727));
#38158=CARTESIAN_POINT('Ctrl Pts',(4.42365105696813,-5.12089839053508,-39.9704389376946));
#38159=CARTESIAN_POINT('Ctrl Pts',(4.55907936157832,-5.00390962857496,-39.9620046026066));
#38160=CARTESIAN_POINT('Ctrl Pts',(4.68994653111973,-4.88147391657323,-39.9535702675186));
#38161=CARTESIAN_POINT('Ctrl Pts',(4.81580817120893,-4.75397524794958,-39.9451359324305));
#38162=CARTESIAN_POINT('Ctrl Pts',(4.94159400663235,-4.6265533699506,-39.9367066772219));
#38163=CARTESIAN_POINT('Ctrl Pts',(5.0623800893322,-4.49407485134633,-39.9282774220133));
#38164=CARTESIAN_POINT('Ctrl Pts',(5.17775751289374,-4.35696180126387,-39.9198481668047));
#38165=CARTESIAN_POINT('Ctrl Pts',(5.29308314431078,-4.21991030030153,-39.9114226954317));
#38166=CARTESIAN_POINT('Ctrl Pts',(5.40300474327351,-4.07822867066769,-39.9029972240586));
#38167=CARTESIAN_POINT('Ctrl Pts',(5.50715221287519,-3.93237377473505,-39.8945717526856));
#38168=CARTESIAN_POINT('Ctrl Pts',(5.61126889346346,-3.78656199774099,-39.8861487721264));
#38169=CARTESIAN_POINT('Ctrl Pts',(5.70961465529431,-3.63657968585611,-39.8777257915671));
#38170=CARTESIAN_POINT('Ctrl Pts',(5.8018612090653,-3.48291480095959,-39.8693028110079));
#38171=CARTESIAN_POINT('Ctrl Pts',(5.89410929024782,-3.3292473716914,-39.8608796909816));
#38172=CARTESIAN_POINT('Ctrl Pts',(5.98025778436389,-3.17189752996982,-39.8524565709552));
#38173=CARTESIAN_POINT('Ctrl Pts',(6.06002272715309,-3.01138067111883,-39.8440334509289));
#38174=CARTESIAN_POINT('Ctrl Pts',(6.13979042834697,-2.85085826132728,-39.835610039617));
#38175=CARTESIAN_POINT('Ctrl Pts',(6.21317398949544,-2.68716891462428,-39.8271866283052));
#38176=CARTESIAN_POINT('Ctrl Pts',(6.27993619471869,-2.52085112417655,-39.8187632169933));
#38177=CARTESIAN_POINT('Ctrl Pts',(6.34671001966215,-2.35450438671927,-39.8103383396172));
#38178=CARTESIAN_POINT('Ctrl Pts',(6.40686006685966,-2.18552860293806,-39.8019134622411));
#38179=CARTESIAN_POINT('Ctrl Pts',(6.46019777310973,-2.01448100817756,-39.793488584865));
#38180=CARTESIAN_POINT('Ctrl Pts',(6.51355220361928,-1.84337978073281,-39.7850610658335));
#38181=CARTESIAN_POINT('Ctrl Pts',(6.56008993526042,-1.67020576537716,-39.7766335468021));
#38182=CARTESIAN_POINT('Ctrl Pts',(6.5996725482858,-1.495530426104,-39.7682060277707));
#38183=CARTESIAN_POINT('Ctrl Pts',(6.63929065746871,-1.32069844473765,-39.7597709512659));
#38184=CARTESIAN_POINT('Ctrl Pts',(6.67194111167981,-1.14436277484692,-39.7513358747611));
#38185=CARTESIAN_POINT('Ctrl Pts',(6.69753659428511,-0.967105251878937,
-39.7429007982563));
#38186=CARTESIAN_POINT('Ctrl Pts',(6.72314444735561,-0.789762059183462,
-39.7344616450235));
#38187=CARTESIAN_POINT('Ctrl Pts',(6.74169048893664,-0.611496455804941,
-39.7260224917908));
#38188=CARTESIAN_POINT('Ctrl Pts',(6.75313933945475,-0.432894977920331,
-39.717583338558));
#38189=CARTESIAN_POINT('Ctrl Pts',(6.76460091285572,-0.254095023719107,
-39.7091348070599));
#38190=CARTESIAN_POINT('Ctrl Pts',(6.7689495227256,-0.0749587824602956,
-39.7006862755618));
#38191=CARTESIAN_POINT('Ctrl Pts',(6.76620191111585,0.103926406712928,-39.6922377440637));
#38192=CARTESIAN_POINT('Ctrl Pts',(6.76468376655499,0.202766277674943,-39.6875696562977));
#38193=CARTESIAN_POINT('Ctrl Pts',(6.76100012467404,0.30152955400974,-39.6829015685317));
#38194=CARTESIAN_POINT('Ctrl Pts',(6.75516059642078,0.400117878336026,-39.6782334807658));
#38195=CARTESIAN_POINT('Ctrl Pts',(6.74485182667636,0.574160076761794,-39.669992705169));
#38196=CARTESIAN_POINT('Ctrl Pts',(6.72779840754416,0.748043914453889,-39.6617519295723));
#38197=CARTESIAN_POINT('Ctrl Pts',(6.70400359479417,0.921208337449707,-39.6535111539755));
#38198=CARTESIAN_POINT('Ctrl Pts',(6.68023513737897,1.09418096207374,-39.6452795059311));
#38199=CARTESIAN_POINT('Ctrl Pts',(6.64974020216558,1.2664354092589,-39.6370478578868));
#38200=CARTESIAN_POINT('Ctrl Pts',(6.61257401127576,1.43741223919948,-39.6288162098424));
#38201=CARTESIAN_POINT('Ctrl Pts',(6.5754423626094,1.60823016343237,-39.6205922122841));
#38202=CARTESIAN_POINT('Ctrl Pts',(6.53165188141004,1.77777248957256,-39.6123682147258));
#38203=CARTESIAN_POINT('Ctrl Pts',(6.48130940631116,1.94548641209917,-39.6041442171676));
#38204=CARTESIAN_POINT('Ctrl Pts',(6.43101140898456,2.11305215872381,-39.5959274855431));
#38205=CARTESIAN_POINT('Ctrl Pts',(6.37417305716934,2.27879238193669,-39.5877107539186));
#38206=CARTESIAN_POINT('Ctrl Pts',(6.31095189393438,2.44216608617147,-39.5794940222941));
#38207=CARTESIAN_POINT('Ctrl Pts',(6.2477631212419,2.60545608800921,-39.5712815004054));
#38208=CARTESIAN_POINT('Ctrl Pts',(6.17819817806482,2.76638165460895,-39.5630689785167));
#38209=CARTESIAN_POINT('Ctrl Pts',(6.10246405710077,2.92441813559437,-39.554856456628));
#38210=CARTESIAN_POINT('Ctrl Pts',(6.02675526199128,3.08240176841991,-39.5466466810461));
#38211=CARTESIAN_POINT('Ctrl Pts',(5.94488155242803,3.23749791976992,-39.5384369054643));
#38212=CARTESIAN_POINT('Ctrl Pts',(5.85709758374302,3.38920298809495,-39.5302271298824));
#38213=CARTESIAN_POINT('Ctrl Pts',(5.81875582686446,3.45546382061478,-39.5266413131997));
#38214=CARTESIAN_POINT('Ctrl Pts',(5.77928716420472,3.52107802441721,-39.523055496517));
#38215=CARTESIAN_POINT('Ctrl Pts',(5.73871556846833,3.5860051065523,-39.5194696798343));
#38216=CARTESIAN_POINT('Ctrl Pts',(5.63848392311761,3.74640669175261,-39.5106109623125));
#38217=CARTESIAN_POINT('Ctrl Pts',(5.53162178112995,3.90244658083081,-39.5017522447907));
#38218=CARTESIAN_POINT('Ctrl Pts',(5.41853445131823,4.05361238895353,-39.492893527269));
#38219=CARTESIAN_POINT('Ctrl Pts',(5.30523555327521,4.20506100402473,-39.4840182365095));
#38220=CARTESIAN_POINT('Ctrl Pts',(5.18568834837483,4.35161710752813,-39.4751429457501));
#38221=CARTESIAN_POINT('Ctrl Pts',(5.06033754288159,4.49280234954791,-39.4662676549906));
#38222=CARTESIAN_POINT('Ctrl Pts',(4.9346307129163,4.63438858939973,-39.4573671564098));
#38223=CARTESIAN_POINT('Ctrl Pts',(4.80308747005726,4.77057324658558,-39.448466657829));
#38224=CARTESIAN_POINT('Ctrl Pts',(4.66619063681407,4.90091358227307,-39.4395661592483));
#38225=CARTESIAN_POINT('Ctrl Pts',(4.52910848614448,5.03143035984746,-39.4306536120506));
#38226=CARTESIAN_POINT('Ctrl Pts',(4.38665846077222,5.15608683824668,-39.421741064853));
#38227=CARTESIAN_POINT('Ctrl Pts',(4.23935652569372,5.27448056665849,-39.4128285176554));
#38228=CARTESIAN_POINT('Ctrl Pts',(4.09172933355657,5.39313571998537,-39.4038962906831));
#38229=CARTESIAN_POINT('Ctrl Pts',(3.93922900593053,5.50550030037312,-39.3949640637109));
#38230=CARTESIAN_POINT('Ctrl Pts',(3.78240289183726,5.61121353753546,-39.3860318367386));
#38231=CARTESIAN_POINT('Ctrl Pts',(3.63418410439051,5.71112475397963,-39.3775898507933));
#38232=CARTESIAN_POINT('Ctrl Pts',(3.48210172969147,5.80509498490515,-39.3691478648481));
#38233=CARTESIAN_POINT('Ctrl Pts',(3.32663794447754,5.89285745511991,-39.3607058789028));
#38234=CARTESIAN_POINT('Ctrl Pts',(3.25162616590813,5.93520313050273,-39.3566325934135));
#38235=CARTESIAN_POINT('Ctrl Pts',(3.17575653689587,5.97614407567335,-39.3525593079243));
#38236=CARTESIAN_POINT('Ctrl Pts',(3.09908550384721,6.01564277861012,-39.3484860224351));
#38237=CARTESIAN_POINT('Origin',(0.,0.,-63.6971797838103));
#38238=CARTESIAN_POINT('',(3.09908550384718,6.01564277861013,-36.9542436419538));
#38239=CARTESIAN_POINT('',(3.09908550384721,6.01564277861012,-37.3484709211108));
#38240=CARTESIAN_POINT('',(3.09908550384721,6.01564277861012,-63.6971797838103));
#38241=CARTESIAN_POINT('',(-6.767,6.39834729252928E-13,-38.30282021619));
#38242=CARTESIAN_POINT('Ctrl Pts',(-6.767,6.39834728801335E-13,-38.30282021619));
#38243=CARTESIAN_POINT('Ctrl Pts',(-6.76700000000002,-0.186007249559384,
-38.2940707043773));
#38244=CARTESIAN_POINT('Ctrl Pts',(-6.7593263729425,-0.372014355815586,
-38.2853211925645));
#38245=CARTESIAN_POINT('Ctrl Pts',(-6.74400518263366,-0.557389537585977,
-38.2765716807518));
#38246=CARTESIAN_POINT('Ctrl Pts',(-6.72868405703732,-0.742763936382592,
-38.2678222058946));
#38247=CARTESIAN_POINT('Ctrl Pts',(-6.70571545643564,-0.927506130405041,
-38.2590727310374));
#38248=CARTESIAN_POINT('Ctrl Pts',(-6.67517739401571,-1.1109886400957,-38.2503232561802));
#38249=CARTESIAN_POINT('Ctrl Pts',(-6.64463945804385,-1.29447039004563,
-38.2415738175516));
#38250=CARTESIAN_POINT('Ctrl Pts',(-6.6065321700272,-1.47669218339296,-38.2328243789231));
#38251=CARTESIAN_POINT('Ctrl Pts',(-6.56098496085476,-1.65703510627798,
-38.2240749402946));
#38252=CARTESIAN_POINT('Ctrl Pts',(-6.51543793649547,-1.83737729740044,
-38.215325537168));
#38253=CARTESIAN_POINT('Ctrl Pts',(-6.4624511215688,-2.01584035545007,-38.2065761340413));
#38254=CARTESIAN_POINT('Ctrl Pts',(-6.40220448361692,-2.19181813797483,
-38.1978267309147));
#38255=CARTESIAN_POINT('Ctrl Pts',(-6.34195808511945,-2.36779522106378,
-38.1890773625632));
#38256=CARTESIAN_POINT('Ctrl Pts',(-6.27445201416324,-2.54128677725819,
-38.1803279942116));
#38257=CARTESIAN_POINT('Ctrl Pts',(-6.19991555052691,-2.71170355428734,
-38.1715786258601));
#38258=CARTESIAN_POINT('Ctrl Pts',(-6.12537937695073,-2.88211966813618,
-38.1628292915569));
#38259=CARTESIAN_POINT('Ctrl Pts',(-6.04381298028288,-3.04946076419995,
-38.1540799572537));
#38260=CARTESIAN_POINT('Ctrl Pts',(-5.95549339308798,-3.21315848424652,
-38.1453306229505));
#38261=CARTESIAN_POINT('Ctrl Pts',(-5.86717414225611,-3.37685558085427,
-38.136581321969));
#38262=CARTESIAN_POINT('Ctrl Pts',(-5.77210188843852,-3.5369090770035,-38.1278320209874));
#38263=CARTESIAN_POINT('Ctrl Pts',(-5.67059953311141,-3.69277537024345,
-38.1190827200058));
#38264=CARTESIAN_POINT('Ctrl Pts',(-5.56909755592451,-3.84864108281398,
-38.1103334516192));
#38265=CARTESIAN_POINT('Ctrl Pts',(-5.46116568154682,-4.00031938355217,
-38.1015841832326));
#38266=CARTESIAN_POINT('Ctrl Pts',(-5.34717048488064,-4.14729511918567,
-38.092834914846));
#38267=CARTESIAN_POINT('Ctrl Pts',(-5.23317570342969,-4.29427031947589,
-38.0840856783276));
#38268=CARTESIAN_POINT('Ctrl Pts',(-5.11311781951186,-4.43654276249972,
-38.0753364418092));
#38269=CARTESIAN_POINT('Ctrl Pts',(-4.98740458928858,-4.57362924412804,
-38.0665872052909));
#38270=CARTESIAN_POINT('Ctrl Pts',(-4.86169180652326,-4.71071523781696,
-38.0578379999142));
#38271=CARTESIAN_POINT('Ctrl Pts',(-4.73032391141129,-4.84261509584923,
-38.0490887945374));
#38272=CARTESIAN_POINT('Ctrl Pts',(-4.59374706946854,-4.96888084600036,
-38.0403395891607));
#38273=CARTESIAN_POINT('Ctrl Pts',(-4.45717070231063,-5.0951461572113,-38.031590414199));
#38274=CARTESIAN_POINT('Ctrl Pts',(-4.31538563496948,-5.21577720520924,
-38.0228412392373));
#38275=CARTESIAN_POINT('Ctrl Pts',(-4.1688734095166,-5.33036429293772,-38.0140920642756));
#38276=CARTESIAN_POINT('Ctrl Pts',(-4.02236168122134,-5.44495099183965,
-38.0053429190024));
#38277=CARTESIAN_POINT('Ctrl Pts',(-3.87112305262826,-5.55349359498176,
-37.9965937737292));
#38278=CARTESIAN_POINT('Ctrl Pts',(-3.71567116928637,-5.65562346357447,
-37.9878446284559));
#38279=CARTESIAN_POINT('Ctrl Pts',(-3.56021980052937,-5.75775299409159,
-37.9790955121445));
#38280=CARTESIAN_POINT('Ctrl Pts',(-3.40055544441694,-5.85346967520106,
-37.9703463958331));
#38281=CARTESIAN_POINT('Ctrl Pts',(-3.23722035886438,-5.94244843041603,
-37.9615972795218));
#38282=CARTESIAN_POINT('Ctrl Pts',(-3.07388580043084,-6.03142689847658,
-37.9528481914458));
#38283=CARTESIAN_POINT('Ctrl Pts',(-2.90688078788816,-6.11366734708095,
-37.9440991033697));
#38284=CARTESIAN_POINT('Ctrl Pts',(-2.73677250609987,-6.18889047001608,
-37.9353500152937));
#38285=CARTESIAN_POINT('Ctrl Pts',(-2.56666475916546,-6.26411335643492,
-37.9266009547266));
#38286=CARTESIAN_POINT('Ctrl Pts',(-2.39345402456724,-6.33231884545395,
-37.9178518941594));
#38287=CARTESIAN_POINT('Ctrl Pts',(-2.21772855943716,-6.39327529805004,
-37.9091028335923));
#38288=CARTESIAN_POINT('Ctrl Pts',(-2.04200363223247,-6.45423156404811,
-37.9003537998075));
#38289=CARTESIAN_POINT('Ctrl Pts',(-1.86376426060696,-6.5079387441255,-37.8916047660227));
#38290=CARTESIAN_POINT('Ctrl Pts',(-1.68361577621356,-6.55421443943398,
-37.8828557322379));
#38291=CARTESIAN_POINT('Ctrl Pts',(-1.50346782832887,-6.60048999692662,
-37.874106724509));
#38292=CARTESIAN_POINT('Ctrl Pts',(-1.32141105657063,-6.63933404265226,
-37.8653577167801));
#38293=CARTESIAN_POINT('Ctrl Pts',(-1.13806375346216,-6.67061465631584,
-37.8566087090512));
#38294=CARTESIAN_POINT('Ctrl Pts',(-0.954716981166758,-6.70189517941817,
-37.8478597266518));
#38295=CARTESIAN_POINT('Ctrl Pts',(-0.770079967438979,-6.72561226609042,
-37.8391107442523));
#38296=CARTESIAN_POINT('Ctrl Pts',(-0.584779764069715,-6.74168536996014,
-37.8303617618529));
#38297=CARTESIAN_POINT('Ctrl Pts',(-0.391489587589589,-6.75845153117892,
-37.8212355314373));
#38298=CARTESIAN_POINT('Ctrl Pts',(-0.197478091801861,-6.76689985146404,
-37.8121093010217));
#38299=CARTESIAN_POINT('Ctrl Pts',(-0.00346214752765282,-6.76699911434415,
-37.802983070606));
#38300=CARTESIAN_POINT('Ctrl Pts',(0.184490798488006,-6.76709527525926,
-37.7941420348909));
#38301=CARTESIAN_POINT('Ctrl Pts',(0.372447602158131,-6.75935633790745,
-37.7853009991758));
#38302=CARTESIAN_POINT('Ctrl Pts',(0.559756448197546,-6.74380914014485,
-37.7764599634607));
#38303=CARTESIAN_POINT('Ctrl Pts',(0.745136131046712,-6.72842206873117,
-37.7677099848474));
#38304=CARTESIAN_POINT('Ctrl Pts',(0.929880851948416,-6.70538686355677,
-37.758960006234));
#38305=CARTESIAN_POINT('Ctrl Pts',(1.11336305057802,-6.67478177303256,-37.7502100276207));
#38306=CARTESIAN_POINT('Ctrl Pts',(1.2968433709046,-6.64417699581195,-37.7414601385807));
#38307=CARTESIAN_POINT('Ctrl Pts',(1.47906091205525,-6.60600253547985,-37.7327102495408));
#38308=CARTESIAN_POINT('Ctrl Pts',(1.65939671095554,-6.56038806441128,-37.7239603605008));
#38309=CARTESIAN_POINT('Ctrl Pts',(1.83973072369499,-6.51477404513754,-37.7152105581253));
#38310=CARTESIAN_POINT('Ctrl Pts',(2.0181827535738,-6.46172023288554,-37.7064607557498));
#38311=CARTESIAN_POINT('Ctrl Pts',(2.19414664033674,-6.40140683917988,-37.6977109533743));
#38312=CARTESIAN_POINT('Ctrl Pts',(2.370108842716,-6.3410940228137,-37.6889612347548));
#38313=CARTESIAN_POINT('Ctrl Pts',(2.5435826784814,-6.27352185699656,-37.6802115161352));
#38314=CARTESIAN_POINT('Ctrl Pts',(2.71397890842068,-6.19891986435119,-37.6714617975157));
#38315=CARTESIAN_POINT('Ctrl Pts',(2.88437356389272,-6.12431856103088,-37.6627121597439));
#38316=CARTESIAN_POINT('Ctrl Pts',(3.05169040787505,-6.04268767582389,-37.653962521972));
#38317=CARTESIAN_POINT('Ctrl Pts',(3.21536112512389,-5.95430447953764,-37.6452128842002));
#38318=CARTESIAN_POINT('Ctrl Pts',(3.37903038443164,-5.86592207054857,-37.6364633243682));
#38319=CARTESIAN_POINT('Ctrl Pts',(3.5390533298028,-5.77078760703188,-37.6277137645361));
#38320=CARTESIAN_POINT('Ctrl Pts',(3.69488643042185,-5.66922422085108,-37.618964204704));
#38321=CARTESIAN_POINT('Ctrl Pts',(3.85071819469032,-5.56766170562958,-37.610214719904));
#38322=CARTESIAN_POINT('Ctrl Pts',(4.0023599459951,-5.45967053456042,-37.6014652351041));
#38323=CARTESIAN_POINT('Ctrl Pts',(4.14929662974583,-5.34561750206465,-37.5927157503041));
#38324=CARTESIAN_POINT('Ctrl Pts',(4.29623210225319,-5.2315654097424,-37.5839663376287));
#38325=CARTESIAN_POINT('Ctrl Pts',(4.43846235842385,-5.11145173171954,-37.5752169249533));
#38326=CARTESIAN_POINT('Ctrl Pts',(4.57550431797689,-4.98568443006322,-37.566467512278));
#38327=CARTESIAN_POINT('Ctrl Pts',(4.71254519337751,-4.85991812336441,-37.5577181688201));
#38328=CARTESIAN_POINT('Ctrl Pts',(4.84439764315236,-4.72849847630843,-37.5489688253622));
#38329=CARTESIAN_POINT('Ctrl Pts',(4.97061384196934,-4.59187184425076,-37.5402194819043));
#38330=CARTESIAN_POINT('Ctrl Pts',(5.09682908420447,-4.45524624767472,-37.5314702047569));
#38331=CARTESIAN_POINT('Ctrl Pts',(5.21740796650404,-4.3134139555661,-37.5227209276096));
#38332=CARTESIAN_POINT('Ctrl Pts',(5.33194095942477,-4.16685668162567,-37.5139716504622));
#38333=CARTESIAN_POINT('Ctrl Pts',(5.44647312235358,-4.02030046974909,-37.5052224367187));
#38334=CARTESIAN_POINT('Ctrl Pts',(5.55495930712513,-3.86901957035225,-37.4964732229751));
#38335=CARTESIAN_POINT('Ctrl Pts',(5.65703106080017,-3.71352778058036,-37.4877240092316));
#38336=CARTESIAN_POINT('Ctrl Pts',(5.75910210868956,-3.55803706597247,-37.4789748559854));
#38337=CARTESIAN_POINT('Ctrl Pts',(5.85475865698766,-3.39833575880526,-37.4702257027392));
#38338=CARTESIAN_POINT('Ctrl Pts',(5.94367583069276,-3.23496624706329,-37.461476549493));
#38339=CARTESIAN_POINT('Ctrl Pts',(6.03259241910284,-3.07159781069694,-37.4527274538378));
#38340=CARTESIAN_POINT('Ctrl Pts',(6.11476958471167,-2.90456146975415,-37.4439783581827));
#38341=CARTESIAN_POINT('Ctrl Pts',(6.18992823574577,-2.73442451647825,-37.4352292625276));
#38342=CARTESIAN_POINT('Ctrl Pts',(6.26508641701117,-2.56428862661971,-37.4264802215575));
#38343=CARTESIAN_POINT('Ctrl Pts',(6.33322605570469,-2.3910524253082,-37.4177311805873));
#38344=CARTESIAN_POINT('Ctrl Pts',(6.3941157374793,-2.21530425353259,-37.4089821396172));
#38345=CARTESIAN_POINT('Ctrl Pts',(6.45500505889272,-2.03955712188095,-37.4002331504262));
#38346=CARTESIAN_POINT('Ctrl Pts',(6.50864441545061,-1.86129832025111,-37.3914841612352));
#38347=CARTESIAN_POINT('Ctrl Pts',(6.55485164050023,-1.68113324011853,-37.3827351720442));
#38348=CARTESIAN_POINT('Ctrl Pts',(6.60199852639213,-1.49730435912441,-37.3738082651674));
#38349=CARTESIAN_POINT('Ctrl Pts',(6.641407674411,-1.31149113173193,-37.3648813582905));
#38350=CARTESIAN_POINT('Ctrl Pts',(6.67293975269679,-1.12435050445973,-37.3559544514136));
#38351=CARTESIAN_POINT('Ctrl Pts',(6.70384664831571,-0.940920291559148,
-37.3472045372296));
#38352=CARTESIAN_POINT('Ctrl Pts',(6.72718585889718,-0.756215114273333,
-37.3384546230456));
#38353=CARTESIAN_POINT('Ctrl Pts',(6.74287810451903,-0.570862389370528,
-37.3297047088616));
#38354=CARTESIAN_POINT('Ctrl Pts',(6.75857004154149,-0.385513309563553,
-37.320954966751));
#38355=CARTESIAN_POINT('Ctrl Pts',(6.76661529035569,-0.199516993254733,
-37.3122052246405));
#38356=CARTESIAN_POINT('Ctrl Pts',(6.76698652348897,-0.0135052182006522,
-37.3034554825299));
#38357=CARTESIAN_POINT('Ctrl Pts',(6.76735774981513,0.172503146042231,-37.2947059008592));
#38358=CARTESIAN_POINT('Ctrl Pts',(6.76005524147462,0.358526681836741,-37.2859563191886));
#38359=CARTESIAN_POINT('Ctrl Pts',(6.74510380214856,0.543933542118062,-37.2772067375179));
#38360=CARTESIAN_POINT('Ctrl Pts',(6.73015261710945,0.729337249087885,-37.268457304656));
#38361=CARTESIAN_POINT('Ctrl Pts',(6.70755278444563,0.914124015857789,-37.2597078717941));
#38362=CARTESIAN_POINT('Ctrl Pts',(6.67738106408238,1.09766621749694,-37.2509584389322));
#38363=CARTESIAN_POINT('Ctrl Pts',(6.64720981677196,1.2812055414362,-37.2422091432498));
#38364=CARTESIAN_POINT('Ctrl Pts',(6.60946696581459,1.46350005650908,-37.2334598475675));
#38365=CARTESIAN_POINT('Ctrl Pts',(6.56428070010925,1.64393062206811,-37.2247105518851));
#38366=CARTESIAN_POINT('Ctrl Pts',(6.51909508282663,1.82435859844928,-37.2159613817552));
#38367=CARTESIAN_POINT('Ctrl Pts',(6.46646633415577,2.00292240086837,-37.2072122116251));
#38368=CARTESIAN_POINT('Ctrl Pts',(6.406573195971,2.17901557696726,-37.1984630414952));
#38369=CARTESIAN_POINT('Ctrl Pts',(6.34668083768194,2.35510646007706,-37.1897139852921));
#38370=CARTESIAN_POINT('Ctrl Pts',(6.27952437143776,2.52872650996801,-37.180964929089));
#38371=CARTESIAN_POINT('Ctrl Pts',(6.20533187335019,2.69928607998195,-37.1722158728859));
#38372=CARTESIAN_POINT('Ctrl Pts',(6.12831449784133,2.87633970115651,-37.1631336965971));
#38373=CARTESIAN_POINT('Ctrl Pts',(6.04371489463032,3.05009490562587,-37.1540515203083));
#38374=CARTESIAN_POINT('Ctrl Pts',(5.9518426512037,3.21991584599854,-37.1449693440194));
#38375=CARTESIAN_POINT('Ctrl Pts',(5.86333281335362,3.38352155905526,-37.136219563665));
#38376=CARTESIAN_POINT('Ctrl Pts',(5.76807337235546,3.54347560904051,-37.1274697833106));
#38377=CARTESIAN_POINT('Ctrl Pts',(5.66638790086206,3.69923467178875,-37.1187200029562));
#38378=CARTESIAN_POINT('Ctrl Pts',(5.56470608502585,3.85498813489992,-37.1099705371619));
#38379=CARTESIAN_POINT('Ctrl Pts',(5.45659885766785,4.00654667256488,-37.1012210713676));
#38380=CARTESIAN_POINT('Ctrl Pts',(5.34243340580332,4.15339551506437,-37.0924716055734));
#38381=CARTESIAN_POINT('Ctrl Pts',(5.22827145140408,4.30023985884096,-37.0837224078195));
#38382=CARTESIAN_POINT('Ctrl Pts',(5.10805181977893,4.44237456993268,-37.0749732100656));
#38383=CARTESIAN_POINT('Ctrl Pts',(4.98218281282345,4.57931691626673,-37.0662240123117));
#38384=CARTESIAN_POINT('Ctrl Pts',(4.85631699296016,4.71625579512381,-37.0574750360937));
#38385=CARTESIAN_POINT('Ctrl Pts',(4.72480227791618,4.84800236135984,-37.0487260598757));
#38386=CARTESIAN_POINT('Ctrl Pts',(4.58808530847887,4.97410918679117,-37.0399770836577));
#38387=CARTESIAN_POINT('Ctrl Pts',(4.45135945056731,5.10022421089218,-37.0312275386365));
#38388=CARTESIAN_POINT('Ctrl Pts',(4.30943087207787,5.22069856612195,-37.0224779936153));
#38389=CARTESIAN_POINT('Ctrl Pts',(4.16278164322201,5.33512305301891,-37.0137284485941));
#38390=CARTESIAN_POINT('Ctrl Pts',(4.01614103534133,5.44954081331616,-37.0049794179269));
#38391=CARTESIAN_POINT('Ctrl Pts',(3.86478055833165,5.55790924068509,-36.9962303872596));
#38392=CARTESIAN_POINT('Ctrl Pts',(3.70921425811715,5.65986029751446,-36.9874813565924));
#38393=CARTESIAN_POINT('Ctrl Pts',(3.55364584529888,5.76181273884797,-36.9787322071125));
#38394=CARTESIAN_POINT('Ctrl Pts',(3.39387173464118,5.85734747818194,-36.9699830576327));
#38395=CARTESIAN_POINT('Ctrl Pts',(3.23043456092184,5.94614005448928,-36.9612339081528));
#38396=CARTESIAN_POINT('Ctrl Pts',(3.18690768806243,5.9697874481136,-36.9589038194198));
#38397=CARTESIAN_POINT('Ctrl Pts',(3.14312114982806,5.99295688499339,-36.9565737306868));
#38398=CARTESIAN_POINT('Ctrl Pts',(3.09908550384719,6.01564277861013,-36.9542436419538));
#38399=CARTESIAN_POINT('Ctrl Pts',(3.0990855038472,6.01564277861013,-38.9542099095282));
#38400=CARTESIAN_POINT('Ctrl Pts',(2.93954625881631,6.0978327921741,-38.9457836090008));
#38401=CARTESIAN_POINT('Ctrl Pts',(2.77668881039921,6.1736963075324,-38.9373573084735));
#38402=CARTESIAN_POINT('Ctrl Pts',(2.61104376445001,6.24297520899504,-38.9289310079462));
#38403=CARTESIAN_POINT('Ctrl Pts',(2.48599841881969,6.29527381007088,-38.9225699987425));
#38404=CARTESIAN_POINT('Ctrl Pts',(2.35936505171891,6.34382093289626,-38.9162089895389));
#38405=CARTESIAN_POINT('Ctrl Pts',(2.23138005412037,6.38852346431269,-38.9098479803352));
#38406=CARTESIAN_POINT('Ctrl Pts',(2.05796398281955,6.44909413682038,-38.9012289918107));
#38407=CARTESIAN_POINT('Ctrl Pts',(1.88214334099229,6.50257761206384,-38.8926100032862));
#38408=CARTESIAN_POINT('Ctrl Pts',(1.70451273536023,6.5488109863543,-38.8839910147617));
#38409=CARTESIAN_POINT('Ctrl Pts',(1.52677571314328,6.59507205856192,-38.8753668626939));
#38410=CARTESIAN_POINT('Ctrl Pts',(1.34722685747579,6.63407428498897,-38.8667427106261));
#38411=CARTESIAN_POINT('Ctrl Pts',(1.16647210396409,6.66570565136757,-38.8581185585584));
#38412=CARTESIAN_POINT('Ctrl Pts',(0.979526451516919,6.69842040055429,-38.8491990269621));
#38413=CARTESIAN_POINT('Ctrl Pts',(0.791291188010618,6.72325038873687,-38.8402794953659));
#38414=CARTESIAN_POINT('Ctrl Pts',(0.602443060545144,6.74012992150752,-38.8313599637697));
#38415=CARTESIAN_POINT('Ctrl Pts',(0.419508682656814,6.75648087434929,-38.8227197459104));
#38416=CARTESIAN_POINT('Ctrl Pts',(0.23599954997781,6.76537180209201,-38.8140795280512));
#38417=CARTESIAN_POINT('Ctrl Pts',(0.0525318974627829,6.76679609562376,
-38.805439310192));
#38418=CARTESIAN_POINT('Ctrl Pts',(-0.139832238302195,6.76828945421071,
-38.7963801217272));
#38419=CARTESIAN_POINT('Ctrl Pts',(-0.332150383408293,6.76157406414995,
-38.7873209332625));
#38420=CARTESIAN_POINT('Ctrl Pts',(-0.523716488820115,6.74670364247148,
-38.7782617447978));
#38421=CARTESIAN_POINT('Ctrl Pts',(-0.715282594231936,6.73183322079301,
-38.769202556333));
#38422=CARTESIAN_POINT('Ctrl Pts',(-0.906096284047167,6.708807846224,-38.7601433678683));
#38423=CARTESIAN_POINT('Ctrl Pts',(-1.09546147671801,6.67774311822691,-38.7510841794036));
#38424=CARTESIAN_POINT('Ctrl Pts',(-1.28449860747761,6.6467322076917,-38.7420406853473));
#38425=CARTESIAN_POINT('Ctrl Pts',(-1.47226654297517,6.60768204225785,-38.7329971912911));
#38426=CARTESIAN_POINT('Ctrl Pts',(-1.65810469081281,6.5607147350197,-38.7239536972348));
#38427=CARTESIAN_POINT('Ctrl Pts',(-1.84377285317746,6.5137903886054,-38.7149184752294));
#38428=CARTESIAN_POINT('Ctrl Pts',(-2.02751452141858,6.45896341691647,-38.7058832532241));
#38429=CARTESIAN_POINT('Ctrl Pts',(-2.20868076779968,6.39640666827492,-38.6968480312187));
#38430=CARTESIAN_POINT('Ctrl Pts',(-2.38952783869297,6.33396013100642,-38.6878287273076));
#38431=CARTESIAN_POINT('Ctrl Pts',(-2.56780832345928,6.26381108821348,-38.6788094233965));
#38432=CARTESIAN_POINT('Ctrl Pts',(-2.74289002919077,6.1861816403793,-38.6697901194854));
#38433=CARTESIAN_POINT('Ctrl Pts',(-2.91775208269464,6.10864958410909,-38.660782130921));
#38434=CARTESIAN_POINT('Ctrl Pts',(-3.08942314891028,6.0236559476321,-38.6517741423566));
#38435=CARTESIAN_POINT('Ctrl Pts',(-3.25729014899516,5.9314711400511,-38.6427661537921));
#38436=CARTESIAN_POINT('Ctrl Pts',(-3.42477801557925,5.83949453508765,-38.6337785100855));
#38437=CARTESIAN_POINT('Ctrl Pts',(-3.58847875738045,5.74035929295689,-38.6247908663788));
#38438=CARTESIAN_POINT('Ctrl Pts',(-3.74780348985188,5.63438177633128,-38.6158032226721));
#38439=CARTESIAN_POINT('Ctrl Pts',(-3.88656428900939,5.54208270467062,-38.6079756079388));
#38440=CARTESIAN_POINT('Ctrl Pts',(-4.02200601069406,5.44459439207581,-38.6001479932054));
#38441=CARTESIAN_POINT('Ctrl Pts',(-4.15375404391448,5.34215465357042,-38.5923203784721));
#38442=CARTESIAN_POINT('Ctrl Pts',(-4.29047642808377,5.2358471441543,-38.5841972200268));
#38443=CARTESIAN_POINT('Ctrl Pts',(-4.42315879319529,5.12425345235888,-38.5760740615816));
#38444=CARTESIAN_POINT('Ctrl Pts',(-4.55137299668703,5.00772331953635,-38.5679509031363));
#38445=CARTESIAN_POINT('Ctrl Pts',(-4.67957816040648,4.89120140269798,-38.5598283174162));
#38446=CARTESIAN_POINT('Ctrl Pts',(-4.80331551914681,4.76974398428607,-38.5517057316961));
#38447=CARTESIAN_POINT('Ctrl Pts',(-4.92219172300998,4.64373961823142,-38.543583145976));
#38448=CARTESIAN_POINT('Ctrl Pts',(-5.04108221107229,4.51772011145559,-38.5354595842437));
#38449=CARTESIAN_POINT('Ctrl Pts',(-5.15511013084091,4.3871528361571,-38.5273360225113));
#38450=CARTESIAN_POINT('Ctrl Pts',(-5.26392059652226,4.25246151699328,-38.519212460779));
#38451=CARTESIAN_POINT('Ctrl Pts',(-5.37281031771664,4.11767209118562,-38.5110829819959));
#38452=CARTESIAN_POINT('Ctrl Pts',(-5.4764747643854,3.97875290699445,-38.5029535032127));
#38453=CARTESIAN_POINT('Ctrl Pts',(-5.57460041236353,3.83615943913654,-38.4948240244296));
#38454=CARTESIAN_POINT('Ctrl Pts',(-5.6727660644412,3.69350783843162,-38.486691231401));
#38455=CARTESIAN_POINT('Ctrl Pts',(-5.76538822119881,3.54717927727347,-38.4785584383725));
#38456=CARTESIAN_POINT('Ctrl Pts',(-5.85219810773909,3.39765600197769,-38.4704256453439));
#38457=CARTESIAN_POINT('Ctrl Pts',(-5.9391023868613,3.24797014280378,-38.4622840091368));
#38458=CARTESIAN_POINT('Ctrl Pts',(-6.02018160151472,3.09508295424076,-38.4541423729296));
#38459=CARTESIAN_POINT('Ctrl Pts',(-6.09521378633161,2.93949960008725,-38.4460007367224));
#38460=CARTESIAN_POINT('Ctrl Pts',(-6.13344166534192,2.86023199441758,-38.4418526836618));
#38461=CARTESIAN_POINT('Ctrl Pts',(-6.17010065573144,2.78026483816001,-38.4377046306012));
#38462=CARTESIAN_POINT('Ctrl Pts',(-6.20516632234485,2.69966662979659,-38.4335565775406));
#38463=CARTESIAN_POINT('Ctrl Pts',(-6.2836902509147,2.51917988684769,-38.42426767892));
#38464=CARTESIAN_POINT('Ctrl Pts',(-6.35435036609351,2.33523149083991,-38.4149787802994));
#38465=CARTESIAN_POINT('Ctrl Pts',(-6.41687785198368,2.14848030773412,-38.4056898816789));
#38466=CARTESIAN_POINT('Ctrl Pts',(-6.47927456533099,1.96211970369527,-38.396420410241));
#38467=CARTESIAN_POINT('Ctrl Pts',(-6.53357255989753,1.77296819610722,-38.3871509388031));
#38468=CARTESIAN_POINT('Ctrl Pts',(-6.57955268183747,1.58170019501973,-38.3778814673653));
#38469=CARTESIAN_POINT('Ctrl Pts',(-6.62545405419011,1.39075977627676,-38.3686278716367));
#38470=CARTESIAN_POINT('Ctrl Pts',(-6.66306594648214,1.1977102803237,-38.3593742759082));
#38471=CARTESIAN_POINT('Ctrl Pts',(-6.69221929528,1.00323970409974,-38.3501206801796));
#38472=CARTESIAN_POINT('Ctrl Pts',(-6.72127264703585,0.809436168993859,
-38.3408988246195));
#38473=CARTESIAN_POINT('Ctrl Pts',(-6.74192532171844,0.614221465069455,
-38.3316769690594));
#38474=CARTESIAN_POINT('Ctrl Pts',(-6.75405965128696,0.41829084003543,-38.3224551134992));
#38475=CARTESIAN_POINT('Ctrl Pts',(-6.76267166772411,0.27923431006346,-38.3159101477295));
#38476=CARTESIAN_POINT('Ctrl Pts',(-6.76699396276897,0.139817469194059,
-38.3093651819597));
#38477=CARTESIAN_POINT('Ctrl Pts',(-6.76699999367839,0.000292500793738614,
-38.30282021619));
#38478=CARTESIAN_POINT('',(-6.76699993162883,0.00096194355167065,-38.6971797837635));
#38479=CARTESIAN_POINT('Ctrl Pts',(3.09908550384721,6.01564277861012,-39.3484860224351));
#38480=CARTESIAN_POINT('Ctrl Pts',(2.94437133429452,6.09534705257489,-39.3402665560113));
#38481=CARTESIAN_POINT('Ctrl Pts',(2.78639218245449,6.16917587646048,-39.3320470895876));
#38482=CARTESIAN_POINT('Ctrl Pts',(2.62563398538058,6.23685298646798,-39.3238276231638));
#38483=CARTESIAN_POINT('Ctrl Pts',(2.46502959728258,6.30446534489718,-39.3156160208971));
#38484=CARTESIAN_POINT('Ctrl Pts',(2.3016517873046,6.36593757261412,-39.3074044186305));
#38485=CARTESIAN_POINT('Ctrl Pts',(2.13601085070116,6.42103937425141,-39.2991928163638));
#38486=CARTESIAN_POINT('Ctrl Pts',(1.97049517578476,6.47609950657209,-39.2909874239096));
#38487=CARTESIAN_POINT('Ctrl Pts',(1.80272012168599,6.52479869529337,-39.2827820314554));
#38488=CARTESIAN_POINT('Ctrl Pts',(1.63321579930917,6.56695478535424,-39.2745766390012));
#38489=CARTESIAN_POINT('Ctrl Pts',(1.46380567465356,6.60908744823895,-39.2663758064854));
#38490=CARTESIAN_POINT('Ctrl Pts',(1.29266854312108,6.64468416961378,-39.2581749739696));
#38491=CARTESIAN_POINT('Ctrl Pts',(1.12034959639276,6.67361264847328,-39.2499741414538));
#38492=CARTESIAN_POINT('Ctrl Pts',(0.939296608403607,6.70400737659191,-39.2413576471032));
#38493=CARTESIAN_POINT('Ctrl Pts',(0.756939281898732,6.72704018589386,-39.2327411527526));
#38494=CARTESIAN_POINT('Ctrl Pts',(0.57392272231459,6.74261831255567,-39.224124658402));
#38495=CARTESIAN_POINT('Ctrl Pts',(0.399790550416843,6.7574402119285,-39.2159264446512));
#38496=CARTESIAN_POINT('Ctrl Pts',(0.225062026447252,6.7655140351368,-39.2077282309004));
#38497=CARTESIAN_POINT('Ctrl Pts',(0.0502982204209523,6.76681306739166,
-39.1995300171496));
#38498=CARTESIAN_POINT('Ctrl Pts',(-0.124481183155672,6.76811221558425,
-39.1913310717137));
#38499=CARTESIAN_POINT('Ctrl Pts',(-0.299295516341745,6.76263536508475,
-39.1831321262779));
#38500=CARTESIAN_POINT('Ctrl Pts',(-0.473583718648115,6.75040794777852,
-39.1749331808421));
#38501=CARTESIAN_POINT('Ctrl Pts',(-0.647919136903179,6.73817721797552,
-39.166732014252));
#38502=CARTESIAN_POINT('Ctrl Pts',(-0.821727782612122,6.71919230341321,
-39.158530847662));
#38503=CARTESIAN_POINT('Ctrl Pts',(-0.994453669868803,6.69353052570051,
-39.1503296810719));
#38504=CARTESIAN_POINT('Ctrl Pts',(-1.16725772738974,6.66785713428022,-39.1421248028936));
#38505=CARTESIAN_POINT('Ctrl Pts',(-1.33897769596545,6.63550091300536,-39.1339199247154));
#38506=CARTESIAN_POINT('Ctrl Pts',(-1.50906767778191,6.59659031196223,-39.1257150465371));
#38507=CARTESIAN_POINT('Ctrl Pts',(-1.67935628910185,6.55763427148003,-39.1175005867782));
#38508=CARTESIAN_POINT('Ctrl Pts',(-1.84801076260359,6.51210864508346,-39.1092861270193));
#38509=CARTESIAN_POINT('Ctrl Pts',(-2.01449935509248,6.46019205196966,-39.1010716672604));
#38510=CARTESIAN_POINT('Ctrl Pts',(-2.18110096466695,6.40824021642898,-39.0928516312978));
#38511=CARTESIAN_POINT('Ctrl Pts',(-2.34553342605553,6.34988888699901,-39.0846315953352));
#38512=CARTESIAN_POINT('Ctrl Pts',(-2.50728500844487,6.28536481729005,-39.0764115593726));
#38513=CARTESIAN_POINT('Ctrl Pts',(-2.66926134676726,6.22075109054481,-39.0681801015629));
#38514=CARTESIAN_POINT('Ctrl Pts',(-2.82854904072158,6.14994764018784,-39.0599486437531));
#38515=CARTESIAN_POINT('Ctrl Pts',(-2.98466015274912,6.07322754164469,-39.0517171859434));
#38516=CARTESIAN_POINT('Ctrl Pts',(-3.03864081228131,6.04669899114661,-39.0488708829755));
#38517=CARTESIAN_POINT('Ctrl Pts',(-3.09224190821867,6.01946339359807,-39.0460245800076));
#38518=CARTESIAN_POINT('Ctrl Pts',(-3.14544408829237,5.99153323344088,-39.0431782770398));
#38519=CARTESIAN_POINT('Ctrl Pts',(-3.29630219927205,5.91233551645193,-39.0351074068534));
#38520=CARTESIAN_POINT('Ctrl Pts',(-3.44444266254927,5.82729181424176,-39.0270365366669));
#38521=CARTESIAN_POINT('Ctrl Pts',(-3.58936826272957,5.73661263068282,-39.0189656664805));
#38522=CARTESIAN_POINT('Ctrl Pts',(-3.73411351426522,5.64604629031952,-39.0109048398647));
#38523=CARTESIAN_POINT('Ctrl Pts',(-3.87565155077558,5.54985861793858,-39.0028440132489));
#38524=CARTESIAN_POINT('Ctrl Pts',(-4.0135065113057,5.44830748799173,-38.9947831866331));
#38525=CARTESIAN_POINT('Ctrl Pts',(-4.15122015154176,5.34686046191965,-38.9867306234733));
#38526=CARTESIAN_POINT('Ctrl Pts',(-4.28525793171493,5.24006113943915,-38.9786780603134));
#38527=CARTESIAN_POINT('Ctrl Pts',(-4.41517002262306,5.12821242455212,-38.9706254971535));
#38528=CARTESIAN_POINT('Ctrl Pts',(-4.54497738170151,5.01645387925959,-38.9625794257656));
#38529=CARTESIAN_POINT('Ctrl Pts',(-4.67066539023081,4.89965428580147,-38.9545333543777));
#38530=CARTESIAN_POINT('Ctrl Pts',(-4.791814665727,4.77815876769741,-38.9464872829898));
#38531=CARTESIAN_POINT('Ctrl Pts',(-4.9128927737769,4.65673462043501,-38.9384459381539));
#38532=CARTESIAN_POINT('Ctrl Pts',(-5.02943719377697,4.53062030350734,-38.9304045933181));
#38533=CARTESIAN_POINT('Ctrl Pts',(-5.1410630949805,4.40019991062105,-38.9223632484822));
#38534=CARTESIAN_POINT('Ctrl Pts',(-5.25484080008599,4.26726541386387,-38.9141668912611));
#38535=CARTESIAN_POINT('Ctrl Pts',(-5.36350812498187,4.12985739148594,-38.9059705340401));
#38536=CARTESIAN_POINT('Ctrl Pts',(-5.46669812488634,3.98842081673489,-38.897774176819));
#38537=CARTESIAN_POINT('Ctrl Pts',(-5.56790437830955,3.84970324874557,-38.8897353881105));
#38538=CARTESIAN_POINT('Ctrl Pts',(-5.66384178073572,3.70711094025673,-38.881696599402));
#38539=CARTESIAN_POINT('Ctrl Pts',(-5.75420613299375,3.56109544649075,-38.8736578106935));
#38540=CARTESIAN_POINT('Ctrl Pts',(-5.84458015505619,3.415064327744,-38.8656181617618));
#38541=CARTESIAN_POINT('Ctrl Pts',(-5.92937974285766,3.26560961188173,-38.85757851283));
#38542=CARTESIAN_POINT('Ctrl Pts',(-6.00834534648432,3.11320979013305,-38.8495388638983));
#38543=CARTESIAN_POINT('Ctrl Pts',(-6.08733503563694,2.96076348447623,-38.8414967627701));
#38544=CARTESIAN_POINT('Ctrl Pts',(-6.16048702692392,2.80537061629134,-38.833454661642));
#38545=CARTESIAN_POINT('Ctrl Pts',(-6.22758890188882,2.64753195808307,-38.8254125605138));
#38546=CARTESIAN_POINT('Ctrl Pts',(-6.2969552014982,2.48436686529029,-38.817099070069));
#38547=CARTESIAN_POINT('Ctrl Pts',(-6.35985573377751,2.31858842465414,-38.8087855796243));
#38548=CARTESIAN_POINT('Ctrl Pts',(-6.41611129451752,2.1507684339242,-38.8004720891795));
#38549=CARTESIAN_POINT('Ctrl Pts',(-6.47062628872235,1.98814085183718,-38.7924158210088));
#38550=CARTESIAN_POINT('Ctrl Pts',(-6.5189013502021,1.82359654469976,-38.784359552838));
#38551=CARTESIAN_POINT('Ctrl Pts',(-6.56082529297568,1.65766717861295,-38.7763032846673));
#38552=CARTESIAN_POINT('Ctrl Pts',(-6.60475707082873,1.4837910694504,-38.7678611830855));
#38553=CARTESIAN_POINT('Ctrl Pts',(-6.64171433038961,1.30839444740119,-38.7594190815037));
#38554=CARTESIAN_POINT('Ctrl Pts',(-6.67163014485131,1.13209549522611,-38.750976979922));
#38555=CARTESIAN_POINT('Ctrl Pts',(-6.70154595931302,0.955796543051042,
-38.7425348783402));
#38556=CARTESIAN_POINT('Ctrl Pts',(-6.72442035542752,0.778595728902839,
-38.7340927767585));
#38557=CARTESIAN_POINT('Ctrl Pts',(-6.74024886421216,0.601110845424283,
-38.7256506751767));
#38558=CARTESIAN_POINT('Ctrl Pts',(-6.75804268603638,0.401588929867985,
-38.7161603780545));
#38559=CARTESIAN_POINT('Ctrl Pts',(-6.76697144454004,0.201360324820626,
-38.7066700809323));
#38560=CARTESIAN_POINT('Ctrl Pts',(-6.76699993162869,0.000961944536271024,
-38.6971797838101));
#38561=CARTESIAN_POINT('Ctrl Pts',(-6.76699993162883,0.000961943551675157,
-38.6971797837635));
#38562=CARTESIAN_POINT('Ctrl Pts',(-6.76702456299972,-0.17231276141232,
-38.6889739867329));
#38563=CARTESIAN_POINT('Ctrl Pts',(-6.76038966563165,-0.34584484753625,
-38.6807681897024));
#38564=CARTESIAN_POINT('Ctrl Pts',(-6.74706194009427,-0.519080125348007,
-38.6725623926718));
#38565=CARTESIAN_POINT('Ctrl Pts',(-6.73374985689133,-0.6921120823349,-38.6643662265285));
#38566=CARTESIAN_POINT('Ctrl Pts',(-6.71376061346842,-0.864847568095618,
-38.6561700603851));
#38567=CARTESIAN_POINT('Ctrl Pts',(-6.68711287393178,-1.0367306358432,-38.6479738942418));
#38568=CARTESIAN_POINT('Ctrl Pts',(-6.66049097002691,-1.20844705877502,
-38.6397856744809));
#38569=CARTESIAN_POINT('Ctrl Pts',(-6.62722348061152,-1.37931235505076,
-38.63159745472));
#38570=CARTESIAN_POINT('Ctrl Pts',(-6.58738100010477,-1.54877388906794,
-38.6234092349592));
#38571=CARTESIAN_POINT('Ctrl Pts',(-6.54756901736165,-1.71810570732088,
-38.6152272829404));
#38572=CARTESIAN_POINT('Ctrl Pts',(-6.50119214995199,-1.88603555350871,
-38.6070453309215));
#38573=CARTESIAN_POINT('Ctrl Pts',(-6.44837238636049,-2.05201914387354,
-38.5988633789027));
#38574=CARTESIAN_POINT('Ctrl Pts',(-6.3955819855785,-2.21791046300856,-38.590685975278));
#38575=CARTESIAN_POINT('Ctrl Pts',(-6.33635593265055,-2.38185733840268,
-38.5825085716532));
#38576=CARTESIAN_POINT('Ctrl Pts',(-6.27086657931742,-2.54332879203612,
-38.5743311680285));
#38577=CARTESIAN_POINT('Ctrl Pts',(-6.20539643680379,-2.70475287920779,
-38.5661561631848));
#38578=CARTESIAN_POINT('Ctrl Pts',(-6.13366678753111,-2.86370265619969,
-38.5579811583412));
#38579=CARTESIAN_POINT('Ctrl Pts',(-6.05589886771911,-3.01966519732873,
-38.5498061534976));
#38580=CARTESIAN_POINT('Ctrl Pts',(-5.97813938880849,-3.17561081034101,
-38.541632035966));
#38581=CARTESIAN_POINT('Ctrl Pts',(-5.89434310579912,-3.32856951025794,
-38.5334579184344));
#38582=CARTESIAN_POINT('Ctrl Pts',(-5.80477815147919,-3.4780511226993,-38.5252838009027));
#38583=CARTESIAN_POINT('Ctrl Pts',(-5.71520636675548,-3.62754413490944,
-38.5171090599965));
#38584=CARTESIAN_POINT('Ctrl Pts',(-5.61986522085826,-3.77355922230813,
-38.5089343190902));
#38585=CARTESIAN_POINT('Ctrl Pts',(-5.51906729291426,-3.91563343742543,
-38.5007595781839));
#38586=CARTESIAN_POINT('Ctrl Pts',(-5.41819964722992,-4.05780591937658,
-38.4925791831489));
#38587=CARTESIAN_POINT('Ctrl Pts',(-5.31186788789913,-4.19603178831862,
-38.4843987881138));
#38588=CARTESIAN_POINT('Ctrl Pts',(-5.20042661905157,-4.32987897981686,
-38.4762183930788));
#38589=CARTESIAN_POINT('Ctrl Pts',(-5.08894540440009,-4.46377414845788,
-38.4680350658046));
#38590=CARTESIAN_POINT('Ctrl Pts',(-4.97235126916519,-4.59328724112423,
-38.4598517385303));
#38591=CARTESIAN_POINT('Ctrl Pts',(-4.85103704135763,-4.718021685344,-38.4516684112561));
#38592=CARTESIAN_POINT('Ctrl Pts',(-4.72958736508698,-4.84289539673027,
-38.4434759472209));
#38593=CARTESIAN_POINT('Ctrl Pts',(-4.60340732654163,-4.9629795486941,-38.4352834831857));
#38594=CARTESIAN_POINT('Ctrl Pts',(-4.47292502481537,-5.07791598220967,
-38.4270910191505));
#38595=CARTESIAN_POINT('Ctrl Pts',(-4.37222348491334,-5.16661978106009,
-38.4207683705382));
#38596=CARTESIAN_POINT('Ctrl Pts',(-4.26896015810002,-5.25225827422651,
-38.4144457219259));
#38597=CARTESIAN_POINT('Ctrl Pts',(-4.16334399683779,-5.33468422345641,
-38.4081230733136));
#38598=CARTESIAN_POINT('Ctrl Pts',(-4.02217457272462,-5.44485698154289,
-38.3996720497885));
#38599=CARTESIAN_POINT('Ctrl Pts',(-3.87650987115763,-5.54951598081996,
-38.3912210262633));
#38600=CARTESIAN_POINT('Ctrl Pts',(-3.72680741947126,-5.64829137511283,
-38.3827700027381));
#38601=CARTESIAN_POINT('Ctrl Pts',(-3.57723677634384,-5.74697980060703,
-38.3743264200879));
#38602=CARTESIAN_POINT('Ctrl Pts',(-3.42363574452268,-5.83979476480231,
-38.3658828374378));
#38603=CARTESIAN_POINT('Ctrl Pts',(-3.26649324084622,-5.92640792618142,
-38.3574392547876));
#38604=CARTESIAN_POINT('Ctrl Pts',(-3.10946773465818,-6.01295660136419,
-38.3490019586477));
#38605=CARTESIAN_POINT('Ctrl Pts',(-2.94890630218418,-6.09331251888087,
-38.3405646625078));
#38606=CARTESIAN_POINT('Ctrl Pts',(-2.785325371087,-6.16719154698304,-38.3321273663679));
#38607=CARTESIAN_POINT('Ctrl Pts',(-2.62186114251269,-6.24101786803122,
-38.3236960895956));
#38608=CARTESIAN_POINT('Ctrl Pts',(-2.45538201356443,-6.30837638044795,
-38.3152648128232));
#38609=CARTESIAN_POINT('Ctrl Pts',(-2.28642763911666,-6.36902956902254,
-38.3068335360509));
#38610=CARTESIAN_POINT('Ctrl Pts',(-2.11754568463057,-6.42965675944463,
-38.298405873229));
#38611=CARTESIAN_POINT('Ctrl Pts',(-1.94619091117425,-6.48358424396456,
-38.2899782104071));
#38612=CARTESIAN_POINT('Ctrl Pts',(-1.77292212762096,-6.53062295109678,
-38.2815505475852));
#38613=CARTESIAN_POINT('Ctrl Pts',(-1.5997066830516,-6.57764717785468,-38.2731254791312));
#38614=CARTESIAN_POINT('Ctrl Pts',(-1.42457872294707,-6.61778676956985,
-38.2647004106772));
#38615=CARTESIAN_POINT('Ctrl Pts',(-1.24811171909707,-6.65090265577933,
-38.2562753422233));
#38616=CARTESIAN_POINT('Ctrl Pts',(-1.19982494532777,-6.65996417589743,
-38.2539699856096));
#38617=CARTESIAN_POINT('Ctrl Pts',(-1.15143798463569,-6.66850009729251,
-38.2516646289958));
#38618=CARTESIAN_POINT('Ctrl Pts',(-1.1029627353664,-6.67650823442861,-38.2493592723821));
#38619=CARTESIAN_POINT('Ctrl Pts',(-0.921729335428296,-6.70644808914259,
-38.2407402838577));
#38620=CARTESIAN_POINT('Ctrl Pts',(-0.739342141307451,-6.7289934132114,
-38.2321212953332));
#38621=CARTESIAN_POINT('Ctrl Pts',(-0.556414885681503,-6.74408566634441,
-38.2235023068087));
#38622=CARTESIAN_POINT('Ctrl Pts',(-0.373378040304804,-6.75918696108389,
-38.2148781547409));
#38623=CARTESIAN_POINT('Ctrl Pts',(-0.189800790848503,-6.76682624899216,
-38.2062540026732));
#38624=CARTESIAN_POINT('Ctrl Pts',(-0.00629930563155577,-6.76699706803162,
-38.1976298506054));
#38625=CARTESIAN_POINT('Ctrl Pts',(0.183487154821004,-6.76717373766914,
-38.1887103190092));
#38626=CARTESIAN_POINT('Ctrl Pts',(0.373192211341671,-6.75936129432861,
-38.1797907874129));
#38627=CARTESIAN_POINT('Ctrl Pts',(0.562137874734621,-6.74361105119422,
-38.1708712558167));
#38628=CARTESIAN_POINT('Ctrl Pts',(0.745166734228464,-6.72835402446034,
-38.1622310379575));
#38629=CARTESIAN_POINT('Ctrl Pts',(0.927482744725567,-6.70564889972387,
-38.1535908200982));
#38630=CARTESIAN_POINT('Ctrl Pts',(1.10847766379766,-6.67559482509699,-38.1449506022389));
#38631=CARTESIAN_POINT('Ctrl Pts',(1.29824916143105,-6.64408340598551,-38.1358914137742));
#38632=CARTESIAN_POINT('Ctrl Pts',(1.48656788135299,-6.60449268576423,-38.1268322253095));
#38633=CARTESIAN_POINT('Ctrl Pts',(1.67274744058781,-6.55699664480675,-38.1177730368448));
#38634=CARTESIAN_POINT('Ctrl Pts',(1.85892699982264,-6.50950060384926,-38.1087138483801));
#38635=CARTESIAN_POINT('Ctrl Pts',(2.04296704153323,-6.45409938416893,-38.0996546599154));
#38636=CARTESIAN_POINT('Ctrl Pts',(2.22420161295695,-6.39102622314443,-38.0905954714507));
#38637=CARTESIAN_POINT('Ctrl Pts',(2.40512220820077,-6.3280623319463,-38.0815519773944));
#38638=CARTESIAN_POINT('Ctrl Pts',(2.58341399668192,-6.25739585345925,-38.0725084833381));
#38639=CARTESIAN_POINT('Ctrl Pts',(2.75844710605893,-6.17926035728186,-38.0634649892818));
#38640=CARTESIAN_POINT('Ctrl Pts',(2.93332011329166,-6.10119633135673,-38.0544297672764));
#38641=CARTESIAN_POINT('Ctrl Pts',(3.10494017518044,-6.01567702458991,-38.0453945452711));
#38642=CARTESIAN_POINT('Ctrl Pts',(3.27269761034307,-5.92298399046078,-38.0363593232657));
#38643=CARTESIAN_POINT('Ctrl Pts',(3.44015949342455,-5.83045426127918,-38.0273400193546));
#38644=CARTESIAN_POINT('Ctrl Pts',(3.60377213061202,-5.73077615733481,-38.0183207154435));
#38645=CARTESIAN_POINT('Ctrl Pts',(3.76295077228059,-5.62427688555542,-38.0093014115324));
#38646=CARTESIAN_POINT('Ctrl Pts',(3.92192971322564,-5.51791122455072,-38.0002934229679));
#38647=CARTESIAN_POINT('Ctrl Pts',(4.07648556270885,-5.40474160580249,-37.9912854344035));
#38648=CARTESIAN_POINT('Ctrl Pts',(4.22606068508645,-5.2851395521752,-37.9822774458391));
#38649=CARTESIAN_POINT('Ctrl Pts',(4.37529798681038,-5.16580762397582,-37.9732898021324));
#38650=CARTESIAN_POINT('Ctrl Pts',(4.51957683014816,-5.04007240828892,-37.9643021584257));
#38651=CARTESIAN_POINT('Ctrl Pts',(4.65837129463945,-4.90834655268749,-37.9553145147191));
#38652=CARTESIAN_POINT('Ctrl Pts',(4.77925165334199,-4.79362246240146,-37.9474868999857));
#38653=CARTESIAN_POINT('Ctrl Pts',(4.89597234147034,-4.67435506522983,-37.9396592852524));
#38654=CARTESIAN_POINT('Ctrl Pts',(5.00820507123561,-4.55084288505437,-37.9318316705191));
#38655=CARTESIAN_POINT('Ctrl Pts',(5.12467532145758,-4.42266731131056,-37.9237085120738));
#38656=CARTESIAN_POINT('Ctrl Pts',(5.23625901429123,-4.28997653712542,-37.9155853536285));
#38657=CARTESIAN_POINT('Ctrl Pts',(5.3425943139521,-4.15318853370838,-37.9074621951833));
#38658=CARTESIAN_POINT('Ctrl Pts',(5.44892211641825,-4.01641017456092,-37.8993396094631));
#38659=CARTESIAN_POINT('Ctrl Pts',(5.55000203814904,-3.87553545057345,-37.891217023743));
#38660=CARTESIAN_POINT('Ctrl Pts',(5.64551317557136,-3.73101460523142,-37.8830944380229));
#38661=CARTESIAN_POINT('Ctrl Pts',(5.74103578964029,-3.58647639422174,-37.8749708762904));
#38662=CARTESIAN_POINT('Ctrl Pts',(5.83098808616751,-3.43829149547754,-37.866847314558));
#38663=CARTESIAN_POINT('Ctrl Pts',(5.91509308643174,-3.28693820733633,-37.8587237528255));
#38664=CARTESIAN_POINT('Ctrl Pts',(5.99925934720783,-3.13547467628599,-37.8505942740424));
#38665=CARTESIAN_POINT('Ctrl Pts',(6.07756962728576,-2.98083846683454,-37.8424647952593));
#38666=CARTESIAN_POINT('Ctrl Pts',(6.14979314090534,-2.82353206535248,-37.8343353164761));
#38667=CARTESIAN_POINT('Ctrl Pts',(6.22204609878018,-2.66616153281938,-37.8262025234476));
#38668=CARTESIAN_POINT('Ctrl Pts',(6.28820720415832,-2.50611897639113,-37.818069730419));
#38669=CARTESIAN_POINT('Ctrl Pts',(6.34809434810833,-2.3439255848928,-37.8099369373905));
#38670=CARTESIAN_POINT('Ctrl Pts',(6.40804661024213,-2.18155583268699,-37.8017953011833));
#38671=CARTESIAN_POINT('Ctrl Pts',(6.46171117191644,-2.01703092182005,-37.7936536649762));
#38672=CARTESIAN_POINT('Ctrl Pts',(6.50895596995547,-1.8508865932793,-37.785512028769));
#38673=CARTESIAN_POINT('Ctrl Pts',(6.53302655283478,-1.76623831461031,-37.7813639757086));
#38674=CARTESIAN_POINT('Ctrl Pts',(6.55543153589605,-1.68116984577571,-37.7772159226481));
#38675=CARTESIAN_POINT('Ctrl Pts',(6.57615859055716,-1.59575286051483,-37.7730678695876));
#38676=CARTESIAN_POINT('Ctrl Pts',(6.61833528361732,-1.42194109476349,-37.7646271546095));
#38677=CARTESIAN_POINT('Ctrl Pts',(6.65364800675882,-1.24632775325899,-37.7561864396314));
#38678=CARTESIAN_POINT('Ctrl Pts',(6.6819531313822,-1.06948181378257,-37.7477457246534));
#38679=CARTESIAN_POINT('Ctrl Pts',(6.71023686165885,-0.892769542798911,
-37.7393113895654));
#38680=CARTESIAN_POINT('Ctrl Pts',(6.73152349951128,-0.714826859088382,
-37.7308770544773));
#38681=CARTESIAN_POINT('Ctrl Pts',(6.74572030332436,-0.536233707740832,
-37.7224427193893));
#38682=CARTESIAN_POINT('Ctrl Pts',(6.75990855660553,-0.357748120494308,
-37.7140134641807));
#38683=CARTESIAN_POINT('Ctrl Pts',(6.76701546259102,-0.17861317819431,-37.7055842089721));
#38684=CARTESIAN_POINT('Ctrl Pts',(6.76699997472549,0.000584863454290374,
-37.6971549537635));
#38685=CARTESIAN_POINT('Ctrl Pts',(6.76698449381236,0.179702464314105,-37.6887294823905));
#38686=CARTESIAN_POINT('Ctrl Pts',(6.75985299394651,0.358882775184343,-37.6803040110175));
#38687=CARTESIAN_POINT('Ctrl Pts',(6.74561649975955,0.537537941146272,-37.6718785396446));
#38688=CARTESIAN_POINT('Ctrl Pts',(6.73138421429322,0.716140291458942,-37.6634555590853));
#38689=CARTESIAN_POINT('Ctrl Pts',(6.71005114972376,0.894217474456715,-37.6550325785261));
#38690=CARTESIAN_POINT('Ctrl Pts',(6.68168034297353,1.07118476199073,-37.6466095979669));
#38691=CARTESIAN_POINT('Ctrl Pts',(6.65330906646156,1.24815497973616,-37.6381864779405));
#38692=CARTESIAN_POINT('Ctrl Pts',(6.61789986118044,1.42401493512585,-37.6297633579142));
#38693=CARTESIAN_POINT('Ctrl Pts',(6.57556734176414,1.59818745268662,-37.6213402378879));
#38694=CARTESIAN_POINT('Ctrl Pts',(6.53323335841875,1.77236599342335,-37.612916826576));
#38695=CARTESIAN_POINT('Ctrl Pts',(6.48397566216803,1.94485665586912,-37.6044934152642));
#38696=CARTESIAN_POINT('Ctrl Pts',(6.42795950765314,2.11509469480013,-37.5960700039523));
#38697=CARTESIAN_POINT('Ctrl Pts',(6.37193360372924,2.28536236304583,-37.5876451265762));
#38698=CARTESIAN_POINT('Ctrl Pts',(6.30914700061127,2.45337630934582,-37.5792202492001));
#38699=CARTESIAN_POINT('Ctrl Pts',(6.23981424521007,2.61858877742831,-37.5707953718239));
#38700=CARTESIAN_POINT('Ctrl Pts',(6.17045975023532,2.78385304856668,-37.5623678527925));
#38701=CARTESIAN_POINT('Ctrl Pts',(6.09455513969854,2.9463137827764,-37.5539403337611));
#38702=CARTESIAN_POINT('Ctrl Pts',(6.01236248700822,3.10544462594591,-37.5455128147296));
#38703=CARTESIAN_POINT('Ctrl Pts',(5.93009612712363,3.26471817150532,-37.5370777382249));
#38704=CARTESIAN_POINT('Ctrl Pts',(5.84153061099496,3.42065556275218,-37.5286426617201));
#38705=CARTESIAN_POINT('Ctrl Pts',(5.74697378902983,3.57275541679027,-37.5202075852153));
#38706=CARTESIAN_POINT('Ctrl Pts',(5.6523712671303,3.72492878168888,-37.5117684319825));
#38707=CARTESIAN_POINT('Ctrl Pts',(5.55177184719688,3.87326063165815,-37.5033292787497));
#38708=CARTESIAN_POINT('Ctrl Pts',(5.44552614318835,4.01727943064112,-37.494890125517));
#38709=CARTESIAN_POINT('Ctrl Pts',(5.33916237041437,4.16145827488856,-37.4864415940188));
#38710=CARTESIAN_POINT('Ctrl Pts',(5.2271399805179,4.30131422757586,-37.4779930625207));
#38711=CARTESIAN_POINT('Ctrl Pts',(5.10984998236812,4.43640870047976,-37.4695445310226));
#38712=CARTESIAN_POINT('Ctrl Pts',(5.04504345290673,4.51105277991045,-37.4648764432566));
#38713=CARTESIAN_POINT('Ctrl Pts',(4.97862943853597,4.58424384948346,-37.4602083554906));
#38714=CARTESIAN_POINT('Ctrl Pts',(4.91067862684337,4.65591284538958,-37.4555402677246));
#38715=CARTESIAN_POINT('Ctrl Pts',(4.79069238073492,4.78246459020229,-37.447297447461));
#38716=CARTESIAN_POINT('Ctrl Pts',(4.66564531357555,4.90454994027631,-37.4390546271974));
#38717=CARTESIAN_POINT('Ctrl Pts',(4.53590146638694,5.02174141978944,-37.4308118069338));
#38718=CARTESIAN_POINT('Ctrl Pts',(4.40634680531483,5.13876201643316,-37.4225810059465));
#38719=CARTESIAN_POINT('Ctrl Pts',(4.2721092754121,5.25090272790146,-37.4143502049592));
#38720=CARTESIAN_POINT('Ctrl Pts',(4.13359124472159,5.35777121773233,-37.406119403972));
#38721=CARTESIAN_POINT('Ctrl Pts',(3.99519018441227,5.4645494633695,-37.3978955534151));
#38722=CARTESIAN_POINT('Ctrl Pts',(3.85251609900339,5.56606413430345,-37.3896717028583));
#38723=CARTESIAN_POINT('Ctrl Pts',(3.70600667392114,5.6619611030854,-37.3814478523014));
#38724=CARTESIAN_POINT('Ctrl Pts',(3.55961814680442,5.75777893874386,-37.3732307879755));
#38725=CARTESIAN_POINT('Ctrl Pts',(3.40940088306261,5.84798811539616,-37.3650137236496));
#38726=CARTESIAN_POINT('Ctrl Pts',(3.25582383722723,5.93227613492014,-37.3567966593237));
#38727=CARTESIAN_POINT('Ctrl Pts',(3.20395444979805,5.96074372209468,-37.3540214132527));
#38728=CARTESIAN_POINT('Ctrl Pts',(3.15170206751786,5.988536243908,-37.3512461671817));
#38729=CARTESIAN_POINT('Ctrl Pts',(3.09908550384721,6.01564277861012,-37.3484709211107));
#38730=CARTESIAN_POINT('Origin',(0.,0.,-63.6971797838103));
#38731=CARTESIAN_POINT('',(3.09908550384724,6.01564277861011,-34.9544861942313));
#38732=CARTESIAN_POINT('',(3.0990855038472,6.01564277861013,-35.3486949847746));
#38733=CARTESIAN_POINT('',(3.09908550384721,6.01564277861012,-63.6971797838103));
#38734=CARTESIAN_POINT('',(-6.76699965717165,-0.00196728107387918,-36.30282021619));
#38735=CARTESIAN_POINT('Ctrl Pts',(-6.76699958899529,-0.00235850324450193,
-36.30282021619));
#38736=CARTESIAN_POINT('Ctrl Pts',(-6.76693518406772,-0.187148632078428,
-36.2941557813363));
#38737=CARTESIAN_POINT('Ctrl Pts',(-6.75929728402724,-0.371773878308019,
-36.2854913464826));
#38738=CARTESIAN_POINT('Ctrl Pts',(-6.744151692339,-0.555614030349293,-36.276826911629));
#38739=CARTESIAN_POINT('Ctrl Pts',(-6.72898809559704,-0.739672731251764,
-36.2681521765098));
#38740=CARTESIAN_POINT('Ctrl Pts',(-6.70629902098999,-0.922944181880305,
-36.2594774413907));
#38741=CARTESIAN_POINT('Ctrl Pts',(-6.67620166752469,-1.10481686018114,
-36.2508027062715));
#38742=CARTESIAN_POINT('Ctrl Pts',(-6.64604452067217,-1.28705085873868,
-36.2421107373515));
#38743=CARTESIAN_POINT('Ctrl Pts',(-6.60844972316436,-1.46788023873274,
-36.2334187684315));
#38744=CARTESIAN_POINT('Ctrl Pts',(-6.56358525718865,-1.64670506515762,
-36.2247267995115));
#38745=CARTESIAN_POINT('Ctrl Pts',(-6.53973275556198,-1.7417785129392,-36.2201056545075));
#38746=CARTESIAN_POINT('Ctrl Pts',(-6.51382625408026,-1.83628563886716,
-36.2154845095034));
#38747=CARTESIAN_POINT('Ctrl Pts',(-6.48589658976399,-1.93013844759589,
-36.2108633644994));
#38748=CARTESIAN_POINT('Ctrl Pts',(-6.43488188762416,-2.10156453521602,
-36.2024226495213));
#38749=CARTESIAN_POINT('Ctrl Pts',(-6.37702900081694,-2.27109352276146,
-36.1939819345432));
#38750=CARTESIAN_POINT('Ctrl Pts',(-6.3125001209302,-2.43816144323058,-36.1855412195651));
#38751=CARTESIAN_POINT('Ctrl Pts',(-6.24802001501109,-2.60510308589419,
-36.1771068844771));
#38752=CARTESIAN_POINT('Ctrl Pts',(-6.17687409466979,-2.76958705975169,
-36.1686725493891));
#38753=CARTESIAN_POINT('Ctrl Pts',(-6.0992740452056,-2.93106552664407,-36.1602382143011));
#38754=CARTESIAN_POINT('Ctrl Pts',(-6.0217207331413,-3.09244673736546,-36.1518089590924));
#38755=CARTESIAN_POINT('Ctrl Pts',(-5.93772118578649,-3.25082575021071,
-36.1433797038838));
#38756=CARTESIAN_POINT('Ctrl Pts',(-5.8475349372065,-3.40567528665746,-36.1349504486752));
#38757=CARTESIAN_POINT('Ctrl Pts',(-5.75738917262334,-3.56045531219494,
-36.1265249773022));
#38758=CARTESIAN_POINT('Ctrl Pts',(-5.66106241171812,-3.71170873274347,
-36.1180995059292));
#38759=CARTESIAN_POINT('Ctrl Pts',(-5.55885999157159,-3.85893309013057,
-36.1096740345562));
#38760=CARTESIAN_POINT('Ctrl Pts',(-5.45668778542541,-4.00611392372658,
-36.1012510539969));
#38761=CARTESIAN_POINT('Ctrl Pts',(-5.34864357397227,-4.14926779590544,
-36.0928280734377));
#38762=CARTESIAN_POINT('Ctrl Pts',(-5.23507606828636,-4.28792112325489,
-36.0844050928785));
#38763=CARTESIAN_POINT('Ctrl Pts',(-5.12150668215806,-4.42657674641591,
-36.0759819728521));
#38764=CARTESIAN_POINT('Ctrl Pts',(-5.00241402517405,-4.56073141379927,
-36.0675588528258));
#38765=CARTESIAN_POINT('Ctrl Pts',(-4.87818757972632,-4.68994402280068,
-36.0591357327995));
#38766=CARTESIAN_POINT('Ctrl Pts',(-4.75395683832092,-4.81916110018963,
-36.0507123214876));
#38767=CARTESIAN_POINT('Ctrl Pts',(-4.62459218548861,-4.94343553790109,
-36.0422889101758));
#38768=CARTESIAN_POINT('Ctrl Pts',(-4.49052061019821,-5.06236245733009,
-36.0338654988639));
#38769=CARTESIAN_POINT('Ctrl Pts',(-4.35642570023534,-5.18131007555901,
-36.0254406214878));
#38770=CARTESIAN_POINT('Ctrl Pts',(-4.21762248400595,-5.29490809863485,
-36.0170157441117));
#38771=CARTESIAN_POINT('Ctrl Pts',(-4.07457199843356,-5.40279113325522,
-36.0085908667356));
#38772=CARTESIAN_POINT('Ctrl Pts',(-3.93147665878687,-5.51070799504947,
-36.0001633477041));
#38773=CARTESIAN_POINT('Ctrl Pts',(-3.78413166080402,-5.61290609498366,
-35.9917358286727));
#38774=CARTESIAN_POINT('Ctrl Pts',(-3.63302834270189,-5.70906245027367,
-35.9833083096412));
#38775=CARTESIAN_POINT('Ctrl Pts',(-3.48178952098421,-5.80530503486666,
-35.9748732331365));
#38776=CARTESIAN_POINT('Ctrl Pts',(-3.32678592639158,-5.89549486965611,
-35.9664381566317));
#38777=CARTESIAN_POINT('Ctrl Pts',(-3.16853589061581,-5.97935358629003,
-35.9580030801269));
#38778=CARTESIAN_POINT('Ctrl Pts',(-3.01020937155624,-6.06325283239362,
-35.9495639268941));
#38779=CARTESIAN_POINT('Ctrl Pts',(-2.84863358030992,-6.14081470891375,
-35.9411247736614));
#38780=CARTESIAN_POINT('Ctrl Pts',(-2.68434878449117,-6.21180815891804,
-35.9326856204286));
#38781=CARTESIAN_POINT('Ctrl Pts',(-2.51988142220354,-6.28288050254982,
-35.9242370889305));
#38782=CARTESIAN_POINT('Ctrl Pts',(-2.35269934930984,-6.3473697097327,-35.9157885574324));
#38783=CARTESIAN_POINT('Ctrl Pts',(-2.18336116201439,-6.40509352283065,
-35.9073400259343));
#38784=CARTESIAN_POINT('Ctrl Pts',(-2.08979631934266,-6.43698780242099,
-35.9026719381683));
#38785=CARTESIAN_POINT('Ctrl Pts',(-1.99557349648872,-6.46681754635892,
-35.8980038504023));
#38786=CARTESIAN_POINT('Ctrl Pts',(-1.90078853251652,-6.49455864202131,
-35.8933357626363));
#38787=CARTESIAN_POINT('Ctrl Pts',(-1.73346056929066,-6.543531188302,-35.8850949870396));
#38788=CARTESIAN_POINT('Ctrl Pts',(-1.56400775857775,-6.58610057937274,
-35.8768542114428));
#38789=CARTESIAN_POINT('Ctrl Pts',(-1.39295940348758,-6.6220807228722,-35.8686134358461));
#38790=CARTESIAN_POINT('Ctrl Pts',(-1.22210050299461,-6.658021014462,-35.8603817878017));
#38791=CARTESIAN_POINT('Ctrl Pts',(-1.04964992212572,-6.68738651814767,
-35.8521501397573));
#38792=CARTESIAN_POINT('Ctrl Pts',(-0.876152964625214,-6.71004060960725,
-35.8439184917129));
#38793=CARTESIAN_POINT('Ctrl Pts',(-0.702817255036443,-6.73267364637519,
-35.8356944941546));
#38794=CARTESIAN_POINT('Ctrl Pts',(-0.528437456303542,-6.7486076474621,
-35.8274704965963));
#38795=CARTESIAN_POINT('Ctrl Pts',(-0.353570028647881,-6.75775681974736,
-35.8192464990381));
#38796=CARTESIAN_POINT('Ctrl Pts',(-0.178857097044056,-6.76689790870336,
-35.8110297674136));
#38797=CARTESIAN_POINT('Ctrl Pts',(-0.00365774913480038,-6.76926609785636,
-35.8028130357891));
#38798=CARTESIAN_POINT('Ctrl Pts',(0.171465578530179,-6.76482731157118,
-35.7945963041645));
#38799=CARTESIAN_POINT('Ctrl Pts',(0.346499184031142,-6.76039079944054,
-35.7863837822759));
#38800=CARTESIAN_POINT('Ctrl Pts',(0.521456492059731,-6.7491542665203,-35.7781712603872));
#38801=CARTESIAN_POINT('Ctrl Pts',(0.695773782498911,-6.73113570236013,
-35.7699587384985));
#38802=CARTESIAN_POINT('Ctrl Pts',(0.870032780397239,-6.71312316369452,
-35.7617489629166));
#38803=CARTESIAN_POINT('Ctrl Pts',(1.04365183355713,-6.6883331483432,-35.7535391873348));
#38804=CARTESIAN_POINT('Ctrl Pts',(1.21607096902238,-6.65683561448688,-35.7453294117529));
#38805=CARTESIAN_POINT('Ctrl Pts',(1.29137916791349,-6.64307831001003,-35.7417435950702));
#38806=CARTESIAN_POINT('Ctrl Pts',(1.36645852944062,-6.6280420689442,-35.7381577783875));
#38807=CARTESIAN_POINT('Ctrl Pts',(1.44126284911144,-6.61173580837674,-35.7345719617048));
#38808=CARTESIAN_POINT('Ctrl Pts',(1.62606603232124,-6.57145138533304,-35.7257132441831));
#38809=CARTESIAN_POINT('Ctrl Pts',(1.80899833781516,-6.52345413561644,-35.7168545266613));
#38810=CARTESIAN_POINT('Ctrl Pts',(1.98944073126631,-6.46795288918979,-35.7079958091395));
#38811=CARTESIAN_POINT('Ctrl Pts',(2.1702207034546,-6.41234780884518,-35.6991205183801));
#38812=CARTESIAN_POINT('Ctrl Pts',(2.34850120656789,-6.34921075250704,-35.6902452276207));
#38813=CARTESIAN_POINT('Ctrl Pts',(2.523681965802,-6.27879911571359,-35.6813699368612));
#38814=CARTESIAN_POINT('Ctrl Pts',(2.69936027778126,-6.20818749403979,-35.6724694382804));
#38815=CARTESIAN_POINT('Ctrl Pts',(2.87192098591952,-6.1302600431543,-35.6635689396997));
#38816=CARTESIAN_POINT('Ctrl Pts',(3.04078449077462,-6.04532204937542,-35.6546684411189));
#38817=CARTESIAN_POINT('Ctrl Pts',(3.20987658638236,-5.96026907492061,-35.6457558939213));
#38818=CARTESIAN_POINT('Ctrl Pts',(3.37526125240075,-5.86818672274897,-35.6368433467236));
#38819=CARTESIAN_POINT('Ctrl Pts',(3.53638564474794,-5.76942506421747,-35.627930799526));
#38820=CARTESIAN_POINT('Ctrl Pts',(3.6978658154893,-5.67044533029858,-35.6189985725537));
#38821=CARTESIAN_POINT('Ctrl Pts',(3.8550666747862,-5.56475692654458,-35.6100663455815));
#38822=CARTESIAN_POINT('Ctrl Pts',(4.00746403775423,-5.45275352332256,-35.6011341186092));
#38823=CARTESIAN_POINT('Ctrl Pts',(4.15149714397457,-5.34689737358918,-35.5926921326639));
#38824=CARTESIAN_POINT('Ctrl Pts',(4.29123969267153,-5.23540085759743,-35.5842501467186));
#38825=CARTESIAN_POINT('Ctrl Pts',(4.42627796346352,-5.11862797926918,-35.5758081607733));
#38826=CARTESIAN_POINT('Ctrl Pts',(4.55782891504988,-5.00487072235626,-35.5675841863557));
#38827=CARTESIAN_POINT('Ctrl Pts',(4.68516603952161,-4.88588801639151,-35.5593602119381));
#38828=CARTESIAN_POINT('Ctrl Pts',(4.80784948061873,-4.76202397849006,-35.5511362375206));
#38829=CARTESIAN_POINT('Ctrl Pts',(4.93040335609873,-4.63829075303049,-35.5429209484179));
#38830=CARTESIAN_POINT('Ctrl Pts',(5.04831308484545,-4.50968671395908,-35.5347056593153));
#38831=CARTESIAN_POINT('Ctrl Pts',(5.16117197961678,-4.37659602851561,-35.5264903702126));
#38832=CARTESIAN_POINT('Ctrl Pts',(5.27393432153411,-4.24361920459406,-35.5182821094404));
#38833=CARTESIAN_POINT('Ctrl Pts',(5.38165420473158,-4.10616365083521,-35.5100738486682));
#38834=CARTESIAN_POINT('Ctrl Pts',(5.48396185591917,-3.9646502194801,-35.5018655878961));
#38835=CARTESIAN_POINT('Ctrl Pts',(5.58620249592566,-3.82322947896547,-35.4936627035082));
#38836=CARTESIAN_POINT('Ctrl Pts',(5.68303775583713,-3.67775644467268,-35.4854598191203));
#38837=CARTESIAN_POINT('Ctrl Pts',(5.77413817168248,-3.52868493554176,-35.4772569347324));
#38838=CARTESIAN_POINT('Ctrl Pts',(5.86519718091487,-3.37968118182362,-35.4690577786882));
#38839=CARTESIAN_POINT('Ctrl Pts',(5.95052635246151,-3.22708251709033,-35.460858622644));
#38840=CARTESIAN_POINT('Ctrl Pts',(6.02983954427082,-3.07137169198843,-35.4526594665998));
#38841=CARTESIAN_POINT('Ctrl Pts',(6.10914583776106,-2.91567440994198,-35.4444610236827));
#38842=CARTESIAN_POINT('Ctrl Pts',(6.18243702350282,-2.75686582210234,-35.4362625807657));
#38843=CARTESIAN_POINT('Ctrl Pts',(6.24947276527891,-2.59545355497592,-35.4280641378487));
#38844=CARTESIAN_POINT('Ctrl Pts',(6.31650783945839,-2.43404289532458,-35.4198657765785));
#38845=CARTESIAN_POINT('Ctrl Pts',(6.37728745520165,-2.27002893889326,-35.4116674153083));
#38846=CARTESIAN_POINT('Ctrl Pts',(6.43161936994523,-2.10393946684437,-35.403469054038));
#38847=CARTESIAN_POINT('Ctrl Pts',(6.48596061338865,-1.937821477508,-35.3952692851228));
#38848=CARTESIAN_POINT('Ctrl Pts',(6.53385183871864,-1.76962760350437,-35.3870695162075));
#38849=CARTESIAN_POINT('Ctrl Pts',(6.57515062560832,-1.59990101273879,-35.3788697472922));
#38850=CARTESIAN_POINT('Ctrl Pts',(6.61646400572987,-1.43011444782673,-35.3706670809279));
#38851=CARTESIAN_POINT('Ctrl Pts',(6.65118022228053,-1.25879443559642,-35.3624644145636));
#38852=CARTESIAN_POINT('Ctrl Pts',(6.67920792109747,-1.08649461422909,-35.3542617481993));
#38853=CARTESIAN_POINT('Ctrl Pts',(6.70726745237469,-0.91399910333133,-35.3460497656563));
#38854=CARTESIAN_POINT('Ctrl Pts',(6.72862323197611,-0.740521914505824,
-35.3378377831133));
#38855=CARTESIAN_POINT('Ctrl Pts',(6.74323566301143,-0.566623149095401,
-35.3296258005702));
#38856=CARTESIAN_POINT('Ctrl Pts',(6.75785671265607,-0.392621815842825,
-35.3214089744889));
#38857=CARTESIAN_POINT('Ctrl Pts',(6.76572646938014,-0.218198768086149,
-35.3131921484076));
#38858=CARTESIAN_POINT('Ctrl Pts',(6.76685750815821,-0.043914283358825,
-35.3049753223263));
#38859=CARTESIAN_POINT('Ctrl Pts',(6.76799029116142,0.130638973215197,-35.2967458247125));
#38860=CARTESIAN_POINT('Ctrl Pts',(6.76236360065717,0.305052881495234,-35.2885163270986));
#38861=CARTESIAN_POINT('Ctrl Pts',(6.7500420401126,0.478770776794607,-35.2802868294848));
#38862=CARTESIAN_POINT('Ctrl Pts',(6.73905912604876,0.633615506772126,-35.2729514059599));
#38863=CARTESIAN_POINT('Ctrl Pts',(6.72275777400732,0.78790716291095,-35.2656159824351));
#38864=CARTESIAN_POINT('Ctrl Pts',(6.70121782300113,0.941259097534815,-35.2582805589102));
#38865=CARTESIAN_POINT('Ctrl Pts',(6.67751751762014,1.10999149995793,-35.250209427384));
#38866=CARTESIAN_POINT('Ctrl Pts',(6.64739683500269,1.27813628400426,-35.2421382958579));
#38867=CARTESIAN_POINT('Ctrl Pts',(6.61088632372678,1.44515432212698,-35.2340671643317));
#38868=CARTESIAN_POINT('Ctrl Pts',(6.57442149695097,1.61196337562268,-35.2260061319687));
#38869=CARTESIAN_POINT('Ctrl Pts',(6.53158282944332,1.77764812867464,-35.2179450996057));
#38870=CARTESIAN_POINT('Ctrl Pts',(6.48245267133049,1.94167359871843,-35.2098840672426));
#38871=CARTESIAN_POINT('Ctrl Pts',(6.43337321381493,2.10552980023922,-35.2018313535818));
#38872=CARTESIAN_POINT('Ctrl Pts',(6.37801529274396,2.26772977208575,-35.193778639921));
#38873=CARTESIAN_POINT('Ctrl Pts',(6.31651243020506,2.4277478697478,-35.1857259262602));
#38874=CARTESIAN_POINT('Ctrl Pts',(6.25505956869748,2.5876358747673,-35.1776797593514));
#38875=CARTESIAN_POINT('Ctrl Pts',(6.18747184257628,2.74534518985611,-35.1696335924426));
#38876=CARTESIAN_POINT('Ctrl Pts',(6.11393278631222,2.90036461233007,-35.1615874255338));
#38877=CARTESIAN_POINT('Ctrl Pts',(6.04043742973722,3.05529191639912,-35.1535460399617));
#38878=CARTESIAN_POINT('Ctrl Pts',(5.96099794307738,3.20753217389843,-35.1455046543896));
#38879=CARTESIAN_POINT('Ctrl Pts',(5.87584619560389,3.35659358362124,-35.1374632688175));
#38880=CARTESIAN_POINT('Ctrl Pts',(5.79071677786396,3.50561590428644,-35.1294239919749));
#38881=CARTESIAN_POINT('Ctrl Pts',(5.69987826131055,3.65146071018358,-35.1213847151323));
#38882=CARTESIAN_POINT('Ctrl Pts',(5.60360876930624,3.79366020625916,-35.1133454382897));
#38883=CARTESIAN_POINT('Ctrl Pts',(5.50734934030068,3.9358448382971,-35.1053070017884));
#38884=CARTESIAN_POINT('Ctrl Pts',(5.40566027432216,4.0743846093166,-35.0972685652871));
#38885=CARTESIAN_POINT('Ctrl Pts',(5.29886326791086,4.20884034717225,-35.0892301287858));
#38886=CARTESIAN_POINT('Ctrl Pts',(5.19205628380869,4.34330864678251,-35.08119094128));
#38887=CARTESIAN_POINT('Ctrl Pts',(5.08014064171457,4.47369186142722,-35.0731517537742));
#38888=CARTESIAN_POINT('Ctrl Pts',(4.96347849765918,4.59958369890961,-35.0651125662683));
#38889=CARTESIAN_POINT('Ctrl Pts',(4.84678235582765,4.72551222389283,-35.057071035976));
#38890=CARTESIAN_POINT('Ctrl Pts',(4.72533721287457,4.84694649318234,-35.0490295056837));
#38891=CARTESIAN_POINT('Ctrl Pts',(4.59954214525066,4.96351700451031,-35.0409879753914));
#38892=CARTESIAN_POINT('Ctrl Pts',(4.4736185205672,5.08020664580457,-35.0329382270067));
#38893=CARTESIAN_POINT('Ctrl Pts',(4.34333636856366,5.19202235009193,-35.0248884786219));
#38894=CARTESIAN_POINT('Ctrl Pts',(4.20912845914178,5.29863441034034,-35.0168387302372));
#38895=CARTESIAN_POINT('Ctrl Pts',(4.07484461333391,5.40530679292441,-35.0087844272118));
#38896=CARTESIAN_POINT('Ctrl Pts',(3.93663088636786,5.50676944735738,-35.0007301241865));
#38897=CARTESIAN_POINT('Ctrl Pts',(3.7949486641671,5.60273626332138,-34.9926758211611));
#38898=CARTESIAN_POINT('Ctrl Pts',(3.65307088193487,5.69883553961285,-34.9846104010052));
#38899=CARTESIAN_POINT('Ctrl Pts',(3.50771536059478,5.78942363358591,-34.9765449808494));
#38900=CARTESIAN_POINT('Ctrl Pts',(3.35936841129851,5.87426019828623,-34.9684795606935));
#38901=CARTESIAN_POINT('Ctrl Pts',(3.27357526868321,5.92332352940866,-34.9638151052061));
#38902=CARTESIAN_POINT('Ctrl Pts',(3.18678200517044,5.97046407269439,-34.9591506497187));
#38903=CARTESIAN_POINT('Ctrl Pts',(3.09908550384724,6.01564277861011,-34.9544861942313));
#38904=CARTESIAN_POINT('Ctrl Pts',(3.09908550384719,6.01564277861013,-36.9542436419538));
#38905=CARTESIAN_POINT('Ctrl Pts',(2.93373232018322,6.10082796552483,-36.9454941940545));
#38906=CARTESIAN_POINT('Ctrl Pts',(2.76486502144414,6.17919158180196,-36.9367447461552));
#38907=CARTESIAN_POINT('Ctrl Pts',(2.59305716434334,6.25046746591386,-36.927995298256));
#38908=CARTESIAN_POINT('Ctrl Pts',(2.42125069459268,6.3217427744723,-36.9192459210085));
#38909=CARTESIAN_POINT('Ctrl Pts',(2.24650397871046,6.3859303555783,-36.9104965437611));
#38910=CARTESIAN_POINT('Ctrl Pts',(2.06941053323762,6.44281220003542,-36.9017471665137));
#38911=CARTESIAN_POINT('Ctrl Pts',(1.89231845896672,6.49969360406689,-36.8929978570111));
#38912=CARTESIAN_POINT('Ctrl Pts',(1.71287996431492,6.54926929700884,-36.8842485475085));
#38913=CARTESIAN_POINT('Ctrl Pts',(1.53170449173489,6.59137090065482,-36.8754992380059));
#38914=CARTESIAN_POINT('Ctrl Pts',(1.3505303617816,6.63347219230085,-36.8667499933413));
#38915=CARTESIAN_POINT('Ctrl Pts',(1.16761955878839,6.66809944062455,-36.8580007486767));
#38916=CARTESIAN_POINT('Ctrl Pts',(0.983593309310475,6.69513503985392,-36.8492515040122));
#38917=CARTESIAN_POINT('Ctrl Pts',(0.799568362459997,6.72217044771214,-36.840502321279));
#38918=CARTESIAN_POINT('Ctrl Pts',(0.61442826843864,6.74161427235977,-36.8317531385458));
#38919=CARTESIAN_POINT('Ctrl Pts',(0.428801816330342,6.75340047696802,-36.8230039558126));
#38920=CARTESIAN_POINT('Ctrl Pts',(0.243176616522986,6.76518660206241,-36.8142548321045));
#38921=CARTESIAN_POINT('Ctrl Pts',(0.0570653511657919,6.76931519233996,
-36.8055057083964));
#38922=CARTESIAN_POINT('Ctrl Pts',(-0.128899900799569,6.76577222610796,
-36.7967565846883));
#38923=CARTESIAN_POINT('Ctrl Pts',(-0.314863959941717,6.76222928260135,
-36.788007517099));
#38924=CARTESIAN_POINT('Ctrl Pts',(-0.500681721080533,6.75101488651278,
-36.7792584495097));
#38925=CARTESIAN_POINT('Ctrl Pts',(-0.685722110173307,6.73216712415991,
-36.7705093819204));
#38926=CARTESIAN_POINT('Ctrl Pts',(-0.870761373827663,6.71331947644145,
-36.7617603675441));
#38927=CARTESIAN_POINT('Ctrl Pts',(-1.05502298984352,6.68683858439995,-36.7530113531677));
#38928=CARTESIAN_POINT('Ctrl Pts',(-1.23788117676073,6.65281438131423,-36.7442623387914));
#38929=CARTESIAN_POINT('Ctrl Pts',(-1.43009641451808,6.61704912302374,-36.7350656279038));
#38930=CARTESIAN_POINT('Ctrl Pts',(-1.62076048992713,6.57294837083161,-36.7258689170163));
#38931=CARTESIAN_POINT('Ctrl Pts',(-1.80915798961151,6.52067760042044,-36.7166722061288));
#38932=CARTESIAN_POINT('Ctrl Pts',(-1.98840443003026,6.47094578577405,-36.7079222084223));
#38933=CARTESIAN_POINT('Ctrl Pts',(-2.165598959522,6.41381888474472,-36.6991722107158));
#38934=CARTESIAN_POINT('Ctrl Pts',(-2.34013966242325,6.34949095285233,-36.6904222130093));
#38935=CARTESIAN_POINT('Ctrl Pts',(-2.51467682554014,6.28516432556685,-36.6816723927577));
#38936=CARTESIAN_POINT('Ctrl Pts',(-2.68656000078837,6.21363705879663,-36.6729225725061));
#38937=CARTESIAN_POINT('Ctrl Pts',(-2.85520533840879,6.13515211510863,-36.6641727522545));
#38938=CARTESIAN_POINT('Ctrl Pts',(-3.02384747998321,6.05666865881124,-36.6554230978232));
#38939=CARTESIAN_POINT('Ctrl Pts',(-3.18925164684534,5.97122791039846,-36.646673443392));
#38940=CARTESIAN_POINT('Ctrl Pts',(-3.35085601829158,5.87912008251908,-36.6379237889607));
#38941=CARTESIAN_POINT('Ctrl Pts',(-3.51245754191427,5.78701387778169,-36.6291742887176));
#38942=CARTESIAN_POINT('Ctrl Pts',(-3.67025915510954,5.68824097060971,-36.6204247884744));
#38943=CARTESIAN_POINT('Ctrl Pts',(-3.8237248792886,5.58313684656837,-36.6116752882313));
#38944=CARTESIAN_POINT('Ctrl Pts',(-3.97718810300834,5.47803443501747,-36.6029259305462));
#38945=CARTESIAN_POINT('Ctrl Pts',(-4.12631534263071,5.36660117496341,-36.5941765728611));
#38946=CARTESIAN_POINT('Ctrl Pts',(-4.27060009886279,5.24921554097306,-36.5854272151759));
#38947=CARTESIAN_POINT('Ctrl Pts',(-4.41488269594255,5.13183166360255,-36.5766779884208));
#38948=CARTESIAN_POINT('Ctrl Pts',(-4.55432273235118,5.00849577139443,-36.5679287616656));
#38949=CARTESIAN_POINT('Ctrl Pts',(-4.68844662480226,4.87962675277325,-36.5591795349104));
#38950=CARTESIAN_POINT('Ctrl Pts',(-4.8225686883517,4.75075949139869,-36.5504304274589));
#38951=CARTESIAN_POINT('Ctrl Pts',(-4.95137454637869,4.61635945312518,-36.5416813200074));
#38952=CARTESIAN_POINT('Ctrl Pts',(-5.07442674461079,4.47688309134589,-36.5329322125559));
#38953=CARTESIAN_POINT('Ctrl Pts',(-5.19747742838539,4.33740844616351,-36.5241832127836));
#38954=CARTESIAN_POINT('Ctrl Pts',(-5.31477440450927,4.19285781736029,-36.5154342130112));
#38955=CARTESIAN_POINT('Ctrl Pts',(-5.42591931531152,4.04372211999407,-36.5066852132388));
#38956=CARTESIAN_POINT('Ctrl Pts',(-5.53707636462979,3.89457013500804,-36.4979352579582));
#38957=CARTESIAN_POINT('Ctrl Pts',(-5.64207983273467,3.74083230916426,-36.4891853026777));
#38958=CARTESIAN_POINT('Ctrl Pts',(-5.74057303468742,3.58303087251836,-36.4804353473971));
#38959=CARTESIAN_POINT('Ctrl Pts',(-5.83906243363762,3.42523552887436,-36.4716857299683));
#38960=CARTESIAN_POINT('Ctrl Pts',(-5.93104191768424,3.26337713156995,-36.4629361125395));
#38961=CARTESIAN_POINT('Ctrl Pts',(-6.01619906699656,3.09800545291155,-36.4541864951107));
#38962=CARTESIAN_POINT('Ctrl Pts',(-6.10135338095374,2.93263928039612,-36.4454371690053));
#38963=CARTESIAN_POINT('Ctrl Pts',(-6.17968568352823,2.76376031540258,-36.4366878428999));
#38964=CARTESIAN_POINT('Ctrl Pts',(-6.25092992694864,2.59194213831594,-36.4279385167945));
#38965=CARTESIAN_POINT('Ctrl Pts',(-6.32217217691082,2.42012876880875,-36.4191894355007));
#38966=CARTESIAN_POINT('Ctrl Pts',(-6.3863266548383,2.24537661647729,-36.4104403542069));
#38967=CARTESIAN_POINT('Ctrl Pts',(-6.4431754786933,2.06827917621518,-36.4016912729131));
#38968=CARTESIAN_POINT('Ctrl Pts',(-6.5000294423592,1.8911657242348,-36.3929414005982));
#38969=CARTESIAN_POINT('Ctrl Pts',(-6.54957634250385,1.7117068328925,-36.3841915282832));
#38970=CARTESIAN_POINT('Ctrl Pts',(-6.59164787708384,1.53051209225411,-36.3754416559682));
#38971=CARTESIAN_POINT('Ctrl Pts',(-6.63371649075002,1.34932993148067,-36.3666923911334));
#38972=CARTESIAN_POINT('Ctrl Pts',(-6.6683107125712,1.1664124417403,-36.3579431262987));
#38973=CARTESIAN_POINT('Ctrl Pts',(-6.69531304840331,0.982380875160164,
-36.3491938614639));
#38974=CARTESIAN_POINT('Ctrl Pts',(-6.72231677033043,0.798339861795949,
-36.3404441475082));
#38975=CARTESIAN_POINT('Ctrl Pts',(-6.74172778477889,0.613184940730217,
-36.3316944335525));
#38976=CARTESIAN_POINT('Ctrl Pts',(-6.75348015835518,0.42754502769057,-36.3229447195969));
#38977=CARTESIAN_POINT('Ctrl Pts',(-6.7624903836522,0.285219953547091,-36.3162365517946));
#38978=CARTESIAN_POINT('Ctrl Pts',(-6.76699999999999,0.142609995757826,
-36.3095283839923));
#38979=CARTESIAN_POINT('Ctrl Pts',(-6.767,6.92579744391243E-13,-36.30282021619));
#38980=CARTESIAN_POINT('',(-6.766998182033,0.00496027842551228,-36.697179783844));
#38981=CARTESIAN_POINT('Ctrl Pts',(3.09908550384721,6.01564277861012,-37.3484709211107));
#38982=CARTESIAN_POINT('Ctrl Pts',(2.93573755334438,6.09979492728598,-37.3398551787245));
#38983=CARTESIAN_POINT('Ctrl Pts',(2.76887746110941,6.17733142416523,-37.3312394363382));
#38984=CARTESIAN_POINT('Ctrl Pts',(2.59908859426785,6.24796186601253,-37.3226236939519));
#38985=CARTESIAN_POINT('Ctrl Pts',(2.42929972742626,6.31859230785985,-37.3140079515656));
#38986=CARTESIAN_POINT('Ctrl Pts',(2.25658249603023,6.38231650272491,-37.3053922091793));
#38987=CARTESIAN_POINT('Ctrl Pts',(2.08154640978273,6.43890157899006,-37.296776466793));
#38988=CARTESIAN_POINT('Ctrl Pts',(1.90157407836224,6.49708242796451,-37.2879177492713));
#38989=CARTESIAN_POINT('Ctrl Pts',(1.71933738879032,6.54765666396894,-37.2790590317495));
#38990=CARTESIAN_POINT('Ctrl Pts',(1.53547637484139,6.59049325182144,-37.2702003142278));
#38991=CARTESIAN_POINT('Ctrl Pts',(1.35127138646322,6.63340998005031,-37.2613250234683));
#38992=CARTESIAN_POINT('Ctrl Pts',(1.16543625335621,6.66856007218692,-37.2524497327088));
#38993=CARTESIAN_POINT('Ctrl Pts',(0.978619236211917,6.69586390173188,-37.2435744419492));
#38994=CARTESIAN_POINT('Ctrl Pts',(0.791271616735659,6.72324528029164,-37.2346739433685));
#38995=CARTESIAN_POINT('Ctrl Pts',(0.602936790772713,6.74273576320412,-37.2257734447877));
#38996=CARTESIAN_POINT('Ctrl Pts',(0.414269250765005,6.75430751357018,-37.2168729462069));
#38997=CARTESIAN_POINT('Ctrl Pts',(0.225346311255239,6.76589492863024,-37.2079603990093));
#38998=CARTESIAN_POINT('Ctrl Pts',(0.0360900172276769,6.76954218877923,
-37.1990478518116));
#38999=CARTESIAN_POINT('Ctrl Pts',(-0.152845724085443,6.76527362230301,
-37.190135304614));
#39000=CARTESIAN_POINT('Ctrl Pts',(-0.342198653966852,6.76099563041514,
-37.1812030776417));
#39001=CARTESIAN_POINT('Ctrl Pts',(-0.531229355054916,6.74876685705625,
-37.1722708506695));
#39002=CARTESIAN_POINT('Ctrl Pts',(-0.719286747375817,6.72866372878371,
-37.1633386236972));
#39003=CARTESIAN_POINT('Ctrl Pts',(-0.897022699205253,6.70966395114046,
-37.154896637752));
#39004=CARTESIAN_POINT('Ctrl Pts',(-1.07388913092905,6.68363092743483,-37.1464546518068));
#39005=CARTESIAN_POINT('Ctrl Pts',(-1.24934535075696,6.65067103340272,-37.1380126658615));
#39006=CARTESIAN_POINT('Ctrl Pts',(-1.42027047105775,6.61856231786066,-37.129788691444));
#39007=CARTESIAN_POINT('Ctrl Pts',(-1.59018359197934,6.57981752561607,-37.1215647170264));
#39008=CARTESIAN_POINT('Ctrl Pts',(-1.75853144301131,6.53451269521611,-37.1133407426088));
#39009=CARTESIAN_POINT('Ctrl Pts',(-1.92670150237886,6.4892557111127,-37.1051254535062));
#39010=CARTESIAN_POINT('Ctrl Pts',(-2.09330924027813,6.43745257732025,-37.0969101644035));
#39011=CARTESIAN_POINT('Ctrl Pts',(-2.25780989650979,6.37923063317376,-37.0886948753009));
#39012=CARTESIAN_POINT('Ctrl Pts',(-2.42216981941357,6.32105849896811,-37.0804866145287));
#39013=CARTESIAN_POINT('Ctrl Pts',(-2.58442591466463,6.25647861007735,-37.0722783537565));
#39014=CARTESIAN_POINT('Ctrl Pts',(-2.74404686196727,6.18566858304966,-37.0640700929843));
#39015=CARTESIAN_POINT('Ctrl Pts',(-2.90356325806401,6.1149049363614,-37.0558672085965));
#39016=CARTESIAN_POINT('Ctrl Pts',(-3.06044761763232,6.0379194247961,-37.0476643242087));
#39017=CARTESIAN_POINT('Ctrl Pts',(-3.21418686550801,5.95493843743122,-37.0394614398208));
#39018=CARTESIAN_POINT('Ctrl Pts',(-3.36785623640807,5.87199516626771,-37.0312622837766));
#39019=CARTESIAN_POINT('Ctrl Pts',(-3.51838302864861,5.78306201827077,-37.0230631277325));
#39020=CARTESIAN_POINT('Ctrl Pts',(-3.6652770460092,5.68841218408073,-37.0148639716883));
#39021=CARTESIAN_POINT('Ctrl Pts',(-3.81215828716303,5.59377058212419,-37.0066655287713));
#39022=CARTESIAN_POINT('Ctrl Pts',(-3.95540707695803,5.49341347125853,-36.9984670858543));
#39023=CARTESIAN_POINT('Ctrl Pts',(-4.09456028555036,5.38765858866296,-36.9902686429373));
#39024=CARTESIAN_POINT('Ctrl Pts',(-4.23371210834143,5.28190475926086,-36.9820702816671));
#39025=CARTESIAN_POINT('Ctrl Pts',(-4.36876814494653,5.17075348139762,-36.9738719203968));
#39026=CARTESIAN_POINT('Ctrl Pts',(-4.49929668468071,5.0545641101109,-36.9656735591266));
#39027=CARTESIAN_POINT('Ctrl Pts',(-4.62984763594943,4.93835478930116,-36.9574737902113));
#39028=CARTESIAN_POINT('Ctrl Pts',(-4.75586927367679,4.8171058901698,-36.949274021296));
#39029=CARTESIAN_POINT('Ctrl Pts',(-4.87696519934859,4.69121513515878,-36.9410742523807));
#39030=CARTESIAN_POINT('Ctrl Pts',(-4.99810391516209,4.56527989571762,-36.9328715860164));
#39031=CARTESIAN_POINT('Ctrl Pts',(-5.11431320322787,4.43469979137637,-36.924668919652));
#39032=CARTESIAN_POINT('Ctrl Pts',(-5.22523552614307,4.29990728927175,-36.9164662532877));
#39033=CARTESIAN_POINT('Ctrl Pts',(-5.3362838290913,4.16496169657707,-36.9082542707447));
#39034=CARTESIAN_POINT('Ctrl Pts',(-5.44203294257358,4.0257944254142,-36.9000422882016));
#39035=CARTESIAN_POINT('Ctrl Pts',(-5.54216680392175,3.88286957255942,-36.8918303056586));
#39036=CARTESIAN_POINT('Ctrl Pts',(-5.64235972557483,3.73986042069455,-36.8836134795773));
#39037=CARTESIAN_POINT('Ctrl Pts',(-5.73693059923295,3.593089570335,-36.875396653496));
#39038=CARTESIAN_POINT('Ctrl Pts',(-5.82560835885852,3.44304752351718,-36.8671798274147));
#39039=CARTESIAN_POINT('Ctrl Pts',(-5.91442287239662,3.29277409019349,-36.8589503298008));
#39040=CARTESIAN_POINT('Ctrl Pts',(-5.99732594044969,3.13921969476663,-36.850720832187));
#39041=CARTESIAN_POINT('Ctrl Pts',(-6.07409327636515,2.98289789802059,-36.8424913345731));
#39042=CARTESIAN_POINT('Ctrl Pts',(-6.14252040864462,2.84355930906805,-36.8351559110483));
#39043=CARTESIAN_POINT('Ctrl Pts',(-6.20607320552896,2.70202241903317,-36.8278204875234));
#39044=CARTESIAN_POINT('Ctrl Pts',(-6.26462609939512,2.55866153189076,-36.8204850639985));
#39045=CARTESIAN_POINT('Ctrl Pts',(-6.3371380022418,2.38112341149918,-36.8114008756202));
#39046=CARTESIAN_POINT('Ctrl Pts',(-6.40218349129019,2.20029400097097,-36.8023166872419));
#39047=CARTESIAN_POINT('Ctrl Pts',(-6.45947873997281,2.01678541442548,-36.7932324988636));
#39048=CARTESIAN_POINT('Ctrl Pts',(-6.51649563618737,1.834168351508,-36.7841924433988));
#39049=CARTESIAN_POINT('Ctrl Pts',(-6.56583729367326,1.64889827935473,-36.7751523879341));
#39050=CARTESIAN_POINT('Ctrl Pts',(-6.60726903101154,1.46160355494775,-36.7661123324693));
#39051=CARTESIAN_POINT('Ctrl Pts',(-6.64857467197834,1.27487885696642,-36.7570997901687));
#39052=CARTESIAN_POINT('Ctrl Pts',(-6.68201834175108,1.08614201070574,-36.7480872478681));
#39053=CARTESIAN_POINT('Ctrl Pts',(-6.70741420988106,0.896037731954226,
-36.7390747055675));
#39054=CARTESIAN_POINT('Ctrl Pts',(-6.73268694761279,0.706855162806453,
-36.7301058600572));
#39055=CARTESIAN_POINT('Ctrl Pts',(-6.74998963237898,0.516318601169058,
-36.7211370145468));
#39056=CARTESIAN_POINT('Ctrl Pts',(-6.75918712047647,0.325082251722556,
-36.7121681690365));
#39057=CARTESIAN_POINT('Ctrl Pts',(-6.76431061506854,0.218553339501031,
-36.707172040639));
#39058=CARTESIAN_POINT('Ctrl Pts',(-6.76691986186397,0.111807595444429,
-36.7021759122415));
#39059=CARTESIAN_POINT('Ctrl Pts',(-6.766998182033,0.00496027842553114,
-36.697179783844));
#39060=CARTESIAN_POINT('Ctrl Pts',(-6.76699818203353,0.00496027770000192,
-36.6971797838101));
#39061=CARTESIAN_POINT('Ctrl Pts',(-6.76712516176854,-0.168270272665018,
-36.6890796078194));
#39062=CARTESIAN_POINT('Ctrl Pts',(-6.76059593780152,-0.341532716517958,
-36.6809794318287));
#39063=CARTESIAN_POINT('Ctrl Pts',(-6.74742994385826,-0.514274394389723,
-36.672879255838));
#39064=CARTESIAN_POINT('Ctrl Pts',(-6.73426271426744,-0.687032284317682,
-36.6647783196341));
#39065=CARTESIAN_POINT('Ctrl Pts',(-6.71445750083666,-0.85926894536719,
-36.6566773834301));
#39066=CARTESIAN_POINT('Ctrl Pts',(-6.68808571516971,-1.03043605650368,
-36.6485764472262));
#39067=CARTESIAN_POINT('Ctrl Pts',(-6.66170642162143,-1.20165189783899,
-36.6404732047368));
#39068=CARTESIAN_POINT('Ctrl Pts',(-6.62875688817058,-1.37179722067042,
-36.6323699622473));
#39069=CARTESIAN_POINT('Ctrl Pts',(-6.58935981068275,-1.54033317349169,
-36.6242667197578));
#39070=CARTESIAN_POINT('Ctrl Pts',(-6.54994399759125,-1.70894927496912,
-36.6161596237049));
#39071=CARTESIAN_POINT('Ctrl Pts',(-6.50407461742164,-1.87595412586907,
-36.6080525276519));
#39072=CARTESIAN_POINT('Ctrl Pts',(-6.45192443716212,-2.04082337725494,
-36.599945431599));
#39073=CARTESIAN_POINT('Ctrl Pts',(-6.39970252262244,-2.20591941169334,
-36.59182718397));
#39074=CARTESIAN_POINT('Ctrl Pts',(-6.34118266034671,-2.36887362892636,
-36.5837089363411));
#39075=CARTESIAN_POINT('Ctrl Pts',(-6.27658645573511,-2.52917999827663,
-36.5755906887121));
#39076=CARTESIAN_POINT('Ctrl Pts',(-6.2119444340683,-2.68960007037182,-36.5674666829399));
#39077=CARTESIAN_POINT('Ctrl Pts',(-6.14121763327434,-2.8473682199109,-36.5593426771676));
#39078=CARTESIAN_POINT('Ctrl Pts',(-6.06467380902991,-3.00200276316772,
-36.5512186713954));
#39079=CARTESIAN_POINT('Ctrl Pts',(-5.9879908607999,-3.15691836598982,-36.5430798996499));
#39080=CARTESIAN_POINT('Ctrl Pts',(-5.90546993777691,-3.30868866097301,
-36.5349411279045));
#39081=CARTESIAN_POINT('Ctrl Pts',(-5.81742309480156,-3.45685949035675,
-36.526802356159));
#39082=CARTESIAN_POINT('Ctrl Pts',(-5.73143683440478,-3.60156264027164,
-36.5188540581511));
#39083=CARTESIAN_POINT('Ctrl Pts',(-5.64018065764468,-3.74283271596098,
-36.5109057601433));
#39084=CARTESIAN_POINT('Ctrl Pts',(-5.54398136462814,-3.88027829268159,
-36.5029574621355));
#39085=CARTESIAN_POINT('Ctrl Pts',(-5.44311577373594,-4.02439088308348,
-36.4946236194428));
#39086=CARTESIAN_POINT('Ctrl Pts',(-5.33649843438387,-4.16475245015001,
-36.4862897767501));
#39087=CARTESIAN_POINT('Ctrl Pts',(-5.22443389202061,-4.30088124782659,
-36.4779559340574));
#39088=CARTESIAN_POINT('Ctrl Pts',(-5.11250143189811,-4.43684960049309,
-36.4696319138527));
#39089=CARTESIAN_POINT('Ctrl Pts',(-4.99513477761626,-4.56859485575408,
-36.4613078936479));
#39090=CARTESIAN_POINT('Ctrl Pts',(-4.87268163256819,-4.6956642456241,-36.4529838734432));
#39091=CARTESIAN_POINT('Ctrl Pts',(-4.75035036243681,-4.8226071661307,-36.4446681379523));
#39092=CARTESIAN_POINT('Ctrl Pts',(-4.6229429275459,-4.94488324422499,-36.4363524024615));
#39093=CARTESIAN_POINT('Ctrl Pts',(-4.49084730340559,-5.06207264838177,
-36.4280366669706));
#39094=CARTESIAN_POINT('Ctrl Pts',(-4.35885894779976,-5.17916688863193,
-36.4197276842905));
#39095=CARTESIAN_POINT('Ctrl Pts',(-4.22219024794498,-5.2911824558007,-36.4114187016105));
#39096=CARTESIAN_POINT('Ctrl Pts',(-4.08126619978474,-5.39773611864221,
-36.4031097189304));
#39097=CARTESIAN_POINT('Ctrl Pts',(-3.9404307825521,-5.5042227670167,-36.3948059619933));
#39098=CARTESIAN_POINT('Ctrl Pts',(-3.79534562727522,-5.60525414773612,
-36.3865022050561));
#39099=CARTESIAN_POINT('Ctrl Pts',(-3.64646916298839,-5.7004869654596,-36.3781984481189));
#39100=CARTESIAN_POINT('Ctrl Pts',(-3.49765313895715,-5.79568112095482,
-36.3698980623069));
#39101=CARTESIAN_POINT('Ctrl Pts',(-3.34504916538819,-5.88508121700561,
-36.3615976764949));
#39102=CARTESIAN_POINT('Ctrl Pts',(-3.18914527362632,-5.96838683596388,
-36.3532972906829));
#39103=CARTESIAN_POINT('Ctrl Pts',(-3.03327425793842,-6.05167488793481,
-36.3449986552062));
#39104=CARTESIAN_POINT('Ctrl Pts',(-2.87410501696344,-6.12887085936584,
-36.3367000197296));
#39105=CARTESIAN_POINT('Ctrl Pts',(-2.7121510537312,-6.19971980509964,-36.3284013842529));
#39106=CARTESIAN_POINT('Ctrl Pts',(-2.5502043598772,-6.27056557074588,-36.3201031212644));
#39107=CARTESIAN_POINT('Ctrl Pts',(-2.38547351152884,-6.33506473918674,
-36.3118048582758));
#39108=CARTESIAN_POINT('Ctrl Pts',(-2.21849307800729,-6.39301004714006,
-36.3035065952872));
#39109=CARTESIAN_POINT('Ctrl Pts',(-2.0514924238677,-6.45096237202294,-36.2952073274144));
#39110=CARTESIAN_POINT('Ctrl Pts',(-1.88224197047683,-6.50235914154458,
-36.2869080595416));
#39111=CARTESIAN_POINT('Ctrl Pts',(-1.71129275473856,-6.54704254664496,
-36.2786087916688));
#39112=CARTESIAN_POINT('Ctrl Pts',(-1.54022350509793,-6.59175732669761,
-36.2703036963723));
#39113=CARTESIAN_POINT('Ctrl Pts',(-1.36745344656601,-6.62974923514353,
-36.2619986010758));
#39114=CARTESIAN_POINT('Ctrl Pts',(-1.19354603792688,-6.66091111300467,
-36.2536935057793));
#39115=CARTESIAN_POINT('Ctrl Pts',(-1.01957521360319,-6.69208435410693,
-36.2453853820132));
#39116=CARTESIAN_POINT('Ctrl Pts',(-0.844466556129819,-6.71642254649862,
-36.237077258247));
#39117=CARTESIAN_POINT('Ctrl Pts',(-0.668790248606514,-6.73387025442047,
-36.2287691344809));
#39118=CARTESIAN_POINT('Ctrl Pts',(-0.49292719818365,-6.75133650915501,
-36.2204521792273));
#39119=CARTESIAN_POINT('Ctrl Pts',(-0.316495639097168,-6.76189761811846,
-36.2121352239736));
#39120=CARTESIAN_POINT('Ctrl Pts',(-0.140068470103331,-6.76555022327696,
-36.2038182687199));
#39121=CARTESIAN_POINT('Ctrl Pts',(-0.0100443308303591,-6.76824213770571,
-36.1976887992374));
#39122=CARTESIAN_POINT('Ctrl Pts',(0.11997738168582,-6.7671828108584,-36.191559329755));
#39123=CARTESIAN_POINT('Ctrl Pts',(0.24976870186275,-6.76238897103456,-36.1854298602725));
#39124=CARTESIAN_POINT('Ctrl Pts',(0.428718854614736,-6.75577945070935,
-36.1769788367473));
#39125=CARTESIAN_POINT('Ctrl Pts',(0.607557888684686,-6.74205679406928,
-36.1685278132221));
#39126=CARTESIAN_POINT('Ctrl Pts',(0.785697601848088,-6.7212326457615,-36.1600767896969));
#39127=CARTESIAN_POINT('Ctrl Pts',(0.963680468288821,-6.70042683249737,
-36.1516332070468));
#39128=CARTESIAN_POINT('Ctrl Pts',(1.14096491337727,-6.67253202859512,-36.1431896243966));
#39129=CARTESIAN_POINT('Ctrl Pts',(1.31696544471025,-6.63761184594573,-36.1347460417465));
#39130=CARTESIAN_POINT('Ctrl Pts',(1.49283493816366,-6.6027176624604,-36.1263087456067));
#39131=CARTESIAN_POINT('Ctrl Pts',(1.66742209934474,-6.56080859150973,-36.1178714494669));
#39132=CARTESIAN_POINT('Ctrl Pts',(1.84014885509666,-6.51199978432789,-36.1094341533271));
#39133=CARTESIAN_POINT('Ctrl Pts',(2.01275238347909,-6.46322579850821,-36.1010028765548));
#39134=CARTESIAN_POINT('Ctrl Pts',(2.18349783564774,-6.40756198500263,-36.0925715997824));
#39135=CARTESIAN_POINT('Ctrl Pts',(2.35181938481972,-6.34517411748379,-36.0841403230101));
#39136=CARTESIAN_POINT('Ctrl Pts',(2.5200687852818,-6.28281299166367,-36.0757126601882));
#39137=CARTESIAN_POINT('Ctrl Pts',(2.68589604373395,-6.21373367256571,-36.0672849973664));
#39138=CARTESIAN_POINT('Ctrl Pts',(2.84875187271498,-6.13815133144361,-36.0588573345445));
#39139=CARTESIAN_POINT('Ctrl Pts',(3.01155756823131,-6.06259225755519,-36.0504322660905));
#39140=CARTESIAN_POINT('Ctrl Pts',(3.1713933581389,-5.98053429329852,-36.0420071976366));
#39141=CARTESIAN_POINT('Ctrl Pts',(3.32773093316721,-5.89224030708542,-36.0335821291826));
#39142=CARTESIAN_POINT('Ctrl Pts',(3.37050967906797,-5.86808036984646,-36.0312767725687));
#39143=CARTESIAN_POINT('Ctrl Pts',(3.4130266334959,-5.84345378856547,-36.0289714159548));
#39144=CARTESIAN_POINT('Ctrl Pts',(3.45527128580487,-5.81836655269264,-36.026666059341));
#39145=CARTESIAN_POINT('Ctrl Pts',(3.61321048327226,-5.72457342897485,-36.0180470708165));
#39146=CARTESIAN_POINT('Ctrl Pts',(3.76727095094069,-5.62437985373978,-36.009428082292));
#39147=CARTESIAN_POINT('Ctrl Pts',(3.91694543125652,-5.51813623323661,-36.0008090937675));
#39148=CARTESIAN_POINT('Ctrl Pts',(4.06670957994318,-5.41182896332346,-35.9921849416998));
#39149=CARTESIAN_POINT('Ctrl Pts',(4.21208224937313,-5.29946459076497,-35.983560789632));
#39150=CARTESIAN_POINT('Ctrl Pts',(4.35258785275091,-5.18143493485012,-35.9749366375642));
#39151=CARTESIAN_POINT('Ctrl Pts',(4.49790581084434,-5.05936273146688,-35.966017105968));
#39152=CARTESIAN_POINT('Ctrl Pts',(4.63801713464026,-4.93123053533874,-35.9570975743717));
#39153=CARTESIAN_POINT('Ctrl Pts',(4.77243614129764,-4.79751417686661,-35.9481780427755));
#39154=CARTESIAN_POINT('Ctrl Pts',(4.90264583778416,-4.66798512524732,-35.9395378249162));
#39155=CARTESIAN_POINT('Ctrl Pts',(5.02751415666685,-4.53321660773519,-35.930897607057));
#39156=CARTESIAN_POINT('Ctrl Pts',(5.14663957971879,-4.39367614150975,-35.9222573891977));
#39157=CARTESIAN_POINT('Ctrl Pts',(5.27154148334465,-4.24736925404713,-35.913198200733));
#39158=CARTESIAN_POINT('Ctrl Pts',(5.39012945090665,-4.09581642711831,-35.9041390122683));
#39159=CARTESIAN_POINT('Ctrl Pts',(5.50199036545045,-3.93959274779646,-35.8950798238035));
#39160=CARTESIAN_POINT('Ctrl Pts',(5.61385127999425,-3.7833690684746,-35.8860206353388));
#39161=CARTESIAN_POINT('Ctrl Pts',(5.71898495995174,-3.62247487518775,-35.8769614468741));
#39162=CARTESIAN_POINT('Ctrl Pts',(5.81703207616521,-3.45751743666826,-35.8679022584094));
#39163=CARTESIAN_POINT('Ctrl Pts',(5.91490933262873,-3.29284577533776,-35.8588587643532));
#39164=CARTESIAN_POINT('Ctrl Pts',(6.00581545573631,-3.12397366454647,-35.8498152702969));
#39165=CARTESIAN_POINT('Ctrl Pts',(6.08941893511293,-2.95148539428676,-35.8407717762406));
#39166=CARTESIAN_POINT('Ctrl Pts',(6.17294594269256,-2.77915489841738,-35.8317365542353));
#39167=CARTESIAN_POINT('Ctrl Pts',(6.24918353883517,-2.60321506095434,-35.82270133223));
#39168=CARTESIAN_POINT('Ctrl Pts',(6.31784655891654,-2.4242738826268,-35.8136661102246));
#39169=CARTESIAN_POINT('Ctrl Pts',(6.38638860970443,-2.24564795970009,-35.8046468063135));
#39170=CARTESIAN_POINT('Ctrl Pts',(6.44738264706108,-2.06403147680182,-35.7956275024024));
#39171=CARTESIAN_POINT('Ctrl Pts',(6.50059197864906,-1.88005130970501,-35.7866081984913));
#39172=CARTESIAN_POINT('Ctrl Pts',(6.55373455541437,-1.6963019585772,-35.7776002099269));
#39173=CARTESIAN_POINT('Ctrl Pts',(6.59911185095206,-1.51019506921802,-35.7685922213624));
#39174=CARTESIAN_POINT('Ctrl Pts',(6.63653645356359,-1.32237396394578,-35.759584232798));
#39175=CARTESIAN_POINT('Ctrl Pts',(6.67387653139898,-1.13497705921994,-35.7505965890913));
#39176=CARTESIAN_POINT('Ctrl Pts',(6.7032997225382,-0.9458738997491,-35.7416089453847));
#39177=CARTESIAN_POINT('Ctrl Pts',(6.72466936137,-0.755718850004144,-35.732621301678));
#39178=CARTESIAN_POINT('Ctrl Pts',(6.74328083565911,-0.590106981355902,
-35.7247936869446));
#39179=CARTESIAN_POINT('Ctrl Pts',(6.75578424925169,-0.42369755940464,-35.7169660722113));
#39180=CARTESIAN_POINT('Ctrl Pts',(6.76212065723859,-0.256930373734165,
-35.7091384574779));
#39181=CARTESIAN_POINT('Ctrl Pts',(6.76869630611822,-0.0838666348017703,
-35.7010152990326));
#39182=CARTESIAN_POINT('Ctrl Pts',(6.76862585696639,0.0895050961617428,
-35.6928921405873));
#39183=CARTESIAN_POINT('Ctrl Pts',(6.76190161212426,0.262632039079982,-35.684768982142));
#39184=CARTESIAN_POINT('Ctrl Pts',(6.7551778413766,0.435746775642425,-35.6766463964219));
#39185=CARTESIAN_POINT('Ctrl Pts',(6.74180122360032,0.60861639278875,-35.6685238107018));
#39186=CARTESIAN_POINT('Ctrl Pts',(6.72181615884099,0.780689776251874,-35.6604012249817));
#39187=CARTESIAN_POINT('Ctrl Pts',(6.70182869267044,0.952783836103028,-35.6522776632493));
#39188=CARTESIAN_POINT('Ctrl Pts',(6.67523124174807,1.12408110832392,-35.6441541015169));
#39189=CARTESIAN_POINT('Ctrl Pts',(6.64211987778535,1.29403729819843,-35.6360305397846));
#39190=CARTESIAN_POINT('Ctrl Pts',(6.60898439612312,1.46411728098961,-35.6279010610014));
#39191=CARTESIAN_POINT('Ctrl Pts',(6.56932559524705,1.63285387083436,-35.6197715822183));
#39192=CARTESIAN_POINT('Ctrl Pts',(6.52329046392428,1.79971401152366,-35.6116421034352));
#39193=CARTESIAN_POINT('Ctrl Pts',(6.47723656488886,1.96664217815496,-35.6035093104067));
#39194=CARTESIAN_POINT('Ctrl Pts',(6.42480126454203,2.13169202217281,-35.5953765173782));
#39195=CARTESIAN_POINT('Ctrl Pts',(6.36618083681926,2.2943475222632,-35.5872437243496));
#39196=CARTESIAN_POINT('Ctrl Pts',(6.30749666827451,2.45717988553384,-35.5791020881425));
#39197=CARTESIAN_POINT('Ctrl Pts',(6.24261407667555,2.61761236598165,-35.5709604519354));
#39198=CARTESIAN_POINT('Ctrl Pts',(6.17177699602401,2.77515003402498,-35.5628188157283));
#39199=CARTESIAN_POINT('Ctrl Pts',(6.13568646560412,2.8554133360767,-35.5586707626677));
#39200=CARTESIAN_POINT('Ctrl Pts',(6.09805102824434,2.93492560878375,-35.554522709607));
#39201=CARTESIAN_POINT('Ctrl Pts',(6.05890740362131,3.01362407648048,-35.5503746565464));
#39202=CARTESIAN_POINT('Ctrl Pts',(5.97926234502005,3.17375089488067,-35.5419346632583));
#39203=CARTESIAN_POINT('Ctrl Pts',(5.89320674020421,3.33083675555393,-35.5334946699701));
#39204=CARTESIAN_POINT('Ctrl Pts',(5.80099700859093,3.48435398694206,-35.5250546766819));
#39205=CARTESIAN_POINT('Ctrl Pts',(5.70885313141505,3.63776157924195,-35.5166207110765));
#39206=CARTESIAN_POINT('Ctrl Pts',(5.61056405831751,3.78760533720003,-35.5081867454711));
#39207=CARTESIAN_POINT('Ctrl Pts',(5.50643222722078,3.93338189437848,-35.4997527798657));
#39208=CARTESIAN_POINT('Ctrl Pts',(5.40236020939849,4.07907471757155,-35.4913236587261));
#39209=CARTESIAN_POINT('Ctrl Pts',(5.29245231666745,4.22070472623775,-35.4828945375865));
#39210=CARTESIAN_POINT('Ctrl Pts',(5.17705462422063,4.35779696840454,-35.474465416447));
#39211=CARTESIAN_POINT('Ctrl Pts',(5.06170710095617,4.49482960967679,-35.4660399598704));
#39212=CARTESIAN_POINT('Ctrl Pts',(4.94087475063419,4.62732816293984,-35.4576145032938));
#39213=CARTESIAN_POINT('Ctrl Pts',(4.81494453202444,4.75484996120046,-35.4491890467173));
#39214=CARTESIAN_POINT('Ctrl Pts',(4.6890396650411,4.88234608742599,-35.4407652863105));
#39215=CARTESIAN_POINT('Ctrl Pts',(4.55803920736126,5.00486721656025,-35.4323415259037));
#39216=CARTESIAN_POINT('Ctrl Pts',(4.42236802073555,5.12200645149687,-35.4239177654969));
#39217=CARTESIAN_POINT('Ctrl Pts',(4.28671878876183,5.23912673066845,-35.4154953682441));
#39218=CARTESIAN_POINT('Ctrl Pts',(4.14640058850214,5.35086663585823,-35.4070729709914));
#39219=CARTESIAN_POINT('Ctrl Pts',(4.00187264440221,5.45685846783525,-35.3986505737386));
#39220=CARTESIAN_POINT('Ctrl Pts',(3.85731176433453,5.5628744539202,-35.3902262571352));
#39221=CARTESIAN_POINT('Ctrl Pts',(3.70853949033344,5.66313954913234,-35.3818019405318));
#39222=CARTESIAN_POINT('Ctrl Pts',(3.55604606397443,5.75732797319138,-35.3733776239284));
#39223=CARTESIAN_POINT('Ctrl Pts',(3.4071144891321,5.84931639959086,-35.3651500775438));
#39224=CARTESIAN_POINT('Ctrl Pts',(3.25463392784788,5.93550872083648,-35.3569225311592));
#39225=CARTESIAN_POINT('Ctrl Pts',(3.0990855038472,6.01564277861013,-35.3486949847746));
#39226=CARTESIAN_POINT('Origin',(0.,0.,-63.6971797838103));
#39227=CARTESIAN_POINT('',(3.09908550384723,6.01564277861011,-32.9539663901326));
#39228=CARTESIAN_POINT('',(3.09908550384718,6.01564277861014,-33.3487628447403));
#39229=CARTESIAN_POINT('',(3.09908550384721,6.01564277861012,-63.6971797838103));
#39230=CARTESIAN_POINT('',(-6.76699999651487,-0.00021718149412733,-34.30282021619));
#39231=CARTESIAN_POINT('Ctrl Pts',(-6.76699999651487,-0.000217181494128159,
-34.30282021619));
#39232=CARTESIAN_POINT('Ctrl Pts',(-6.7669938648465,-0.191269370176862,
-34.2938005713136));
#39233=CARTESIAN_POINT('Ctrl Pts',(-6.7588924502058,-0.38237811217807,-34.2847809264371));
#39234=CARTESIAN_POINT('Ctrl Pts',(-6.74270737712069,-0.572875402266653,
-34.2757612815607));
#39235=CARTESIAN_POINT('Ctrl Pts',(-6.72653787596974,-0.763189411671673,
-34.266750314638));
#39236=CARTESIAN_POINT('Ctrl Pts',(-6.70230026323093,-0.952892902147142,
-34.2577393477154));
#39237=CARTESIAN_POINT('Ctrl Pts',(-6.67005812475392,-1.14132099446397,
-34.2487283807927));
#39238=CARTESIAN_POINT('Ctrl Pts',(-6.63787300301086,-1.3294158720837,-34.2397333487903));
#39239=CARTESIAN_POINT('Ctrl Pts',(-6.59771166086158,-1.51623961630588,
-34.2307383167878));
#39240=CARTESIAN_POINT('Ctrl Pts',(-6.5496890263464,-1.70113569657378,-34.2217432847854));
#39241=CARTESIAN_POINT('Ctrl Pts',(-6.50172615196388,-1.88580168920914,
-34.2127594463443));
#39242=CARTESIAN_POINT('Ctrl Pts',(-6.44592156777571,-2.06854457076069,
-34.2037756079032));
#39243=CARTESIAN_POINT('Ctrl Pts',(-6.38244100642491,-2.24871870172901,
-34.1947917694621));
#39244=CARTESIAN_POINT('Ctrl Pts',(-6.31909761565152,-2.42850350738176,
-34.1858273435511));
#39245=CARTESIAN_POINT('Ctrl Pts',(-6.24811143560728,-2.60573041346402,
-34.17686291764));
#39246=CARTESIAN_POINT('Ctrl Pts',(-6.16969755941112,-2.77976995907873,
-34.167898491729));
#39247=CARTESIAN_POINT('Ctrl Pts',(-6.10857035845828,-2.91544174058734,
-34.1609103119492));
#39248=CARTESIAN_POINT('Ctrl Pts',(-6.0429304192004,-3.0491767919573,-34.1539221321694));
#39249=CARTESIAN_POINT('Ctrl Pts',(-5.97290064038415,-3.18068340771267,
-34.1469339523896));
#39250=CARTESIAN_POINT('Ctrl Pts',(-5.89149704071466,-3.33354854714038,
-34.1388107939443));
#39251=CARTESIAN_POINT('Ctrl Pts',(-5.80419510917805,-3.48333551189467,
-34.130687635499));
#39252=CARTESIAN_POINT('Ctrl Pts',(-5.71126635389772,-3.62956273328288,
-34.1225644770537));
#39253=CARTESIAN_POINT('Ctrl Pts',(-5.61834415058117,-3.7757796448864,-34.1144418913336));
#39254=CARTESIAN_POINT('Ctrl Pts',(-5.51979611007115,-3.91843700413229,
-34.1063193056135));
#39255=CARTESIAN_POINT('Ctrl Pts',(-5.41593792345498,-4.05708089755211,
-34.0981967198934));
#39256=CARTESIAN_POINT('Ctrl Pts',(-5.3120672572083,-4.19574145046328,-34.090073158161));
#39257=CARTESIAN_POINT('Ctrl Pts',(-5.20288539471126,-4.3303872850359,-34.0819495964286));
#39258=CARTESIAN_POINT('Ctrl Pts',(-5.08874924847139,-4.46059638234417,
-34.0738260346962));
#39259=CARTESIAN_POINT('Ctrl Pts',(-4.97452996759335,-4.5909003215281,-34.0656965559131));
#39260=CARTESIAN_POINT('Ctrl Pts',(-4.85534943715149,-4.71676079349159,
-34.05756707713));
#39261=CARTESIAN_POINT('Ctrl Pts',(-4.73160291533413,-4.83779111285322,
-34.0494375983469));
#39262=CARTESIAN_POINT('Ctrl Pts',(-4.60780594423763,-4.95887077414605,
-34.0413048053183));
#39263=CARTESIAN_POINT('Ctrl Pts',(-4.47943954241164,-5.07511611218259,
-34.0331720122898));
#39264=CARTESIAN_POINT('Ctrl Pts',(-4.3469329867438,-5.1861799630131,-34.0250392192612));
#39265=CARTESIAN_POINT('Ctrl Pts',(-4.21428235029912,-5.29736457893201,
-34.0168975830541));
#39266=CARTESIAN_POINT('Ctrl Pts',(-4.07748285748908,-5.40335623068946,
-34.0087559468469));
#39267=CARTESIAN_POINT('Ctrl Pts',(-3.93699435812846,-5.50384996380395,
-34.0006143106398));
#39268=CARTESIAN_POINT('Ctrl Pts',(-3.86541737594449,-5.55505015583014,
-33.9964662575792));
#39269=CARTESIAN_POINT('Ctrl Pts',(-3.79288325329798,-5.60482393113451,
-33.9923182045186));
#39270=CARTESIAN_POINT('Ctrl Pts',(-3.71945531104089,-5.65313551838002,
-33.9881701514581));
#39271=CARTESIAN_POINT('Ctrl Pts',(-3.57003959167336,-5.75144292480034,
-33.97972943648));
#39272=CARTESIAN_POINT('Ctrl Pts',(-3.4166136099478,-5.84389562763648,-33.9712887215019));
#39273=CARTESIAN_POINT('Ctrl Pts',(-3.25966460728389,-5.93016657843781,
-33.9628480065238));
#39274=CARTESIAN_POINT('Ctrl Pts',(-3.10283423407095,-6.0163723215898,-33.9544136714358));
#39275=CARTESIAN_POINT('Ctrl Pts',(-2.94248643931854,-6.09640546694306,
-33.9459793363478));
#39276=CARTESIAN_POINT('Ctrl Pts',(-2.77913594602292,-6.16998317611347,
-33.9375450012598));
#39277=CARTESIAN_POINT('Ctrl Pts',(-2.61588383639307,-6.24351657048201,
-33.9291157460512));
#39278=CARTESIAN_POINT('Ctrl Pts',(-2.44963293694206,-6.31060214342651,
-33.9206864908425));
#39279=CARTESIAN_POINT('Ctrl Pts',(-2.28092134062876,-6.37100359738278,
-33.9122572356339));
#39280=CARTESIAN_POINT('Ctrl Pts',(-2.11228547780905,-6.43137793753522,
-33.9038317642609));
#39281=CARTESIAN_POINT('Ctrl Pts',(-1.94119143394642,-6.48507402909674,
-33.8954062928879));
#39282=CARTESIAN_POINT('Ctrl Pts',(-1.76819636321376,-6.53190405786227,
-33.8869808215149));
#39283=CARTESIAN_POINT('Ctrl Pts',(-1.59525243484278,-6.57872024231272,
-33.8785578409556));
#39284=CARTESIAN_POINT('Ctrl Pts',(-1.42040892184351,-6.61867432483879,
-33.8701348603964));
#39285=CARTESIAN_POINT('Ctrl Pts',(-1.24423757045886,-6.65162851249667,
-33.8617118798371));
#39286=CARTESIAN_POINT('Ctrl Pts',(-1.06806330204222,-6.68458324580751,
-33.8532887598108));
#39287=CARTESIAN_POINT('Ctrl Pts',(-0.890561477743755,-6.7105377848897,
-33.8448656397845));
#39288=CARTESIAN_POINT('Ctrl Pts',(-0.71231412258111,-6.72940544110485,
-33.8364425197582));
#39289=CARTESIAN_POINT('Ctrl Pts',(-0.534060603327663,-6.74827374979501,
-33.8280191084463));
#39290=CARTESIAN_POINT('Ctrl Pts',(-0.35506183343988,-6.76005465169477,
-33.8195956971344));
#39291=CARTESIAN_POINT('Ctrl Pts',(-0.175905208564063,-6.76471332412542,
-33.8111722858226));
#39292=CARTESIAN_POINT('Ctrl Pts',(0.00328259787393709,-6.76937280738116,
-33.8027474084465));
#39293=CARTESIAN_POINT('Ctrl Pts',(0.18262798070206,-6.7669075811072,-33.7943225310703));
#39294=CARTESIAN_POINT('Ctrl Pts',(0.361542919830847,-6.75733495670595,
-33.7858976536942));
#39295=CARTESIAN_POINT('Ctrl Pts',(0.540513958482216,-6.74775933076854,
-33.7774701346628));
#39296=CARTESIAN_POINT('Ctrl Pts',(0.719053951462811,-6.73107188137891,
-33.7690426156314));
#39297=CARTESIAN_POINT('Ctrl Pts',(0.896579004388525,-6.70734187952945,
-33.7606150966));
#39298=CARTESIAN_POINT('Ctrl Pts',(1.07426325492059,-6.68359059753147,-33.7521800200952));
#39299=CARTESIAN_POINT('Ctrl Pts',(1.25093041590619,-6.65278418804784,-33.7437449435904));
#39300=CARTESIAN_POINT('Ctrl Pts',(1.42600466859868,-6.61504343788722,-33.7353098670856));
#39301=CARTESIAN_POINT('Ctrl Pts',(1.60116353582971,-6.57728444737367,-33.7268707138529));
#39302=CARTESIAN_POINT('Ctrl Pts',(1.77472763532533,-6.53258451032157,-33.7184315606201));
#39303=CARTESIAN_POINT('Ctrl Pts',(1.94613483011703,-6.48111473613956,-33.7099924073873));
#39304=CARTESIAN_POINT('Ctrl Pts',(2.11773250635989,-6.42958776460776,-33.7015438758892));
#39305=CARTESIAN_POINT('Ctrl Pts',(2.2871681715165,-6.37127602725521,-33.6930953443911));
#39306=CARTESIAN_POINT('Ctrl Pts',(2.45389708841369,-6.30639977161889,-33.684646812893));
#39307=CARTESIAN_POINT('Ctrl Pts',(2.54602022453233,-6.27055353546456,-33.679978725127));
#39308=CARTESIAN_POINT('Ctrl Pts',(2.63731737974505,-6.23270405171612,-33.675310637361));
#39309=CARTESIAN_POINT('Ctrl Pts',(2.72769970169339,-6.19289458471415,-33.6706425495951));
#39310=CARTESIAN_POINT('Ctrl Pts',(2.88725549207892,-6.12261722476807,-33.6624017739983));
#39311=CARTESIAN_POINT('Ctrl Pts',(3.04431386512154,-6.04607262618752,-33.6541609984016));
#39312=CARTESIAN_POINT('Ctrl Pts',(3.1983500263171,-5.96345924016903,-33.6459202228048));
#39313=CARTESIAN_POINT('Ctrl Pts',(3.35221557576458,-5.88093735743194,-33.6376885747604));
#39314=CARTESIAN_POINT('Ctrl Pts',(3.50306526792112,-5.79236023834901,-33.6294569267161));
#39315=CARTESIAN_POINT('Ctrl Pts',(3.65039391979644,-5.69797448487734,-33.6212252786717));
#39316=CARTESIAN_POINT('Ctrl Pts',(3.797585644559,-5.60367645343764,-33.6130012811134));
#39317=CARTESIAN_POINT('Ctrl Pts',(3.94126254841058,-5.5035807297708,-33.6047772835551));
#39318=CARTESIAN_POINT('Ctrl Pts',(4.08094364387114,-5.39797999028783,-33.5965532859968));
#39319=CARTESIAN_POINT('Ctrl Pts',(4.22050133054114,-5.29247254946849,-33.5883365543723));
#39320=CARTESIAN_POINT('Ctrl Pts',(4.35606996238116,-5.18147000044937,-33.5801198227478));
#39321=CARTESIAN_POINT('Ctrl Pts',(4.48719728141066,-5.06530843658121,-33.5719030911233));
#39322=CARTESIAN_POINT('Ctrl Pts',(4.61825741906009,-4.9492063865827,-33.5636905692346));
#39323=CARTESIAN_POINT('Ctrl Pts',(4.7448805100339,-4.82795082119743,-33.5554780473459));
#39324=CARTESIAN_POINT('Ctrl Pts',(4.86664684013806,-4.70191849497354,-33.5472655254572));
#39325=CARTESIAN_POINT('Ctrl Pts',(4.98837245099535,-4.57592831456616,-33.5390557498754));
#39326=CARTESIAN_POINT('Ctrl Pts',(5.10524428949107,-4.44516481106522,-33.5308459742936));
#39327=CARTESIAN_POINT('Ctrl Pts',(5.21687897201709,-4.3100420869553,-33.5226361987117));
#39328=CARTESIAN_POINT('Ctrl Pts',(5.26563810105552,-4.25102399157652,-33.519050382029));
#39329=CARTESIAN_POINT('Ctrl Pts',(5.31339861499413,-4.19117474445455,-33.5154645653463));
#39330=CARTESIAN_POINT('Ctrl Pts',(5.36013090501688,-4.13053092000083,-33.5118787486636));
#39331=CARTESIAN_POINT('Ctrl Pts',(5.47558247242473,-3.98071107202465,-33.5030200311418));
#39332=CARTESIAN_POINT('Ctrl Pts',(5.58463619895538,-3.82619489454296,-33.49416131362));
#39333=CARTESIAN_POINT('Ctrl Pts',(5.6869529359615,-3.66754077061985,-33.4853025960983));
#39334=CARTESIAN_POINT('Ctrl Pts',(5.78946109114947,-3.50858983031233,-33.4764273053388));
#39335=CARTESIAN_POINT('Ctrl Pts',(5.88520692836807,-3.34548569079147,-33.4675520145794));
#39336=CARTESIAN_POINT('Ctrl Pts',(5.97389692410437,-3.17881181263949,-33.4586767238199));
#39337=CARTESIAN_POINT('Ctrl Pts',(6.06283881937008,-3.01166454319774,-33.4497762252391));
#39338=CARTESIAN_POINT('Ctrl Pts',(6.14468464771538,-2.8409274764045,-33.4408757266584));
#39339=CARTESIAN_POINT('Ctrl Pts',(6.21918754204155,-2.66720740043125,-33.4319752280776));
#39340=CARTESIAN_POINT('Ctrl Pts',(6.29379129103547,-2.49325215935867,-33.42306268088));
#39341=CARTESIAN_POINT('Ctrl Pts',(6.36103215381326,-2.31630608365107,-33.4141501336823));
#39342=CARTESIAN_POINT('Ctrl Pts',(6.42071257160129,-2.13699299785496,-33.4052375864847));
#39343=CARTESIAN_POINT('Ctrl Pts',(6.48052476958043,-1.95728397125298,-33.3963053595125));
#39344=CARTESIAN_POINT('Ctrl Pts',(6.53274304917183,-1.77519772759828,-33.3873731325402));
#39345=CARTESIAN_POINT('Ctrl Pts',(6.57721985283051,-1.5913729944712,-33.3784409055679));
#39346=CARTESIAN_POINT('Ctrl Pts',(6.61925556828464,-1.4176373943489,-33.3699989196226));
#39347=CARTESIAN_POINT('Ctrl Pts',(6.65437666351834,-1.24234916980446,-33.3615569336774));
#39348=CARTESIAN_POINT('Ctrl Pts',(6.68250099371985,-1.06605322049759,-33.3531149477321));
#39349=CARTESIAN_POINT('Ctrl Pts',(6.70989902228651,-0.894310056458122,
-33.3448909733145));
#39350=CARTESIAN_POINT('Ctrl Pts',(6.73070831014295,-0.721282309763172,
-33.3366669988969));
#39351=CARTESIAN_POINT('Ctrl Pts',(6.74481391059258,-0.547516494250918,
-33.3284430244794));
#39352=CARTESIAN_POINT('Ctrl Pts',(6.75890461415955,-0.373934192299406,
-33.3202277353767));
#39353=CARTESIAN_POINT('Ctrl Pts',(6.76630569969628,-0.1996157281842,-33.3120124462741));
#39354=CARTESIAN_POINT('Ctrl Pts',(6.76695338696486,-0.0251168995863532,
-33.3037971571714));
#39355=CARTESIAN_POINT('Ctrl Pts',(6.76760052012511,0.149232642063764,-33.2955888963992));
#39356=CARTESIAN_POINT('Ctrl Pts',(6.76150576048054,0.323761884313008,-33.2873806356271));
#39357=CARTESIAN_POINT('Ctrl Pts',(6.74865719260139,0.497910731707596,-33.2791723748549));
#39358=CARTESIAN_POINT('Ctrl Pts',(6.73581704049269,0.67194551216964,-33.270969490467));
#39359=CARTESIAN_POINT('Ctrl Pts',(6.7162319180324,0.845600037727389,-33.2627666060791));
#39360=CARTESIAN_POINT('Ctrl Pts',(6.68994197807794,1.01831494634549,-33.2545637216912));
#39361=CARTESIAN_POINT('Ctrl Pts',(6.66366398732654,1.1909513532432,-33.246364565647));
#39362=CARTESIAN_POINT('Ctrl Pts',(6.63068730424331,1.36264864025744,-33.2381654096028));
#39363=CARTESIAN_POINT('Ctrl Pts',(6.59110385667708,1.53285320578864,-33.2299662535586));
#39364=CARTESIAN_POINT('Ctrl Pts',(6.55152385190826,1.70304296766142,-33.2217678106416));
#39365=CARTESIAN_POINT('Ctrl Pts',(6.50533830008708,1.87173991571334,-33.2135693677246));
#39366=CARTESIAN_POINT('Ctrl Pts',(6.45269019283601,2.03840091132192,-33.2053709248076));
#39367=CARTESIAN_POINT('Ctrl Pts',(6.40004260989775,2.2050602471843,-33.1971725635373));
#39368=CARTESIAN_POINT('Ctrl Pts',(6.34093270676223,2.36968332863238,-33.1889742022671));
#39369=CARTESIAN_POINT('Ctrl Pts',(6.27555324913947,2.53174256535198,-33.1807758409969));
#39370=CARTESIAN_POINT('Ctrl Pts',(6.21016256597204,2.69382962737433,-33.1725760720816));
#39371=CARTESIAN_POINT('Ctrl Pts',(6.13850031787242,2.85335163498853,-33.1643763031663));
#39372=CARTESIAN_POINT('Ctrl Pts',(6.06080729700758,3.00980130715297,-33.156176534251));
#39373=CARTESIAN_POINT('Ctrl Pts',(5.983086822739,3.16630626196657,-33.1479738678867));
#39374=CARTESIAN_POINT('Ctrl Pts',(5.89933149012313,3.31973639766562,-33.1397712015224));
#39375=CARTESIAN_POINT('Ctrl Pts',(5.80982790369007,3.46960930502329,-33.1315685351581));
#39376=CARTESIAN_POINT('Ctrl Pts',(5.72022266355448,3.61965243054262,-33.1233565526151));
#39377=CARTESIAN_POINT('Ctrl Pts',(5.62485631087446,3.7661299480724,-33.1151445700721));
#39378=CARTESIAN_POINT('Ctrl Pts',(5.52405921104255,3.90858783103258,-33.106932587529));
#39379=CARTESIAN_POINT('Ctrl Pts',(5.42320265971882,4.05112973757754,-33.0987157614477));
#39380=CARTESIAN_POINT('Ctrl Pts',(5.31690919426824,4.189646999542,-33.0904989353664));
#39381=CARTESIAN_POINT('Ctrl Pts',(5.2055492098384,4.32371905007146,-33.0822821092851));
#39382=CARTESIAN_POINT('Ctrl Pts',(5.09401749222929,4.45799785906633,-33.0740526116713));
#39383=CARTESIAN_POINT('Ctrl Pts',(4.9774038813645,4.58781749089686,-33.0658231140574));
#39384=CARTESIAN_POINT('Ctrl Pts',(4.85611625261524,4.71279364507784,-33.0575936164436));
#39385=CARTESIAN_POINT('Ctrl Pts',(4.74800562825541,4.82419206384428,-33.0502581929187));
#39386=CARTESIAN_POINT('Ctrl Pts',(4.6361820424265,4.93174267929951,-33.0429227693939));
#39387=CARTESIAN_POINT('Ctrl Pts',(4.52095554968146,5.03520108017589,-33.035587345869));
#39388=CARTESIAN_POINT('Ctrl Pts',(4.39417909650282,5.14902984300791,-33.0275166413384));
#39389=CARTESIAN_POINT('Ctrl Pts',(4.26286932038105,5.25827529688711,-33.0194459368078));
#39390=CARTESIAN_POINT('Ctrl Pts',(4.12739668916492,5.36254469168048,-33.0113752322772));
#39391=CARTESIAN_POINT('Ctrl Pts',(3.99207256961981,5.46669978130447,-33.0033133752444));
#39392=CARTESIAN_POINT('Ctrl Pts',(3.85259496140558,5.56588943448039,-32.9952515182117));
#39393=CARTESIAN_POINT('Ctrl Pts',(3.70937148115886,5.65975725758317,-32.9871896611789));
#39394=CARTESIAN_POINT('Ctrl Pts',(3.56631248760859,5.75351727707652,-32.9791370628811));
#39395=CARTESIAN_POINT('Ctrl Pts',(3.41951649686986,5.84196743257849,-32.9710844645832));
#39396=CARTESIAN_POINT('Ctrl Pts',(3.26942412133972,5.92479155032496,-32.9630318662853));
#39397=CARTESIAN_POINT('Ctrl Pts',(3.21310031955796,5.95587220431704,-32.9600100409011));
#39398=CARTESIAN_POINT('Ctrl Pts',(3.15631264399957,5.98616100799977,-32.9569882155169));
#39399=CARTESIAN_POINT('Ctrl Pts',(3.09908550384723,6.01564277861011,-32.9539663901326));
#39400=CARTESIAN_POINT('Ctrl Pts',(3.09908550384724,6.01564277861011,-34.9544861942313));
#39401=CARTESIAN_POINT('Ctrl Pts',(3.01301923408008,6.05998163628863,-34.9499084485033));
#39402=CARTESIAN_POINT('Ctrl Pts',(2.92608302260693,6.10243092898755,-34.9453307027752));
#39403=CARTESIAN_POINT('Ctrl Pts',(2.83836998641864,6.14295896292641,-34.9407529570472));
#39404=CARTESIAN_POINT('Ctrl Pts',(2.67868731963912,6.21674074976132,-34.9324191143545));
#39405=CARTESIAN_POINT('Ctrl Pts',(2.51592169567249,6.28438672683791,-34.9240852716618));
#39406=CARTESIAN_POINT('Ctrl Pts',(2.35057870886505,6.34563383228424,-34.9157514289691));
#39407=CARTESIAN_POINT('Ctrl Pts',(2.18543059968516,6.40680875026841,-34.9074274087644));
#39408=CARTESIAN_POINT('Ctrl Pts',(2.01771150254169,6.46159970093205,-34.8991033885596));
#39409=CARTESIAN_POINT('Ctrl Pts',(1.8479497256929,6.50979038151856,-34.8907793683549));
#39410=CARTESIAN_POINT('Ctrl Pts',(1.67835690900003,6.55793309898252,-34.882463632864));
#39411=CARTESIAN_POINT('Ctrl Pts',(1.50672579562963,6.59948853981487,-34.8741478973731));
#39412=CARTESIAN_POINT('Ctrl Pts',(1.33360292203884,6.63428912893684,-34.8658321618823));
#39413=CARTESIAN_POINT('Ctrl Pts',(1.1606206332488,6.66906145816577,-34.8575231792023));
#39414=CARTESIAN_POINT('Ctrl Pts',(0.986149337592733,6.69708979739558,-34.8492141965222));
#39415=CARTESIAN_POINT('Ctrl Pts',(0.810749146081458,6.71825682912824,-34.8409052138422));
#39416=CARTESIAN_POINT('Ctrl Pts',(0.635459268471964,6.73941054834487,-34.832601456905));
#39417=CARTESIAN_POINT('Ctrl Pts',(0.459242003630512,6.75371151836466,-34.8242976999679));
#39418=CARTESIAN_POINT('Ctrl Pts',(0.282666258558173,6.76109375665452,-34.8159939430307));
#39419=CARTESIAN_POINT('Ctrl Pts',(0.106162198981455,6.76847299793361,-34.8076935572187));
#39420=CARTESIAN_POINT('Ctrl Pts',(-0.0706997038729907,6.7689390898049,
-34.7993931714067));
#39421=CARTESIAN_POINT('Ctrl Pts',(-0.247346537768416,6.76247799924362,
-34.7910927855947));
#39422=CARTESIAN_POINT('Ctrl Pts',(-0.423956121442899,6.75601827115822,
-34.782794150118));
#39423=CARTESIAN_POINT('Ctrl Pts',(-0.600350379152984,6.74263428354,-34.7744955146414));
#39424=CARTESIAN_POINT('Ctrl Pts',(-0.775957268691582,6.72236411667538,
-34.7661968791648));
#39425=CARTESIAN_POINT('Ctrl Pts',(-0.951556276034575,6.70209485964647,
-34.7578986161762));
#39426=CARTESIAN_POINT('Ctrl Pts',(-1.12636764018125,6.67494007935993,-34.7496003531876));
#39427=CARTESIAN_POINT('Ctrl Pts',(-1.29982510772464,6.64098966188991,-34.741302090199));
#39428=CARTESIAN_POINT('Ctrl Pts',(-1.473303580227,6.60703513316924,-34.7330028223262));
#39429=CARTESIAN_POINT('Ctrl Pts',(-1.64542748826131,6.56628339488382,-34.7247035544534));
#39430=CARTESIAN_POINT('Ctrl Pts',(-1.81564123312953,6.51887535642153,-34.7164042865806));
#39431=CARTESIAN_POINT('Ctrl Pts',(-1.98597449548109,6.47143402987518,-34.7080991912841));
#39432=CARTESIAN_POINT('Ctrl Pts',(-2.15439457918814,6.41732715751474,-34.6997940959876));
#39433=CARTESIAN_POINT('Ctrl Pts',(-2.32036063819031,6.35674566965968,-34.6914890006911));
#39434=CARTESIAN_POINT('Ctrl Pts',(-2.48638721704772,6.29614209064395,-34.683180876925));
#39435=CARTESIAN_POINT('Ctrl Pts',(-2.64995766349802,6.22905931655855,-34.6748727531588));
#39436=CARTESIAN_POINT('Ctrl Pts',(-2.81055134778003,6.15573635899816,-34.6665646293927));
#39437=CARTESIAN_POINT('Ctrl Pts',(-2.97131574222061,6.0823354595575,-34.6582476741391));
#39438=CARTESIAN_POINT('Ctrl Pts',(-3.12909673887959,6.00268127474854,-34.6499307188854));
#39439=CARTESIAN_POINT('Ctrl Pts',(-3.28339756684109,5.91705918662827,-34.6416137636317));
#39440=CARTESIAN_POINT('Ctrl Pts',(-3.39711492941807,5.85395701039238,-34.6354842941492));
#39441=CARTESIAN_POINT('Ctrl Pts',(-3.50894256167725,5.78761435019159,-34.6293548246667));
#39442=CARTESIAN_POINT('Ctrl Pts',(-3.61869188062726,5.71816037490051,-34.6232253551841));
#39443=CARTESIAN_POINT('Ctrl Pts',(-3.77000906704334,5.62240050844298,-34.614774331659));
#39444=CARTESIAN_POINT('Ctrl Pts',(-3.91765088171373,5.52054960774435,-34.6063233081338));
#39445=CARTESIAN_POINT('Ctrl Pts',(-4.06111487832845,5.41291372044847,-34.5978722846086));
#39446=CARTESIAN_POINT('Ctrl Pts',(-4.20445255915799,5.30537260335235,-34.5894287019585));
#39447=CARTESIAN_POINT('Ctrl Pts',(-4.34361948984515,5.19205684999914,-34.5809851193084));
#39448=CARTESIAN_POINT('Ctrl Pts',(-4.47814171585854,5.07331605290737,-34.5725415366582));
#39449=CARTESIAN_POINT('Ctrl Pts',(-4.61256378588424,4.95466366203785,-34.5641042405184));
#39450=CARTESIAN_POINT('Ctrl Pts',(-4.74234779714123,4.83059449786061,-34.5556669443786));
#39451=CARTESIAN_POINT('Ctrl Pts',(-4.86705214129365,4.70149895819716,-34.5472296482387));
#39452=CARTESIAN_POINT('Ctrl Pts',(-4.99166751840477,4.57249551835818,-34.5387983714664));
#39453=CARTESIAN_POINT('Ctrl Pts',(-5.11121022724892,4.43847309362074,-34.5303670946941));
#39454=CARTESIAN_POINT('Ctrl Pts',(-5.22527471574947,4.29985966572739,-34.5219358179217));
#39455=CARTESIAN_POINT('Ctrl Pts',(-5.33929031208093,4.16130565256728,-34.5135081550998));
#39456=CARTESIAN_POINT('Ctrl Pts',(-5.44783215899378,4.01816481478249,-34.5050804922779));
#39457=CARTESIAN_POINT('Ctrl Pts',(-5.5505338541505,3.87089949933206,-34.496652829456));
#39458=CARTESIAN_POINT('Ctrl Pts',(-5.65320393366362,3.72367951797005,-34.4882277610021));
#39459=CARTESIAN_POINT('Ctrl Pts',(-5.75003725735343,3.57233786257888,-34.4798026925481));
#39460=CARTESIAN_POINT('Ctrl Pts',(-5.84070955289625,3.41736754223284,-34.4713776240941));
#39461=CARTESIAN_POINT('Ctrl Pts',(-5.86552026836535,3.37496291906495,-34.4690722674803));
#39462=CARTESIAN_POINT('Ctrl Pts',(-5.88986993550112,3.33228677081255,-34.4667669108665));
#39463=CARTESIAN_POINT('Ctrl Pts',(-5.91375248523771,3.28934956235192,-34.4644615542527));
#39464=CARTESIAN_POINT('Ctrl Pts',(-6.00304167411293,3.12882111968981,-34.4558425657282));
#39465=CARTESIAN_POINT('Ctrl Pts',(-6.08575826444504,2.96471339317893,-34.4472235772037));
#39466=CARTESIAN_POINT('Ctrl Pts',(-6.16164022538411,2.79758444607638,-34.4386045886792));
#39467=CARTESIAN_POINT('Ctrl Pts',(-6.23756764638927,2.63035537382041,-34.4299804366115));
#39468=CARTESIAN_POINT('Ctrl Pts',(-6.30665214078173,2.46010174574732,-34.4213562845437));
#39469=CARTESIAN_POINT('Ctrl Pts',(-6.3686798857243,2.28740147616695,-34.4127321324759));
#39470=CARTESIAN_POINT('Ctrl Pts',(-6.4328320976185,2.10878617589184,-34.4038126008797));
#39471=CARTESIAN_POINT('Ctrl Pts',(-6.489435497163,1.92755401014723,-34.3948930692835));
#39472=CARTESIAN_POINT('Ctrl Pts',(-6.53830981141823,1.74436057336554,-34.3859735376872));
#39473=CARTESIAN_POINT('Ctrl Pts',(-6.58565363416623,1.56690381040624,-34.377333319828));
#39474=CARTESIAN_POINT('Ctrl Pts',(-6.62574509461208,1.38760705870056,-34.3686931019687));
#39475=CARTESIAN_POINT('Ctrl Pts',(-6.65847246900525,1.20707637682922,-34.3600528841095));
#39476=CARTESIAN_POINT('Ctrl Pts',(-6.69278681818168,1.01779162760461,-34.3509936956447));
#39477=CARTESIAN_POINT('Ctrl Pts',(-6.71900509300623,0.827150689016133,
-34.34193450718));
#39478=CARTESIAN_POINT('Ctrl Pts',(-6.73705967588828,0.635858414680623,
-34.3328753187153));
#39479=CARTESIAN_POINT('Ctrl Pts',(-6.75511425877033,0.444566140345081,
-34.3238161302506));
#39480=CARTESIAN_POINT('Ctrl Pts',(-6.76500516310217,0.252622914086894,
-34.3147569417859));
#39481=CARTESIAN_POINT('Ctrl Pts',(-6.76672744690538,0.0607343337615893,
-34.3056977533212));
#39482=CARTESIAN_POINT('Ctrl Pts',(-6.76690980082569,0.04041733674841,-34.3047385742774));
#39483=CARTESIAN_POINT('Ctrl Pts',(-6.76700064857688,0.0200999438642893,
-34.3037793952337));
#39484=CARTESIAN_POINT('Ctrl Pts',(-6.76699999651487,-0.000217181494126501,
-34.30282021619));
#39485=CARTESIAN_POINT('',(-6.76699750788529,-0.00580760486991878,-34.69717978378));
#39486=CARTESIAN_POINT('Ctrl Pts',(3.0990855038472,6.01564277861013,-35.3486949847746));
#39487=CARTESIAN_POINT('Ctrl Pts',(2.9397578610707,6.09772378080103,-35.3402675411684));
#39488=CARTESIAN_POINT('Ctrl Pts',(2.77721167747412,6.17344824237863,-35.3318400975623));
#39489=CARTESIAN_POINT('Ctrl Pts',(2.6119859135409,6.24258108377168,-35.3234126539561));
#39490=CARTESIAN_POINT('Ctrl Pts',(2.44661212069491,6.31177586259569,-35.3149776600425));
#39491=CARTESIAN_POINT('Ctrl Pts',(2.27855425848195,6.37436709208856,-35.3065426661289));
#39492=CARTESIAN_POINT('Ctrl Pts',(2.10837033981459,6.43016823342828,-35.2981076722153));
#39493=CARTESIAN_POINT('Ctrl Pts',(1.93810468087938,6.48599617636167,-35.289668626928));
#39494=CARTESIAN_POINT('Ctrl Pts',(1.76571124808744,6.53502743067727,-35.2812295816406));
#39495=CARTESIAN_POINT('Ctrl Pts',(1.59176166204321,6.57712580168948,-35.2727905363533));
#39496=CARTESIAN_POINT('Ctrl Pts',(1.41761785380289,6.61927117734398,-35.2643420685088));
#39497=CARTESIAN_POINT('Ctrl Pts',(1.24191474644245,6.65446813147599,-35.2558936006643));
#39498=CARTESIAN_POINT('Ctrl Pts',(1.06523377548364,6.68263166750711,-35.2474451328199));
#39499=CARTESIAN_POINT('Ctrl Pts',(0.963471630884538,6.69885289274981,-35.2425791067744));
#39500=CARTESIAN_POINT('Ctrl Pts',(0.861385212995945,6.7127418374066,-35.2377130807289));
#39501=CARTESIAN_POINT('Ctrl Pts',(0.759086148044961,6.7242900903996,-35.2328470546834));
#39502=CARTESIAN_POINT('Ctrl Pts',(0.585839307576767,6.74384743772162,-35.2246062790866));
#39503=CARTESIAN_POINT('Ctrl Pts',(0.411596968069216,6.75673212776572,-35.2163655034899));
#39504=CARTESIAN_POINT('Ctrl Pts',(0.23691250157723,6.76285157803988,-35.2081247278931));
#39505=CARTESIAN_POINT('Ctrl Pts',(0.0624215170694169,6.76896425035944,
-35.1998930798487));
#39506=CARTESIAN_POINT('Ctrl Pts',(-0.112510266890498,6.76832659096517,
-35.1916614318043));
#39507=CARTESIAN_POINT('Ctrl Pts',(-0.287322196330214,6.76089749630151,
-35.18342978376));
#39508=CARTESIAN_POINT('Ctrl Pts',(-0.461971655723405,6.7534753062316,-35.1752057862017));
#39509=CARTESIAN_POINT('Ctrl Pts',(-0.636501129060441,6.73927426636674,
-35.1669817886434));
#39510=CARTESIAN_POINT('Ctrl Pts',(-0.810347686599929,6.71830526448614,
-35.1587577910852));
#39511=CARTESIAN_POINT('Ctrl Pts',(-0.984040650031187,6.69735478880007,
-35.1505410594607));
#39512=CARTESIAN_POINT('Ctrl Pts',(-1.15705154834542,6.66964831135703,-35.1423243278361));
#39513=CARTESIAN_POINT('Ctrl Pts',(-1.32882043143063,6.63524869624436,-35.1341075962116));
#39514=CARTESIAN_POINT('Ctrl Pts',(-1.50050131095741,6.60086670532814,-35.125895074323));
#39515=CARTESIAN_POINT('Ctrl Pts',(-1.67094109457323,6.55979847593406,-35.1176825524343));
#39516=CARTESIAN_POINT('Ctrl Pts',(-1.83958749467868,6.5121583863894,-35.1094700305456));
#39517=CARTESIAN_POINT('Ctrl Pts',(-2.00817749861661,6.46453422791988,-35.1012602549637));
#39518=CARTESIAN_POINT('Ctrl Pts',(-2.17497497173797,6.41034268391535,-35.0930504793819));
#39519=CARTESIAN_POINT('Ctrl Pts',(-2.33944022862973,6.3497486892529,-35.0848407038001));
#39520=CARTESIAN_POINT('Ctrl Pts',(-2.41127438000354,6.32328280662706,-35.0812548871173));
#39521=CARTESIAN_POINT('Ctrl Pts',(-2.48266379697164,6.29559616331778,-35.0776690704346));
#39522=CARTESIAN_POINT('Ctrl Pts',(-2.55356448819593,6.26670546656093,-35.0740832537519));
#39523=CARTESIAN_POINT('Ctrl Pts',(-2.72872380369538,6.19533134339162,-35.0652245362301));
#39524=CARTESIAN_POINT('Ctrl Pts',(-2.90071750942194,6.11667939132356,-35.0563658187084));
#39525=CARTESIAN_POINT('Ctrl Pts',(-3.06897154411131,6.03106148712108,-35.0475071011866));
#39526=CARTESIAN_POINT('Ctrl Pts',(-3.23754035507439,5.9452834055719,-35.0386318104273));
#39527=CARTESIAN_POINT('Ctrl Pts',(-3.40235528218208,5.85251344558974,-35.0297565196679));
#39528=CARTESIAN_POINT('Ctrl Pts',(-3.56286907291655,5.75310811381594,-35.0208812289086));
#39529=CARTESIAN_POINT('Ctrl Pts',(-3.72383875890983,5.65342044854762,-35.0119807303278));
#39530=CARTESIAN_POINT('Ctrl Pts',(-3.88048264056111,5.54705983583765,-35.003080231747));
#39531=CARTESIAN_POINT('Ctrl Pts',(-4.03228204586679,5.43442641891307,-34.9941797331662));
#39532=CARTESIAN_POINT('Ctrl Pts',(-4.18428694223035,5.32164052998145,-34.9852671859686));
#39533=CARTESIAN_POINT('Ctrl Pts',(-4.33143405797199,5.20256503433119,-34.9763546387709));
#39534=CARTESIAN_POINT('Ctrl Pts',(-4.47323875905405,5.07763960955252,-34.9674420915733));
#39535=CARTESIAN_POINT('Ctrl Pts',(-4.61535657876507,4.95243833723544,-34.9585098646011));
#39536=CARTESIAN_POINT('Ctrl Pts',(-4.75210819332307,4.82136147136103,-34.9495776376288));
#39537=CARTESIAN_POINT('Ctrl Pts',(-4.88304467894395,4.68488672898686,-34.9406454106566));
#39538=CARTESIAN_POINT('Ctrl Pts',(-5.00679477785951,4.55590233790446,-34.9322034247112));
#39539=CARTESIAN_POINT('Ctrl Pts',(-5.1253507629051,4.42209676475768,-34.9237614387658));
#39540=CARTESIAN_POINT('Ctrl Pts',(-5.23836745235438,4.28389955929342,-34.9153194528204));
#39541=CARTESIAN_POINT('Ctrl Pts',(-5.34670294374354,4.15142653928605,-34.9072271374274));
#39542=CARTESIAN_POINT('Ctrl Pts',(-5.45018002904958,4.01463327173237,-34.8991348220344));
#39543=CARTESIAN_POINT('Ctrl Pts',(-5.54842804094167,3.87391730351749,-34.8910425066414));
#39544=CARTESIAN_POINT('Ctrl Pts',(-5.64654032475745,3.73339573218966,-34.8829613706542));
#39545=CARTESIAN_POINT('Ctrl Pts',(-5.73943771506141,3.588962557331,-34.8748802346671));
#39546=CARTESIAN_POINT('Ctrl Pts',(-5.82678883261555,3.44104938937335,-34.86679909868));
#39547=CARTESIAN_POINT('Ctrl Pts',(-5.91407045960886,3.29325389099205,-34.8587243914906));
#39548=CARTESIAN_POINT('Ctrl Pts',(-5.9958144054164,3.14198422553593,-34.8506496843013));
#39549=CARTESIAN_POINT('Ctrl Pts',(-6.07173145988988,2.98770247497698,-34.842574977112));
#39550=CARTESIAN_POINT('Ctrl Pts',(-6.14760302267668,2.83351317448876,-34.8345051085199));
#39551=CARTESIAN_POINT('Ctrl Pts',(-6.21765447963233,2.67631571287037,-34.8264352399278));
#39552=CARTESIAN_POINT('Ctrl Pts',(-6.28164167632996,2.51659826952863,-34.8183653713357));
#39553=CARTESIAN_POINT('Ctrl Pts',(-6.34560308667609,2.35694519109657,-34.810298754839));
#39554=CARTESIAN_POINT('Ctrl Pts',(-6.40350496398756,2.19477449671422,-34.8022321383423));
#39555=CARTESIAN_POINT('Ctrl Pts',(-6.4551506293771,2.03059581208385,-34.7941655218456));
#39556=CARTESIAN_POINT('Ctrl Pts',(-6.50689571333092,1.8661010813925,-34.7860833770093));
#39557=CARTESIAN_POINT('Ctrl Pts',(-6.55236033583749,1.69959096963597,-34.778001232173));
#39558=CARTESIAN_POINT('Ctrl Pts',(-6.59139632965033,1.53159505923469,-34.7699190873367));
#39559=CARTESIAN_POINT('Ctrl Pts',(-6.6303565999565,1.36392503369507,-34.7618526205526));
#39560=CARTESIAN_POINT('Ctrl Pts',(-6.6629130929852,1.19477533563551,-34.7537861537685));
#39561=CARTESIAN_POINT('Ctrl Pts',(-6.6889694020591,1.02468401876733,-34.7457196869844));
#39562=CARTESIAN_POINT('Ctrl Pts',(-6.71510167602282,0.854096815543634,
-34.737629703122));
#39563=CARTESIAN_POINT('Ctrl Pts',(-6.7346957445689,0.682562865173304,-34.7295397192596));
#39564=CARTESIAN_POINT('Ctrl Pts',(-6.74770664325823,0.510631037569024,
-34.7214497353973));
#39565=CARTESIAN_POINT('Ctrl Pts',(-6.76071754194755,0.338699209964744,
-34.7133597515349));
#39566=CARTESIAN_POINT('Ctrl Pts',(-6.76714527485211,0.166369881176929,
-34.7052697676725));
#39567=CARTESIAN_POINT('Ctrl Pts',(-6.76699750788584,-0.0058076042296127,
-34.6971797838101));
#39568=CARTESIAN_POINT('Ctrl Pts',(-6.76699750788529,-0.00580760486992044,
-34.69717978378));
#39569=CARTESIAN_POINT('Ctrl Pts',(-6.76681016756483,-0.224095782195824,
-34.6869232288782));
#39570=CARTESIAN_POINT('Ctrl Pts',(-6.75605708735273,-0.441891872896532,
-34.6766666739764));
#39571=CARTESIAN_POINT('Ctrl Pts',(-6.73490233367366,-0.658315696210507,
-34.6664101190746));
#39572=CARTESIAN_POINT('Ctrl Pts',(-6.71347909904819,-0.877486215316188,
-34.6560233953413));
#39573=CARTESIAN_POINT('Ctrl Pts',(-6.68138856748068,-1.09524956911206,
-34.645636671608));
#39574=CARTESIAN_POINT('Ctrl Pts',(-6.63884856683888,-1.31071686743604,
-34.6352499478748));
#39575=CARTESIAN_POINT('Ctrl Pts',(-6.59578266898006,-1.52884786230068,
-34.6247348191339));
#39576=CARTESIAN_POINT('Ctrl Pts',(-6.54200733234682,-1.74462585407272,
-34.614219690393));
#39577=CARTESIAN_POINT('Ctrl Pts',(-6.47779638330922,-1.95715176120453,
-34.6037045616522));
#39578=CARTESIAN_POINT('Ctrl Pts',(-6.4657610015762,-1.99698656288283,-34.6017336580872));
#39579=CARTESIAN_POINT('Ctrl Pts',(-6.45335913126745,-2.03670717311506,
-34.5997627545222));
#39580=CARTESIAN_POINT('Ctrl Pts',(-6.44059276114684,-2.07630775297472,
-34.5977918509573));
#39581=CARTESIAN_POINT('Ctrl Pts',(-6.38831434538541,-2.23847253111752,
-34.5897209807709));
#39582=CARTESIAN_POINT('Ctrl Pts',(-6.32981178682534,-2.39895766683898,
-34.5816501105845));
#39583=CARTESIAN_POINT('Ctrl Pts',(-6.26520760747365,-2.55723730522889,
-34.5735792403981));
#39584=CARTESIAN_POINT('Ctrl Pts',(-6.20068382300171,-2.71531997691133,
-34.5655184137823));
#39585=CARTESIAN_POINT('Ctrl Pts',(-6.13007366509786,-2.87120227128112,
-34.5574575871665));
#39586=CARTESIAN_POINT('Ctrl Pts',(-6.05354997673014,-3.0243712866033,-34.5493967605507));
#39587=CARTESIAN_POINT('Ctrl Pts',(-5.97710473566744,-3.17738328261918,
-34.5413441973908));
#39588=CARTESIAN_POINT('Ctrl Pts',(-5.89475819341828,-3.32768720397726,
-34.5332916342309));
#39589=CARTESIAN_POINT('Ctrl Pts',(-5.80673200582719,-3.47478811044676,
-34.5252390710711));
#39590=CARTESIAN_POINT('Ctrl Pts',(-5.71877678271408,-3.62177042789947,
-34.5171929996832));
#39591=CARTESIAN_POINT('Ctrl Pts',(-5.62515121821254,-3.76555455147239,
-34.5091469282953));
#39592=CARTESIAN_POINT('Ctrl Pts',(-5.52612376605051,-3.90566833234617,
-34.5011008569075));
#39593=CARTESIAN_POINT('Ctrl Pts',(-5.42715448617896,-4.04569980534085,
-34.4930595120716));
#39594=CARTESIAN_POINT('Ctrl Pts',(-5.32278985047443,-4.18206492398033,
-34.4850181672357));
#39595=CARTESIAN_POINT('Ctrl Pts',(-5.21334260978889,-4.31431893037123,
-34.4769768223999));
#39596=CARTESIAN_POINT('Ctrl Pts',(-5.1017855630724,-4.44912238705942,-34.4687804651788));
#39597=CARTESIAN_POINT('Ctrl Pts',(-4.98494816323669,-4.57965427631834,
-34.4605841079577));
#39598=CARTESIAN_POINT('Ctrl Pts',(-4.86320620052541,-4.70547706945547,
-34.4523877507367));
#39599=CARTESIAN_POINT('Ctrl Pts',(-4.74380463116985,-4.82888101848579,
-34.4443489620282));
#39600=CARTESIAN_POINT('Ctrl Pts',(-4.61968564584448,-4.94775502366046,
-34.4363101733197));
#39601=CARTESIAN_POINT('Ctrl Pts',(-4.49124223287662,-5.06172225686332,
-34.4282713846112));
#39602=CARTESIAN_POINT('Ctrl Pts',(-4.36278507529989,-5.17570168559266,
-34.4202317356794));
#39603=CARTESIAN_POINT('Ctrl Pts',(-4.23000284797881,-5.28477304889399,
-34.4121920867477));
#39604=CARTESIAN_POINT('Ctrl Pts',(-4.09332270285892,-5.3885989134709,-34.404152437816));
#39605=CARTESIAN_POINT('Ctrl Pts',(-3.95660086853438,-5.49245644627374,
-34.3961103366878));
#39606=CARTESIAN_POINT('Ctrl Pts',(-3.81597904710695,-5.59106506988513,
-34.3880682355596));
#39607=CARTESIAN_POINT('Ctrl Pts',(-3.6719143915468,-5.6841299862997,-34.3800261344314));
#39608=CARTESIAN_POINT('Ctrl Pts',(-3.52298811987531,-5.78033547800169,
-34.3717126439867));
#39609=CARTESIAN_POINT('Ctrl Pts',(-3.37038295108125,-5.87061632202818,
-34.3633991535419));
#39610=CARTESIAN_POINT('Ctrl Pts',(-3.2146316913088,-5.95469832058964,-34.3550856630971));
#39611=CARTESIAN_POINT('Ctrl Pts',(-3.06369942946313,-6.03617879299113,
-34.3470293949264));
#39612=CARTESIAN_POINT('Ctrl Pts',(-2.90981322243165,-6.11183819992559,
-34.3389731267556));
#39613=CARTESIAN_POINT('Ctrl Pts',(-2.75347794691015,-6.18147621494085,
-34.3309168585849));
#39614=CARTESIAN_POINT('Ctrl Pts',(-2.58965541161322,-6.25444935638185,
-34.3224747570031));
#39615=CARTESIAN_POINT('Ctrl Pts',(-2.42314390779816,-6.32080998595858,
-34.3140326554214));
#39616=CARTESIAN_POINT('Ctrl Pts',(-2.25454111502833,-6.38038661529588,
-34.3055905538396));
#39617=CARTESIAN_POINT('Ctrl Pts',(-2.0859383222585,-6.43996324463319,-34.2971484522578));
#39618=CARTESIAN_POINT('Ctrl Pts',(-1.91524470638034,-6.49275582016111,
-34.2887063506761));
#39619=CARTESIAN_POINT('Ctrl Pts',(-1.74306822618245,-6.53865446088667,
-34.2802642490943));
#39620=CARTESIAN_POINT('Ctrl Pts',(-1.57309968369904,-6.58396451169691,
-34.2719304064016));
#39621=CARTESIAN_POINT('Ctrl Pts',(-1.40114588204097,-6.62270101457491,
-34.2635965637089));
#39622=CARTESIAN_POINT('Ctrl Pts',(-1.22775003275432,-6.65469149225355,
-34.2552627210162));
#39623=CARTESIAN_POINT('Ctrl Pts',(-1.05455855241248,-6.68664426510711,
-34.2469387008115));
#39624=CARTESIAN_POINT('Ctrl Pts',(-0.879928749428964,-6.71186678938897,
-34.2386146806067));
#39625=CARTESIAN_POINT('Ctrl Pts',(-0.704418195599665,-6.7302365490158,
-34.230290660402));
#39626=CARTESIAN_POINT('Ctrl Pts',(-0.529082323557154,-6.74858802562566,
-34.2219749249111));
#39627=CARTESIAN_POINT('Ctrl Pts',(-0.352867790939159,-6.76010029012006,
-34.2136591894203));
#39628=CARTESIAN_POINT('Ctrl Pts',(-0.176341772977713,-6.76470195789165,
-34.2053434539294));
#39629=CARTESIAN_POINT('Ctrl Pts',(4.08966522569276E-5,-6.76929988886905,
-34.1970344712494));
#39630=CARTESIAN_POINT('Ctrl Pts',(0.176734201389097,-6.76699839607443,
-34.1887254885693));
#39631=CARTESIAN_POINT('Ctrl Pts',(0.353166209611189,-6.75777793571148,
-34.1804165058893));
#39632=CARTESIAN_POINT('Ctrl Pts',(0.529487254994421,-6.74856327434422,
-34.1721127489521));
#39633=CARTESIAN_POINT('Ctrl Pts',(0.705546984982687,-6.73243833563828,
-34.163808992015));
#39634=CARTESIAN_POINT('Ctrl Pts',(0.880773604091035,-6.70943565870756,
-34.1555052350778));
#39635=CARTESIAN_POINT('Ctrl Pts',(1.05592908541612,-6.68644232030915,-34.1472048492658));
#39636=CARTESIAN_POINT('Ctrl Pts',(1.23025178548296,-6.65657685255211,-34.1389044634537));
#39637=CARTESIAN_POINT('Ctrl Pts',(1.40317487012166,-6.61992366148274,-34.1306040776417));
#39638=CARTESIAN_POINT('Ctrl Pts',(1.57606148978124,-6.58327819961766,-34.1223054421651));
#39639=CARTESIAN_POINT('Ctrl Pts',(1.74754874197225,-6.5398479381213,-34.1140068066884));
#39640=CARTESIAN_POINT('Ctrl Pts',(1.91707958499378,-6.48976847543886,-34.1057081712118));
#39641=CARTESIAN_POINT('Ctrl Pts',(2.08660281854565,-6.43969126059609,-34.0974099082232));
#39642=CARTESIAN_POINT('Ctrl Pts',(2.25416948445153,-6.38296553799724,-34.0891116452347));
#39643=CARTESIAN_POINT('Ctrl Pts',(2.41923712668085,-6.31977695214704,-34.0808133822461));
#39644=CARTESIAN_POINT('Ctrl Pts',(2.58432475789711,-6.2565807144288,-34.0725141143733));
#39645=CARTESIAN_POINT('Ctrl Pts',(2.74691243786262,-6.18692017887483,-34.0642148465005));
#39646=CARTESIAN_POINT('Ctrl Pts',(2.90647695590489,-6.11102943085646,-34.0559155786277));
#39647=CARTESIAN_POINT('Ctrl Pts',(3.066153513957,-6.03508539530113,-34.0476104833311));
#39648=CARTESIAN_POINT('Ctrl Pts',(3.22280235401065,-5.95290255559377,-34.0393053880346));
#39649=CARTESIAN_POINT('Ctrl Pts',(3.37592337612668,-5.8647617478054,-34.0310002927381));
#39650=CARTESIAN_POINT('Ctrl Pts',(3.52910023412966,-5.77658879929519,-34.022692168972));
#39651=CARTESIAN_POINT('Ctrl Pts',(3.67874641249367,-5.68245373233268,-34.0143840452059));
#39652=CARTESIAN_POINT('Ctrl Pts',(3.82438997219138,-5.58268128595947,-34.0060759214398));
#39653=CARTESIAN_POINT('Ctrl Pts',(3.97018835015152,-5.48280278205224,-33.9977589661861));
#39654=CARTESIAN_POINT('Ctrl Pts',(4.11197532565338,-5.37727512860384,-33.9894420109324));
#39655=CARTESIAN_POINT('Ctrl Pts',(4.24931041585057,-5.26646465759943,-33.9811250556788));
#39656=CARTESIAN_POINT('Ctrl Pts',(4.35052428782257,-5.18479902641009,-33.9749955861963));
#39657=CARTESIAN_POINT('Ctrl Pts',(4.44932080234844,-5.10026491130442,-33.9688661167137));
#39658=CARTESIAN_POINT('Ctrl Pts',(4.54553631636467,-5.01302190266609,-33.9627366472312));
#39659=CARTESIAN_POINT('Ctrl Pts',(4.67819373064139,-4.89273535576128,-33.954285623706));
#39660=CARTESIAN_POINT('Ctrl Pts',(4.8061858353245,-4.76707815321763,-33.9458346001809));
#39661=CARTESIAN_POINT('Ctrl Pts',(4.92907009953112,-4.63643795967424,-33.9373835766557));
#39662=CARTESIAN_POINT('Ctrl Pts',(5.05184616779529,-4.50591279093858,-33.9289399940055));
#39663=CARTESIAN_POINT('Ctrl Pts',(5.16952313349309,-4.37041361640582,-33.9204964113554));
#39664=CARTESIAN_POINT('Ctrl Pts',(5.28169400177359,-4.23036611555417,-33.9120528287053));
#39665=CARTESIAN_POINT('Ctrl Pts',(5.39378135534839,-4.09042288442956,-33.9036155325654));
#39666=CARTESIAN_POINT('Ctrl Pts',(5.50037057703699,-3.94593833543775,-33.8951782364256));
#39667=CARTESIAN_POINT('Ctrl Pts',(5.60109353563225,-3.79737280301772,-33.8867409402858));
#39668=CARTESIAN_POINT('Ctrl Pts',(5.70174463607636,-3.64891326077741,-33.8783096635134));
#39669=CARTESIAN_POINT('Ctrl Pts',(5.79653763580677,-3.49637881623328,-33.8698783867411));
#39670=CARTESIAN_POINT('Ctrl Pts',(5.88514637004556,-3.34026064898229,-33.8614471099688));
#39671=CARTESIAN_POINT('Ctrl Pts',(5.97371712337331,-3.18420939962909,-33.8530194471468));
#39672=CARTESIAN_POINT('Ctrl Pts',(6.05610873237419,-3.02457777763841,-33.8445917843249));
#39673=CARTESIAN_POINT('Ctrl Pts',(6.13203949449097,-2.86188410631929,-33.836164121503));
#39674=CARTESIAN_POINT('Ctrl Pts',(6.20794688211602,-2.69924051854693,-33.827739053049));
#39675=CARTESIAN_POINT('Ctrl Pts',(6.27739724921018,-2.53353706129902,-33.819313984595));
#39676=CARTESIAN_POINT('Ctrl Pts',(6.34015565664528,-2.36531504233766,-33.8108889161411));
#39677=CARTESIAN_POINT('Ctrl Pts',(6.35732827790547,-2.31928434880494,-33.8085835595273));
#39678=CARTESIAN_POINT('Ctrl Pts',(6.37400012285963,-2.27306520228473,-33.8062782029135));
#39679=CARTESIAN_POINT('Ctrl Pts',(6.39016700662039,-2.2266689532798,-33.8039728462997));
#39680=CARTESIAN_POINT('Ctrl Pts',(6.45060979658932,-2.05320826812559,-33.7953538577752));
#39681=CARTESIAN_POINT('Ctrl Pts',(6.50396361824192,-1.87734823875085,-33.7867348692508));
#39682=CARTESIAN_POINT('Ctrl Pts',(6.55006600635919,-1.6996835918305,-33.7781158807263));
#39683=CARTESIAN_POINT('Ctrl Pts',(6.59619601392121,-1.52191250793146,-33.7694917286585));
#39684=CARTESIAN_POINT('Ctrl Pts',(6.63506584174416,-1.34233494328947,-33.7608675765907));
#39685=CARTESIAN_POINT('Ctrl Pts',(6.66656392236928,-1.16155691593838,-33.7522434245229));
#39686=CARTESIAN_POINT('Ctrl Pts',(6.69914082072965,-0.974587192516405,
-33.7433238929267));
#39687=CARTESIAN_POINT('Ctrl Pts',(6.72383200935134,-0.786333672111318,
-33.7344043613305));
#39688=CARTESIAN_POINT('Ctrl Pts',(6.74057229283507,-0.597473150078047,
-33.7254848297342));
#39689=CARTESIAN_POINT('Ctrl Pts',(6.75678835695958,-0.414526765755616,
-33.716844611875));
#39690=CARTESIAN_POINT('Ctrl Pts',(6.76554397422496,-0.231011127350753,
-33.7082043940157));
#39691=CARTESIAN_POINT('Ctrl Pts',(6.76683298989388,-0.0475424745237331,
-33.6995641761565));
#39692=CARTESIAN_POINT('Ctrl Pts',(6.76818451089358,0.14482271005868,-33.6905049876918));
#39693=CARTESIAN_POINT('Ctrl Pts',(6.76132731938759,0.337135851381192,-33.6814457992271));
#39694=CARTESIAN_POINT('Ctrl Pts',(6.74631565298735,0.528690940207873,-33.6723866107623));
#39695=CARTESIAN_POINT('Ctrl Pts',(6.7313039865871,0.720246029034587,-33.6633274222976));
#39696=CARTESIAN_POINT('Ctrl Pts',(6.70813792429692,0.911042689521306,-33.6542682338329));
#39697=CARTESIAN_POINT('Ctrl Pts',(6.67693357879445,1.10038492554522,-33.6452090453682));
#39698=CARTESIAN_POINT('Ctrl Pts',(6.64578329263131,1.28939913942923,-33.6361655513119));
#39699=CARTESIAN_POINT('Ctrl Pts',(6.60659468957936,1.47713823075668,-33.6271220572556));
#39700=CARTESIAN_POINT('Ctrl Pts',(6.55949036977891,1.66294169734775,-33.6180785631993));
#39701=CARTESIAN_POINT('Ctrl Pts',(6.51242913612754,1.8485752101873,-33.609043341194));
#39702=CARTESIAN_POINT('Ctrl Pts',(6.45746669982507,2.03227640252955,-33.6000081191887));
#39703=CARTESIAN_POINT('Ctrl Pts',(6.3947763876249,2.21339647426191,-33.5909728971833));
#39704=CARTESIAN_POINT('Ctrl Pts',(6.33219652210728,2.39419745185733,-33.5819535932722));
#39705=CARTESIAN_POINT('Ctrl Pts',(6.26191604559772,2.57242616468167,-33.5729342893611));
#39706=CARTESIAN_POINT('Ctrl Pts',(6.18415752465822,2.74745058376182,-33.56391498545));
#39707=CARTESIAN_POINT('Ctrl Pts',(6.1064965572145,2.92225542248314,-33.5549069968856));
#39708=CARTESIAN_POINT('Ctrl Pts',(6.02137636442516,3.09386377308503,-33.5458990083212));
#39709=CARTESIAN_POINT('Ctrl Pts',(5.92906780736512,3.26166275627426,-33.5368910197569));
#39710=CARTESIAN_POINT('Ctrl Pts',(5.83696773241452,3.42908275958242,-33.5279033760502));
#39711=CARTESIAN_POINT('Ctrl Pts',(5.73771181462949,3.59271036080958,-33.5189157323435));
#39712=CARTESIAN_POINT('Ctrl Pts',(5.63161685080284,3.75195690883485,-33.5099280886368));
#39713=CARTESIAN_POINT('Ctrl Pts',(5.53921549077015,3.89064961475902,-33.5021004739035));
#39714=CARTESIAN_POINT('Ctrl Pts',(5.44162733849227,4.0260194178936,-33.4942728591701));
#39715=CARTESIAN_POINT('Ctrl Pts',(5.33909048514265,4.15769188269877,-33.4864452444367));
#39716=CARTESIAN_POINT('Ctrl Pts',(5.23268593916626,4.29433103611042,-33.4783223718833));
#39717=CARTESIAN_POINT('Ctrl Pts',(5.12099856321383,4.42692655870261,-33.47019949933));
#39718=CARTESIAN_POINT('Ctrl Pts',(5.0043783765593,4.55505061050102,-33.4620766267766));
#39719=CARTESIAN_POINT('Ctrl Pts',(4.88776807567165,4.68316380136237,-33.4539544427903));
#39720=CARTESIAN_POINT('Ctrl Pts',(4.76622604397042,4.80680600640928,-33.4458322588041));
#39721=CARTESIAN_POINT('Ctrl Pts',(4.64014106541251,4.92558421845292,-33.4377100748178));
#39722=CARTESIAN_POINT('Ctrl Pts',(4.51400044247048,5.04441485022595,-33.4295843063131));
#39723=CARTESIAN_POINT('Ctrl Pts',(4.38331313241626,5.15837694765739,-33.4214585378084));
#39724=CARTESIAN_POINT('Ctrl Pts',(4.2485034687129,5.26711565055624,-33.4133327693038));
#39725=CARTESIAN_POINT('Ctrl Pts',(4.11366266659085,5.37587946998729,-33.4052051239041));
#39726=CARTESIAN_POINT('Ctrl Pts',(3.97469790425233,5.47941726831582,-33.3970774785045));
#39727=CARTESIAN_POINT('Ctrl Pts',(3.83206458138181,5.57741607235099,-33.3889498331048));
#39728=CARTESIAN_POINT('Ctrl Pts',(3.68930618332906,5.67550081155212,-33.3808150605717));
#39729=CARTESIAN_POINT('Ctrl Pts',(3.54287310595884,5.76803665496158,-33.3726802880385));
#39730=CARTESIAN_POINT('Ctrl Pts',(3.39324814791047,5.85475499117616,-33.3645455155054));
#39731=CARTESIAN_POINT('Ctrl Pts',(3.29648324385166,5.91083715549818,-33.3592846252504));
#39732=CARTESIAN_POINT('Ctrl Pts',(3.19838388179903,5.96448712077082,-33.3540237349953));
#39733=CARTESIAN_POINT('Ctrl Pts',(3.09908550384718,6.01564277861014,-33.3487628447403));
#39734=CARTESIAN_POINT('Origin',(0.,0.,-63.6971797838103));
#39735=CARTESIAN_POINT('',(3.09908550384721,6.01564277861012,-30.9542680870819));
#39736=CARTESIAN_POINT('',(3.0990855038472,6.01564277861013,-31.3484270467647));
#39737=CARTESIAN_POINT('',(3.09908550384721,6.01564277861012,-63.6971797838103));
#39738=CARTESIAN_POINT('',(-6.76699974407564,0.00186109651007785,-32.3028202161598));
#39739=CARTESIAN_POINT('Ctrl Pts',(-6.76699974407564,0.00186109651002826,
-32.3028202161599));
#39740=CARTESIAN_POINT('Ctrl Pts',(-6.76704658566934,-0.168456267928749,
-32.2948236154397));
#39741=CARTESIAN_POINT('Ctrl Pts',(-6.76065907798607,-0.338861495845034,
-32.2868270147195));
#39742=CARTESIAN_POINT('Ctrl Pts',(-6.74784363645294,-0.508817509507621,
-32.2788304139993));
#39743=CARTESIAN_POINT('Ctrl Pts',(-6.73502917781086,-0.678760488251144,
-32.2708344265852));
#39744=CARTESIAN_POINT('Ctrl Pts',(-6.7157877893052,-0.848253943265322,
-32.262838439171));
#39745=CARTESIAN_POINT('Ctrl Pts',(-6.69017792726411,-1.01676364094518,
-32.2548424517568));
#39746=CARTESIAN_POINT('Ctrl Pts',(-6.67621983595172,-1.10860614066129,
-32.2504844149084));
#39747=CARTESIAN_POINT('Ctrl Pts',(-6.66037085973537,-1.20015649082171,
-32.2461263780599));
#39748=CARTESIAN_POINT('Ctrl Pts',(-6.64264691453626,-1.2913291481268,-32.2417683412114));
#39749=CARTESIAN_POINT('Ctrl Pts',(-6.607593865287,-1.47164338464694,-32.2331493526869));
#39750=CARTESIAN_POINT('Ctrl Pts',(-6.56520739634836,-1.6504638741543,-32.2245303641624));
#39751=CARTESIAN_POINT('Ctrl Pts',(-6.51564637819431,-1.82719491963047,
-32.2159113756379));
#39752=CARTESIAN_POINT('Ctrl Pts',(-6.46605566856741,-2.00403184277489,
-32.2072872235701));
#39753=CARTESIAN_POINT('Ctrl Pts',(-6.40928191396484,-2.17877653089512,
-32.1986630715023));
#39754=CARTESIAN_POINT('Ctrl Pts',(-6.34553365094708,-2.35084914120371,
-32.1900389194345));
#39755=CARTESIAN_POINT('Ctrl Pts',(-6.27960199277124,-2.52881528470679,
-32.1811193878383));
#39756=CARTESIAN_POINT('Ctrl Pts',(-6.2062097418672,-2.70392273813924,-32.1721998562421));
#39757=CARTESIAN_POINT('Ctrl Pts',(-6.12564112338535,-2.87555382969791,
-32.1632803246459));
#39758=CARTESIAN_POINT('Ctrl Pts',(-6.04759549859063,-3.04181032046688,
-32.1546401067866));
#39759=CARTESIAN_POINT('Ctrl Pts',(-5.9628163395388,-3.20480462884413,-32.1459998889273));
#39760=CARTESIAN_POINT('Ctrl Pts',(-5.87160842070543,-3.36400112275562,
-32.1373596710681));
#39761=CARTESIAN_POINT('Ctrl Pts',(-5.7759777618907,-3.53091717334071,-32.1283004826034));
#39762=CARTESIAN_POINT('Ctrl Pts',(-5.67327957934809,-3.69365760686278,
-32.1192412941387));
#39763=CARTESIAN_POINT('Ctrl Pts',(-5.56391600898354,-3.85163960476272,
-32.110182105674));
#39764=CARTESIAN_POINT('Ctrl Pts',(-5.454552438619,-4.00962160266263,-32.1011229172093));
#39765=CARTESIAN_POINT('Ctrl Pts',(-5.33852373783123,-4.16284487990282,
-32.0920637287446));
#39766=CARTESIAN_POINT('Ctrl Pts',(-5.21628047439728,-4.31076640661748,
-32.0830045402799));
#39767=CARTESIAN_POINT('Ctrl Pts',(-5.09424898884043,-4.45843166966553,
-32.0739610462236));
#39768=CARTESIAN_POINT('Ctrl Pts',(-4.96591268640582,-4.60095011232842,
-32.0649175521673));
#39769=CARTESIAN_POINT('Ctrl Pts',(-4.83170988049905,-4.73781264199925,
-32.055874058111));
#39770=CARTESIAN_POINT('Ctrl Pts',(-4.69762982940854,-4.8745499840142,-32.0468388361057));
#39771=CARTESIAN_POINT('Ctrl Pts',(-4.55769415477322,-5.00564157198395,
-32.0378036141004));
#39772=CARTESIAN_POINT('Ctrl Pts',(-4.41237911784053,-5.13061395160899,
-32.0287683920951));
#39773=CARTESIAN_POINT('Ctrl Pts',(-4.2673200943678,-5.25536615710765,-32.019749088184));
#39774=CARTESIAN_POINT('Ctrl Pts',(-4.11690081379617,-5.3740205269628,-32.0107297842729));
#39775=CARTESIAN_POINT('Ctrl Pts',(-3.96163164959631,-5.48614287755221,
-32.0017104803618));
#39776=CARTESIAN_POINT('Ctrl Pts',(-3.80655728140831,-5.59812456282119,
-31.9927024917974));
#39777=CARTESIAN_POINT('Ctrl Pts',(-3.64664536464657,-5.70359044400696,
-31.983694503233));
#39778=CARTESIAN_POINT('Ctrl Pts',(-3.48243837122316,-5.8021471879497,-31.9746865146687));
#39779=CARTESIAN_POINT('Ctrl Pts',(-3.31860224504604,-5.90048133803412,
-31.965698870962));
#39780=CARTESIAN_POINT('Ctrl Pts',(-3.15049060921926,-5.99193737664443,
-31.9567112272553));
#39781=CARTESIAN_POINT('Ctrl Pts',(-2.97867344019052,-6.07616602280613,
-31.9477235835487));
#39782=CARTESIAN_POINT('Ctrl Pts',(-2.82903259464324,-6.14952333571139,
-31.9398959688152));
#39783=CARTESIAN_POINT('Ctrl Pts',(-2.67658157812106,-6.21739909447239,
-31.9320683540818));
#39784=CARTESIAN_POINT('Ctrl Pts',(-2.52171455837233,-6.27958953165675,
-31.9242407393484));
#39785=CARTESIAN_POINT('Ctrl Pts',(-2.36100029455,-6.34412806507136,-31.9161175809031));
#39786=CARTESIAN_POINT('Ctrl Pts',(-2.19775536071387,-6.40251345397151,
-31.9079944224579));
#39787=CARTESIAN_POINT('Ctrl Pts',(-2.03249757759334,-6.45455208338094,
-31.8998712640126));
#39788=CARTESIAN_POINT('Ctrl Pts',(-1.86725144601121,-6.50658704379471,
-31.8917486782925));
#39789=CARTESIAN_POINT('Ctrl Pts',(-1.69999309695263,-6.55227602611667,
-31.8836260925724));
#39790=CARTESIAN_POINT('Ctrl Pts',(-1.53125634743834,-6.59147502448654,
-31.8755035068523));
#39791=CARTESIAN_POINT('Ctrl Pts',(-1.3624993224679,-6.63067873301928,-31.8673799451199));
#39792=CARTESIAN_POINT('Ctrl Pts',(-1.19226390010267,-6.66339082310288,
-31.8592563833876));
#39793=CARTESIAN_POINT('Ctrl Pts',(-1.02109489801628,-6.6895182344654,-31.8511328216553));
#39794=CARTESIAN_POINT('Ctrl Pts',(-0.849801219622619,-6.71566467654685,
-31.8430033428722));
#39795=CARTESIAN_POINT('Ctrl Pts',(-0.677572965566393,-6.73521680543398,
-31.8348738640891));
#39796=CARTESIAN_POINT('Ctrl Pts',(-0.504961539524183,-6.74813328585035,
-31.8267443853059));
#39797=CARTESIAN_POINT('Ctrl Pts',(-0.332279742841576,-6.76105503208845,
-31.8186115922774));
#39798=CARTESIAN_POINT('Ctrl Pts',(-0.159214828318478,-6.76733572424922,
-31.8104787992489));
#39799=CARTESIAN_POINT('Ctrl Pts',(0.0136812215726762,-6.76698616994126,
-31.8023460062203));
#39800=CARTESIAN_POINT('Ctrl Pts',(0.18676526968823,-6.76663623554602,-31.7942043700132));
#39801=CARTESIAN_POINT('Ctrl Pts',(0.359679721161646,-6.7596416700172,-31.7860627338061));
#39802=CARTESIAN_POINT('Ctrl Pts',(0.531876381940679,-6.74606526164206,
-31.7779210975989));
#39803=CARTESIAN_POINT('Ctrl Pts',(0.619608241681404,-6.73914826598162,
-31.7737730445382));
#39804=CARTESIAN_POINT('Ctrl Pts',(0.707153903593955,-6.73052360732793,
-31.7696249914775));
#39805=CARTESIAN_POINT('Ctrl Pts',(0.794441887476215,-6.72020469088727,
-31.7654769384169));
#39806=CARTESIAN_POINT('Ctrl Pts',(0.972060876959575,-6.69920712135667,
-31.7570362234388));
#39807=CARTESIAN_POINT('Ctrl Pts',(1.14897812505722,-6.67114787233272,-31.7485955084607));
#39808=CARTESIAN_POINT('Ctrl Pts',(1.32461025384826,-6.63609046618565,-31.7401547934826));
#39809=CARTESIAN_POINT('Ctrl Pts',(1.50010963160125,-6.60105955807791,-31.7317204583946));
#39810=CARTESIAN_POINT('Ctrl Pts',(1.67432550058884,-6.55904110225151,-31.7232861233066));
#39811=CARTESIAN_POINT('Ctrl Pts',(1.84668192470545,-6.51015014181441,-31.7148517882185));
#39812=CARTESIAN_POINT('Ctrl Pts',(2.01893454101275,-6.46128862770358,-31.7064225330099));
#39813=CARTESIAN_POINT('Ctrl Pts',(2.18932962521364,-6.40556295188272,-31.6979932778013));
#39814=CARTESIAN_POINT('Ctrl Pts',(2.35730332960249,-6.34313881388741,-31.6895640225927));
#39815=CARTESIAN_POINT('Ctrl Pts',(2.52520163173223,-6.28074269766518,-31.6811385512197));
#39816=CARTESIAN_POINT('Ctrl Pts',(2.69068040928394,-6.21165423065285,-31.6727130798467));
#39817=CARTESIAN_POINT('Ctrl Pts',(2.8531924503838,-6.13608848054466,-31.6642876084737));
#39818=CARTESIAN_POINT('Ctrl Pts',(3.01565644820917,-6.06054506986468,-31.6558646279145));
#39819=CARTESIAN_POINT('Ctrl Pts',(3.17515515662037,-5.9785283352109,-31.6474416473553));
#39820=CARTESIAN_POINT('Ctrl Pts',(3.3311624091704,-5.8903010113007,-31.6390186667961));
#39821=CARTESIAN_POINT('Ctrl Pts',(3.48717224487779,-5.80207222652854,-31.6305955467697));
#39822=CARTESIAN_POINT('Ctrl Pts',(3.63969021581832,-5.70763280537124,-31.6221724267434));
#39823=CARTESIAN_POINT('Ctrl Pts',(3.78821519843597,-5.60729120077946,-31.6137493067171));
#39824=CARTESIAN_POINT('Ctrl Pts',(3.93674531729517,-5.50694612620767,-31.6053258954052));
#39825=CARTESIAN_POINT('Ctrl Pts',(4.08128189606481,-5.40069864779729,-31.5969024840933));
#39826=CARTESIAN_POINT('Ctrl Pts',(4.22135309971023,-5.28890035901291,-31.5884790727814));
#39827=CARTESIAN_POINT('Ctrl Pts',(4.36144868224157,-5.17708261214109,-31.5800541954053));
#39828=CARTESIAN_POINT('Ctrl Pts',(4.49707707953395,-5.0597123368144,-31.5716293180292));
#39829=CARTESIAN_POINT('Ctrl Pts',(4.62779954899389,-4.93718141598341,-31.5632044406531));
#39830=CARTESIAN_POINT('Ctrl Pts',(4.75856300702829,-4.81461207507213,-31.5547769216216));
#39831=CARTESIAN_POINT('Ctrl Pts',(4.88441722710938,-4.68687909049526,-31.5463494025901));
#39832=CARTESIAN_POINT('Ctrl Pts',(5.00496008102947,-4.55441144246998,-31.5379218835586));
#39833=CARTESIAN_POINT('Ctrl Pts',(5.12561103312129,-4.42182500257858,-31.5294868070538));
#39834=CARTESIAN_POINT('Ctrl Pts',(5.24094087717673,-4.28449566228239,-31.521051730549));
#39835=CARTESIAN_POINT('Ctrl Pts',(5.35058683568231,-4.1428866160955,-31.5126166540442));
#39836=CARTESIAN_POINT('Ctrl Pts',(5.4602857868012,-4.00120912932467,-31.5041775008115));
#39837=CARTESIAN_POINT('Ctrl Pts',(5.56429517607593,-3.85524807990081,-31.4957383475787));
#39838=CARTESIAN_POINT('Ctrl Pts',(5.66229509756711,-3.70549635380572,-31.4872991943459));
#39839=CARTESIAN_POINT('Ctrl Pts',(5.76040392444774,-3.55557821155638,-31.4788506628478));
#39840=CARTESIAN_POINT('Ctrl Pts',(5.85248976380151,-3.40186125891017,-31.4704021313497));
#39841=CARTESIAN_POINT('Ctrl Pts',(5.93827766318478,-3.2448647729791,-31.4619535998515));
#39842=CARTESIAN_POINT('Ctrl Pts',(5.98567826098805,-3.15811912074092,-31.4572855120856));
#39843=CARTESIAN_POINT('Ctrl Pts',(6.03115697502175,-3.0703726647477,-31.4526174243198));
#39844=CARTESIAN_POINT('Ctrl Pts',(6.07467368380423,-2.98171572006728,-31.4479493365539));
#39845=CARTESIAN_POINT('Ctrl Pts',(6.15149559670978,-2.82520581218904,-31.4397085609571));
#39846=CARTESIAN_POINT('Ctrl Pts',(6.22237115158676,-2.66550902500934,-31.4314677853604));
#39847=CARTESIAN_POINT('Ctrl Pts',(6.28702661886985,-2.50311511793245,-31.4232270097636));
#39848=CARTESIAN_POINT('Ctrl Pts',(6.35161047321313,-2.34090107971402,-31.4149953617193));
#39849=CARTESIAN_POINT('Ctrl Pts',(6.40998782761032,-2.17599619760905,-31.406763713675));
#39850=CARTESIAN_POINT('Ctrl Pts',(6.46193096237487,-2.00891444255374,-31.3985320656306));
#39851=CARTESIAN_POINT('Ctrl Pts',(6.51382582123821,-1.8419879731264,-31.3903080680723));
#39852=CARTESIAN_POINT('Ctrl Pts',(6.55929826474335,-1.67288899773513,-31.382084070514));
#39853=CARTESIAN_POINT('Ctrl Pts',(6.59816875328745,-1.50215115855267,-31.3738600729558));
#39854=CARTESIAN_POINT('Ctrl Pts',(6.63700489960395,-1.3315641669143,-31.3656433413313));
#39855=CARTESIAN_POINT('Ctrl Pts',(6.6692506377745,-1.15934154297199,-31.3574266097067));
#39856=CARTESIAN_POINT('Ctrl Pts',(6.69477636597363,-0.98603164736275,-31.3492098780822));
#39857=CARTESIAN_POINT('Ctrl Pts',(6.72028901639722,-0.812810544829176,
-31.3409973561935));
#39858=CARTESIAN_POINT('Ctrl Pts',(6.7390884620531,-0.638503631174716,-31.3327848343048));
#39859=CARTESIAN_POINT('Ctrl Pts',(6.75109618269687,-0.463669421005698,
-31.3245723124161));
#39860=CARTESIAN_POINT('Ctrl Pts',(6.7630998879011,-0.288893676237496,-31.3163625368343));
#39861=CARTESIAN_POINT('Ctrl Pts',(6.76831636821242,-0.113591340786384,
-31.3081527612524));
#39862=CARTESIAN_POINT('Ctrl Pts',(6.76671894874299,0.0616738901205327,
-31.2999429856705));
#39863=CARTESIAN_POINT('Ctrl Pts',(6.76602123741997,0.138225189559716,-31.2963571689877));
#39864=CARTESIAN_POINT('Ctrl Pts',(6.76402429762049,0.214769368334944,-31.292771352305));
#39865=CARTESIAN_POINT('Ctrl Pts',(6.76072902687091,0.291259377918038,-31.2891855356222));
#39866=CARTESIAN_POINT('Ctrl Pts',(6.75258809962594,0.48022703802957,-31.2803268181004));
#39867=CARTESIAN_POINT('Ctrl Pts',(6.73652816999348,0.668668124403733,-31.2714681005787));
#39868=CARTESIAN_POINT('Ctrl Pts',(6.7126493121296,0.855937037617868,-31.2626093830569));
#39869=CARTESIAN_POINT('Ctrl Pts',(6.68872578075796,1.04355630089041,-31.2537340922975));
#39870=CARTESIAN_POINT('Ctrl Pts',(6.65695412098099,1.22999875128215,-31.2448588015381));
#39871=CARTESIAN_POINT('Ctrl Pts',(6.61748546232807,1.41462898170394,-31.2359835107787));
#39872=CARTESIAN_POINT('Ctrl Pts',(6.57790470380997,1.59978360349453,-31.227083012198));
#39873=CARTESIAN_POINT('Ctrl Pts',(6.53058325401584,1.78311545011171,-31.2181825136172));
#39874=CARTESIAN_POINT('Ctrl Pts',(6.47572296005789,1.96400130971929,-31.2092820150364));
#39875=CARTESIAN_POINT('Ctrl Pts',(6.4207884016467,2.14513203475675,-31.2003694678388));
#39876=CARTESIAN_POINT('Ctrl Pts',(6.35829469482546,2.32380991235501,-31.1914569206412));
#39877=CARTESIAN_POINT('Ctrl Pts',(6.28849238220523,2.49943044691122,-31.1825443734436));
#39878=CARTESIAN_POINT('Ctrl Pts',(6.21853593926143,2.67543876875986,-31.1736121464713));
#39879=CARTESIAN_POINT('Ctrl Pts',(6.14123870780059,2.84837600263461,-31.1646799194991));
#39880=CARTESIAN_POINT('Ctrl Pts',(6.05689908236603,3.01765844754398,-31.1557476925268));
#39881=CARTESIAN_POINT('Ctrl Pts',(5.97718839714009,3.17764990601824,-31.1473057065815));
#39882=CARTESIAN_POINT('Ctrl Pts',(5.89118762133789,3.33437680082602,-31.1388637206362));
#39883=CARTESIAN_POINT('Ctrl Pts',(5.79918477858274,3.48736933860672,-31.1304217346908));
#39884=CARTESIAN_POINT('Ctrl Pts',(5.70956342756009,3.63640166762703,-31.1221982693817));
#39885=CARTESIAN_POINT('Ctrl Pts',(5.61407463849383,3.78217460051554,-31.1139748040727));
#39886=CARTESIAN_POINT('Ctrl Pts',(5.51298232745837,3.92419607781412,-31.1057513387636));
#39887=CARTESIAN_POINT('Ctrl Pts',(5.41199195061199,4.06607435090683,-31.0975361654033));
#39888=CARTESIAN_POINT('Ctrl Pts',(5.305409507286,4.20420840997081,-31.089320992043));
#39889=CARTESIAN_POINT('Ctrl Pts',(5.19354407300965,4.33813196683853,-31.0811058186827));
#39890=CARTESIAN_POINT('Ctrl Pts',(5.08177110580615,4.47194482356577,-31.072897435919));
#39891=CARTESIAN_POINT('Ctrl Pts',(4.96472407208927,4.60155383497081,-31.0646890531553));
#39892=CARTESIAN_POINT('Ctrl Pts',(4.84275452513964,4.7265227820502,-31.0564806703916));
#39893=CARTESIAN_POINT('Ctrl Pts',(4.71618856164337,4.85620117792674,-31.0479629551158));
#39894=CARTESIAN_POINT('Ctrl Pts',(4.58432206138568,4.98088264727668,-31.03944523984));
#39895=CARTESIAN_POINT('Ctrl Pts',(4.44759350135276,5.10011774831961,-31.0309275245641));
#39896=CARTESIAN_POINT('Ctrl Pts',(4.31597847507724,5.21489355633625,-31.0227283647137));
#39897=CARTESIAN_POINT('Ctrl Pts',(4.17985876899612,5.32462273389042,-31.0145292048632));
#39898=CARTESIAN_POINT('Ctrl Pts',(4.03966251238306,5.42894241874484,-31.0063300450128));
#39899=CARTESIAN_POINT('Ctrl Pts',(3.89950189218883,5.53323558662888,-30.9981329693028));
#39900=CARTESIAN_POINT('Ctrl Pts',(3.75526707419318,5.63212178862292,-30.9899358935928));
#39901=CARTESIAN_POINT('Ctrl Pts',(3.60741812487521,5.72527933574615,-30.9817388178829));
#39902=CARTESIAN_POINT('Ctrl Pts',(3.45956971450485,5.81843654328605,-30.9735417720534));
#39903=CARTESIAN_POINT('Ctrl Pts',(3.30810750176141,5.90586494564656,-30.9653447262238));
#39904=CARTESIAN_POINT('Ctrl Pts',(3.15351944059881,5.98728687618736,-30.9571476803943));
#39905=CARTESIAN_POINT('Ctrl Pts',(3.13541736023296,5.99682128860645,-30.9561878159569));
#39906=CARTESIAN_POINT('Ctrl Pts',(3.11727244616411,6.00627339093736,-30.9552279515194));
#39907=CARTESIAN_POINT('Ctrl Pts',(3.09908550384721,6.01564277861012,-30.9542680870819));
#39908=CARTESIAN_POINT('Ctrl Pts',(3.09908550384723,6.01564277861011,-32.9539663901326));
#39909=CARTESIAN_POINT('Ctrl Pts',(2.94674704149251,6.09412315680687,-32.9459223007143));
#39910=CARTESIAN_POINT('Ctrl Pts',(2.79129257097801,6.16688148165184,-32.937878211296));
#39911=CARTESIAN_POINT('Ctrl Pts',(2.63320140856036,6.23366179239424,-32.9298341218777));
#39912=CARTESIAN_POINT('Ctrl Pts',(2.47519013293361,6.30040835764044,-32.921794097307));
#39913=CARTESIAN_POINT('Ctrl Pts',(2.31454516101582,6.36118277802486,-32.9137540727364));
#39914=CARTESIAN_POINT('Ctrl Pts',(2.15176855625465,6.41577595309513,-32.9057140481657));
#39915=CARTESIAN_POINT('Ctrl Pts',(1.9890111333849,6.47036269480628,-32.8976749710462));
#39916=CARTESIAN_POINT('Ctrl Pts',(1.82412292827275,6.51876951353359,-32.8896358939267));
#39917=CARTESIAN_POINT('Ctrl Pts',(1.65762420155657,6.56083615146834,-32.8815968168071));
#39918=CARTESIAN_POINT('Ctrl Pts',(1.49112888342494,6.60290192820918,-32.8735579042647));
#39919=CARTESIAN_POINT('Ctrl Pts',(1.32302347111279,6.63862768989094,-32.8655189917222));
#39920=CARTESIAN_POINT('Ctrl Pts',(1.15384124118038,6.66790367283086,-32.8574800791798));
#39921=CARTESIAN_POINT('Ctrl Pts',(0.984628981384295,6.69718485226085,-32.8494397397295));
#39922=CARTESIAN_POINT('Ctrl Pts',(0.814339891447124,6.72001391017923,-32.8413994002792));
#39923=CARTESIAN_POINT('Ctrl Pts',(0.643515094834652,6.73633263153772,-32.833359060829));
#39924=CARTESIAN_POINT('Ctrl Pts',(0.472626148960312,6.75265748101081,-32.825315702017));
#39925=CARTESIAN_POINT('Ctrl Pts',(0.301201467382972,6.76246709214905,-32.8172723432051));
#39926=CARTESIAN_POINT('Ctrl Pts',(0.129784770481594,6.76575530989342,-32.8092289843932));
#39927=CARTESIAN_POINT('Ctrl Pts',(-0.0418364582406628,6.76904745108968,
-32.8011760283666));
#39928=CARTESIAN_POINT('Ctrl Pts',(-0.21344930978222,6.76580265238947,-32.7931230723401));
#39929=CARTESIAN_POINT('Ctrl Pts',(-0.384511736156809,6.75606688279192,
-32.7850701163136));
#39930=CARTESIAN_POINT('Ctrl Pts',(-0.555683056889247,6.74632491563012,
-32.7770120339628));
#39931=CARTESIAN_POINT('Ctrl Pts',(-0.726302884308395,6.7300837842317,-32.7689539516119));
#39932=CARTESIAN_POINT('Ctrl Pts',(-0.895837323044223,6.70744097928867,
-32.7608958692611));
#39933=CARTESIAN_POINT('Ctrl Pts',(-1.06564251148265,6.68476201335824,-32.7528249180005));
#39934=CARTESIAN_POINT('Ctrl Pts',(-1.23435848265583,6.65566101806081,-32.7447539667399));
#39935=CARTESIAN_POINT('Ctrl Pts',(-1.40146345646603,6.6202861856713,-32.7366830154792));
#39936=CARTESIAN_POINT('Ctrl Pts',(-1.52999193641433,6.59307769910277,-32.7304752583215));
#39937=CARTESIAN_POINT('Ctrl Pts',(-1.65756762294372,6.56215871816995,-32.7242675011637));
#39938=CARTESIAN_POINT('Ctrl Pts',(-1.78396096288756,6.52761612557703,-32.718059744006));
#39939=CARTESIAN_POINT('Ctrl Pts',(-1.95364257022628,6.48124309171767,-32.7097259013133));
#39940=CARTESIAN_POINT('Ctrl Pts',(-2.12173195195283,6.4281904168494,-32.7013920586206));
#39941=CARTESIAN_POINT('Ctrl Pts',(-2.28767289072268,6.36858239681741,-32.6930582159279));
#39942=CARTESIAN_POINT('Ctrl Pts',(-2.45341824710276,6.30904463237813,-32.6847341957232));
#39943=CARTESIAN_POINT('Ctrl Pts',(-2.61701988034437,6.24296703086413,-32.6764101755184));
#39944=CARTESIAN_POINT('Ctrl Pts',(-2.77793430400726,6.17052428911999,-32.6680861553137));
#39945=CARTESIAN_POINT('Ctrl Pts',(-2.93868857309032,6.09815364804029,-32.6597704198228));
#39946=CARTESIAN_POINT('Ctrl Pts',(-3.09676064591749,6.01943063023907,-32.6514546843319));
#39947=CARTESIAN_POINT('Ctrl Pts',(-3.25162446653574,5.93457895125056,-32.6431389488411));
#39948=CARTESIAN_POINT('Ctrl Pts',(-3.40636252965612,5.84979617625006,-32.634829966161));
#39949=CARTESIAN_POINT('Ctrl Pts',(-3.55789722807418,5.75889482321709,-32.626520983481));
#39950=CARTESIAN_POINT('Ctrl Pts',(-3.70572448192878,5.66214580031578,-32.618212000801));
#39951=CARTESIAN_POINT('Ctrl Pts',(-3.85345876324445,5.56545762547912,-32.6099082438638));
#39952=CARTESIAN_POINT('Ctrl Pts',(-3.9974899566244,5.46292930009872,-32.6016044869267));
#39953=CARTESIAN_POINT('Ctrl Pts',(-4.13734030809213,5.3548766722527,-32.5933007299895));
#39954=CARTESIAN_POINT('Ctrl Pts',(-4.2771338836885,5.24686791116878,-32.5850003441775));
#39955=CARTESIAN_POINT('Ctrl Pts',(-4.41274972461563,5.13333952875915,-32.5766999583655));
#39956=CARTESIAN_POINT('Ctrl Pts',(-4.54374046386894,5.01464969833389,-32.5683995725534));
#39957=CARTESIAN_POINT('Ctrl Pts',(-4.67470358058384,4.89598489650543,-32.5601009370768));
#39958=CARTESIAN_POINT('Ctrl Pts',(-4.80104328110679,4.77216104844101,-32.5518023016001));
#39959=CARTESIAN_POINT('Ctrl Pts',(-4.92234642091017,4.6435756387242,-32.5435036661235));
#39960=CARTESIAN_POINT('Ctrl Pts',(-5.04364411596642,4.51499600062255,-32.5352054031349));
#39961=CARTESIAN_POINT('Ctrl Pts',(-5.15990546228823,4.38165547985473,-32.5269071401463));
#39962=CARTESIAN_POINT('Ctrl Pts',(-5.27075510311867,4.24398746969739,-32.5186088771578));
#39963=CARTESIAN_POINT('Ctrl Pts',(-5.38161816736721,4.10630278853197,-32.510309609285));
#39964=CARTESIAN_POINT('Ctrl Pts',(-5.48706800265771,3.96428984501167,-32.5020103414122));
#39965=CARTESIAN_POINT('Ctrl Pts',(-5.58677025902328,3.81841420918331,-32.4937110735394));
#39966=CARTESIAN_POINT('Ctrl Pts',(-5.68654252244277,3.67243614514644,-32.4854059782429));
#39967=CARTESIAN_POINT('Ctrl Pts',(-5.78055894636304,3.52259025676187,-32.4771008829464));
#39968=CARTESIAN_POINT('Ctrl Pts',(-5.86852867744744,3.36937088519162,-32.4687957876499));
#39969=CARTESIAN_POINT('Ctrl Pts',(-5.95653048687016,3.2160956418712,-32.4604876638838));
#39970=CARTESIAN_POINT('Ctrl Pts',(-6.0384810419881,3.05944476875903,-32.4521795401177));
#39971=CARTESIAN_POINT('Ctrl Pts',(-6.11413591731701,2.89993637595277,-32.4438714163516));
#39972=CARTESIAN_POINT('Ctrl Pts',(-6.18987121334135,2.74025842664641,-32.4355544610979));
#39973=CARTESIAN_POINT('Ctrl Pts',(-6.25929731614242,2.57771720629242,-32.4272375058442));
#39974=CARTESIAN_POINT('Ctrl Pts',(-6.32221791334578,2.41285093948418,-32.4189205505905));
#39975=CARTESIAN_POINT('Ctrl Pts',(-6.36858943617088,2.29134700922621,-32.412791081108));
#39976=CARTESIAN_POINT('Ctrl Pts',(-6.41142852680388,2.16858064488716,-32.4066616116255));
#39977=CARTESIAN_POINT('Ctrl Pts',(-6.4506740762854,2.04477210503751,-32.4005321421429));
#39978=CARTESIAN_POINT('Ctrl Pts',(-6.50830866478331,1.86295138036853,-32.3915306258945));
#39979=CARTESIAN_POINT('Ctrl Pts',(-6.55828335742479,1.67859318478716,-32.3825291096461));
#39980=CARTESIAN_POINT('Ctrl Pts',(-6.60039647752542,1.49233218134237,-32.3735275933976));
#39981=CARTESIAN_POINT('Ctrl Pts',(-6.64245259760231,1.30632328179281,-32.3645382606834));
#39982=CARTESIAN_POINT('Ctrl Pts',(-6.67666832357005,1.11841694940868,-32.3555489279692));
#39983=CARTESIAN_POINT('Ctrl Pts',(-6.70289203373836,0.929261741409192,
-32.346559595255));
#39984=CARTESIAN_POINT('Ctrl Pts',(-6.7290565298193,0.740533652720438,-32.3375905607796));
#39985=CARTESIAN_POINT('Ctrl Pts',(-6.74726499411421,0.550562556810063,
-32.3286215263043));
#39986=CARTESIAN_POINT('Ctrl Pts',(-6.75741703542808,0.360005568438032,
-32.3196524918289));
#39987=CARTESIAN_POINT('Ctrl Pts',(-6.76376784751614,0.240798840667619,
-32.3140417332826));
#39988=CARTESIAN_POINT('Ctrl Pts',(-6.76696687798998,0.121363075749445,
-32.3084309747363));
#39989=CARTESIAN_POINT('Ctrl Pts',(-6.76699974407546,0.00186109715245153,
-32.30282021619));
#39990=CARTESIAN_POINT('',(-6.76699995539293,0.000776989150092258,-32.6971797837746));
#39991=CARTESIAN_POINT('Ctrl Pts',(3.09908550384718,6.01564277861014,-33.3487628447403));
#39992=CARTESIAN_POINT('Ctrl Pts',(2.96644959077812,6.08397297217539,-33.3417357109953));
#39993=CARTESIAN_POINT('Ctrl Pts',(2.8316741744699,6.14785184684299,-33.3347085772502));
#39994=CARTESIAN_POINT('Ctrl Pts',(2.69509059765216,6.20715519948123,-33.3276814435052));
#39995=CARTESIAN_POINT('Ctrl Pts',(2.53103181003941,6.27838803992871,-33.3192407285271));
#39996=CARTESIAN_POINT('Ctrl Pts',(2.36402599205973,6.34316528046175,-33.310800013549));
#39997=CARTESIAN_POINT('Ctrl Pts',(2.19460924522626,6.40124825801714,-33.3023592985709));
#39998=CARTESIAN_POINT('Ctrl Pts',(2.02532055155202,6.45928733372154,-33.2939249634829));
#39999=CARTESIAN_POINT('Ctrl Pts',(1.85362487592134,6.51064212519106,-33.2854906283949));
#40000=CARTESIAN_POINT('Ctrl Pts',(1.68007781421692,6.55512223670742,-33.2770562933069));
#40001=CARTESIAN_POINT('Ctrl Pts',(1.50663527742571,6.59957555848877,-33.2686270380982));
#40002=CARTESIAN_POINT('Ctrl Pts',(1.33134389977629,6.63716237249768,-33.2601977828896));
#40003=CARTESIAN_POINT('Ctrl Pts',(1.15477432116531,6.66774214162314,-33.251768527681));
#40004=CARTESIAN_POINT('Ctrl Pts',(0.978284003443115,6.69830818369721,-33.2433430563079));
#40005=CARTESIAN_POINT('Ctrl Pts',(0.800516956786865,6.72187339571259,-33.2349175849349));
#40006=CARTESIAN_POINT('Ctrl Pts',(0.622054287099278,6.73834827416196,-33.2264921135619));
#40007=CARTESIAN_POINT('Ctrl Pts',(0.443644376154458,6.75481828215928,-33.2180691330027));
#40008=CARTESIAN_POINT('Ctrl Pts',(0.264539583932974,6.76420210609244,-33.2096461524435));
#40009=CARTESIAN_POINT('Ctrl Pts',(0.0853268156944474,6.7664620249081,-33.2012231718842));
#40010=CARTESIAN_POINT('Ctrl Pts',(-0.0938889199359123,6.76872198114334,
-33.1928000518579));
#40011=CARTESIAN_POINT('Ctrl Pts',(-0.273212301935094,6.76385778577173,
-33.1843769318316));
#40012=CARTESIAN_POINT('Ctrl Pts',(-0.452055060805209,6.75188382764399,
-33.1759538118053));
#40013=CARTESIAN_POINT('Ctrl Pts',(-0.630904004356051,6.73990945543681,
-33.1675304004934));
#40014=CARTESIAN_POINT('Ctrl Pts',(-0.80927195886621,6.72082485235693,-33.1591069891815));
#40015=CARTESIAN_POINT('Ctrl Pts',(-0.986574256654533,6.69469642598576,
-33.1506835778697));
#40016=CARTESIAN_POINT('Ctrl Pts',(-1.16390741326628,6.66856345205653,-33.1422587004936));
#40017=CARTESIAN_POINT('Ctrl Pts',(-1.34017421345398,6.63538425927048,-33.1338338231174));
#40018=CARTESIAN_POINT('Ctrl Pts',(-1.51479831322526,6.59527672431187,-33.1254089457413));
#40019=CARTESIAN_POINT('Ctrl Pts',(-1.68947716710864,6.55515661346902,-33.1169814267099));
#40020=CARTESIAN_POINT('Ctrl Pts',(-1.86251196875455,6.50810390387631,-33.1085539076785));
#40021=CARTESIAN_POINT('Ctrl Pts',(-2.03333934774553,6.45428695495558,-33.100126388647));
#40022=CARTESIAN_POINT('Ctrl Pts',(-2.2043199181278,6.40042174507499,-33.0916913121423));
#40023=CARTESIAN_POINT('Ctrl Pts',(-2.37308879208708,6.33978027561281,-33.0832562356375));
#40024=CARTESIAN_POINT('Ctrl Pts',(-2.53909938812987,6.27258027427298,-33.0748211591327));
#40025=CARTESIAN_POINT('Ctrl Pts',(-2.70519021818626,6.20534779473026,-33.0663820058999));
#40026=CARTESIAN_POINT('Ctrl Pts',(-2.86851980578215,6.13155059409251,-33.0579428526671));
#40027=CARTESIAN_POINT('Ctrl Pts',(-3.0285636768799,6.05145363157347,-33.0495036994344));
#40028=CARTESIAN_POINT('Ctrl Pts',(-3.18878540159028,5.9712676588721,-33.0410551679362));
#40029=CARTESIAN_POINT('Ctrl Pts',(-3.34571381937356,5.88476809221298,-33.0326066364382));
#40030=CARTESIAN_POINT('Ctrl Pts',(-3.49885002351674,5.79226531789911,-33.02415810494));
#40031=CARTESIAN_POINT('Ctrl Pts',(-3.5834627448222,5.74115453383082,-33.0194900171741));
#40032=CARTESIAN_POINT('Ctrl Pts',(-3.66691824116116,5.68821179022224,-33.0148219294081));
#40033=CARTESIAN_POINT('Ctrl Pts',(-3.74913639405821,5.63349494530244,-33.0101538416421));
#40034=CARTESIAN_POINT('Ctrl Pts',(-3.8942796265701,5.53690095158362,-33.0019130660453));
#40035=CARTESIAN_POINT('Ctrl Pts',(-4.03588784783809,5.43456073571528,-32.9936722904486));
#40036=CARTESIAN_POINT('Ctrl Pts',(-4.1734780613004,5.3267597910779,-32.9854315148518));
#40037=CARTESIAN_POINT('Ctrl Pts',(-4.31091587868448,5.21907824767393,-32.9771998668075));
#40038=CARTESIAN_POINT('Ctrl Pts',(-4.44434427217922,5.105948236368,-32.9689682187631));
#40039=CARTESIAN_POINT('Ctrl Pts',(-4.57330782221945,4.98769932566373,-32.9607365707188));
#40040=CARTESIAN_POINT('Ctrl Pts',(-4.70215151365581,4.86956031538746,-32.9525125731605));
#40041=CARTESIAN_POINT('Ctrl Pts',(-4.82653836504406,4.74631211946352,-32.9442885756022));
#40042=CARTESIAN_POINT('Ctrl Pts',(-4.94604469392578,4.61832554998981,-32.9360645780439));
#40043=CARTESIAN_POINT('Ctrl Pts',(-5.06544543850151,4.4904520571476,-32.9278478464194));
#40044=CARTESIAN_POINT('Ctrl Pts',(-5.17997401287459,4.3578487936894,-32.9196311147949));
#40045=CARTESIAN_POINT('Ctrl Pts',(-5.28924248288343,4.22092441975229,-32.9114143831704));
#40046=CARTESIAN_POINT('Ctrl Pts',(-5.39845497060967,4.08407019724126,-32.9032018612817));
#40047=CARTESIAN_POINT('Ctrl Pts',(-5.50241249986528,3.94289955080353,-32.894989339393));
#40048=CARTESIAN_POINT('Ctrl Pts',(-5.60076617008913,3.79785561968661,-32.8867768175043));
#40049=CARTESIAN_POINT('Ctrl Pts',(-5.69908695037244,3.65286019195811,-32.8785670419225));
#40050=CARTESIAN_POINT('Ctrl Pts',(-5.79180740530984,3.50399435397829,-32.8703572663407));
#40051=CARTESIAN_POINT('Ctrl Pts',(-5.8786208305718,3.35173181062675,-32.8621474907588));
#40052=CARTESIAN_POINT('Ctrl Pts',(-5.91653867929808,3.28522748749861,-32.8585616740761));
#40053=CARTESIAN_POINT('Ctrl Pts',(-5.95333019236971,3.21807554308386,-32.8549758573934));
#40054=CARTESIAN_POINT('Ctrl Pts',(-5.98897247047381,3.15031708688297,-32.8513900407106));
#40055=CARTESIAN_POINT('Ctrl Pts',(-6.07640315339711,2.98410526164082,-32.8425940148087));
#40056=CARTESIAN_POINT('Ctrl Pts',(-6.15682981791816,2.81440555629455,-32.8337979889067));
#40057=CARTESIAN_POINT('Ctrl Pts',(-6.23001551085722,2.6418167488451,-32.8250019630047));
#40058=CARTESIAN_POINT('Ctrl Pts',(-6.30332443844021,2.46893732557474,-32.8161911258046));
#40059=CARTESIAN_POINT('Ctrl Pts',(-6.36936792808263,2.29315932964415,-32.8073802886045));
#40060=CARTESIAN_POINT('Ctrl Pts',(-6.42795827965447,2.11509842679285,-32.7985694514043));
#40061=CARTESIAN_POINT('Ctrl Pts',(-6.48670226317345,1.93657062380388,-32.7897355109792));
#40062=CARTESIAN_POINT('Ctrl Pts',(-6.53795392300957,1.75574819589847,-32.7809015705541));
#40063=CARTESIAN_POINT('Ctrl Pts',(-6.58157557974711,1.57326154471419,-32.7720676301289));
#40064=CARTESIAN_POINT('Ctrl Pts',(-6.62525363021519,1.39053897624012,-32.7632222692559));
#40065=CARTESIAN_POINT('Ctrl Pts',(-6.6612819206485,1.20614815230693,-32.754376908383));
#40066=CARTESIAN_POINT('Ctrl Pts',(-6.68957426973306,1.0207277255593,-32.74553154751));
#40067=CARTESIAN_POINT('Ctrl Pts',(-6.71792717479372,0.834910431273443,
-32.7366672543292));
#40068=CARTESIAN_POINT('Ctrl Pts',(-6.73851098454875,0.648059395695866,
-32.7278029611484));
#40069=CARTESIAN_POINT('Ctrl Pts',(-6.75129134058409,0.460819090917759,
-32.7189386679676));
#40070=CARTESIAN_POINT('Ctrl Pts',(-6.76174851149789,0.307614918545673,
-32.7116857065818));
#40071=CARTESIAN_POINT('Ctrl Pts',(-6.76698234500998,0.154150231762921,
-32.7044327451959));
#40072=CARTESIAN_POINT('Ctrl Pts',(-6.76699995539284,0.000776989901219398,
-32.6971797838101));
#40073=CARTESIAN_POINT('Ctrl Pts',(-6.76699995539293,0.000776989150042673,
-32.6971797837746));
#40074=CARTESIAN_POINT('Ctrl Pts',(-6.76700364076461,-0.0313198683675472,
-32.695661935776));
#40075=CARTESIAN_POINT('Ctrl Pts',(-6.76677896688004,-0.0634170283982404,
-32.6941440877775));
#40076=CARTESIAN_POINT('Ctrl Pts',(-6.76632591716142,-0.0955122125681283,
-32.692626239779));
#40077=CARTESIAN_POINT('Ctrl Pts',(-6.76387121201341,-0.269409713373156,
-32.6844022653615));
#40078=CARTESIAN_POINT('Ctrl Pts',(-6.75470508379871,-0.44344307132773,
-32.6761782909439));
#40079=CARTESIAN_POINT('Ctrl Pts',(-6.73880799304889,-0.617054157121077,
-32.6679543165263));
#40080=CARTESIAN_POINT('Ctrl Pts',(-6.72292769116931,-0.790481892763339,
-32.6597390274237));
#40081=CARTESIAN_POINT('Ctrl Pts',(-6.70033061469403,-0.963487890154671,
-32.651523738321));
#40082=CARTESIAN_POINT('Ctrl Pts',(-6.67104922470096,-1.13551364660086,
-32.6433084492184));
#40083=CARTESIAN_POINT('Ctrl Pts',(-6.64179288547393,-1.30739223185811,
-32.6351001884462));
#40084=CARTESIAN_POINT('Ctrl Pts',(-6.60586368163906,-1.47829189483929,
-32.626891927674));
#40085=CARTESIAN_POINT('Ctrl Pts',(-6.56334590791908,-1.6476587914377,-32.6186836669018));
#40086=CARTESIAN_POINT('Ctrl Pts',(-6.52085598320365,-1.81691475326548,
-32.6104807825139));
#40087=CARTESIAN_POINT('Ctrl Pts',(-6.47178617161156,-1.98463960192755,
-32.6022778981261));
#40088=CARTESIAN_POINT('Ctrl Pts',(-6.41627193933049,-2.15028914347818,
-32.5940750137382));
#40089=CARTESIAN_POINT('Ctrl Pts',(-6.36078293916598,-2.31586339463268,
-32.585875857694));
#40090=CARTESIAN_POINT('Ctrl Pts',(-6.29885546754327,-2.47936387858849,
-32.5776767016497));
#40091=CARTESIAN_POINT('Ctrl Pts',(-6.23067501123257,-2.64026095384566,
-32.5694775456055));
#40092=CARTESIAN_POINT('Ctrl Pts',(-6.1625004849638,-2.80114403496942,-32.5612791026885));
#40093=CARTESIAN_POINT('Ctrl Pts',(-6.0880741892412,-2.9594238251642,-32.5530806597715));
#40094=CARTESIAN_POINT('Ctrl Pts',(-6.00763012443662,-3.11458974633285,
-32.5448822168545));
#40095=CARTESIAN_POINT('Ctrl Pts',(-5.92718686075979,-3.2697541222324,-32.5366838555843));
#40096=CARTESIAN_POINT('Ctrl Pts',(-5.8407261115259,-3.42180437193956,-32.528485494314));
#40097=CARTESIAN_POINT('Ctrl Pts',(-5.74852824819261,-3.57025376965442,
-32.5202871330438));
#40098=CARTESIAN_POINT('Ctrl Pts',(-5.6563145546388,-3.71872865588514,-32.5120873641285));
#40099=CARTESIAN_POINT('Ctrl Pts',(-5.55836197372408,-3.86360115364792,
-32.5038875952133));
#40100=CARTESIAN_POINT('Ctrl Pts',(-5.45499470992903,-4.00441278025209,
-32.495687826298));
#40101=CARTESIAN_POINT('Ctrl Pts',(-5.35159092054627,-4.14527416368671,
-32.4874851599337));
#40102=CARTESIAN_POINT('Ctrl Pts',(-5.24276884905177,-4.28207152856614,
-32.4792824935694));
#40103=CARTESIAN_POINT('Ctrl Pts',(-5.12889356935204,-4.41437875065782,
-32.4710798272051));
#40104=CARTESIAN_POINT('Ctrl Pts',(-5.01488895579823,-4.54683624068299,
-32.4628678446621));
#40105=CARTESIAN_POINT('Ctrl Pts',(-4.89581990250523,-4.67479312761385,
-32.454655862119));
#40106=CARTESIAN_POINT('Ctrl Pts',(-4.77208972971953,-4.79785875276725,
-32.446443879576));
#40107=CARTESIAN_POINT('Ctrl Pts',(-4.64828657920569,-4.92099696368963,
-32.4382270534947));
#40108=CARTESIAN_POINT('Ctrl Pts',(-4.51981709256398,-5.0392379196295,-32.4300102274134));
#40109=CARTESIAN_POINT('Ctrl Pts',(-4.38711829001342,-5.15223078961237,
-32.4217934013322));
#40110=CARTESIAN_POINT('Ctrl Pts',(-4.254214846744,-5.26539791092002,-32.4135639037183));
#40111=CARTESIAN_POINT('Ctrl Pts',(-4.11706933552169,-5.3733005512914,-32.4053344061045));
#40112=CARTESIAN_POINT('Ctrl Pts',(-3.97614948353633,-5.47563003539993,
-32.3971049084906));
#40113=CARTESIAN_POINT('Ctrl Pts',(-3.85053953188731,-5.56684217740868,
-32.3897694849658));
#40114=CARTESIAN_POINT('Ctrl Pts',(-3.72193134591881,-5.65362687499,-32.3824340614409));
#40115=CARTESIAN_POINT('Ctrl Pts',(-3.59067229527631,-5.7357964981278,-32.3750986379161));
#40116=CARTESIAN_POINT('Ctrl Pts',(-3.44625326412708,-5.82620441518474,
-32.3670277677297));
#40117=CARTESIAN_POINT('Ctrl Pts',(-3.29815374402904,-5.91131939795726,
-32.3589568975433));
#40118=CARTESIAN_POINT('Ctrl Pts',(-3.14680608435033,-5.99081801321787,
-32.3508860273568));
#40119=CARTESIAN_POINT('Ctrl Pts',(-2.9956467650705,-6.07021769863087,-32.3428252007411));
#40120=CARTESIAN_POINT('Ctrl Pts',(-2.84124767496596,-6.14401475190585,
-32.3347643741253));
#40121=CARTESIAN_POINT('Ctrl Pts',(-2.68407132278089,-6.21192805288545,
-32.3267035475095));
#40122=CARTESIAN_POINT('Ctrl Pts',(-2.52705609797334,-6.27977173339141,
-32.3186509843496));
#40123=CARTESIAN_POINT('Ctrl Pts',(-2.36726961640093,-6.34174351812268,
-32.3105984211897));
#40124=CARTESIAN_POINT('Ctrl Pts',(-2.20520016739459,-6.39760746074053,
-32.3025458580298));
#40125=CARTESIAN_POINT('Ctrl Pts',(-2.04326137466428,-6.45342636726582,
-32.2944997866419));
#40126=CARTESIAN_POINT('Ctrl Pts',(-1.87904362853917,-6.50314711120076,
-32.2864537152541));
#40127=CARTESIAN_POINT('Ctrl Pts',(-1.71305634720513,-6.54658131785593,
-32.2784076438662));
#40128=CARTESIAN_POINT('Ctrl Pts',(-1.54716657277489,-6.58999000969468,
-32.2703662990303));
#40129=CARTESIAN_POINT('Ctrl Pts',(-1.37950969241191,-6.62711942168255,
-32.2623249541944));
#40130=CARTESIAN_POINT('Ctrl Pts',(-1.21061137812345,-6.65783065954355,
-32.2542836093585));
#40131=CARTESIAN_POINT('Ctrl Pts',(-1.03845722403718,-6.68913391557174,
-32.2460872521374));
#40132=CARTESIAN_POINT('Ctrl Pts',(-0.865013660771462,-6.71376890035964,
-32.2378908949164));
#40133=CARTESIAN_POINT('Ctrl Pts',(-0.690849936269294,-6.73164284298838,
-32.2296945376953));
#40134=CARTESIAN_POINT('Ctrl Pts',(-0.520034372208636,-6.74917317314665,
-32.2216557489868));
#40135=CARTESIAN_POINT('Ctrl Pts',(-0.348526471807505,-6.76020003690927,
-32.2136169602783));
#40136=CARTESIAN_POINT('Ctrl Pts',(-0.176869554794799,-6.76468817910972,
-32.2055781715698));
#40137=CARTESIAN_POINT('Ctrl Pts',(-0.00519426893594305,-6.76917680158205,
-32.197538522638));
#40138=CARTESIAN_POINT('Ctrl Pts',(0.166629691918991,-6.76712529941602,
-32.1894988737063));
#40139=CARTESIAN_POINT('Ctrl Pts',(0.338058236840963,-6.7585505567765,-32.1814592247745));
#40140=CARTESIAN_POINT('Ctrl Pts',(0.509539069676452,-6.74997319873007,
-32.1734171236463));
#40141=CARTESIAN_POINT('Ctrl Pts',(0.680623873718714,-6.73486865842038,
-32.1653750225181));
#40142=CARTESIAN_POINT('Ctrl Pts',(0.850773058213182,-6.71330575822512,
-32.1573329213899));
#40143=CARTESIAN_POINT('Ctrl Pts',(1.02666410918672,-6.69101519486657,-32.1490194309452));
#40144=CARTESIAN_POINT('Ctrl Pts',(1.20155485529246,-6.66182281114754,-32.1407059405004));
#40145=CARTESIAN_POINT('Ctrl Pts',(1.37486108899908,-6.6258619051378,-32.1323924500557));
#40146=CARTESIAN_POINT('Ctrl Pts',(1.54280516780542,-6.59101364201605,-32.1243361818849));
#40147=CARTESIAN_POINT('Ctrl Pts',(1.70926098515278,-6.54980961983952,-32.1162799137142));
#40148=CARTESIAN_POINT('Ctrl Pts',(1.87371326938176,-6.50242167074258,-32.1082236455434));
#40149=CARTESIAN_POINT('Ctrl Pts',(2.04604155580157,-6.45276420260152,-32.0997815439617));
#40150=CARTESIAN_POINT('Ctrl Pts',(2.21616922062781,-6.39631606958526,-32.0913394423799));
#40151=CARTESIAN_POINT('Ctrl Pts',(2.38352855884928,-6.33333092528331,-32.0828973407982));
#40152=CARTESIAN_POINT('Ctrl Pts',(2.55088789707078,-6.27034578098134,-32.0744552392165));
#40153=CARTESIAN_POINT('Ctrl Pts',(2.71547851777711,-6.20082388437573,-32.0660131376348));
#40154=CARTESIAN_POINT('Ctrl Pts',(2.87676452164858,-6.12507264340465,-32.057571036053));
#40155=CARTESIAN_POINT('Ctrl Pts',(3.03598224389287,-6.05029281282366,-32.0492371933604));
#40156=CARTESIAN_POINT('Ctrl Pts',(3.19248603147525,-5.96920526117568,-32.0409033506677));
#40157=CARTESIAN_POINT('Ctrl Pts',(3.34574921568815,-5.88202781238938,-32.032569507975));
#40158=CARTESIAN_POINT('Ctrl Pts',(3.49883175984881,-5.79495311325547,-32.0242454877702));
#40159=CARTESIAN_POINT('Ctrl Pts',(3.64868100957273,-5.70180298615775,-32.0159214675655));
#40160=CARTESIAN_POINT('Ctrl Pts',(3.79479148025796,-5.60284272680945,-32.0075974473608));
#40161=CARTESIAN_POINT('Ctrl Pts',(3.94075653041124,-5.50398096042671,-31.9992817118699));
#40162=CARTESIAN_POINT('Ctrl Pts',(4.08298992903231,-5.3993207767074,-31.9909659763791));
#40163=CARTESIAN_POINT('Ctrl Pts',(4.22101176860237,-5.28917277552174,-31.9826502408882));
#40164=CARTESIAN_POINT('Ctrl Pts',(4.35892152724194,-5.17911422025639,-31.9743412582082));
#40165=CARTESIAN_POINT('Ctrl Pts',(4.4926262708117,-5.06357694335015,-31.9660322755281));
#40166=CARTESIAN_POINT('Ctrl Pts',(4.62167583407019,-4.94291427042505,-31.9577232928481));
#40167=CARTESIAN_POINT('Ctrl Pts',(4.75064423458499,-4.82232748550259,-31.9494195359109));
#40168=CARTESIAN_POINT('Ctrl Pts',(4.87496303615949,-4.69662196554811,-31.9411157789737));
#40169=CARTESIAN_POINT('Ctrl Pts',(4.99421571495734,-4.56619079676629,-31.9328120220365));
#40170=CARTESIAN_POINT('Ctrl Pts',(5.11341998004209,-4.43581257989507,-31.9245116362245));
#40171=CARTESIAN_POINT('Ctrl Pts',(5.22756198620456,-4.30071279324783,-31.9162112504125));
#40172=CARTESIAN_POINT('Ctrl Pts',(5.33626240364882,-4.16132101133813,-31.9079108646005));
#40173=CARTESIAN_POINT('Ctrl Pts',(5.4449398990034,-4.02195862352828,-31.8996122291238));
#40174=CARTESIAN_POINT('Ctrl Pts',(5.5481778779696,-3.87830631767617,-31.8913135936472));
#40175=CARTESIAN_POINT('Ctrl Pts',(5.64563746672557,-3.73082652964521,-31.8830149581705));
#40176=CARTESIAN_POINT('Ctrl Pts',(5.7430926809631,-3.58335336131232,-31.874716695182));
#40177=CARTESIAN_POINT('Ctrl Pts',(5.83476983025493,-3.43205334338494,-31.8664184321934));
#40178=CARTESIAN_POINT('Ctrl Pts',(5.9203734258444,-3.2774178095805,-31.8581201692048));
#40179=CARTESIAN_POINT('Ctrl Pts',(6.00598738766399,-3.12276355007282,-31.849820901332));
#40180=CARTESIAN_POINT('Ctrl Pts',(6.08552616234302,-2.9647732743823,-31.8415216334592));
#40181=CARTESIAN_POINT('Ctrl Pts',(6.15874017766571,-2.80396298549145,-31.8332223655864));
#40182=CARTESIAN_POINT('Ctrl Pts',(6.23200560102765,-2.64303978185873,-31.8249172702899));
#40183=CARTESIAN_POINT('Ctrl Pts',(6.29893724685141,-2.47929292533969,-31.8166121749934));
#40184=CARTESIAN_POINT('Ctrl Pts',(6.35933332849873,-2.31325930605396,-31.8083070796969));
#40185=CARTESIAN_POINT('Ctrl Pts',(6.41975143369796,-2.14716514227706,-31.7999989559308));
#40186=CARTESIAN_POINT('Ctrl Pts',(6.47362911274582,-1.9787828830234,-31.7916908321647));
#40187=CARTESIAN_POINT('Ctrl Pts',(6.52081439472444,-1.80866487486061,-31.7833827083986));
#40188=CARTESIAN_POINT('Ctrl Pts',(6.56804983438527,-1.63836603223771,-31.7750657531449));
#40189=CARTESIAN_POINT('Ctrl Pts',(6.60857857753647,-1.46632809152995,-31.7667487978912));
#40190=CARTESIAN_POINT('Ctrl Pts',(6.64229950269269,-1.29311496647761,-31.7584318426375));
#40191=CARTESIAN_POINT('Ctrl Pts',(6.66715131148143,-1.16545952868767,-31.752302373155));
#40192=CARTESIAN_POINT('Ctrl Pts',(6.68830654293802,-1.03716602112991,-31.7461729036724));
#40193=CARTESIAN_POINT('Ctrl Pts',(6.7057427584848,-0.908461918315057,-31.7400434341898));
#40194=CARTESIAN_POINT('Ctrl Pts',(6.72978299038332,-0.731010769603445,
-31.7315924106647));
#40195=CARTESIAN_POINT('Ctrl Pts',(6.74679555423204,-0.552454660540933,
-31.7231413871395));
#40196=CARTESIAN_POINT('Ctrl Pts',(6.75669149813917,-0.37337514509378,-31.7146903636143));
#40197=CARTESIAN_POINT('Ctrl Pts',(6.76657872896178,-0.19445330383817,-31.7062467809642));
#40198=CARTESIAN_POINT('Ctrl Pts',(6.76936181090752,-0.0150093041905303,
-31.6978031983141));
#40199=CARTESIAN_POINT('Ctrl Pts',(6.76500345896609,0.164369097390344,-31.689359615664));
#40200=CARTESIAN_POINT('Ctrl Pts',(6.76064835195343,0.343613946164104,-31.6809223195242));
#40201=CARTESIAN_POINT('Ctrl Pts',(6.74916241830657,0.522792963925201,-31.6724850233844));
#40202=CARTESIAN_POINT('Ctrl Pts',(6.73056042233343,0.701316905057112,-31.6640477272445));
#40203=CARTESIAN_POINT('Ctrl Pts',(6.71197169746612,0.879713482968431,-31.6556164504722));
#40204=CARTESIAN_POINT('Ctrl Pts',(6.68627707100798,1.05745558755062,-31.6471851736999));
#40205=CARTESIAN_POINT('Ctrl Pts',(6.65354327729324,1.23395739682776,-31.6387538969276));
#40206=CARTESIAN_POINT('Ctrl Pts',(6.62082351446716,1.41038355104167,-31.6303262341056));
#40207=CARTESIAN_POINT('Ctrl Pts',(6.58107065972707,1.58557014445998,-31.6218985712836));
#40208=CARTESIAN_POINT('Ctrl Pts',(6.5344029435084,1.75893921778688,-31.6134709084617));
#40209=CARTESIAN_POINT('Ctrl Pts',(6.48774959345892,1.93225492125471,-31.6050458400077));
#40210=CARTESIAN_POINT('Ctrl Pts',(6.43418571309681,2.10375390070893,-31.5966207715538));
#40211=CARTESIAN_POINT('Ctrl Pts',(6.3738801113642,2.27287072354674,-31.5881957030998));
#40212=CARTESIAN_POINT('Ctrl Pts',(6.35737865282271,2.31914626280926,-31.585890346486));
#40213=CARTESIAN_POINT('Ctrl Pts',(6.34037270536527,2.3652435259633,-31.5835849898723));
#40214=CARTESIAN_POINT('Ctrl Pts',(6.32286637598616,2.41115113409002,-31.5812796332585));
#40215=CARTESIAN_POINT('Ctrl Pts',(6.25741582871609,2.58278494782026,-31.572660644734));
#40216=CARTESIAN_POINT('Ctrl Pts',(6.18499657830533,2.75168975055454,-31.5640416562095));
#40217=CARTESIAN_POINT('Ctrl Pts',(6.10586728046743,2.91730590670867,-31.555422667685));
#40218=CARTESIAN_POINT('Ctrl Pts',(6.0266905771185,3.08302128172017,-31.5467985156172));
#40219=CARTESIAN_POINT('Ctrl Pts',(5.94079593493681,3.24544380381087,-31.5381743635494));
#40220=CARTESIAN_POINT('Ctrl Pts',(5.84848822186665,3.40403797256833,-31.5295502114816));
#40221=CARTESIAN_POINT('Ctrl Pts',(5.75301894479092,3.56806403427124,-31.5206306798854));
#40222=CARTESIAN_POINT('Ctrl Pts',(5.65068970730467,3.72799455010796,-31.5117111482892));
#40223=CARTESIAN_POINT('Ctrl Pts',(5.54188643122727,3.88326972838342,-31.5027916166929));
#40224=CARTESIAN_POINT('Ctrl Pts',(5.43649031272387,4.03368248873555,-31.4941513988337));
#40225=CARTESIAN_POINT('Ctrl Pts',(5.32501970799295,4.17972684724951,-31.4855111809744));
#40226=CARTESIAN_POINT('Ctrl Pts',(5.2078667173747,4.32092736042402,-31.4768709631152));
#40227=CARTESIAN_POINT('Ctrl Pts',(5.08503289090163,4.46897479174999,-31.4678117746505));
#40228=CARTESIAN_POINT('Ctrl Pts',(4.95595215179736,4.61169664779443,-31.4587525861858));
#40229=CARTESIAN_POINT('Ctrl Pts',(4.82112061059534,4.74858769089219,-31.4496933977211));
#40230=CARTESIAN_POINT('Ctrl Pts',(4.68628906939334,4.88547873398993,-31.4406342092564));
#40231=CARTESIAN_POINT('Ctrl Pts',(4.54570702855292,5.01653872745792,-31.4315750207917));
#40232=CARTESIAN_POINT('Ctrl Pts',(4.39991149110873,5.14130993720563,-31.422515832327));
#40233=CARTESIAN_POINT('Ctrl Pts',(4.25436304851726,5.26586968421424,-31.4134719974107));
#40234=CARTESIAN_POINT('Ctrl Pts',(4.10348522547124,5.38427734437918,-31.4044281624944));
#40235=CARTESIAN_POINT('Ctrl Pts',(3.94779719257886,5.49610646969894,-31.3953843275781));
#40236=CARTESIAN_POINT('Ctrl Pts',(3.79229985677368,5.6077986192469,-31.3863515701541));
#40237=CARTESIAN_POINT('Ctrl Pts',(3.63200427101384,5.71292818765523,-31.37731881273));
#40238=CARTESIAN_POINT('Ctrl Pts',(3.46746036859561,5.81111070211357,-31.368286055306));
#40239=CARTESIAN_POINT('Ctrl Pts',(3.34687412860517,5.88306390169944,-31.3616663857922));
#40240=CARTESIAN_POINT('Ctrl Pts',(3.2240069292606,5.95128686638822,-31.3550467162785));
#40241=CARTESIAN_POINT('Ctrl Pts',(3.0990855038472,6.01564277861013,-31.3484270467647));
#40242=CARTESIAN_POINT('Origin',(0.,0.,-63.6971797838103));
#40243=CARTESIAN_POINT('',(3.09908550384723,6.01564277861011,-28.9543744409077));
#40244=CARTESIAN_POINT('',(3.09908550384723,6.01564277861011,-29.348603209574));
#40245=CARTESIAN_POINT('',(3.09908550384721,6.01564277861012,-63.6971797838103));
#40246=CARTESIAN_POINT('',(-6.76699999859312,0.000137987943152793,-30.3028202161642));
#40247=CARTESIAN_POINT('Ctrl Pts',(-6.76699999859312,0.000137987943145954,
-30.3028202161641));
#40248=CARTESIAN_POINT('Ctrl Pts',(-6.76700388479958,-0.190443583885455,
-30.2938915872868));
#40249=CARTESIAN_POINT('Ctrl Pts',(-6.75895235621057,-0.380837284568577,
-30.2849629584095));
#40250=CARTESIAN_POINT('Ctrl Pts',(-6.74291859928137,-0.570383873777514,
-30.2760343295323));
#40251=CARTESIAN_POINT('Ctrl Pts',(-6.72683535805985,-0.760515452447654,
-30.2670781446128));
#40252=CARTESIAN_POINT('Ctrl Pts',(-6.70272060340288,-0.949794440188979,
-30.2581219596934));
#40253=CARTESIAN_POINT('Ctrl Pts',(-6.67069935526168,-1.13756718997665,
-30.249165774774));
#40254=CARTESIAN_POINT('Ctrl Pts',(-6.63863002257894,-1.32562190774221,
-30.2401961408459));
#40255=CARTESIAN_POINT('Ctrl Pts',(-6.59863052172635,-1.51216562698233,
-30.2312265069177));
#40256=CARTESIAN_POINT('Ctrl Pts',(-6.55087651698734,-1.69655706039727,
-30.2222568729896));
#40257=CARTESIAN_POINT('Ctrl Pts',(-6.50301856834516,-1.88134985000013,
-30.2132677152798));
#40258=CARTESIAN_POINT('Ctrl Pts',(-6.44737241789432,-2.06398074481492,
-30.20427855757));
#40259=CARTESIAN_POINT('Ctrl Pts',(-6.38416375623423,-2.24382310657175,
-30.1952893998603));
#40260=CARTESIAN_POINT('Ctrl Pts',(-6.34326185575947,-2.36019789111124,
-30.1894725762741));
#40261=CARTESIAN_POINT('Ctrl Pts',(-6.29919429622271,-2.47540542601184,
-30.1836557526879));
#40262=CARTESIAN_POINT('Ctrl Pts',(-6.25203279118684,-2.58928078390979,
-30.1778389291016));
#40263=CARTESIAN_POINT('Ctrl Pts',(-6.18351378203424,-2.75472560345341,
-30.1693879055764));
#40264=CARTESIAN_POINT('Ctrl Pts',(-6.10836566388483,-2.91758895645562,
-30.1609368820512));
#40265=CARTESIAN_POINT('Ctrl Pts',(-6.0268042065883,-3.07732352141428,-30.152485858526));
#40266=CARTESIAN_POINT('Ctrl Pts',(-5.94531456173106,-3.23691744483554,
-30.1440422758759));
#40267=CARTESIAN_POINT('Ctrl Pts',(-5.8574229828226,-3.39338777720544,-30.1355986932257));
#40268=CARTESIAN_POINT('Ctrl Pts',(-5.76339300972036,-3.54620783591522,
-30.1271551105756));
#40269=CARTESIAN_POINT('Ctrl Pts',(-5.66943304486209,-3.69891411533101,
-30.1187178144358));
#40270=CARTESIAN_POINT('Ctrl Pts',(-5.56934396948447,-3.84797525737609,
-30.1102805182959));
#40271=CARTESIAN_POINT('Ctrl Pts',(-5.46343505218162,-3.99288948389424,
-30.101843222156));
#40272=CARTESIAN_POINT('Ctrl Pts',(-5.35760169281609,-4.13770032516097,
-30.0934119453837));
#40273=CARTESIAN_POINT('Ctrl Pts',(-5.24595696853239,-4.27836988515905,
-30.0849806686113));
#40274=CARTESIAN_POINT('Ctrl Pts',(-5.12885333600842,-4.41442549577126,
-30.076549391839));
#40275=CARTESIAN_POINT('Ctrl Pts',(-5.01179989834027,-4.55042278802381,
-30.068121729017));
#40276=CARTESIAN_POINT('Ctrl Pts',(-4.88929243294571,-4.68180982275689,
-30.0596940661951));
#40277=CARTESIAN_POINT('Ctrl Pts',(-4.76172394130033,-4.80814663949086,
-30.0512664033731));
#40278=CARTESIAN_POINT('Ctrl Pts',(-4.63419472028228,-4.93444456475575,
-30.0428413349191));
#40279=CARTESIAN_POINT('Ctrl Pts',(-4.50160781528299,-5.05569513941955,
-30.0344162664651));
#40280=CARTESIAN_POINT('Ctrl Pts',(-4.36439363267744,-5.17149467939827,
-30.0259911980111));
#40281=CARTESIAN_POINT('Ctrl Pts',(-4.32684763230044,-5.20318097806753,
-30.0236858413975));
#40282=CARTESIAN_POINT('Ctrl Pts',(-4.28895537736297,-5.23445935613614,
-30.0213804847839));
#40283=CARTESIAN_POINT('Ctrl Pts',(-4.25072614289869,-5.26532204694809,
-30.0190751281703));
#40284=CARTESIAN_POINT('Ctrl Pts',(-4.10779930407347,-5.38070774318834,
-30.0104561396458));
#40285=CARTESIAN_POINT('Ctrl Pts',(-3.96022357502899,-5.49022844631624,
-30.0018371511213));
#40286=CARTESIAN_POINT('Ctrl Pts',(-3.80850408783043,-5.59353069295047,
-29.9932181625969));
#40287=CARTESIAN_POINT('Ctrl Pts',(-3.65669370711997,-5.69689482684885,
-29.9845940105291));
#40288=CARTESIAN_POINT('Ctrl Pts',(-3.50073486539035,-5.79403289829253,
-29.9759698584614));
#40289=CARTESIAN_POINT('Ctrl Pts',(-3.34116048499428,-5.88463555485918,
-29.9673457063936));
#40290=CARTESIAN_POINT('Ctrl Pts',(-3.17612063913872,-5.97834137678842,
-29.9584261747974));
#40291=CARTESIAN_POINT('Ctrl Pts',(-3.0072135185948,-6.06505600859998,-29.9495066432011));
#40292=CARTESIAN_POINT('Ctrl Pts',(-2.8350543133621,-6.1444898926019,-29.9405871116049));
#40293=CARTESIAN_POINT('Ctrl Pts',(-2.66828624671713,-6.22143631694905,
-29.9319468937456));
#40294=CARTESIAN_POINT('Ctrl Pts',(-2.49846698929844,-6.2915510100068,-29.9233066758864));
#40295=CARTESIAN_POINT('Ctrl Pts',(-2.32617462618558,-6.35462041419394,
-29.9146664580271));
#40296=CARTESIAN_POINT('Ctrl Pts',(-2.14552767793693,-6.42074810081001,
-29.9056072695623));
#40297=CARTESIAN_POINT('Ctrl Pts',(-1.96216218528791,-6.47913013149219,
-29.8965480810976));
#40298=CARTESIAN_POINT('Ctrl Pts',(-1.77676110815794,-6.52957953964399,
-29.8874888926328));
#40299=CARTESIAN_POINT('Ctrl Pts',(-1.59136003102797,-6.58002894779578,
-29.8784297041681));
#40300=CARTESIAN_POINT('Ctrl Pts',(-1.40392374989238,-6.62254568108135,
-29.8693705157033));
#40301=CARTESIAN_POINT('Ctrl Pts',(-1.21514665878078,-6.65700440120434,
-29.8603113272386));
#40302=CARTESIAN_POINT('Ctrl Pts',(-1.02669661073589,-6.69140342401216,
-29.8512678331823));
#40303=CARTESIAN_POINT('Ctrl Pts',(-0.836736937202911,-6.71780485300529,
-29.842224339126));
#40304=CARTESIAN_POINT('Ctrl Pts',(-0.645930803590734,-6.73610142418986,
-29.8331808450697));
#40305=CARTESIAN_POINT('Ctrl Pts',(-0.455299199650862,-6.75438125956771,
-29.8241456230643));
#40306=CARTESIAN_POINT('Ctrl Pts',(-0.263822918229505,-6.76457101547801,
-29.815110401059));
#40307=CARTESIAN_POINT('Ctrl Pts',(-0.0721712101117952,-6.76661512991769,
-29.8060751790536));
#40308=CARTESIAN_POINT('Ctrl Pts',(0.11914284941797,-6.76865564307273,-29.7970558751425));
#40309=CARTESIAN_POINT('Ctrl Pts',(0.310631480718239,-6.76257916907742,
-29.7880365712314));
#40310=CARTESIAN_POINT('Ctrl Pts',(0.501624621187765,-6.7483821571854,-29.7790172673203));
#40311=CARTESIAN_POINT('Ctrl Pts',(0.692378147423253,-6.73420295643634,
-29.7700092787558));
#40312=CARTESIAN_POINT('Ctrl Pts',(0.882637186657034,-6.71192356669804,
-29.7610012901914));
#40313=CARTESIAN_POINT('Ctrl Pts',(1.07173342245696,-6.68159236044737,-29.7519933016269));
#40314=CARTESIAN_POINT('Ctrl Pts',(1.2604025777839,-6.65132965828859,-29.7430056579202));
#40315=CARTESIAN_POINT('Ctrl Pts',(1.44791393722817,-6.61305147679858,-29.7340180142136));
#40316=CARTESIAN_POINT('Ctrl Pts',(1.63360650694425,-6.56685760318201,-29.7250303705069));
#40317=CARTESIAN_POINT('Ctrl Pts',(1.79533186477981,-6.5266259409681,-29.7172027557736));
#40318=CARTESIAN_POINT('Ctrl Pts',(1.95567757885048,-6.48039085641162,-29.7093751410404));
#40319=CARTESIAN_POINT('Ctrl Pts',(2.11421086436455,-6.42825026122995,-29.7015475263071));
#40320=CARTESIAN_POINT('Ctrl Pts',(2.27872981949548,-6.37414101715936,-29.6934243678618));
#40321=CARTESIAN_POINT('Ctrl Pts',(2.44122283603883,-6.3136944983611,-29.6853012094166));
#40322=CARTESIAN_POINT('Ctrl Pts',(2.6011690606084,-6.24709600679657,-29.6771780509713));
#40323=CARTESIAN_POINT('Ctrl Pts',(2.76110400813265,-6.18050221077398,-29.6690554652512));
#40324=CARTESIAN_POINT('Ctrl Pts',(2.91849218345026,-6.10775744666156,-29.660932879531));
#40325=CARTESIAN_POINT('Ctrl Pts',(3.07283243885395,-6.02909527232129,-29.6528102938109));
#40326=CARTESIAN_POINT('Ctrl Pts',(3.22719123982684,-5.95042364591167,-29.6446867320786));
#40327=CARTESIAN_POINT('Ctrl Pts',(3.37850106605793,-5.86583336070378,-29.6365631703462));
#40328=CARTESIAN_POINT('Ctrl Pts',(3.52628515822614,-5.77560403619171,-29.6284396086139));
#40329=CARTESIAN_POINT('Ctrl Pts',(3.67417689356898,-5.68530899032364,-29.6203101298308));
#40330=CARTESIAN_POINT('Ctrl Pts',(3.8185374530025,-5.58936689258128,-29.6121806510477));
#40331=CARTESIAN_POINT('Ctrl Pts',(3.95891834508355,-5.48810117772632,-29.6040511722646));
#40332=CARTESIAN_POINT('Ctrl Pts',(4.09935646798361,-5.38679417862166,-29.5959183792361));
#40333=CARTESIAN_POINT('Ctrl Pts',(4.23581140132458,-5.28015946148076,-29.5877855862076));
#40334=CARTESIAN_POINT('Ctrl Pts',(4.36786778669794,-5.16856072789383,-29.579652793179));
#40335=CARTESIAN_POINT('Ctrl Pts',(4.50006776335609,-5.0568406476148,-29.5715111569719));
#40336=CARTESIAN_POINT('Ctrl Pts',(4.6278593694121,-4.94014601664691,-29.5633695207648));
#40337=CARTESIAN_POINT('Ctrl Pts',(4.75086361636828,-4.8188778671666,-29.5552278845577));
#40338=CARTESIAN_POINT('Ctrl Pts',(4.81353260944063,-4.75709339217701,-29.551079831497));
#40339=CARTESIAN_POINT('Ctrl Pts',(4.87495954492782,-4.6941222936225,-29.5469317784364));
#40340=CARTESIAN_POINT('Ctrl Pts',(4.93509836574921,-4.63002085528559,-29.5427837253757));
#40341=CARTESIAN_POINT('Ctrl Pts',(5.05747255871364,-4.49958328306187,-29.5343430103976));
#40342=CARTESIAN_POINT('Ctrl Pts',(5.17476269518204,-4.36419473843019,-29.5259022954195));
#40343=CARTESIAN_POINT('Ctrl Pts',(5.28656334043379,-4.22427947081884,-29.5174615804414));
#40344=CARTESIAN_POINT('Ctrl Pts',(5.39827948149022,-4.08446995775906,-29.5090272453534));
#40345=CARTESIAN_POINT('Ctrl Pts',(5.50451419515488,-3.94014080183503,-29.5005929102654));
#40346=CARTESIAN_POINT('Ctrl Pts',(5.60490091563784,-3.79175087866834,-29.4921585751774));
#40347=CARTESIAN_POINT('Ctrl Pts',(5.70522717463469,-3.64345032863024,-29.4837293199688));
#40348=CARTESIAN_POINT('Ctrl Pts',(5.79971227605554,-3.49109416277208,-29.4753000647601));
#40349=CARTESIAN_POINT('Ctrl Pts',(5.88803152156129,-3.33517222960084,-29.4668708095515));
#40350=CARTESIAN_POINT('Ctrl Pts',(5.97631112115577,-3.17932028872962,-29.4584453381785));
#40351=CARTESIAN_POINT('Ctrl Pts',(6.05843021950572,-3.01990606169661,-29.4500198668055));
#40352=CARTESIAN_POINT('Ctrl Pts',(6.13410863538623,-2.85744645606528,-29.4415943954324));
#40353=CARTESIAN_POINT('Ctrl Pts',(6.20976467853105,-2.69503487820748,-29.4331714148732));
#40354=CARTESIAN_POINT('Ctrl Pts',(6.27898369568356,-2.5295800190689,-29.424748434314));
#40355=CARTESIAN_POINT('Ctrl Pts',(6.34153230108522,-2.36162170431523,-29.4163254537548));
#40356=CARTESIAN_POINT('Ctrl Pts',(6.40408194216229,-2.1936606085196,-29.4079023337285));
#40357=CARTESIAN_POINT('Ctrl Pts',(6.45996082829072,-2.02319628435379,-29.3994792137021));
#40358=CARTESIAN_POINT('Ctrl Pts',(6.50898417274263,-1.8507874105326,-29.3910560936758));
#40359=CARTESIAN_POINT('Ctrl Pts',(6.55800921250346,-1.67837257452531,-29.382632682364));
#40360=CARTESIAN_POINT('Ctrl Pts',(6.60017814651254,-1.50401337552693,-29.3742092710521));
#40361=CARTESIAN_POINT('Ctrl Pts',(6.6353563755266,-1.32828263925963,-29.3657858597403));
#40362=CARTESIAN_POINT('Ctrl Pts',(6.67054072718416,-1.15252131769337,-29.3573609823642));
#40363=CARTESIAN_POINT('Ctrl Pts',(6.69873188263415,-0.97538830993719,-29.348936104988));
#40364=CARTESIAN_POINT('Ctrl Pts',(6.71984650463333,-0.797465957998982,
-29.3405112276119));
#40365=CARTESIAN_POINT('Ctrl Pts',(6.74096774720992,-0.619487817768444,
-29.3320837085805));
#40366=CARTESIAN_POINT('Ctrl Pts',(6.75500799321,-0.440720170939507,-29.3236561895491));
#40367=CARTESIAN_POINT('Ctrl Pts',(6.76193580646864,-0.261750165610784,
-29.3152286705177));
#40368=CARTESIAN_POINT('Ctrl Pts',(6.76886983232248,-0.0826196668977874,
-29.3067935940129));
#40369=CARTESIAN_POINT('Ctrl Pts',(6.76867866805481,0.0967132193563114,
-29.2983585175081));
#40370=CARTESIAN_POINT('Ctrl Pts',(6.76138301570507,0.275660506665534,-29.2899234410033));
#40371=CARTESIAN_POINT('Ctrl Pts',(6.75408383731852,0.454694280376415,-29.2814842877706));
#40372=CARTESIAN_POINT('Ctrl Pts',(6.7396733445118,0.633341750840649,-29.2730451345378));
#40373=CARTESIAN_POINT('Ctrl Pts',(6.71822415898553,0.811019820733883,-29.264605981305));
#40374=CARTESIAN_POINT('Ctrl Pts',(6.69675113740043,0.988895340778397,-29.2561574498069));
#40375=CARTESIAN_POINT('Ctrl Pts',(6.66822384176986,1.16579897766599,-29.2477089183088));
#40376=CARTESIAN_POINT('Ctrl Pts',(6.63276628116368,1.34115638888911,-29.2392603868107));
#40377=CARTESIAN_POINT('Ctrl Pts',(6.61317482850513,1.43804704807635,-29.2345922990447));
#40378=CARTESIAN_POINT('Ctrl Pts',(6.59146851904817,1.5344658745573,-29.2299242112787));
#40379=CARTESIAN_POINT('Ctrl Pts',(6.56767481186212,1.630317933911,-29.2252561235126));
#40380=CARTESIAN_POINT('Ctrl Pts',(6.52567075980433,1.79952968639066,-29.2170153479159));
#40381=CARTESIAN_POINT('Ctrl Pts',(6.477065097266,1.96735071512019,-29.2087745723191));
#40382=CARTESIAN_POINT('Ctrl Pts',(6.42196376187807,2.13323004880508,-29.2005337967224));
#40383=CARTESIAN_POINT('Ctrl Pts',(6.36692345719267,2.29892565314476,-29.192302148678));
#40384=CARTESIAN_POINT('Ctrl Pts',(6.30540191671621,2.46268351007463,-29.1840705006336));
#40385=CARTESIAN_POINT('Ctrl Pts',(6.23755587019177,2.62396375093792,-29.1758388525892));
#40386=CARTESIAN_POINT('Ctrl Pts',(6.16977287971997,2.78509409809512,-29.1676148550309));
#40387=CARTESIAN_POINT('Ctrl Pts',(6.0956772265536,2.94375108905025,-29.1593908574725));
#40388=CARTESIAN_POINT('Ctrl Pts',(6.01547516936666,3.09941082896946,-29.1511668599142));
#40389=CARTESIAN_POINT('Ctrl Pts',(5.9353439710092,3.25493304290299,-29.1429501282897));
#40390=CARTESIAN_POINT('Ctrl Pts',(5.84911728383338,3.40746296864367,-29.1347333966652));
#40391=CARTESIAN_POINT('Ctrl Pts',(5.75704905105121,3.55649760632429,-29.1265166650407));
#40392=CARTESIAN_POINT('Ctrl Pts',(5.66502798823345,3.70545588804214,-29.118304143152));
#40393=CARTESIAN_POINT('Ctrl Pts',(5.56717152689508,3.85092214625655,-29.1100916212633));
#40394=CARTESIAN_POINT('Ctrl Pts',(5.46377923073043,3.99241850484625,-29.1018790993747));
#40395=CARTESIAN_POINT('Ctrl Pts',(5.36042150944697,4.13386754637301,-29.0936693237928));
#40396=CARTESIAN_POINT('Ctrl Pts',(5.25153185084407,4.27134904596709,-29.0854595482109));
#40397=CARTESIAN_POINT('Ctrl Pts',(5.13745282101675,4.40441454813543,-29.0772497726291));
#40398=CARTESIAN_POINT('Ctrl Pts',(5.08762606458192,4.46253410241685,-29.0736639559464));
#40399=CARTESIAN_POINT('Ctrl Pts',(5.03680986332872,4.51981160902196,-29.0700781392637));
#40400=CARTESIAN_POINT('Ctrl Pts',(4.98503519945453,4.57621164941039,-29.066492322581));
#40401=CARTESIAN_POINT('Ctrl Pts',(4.85719369768314,4.71547408635725,-29.0576382585371));
#40402=CARTESIAN_POINT('Ctrl Pts',(4.72363850840139,4.8492402212088,-29.0487841944932));
#40403=CARTESIAN_POINT('Ctrl Pts',(4.58486112874115,4.97708121594961,-29.0399301304493));
#40404=CARTESIAN_POINT('Ctrl Pts',(4.44569336719082,5.10528182844138,-29.0310511598517));
#40405=CARTESIAN_POINT('Ctrl Pts',(4.30127421369035,5.22752377461368,-29.0221721892541));
#40406=CARTESIAN_POINT('Ctrl Pts',(4.15212909194728,5.3434177268678,-29.0132932186565));
#40407=CARTESIAN_POINT('Ctrl Pts',(4.00276279421828,5.45948354501236,-29.0044010809164));
#40408=CARTESIAN_POINT('Ctrl Pts',(3.84865673546643,5.56918240899693,-28.9955089431762));
#40409=CARTESIAN_POINT('Ctrl Pts',(3.69036506749606,5.67216842738338,-28.9866168054361));
#40410=CARTESIAN_POINT('Ctrl Pts',(3.53175314594796,5.77536280569974,-28.9777066772423));
#40411=CARTESIAN_POINT('Ctrl Pts',(3.36893890085892,5.87181704189946,-28.9687965490484));
#40412=CARTESIAN_POINT('Ctrl Pts',(3.20250276976003,5.96123015909295,-28.9598864208546));
#40413=CARTESIAN_POINT('Ctrl Pts',(3.16818255209653,5.97966772804983,-28.9580490942056));
#40414=CARTESIAN_POINT('Ctrl Pts',(3.13370839824824,5.99780606288608,-28.9562117675566));
#40415=CARTESIAN_POINT('Ctrl Pts',(3.09908550384723,6.01564277861011,-28.9543744409077));
#40416=CARTESIAN_POINT('Ctrl Pts',(3.09908550384721,6.01564277861012,-30.9542680870819));
#40417=CARTESIAN_POINT('Ctrl Pts',(2.94371447950243,6.09568544520211,-30.9460679664523));
#40418=CARTESIAN_POINT('Ctrl Pts',(2.78527441477496,6.16968742560315,-30.9378678458226));
#40419=CARTESIAN_POINT('Ctrl Pts',(2.6242794472051,6.23742305627708,-30.929667725193));
#40420=CARTESIAN_POINT('Ctrl Pts',(2.46322305524189,6.30518453011918,-30.9214644759722));
#40421=CARTESIAN_POINT('Ctrl Pts',(2.2996101490492,6.36667475273516,-30.9132612267514));
#40422=CARTESIAN_POINT('Ctrl Pts',(2.1339731655378,6.42171686768925,-30.9050579775305));
#40423=CARTESIAN_POINT('Ctrl Pts',(1.96814645873079,6.47682202877727,-30.8968453321746));
#40424=CARTESIAN_POINT('Ctrl Pts',(1.80029138397078,6.52546421516487,-30.8886326868187));
#40425=CARTESIAN_POINT('Ctrl Pts',(1.6309547958345,6.56751668851663,-30.8804200414627));
#40426=CARTESIAN_POINT('Ctrl Pts',(1.46151405033017,6.60959502795553,-30.8722023445847));
#40427=CARTESIAN_POINT('Ctrl Pts',(1.29059032549375,6.64507550236139,-30.8639846477066));
#40428=CARTESIAN_POINT('Ctrl Pts',(1.11873877346133,6.67388286957108,-30.8557669508285));
#40429=CARTESIAN_POINT('Ctrl Pts',(0.94662984775507,6.70273338016728,-30.8475369467073));
#40430=CARTESIAN_POINT('Ctrl Pts',(0.773590673694652,6.72489077018064,-30.8393069425861));
#40431=CARTESIAN_POINT('Ctrl Pts',(0.600180819029017,6.74033174142562,-30.8310769384649));
#40432=CARTESIAN_POINT('Ctrl Pts',(0.472474212952908,6.75170314840832,-30.8250160032525));
#40433=CARTESIAN_POINT('Ctrl Pts',(0.344566632330296,6.75943299989573,-30.8189550680401));
#40434=CARTESIAN_POINT('Ctrl Pts',(0.216680517030194,6.76353003641882,-30.8128941328278));
#40435=CARTESIAN_POINT('Ctrl Pts',(0.0463846469923235,6.76898573735741,
-30.8048232626414));
#40436=CARTESIAN_POINT('Ctrl Pts',(-0.124428369577882,6.76801541995605,
-30.7967523924549));
#40437=CARTESIAN_POINT('Ctrl Pts',(-0.295222157570116,6.76055714254969,
-30.7886815222685));
#40438=CARTESIAN_POINT('Ctrl Pts',(-0.465803405968926,6.75310814638984,
-30.7806206956527));
#40439=CARTESIAN_POINT('Ctrl Pts',(-0.636365105444776,6.73918727108163,
-30.7725598690369));
#40440=CARTESIAN_POINT('Ctrl Pts',(-0.806366110133777,6.71878431685582,
-30.7644990424211));
#40441=CARTESIAN_POINT('Ctrl Pts',(-0.976192840410988,6.69840227846432,
-30.7564464792612));
#40442=CARTESIAN_POINT('Ctrl Pts',(-1.14545965252415,6.67155142907742,-30.7483939161014));
#40443=CARTESIAN_POINT('Ctrl Pts',(-1.31362585340333,6.63827357957401,-30.7403413529415));
#40444=CARTESIAN_POINT('Ctrl Pts',(-1.48165648296141,6.60502255782789,-30.7322952815536));
#40445=CARTESIAN_POINT('Ctrl Pts',(-1.64858790323685,6.56535492057922,-30.7242492101657));
#40446=CARTESIAN_POINT('Ctrl Pts',(-1.81388510042842,6.51936422072304,-30.7162031387778));
#40447=CARTESIAN_POINT('Ctrl Pts',(-1.97908519609627,6.47340053745946,-30.7081617939419));
#40448=CARTESIAN_POINT('Ctrl Pts',(-2.14265262133072,6.42112128564826,-30.7001204491059));
#40449=CARTESIAN_POINT('Ctrl Pts',(-2.30406321494482,6.36267095656676,-30.69207910427));
#40450=CARTESIAN_POINT('Ctrl Pts',(-2.46858530814144,6.30309388499294,-30.683882747049));
#40451=CARTESIAN_POINT('Ctrl Pts',(-2.63086617898871,6.23710546880609,-30.6756863898279));
#40452=CARTESIAN_POINT('Ctrl Pts',(-2.79036721872086,6.1649119851534,-30.6674900326068));
#40453=CARTESIAN_POINT('Ctrl Pts',(-2.94680197657918,6.09410636436796,-30.6594512438983));
#40454=CARTESIAN_POINT('Ctrl Pts',(-3.1005624706329,6.01733226656811,-30.6514124551898));
#40455=CARTESIAN_POINT('Ctrl Pts',(-3.25116144052422,5.93483262507448,-30.6433736664813));
#40456=CARTESIAN_POINT('Ctrl Pts',(-3.40177652586958,5.85232415537186,-30.6353340175495));
#40457=CARTESIAN_POINT('Ctrl Pts',(-3.54922908580803,5.76408910138276,-30.6272943686178));
#40458=CARTESIAN_POINT('Ctrl Pts',(-3.69305743016558,5.67041584167324,-30.6192547196861));
#40459=CARTESIAN_POINT('Ctrl Pts',(-3.83692964402033,5.57671401041321,-30.6112126185579));
#40460=CARTESIAN_POINT('Ctrl Pts',(-3.97717512916192,5.47757087545426,-30.6031705174297));
#40461=CARTESIAN_POINT('Ctrl Pts',(-4.11336221975358,5.37331743423967,-30.5951284163015));
#40462=CARTESIAN_POINT('Ctrl Pts',(-4.25414508958853,5.26554584898444,-30.5868149258568));
#40463=CARTESIAN_POINT('Ctrl Pts',(-4.39059051552245,5.15231328263402,-30.578501435412));
#40464=CARTESIAN_POINT('Ctrl Pts',(-4.52226071961451,5.03402890176762,-30.5701879449673));
#40465=CARTESIAN_POINT('Ctrl Pts',(-4.64985700198412,4.91940428061649,-30.5621316767965));
#40466=CARTESIAN_POINT('Ctrl Pts',(-4.77296894296149,4.80003610830509,-30.5540754086258));
#40467=CARTESIAN_POINT('Ctrl Pts',(-4.89123772725468,4.67633216265488,-30.546019140455));
#40468=CARTESIAN_POINT('Ctrl Pts',(-5.01517067856516,4.54670374747496,-30.5375770388733));
#40469=CARTESIAN_POINT('Ctrl Pts',(-5.13378484358296,4.4123144104076,-30.5291349372916));
#40470=CARTESIAN_POINT('Ctrl Pts',(-5.24671726850061,4.27366902139339,-30.5206928357099));
#40471=CARTESIAN_POINT('Ctrl Pts',(-5.35964969341829,4.13502363237914,-30.5122507341281));
#40472=CARTESIAN_POINT('Ctrl Pts',(-5.46690017074366,3.99212261192921,-30.5038086325464));
#40473=CARTESIAN_POINT('Ctrl Pts',(-5.56816028146203,3.84550127811039,-30.4953665309647));
#40474=CARTESIAN_POINT('Ctrl Pts',(-5.67116896999752,3.69634806070966,-30.4867786496534));
#40475=CARTESIAN_POINT('Ctrl Pts',(-5.7682881196305,3.54289853264869,-30.4781907683421));
#40476=CARTESIAN_POINT('Ctrl Pts',(-5.85915963143274,3.38563692876083,-30.4696028870308));
#40477=CARTESIAN_POINT('Ctrl Pts',(-5.94991018504773,3.2285846542673,-30.461026436965));
#40478=CARTESIAN_POINT('Ctrl Pts',(-6.03442952272235,3.06773069020775,-30.4524499868992));
#40479=CARTESIAN_POINT('Ctrl Pts',(-6.11240217391094,2.90358892826943,-30.4438735368333));
#40480=CARTESIAN_POINT('Ctrl Pts',(-6.19027876786987,2.73964937829496,-30.4353076523956));
#40481=CARTESIAN_POINT('Ctrl Pts',(-6.26162461990626,2.57243038834527,-30.4267417679578));
#40482=CARTESIAN_POINT('Ctrl Pts',(-6.32616936136809,2.40247168792633,-30.4181758835201));
#40483=CARTESIAN_POINT('Ctrl Pts',(-6.39064096204112,2.23270558125139,-30.4096197057684));
#40484=CARTESIAN_POINT('Ctrl Pts',(-6.44832670671636,2.06020624724369,-30.4010635280168));
#40485=CARTESIAN_POINT('Ctrl Pts',(-6.49900345467092,1.88553522803883,-30.3925073502651));
#40486=CARTESIAN_POINT('Ctrl Pts',(-6.54961033477658,1.71110502713566,-30.3839629688848));
#40487=CARTESIAN_POINT('Ctrl Pts',(-6.59322741040896,1.53450941620116,-30.3754185875044));
#40488=CARTESIAN_POINT('Ctrl Pts',(-6.62968070160935,1.35632694978333,-30.3668742061241));
#40489=CARTESIAN_POINT('Ctrl Pts',(-6.66610360228398,1.1782930312375,-30.3583369480578));
#40490=CARTESIAN_POINT('Ctrl Pts',(-6.69537456119865,0.998675201964652,
-30.3497996899915));
#40491=CARTESIAN_POINT('Ctrl Pts',(-6.71736986548872,0.818065455953325,
-30.3412624319252));
#40492=CARTESIAN_POINT('Ctrl Pts',(-6.73934393126139,0.637630105493947,
-30.3327334173777));
#40493=CARTESIAN_POINT('Ctrl Pts',(-6.75405631961916,0.45620506097962,-30.3242044028302));
#40494=CARTESIAN_POINT('Ctrl Pts',(-6.76143465766259,0.274390907573759,
-30.3156753882827));
#40495=CARTESIAN_POINT('Ctrl Pts',(-6.76514160429665,0.183045761820821,
-30.3113903309184));
#40496=CARTESIAN_POINT('Ctrl Pts',(-6.76699813350448,0.0916025323879388,
-30.3071052735542));
#40497=CARTESIAN_POINT('Ctrl Pts',(-6.76699999859311,0.000137988494950558,
-30.30282021619));
#40498=CARTESIAN_POINT('',(-6.767,3.39320585518443E-13,-30.6971797838101));
#40499=CARTESIAN_POINT('Ctrl Pts',(3.0990855038472,6.01564277861013,-31.3484270467647));
#40500=CARTESIAN_POINT('Ctrl Pts',(2.92903432523677,6.10324823690256,-31.3394159215786));
#40501=CARTESIAN_POINT('Ctrl Pts',(2.75517565391701,6.18368609644757,-31.3304047963925));
#40502=CARTESIAN_POINT('Ctrl Pts',(2.57810514217839,6.2566494928095,-31.3213936712064));
#40503=CARTESIAN_POINT('Ctrl Pts',(2.40127488857691,6.32951388878159,-31.3123947727662));
#40504=CARTESIAN_POINT('Ctrl Pts',(2.22124171000805,6.39492396748568,-31.303395874326));
#40505=CARTESIAN_POINT('Ctrl Pts',(2.03862336042999,6.4526199170809,-31.2943969758858));
#40506=CARTESIAN_POINT('Ctrl Pts',(1.85638271667096,6.51019653531677,-31.2854166896842));
#40507=CARTESIAN_POINT('Ctrl Pts',(1.67156779962697,6.56009079414926,-31.2764364034827));
#40508=CARTESIAN_POINT('Ctrl Pts',(1.48481382549683,6.60209185816234,-31.2674561172811));
#40509=CARTESIAN_POINT('Ctrl Pts',(1.45913711007258,6.60786656455455,-31.2662214219859));
#40510=CARTESIAN_POINT('Ctrl Pts',(1.43342376993098,6.61349213775955,-31.2649867266906));
#40511=CARTESIAN_POINT('Ctrl Pts',(1.40767548398599,6.61896810173495,-31.2637520313954));
#40512=CARTESIAN_POINT('Ctrl Pts',(1.23827546502397,6.65499490380053,-31.2556288729501));
#40513=CARTESIAN_POINT('Ctrl Pts',(1.06743726754016,6.68452577478008,-31.2475057145048));
#40514=CARTESIAN_POINT('Ctrl Pts',(0.895704241073713,6.70745875220434,-31.2393825560595));
#40515=CARTESIAN_POINT('Ctrl Pts',(0.723983322684397,6.73039011273366,-31.2312599703394));
#40516=CARTESIAN_POINT('Ctrl Pts',(0.55136806378577,6.7467244578645,-31.2231373846193));
#40517=CARTESIAN_POINT('Ctrl Pts',(0.378409067366565,6.75641144230684,-31.2150147988991));
#40518=CARTESIAN_POINT('Ctrl Pts',(0.205429288144462,6.76609959074002,-31.2068912371668));
#40519=CARTESIAN_POINT('Ctrl Pts',(0.0321060546674524,6.76913876871745,
-31.1987676754344));
#40520=CARTESIAN_POINT('Ctrl Pts',(-0.14100792743591,6.76553070825935,-31.1906441137021));
#40521=CARTESIAN_POINT('Ctrl Pts',(-0.314248002533276,6.76192001975734,
-31.182514634919));
#40522=CARTESIAN_POINT('Ctrl Pts',(-0.487278155527502,6.75165243025827,
-31.1743851561358));
#40523=CARTESIAN_POINT('Ctrl Pts',(-0.65954806106113,6.73478176002389,-31.1662556773527));
#40524=CARTESIAN_POINT('Ctrl Pts',(-0.831888198002263,6.71790421191428,
-31.1581228843242));
#40525=CARTESIAN_POINT('Ctrl Pts',(-1.00346710729642,6.69441826679735,-31.1499900912957));
#40526=CARTESIAN_POINT('Ctrl Pts',(-1.17374283375576,6.66442921488457,-31.1418572982672));
#40527=CARTESIAN_POINT('Ctrl Pts',(-1.34420370923653,6.63440755442723,-31.1337156620601));
#40528=CARTESIAN_POINT('Ctrl Pts',(-1.51335821432473,6.59786874103933,-31.1255740258529));
#40529=CARTESIAN_POINT('Ctrl Pts',(-1.68067703873291,6.55496862627702,-31.1174323896457));
#40530=CARTESIAN_POINT('Ctrl Pts',(-1.76592370709553,6.5331116005132,-31.1132843365851));
#40531=CARTESIAN_POINT('Ctrl Pts',(-1.85069413992202,6.50960412564579,-31.1091362835246));
#40532=CARTESIAN_POINT('Ctrl Pts',(-1.93492021399903,6.48447166432686,-31.104988230464));
#40533=CARTESIAN_POINT('Ctrl Pts',(-2.10630863999641,6.43333057726927,-31.0965475154859));
#40534=CARTESIAN_POINT('Ctrl Pts',(-2.2757949243887,6.37535270620505,-31.0881068005078));
#40535=CARTESIAN_POINT('Ctrl Pts',(-2.44281521991742,6.31070065851169,-31.0796660855297));
#40536=CARTESIAN_POINT('Ctrl Pts',(-2.60970927363744,6.24609747788211,-31.0712317504417));
#40537=CARTESIAN_POINT('Ctrl Pts',(-2.7741407442683,6.17483029677232,-31.0627974153536));
#40538=CARTESIAN_POINT('Ctrl Pts',(-2.93556194988327,6.09711120436535,-31.0543630802656));
#40539=CARTESIAN_POINT('Ctrl Pts',(-3.09688593381462,6.01943892105627,-31.045933825057));
#40540=CARTESIAN_POINT('Ctrl Pts',(-3.2552029676386,5.93532261784037,-31.0375045698484));
#40541=CARTESIAN_POINT('Ctrl Pts',(-3.40998596434023,5.84502221749436,-31.0290753146398));
#40542=CARTESIAN_POINT('Ctrl Pts',(-3.56469948000213,5.75476235238695,-31.0206498432668));
#40543=CARTESIAN_POINT('Ctrl Pts',(-3.71588183415688,5.65832409293377,-31.0122243718938));
#40544=CARTESIAN_POINT('Ctrl Pts',(-3.86303079390488,5.55601314661356,-31.0037989005208));
#40545=CARTESIAN_POINT('Ctrl Pts',(-4.01013625214949,5.45373244637857,-30.9953759199617));
#40546=CARTESIAN_POINT('Ctrl Pts',(-4.15321042042536,5.34558271166036,-30.9869529394025));
#40547=CARTESIAN_POINT('Ctrl Pts',(-4.29177997256654,5.23191300262885,-30.9785299588434));
#40548=CARTESIAN_POINT('Ctrl Pts',(-4.43035181913392,5.11824141146121,-30.9701068388171));
#40549=CARTESIAN_POINT('Ctrl Pts',(-4.56441863863559,4.99904986966019,-30.9616837187908));
#40550=CARTESIAN_POINT('Ctrl Pts',(-4.69353961576692,4.87472818475312,-30.9532605987645));
#40551=CARTESIAN_POINT('Ctrl Pts',(-4.82266505811647,4.75040220059536,-30.9448371874526));
#40552=CARTESIAN_POINT('Ctrl Pts',(-4.94684407670967,4.62094595079707,-30.9364137761408));
#40553=CARTESIAN_POINT('Ctrl Pts',(-5.06567210788635,4.48678672274294,-30.927990364829));
#40554=CARTESIAN_POINT('Ctrl Pts',(-5.18452082065161,4.3526041447609,-30.9195654874529));
#40555=CARTESIAN_POINT('Ctrl Pts',(-5.29801646810998,4.21371720624633,-30.9111406100769));
#40556=CARTESIAN_POINT('Ctrl Pts',(-5.40579399699795,4.07058721341541,-30.9027157327008));
#40557=CARTESIAN_POINT('Ctrl Pts',(-5.51360531997894,3.92741234157914,-30.8942882136694));
#40558=CARTESIAN_POINT('Ctrl Pts',(-5.61569474922438,3.77999202921619,-30.8858606946379));
#40559=CARTESIAN_POINT('Ctrl Pts',(-5.71173966431975,3.62881785255703,-30.8774331756064));
#40560=CARTESIAN_POINT('Ctrl Pts',(-5.80787070878275,3.47750810873923,-30.8689980991017));
#40561=CARTESIAN_POINT('Ctrl Pts',(-5.89794622918145,3.32243805598583,-30.8605630225969));
#40562=CARTESIAN_POINT('Ctrl Pts',(-5.98168823942467,3.16412623109898,-30.8521279460921));
#40563=CARTESIAN_POINT('Ctrl Pts',(-6.06547072273255,3.00573789306529,-30.8436887928593));
#40564=CARTESIAN_POINT('Ctrl Pts',(-6.14291344237129,2.84410495650474,-30.8352496396265));
#40565=CARTESIAN_POINT('Ctrl Pts',(-6.21378573983061,2.67976785925159,-30.8268104863938));
#40566=CARTESIAN_POINT('Ctrl Pts',(-6.28473679628267,2.51524813740863,-30.8183619548957));
#40567=CARTESIAN_POINT('Ctrl Pts',(-6.34910271641903,2.34801855968716,-30.8099134233976));
#40568=CARTESIAN_POINT('Ctrl Pts',(-6.40670165452679,2.17863785652497,-30.8014648918995));
#40569=CARTESIAN_POINT('Ctrl Pts',(-6.43852693663505,2.08504952245279,-30.7967968041333));
#40570=CARTESIAN_POINT('Ctrl Pts',(-6.46828719849882,1.99080473063557,-30.7921287163671));
#40571=CARTESIAN_POINT('Ctrl Pts',(-6.49595839816723,1.89599933789036,-30.7874606286009));
#40572=CARTESIAN_POINT('Ctrl Pts',(-6.54949111980473,1.71258876081452,-30.7784297428438));
#40573=CARTESIAN_POINT('Ctrl Pts',(-6.59530470013533,1.52672903902217,-30.7693988570867));
#40574=CARTESIAN_POINT('Ctrl Pts',(-6.63319070558781,1.33905566101768,-30.7603679713296));
#40575=CARTESIAN_POINT('Ctrl Pts',(-6.67098922671683,1.1518156482706,-30.7513579392075));
#40576=CARTESIAN_POINT('Ctrl Pts',(-6.70089663607218,0.962770559905612,
-30.7423479070855));
#40577=CARTESIAN_POINT('Ctrl Pts',(-6.72275420312697,0.772570336175757,
-30.7333378749634));
#40578=CARTESIAN_POINT('Ctrl Pts',(-6.74453441785932,0.58304321705057,-30.7243597286824));
#40579=CARTESIAN_POINT('Ctrl Pts',(-6.75832158011288,0.392369348153801,
-30.7153815824015));
#40580=CARTESIAN_POINT('Ctrl Pts',(-6.76400803109756,0.201207244520965,
-30.7064034361205));
#40581=CARTESIAN_POINT('Ctrl Pts',(-6.76595534646838,0.135744110533633,
-30.7033288853504));
#40582=CARTESIAN_POINT('Ctrl Pts',(-6.76695311776644,0.0702238391348725,
-30.7002543345802));
#40583=CARTESIAN_POINT('Ctrl Pts',(-6.76699838636073,0.00467322065976275,
-30.6971797838101));
#40584=CARTESIAN_POINT('Ctrl Pts',(-6.767,4.3548441435357E-13,-30.6971797838101));
#40585=CARTESIAN_POINT('Ctrl Pts',(-6.76700000000001,-0.186007249559608,
-30.6884302719974));
#40586=CARTESIAN_POINT('Ctrl Pts',(-6.75932637294249,-0.372014355815825,
-30.6796807601846));
#40587=CARTESIAN_POINT('Ctrl Pts',(-6.74400518263364,-0.557389537586234,
-30.6709312483719));
#40588=CARTESIAN_POINT('Ctrl Pts',(-6.7286840570373,-0.742763936382708,
-30.6621817735147));
#40589=CARTESIAN_POINT('Ctrl Pts',(-6.70571545643564,-0.92750613040502,
-30.6534322986575));
#40590=CARTESIAN_POINT('Ctrl Pts',(-6.67517739401573,-1.11098864009554,
-30.6446828238003));
#40591=CARTESIAN_POINT('Ctrl Pts',(-6.64463945804386,-1.29447039004561,
-30.6359333851718));
#40592=CARTESIAN_POINT('Ctrl Pts',(-6.60653217002717,-1.47669218339309,
-30.6271839465432));
#40593=CARTESIAN_POINT('Ctrl Pts',(-6.56098496085469,-1.65703510627825,
-30.6184345079147));
#40594=CARTESIAN_POINT('Ctrl Pts',(-6.51543793649544,-1.83737729740051,
-30.6096851047881));
#40595=CARTESIAN_POINT('Ctrl Pts',(-6.46245112156883,-2.01584035544994,
-30.6009357016615));
#40596=CARTESIAN_POINT('Ctrl Pts',(-6.40220448361703,-2.19181813797451,
-30.5921862985348));
#40597=CARTESIAN_POINT('Ctrl Pts',(-6.34195808511956,-2.36779522106348,
-30.5834369301833));
#40598=CARTESIAN_POINT('Ctrl Pts',(-6.27445201416335,-2.54128677725791,
-30.5746875618318));
#40599=CARTESIAN_POINT('Ctrl Pts',(-6.19991555052702,-2.71170355428708,
-30.5659381934802));
#40600=CARTESIAN_POINT('Ctrl Pts',(-6.12537937695088,-2.88211966813585,
-30.557188859177));
#40601=CARTESIAN_POINT('Ctrl Pts',(-6.04381298028307,-3.04946076419956,
-30.5484395248739));
#40602=CARTESIAN_POINT('Ctrl Pts',(-5.95549339308823,-3.21315848424607,
-30.5396901905707));
#40603=CARTESIAN_POINT('Ctrl Pts',(-5.86717414225637,-3.37685558085382,
-30.5309408895891));
#40604=CARTESIAN_POINT('Ctrl Pts',(-5.7721018884388,-3.53690907700304,-30.5221915886076));
#40605=CARTESIAN_POINT('Ctrl Pts',(-5.67059953311171,-3.69277537024299,
-30.513442287626));
#40606=CARTESIAN_POINT('Ctrl Pts',(-5.56909755592487,-3.84864108281347,
-30.5046930192394));
#40607=CARTESIAN_POINT('Ctrl Pts',(-5.46116568154724,-4.0003193835516,-30.4959437508527));
#40608=CARTESIAN_POINT('Ctrl Pts',(-5.34717048488112,-4.14729511918506,
-30.4871944824661));
#40609=CARTESIAN_POINT('Ctrl Pts',(-5.23317570343023,-4.29427031947523,
-30.4784452459478));
#40610=CARTESIAN_POINT('Ctrl Pts',(-5.11311781951248,-4.43654276249901,
-30.4696960094294));
#40611=CARTESIAN_POINT('Ctrl Pts',(-4.98740458928927,-4.57362924412729,
-30.460946772911));
#40612=CARTESIAN_POINT('Ctrl Pts',(-4.86169180652415,-4.71071523781603,
-30.4521975675343));
#40613=CARTESIAN_POINT('Ctrl Pts',(-4.7303239114124,-4.84261509584814,-30.4434483621576));
#40614=CARTESIAN_POINT('Ctrl Pts',(-4.59374706946988,-4.96888084599912,
-30.4346991567809));
#40615=CARTESIAN_POINT('Ctrl Pts',(-4.45717070231215,-5.09514615720996,
-30.4259499818192));
#40616=CARTESIAN_POINT('Ctrl Pts',(-4.3153856349712,-5.21577720520781,-30.4172008068575));
#40617=CARTESIAN_POINT('Ctrl Pts',(-4.16887340951853,-5.33036429293622,
-30.4084516318959));
#40618=CARTESIAN_POINT('Ctrl Pts',(-4.02236168122339,-5.44495099183813,
-30.3997024866226));
#40619=CARTESIAN_POINT('Ctrl Pts',(-3.87112305263044,-5.55349359498023,
-30.3909533413494));
#40620=CARTESIAN_POINT('Ctrl Pts',(-3.71567116928868,-5.65562346357295,
-30.3822041960761));
#40621=CARTESIAN_POINT('Ctrl Pts',(-3.56021980053185,-5.75775299409006,
-30.3734550797648));
#40622=CARTESIAN_POINT('Ctrl Pts',(-3.40055544441958,-5.85346967519952,
-30.3647059634534));
#40623=CARTESIAN_POINT('Ctrl Pts',(-3.23722035886718,-5.94244843041451,
-30.355956847142));
#40624=CARTESIAN_POINT('Ctrl Pts',(-3.07388580043369,-6.03142689847512,
-30.347207759066));
#40625=CARTESIAN_POINT('Ctrl Pts',(-2.90688078789107,-6.11366734707957,
-30.33845867099));
#40626=CARTESIAN_POINT('Ctrl Pts',(-2.73677250610282,-6.18889047001478,
-30.329709582914));
#40627=CARTESIAN_POINT('Ctrl Pts',(-2.56666475916808,-6.26411335643386,
-30.3209605223468));
#40628=CARTESIAN_POINT('Ctrl Pts',(-2.39345402456951,-6.3323188454531,-30.3122114617796));
#40629=CARTESIAN_POINT('Ctrl Pts',(-2.21772855943907,-6.39327529804938,
-30.3034624012125));
#40630=CARTESIAN_POINT('Ctrl Pts',(-2.04200363223441,-6.4542315640475,-30.2947133674277));
#40631=CARTESIAN_POINT('Ctrl Pts',(-1.86376426060892,-6.50793874412493,
-30.2859643336429));
#40632=CARTESIAN_POINT('Ctrl Pts',(-1.68361577621555,-6.55421443943346,
-30.2772152998581));
#40633=CARTESIAN_POINT('Ctrl Pts',(-1.50346782833073,-6.6004899969262,-30.2684662921292));
#40634=CARTESIAN_POINT('Ctrl Pts',(-1.32141105657236,-6.63933404265192,
-30.2597172844003));
#40635=CARTESIAN_POINT('Ctrl Pts',(-1.13806375346375,-6.67061465631556,
-30.2509682766714));
#40636=CARTESIAN_POINT('Ctrl Pts',(-0.954716981167896,-6.70189517941802,
-30.2422192942719));
#40637=CARTESIAN_POINT('Ctrl Pts',(-0.770079967439657,-6.72561226609035,
-30.2334703118725));
#40638=CARTESIAN_POINT('Ctrl Pts',(-0.584779764069928,-6.74168536996012,
-30.224721329473));
#40639=CARTESIAN_POINT('Ctrl Pts',(-0.391489587589783,-6.75845153117891,
-30.2155950990574));
#40640=CARTESIAN_POINT('Ctrl Pts',(-0.197478091802034,-6.76689985146403,
-30.2064688686418));
#40641=CARTESIAN_POINT('Ctrl Pts',(-0.00346214752780608,-6.76699911434415,
-30.1973426382262));
#40642=CARTESIAN_POINT('Ctrl Pts',(0.18449079848784,-6.76709527525926,-30.188501602511));
#40643=CARTESIAN_POINT('Ctrl Pts',(0.372447602157948,-6.75935633790746,
-30.1796605667959));
#40644=CARTESIAN_POINT('Ctrl Pts',(0.559756448197352,-6.74380914014487,
-30.1708195310808));
#40645=CARTESIAN_POINT('Ctrl Pts',(0.745136131046472,-6.7284220687312,-30.1620695524675));
#40646=CARTESIAN_POINT('Ctrl Pts',(0.929880851948136,-6.7053868635568,-30.1533195738542));
#40647=CARTESIAN_POINT('Ctrl Pts',(1.11336305057769,-6.67478177303261,-30.1445695952409));
#40648=CARTESIAN_POINT('Ctrl Pts',(1.29684337090427,-6.64417699581201,-30.1358197062009));
#40649=CARTESIAN_POINT('Ctrl Pts',(1.47906091205491,-6.60600253547992,-30.1270698171609));
#40650=CARTESIAN_POINT('Ctrl Pts',(1.65939671095518,-6.56038806441137,-30.1183199281209));
#40651=CARTESIAN_POINT('Ctrl Pts',(1.83973072369456,-6.51477404513766,-30.1095701257454));
#40652=CARTESIAN_POINT('Ctrl Pts',(2.0181827535733,-6.46172023288569,-30.1008203233699));
#40653=CARTESIAN_POINT('Ctrl Pts',(2.19414664033618,-6.40140683918008,-30.0920705209944));
#40654=CARTESIAN_POINT('Ctrl Pts',(2.37010884271549,-6.34109402281389,-30.0833208023749));
#40655=CARTESIAN_POINT('Ctrl Pts',(2.54358267848093,-6.27352185699675,-30.0745710837554));
#40656=CARTESIAN_POINT('Ctrl Pts',(2.71397890842027,-6.19891986435137,-30.0658213651358));
#40657=CARTESIAN_POINT('Ctrl Pts',(2.8843735638923,-6.12431856103108,-30.057071727364));
#40658=CARTESIAN_POINT('Ctrl Pts',(3.05169040787463,-6.0426876758241,-30.0483220895922));
#40659=CARTESIAN_POINT('Ctrl Pts',(3.21536112512347,-5.95430447953787,-30.0395724518204));
#40660=CARTESIAN_POINT('Ctrl Pts',(3.37903038443129,-5.86592207054877,-30.0308228919883));
#40661=CARTESIAN_POINT('Ctrl Pts',(3.53905332980253,-5.77078760703205,-30.0220733321562));
#40662=CARTESIAN_POINT('Ctrl Pts',(3.69488643042165,-5.66922422085121,-30.0133237723242));
#40663=CARTESIAN_POINT('Ctrl Pts',(3.85071819469009,-5.56766170562974,-30.0045742875242));
#40664=CARTESIAN_POINT('Ctrl Pts',(4.00235994599484,-5.45967053456061,-29.9958248027242));
#40665=CARTESIAN_POINT('Ctrl Pts',(4.14929662974553,-5.34561750206488,-29.9870753179242));
#40666=CARTESIAN_POINT('Ctrl Pts',(4.29623210225295,-5.2315654097426,-29.9783259052488));
#40667=CARTESIAN_POINT('Ctrl Pts',(4.43846235842365,-5.11145173171971,-29.9695764925735));
#40668=CARTESIAN_POINT('Ctrl Pts',(4.57550431797673,-4.98568443006337,-29.9608270798981));
#40669=CARTESIAN_POINT('Ctrl Pts',(4.71254519337739,-4.85991812336452,-29.9520777364402));
#40670=CARTESIAN_POINT('Ctrl Pts',(4.84439764315228,-4.72849847630851,-29.9433283929823));
#40671=CARTESIAN_POINT('Ctrl Pts',(4.97061384196929,-4.59187184425081,-29.9345790495244));
#40672=CARTESIAN_POINT('Ctrl Pts',(5.09682908420441,-4.45524624767478,-29.925829772377));
#40673=CARTESIAN_POINT('Ctrl Pts',(5.21740796650398,-4.31341395556618,-29.9170804952297));
#40674=CARTESIAN_POINT('Ctrl Pts',(5.3319409594247,-4.16685668162576,-29.9083312180823));
#40675=CARTESIAN_POINT('Ctrl Pts',(5.44647312235341,-4.02030046974932,-29.8995820043388));
#40676=CARTESIAN_POINT('Ctrl Pts',(5.55495930712486,-3.86901957035262,-29.8908327905952));
#40677=CARTESIAN_POINT('Ctrl Pts',(5.65703106079983,-3.71352778058088,-29.8820835768517));
#40678=CARTESIAN_POINT('Ctrl Pts',(5.75910210868914,-3.55803706597315,-29.8733344236055));
#40679=CARTESIAN_POINT('Ctrl Pts',(5.85475865698717,-3.3983357588061,-29.8645852703593));
#40680=CARTESIAN_POINT('Ctrl Pts',(5.94367583069221,-3.2349662470643,-29.8558361171131));
#40681=CARTESIAN_POINT('Ctrl Pts',(6.03259241910233,-3.07159781069795,-29.847087021458));
#40682=CARTESIAN_POINT('Ctrl Pts',(6.11476958471119,-2.90456146975516,-29.8383379258029));
#40683=CARTESIAN_POINT('Ctrl Pts',(6.18992823574533,-2.73442451647925,-29.8295888301477));
#40684=CARTESIAN_POINT('Ctrl Pts',(6.26508641701078,-2.56428862662068,-29.8208397891776));
#40685=CARTESIAN_POINT('Ctrl Pts',(6.33322605570435,-2.39105242530913,-29.8120907482075));
#40686=CARTESIAN_POINT('Ctrl Pts',(6.39411573747899,-2.21530425353348,-29.8033417072374));
#40687=CARTESIAN_POINT('Ctrl Pts',(6.45500505889245,-2.03955712188183,-29.7945927180464));
#40688=CARTESIAN_POINT('Ctrl Pts',(6.50864441545036,-1.86129832025197,-29.7858437288554));
#40689=CARTESIAN_POINT('Ctrl Pts',(6.55485164050002,-1.68113324011938,-29.7770947396644));
#40690=CARTESIAN_POINT('Ctrl Pts',(6.60199852639195,-1.49730435912525,-29.7681678327875));
#40691=CARTESIAN_POINT('Ctrl Pts',(6.64140767441084,-1.31149113173276,-29.7592409259106));
#40692=CARTESIAN_POINT('Ctrl Pts',(6.67293975269666,-1.12435050446054,-29.7503140190337));
#40693=CARTESIAN_POINT('Ctrl Pts',(6.7038466483156,-0.940920291559975,-29.7415641048497));
#40694=CARTESIAN_POINT('Ctrl Pts',(6.72718585889708,-0.756215114274175,
-29.7328141906657));
#40695=CARTESIAN_POINT('Ctrl Pts',(6.74287810451896,-0.570862389371384,
-29.7240642764818));
#40696=CARTESIAN_POINT('Ctrl Pts',(6.75857004154145,-0.385513309564392,
-29.7153145343712));
#40697=CARTESIAN_POINT('Ctrl Pts',(6.76661529035567,-0.199516993255554,
-29.7065647922606));
#40698=CARTESIAN_POINT('Ctrl Pts',(6.76698652348897,-0.0135052182014546,
-29.69781505015));
#40699=CARTESIAN_POINT('Ctrl Pts',(6.76735774981515,0.17250314604148,-29.6890654684794));
#40700=CARTESIAN_POINT('Ctrl Pts',(6.76005524147466,0.358526681836041,-29.6803158868087));
#40701=CARTESIAN_POINT('Ctrl Pts',(6.74510380214861,0.543933542117414,-29.6715663051381));
#40702=CARTESIAN_POINT('Ctrl Pts',(6.73015261710951,0.72933724908729,-29.6628168722762));
#40703=CARTESIAN_POINT('Ctrl Pts',(6.7075527844457,0.914124015857248,-29.6540674394142));
#40704=CARTESIAN_POINT('Ctrl Pts',(6.67738106408246,1.09766621749645,-29.6453180065523));
#40705=CARTESIAN_POINT('Ctrl Pts',(6.64720981677204,1.28120554143583,-29.6365687108699));
#40706=CARTESIAN_POINT('Ctrl Pts',(6.60946696581465,1.46350005650882,-29.6278194151876));
#40707=CARTESIAN_POINT('Ctrl Pts',(6.56428070010928,1.64393062206797,-29.6190701195053));
#40708=CARTESIAN_POINT('Ctrl Pts',(6.51909508282669,1.82435859844906,-29.6103209493753));
#40709=CARTESIAN_POINT('Ctrl Pts',(6.46646633415585,2.00292240086808,-29.6015717792453));
#40710=CARTESIAN_POINT('Ctrl Pts',(6.40657319597112,2.1790155769669,-29.5928226091153));
#40711=CARTESIAN_POINT('Ctrl Pts',(6.34668083768208,2.35510646007669,-29.5840735529122));
#40712=CARTESIAN_POINT('Ctrl Pts',(6.27952437143792,2.52872650996763,-29.5753244967091));
#40713=CARTESIAN_POINT('Ctrl Pts',(6.20533187335035,2.69928607998156,-29.5665754405061));
#40714=CARTESIAN_POINT('Ctrl Pts',(6.1283144978415,2.87633970115614,-29.5574932642172));
#40715=CARTESIAN_POINT('Ctrl Pts',(6.0437148946305,3.05009490562553,-29.5484110879284));
#40716=CARTESIAN_POINT('Ctrl Pts',(5.95184265120387,3.21991584599822,-29.5393289116395));
#40717=CARTESIAN_POINT('Ctrl Pts',(5.86333281335381,3.38352155905493,-29.5305791312851));
#40718=CARTESIAN_POINT('Ctrl Pts',(5.76807337235566,3.54347560904018,-29.5218293509307));
#40719=CARTESIAN_POINT('Ctrl Pts',(5.66638790086228,3.69923467178841,-29.5130795705763));
#40720=CARTESIAN_POINT('Ctrl Pts',(5.5647060850261,3.85498813489955,-29.504330104782));
#40721=CARTESIAN_POINT('Ctrl Pts',(5.45659885766815,4.00654667256449,-29.4955806389878));
#40722=CARTESIAN_POINT('Ctrl Pts',(5.34243340580365,4.15339551506394,-29.4868311731935));
#40723=CARTESIAN_POINT('Ctrl Pts',(5.22827145140433,4.30023985884067,-29.4780819754396));
#40724=CARTESIAN_POINT('Ctrl Pts',(5.1080518197791,4.4423745699325,-29.4693327776857));
#40725=CARTESIAN_POINT('Ctrl Pts',(4.98218281282352,4.57931691626666,-29.4605835799319));
#40726=CARTESIAN_POINT('Ctrl Pts',(4.85631699296011,4.71625579512387,-29.4518346037138));
#40727=CARTESIAN_POINT('Ctrl Pts',(4.724802277916,4.84800236136002,-29.4430856274958));
#40728=CARTESIAN_POINT('Ctrl Pts',(4.58808530847855,4.97410918679147,-29.4343366512778));
#40729=CARTESIAN_POINT('Ctrl Pts',(4.45135945056701,5.10022421089244,-29.4255871062566));
#40730=CARTESIAN_POINT('Ctrl Pts',(4.3094308720776,5.22069856612218,-29.4168375612354));
#40731=CARTESIAN_POINT('Ctrl Pts',(4.16278164322177,5.3351230530191,-29.4080880162142));
#40732=CARTESIAN_POINT('Ctrl Pts',(4.01614103534092,5.44954081331647,-29.399338985547));
#40733=CARTESIAN_POINT('Ctrl Pts',(3.86478055833106,5.55790924068551,-29.3905899548797));
#40734=CARTESIAN_POINT('Ctrl Pts',(3.70921425811636,5.65986029751498,-29.3818409242124));
#40735=CARTESIAN_POINT('Ctrl Pts',(3.55364584529798,5.76181273884852,-29.3730917747326));
#40736=CARTESIAN_POINT('Ctrl Pts',(3.39387173464017,5.85734747818253,-29.3643426252527));
#40737=CARTESIAN_POINT('Ctrl Pts',(3.23043456092071,5.94614005448989,-29.3555934757729));
#40738=CARTESIAN_POINT('Ctrl Pts',(3.18690768806169,5.969787448114,-29.3532633870399));
#40739=CARTESIAN_POINT('Ctrl Pts',(3.14312114982771,5.99295688499357,-29.3509332983069));
#40740=CARTESIAN_POINT('Ctrl Pts',(3.09908550384723,6.01564277861011,-29.348603209574));
#40741=CARTESIAN_POINT('Origin',(0.,0.,-63.6971797838103));
#40742=CARTESIAN_POINT('',(3.09908550384719,6.01564277861013,-26.9540130953596));
#40743=CARTESIAN_POINT('',(3.09908550384723,6.01564277861011,-27.3486843298454));
#40744=CARTESIAN_POINT('',(3.09908550384721,6.01564277861012,-63.6971797838103));
#40745=CARTESIAN_POINT('',(-6.76699602342832,-0.00733613694335467,-28.3028202162144));
#40746=CARTESIAN_POINT('Ctrl Pts',(-6.76699602342776,-0.00733613746203318,
-28.3028202161899));
#40747=CARTESIAN_POINT('Ctrl Pts',(-6.76676555142464,-0.219928000235072,
-28.2927712501011));
#40748=CARTESIAN_POINT('Ctrl Pts',(-6.75651764005179,-0.432142597509886,
-28.2827222840123));
#40749=CARTESIAN_POINT('Ctrl Pts',(-6.73635434321315,-0.643287775939668,
-28.2726733179236));
#40750=CARTESIAN_POINT('Ctrl Pts',(-6.71963244938501,-0.818395412566786,
-28.2643394752309));
#40751=CARTESIAN_POINT('Ctrl Pts',(-6.6960571440256,-0.993074637253249,
-28.2560056325382));
#40752=CARTESIAN_POINT('Ctrl Pts',(-6.66565593329613,-1.16675617800557,
-28.2476717898455));
#40753=CARTESIAN_POINT('Ctrl Pts',(-6.63529055423959,-1.34023301308947,
-28.2393477696408));
#40754=CARTESIAN_POINT('Ctrl Pts',(-6.59811535603069,-1.51271416701442,
-28.2310237494361));
#40755=CARTESIAN_POINT('Ctrl Pts',(-6.55420967939453,-1.68363430665067,
-28.2226997292313));
#40756=CARTESIAN_POINT('Ctrl Pts',(-6.51034770111078,-1.85438433323848,
-28.2143839937404));
#40757=CARTESIAN_POINT('Ctrl Pts',(-6.45976867644582,-2.02357610609857,
-28.2060682582496));
#40758=CARTESIAN_POINT('Ctrl Pts',(-6.40260322104912,-2.19065309755139,
-28.1977525227587));
#40759=CARTESIAN_POINT('Ctrl Pts',(-6.3454841869831,-2.35759441377488,-28.1894435400787));
#40760=CARTESIAN_POINT('Ctrl Pts',(-6.28178949175138,-2.52242404280815,
-28.1811345573986));
#40761=CARTESIAN_POINT('Ctrl Pts',(-6.21170000276441,-2.68459905305365,
-28.1728255747186));
#40762=CARTESIAN_POINT('Ctrl Pts',(-6.14165459494374,-2.84667206706981,
-28.1645218177815));
#40763=CARTESIAN_POINT('Ctrl Pts',(-6.065222546109,-3.00609347116171,-28.1562180608443));
#40764=CARTESIAN_POINT('Ctrl Pts',(-5.98263349844512,-3.16233860035296,
-28.1479143039072));
#40765=CARTESIAN_POINT('Ctrl Pts',(-5.9000779799436,-3.3185202977884,-28.1396139180951));
#40766=CARTESIAN_POINT('Ctrl Pts',(-5.81137060553026,-3.47152798271818,
-28.1313135322831));
#40767=CARTESIAN_POINT('Ctrl Pts',(-5.71678790923481,-3.62085970465948,
-28.1230131464711));
#40768=CARTESIAN_POINT('Ctrl Pts',(-5.62222515796898,-3.77015993642621,
-28.1147145109945));
#40769=CARTESIAN_POINT('Ctrl Pts',(-5.52178973910362,-3.91578545587575,
-28.1064158755178));
#40770=CARTESIAN_POINT('Ctrl Pts',(-5.4158027636553,-4.05726132079061,-28.0981172400412));
#40771=CARTESIAN_POINT('Ctrl Pts',(-5.30982054548079,-4.19873083549666,
-28.0898189770526));
#40772=CARTESIAN_POINT('Ctrl Pts',(-5.19828747593302,-4.33605078861525,
-28.0815207140641));
#40773=CARTESIAN_POINT('Ctrl Pts',(-5.08156649910743,-4.4687773400729,-28.0732224510755));
#40774=CARTESIAN_POINT('Ctrl Pts',(-4.96483138786964,-4.60151996414955,
-28.0649231832026));
#40775=CARTESIAN_POINT('Ctrl Pts',(-4.84290734763171,-4.7296678174379,-28.0566239153298));
#40776=CARTESIAN_POINT('Ctrl Pts',(-4.71619602803271,-4.8528119709266,-28.048324647457));
#40777=CARTESIAN_POINT('Ctrl Pts',(-4.58939573666474,-4.97604259145872,
-28.0400195521605));
#40778=CARTESIAN_POINT('Ctrl Pts',(-4.45780169889509,-5.09426224911316,
-28.031714456864));
#40779=CARTESIAN_POINT('Ctrl Pts',(-4.32185133935365,-5.20709996068129,
-28.0234093615675));
#40780=CARTESIAN_POINT('Ctrl Pts',(-4.1858514052418,-5.31997881874654,-28.0151012378014));
#40781=CARTESIAN_POINT('Ctrl Pts',(-4.04549225547649,-5.42747160272777,
-28.0067931140353));
#40782=CARTESIAN_POINT('Ctrl Pts',(-3.9012426614008,-5.52924901744047,-27.9984849902692));
#40783=CARTESIAN_POINT('Ctrl Pts',(-3.75683973083989,-5.63113462095708,
-27.9901680350156));
#40784=CARTESIAN_POINT('Ctrl Pts',(-3.60853838187039,-5.7272925221305,-27.9818510797619));
#40785=CARTESIAN_POINT('Ctrl Pts',(-3.45683541949477,-5.81743739824731,
-27.9735341245082));
#40786=CARTESIAN_POINT('Ctrl Pts',(-3.34503264432766,-5.88387280042489,
-27.9674046550256));
#40787=CARTESIAN_POINT('Ctrl Pts',(-3.2313828680445,-5.94704317520922,-27.961275185543));
#40788=CARTESIAN_POINT('Ctrl Pts',(-3.11609268191041,-6.00685070546492,
-27.9551457160604));
#40789=CARTESIAN_POINT('Ctrl Pts',(-2.95713600906782,-6.08931050832551,
-27.9466946925352));
#40790=CARTESIAN_POINT('Ctrl Pts',(-2.79476971361754,-6.16552663204085,
-27.93824366901));
#40791=CARTESIAN_POINT('Ctrl Pts',(-2.6295113109288,-6.23521926364242,-27.9297926454848));
#40792=CARTESIAN_POINT('Ctrl Pts',(-2.4643984133519,-6.30485053295324,-27.9213490628347));
#40793=CARTESIAN_POINT('Ctrl Pts',(-2.29639878804057,-6.36796963030381,
-27.9129054801845));
#40794=CARTESIAN_POINT('Ctrl Pts',(-2.12605320903425,-6.42434329347017,
-27.9044618975343));
#40795=CARTESIAN_POINT('Ctrl Pts',(-1.95583445761778,-6.48067498468827,
-27.8960246013945));
#40796=CARTESIAN_POINT('Ctrl Pts',(-1.78327354801447,-6.53027114940594,
-27.8875873052546));
#40797=CARTESIAN_POINT('Ctrl Pts',(-1.60893020449224,-6.57294702527508,
-27.8791500091148));
#40798=CARTESIAN_POINT('Ctrl Pts',(-1.43471124165274,-6.61559245516063,
-27.8707187323424));
#40799=CARTESIAN_POINT('Ctrl Pts',(-1.25871270257502,-6.65132736544411,
-27.86228745557));
#40800=CARTESIAN_POINT('Ctrl Pts',(-1.08150860985812,-6.68001707533767,
-27.8538561787977));
#40801=CARTESIAN_POINT('Ctrl Pts',(-0.904380473229808,-6.70869448778305,
-27.8454285159757));
#40802=CARTESIAN_POINT('Ctrl Pts',(-0.726048139738801,-6.73033266712018,
-27.8370008531538));
#40803=CARTESIAN_POINT('Ctrl Pts',(-0.547095591389842,-6.74484806455133,
-27.8285731903318));
#40804=CARTESIAN_POINT('Ctrl Pts',(-0.368198131713365,-6.75935899356902,
-27.8201481218778));
#40805=CARTESIAN_POINT('Ctrl Pts',(-0.188681167948277,-6.76675148666101,
-27.8117230534238));
#40806=CARTESIAN_POINT('Ctrl Pts',(-0.00913394119624452,-6.76699383560516,
-27.8032979849698));
#40807=CARTESIAN_POINT('Ctrl Pts',(0.0399956758395798,-6.76706014969439,
-27.8009926283563));
#40808=CARTESIAN_POINT('Ctrl Pts',(0.0891275412486155,-6.76659140642043,
-27.7986872717427));
#40809=CARTESIAN_POINT('Ctrl Pts',(0.138249557663999,-6.76558763595637,
-27.7963819151291));
#40810=CARTESIAN_POINT('Ctrl Pts',(0.321901012404443,-6.76183486032942,
-27.7877629266046));
#40811=CARTESIAN_POINT('Ctrl Pts',(0.505332709507144,-6.7506013072657,-27.7791439380802));
#40812=CARTESIAN_POINT('Ctrl Pts',(0.687930573940023,-6.7319418094216,-27.7705249495557));
#40813=CARTESIAN_POINT('Ctrl Pts',(0.870637830788935,-6.71327113287309,
-27.761900797488));
#40814=CARTESIAN_POINT('Ctrl Pts',(1.05250995546141,-6.68716566400971,-27.7532766454202));
#40815=CARTESIAN_POINT('Ctrl Pts',(1.23294001473092,-6.65373187918444,-27.7446524933525));
#40816=CARTESIAN_POINT('Ctrl Pts',(1.4195498520723,-6.61915297823408,-27.7357329617562));
#40817=CARTESIAN_POINT('Ctrl Pts',(1.60461674238068,-6.57673495314702,-27.7268134301599));
#40818=CARTESIAN_POINT('Ctrl Pts',(1.78748355630071,-6.52665239889138,-27.7178938985637));
#40819=CARTESIAN_POINT('Ctrl Pts',(1.96462392454099,-6.47813817198995,-27.7092536807044));
#40820=CARTESIAN_POINT('Ctrl Pts',(2.13969964485953,-6.42243231477914,-27.7006134628452));
#40821=CARTESIAN_POINT('Ctrl Pts',(2.31213091461799,-6.3597436767269,-27.691973244986));
#40822=CARTESIAN_POINT('Ctrl Pts',(2.49292350519993,-6.29401521987917,-27.6829140565212));
#40823=CARTESIAN_POINT('Ctrl Pts',(2.67080844790044,-6.22061009361683,-27.6738548680564));
#40824=CARTESIAN_POINT('Ctrl Pts',(2.84514282360538,-6.13982502301872,-27.6647956795917));
#40825=CARTESIAN_POINT('Ctrl Pts',(3.01947719931033,-6.0590399524206,-27.6557364911269));
#40826=CARTESIAN_POINT('Ctrl Pts',(3.19026068322077,-5.97087514244076,-27.6466773026621));
#40827=CARTESIAN_POINT('Ctrl Pts',(3.35688129178983,-5.8756818321648,-27.6376181141973));
#40828=CARTESIAN_POINT('Ctrl Pts',(3.52321324184415,-5.7806534376204,-27.628574620141));
#40829=CARTESIAN_POINT('Ctrl Pts',(3.6855503812889,-5.67853406541888,-27.6195311260847));
#40830=CARTESIAN_POINT('Ctrl Pts',(3.84331625777254,-5.56966867441335,-27.6104876320284));
#40831=CARTESIAN_POINT('Ctrl Pts',(4.00093782638581,-5.46090286218291,-27.601452410023));
#40832=CARTESIAN_POINT('Ctrl Pts',(4.153996284261,-5.34540348579733,-27.5924171880176));
#40833=CARTESIAN_POINT('Ctrl Pts',(4.30194381513703,-5.22355897941282,-27.5833819660122));
#40834=CARTESIAN_POINT('Ctrl Pts',(4.4496306946715,-5.10192913652328,-27.5743626621011));
#40835=CARTESIAN_POINT('Ctrl Pts',(4.59222444421059,-4.97397663734442,-27.5653433581899));
#40836=CARTESIAN_POINT('Ctrl Pts',(4.7292101174876,-4.84013023219964,-27.5563240542788));
#40837=CARTESIAN_POINT('Ctrl Pts',(4.86602393266931,-4.70645174671902,-27.5473160657144));
#40838=CARTESIAN_POINT('Ctrl Pts',(4.99724354268756,-4.56689427768299,-27.5383080771499));
#40839=CARTESIAN_POINT('Ctrl Pts',(5.12238877167882,-4.42192517708959,-27.5293000885855));
#40840=CARTESIAN_POINT('Ctrl Pts',(5.24725135578692,-4.27728349428773,-27.5203124448788));
#40841=CARTESIAN_POINT('Ctrl Pts',(5.36606678835974,-4.12725475676875,-27.5113248011721));
#40842=CARTESIAN_POINT('Ctrl Pts',(5.47839360298146,-3.97234093839034,-27.5023371574654));
#40843=CARTESIAN_POINT('Ctrl Pts',(5.57622247312257,-3.83742173969105,-27.4945095427323));
#40844=CARTESIAN_POINT('Ctrl Pts',(5.66913006210312,-3.69879774835549,-27.4866819279991));
#40845=CARTESIAN_POINT('Ctrl Pts',(5.75684829687764,-3.55682255485666,-27.478854313266));
#40846=CARTESIAN_POINT('Ctrl Pts',(5.84787846940244,-3.40948686813585,-27.4707311548207));
#40847=CARTESIAN_POINT('Ctrl Pts',(5.93327791108822,-3.25860712323924,-27.4626079963754));
#40848=CARTESIAN_POINT('Ctrl Pts',(6.01276744062879,-3.10466048142374,-27.4544848379301));
#40849=CARTESIAN_POINT('Ctrl Pts',(6.09225136574148,-2.95072469365226,-27.44636225221));
#40850=CARTESIAN_POINT('Ctrl Pts',(6.16582604076437,-2.79372276490383,-27.4382396664899));
#40851=CARTESIAN_POINT('Ctrl Pts',(6.23325843401677,-2.63415608777438,-27.4301170807698));
#40852=CARTESIAN_POINT('Ctrl Pts',(6.30069892996536,-2.47457023706612,-27.4219935190374));
#40853=CARTESIAN_POINT('Ctrl Pts',(6.36199553312253,-2.31241936193011,-27.413869957305));
#40854=CARTESIAN_POINT('Ctrl Pts',(6.41696353120311,-2.14822439219215,-27.4057463955726));
#40855=CARTESIAN_POINT('Ctrl Pts',(6.47197156694739,-1.9839098259033,-27.3976169167895));
#40856=CARTESIAN_POINT('Ctrl Pts',(6.52064167464196,-1.81754853877116,-27.3894874380064));
#40857=CARTESIAN_POINT('Ctrl Pts',(6.56283898308723,-1.64967678109096,-27.3813579592233));
#40858=CARTESIAN_POINT('Ctrl Pts',(6.60505349463245,-1.48173658504981,-27.3732251661947));
#40859=CARTESIAN_POINT('Ctrl Pts',(6.64078987144616,-1.31228504889536,-27.3650923731662));
#40860=CARTESIAN_POINT('Ctrl Pts',(6.66996452079699,-1.14186789573464,-27.3569595801377));
#40861=CARTESIAN_POINT('Ctrl Pts',(6.69917089315295,-0.971265439773515,
-27.3488179439305));
#40862=CARTESIAN_POINT('Ctrl Pts',(6.72180123960825,-0.799695632130619,
-27.3406763077234));
#40863=CARTESIAN_POINT('Ctrl Pts',(6.73782383170312,-0.627709337937163,
-27.3325346715163));
#40864=CARTESIAN_POINT('Ctrl Pts',(6.74598712474247,-0.540084657115235,
-27.3283866184556));
#40865=CARTESIAN_POINT('Ctrl Pts',(6.75243603773168,-0.452351885714152,
-27.324238565395));
#40866=CARTESIAN_POINT('Ctrl Pts',(6.7571715750192,-0.364583743127011,-27.3200905123343));
#40867=CARTESIAN_POINT('Ctrl Pts',(6.76680773924558,-0.1859876970055,-27.3116497973562));
#40868=CARTESIAN_POINT('Ctrl Pts',(6.76936609789953,-0.00687742669364791,
-27.3032090823781));
#40869=CARTESIAN_POINT('Ctrl Pts',(6.76480963877645,0.172161410069907,-27.2947683674001));
#40870=CARTESIAN_POINT('Ctrl Pts',(6.76025662363985,0.351064920845359,-27.286334032312));
#40871=CARTESIAN_POINT('Ctrl Pts',(6.74859951932881,0.52989677359061,-27.277899697224));
#40872=CARTESIAN_POINT('Ctrl Pts',(6.72985334847792,0.708069846823457,-27.269465362136));
#40873=CARTESIAN_POINT('Ctrl Pts',(6.71111846817762,0.886135608962445,-27.2610361069273));
#40874=CARTESIAN_POINT('Ctrl Pts',(6.68530306831416,1.06354305186015,-27.2526068517187));
#40875=CARTESIAN_POINT('Ctrl Pts',(6.65247414806712,1.23970831621745,-27.2441775965101));
#40876=CARTESIAN_POINT('Ctrl Pts',(6.61965996450019,1.41579450117988,-27.2357521251371));
#40877=CARTESIAN_POINT('Ctrl Pts',(6.57983859895231,1.59063929218077,-27.2273266537641));
#40878=CARTESIAN_POINT('Ctrl Pts',(6.53312853419137,1.76366679271754,-27.218901182391));
#40879=CARTESIAN_POINT('Ctrl Pts',(6.48643227828065,1.93664314130556,-27.2104782018318));
#40880=CARTESIAN_POINT('Ctrl Pts',(6.43285147120553,2.10780294926773,-27.2020552212725));
#40881=CARTESIAN_POINT('Ctrl Pts',(6.37255515602749,2.27658291818844,-27.1936322407133));
#40882=CARTESIAN_POINT('Ctrl Pts',(6.31225784246759,2.44536568175523,-27.185209120687));
#40883=CARTESIAN_POINT('Ctrl Pts',(6.2452449045544,2.61176821142514,-27.1767860006606));
#40884=CARTESIAN_POINT('Ctrl Pts',(6.17173470796589,2.77524407836306,-27.1683628806343));
#40885=CARTESIAN_POINT('Ctrl Pts',(6.09822196927221,2.93872559856902,-27.1599394693224));
#40886=CARTESIAN_POINT('Ctrl Pts',(6.01821166053042,3.09927995000798,-27.1515160580106));
#40887=CARTESIAN_POINT('Ctrl Pts',(5.9319696550329,3.2563821968204,-27.1430926466987));
#40888=CARTESIAN_POINT('Ctrl Pts',(5.84571263942648,3.41351178671026,-27.1346677693226));
#40889=CARTESIAN_POINT('Ctrl Pts',(5.75322192516306,3.56718778176935,-27.1262428919465));
#40890=CARTESIAN_POINT('Ctrl Pts',(5.65480873343709,3.71691097394646,-27.1178180145703));
#40891=CARTESIAN_POINT('Ctrl Pts',(5.55636468384588,3.86668111245268,-27.1093904955389));
#40892=CARTESIAN_POINT('Ctrl Pts',(5.45199463750489,4.01249569844281,-27.1009629765075));
#40893=CARTESIAN_POINT('Ctrl Pts',(5.34205261947399,4.15388526692434,-27.092535457476));
#40894=CARTESIAN_POINT('Ctrl Pts',(5.2320120096904,4.29540162810642,-27.0841003809713));
#40895=CARTESIAN_POINT('Ctrl Pts',(5.11638964894084,4.43248477926204,-27.0756653044665));
#40896=CARTESIAN_POINT('Ctrl Pts',(4.99557999268886,4.56469818680784,-27.0672302279617));
#40897=CARTESIAN_POINT('Ctrl Pts',(4.87471194833497,4.6969754939636,-27.0587910747289));
#40898=CARTESIAN_POINT('Ctrl Pts',(4.74865183921287,4.82437812303524,-27.0503519214961));
#40899=CARTESIAN_POINT('Ctrl Pts',(4.61783069589847,4.94650671322883,-27.0419127682634));
#40900=CARTESIAN_POINT('Ctrl Pts',(4.48686417361529,5.06877102252754,-27.0334642367652));
#40901=CARTESIAN_POINT('Ctrl Pts',(4.35112629457193,5.18574936040683,-27.0250157052671));
#40902=CARTESIAN_POINT('Ctrl Pts',(4.21108176802987,5.29708215369239,-27.016567173769));
#40903=CARTESIAN_POINT('Ctrl Pts',(4.13370262336073,5.35859713418308,-27.0118990860031));
#40904=CARTESIAN_POINT('Ctrl Pts',(4.05500924032428,5.41838931959196,-27.0072309982372));
#40905=CARTESIAN_POINT('Ctrl Pts',(3.97508375785797,5.47640375776054,-27.0025629104713));
#40906=CARTESIAN_POINT('Ctrl Pts',(3.83400746665901,5.57880491344033,-26.9943232791461));
#40907=CARTESIAN_POINT('Ctrl Pts',(3.68877700289684,5.67589260201036,-26.986083647821));
#40908=CARTESIAN_POINT('Ctrl Pts',(3.53982801636344,5.76731363934445,-26.9778440164958));
#40909=CARTESIAN_POINT('Ctrl Pts',(3.39622970023635,5.85545057350763,-26.9699003761171));
#40910=CARTESIAN_POINT('Ctrl Pts',(3.24917563626411,5.938320675094,-26.9619567357384));
#40911=CARTESIAN_POINT('Ctrl Pts',(3.09908550384719,6.01564277861013,-26.9540130953596));
#40912=CARTESIAN_POINT('Ctrl Pts',(3.09908550384723,6.01564277861011,-28.9543744409077));
#40913=CARTESIAN_POINT('Ctrl Pts',(2.93074066342593,6.10236918072498,-28.9454409168082));
#40914=CARTESIAN_POINT('Ctrl Pts',(2.75887803291552,6.18196094278929,-28.9365073927087));
#40915=CARTESIAN_POINT('Ctrl Pts',(2.58410552795895,6.25417361610405,-28.9275738686092));
#40916=CARTESIAN_POINT('Ctrl Pts',(2.4546895975365,6.30764581590827,-28.920958752956));
#40917=CARTESIAN_POINT('Ctrl Pts',(2.32367854641631,6.35707296890079,-28.9143436373028));
#40918=CARTESIAN_POINT('Ctrl Pts',(2.19132453108998,6.40237345048251,-28.9077285216496));
#40919=CARTESIAN_POINT('Ctrl Pts',(2.02678076599642,6.45869143812821,-28.8995045472321));
#40920=CARTESIAN_POINT('Ctrl Pts',(1.85984636351425,6.5087367461534,-28.8912805728145));
#40921=CARTESIAN_POINT('Ctrl Pts',(1.69104018799337,6.55230280760828,-28.8830565983969));
#40922=CARTESIAN_POINT('Ctrl Pts',(1.52241228817216,6.5958228590753,-28.8748413092943));
#40923=CARTESIAN_POINT('Ctrl Pts',(1.35191689607876,6.63287720124364,-28.8666260201916));
#40924=CARTESIAN_POINT('Ctrl Pts',(1.18009075940021,6.66330809730259,-28.858410731089));
#40925=CARTESIAN_POINT('Ctrl Pts',(1.00841162313236,6.69371295917195,-28.8502024703168));
#40926=CARTESIAN_POINT('Ctrl Pts',(0.835404360778233,6.71750559811737,-28.8419942095446));
#40927=CARTESIAN_POINT('Ctrl Pts',(0.66161880973207,6.73457864685006,-28.8337859487724));
#40928=CARTESIAN_POINT('Ctrl Pts',(0.48794708766042,6.75164051279098,-28.8255830643845));
#40929=CARTESIAN_POINT('Ctrl Pts',(0.313498447920012,6.76199152053251,-28.8173801799966));
#40930=CARTESIAN_POINT('Ctrl Pts',(0.138830895033099,6.76557573178989,-28.8091772956087));
#40931=CARTESIAN_POINT('Ctrl Pts',(-0.0357572686251395,6.76915831396527,
-28.8009781395645));
#40932=CARTESIAN_POINT('Ctrl Pts',(-0.210563789420254,6.76598021974895,
-28.7927789835203));
#40933=CARTESIAN_POINT('Ctrl Pts',(-0.385027498984551,6.75603750914881,
-28.784579827476));
#40934=CARTESIAN_POINT('Ctrl Pts',(-0.559476034448037,6.74609566332276,
-28.776381384559));
#40935=CARTESIAN_POINT('Ctrl Pts',(-0.733581459842993,6.7293903849033,-28.768182941642));
#40936=CARTESIAN_POINT('Ctrl Pts',(-0.906784197880069,6.70596983429504,
-28.759984498725));
#40937=CARTESIAN_POINT('Ctrl Pts',(-1.07998521102291,6.68254951692774,-28.7517861374548));
#40938=CARTESIAN_POINT('Ctrl Pts',(-1.25228319910867,6.65241410759397,-28.7435877761846));
#40939=CARTESIAN_POINT('Ctrl Pts',(-1.42312540678331,6.61566346457918,-28.7353894149143));
#40940=CARTESIAN_POINT('Ctrl Pts',(-1.59399694778214,6.57890651153984,-28.7271896459991));
#40941=CARTESIAN_POINT('Ctrl Pts',(-1.76341185970093,6.53553213736093,-28.7189898770838));
#40942=CARTESIAN_POINT('Ctrl Pts',(-1.93082919855987,6.48569098909196,-28.7107901081685));
#40943=CARTESIAN_POINT('Ctrl Pts',(-2.09830569557285,6.43583222908489,-28.7025874418043));
#40944=CARTESIAN_POINT('Ctrl Pts',(-2.26378286987201,6.37950224534938,-28.6943847754401));
#40945=CARTESIAN_POINT('Ctrl Pts',(-2.42673646242253,6.31690107109087,-28.6861821090758));
#40946=CARTESIAN_POINT('Ctrl Pts',(-2.58987512952515,6.25422879754511,-28.6779701265328));
#40947=CARTESIAN_POINT('Ctrl Pts',(-2.75048415367643,6.18527123286659,-28.6697581439898));
#40948=CARTESIAN_POINT('Ctrl Pts',(-2.90805977032927,6.11027637445251,-28.6615461614468));
#40949=CARTESIAN_POINT('Ctrl Pts',(-3.0657283272101,6.03523728305754,-28.6533293353655));
#40950=CARTESIAN_POINT('Ctrl Pts',(-3.22035959304848,5.95415396612532,-28.6451125092842));
#40951=CARTESIAN_POINT('Ctrl Pts',(-3.3714759373419,5.86731957574535,-28.6368956832029));
#40952=CARTESIAN_POINT('Ctrl Pts',(-3.52282532486363,5.7803512741941,-28.628666185589));
#40953=CARTESIAN_POINT('Ctrl Pts',(-3.6706486550626,5.68761436624255,-28.6204366879752));
#40954=CARTESIAN_POINT('Ctrl Pts',(-3.814497632205,5.58944512576181,-28.6122071903614));
#40955=CARTESIAN_POINT('Ctrl Pts',(-3.94271848121428,5.50194124765932,-28.6048717668364));
#40956=CARTESIAN_POINT('Ctrl Pts',(-4.06778194823807,5.41012197708436,-28.5975363433115));
#40957=CARTESIAN_POINT('Ctrl Pts',(-4.18939427405906,5.31425108707532,-28.5902009197866));
#40958=CARTESIAN_POINT('Ctrl Pts',(-4.32169451661494,5.20995457011769,-28.5822208215108));
#40959=CARTESIAN_POINT('Ctrl Pts',(-4.45036072809953,5.10050658472618,-28.574240723235));
#40960=CARTESIAN_POINT('Ctrl Pts',(-4.57494775252778,4.98619514877237,-28.5662606249592));
#40961=CARTESIAN_POINT('Ctrl Pts',(-4.6993801079693,4.87202562514088,-28.5582904336037));
#40962=CARTESIAN_POINT('Ctrl Pts',(-4.81974307204676,4.75300491405228,-28.5503202422481));
#40963=CARTESIAN_POINT('Ctrl Pts',(-4.93562074350316,4.62946399449238,-28.5423500508926));
#40964=CARTESIAN_POINT('Ctrl Pts',(-5.05138093085121,4.50604832852617,-28.5343879402209));
#40965=CARTESIAN_POINT('Ctrl Pts',(-5.16266461369269,4.37812184624029,-28.5264258295491));
#40966=CARTESIAN_POINT('Ctrl Pts',(-5.2690894278619,4.24605529888554,-28.5184637188774));
#40967=CARTESIAN_POINT('Ctrl Pts',(-5.37543048518111,4.1140926885504,-28.5105078744258));
#40968=CARTESIAN_POINT('Ctrl Pts',(-5.47692004453577,3.97799679110307,-28.5025520299742));
#40969=CARTESIAN_POINT('Ctrl Pts',(-5.5732132071822,3.83817450714398,-28.4945961855226));
#40970=CARTESIAN_POINT('Ctrl Pts',(-5.66992782327639,3.69774025259395,-28.4866055201347));
#40971=CARTESIAN_POINT('Ctrl Pts',(-5.76140017579024,3.55354719239718,-28.4786148547469));
#40972=CARTESIAN_POINT('Ctrl Pts',(-5.84732194109161,3.40604097409715,-28.470624189359));
#40973=CARTESIAN_POINT('Ctrl Pts',(-5.93280275843591,3.25929175334467,-28.4626745318295));
#40974=CARTESIAN_POINT('Ctrl Pts',(-6.01278963937287,3.10926363788242,-28.4547248743));
#40975=CARTESIAN_POINT('Ctrl Pts',(-6.08702289982685,2.95642372081263,-28.4467752167705));
#40976=CARTESIAN_POINT('Ctrl Pts',(-6.16125164055588,2.80359310946888,-28.4388260432594));
#40977=CARTESIAN_POINT('Ctrl Pts',(-6.2297272909782,2.64795137992276,-28.4308768697483));
#40978=CARTESIAN_POINT('Ctrl Pts',(-6.29223687319425,2.48998878142345,-28.4229276962372));
#40979=CARTESIAN_POINT('Ctrl Pts',(-6.35475543993098,2.33200347891328,-28.4149773801891));
#40980=CARTESIAN_POINT('Ctrl Pts',(-6.41130609288055,2.17169699852571,-28.4070270641409));
#40981=CARTESIAN_POINT('Ctrl Pts',(-6.46172469727903,2.0095778005776,-28.3990767480928));
#40982=CARTESIAN_POINT('Ctrl Pts',(-6.51259395384014,1.84600954690824,-28.3910553704362));
#40983=CARTESIAN_POINT('Ctrl Pts',(-6.55722088757064,1.68059638973622,-28.3830339927797));
#40984=CARTESIAN_POINT('Ctrl Pts',(-6.59548907831681,1.51387344841095,-28.3750126151232));
#40985=CARTESIAN_POINT('Ctrl Pts',(-6.63346996163374,1.34840221872225,-28.3670514598432));
#40986=CARTESIAN_POINT('Ctrl Pts',(-6.66518724716878,1.18164119134741,-28.3590903045632));
#40987=CARTESIAN_POINT('Ctrl Pts',(-6.69057910139988,1.0141204503959,-28.3511291492833));
#40988=CARTESIAN_POINT('Ctrl Pts',(-6.71625907169329,0.844698886613637,
-28.3430776604385));
#40989=CARTESIAN_POINT('Ctrl Pts',(-6.73546915322974,0.674500664825639,
-28.3350261715937));
#40990=CARTESIAN_POINT('Ctrl Pts',(-6.74819954296709,0.504075320065096,
-28.3269746827488));
#40991=CARTESIAN_POINT('Ctrl Pts',(-6.76092993270445,0.333649975304522,
-28.318923193904));
#40992=CARTESIAN_POINT('Ctrl Pts',(-6.76718068348335,0.162997905035864,
-28.3108717050592));
#40993=CARTESIAN_POINT('Ctrl Pts',(-6.76699602342832,-0.00733613694335302,
-28.3028202162144));
#40994=CARTESIAN_POINT('',(-6.76716557178108,-0.00065835778244856,-28.6968932965683));
#40995=CARTESIAN_POINT('Ctrl Pts',(3.09908550384723,6.01564277861011,-29.348603209574));
#40996=CARTESIAN_POINT('Ctrl Pts',(2.9337323201833,6.10082796552479,-29.3398537616747));
#40997=CARTESIAN_POINT('Ctrl Pts',(2.76486502144426,6.1791915818019,-29.3311043137754));
#40998=CARTESIAN_POINT('Ctrl Pts',(2.59305716434351,6.25046746591379,-29.3223548658761));
#40999=CARTESIAN_POINT('Ctrl Pts',(2.42125069459283,6.32174277447224,-29.3136054886287));
#41000=CARTESIAN_POINT('Ctrl Pts',(2.2465039787106,6.38593035557825,-29.3048561113812));
#41001=CARTESIAN_POINT('Ctrl Pts',(2.06941053323774,6.44281220003538,-29.2961067341338));
#41002=CARTESIAN_POINT('Ctrl Pts',(1.89231845896683,6.49969360406686,-29.2873574246312));
#41003=CARTESIAN_POINT('Ctrl Pts',(1.71287996431501,6.54926929700882,-29.2786081151286));
#41004=CARTESIAN_POINT('Ctrl Pts',(1.53170449173496,6.59137090065481,-29.269858805626));
#41005=CARTESIAN_POINT('Ctrl Pts',(1.35053036178162,6.63347219230085,-29.2611095609614));
#41006=CARTESIAN_POINT('Ctrl Pts',(1.16761955878835,6.66809944062456,-29.2523603162969));
#41007=CARTESIAN_POINT('Ctrl Pts',(0.983593309310392,6.69513503985393,-29.2436110716323));
#41008=CARTESIAN_POINT('Ctrl Pts',(0.799568362459799,6.72217044771217,-29.2348618888991));
#41009=CARTESIAN_POINT('Ctrl Pts',(0.614428268438325,6.7416142723598,-29.2261127061659));
#41010=CARTESIAN_POINT('Ctrl Pts',(0.428801816329911,6.75340047696804,-29.2173635234327));
#41011=CARTESIAN_POINT('Ctrl Pts',(0.243176616522344,6.76518660206244,-29.2086143997246));
#41012=CARTESIAN_POINT('Ctrl Pts',(0.0570653511649389,6.76931519233997,
-29.1998652760165));
#41013=CARTESIAN_POINT('Ctrl Pts',(-0.128899900800633,6.76577222610794,
-29.1911161523083));
#41014=CARTESIAN_POINT('Ctrl Pts',(-0.314863959942703,6.7622292826013,-29.1823670847191));
#41015=CARTESIAN_POINT('Ctrl Pts',(-0.500681721081441,6.75101488651271,
-29.1736180171298));
#41016=CARTESIAN_POINT('Ctrl Pts',(-0.685722110174135,6.73216712415982,
-29.1648689495405));
#41017=CARTESIAN_POINT('Ctrl Pts',(-0.870761373828476,6.71331947644134,
-29.1561199351642));
#41018=CARTESIAN_POINT('Ctrl Pts',(-1.05502298984432,6.68683858439982,-29.1473709207878));
#41019=CARTESIAN_POINT('Ctrl Pts',(-1.23788117676151,6.65281438131409,-29.1386219064114));
#41020=CARTESIAN_POINT('Ctrl Pts',(-1.43009641451888,6.61704912302357,-29.1294251955239));
#41021=CARTESIAN_POINT('Ctrl Pts',(-1.62076048992794,6.57294837083141,-29.1202284846364));
#41022=CARTESIAN_POINT('Ctrl Pts',(-1.80915798961233,6.52067760042021,-29.1110317737488));
#41023=CARTESIAN_POINT('Ctrl Pts',(-1.98840443003115,6.47094578577377,-29.1022817760423));
#41024=CARTESIAN_POINT('Ctrl Pts',(-2.16559895952297,6.4138188847444,-29.0935317783358));
#41025=CARTESIAN_POINT('Ctrl Pts',(-2.34013966242429,6.34949095285195,-29.0847817806293));
#41026=CARTESIAN_POINT('Ctrl Pts',(-2.51467682554121,6.28516432556642,-29.0760319603777));
#41027=CARTESIAN_POINT('Ctrl Pts',(-2.68656000078947,6.21363705879615,-29.0672821401261));
#41028=CARTESIAN_POINT('Ctrl Pts',(-2.85520533840993,6.13515211510811,-29.0585323198745));
#41029=CARTESIAN_POINT('Ctrl Pts',(-3.02384747998429,6.0566686588107,-29.0497826654433));
#41030=CARTESIAN_POINT('Ctrl Pts',(-3.18925164684636,5.97122791039791,-29.041033011012));
#41031=CARTESIAN_POINT('Ctrl Pts',(-3.35085601829255,5.87912008251853,-29.0322833565808));
#41032=CARTESIAN_POINT('Ctrl Pts',(-3.51245754191513,5.78701387778117,-29.0235338563377));
#41033=CARTESIAN_POINT('Ctrl Pts',(-3.67025915511029,5.68824097060923,-29.0147843560945));
#41034=CARTESIAN_POINT('Ctrl Pts',(-3.82372487928925,5.58313684656793,-29.0060348558514));
#41035=CARTESIAN_POINT('Ctrl Pts',(-3.97718810300878,5.47803443501715,-28.9972854981663));
#41036=CARTESIAN_POINT('Ctrl Pts',(-4.12631534263096,5.36660117496322,-28.9885361404812));
#41037=CARTESIAN_POINT('Ctrl Pts',(-4.27060009886285,5.24921554097301,-28.979786782796));
#41038=CARTESIAN_POINT('Ctrl Pts',(-4.41488269594267,5.13183166360245,-28.9710375560409));
#41039=CARTESIAN_POINT('Ctrl Pts',(-4.55432273235136,5.00849577139427,-28.9622883292857));
#41040=CARTESIAN_POINT('Ctrl Pts',(-4.68844662480249,4.87962675277302,-28.9535391025305));
#41041=CARTESIAN_POINT('Ctrl Pts',(-4.82256868835199,4.7507594913984,-28.944789995079));
#41042=CARTESIAN_POINT('Ctrl Pts',(-4.95137454637903,4.61635945312482,-28.9360408876275));
#41043=CARTESIAN_POINT('Ctrl Pts',(-5.07442674461117,4.47688309134546,-28.927291780176));
#41044=CARTESIAN_POINT('Ctrl Pts',(-5.19747742838597,4.33740844616283,-28.9185427804037));
#41045=CARTESIAN_POINT('Ctrl Pts',(-5.31477440451002,4.19285781735936,-28.9097937806313));
#41046=CARTESIAN_POINT('Ctrl Pts',(-5.42591931531242,4.04372211999286,-28.9010447808589));
#41047=CARTESIAN_POINT('Ctrl Pts',(-5.53707636463076,3.89457013500667,-28.8922948255783));
#41048=CARTESIAN_POINT('Ctrl Pts',(-5.6420798327357,3.74083230916271,-28.8835448702977));
#41049=CARTESIAN_POINT('Ctrl Pts',(-5.7405730346885,3.58303087251663,-28.8747949150171));
#41050=CARTESIAN_POINT('Ctrl Pts',(-5.83906243363864,3.42523552887262,-28.8660452975883));
#41051=CARTESIAN_POINT('Ctrl Pts',(-5.93104191768521,3.26337713156819,-28.8572956801595));
#41052=CARTESIAN_POINT('Ctrl Pts',(-6.01619906699748,3.09800545290977,-28.8485460627307));
#41053=CARTESIAN_POINT('Ctrl Pts',(-6.10135338095468,2.93263928039419,-28.8397967366253));
#41054=CARTESIAN_POINT('Ctrl Pts',(-6.17968568352917,2.76376031540049,-28.8310474105199));
#41055=CARTESIAN_POINT('Ctrl Pts',(-6.25092992694958,2.59194213831369,-28.8222980844145));
#41056=CARTESIAN_POINT('Ctrl Pts',(-6.32217217691175,2.42012876880634,-28.8135490031207));
#41057=CARTESIAN_POINT('Ctrl Pts',(-6.38632665483921,2.24537661647471,-28.8047999218269));
#41058=CARTESIAN_POINT('Ctrl Pts',(-6.44317547869418,2.06827917621244,-28.7960508405331));
#41059=CARTESIAN_POINT('Ctrl Pts',(-6.50002944236,1.89116572423205,-28.7873009682182));
#41060=CARTESIAN_POINT('Ctrl Pts',(-6.54957634250457,1.71170683288974,-28.7785510959032));
#41061=CARTESIAN_POINT('Ctrl Pts',(-6.59164787708449,1.53051209225135,-28.7698012235882));
#41062=CARTESIAN_POINT('Ctrl Pts',(-6.63371649075056,1.34932993147799,-28.7610519587534));
#41063=CARTESIAN_POINT('Ctrl Pts',(-6.66831071257165,1.16641244173772,-28.7523026939186));
#41064=CARTESIAN_POINT('Ctrl Pts',(-6.69531304840367,0.982380875157681,
-28.7435534290839));
#41065=CARTESIAN_POINT('Ctrl Pts',(-6.72231677033071,0.798339861793501,
-28.7348037151282));
#41066=CARTESIAN_POINT('Ctrl Pts',(-6.74172778477911,0.613184940727803,
-28.7260540011725));
#41067=CARTESIAN_POINT('Ctrl Pts',(-6.75348015835533,0.427545027688197,
-28.7173042872169));
#41068=CARTESIAN_POINT('Ctrl Pts',(-6.76249038365226,0.285219953545373,
-28.7105961194146));
#41069=CARTESIAN_POINT('Ctrl Pts',(-6.767,0.142609995756768,-28.7038879516124));
#41070=CARTESIAN_POINT('Ctrl Pts',(-6.767,2.92894570544878E-13,-28.6971797838101));
#41071=CARTESIAN_POINT('Ctrl Pts',(-6.7669992726319,-0.00313754671095234,
-28.6971797838101));
#41072=CARTESIAN_POINT('Ctrl Pts',(-6.76690773148581,-0.200571697034152,
-28.6879156319988));
#41073=CARTESIAN_POINT('Ctrl Pts',(-6.75817155794658,-0.397750728450315,
-28.6786514801875));
#41074=CARTESIAN_POINT('Ctrl Pts',(-6.74088222003617,-0.593966241128391,
-28.6693873283761));
#41075=CARTESIAN_POINT('Ctrl Pts',(-6.72350447558709,-0.79118507356343,
-28.6600758056591));
#41076=CARTESIAN_POINT('Ctrl Pts',(-6.69748593276225,-0.987430335429607,
-28.6507642829421));
#41077=CARTESIAN_POINT('Ctrl Pts',(-6.66297023084457,-1.18199691322738,
-28.6414527602251));
#41078=CARTESIAN_POINT('Ctrl Pts',(-6.62837627730316,-1.37700459897866,
-28.6321201270647));
#41079=CARTESIAN_POINT('Ctrl Pts',(-6.58524667423045,-1.57032581884113,
-28.6227874939043));
#41080=CARTESIAN_POINT('Ctrl Pts',(-6.53377579614006,-1.76126739757889,
-28.6134548607439));
#41081=CARTESIAN_POINT('Ctrl Pts',(-6.48216851314583,-1.95271499775349,
-28.6040974948225));
#41082=CARTESIAN_POINT('Ctrl Pts',(-6.4221757607285,-2.14177016752003,-28.594740128901));
#41083=CARTESIAN_POINT('Ctrl Pts',(-6.35404225119917,-2.32775343839845,
-28.5853827629796));
#41084=CARTESIAN_POINT('Ctrl Pts',(-6.30400694633252,-2.46433424456539,
-28.5785109805063));
#41085=CARTESIAN_POINT('Ctrl Pts',(-6.24958233640898,-2.59925876060361,
-28.571639198033));
#41086=CARTESIAN_POINT('Ctrl Pts',(-6.19088166755803,-2.73226521009471,
-28.5647674155597));
#41087=CARTESIAN_POINT('Ctrl Pts',(-6.12048668033918,-2.89176913901457,
-28.5565266399629));
#41088=CARTESIAN_POINT('Ctrl Pts',(-6.04382629762756,-3.04877103020393,
-28.5482858643662));
#41089=CARTESIAN_POINT('Ctrl Pts',(-5.96109935751612,-3.2027462356267,-28.5400450887695));
#41090=CARTESIAN_POINT('Ctrl Pts',(-5.87846404645946,-3.35655089681664,
-28.5318134407251));
#41091=CARTESIAN_POINT('Ctrl Pts',(-5.78977572440595,-3.50733523678609,
-28.5235817926807));
#41092=CARTESIAN_POINT('Ctrl Pts',(-5.69528136573571,-3.65459425451083,
-28.5153501446364));
#41093=CARTESIAN_POINT('Ctrl Pts',(-5.60087483003553,-3.80171640983991,
-28.5071261470781));
#41094=CARTESIAN_POINT('Ctrl Pts',(-5.50067319529155,-3.94531947036094,
-28.4989021495199));
#41095=CARTESIAN_POINT('Ctrl Pts',(-5.39496949248503,-4.08492266452571,
-28.4906781519617));
#41096=CARTESIAN_POINT('Ctrl Pts',(-5.28935917931002,-4.22440251872684,
-28.4824614203372));
#41097=CARTESIAN_POINT('Ctrl Pts',(-5.17825670070644,-4.35988926743616,
-28.4742446887127));
#41098=CARTESIAN_POINT('Ctrl Pts',(-5.06199848340014,-4.4909309006101,-28.4660279570882));
#41099=CARTESIAN_POINT('Ctrl Pts',(-4.9457998294826,-4.62190539630404,-28.4578154351995));
#41100=CARTESIAN_POINT('Ctrl Pts',(-4.82445093317755,-4.7484390466513,-28.4496029133108));
#41101=CARTESIAN_POINT('Ctrl Pts',(-4.69832885840152,-4.87011241536697,
-28.4413903914221));
#41102=CARTESIAN_POINT('Ctrl Pts',(-4.57224895945459,-4.99174509592226,
-28.4331806158403));
#41103=CARTESIAN_POINT('Ctrl Pts',(-4.44139931757727,-5.10852048588802,
-28.4249708402585));
#41104=CARTESIAN_POINT('Ctrl Pts',(-4.30619431782448,-5.22005550709341,
-28.4167610646766));
#41105=CARTESIAN_POINT('Ctrl Pts',(-4.24714028657992,-5.26877110665828,
-28.4131752479938));
#41106=CARTESIAN_POINT('Ctrl Pts',(-4.18725584013383,-5.31648747855582,
-28.4095894313109));
#41107=CARTESIAN_POINT('Ctrl Pts',(-4.12657757471939,-5.36317504094571,
-28.4060036146281));
#41108=CARTESIAN_POINT('Ctrl Pts',(-3.97667264076494,-5.47851610926318,
-28.3971448971063));
#41109=CARTESIAN_POINT('Ctrl Pts',(-3.82207609594595,-5.58745587566541,
-28.3882861795845));
#41110=CARTESIAN_POINT('Ctrl Pts',(-3.66334657324155,-5.68965560331373,
-28.3794274620628));
#41111=CARTESIAN_POINT('Ctrl Pts',(-3.50432009309359,-5.79204653023827,
-28.3705521713033));
#41112=CARTESIAN_POINT('Ctrl Pts',(-3.34114540096804,-5.8876720787245,-28.3616768805438));
#41113=CARTESIAN_POINT('Ctrl Pts',(-3.17440617371424,-5.97623915554632,
-28.3528015897844));
#41114=CARTESIAN_POINT('Ctrl Pts',(-3.0071933695647,-6.06505778278009,-28.3439010912036));
#41115=CARTESIAN_POINT('Ctrl Pts',(-2.83639600123169,-6.14677769813225,
-28.3350005926228));
#41116=CARTESIAN_POINT('Ctrl Pts',(-2.66262103874598,-6.2211524819785,-28.3261000940421));
#41117=CARTESIAN_POINT('Ctrl Pts',(-2.48861083686074,-6.29562794706929,
-28.3171875468444));
#41118=CARTESIAN_POINT('Ctrl Pts',(-2.31161523008141,-6.36273832269259,
-28.3082749996468));
#41119=CARTESIAN_POINT('Ctrl Pts',(-2.13225818845227,-6.42228651009734,
-28.2993624524492));
#41120=CARTESIAN_POINT('Ctrl Pts',(-1.95250510895869,-6.48196618571553,
-28.2904302254769));
#41121=CARTESIAN_POINT('Ctrl Pts',(-1.77038041233506,-6.53405019220034,
-28.2814979985046));
#41122=CARTESIAN_POINT('Ctrl Pts',(-1.58652293478772,-6.57839144300433,
-28.2725657715324));
#41123=CARTESIAN_POINT('Ctrl Pts',(-1.41275638740813,-6.62029904535745,
-28.2641237855871));
#41124=CARTESIAN_POINT('Ctrl Pts',(-1.23744231443331,-6.65529088456251,
-28.2556817996419));
#41125=CARTESIAN_POINT('Ctrl Pts',(-1.06112567594325,-6.68328521760474,
-28.2472398136967));
#41126=CARTESIAN_POINT('Ctrl Pts',(-0.889362357011027,-6.71055660614642,
-28.2390158392791));
#41127=CARTESIAN_POINT('Ctrl Pts',(-0.716319313894368,-6.73123830859869,
-28.2307918648615));
#41128=CARTESIAN_POINT('Ctrl Pts',(-0.542543145037324,-6.74521578126104,
-28.222567890444));
#41129=CARTESIAN_POINT('Ctrl Pts',(-0.368950500675128,-6.75917849235611,
-28.2143526013413));
#41130=CARTESIAN_POINT('Ctrl Pts',(-0.194626626851767,-6.76645104443985,
-28.2061373122387));
#41131=CARTESIAN_POINT('Ctrl Pts',(-0.0201273681247383,-6.76697006710185,
-28.197922023136));
#41132=CARTESIAN_POINT('Ctrl Pts',(0.154222603286449,-6.76748864573044,
-28.1897137623638));
#41133=CARTESIAN_POINT('Ctrl Pts',(0.328747304201376,-6.76126520088701,
-28.1815055015917));
#41134=CARTESIAN_POINT('Ctrl Pts',(0.502886630532824,-6.74828823012409,
-28.1732972408195));
#41135=CARTESIAN_POINT('Ctrl Pts',(0.676911896168154,-6.73531975923509,
-28.1650943564316));
#41136=CARTESIAN_POINT('Ctrl Pts',(0.850551933686825,-6.71560660020399,
-28.1568914720437));
#41137=CARTESIAN_POINT('Ctrl Pts',(1.02324741081172,-6.68918931831557,-28.1486885876558));
#41138=CARTESIAN_POINT('Ctrl Pts',(1.19586439504825,-6.66278404350917,-28.1404894316116));
#41139=CARTESIAN_POINT('Ctrl Pts',(1.36753732046336,-6.62968077063963,-28.1322902755674));
#41140=CARTESIAN_POINT('Ctrl Pts',(1.53771265338977,-6.58997183572168,-28.1240911195232));
#41141=CARTESIAN_POINT('Ctrl Pts',(1.70787318520008,-6.55026635451554,-28.1158926766062));
#41142=CARTESIAN_POINT('Ctrl Pts',(1.87653603308155,-6.50395642875941,-28.1076942336892));
#41143=CARTESIAN_POINT('Ctrl Pts',(2.04315816399235,-6.45118545051306,-28.0994957907722));
#41144=CARTESIAN_POINT('Ctrl Pts',(2.20977863554397,-6.39841499780319,-28.0912974295019));
#41145=CARTESIAN_POINT('Ctrl Pts',(2.37435808832747,-6.3391837280583,-28.0830990682317));
#41146=CARTESIAN_POINT('Ctrl Pts',(2.53636907430538,-6.27368479594786,-28.0749007069615));
#41147=CARTESIAN_POINT('Ctrl Pts',(2.69840787730143,-6.20817461777918,-28.0667009380462));
#41148=CARTESIAN_POINT('Ctrl Pts',(2.85787700233019,-6.13639476769248,-28.0585011691309));
#41149=CARTESIAN_POINT('Ctrl Pts',(3.01426934603287,-6.05858641182633,-28.0503014002157));
#41150=CARTESIAN_POINT('Ctrl Pts',(3.17071695212731,-5.98075056180194,-28.0420987338514));
#41151=CARTESIAN_POINT('Ctrl Pts',(3.3240852902191,-5.89688212224843,-28.0338960674871));
#41152=CARTESIAN_POINT('Ctrl Pts',(3.47389216253669,-5.80726805331614,-28.0256934011228));
#41153=CARTESIAN_POINT('Ctrl Pts',(3.62386917801668,-5.71755220520076,-28.0174814185798));
#41154=CARTESIAN_POINT('Ctrl Pts',(3.77027633859534,-5.62207787516147,-28.0092694360368));
#41155=CARTESIAN_POINT('Ctrl Pts',(3.91265986140665,-5.52117576327156,-28.0010574534937));
#41156=CARTESIAN_POINT('Ctrl Pts',(4.05512736394403,-5.42021413795236,-27.9928406274124));
#41157=CARTESIAN_POINT('Ctrl Pts',(4.19356621415738,-5.31381856750332,-27.9846238013311));
#41158=CARTESIAN_POINT('Ctrl Pts',(4.32755611841255,-5.20235975707083,-27.9764069752499));
#41159=CARTESIAN_POINT('Ctrl Pts',(4.46175265445181,-5.09072906105502,-27.968177477636));
#41160=CARTESIAN_POINT('Ctrl Pts',(4.59148626747131,-4.97401976108095,-27.9599479800222));
#41161=CARTESIAN_POINT('Ctrl Pts',(4.7163729578319,-4.85264001576791,-27.9517184824083));
#41162=CARTESIAN_POINT('Ctrl Pts',(4.82769163236163,-4.74444728262724,-27.9443830588834));
#41163=CARTESIAN_POINT('Ctrl Pts',(4.93515976692244,-4.63254442615424,-27.9370476353585));
#41164=CARTESIAN_POINT('Ctrl Pts',(5.03853317892781,-4.51724168103099,-27.9297122118336));
#41165=CARTESIAN_POINT('Ctrl Pts',(5.15227076833743,-4.39037872828305,-27.9216413416472));
#41166=CARTESIAN_POINT('Ctrl Pts',(5.26142151905001,-4.25898564716953,-27.9135704714608));
#41167=CARTESIAN_POINT('Ctrl Pts',(5.36559293037466,-4.12343321826769,-27.9054996012744));
#41168=CARTESIAN_POINT('Ctrl Pts',(5.46963470847495,-3.98804947382741,-27.8974387746586));
#41169=CARTESIAN_POINT('Ctrl Pts',(5.5687092520658,-3.84851697256138,-27.8893779480428));
#41170=CARTESIAN_POINT('Ctrl Pts',(5.6624606030548,-3.70524343584227,-27.881317121427));
#41171=CARTESIAN_POINT('Ctrl Pts',(5.75611584601515,-3.56211677420312,-27.8732645582671));
#41172=CARTESIAN_POINT('Ctrl Pts',(5.84445855350297,-3.41525701855249,-27.8652119951072));
#41173=CARTESIAN_POINT('Ctrl Pts',(5.92717287637335,-3.26510500498592,-27.8571594319473));
#41174=CARTESIAN_POINT('Ctrl Pts',(6.00982051705628,-3.11507404016117,-27.8491133605594));
#41175=CARTESIAN_POINT('Ctrl Pts',(6.08684862519433,-2.96175642513735,-27.8410672891715));
#41176=CARTESIAN_POINT('Ctrl Pts',(6.15798461741865,-2.80562193668985,-27.8330212177837));
#41177=CARTESIAN_POINT('Ctrl Pts',(6.22907882180025,-2.64957916726169,-27.8249798729478));
#41178=CARTESIAN_POINT('Ctrl Pts',(6.2942876463808,-2.49072315710083,-27.8169385281119));
#41179=CARTESIAN_POINT('Ctrl Pts',(6.35338448663524,-2.32954814609673,-27.808897183276));
#41180=CARTESIAN_POINT('Ctrl Pts',(6.4136205321285,-2.16526617681682,-27.8007008260549));
#41181=CARTESIAN_POINT('Ctrl Pts',(6.46750635923963,-1.99857523600003,-27.7925044688339));
#41182=CARTESIAN_POINT('Ctrl Pts',(6.51485336973347,-1.83002037444189,-27.7843081116128));
#41183=CARTESIAN_POINT('Ctrl Pts',(6.56129017123856,-1.66470584735237,-27.7762693229043));
#41184=CARTESIAN_POINT('Ctrl Pts',(6.60143719935804,-1.49759879257117,-27.7682305341958));
#41185=CARTESIAN_POINT('Ctrl Pts',(6.63516695392705,-1.32922853321558,-27.7601917454873));
#41186=CARTESIAN_POINT('Ctrl Pts',(6.66890031788542,-1.16084025671666,-27.7521520965556));
#41187=CARTESIAN_POINT('Ctrl Pts',(6.69621496749303,-0.991188872691557,
-27.7441124476238));
#41188=CARTESIAN_POINT('Ctrl Pts',(6.717034644702,-0.820813366041932,-27.7360727986921));
#41189=CARTESIAN_POINT('Ctrl Pts',(6.73786067218061,-0.650385892668927,
-27.7280306975639));
#41190=CARTESIAN_POINT('Ctrl Pts',(6.75218773871132,-0.479234227539398,
-27.7199885964358));
#41191=CARTESIAN_POINT('Ctrl Pts',(6.75999153019552,-0.307901789025053,
-27.7119464953076));
#41192=CARTESIAN_POINT('Ctrl Pts',(6.7680586689821,-0.130787553856494,-27.7036330048628));
#41193=CARTESIAN_POINT('Ctrl Pts',(6.76915453951254,0.0465194324935302,
-27.6953195144181));
#41194=CARTESIAN_POINT('Ctrl Pts',(6.76331073914564,0.223420781838351,-27.6870060239733));
#41195=CARTESIAN_POINT('Ctrl Pts',(6.75764774798627,0.394848742159236,-27.6789497558026));
#41196=CARTESIAN_POINT('Ctrl Pts',(6.74546822191276,0.565895430864003,-27.6708934876318));
#41197=CARTESIAN_POINT('Ctrl Pts',(6.72685349619744,0.736023804435914,-27.662837219461));
#41198=CARTESIAN_POINT('Ctrl Pts',(6.70734726799422,0.914300021313188,-27.6543951178793));
#41199=CARTESIAN_POINT('Ctrl Pts',(6.68077436121496,1.09156731859551,-27.6459530162975));
#41200=CARTESIAN_POINT('Ctrl Pts',(6.64728777912249,1.26722301964917,-27.6375109147158));
#41201=CARTESIAN_POINT('Ctrl Pts',(6.61380119703002,1.44287872070286,-27.629068813134));
#41202=CARTESIAN_POINT('Ctrl Pts',(6.57340112806252,1.6169223961403,-27.6206267115523));
#41203=CARTESIAN_POINT('Ctrl Pts',(6.52629897085658,1.78877353038229,-27.6121846099705));
#41204=CARTESIAN_POINT('Ctrl Pts',(6.47979489459287,1.95844258010019,-27.6038497022068));
#41205=CARTESIAN_POINT('Ctrl Pts',(6.42661064491424,2.12651407104573,-27.5955147944431));
#41206=CARTESIAN_POINT('Ctrl Pts',(6.3668709788531,2.29243166498767,-27.5871798866793));
#41207=CARTESIAN_POINT('Ctrl Pts',(6.30720301190912,2.45815012582775,-27.5788549824119));
#41208=CARTESIAN_POINT('Ctrl Pts',(6.24099541972999,2.62171951501863,-27.5705300781445));
#41209=CARTESIAN_POINT('Ctrl Pts',(6.16842336475276,2.78259630438413,-27.5622051738771));
#41210=CARTESIAN_POINT('Ctrl Pts',(6.09592510257987,2.94330951081894,-27.5538887345488));
#41211=CARTESIAN_POINT('Ctrl Pts',(6.01707541419289,3.10133525735415,-27.5455722952206));
#41212=CARTESIAN_POINT('Ctrl Pts',(5.9320984733461,3.25614752468694,-27.5372558558923));
#41213=CARTESIAN_POINT('Ctrl Pts',(5.84720606510457,3.41080578924965,-27.5289476895176));
#41214=CARTESIAN_POINT('Ctrl Pts',(5.75619872405018,3.56225664467217,-27.5206395231429));
#41215=CARTESIAN_POINT('Ctrl Pts',(5.65934766262805,3.7099963656999,-27.5123313567682));
#41216=CARTESIAN_POINT('Ctrl Pts',(5.56255213255724,3.85765137742003,-27.5040279540347));
#41217=CARTESIAN_POINT('Ctrl Pts',(5.45991974729519,4.00159920387351,-27.4957245513012));
#41218=CARTESIAN_POINT('Ctrl Pts',(5.3517666754693,4.14136239072799,-27.4874211485676));
#41219=CARTESIAN_POINT('Ctrl Pts',(5.24365765656705,4.28106864922257,-27.4791211279772));
#41220=CARTESIAN_POINT('Ctrl Pts',(5.13003264432549,4.41659338990774,-27.4708211073868));
#41221=CARTESIAN_POINT('Ctrl Pts',(5.01125010095246,4.54748957400717,-27.4625210867964));
#41222=CARTESIAN_POINT('Ctrl Pts',(4.8924962210701,4.67835417146564,-27.4542230690892));
#41223=CARTESIAN_POINT('Ctrl Pts',(4.76858752439499,4.80459218139696,-27.445925051382));
#41224=CARTESIAN_POINT('Ctrl Pts',(4.63992171489285,4.92579084814467,-27.4376270336748));
#41225=CARTESIAN_POINT('Ctrl Pts',(4.51123961457061,5.0470048602719,-27.4293279653271));
#41226=CARTESIAN_POINT('Ctrl Pts',(4.37779944747247,5.16317801195076,-27.4210288969794));
#41227=CARTESIAN_POINT('Ctrl Pts',(4.24003501347875,5.27393516119361,-27.4127298286317));
#41228=CARTESIAN_POINT('Ctrl Pts',(4.10226297319145,5.38469842559528,-27.4044303020732));
#41229=CARTESIAN_POINT('Ctrl Pts',(3.96016646425015,5.4900448773709,-27.3961307755147));
#41230=CARTESIAN_POINT('Ctrl Pts',(3.81421135182252,5.58964048608032,-27.3878312489562));
#41231=CARTESIAN_POINT('Ctrl Pts',(3.66818024325294,5.68928795239097,-27.3795274009869));
#41232=CARTESIAN_POINT('Ctrl Pts',(3.51828680711016,5.78317840071868,-27.3712235530176));
#41233=CARTESIAN_POINT('Ctrl Pts',(3.36502537900307,5.87102147830045,-27.3629197050483));
#41234=CARTESIAN_POINT('Ctrl Pts',(3.27744614500196,5.92121825345732,-27.3581745799806));
#41235=CARTESIAN_POINT('Ctrl Pts',(3.18876761150909,5.96944114562792,-27.353429454913));
#41236=CARTESIAN_POINT('Ctrl Pts',(3.09908550384723,6.01564277861011,-27.3486843298453));
#41237=CARTESIAN_POINT('Origin',(0.,0.,-63.6971797838103));
#41238=CARTESIAN_POINT('',(3.09908550384718,6.01564277861014,-24.9542890874699));
#41239=CARTESIAN_POINT('',(3.0990855038472,6.01564277861013,-25.348603209574));
#41240=CARTESIAN_POINT('',(3.09908550384721,6.01564277861012,-63.6971797838103));
#41241=CARTESIAN_POINT('',(-6.76699450066406,0.0086271653731468,-26.302820216166));
#41242=CARTESIAN_POINT('Ctrl Pts',(-6.76699450066406,0.00862716537319188,
-26.302820216166));
#41243=CARTESIAN_POINT('Ctrl Pts',(-6.76720929633067,-0.159854720834625,
-26.2948897094655));
#41244=CARTESIAN_POINT('Ctrl Pts',(-6.76112789536669,-0.328586091746019,
-26.286959202765));
#41245=CARTESIAN_POINT('Ctrl Pts',(-6.74872146581008,-0.497038808257709,
-26.2790286960646));
#41246=CARTESIAN_POINT('Ctrl Pts',(-6.73632507264396,-0.665355252102513,
-26.2711046048812));
#41247=CARTESIAN_POINT('Ctrl Pts',(-6.71761385734345,-0.833393109637448,
-26.263180513698));
#41248=CARTESIAN_POINT('Ctrl Pts',(-6.69261103071651,-1.00062310163805,
-26.2552564225147));
#41249=CARTESIAN_POINT('Ctrl Pts',(-6.66762271089184,-1.16775606571198,
-26.2473369289405));
#41250=CARTESIAN_POINT('Ctrl Pts',(-6.63635009950524,-1.33408171855351,
-26.2394174353663));
#41251=CARTESIAN_POINT('Ctrl Pts',(-6.59886831744837,-1.49907502446546,
-26.2314979417921));
#41252=CARTESIAN_POINT('Ctrl Pts',(-6.56139431247054,-1.66403409598644,
-26.2235800914303));
#41253=CARTESIAN_POINT('Ctrl Pts',(-6.51771377670204,-1.82766099490035,
-26.2156622410685));
#41254=CARTESIAN_POINT('Ctrl Pts',(-6.46795309912641,-1.98944004873259,
-26.2077443907067));
#41255=CARTESIAN_POINT('Ctrl Pts',(-6.41819600781018,-2.15120744312447,
-26.1998271109856));
#41256=CARTESIAN_POINT('Ctrl Pts',(-6.36235975821465,-2.31112689000894,
-26.1919098312644));
#41257=CARTESIAN_POINT('Ctrl Pts',(-6.30062074567853,-2.4686974742008,-26.1839925515432));
#41258=CARTESIAN_POINT('Ctrl Pts',(-6.23887342452758,-2.62628926367661,
-26.176074206343));
#41259=CARTESIAN_POINT('Ctrl Pts',(-6.17122190041459,-2.7815312041177,-26.1681558611427));
#41260=CARTESIAN_POINT('Ctrl Pts',(-6.09789076943403,-2.93394225642756,
-26.1602375159425));
#41261=CARTESIAN_POINT('Ctrl Pts',(-6.02453460447058,-3.08640533924105,
-26.1523164675558));
#41262=CARTESIAN_POINT('Ctrl Pts',(-5.94549514263107,-3.23603526611232,
-26.1443954191691));
#41263=CARTESIAN_POINT('Ctrl Pts',(-5.86104283849494,-3.38237576938565,
-26.1364743707824));
#41264=CARTESIAN_POINT('Ctrl Pts',(-5.77649437220515,-3.52888290420454,
-26.1285443030435));
#41265=CARTESIAN_POINT('Ctrl Pts',(-5.68652095174598,-3.67209280581836,
-26.1206142353046));
#41266=CARTESIAN_POINT('Ctrl Pts',(-5.59143660638892,-3.81157784608081,
-26.1126841675658));
#41267=CARTESIAN_POINT('Ctrl Pts',(-5.49629311215779,-3.95114965544335,
-26.1047491667901));
#41268=CARTESIAN_POINT('Ctrl Pts',(-5.39603259352157,-4.08699168530267,
-26.0968141660144));
#41269=CARTESIAN_POINT('Ctrl Pts',(-5.29100870928579,-4.21871021027303,
-26.0888791652387));
#41270=CARTESIAN_POINT('Ctrl Pts',(-5.18582476707317,-4.35062947625361,
-26.0809320714026));
#41271=CARTESIAN_POINT('Ctrl Pts',(-5.07586321740119,-4.47841240388381,
-26.0729849775666));
#41272=CARTESIAN_POINT('Ctrl Pts',(-4.961514367973,-4.60170231288352,-26.0650378837305));
#41273=CARTESIAN_POINT('Ctrl Pts',(-4.88929343112213,-4.67957028249356,
-26.0600186241145));
#41274=CARTESIAN_POINT('Ctrl Pts',(-4.81532309359165,-4.75564678488783,
-26.0549993644984));
#41275=CARTESIAN_POINT('Ctrl Pts',(-4.73970804784808,-4.82985057958983,
-26.0499801048823));
#41276=CARTESIAN_POINT('Ctrl Pts',(-4.61415887433898,-4.95305655010088,
-26.0416462621896));
#41277=CARTESIAN_POINT('Ctrl Pts',(-4.48364207027366,-5.07152169441127,
-26.0333124194969));
#41278=CARTESIAN_POINT('Ctrl Pts',(-4.34854524625484,-5.18482817856816,
-26.0249785768042));
#41279=CARTESIAN_POINT('Ctrl Pts',(-4.21360765093424,-5.29800111669907,
-26.0166545565995));
#41280=CARTESIAN_POINT('Ctrl Pts',(-4.07410105347681,-5.40602728522836,
-26.0083305363947));
#41281=CARTESIAN_POINT('Ctrl Pts',(-3.93045018640649,-5.50852524113099,
-26.0000065161899));
#41282=CARTESIAN_POINT('Ctrl Pts',(-3.78694229187903,-5.61092118307651,
-25.9916907806991));
#41283=CARTESIAN_POINT('Ctrl Pts',(-3.63929862691486,-5.70779967364826,
-25.9833750452082));
#41284=CARTESIAN_POINT('Ctrl Pts',(-3.48797748408892,-5.79881902377448,
-25.9750593097174));
#41285=CARTESIAN_POINT('Ctrl Pts',(-3.33677922192115,-5.88976446144245,
-25.9667503270373));
#41286=CARTESIAN_POINT('Ctrl Pts',(-3.1819097291763,-5.97486006077029,-25.9584413443573));
#41287=CARTESIAN_POINT('Ctrl Pts',(-3.02385699088013,-6.0538068930802,-25.9501323616772));
#41288=CARTESIAN_POINT('Ctrl Pts',(-2.8659036562055,-6.13270407360221,-25.9418286047401));
#41289=CARTESIAN_POINT('Ctrl Pts',(-2.70477137611208,-6.20546003888148,
-25.9335248478029));
#41290=CARTESIAN_POINT('Ctrl Pts',(-2.54097369058976,-6.27182124296688,
-25.9252210908657));
#41291=CARTESIAN_POINT('Ctrl Pts',(-2.37724250297927,-6.33815550600313,
-25.9169207050537));
#41292=CARTESIAN_POINT('Ctrl Pts',(-2.21084838794507,-6.39810005041631,
-25.9086203192417));
#41293=CARTESIAN_POINT('Ctrl Pts',(-2.04232613575009,-6.45144890355896,
-25.9003199334296));
#41294=CARTESIAN_POINT('Ctrl Pts',(-1.87383942051301,-6.50478650681666,
-25.892021297953));
#41295=CARTESIAN_POINT('Ctrl Pts',(-1.70322579355409,-6.55153108482973,
-25.8837226624764));
#41296=CARTESIAN_POINT('Ctrl Pts',(-1.53103675948158,-6.59152603280273,
-25.8754240269997));
#41297=CARTESIAN_POINT('Ctrl Pts',(-1.35885545419271,-6.63151918558419,
-25.8671257640111));
#41298=CARTESIAN_POINT('Ctrl Pts',(-1.18509922149033,-6.66476323353771,
-25.8588275010225));
#41299=CARTESIAN_POINT('Ctrl Pts',(-1.01033154485271,-6.69115230505744,
-25.8505292380339));
#41300=CARTESIAN_POINT('Ctrl Pts',(-0.83554270459548,-6.71754457218109,
-25.8422299701611));
#41301=CARTESIAN_POINT('Ctrl Pts',(-0.659742520299974,-6.73708015745405,
-25.8339307022883));
#41302=CARTESIAN_POINT('Ctrl Pts',(-0.483501608820698,-6.74970482275098,
-25.8256314344155));
#41303=CARTESIAN_POINT('Ctrl Pts',(-0.307136947815695,-6.76233835259774,
-25.817326339119));
#41304=CARTESIAN_POINT('Ctrl Pts',(-0.130331288586724,-6.76805124128259,
-25.8090212438225));
#41305=CARTESIAN_POINT('Ctrl Pts',(0.0463418149108182,-6.76684131897526,
-25.800716148526));
#41306=CARTESIAN_POINT('Ctrl Pts',(0.223079342608453,-6.76563095546734,
-25.7924080247599));
#41307=CARTESIAN_POINT('Ctrl Pts',(0.399683870559923,-6.75749275923777,
-25.7840999009938));
#41308=CARTESIAN_POINT('Ctrl Pts',(0.575584705443573,-6.74247664043855,
-25.7757917772277));
#41309=CARTESIAN_POINT('Ctrl Pts',(0.751672521898899,-6.72744455959176,
-25.767474821974));
#41310=CARTESIAN_POINT('Ctrl Pts',(0.927054804690868,-6.70551998554797,
-25.7591578667203));
#41311=CARTESIAN_POINT('Ctrl Pts',(1.10116772692618,-6.67680452291186,-25.7508409114667));
#41312=CARTESIAN_POINT('Ctrl Pts',(1.22948630154825,-6.65564166384445,-25.7447114419842));
#41313=CARTESIAN_POINT('Ctrl Pts',(1.35711558514734,-6.6307914351338,-25.7385819725017));
#41314=CARTESIAN_POINT('Ctrl Pts',(1.48383452984843,-6.60231202595193,-25.7324525030192));
#41315=CARTESIAN_POINT('Ctrl Pts',(1.65854863615358,-6.56304595934251,-25.724001479494));
#41316=CARTESIAN_POINT('Ctrl Pts',(1.83185098681095,-6.51680737513996,-25.7155504559688));
#41317=CARTESIAN_POINT('Ctrl Pts',(2.00316545741816,-6.46371542924089,-25.7070994324436));
#41318=CARTESIAN_POINT('Ctrl Pts',(2.17432909072547,-6.41067022922229,-25.6986558497935));
#41319=CARTESIAN_POINT('Ctrl Pts',(2.34350801744213,-6.35078379244406,-25.6902122671433));
#41320=CARTESIAN_POINT('Ctrl Pts',(2.51013829310537,-6.28422586716026,-25.6817686844932));
#41321=CARTESIAN_POINT('Ctrl Pts',(2.67664450733739,-6.21771749632529,-25.6733313883534));
#41322=CARTESIAN_POINT('Ctrl Pts',(2.84060554636083,-6.1445476612844,-25.6648940922135));
#41323=CARTESIAN_POINT('Ctrl Pts',(3.00147419709432,-6.0649354196213,-25.6564567960737));
#41324=CARTESIAN_POINT('Ctrl Pts',(3.16222808031167,-5.98537997522224,-25.6480255193014));
#41325=CARTESIAN_POINT('Ctrl Pts',(3.31989367946601,-5.89939143869697,-25.639594242529));
#41326=CARTESIAN_POINT('Ctrl Pts',(3.47394509046804,-5.80723639164216,-25.6311629657566));
#41327=CARTESIAN_POINT('Ctrl Pts',(3.62793046945956,-5.71512084557599,-25.6227353029346));
#41328=CARTESIAN_POINT('Ctrl Pts',(3.77830446469358,-5.61684422815872,-25.6143076401127));
#41329=CARTESIAN_POINT('Ctrl Pts',(3.92456647714537,-5.51271865475346,-25.6058799772907));
#41330=CARTESIAN_POINT('Ctrl Pts',(4.07078346436403,-5.40862513531859,-25.5974549088367));
#41331=CARTESIAN_POINT('Ctrl Pts',(4.21289072346152,-5.29868644265154,-25.5890298403827));
#41332=CARTESIAN_POINT('Ctrl Pts',(4.35041701292123,-5.1832577413906,-25.5806047719287));
#41333=CARTESIAN_POINT('Ctrl Pts',(4.38804841528869,-5.15167291554407,-25.578299415315));
#41334=CARTESIAN_POINT('Ctrl Pts',(4.42533700352259,-5.11967727355014,-25.5759940587013));
#41335=CARTESIAN_POINT('Ctrl Pts',(4.46227354144736,-5.08727862823522,-25.5736887020876));
#41336=CARTESIAN_POINT('Ctrl Pts',(4.60036740276721,-4.96615049104538,-25.5650697135631));
#41337=CARTESIAN_POINT('Ctrl Pts',(4.73347610402824,-4.83944037359167,-25.5564507250387));
#41338=CARTESIAN_POINT('Ctrl Pts',(4.86116512889644,-4.70758564336341,-25.5478317365142));
#41339=CARTESIAN_POINT('Ctrl Pts',(4.98893065088635,-4.57565192038416,-25.5392075844464));
#41340=CARTESIAN_POINT('Ctrl Pts',(5.11126980513273,-4.43856765222686,-25.5305834323786));
#41341=CARTESIAN_POINT('Ctrl Pts',(5.22778679387279,-4.29680511983139,-25.5219592803108));
#41342=CARTESIAN_POINT('Ctrl Pts',(5.34829452082279,-4.15018718256418,-25.5130397487146));
#41343=CARTESIAN_POINT('Ctrl Pts',(5.46257397868827,-3.99856512529576,-25.5041202171183));
#41344=CARTESIAN_POINT('Ctrl Pts',(5.57023482799024,-3.84249566831826,-25.4952006855221));
#41345=CARTESIAN_POINT('Ctrl Pts',(5.67452429463413,-3.69131350197723,-25.4865604676629));
#41346=CARTESIAN_POINT('Ctrl Pts',(5.77260327723682,-3.53595854214474,-25.4779202498036));
#41347=CARTESIAN_POINT('Ctrl Pts',(5.86416265558127,-3.37696392472381,-25.4692800319443));
#41348=CARTESIAN_POINT('Ctrl Pts',(5.9601618164407,-3.21025953977097,-25.4602208434796));
#41349=CARTESIAN_POINT('Ctrl Pts',(6.04899319374431,-3.03955408641109,-25.4511616550149));
#41350=CARTESIAN_POINT('Ctrl Pts',(6.1303559622308,-2.86548857550354,-25.4421024665503));
#41351=CARTESIAN_POINT('Ctrl Pts',(6.21171873071729,-2.691423064596,-25.4330432780856));
#41352=CARTESIAN_POINT('Ctrl Pts',(6.28561277385952,-2.51399786209427,-25.4239840896209));
#41353=CARTESIAN_POINT('Ctrl Pts',(6.35179603764721,-2.33387576707272,-25.4149249011562));
#41354=CARTESIAN_POINT('Ctrl Pts',(6.41786464357386,-2.15406572094324,-25.4058814070999));
#41355=CARTESIAN_POINT('Ctrl Pts',(6.47631082476443,-1.97140276102581,-25.3968379130436));
#41356=CARTESIAN_POINT('Ctrl Pts',(6.5269156678898,-1.78652200217481,-25.3877944189874));
#41357=CARTESIAN_POINT('Ctrl Pts',(6.5774742229503,-1.60181035307754,-25.378759196982));
#41358=CARTESIAN_POINT('Ctrl Pts',(6.62020569695263,-1.41488518462245,-25.3697239749767));
#41359=CARTESIAN_POINT('Ctrl Pts',(6.65494108045985,-1.22639643492954,-25.3606887529713));
#41360=CARTESIAN_POINT('Ctrl Pts',(6.68961526778301,-1.03823976138075,-25.3516694490602));
#41361=CARTESIAN_POINT('Ctrl Pts',(6.71632145224507,-0.8485252412071,-25.3426501451492));
#41362=CARTESIAN_POINT('Ctrl Pts',(6.73494173339735,-0.65791249246595,-25.3336308412381));
#41363=CARTESIAN_POINT('Ctrl Pts',(6.75353865410628,-0.467538880732505,
-25.3246228526737));
#41364=CARTESIAN_POINT('Ctrl Pts',(6.76406989302338,-0.276269525572618,
-25.3156148641094));
#41365=CARTESIAN_POINT('Ctrl Pts',(6.76646900867999,-0.0847711895236639,
-25.3066068755451));
#41366=CARTESIAN_POINT('Ctrl Pts',(6.76886270584986,0.106294640826465,-25.2976192318384));
#41367=CARTESIAN_POINT('Ctrl Pts',(6.76316093836758,0.297588182134574,-25.2886315881317));
#41368=CARTESIAN_POINT('Ctrl Pts',(6.74934917479396,0.488441108741004,-25.2796439444251));
#41369=CARTESIAN_POINT('Ctrl Pts',(6.73732008601697,0.654660779766946,-25.2718163296916));
#41370=CARTESIAN_POINT('Ctrl Pts',(6.71914017042194,0.820546046547857,-25.2639887149582));
#41371=CARTESIAN_POINT('Ctrl Pts',(6.6948320114491,0.985653761965331,-25.2561611002248));
#41372=CARTESIAN_POINT('Ctrl Pts',(6.66960606030373,1.15699537477519,-25.2480379417795));
#41373=CARTESIAN_POINT('Ctrl Pts',(6.63778998791161,1.32742277749532,-25.2399147833342));
#41374=CARTESIAN_POINT('Ctrl Pts',(6.59947744861363,1.49639112709215,-25.2317916248889));
#41375=CARTESIAN_POINT('Ctrl Pts',(6.56116761055032,1.66534756353546,-25.2236690391688));
#41376=CARTESIAN_POINT('Ctrl Pts',(6.51636229888125,1.83284479480095,-25.2155464534487));
#41377=CARTESIAN_POINT('Ctrl Pts',(6.46520607973286,1.99834915532427,-25.2074238677286));
#41378=CARTESIAN_POINT('Ctrl Pts',(6.4140437136376,2.16387340290199,-25.1993003059961));
#41379=CARTESIAN_POINT('Ctrl Pts',(6.35652902973073,2.32740395356957,-25.1911767442637));
#41380=CARTESIAN_POINT('Ctrl Pts',(6.2928561433664,2.48842330781878,-25.1830531825312));
#41381=CARTESIAN_POINT('Ctrl Pts',(6.2291368788607,2.64955994555867,-25.1749237037481));
#41382=CARTESIAN_POINT('Ctrl Pts',(6.15925058787047,2.80818139294527,-25.1667942249649));
#41383=CARTESIAN_POINT('Ctrl Pts',(6.08343938395315,2.96379052258551,-25.1586647461818));
#41384=CARTESIAN_POINT('Ctrl Pts',(6.0075972731426,3.11946309132851,-25.1505319531533));
#41385=CARTESIAN_POINT('Ctrl Pts',(5.92582560733681,3.27212057199723,-25.1423991601248));
#41386=CARTESIAN_POINT('Ctrl Pts',(5.83841183260115,3.42129160887273,-25.1342663670963));
#41387=CARTESIAN_POINT('Ctrl Pts',(5.75090300864663,3.57062484662074,-25.1261247308891));
#41388=CARTESIAN_POINT('Ctrl Pts',(5.65774001914182,3.71646376070708,-25.117983094682));
#41389=CARTESIAN_POINT('Ctrl Pts',(5.55925330217142,3.85836645775076,-25.1098414584748));
#41390=CARTESIAN_POINT('Ctrl Pts',(5.50907565760953,3.93066395444538,-25.1056934054142));
#41391=CARTESIAN_POINT('Ctrl Pts',(5.45751675200637,4.00194022615733,-25.1015453523537));
#41392=CARTESIAN_POINT('Ctrl Pts',(5.40462417928148,4.07214028254504,-25.0973972992931));
#41393=CARTESIAN_POINT('Ctrl Pts',(5.2969909396395,4.21499322205623,-25.0889562580256));
#41394=CARTESIAN_POINT('Ctrl Pts',(5.18361096006823,4.35368172516,-25.0805152167581));
#41395=CARTESIAN_POINT('Ctrl Pts',(5.06483308104717,4.4877338224465,-25.0720741754906));
#41396=CARTESIAN_POINT('Ctrl Pts',(4.94614309501864,4.62168672415816,-25.0636393804061));
#41397=CARTESIAN_POINT('Ctrl Pts',(4.82206339181756,4.75100981004534,-25.0552045853217));
#41398=CARTESIAN_POINT('Ctrl Pts',(4.69298359101839,4.87526348153945,-25.0467697902372));
#41399=CARTESIAN_POINT('Ctrl Pts',(4.56399276583258,4.99943150410502,-25.0383408093163));
#41400=CARTESIAN_POINT('Ctrl Pts',(4.43000895672942,5.11853685095818,-25.0299118283954));
#41401=CARTESIAN_POINT('Ctrl Pts',(4.29145934431418,5.23217600010727,-25.0214828474744));
#41402=CARTESIAN_POINT('Ctrl Pts',(4.15296797633668,5.34576737685027,-25.0130574099864));
#41403=CARTESIAN_POINT('Ctrl Pts',(4.00991488863878,5.45389692561738,-25.0046319724983));
#41404=CARTESIAN_POINT('Ctrl Pts',(3.86276155936935,5.55620033255268,-24.9962065350103));
#41405=CARTESIAN_POINT('Ctrl Pts',(3.71564479254461,5.65847832067702,-24.9877831909481));
#41406=CARTESIAN_POINT('Ctrl Pts',(3.56443008805123,5.75493286188631,-24.979359846886));
#41407=CARTESIAN_POINT('Ctrl Pts',(3.40960956477191,5.84524179275896,-24.9709365028239));
#41408=CARTESIAN_POINT('Ctrl Pts',(3.30761675616245,5.90473559440178,-24.9653873643726));
#41409=CARTESIAN_POINT('Ctrl Pts',(3.20405967863177,5.96156311408783,-24.9598382259212));
#41410=CARTESIAN_POINT('Ctrl Pts',(3.09908550384718,6.01564277861014,-24.9542890874699));
#41411=CARTESIAN_POINT('Ctrl Pts',(3.09908550384719,6.01564277861013,-26.9540130953596));
#41412=CARTESIAN_POINT('Ctrl Pts',(2.94369358937914,6.09569620719059,-26.9457888539227));
#41413=CARTESIAN_POINT('Ctrl Pts',(2.78504743618393,6.16980231941268,-26.9375646124858));
#41414=CARTESIAN_POINT('Ctrl Pts',(2.62364130021567,6.23769150630284,-26.9293403710488));
#41415=CARTESIAN_POINT('Ctrl Pts',(2.46237917532573,6.3055201205577,-26.9211234675106));
#41416=CARTESIAN_POINT('Ctrl Pts',(2.29836230241852,6.36714272762714,-26.9129065639724));
#41417=CARTESIAN_POINT('Ctrl Pts',(2.13210812002705,6.42233633224816,-26.9046896604342));
#41418=CARTESIAN_POINT('Ctrl Pts',(1.96594004975562,6.47750134908727,-26.896477012879));
#41419=CARTESIAN_POINT('Ctrl Pts',(1.79753731470756,6.52624388348932,-26.8882643653239));
#41420=CARTESIAN_POINT('Ctrl Pts',(1.62743624522011,6.56838947290307,-26.8800517177687));
#41421=CARTESIAN_POINT('Ctrl Pts',(1.45739277347126,6.61052079144451,-26.8718418510892));
#41422=CARTESIAN_POINT('Ctrl Pts',(1.285652457804,6.64605952932386,-26.8636319844097));
#41423=CARTESIAN_POINT('Ctrl Pts',(1.11276575848564,6.67488137473183,-26.8554221177303));
#41424=CARTESIAN_POINT('Ctrl Pts',(1.03117841971235,6.68848275456407,-26.8515477816668));
#41425=CARTESIAN_POINT('Ctrl Pts',(0.949335959981298,6.70058900574323,-26.8476734456033));
#41426=CARTESIAN_POINT('Ctrl Pts',(0.867297029201273,6.71119101673754,-26.8437991095399));
#41427=CARTESIAN_POINT('Ctrl Pts',(0.679713995189303,6.7354326465349,-26.8349403920181));
#41428=CARTESIAN_POINT('Ctrl Pts',(0.49129776790984,6.7517816425708,-26.8260816744964));
#41429=CARTESIAN_POINT('Ctrl Pts',(0.302701553623098,6.76022638448108,-26.8172229569746));
#41430=CARTESIAN_POINT('Ctrl Pts',(0.11375250610948,6.76868692514719,-26.8083476662152));
#41431=CARTESIAN_POINT('Ctrl Pts',(-0.0753769422491641,6.76921364809673,
-26.7994723754557));
#41432=CARTESIAN_POINT('Ctrl Pts',(-0.264034911035329,6.76184697887749,
-26.7905970846963));
#41433=CARTESIAN_POINT('Ctrl Pts',(-0.453228710871385,6.75445938666131,
-26.7816965861155));
#41434=CARTESIAN_POINT('Ctrl Pts',(-0.641948090647254,6.7391335492757,-26.7727960875347));
#41435=CARTESIAN_POINT('Ctrl Pts',(-0.829544526971442,6.71596194731416,
-26.763895588954));
#41436=CARTESIAN_POINT('Ctrl Pts',(-1.01739491284253,6.69275897792402,-26.7549830417564));
#41437=CARTESIAN_POINT('Ctrl Pts',(-1.20411906216787,6.66168906653027,-26.7460704945588));
#41438=CARTESIAN_POINT('Ctrl Pts',(-1.38907857905345,6.62289586972458,-26.7371579473612));
#41439=CARTESIAN_POINT('Ctrl Pts',(-1.57444650461624,6.58401701375163,-26.7282257203889));
#41440=CARTESIAN_POINT('Ctrl Pts',(-1.75804174927372,6.53738081546298,-26.7192934934167));
#41441=CARTESIAN_POINT('Ctrl Pts',(-1.93923823651591,6.4831816311156,-26.7103612664444));
#41442=CARTESIAN_POINT('Ctrl Pts',(-2.11048984077922,6.43195714321012,-26.7019192804991));
#41443=CARTESIAN_POINT('Ctrl Pts',(-2.27959874031394,6.37397755117248,-26.6934772945537));
#41444=CARTESIAN_POINT('Ctrl Pts',(-2.44605286443069,6.30944644041064,-26.6850353086084));
#41445=CARTESIAN_POINT('Ctrl Pts',(-2.60820836519787,6.24658182449214,-26.6768113341908));
#41446=CARTESIAN_POINT('Ctrl Pts',(-2.7681538183743,6.1773786482961,-26.6685873597733));
#41447=CARTESIAN_POINT('Ctrl Pts',(-2.92535923206763,6.10201297633467,-26.6603633853557));
#41448=CARTESIAN_POINT('Ctrl Pts',(-3.08239862159142,6.02672689783511,-26.652148096253));
#41449=CARTESIAN_POINT('Ctrl Pts',(-3.23670341337504,5.94529143730795,-26.6439328071504));
#41450=CARTESIAN_POINT('Ctrl Pts',(-3.38776137584139,5.85793153428386,-26.6357175180477));
#41451=CARTESIAN_POINT('Ctrl Pts',(-3.53869010545076,5.77064636925881,-26.6275092572755));
#41452=CARTESIAN_POINT('Ctrl Pts',(-3.686377229187,5.67744703461661,-26.6193009965034));
#41453=CARTESIAN_POINT('Ctrl Pts',(-3.83033293459859,5.57860543596062,-26.6110927357312));
#41454=CARTESIAN_POINT('Ctrl Pts',(-3.97419434948814,5.47982857823247,-26.6028898513433));
#41455=CARTESIAN_POINT('Ctrl Pts',(-4.11432891981485,5.37541702011825,-26.5946869669554));
#41456=CARTESIAN_POINT('Ctrl Pts',(-4.25027370070327,5.26568727414666,-26.5864840825675));
#41457=CARTESIAN_POINT('Ctrl Pts',(-4.38615669248902,5.15600740212019,-26.5782849265233));
#41458=CARTESIAN_POINT('Ctrl Pts',(-4.51785341029003,5.04101438269913,-26.5700857704791));
#41459=CARTESIAN_POINT('Ctrl Pts',(-4.6449319713574,4.92106654918035,-26.5618866144349));
#41460=CARTESIAN_POINT('Ctrl Pts',(-4.77199947968023,4.80112914820623,-26.5536881715179));
#41461=CARTESIAN_POINT('Ctrl Pts',(-4.89444936489766,4.67623803127121,-26.5454897286009));
#41462=CARTESIAN_POINT('Ctrl Pts',(-5.0118845100908,4.54679036876696,-26.5372912856839));
#41463=CARTESIAN_POINT('Ctrl Pts',(-5.12931848576894,4.41734399540814,-26.5290929244137));
#41464=CARTESIAN_POINT('Ctrl Pts',(-5.24173757910049,4.28334143181827,-26.5208945631435));
#41465=CARTESIAN_POINT('Ctrl Pts',(-5.34878318189772,4.14521500926648,-26.5126962018732));
#41466=CARTESIAN_POINT('Ctrl Pts',(-5.45584716424772,4.00706487063664,-26.504496432958));
#41467=CARTESIAN_POINT('Ctrl Pts',(-5.55753559820403,3.86478974591198,-26.4962966640427));
#41468=CARTESIAN_POINT('Ctrl Pts',(-5.65353161629358,3.7188532188793,-26.4880968951274));
#41469=CARTESIAN_POINT('Ctrl Pts',(-5.74956155528621,3.57286512409529,-26.4798942287631));
#41470=CARTESIAN_POINT('Ctrl Pts',(-5.83989487455199,3.42321334925615,-26.4716915623988));
#41471=CARTESIAN_POINT('Ctrl Pts',(-5.92425927289701,3.27038851934963,-26.4634888960346));
#41472=CARTESIAN_POINT('Ctrl Pts',(-6.00871948811169,3.11739011863485,-26.4552769134915));
#41473=CARTESIAN_POINT('Ctrl Pts',(-6.0871970653548,2.96121177751405,-26.4470649309485));
#41474=CARTESIAN_POINT('Ctrl Pts',(-6.15946626873234,2.80236762119971,-26.4388529484055));
#41475=CARTESIAN_POINT('Ctrl Pts',(-6.23177809746274,2.64342977645521,-26.4306361223242));
#41476=CARTESIAN_POINT('Ctrl Pts',(-6.29787411752868,2.48182331374087,-26.4224192962429));
#41477=CARTESIAN_POINT('Ctrl Pts',(-6.35757766402478,2.31808007754117,-26.4142024701616));
#41478=CARTESIAN_POINT('Ctrl Pts',(-6.41737328201233,2.15408432562242,-26.4059729725477));
#41479=CARTESIAN_POINT('Ctrl Pts',(-6.47075661670434,1.98794555644227,-26.3977434749339));
#41480=CARTESIAN_POINT('Ctrl Pts',(-6.51760121400132,1.82020971738107,-26.38951397732));
#41481=CARTESIAN_POINT('Ctrl Pts',(-6.55935649204513,1.6706971374456,-26.3821785537951));
#41482=CARTESIAN_POINT('Ctrl Pts',(-6.59591731160973,1.51991598575371,-26.3748431302702));
#41483=CARTESIAN_POINT('Ctrl Pts',(-6.62722876856031,1.36825723062829,-26.3675077067453));
#41484=CARTESIAN_POINT('Ctrl Pts',(-6.67579691731258,1.13301474446292,-26.3561295092542));
#41485=CARTESIAN_POINT('Ctrl Pts',(-6.71187188657008,0.895012061568704,
-26.3447513117631));
#41486=CARTESIAN_POINT('Ctrl Pts',(-6.73519158237264,0.655349791131986,
-26.333373114272));
#41487=CARTESIAN_POINT('Ctrl Pts',(-6.7560643755579,0.440834942932958,-26.3231888149113));
#41488=CARTESIAN_POINT('Ctrl Pts',(-6.76671866160522,0.22499038588721,-26.3130045155506));
#41489=CARTESIAN_POINT('Ctrl Pts',(-6.76699450066341,0.00862716588261877,
-26.30282021619));
#41490=CARTESIAN_POINT('',(-6.767,2.46159836221269E-13,-26.6971797838101));
#41491=CARTESIAN_POINT('Ctrl Pts',(3.09908550384723,6.01564277861011,-27.3486843298453));
#41492=CARTESIAN_POINT('Ctrl Pts',(2.94202003450173,6.09655837435233,-27.3403739174868));
#41493=CARTESIAN_POINT('Ctrl Pts',(2.78187539054827,6.17127148352116,-27.3320635051283));
#41494=CARTESIAN_POINT('Ctrl Pts',(2.61918139267093,6.23956551630692,-27.3237530927698));
#41495=CARTESIAN_POINT('Ctrl Pts',(2.45633190967738,6.30792481705439,-27.3154347382287));
#41496=CARTESIAN_POINT('Ctrl Pts',(2.29092853147358,6.36985266617452,-27.3071163836876));
#41497=CARTESIAN_POINT('Ctrl Pts',(2.12351817934484,6.4251816738511,-27.2987980291465));
#41498=CARTESIAN_POINT('Ctrl Pts',(2.09573825456533,6.43436292012312,-27.2974176888002));
#41499=CARTESIAN_POINT('Ctrl Pts',(2.06790309431458,6.44336257498331,-27.2960373484538));
#41500=CARTESIAN_POINT('Ctrl Pts',(2.04001522898076,6.45218000876654,-27.2946570081075));
#41501=CARTESIAN_POINT('Ctrl Pts',(1.86927400082929,6.50616404287139,-27.2862059845823));
#41502=CARTESIAN_POINT('Ctrl Pts',(1.69624418085032,6.5534122471801,-27.2777549610571));
#41503=CARTESIAN_POINT('Ctrl Pts',(1.52148359721141,6.59373768536606,-27.2693039375319));
#41504=CARTESIAN_POINT('Ctrl Pts',(1.34687688507213,6.63402761820227,-27.2608603548818));
#41505=CARTESIAN_POINT('Ctrl Pts',(1.17054276816465,6.66740685979813,-27.2524167722316));
#41506=CARTESIAN_POINT('Ctrl Pts',(0.993054007324512,6.69373832312982,-27.2439731895814));
#41507=CARTESIAN_POINT('Ctrl Pts',(0.815697392395926,6.72005018186677,-27.2355358934416));
#41508=CARTESIAN_POINT('Ctrl Pts',(0.637188174069064,6.73932467407811,-27.2270985973017));
#41509=CARTESIAN_POINT('Ctrl Pts',(0.458109467011628,6.75147574358631,-27.2186613011619));
#41510=CARTESIAN_POINT('Ctrl Pts',(0.27915851895759,6.76361814423289,-27.2102300243896));
#41511=CARTESIAN_POINT('Ctrl Pts',(0.0996392225044273,6.76864723672818,
-27.2017987476172));
#41512=CARTESIAN_POINT('Ctrl Pts',(-0.0798598080510627,6.76652875639039,
-27.1933674708448));
#41513=CARTESIAN_POINT('Ctrl Pts',(-0.259281898824211,6.76441118410996,
-27.1849398080229));
#41514=CARTESIAN_POINT('Ctrl Pts',(-0.438683410162749,6.75515215054191,
-27.176512145201));
#41515=CARTESIAN_POINT('Ctrl Pts',(-0.617474682917946,6.73876947342431,
-27.1680844823791));
#41516=CARTESIAN_POINT('Ctrl Pts',(-0.796210916648085,6.72239183954268,
-27.1596594139251));
#41517=CARTESIAN_POINT('Ctrl Pts',(-0.974336956710911,6.69889496560102,
-27.1512343454711));
#41518=CARTESIAN_POINT('Ctrl Pts',(-1.15126685130219,6.66834864393673,-27.1428092770171));
#41519=CARTESIAN_POINT('Ctrl Pts',(-1.19968028614615,6.65999023533069,-27.1405039204034));
#41520=CARTESIAN_POINT('Ctrl Pts',(-1.24800419538771,6.65110430743247,-27.1381985637898));
#41521=CARTESIAN_POINT('Ctrl Pts',(-1.29622666598137,6.64169296417704,-27.1358932071761));
#41522=CARTESIAN_POINT('Ctrl Pts',(-1.47651500757769,6.60650697211099,-27.1272742186516));
#41523=CARTESIAN_POINT('Ctrl Pts',(-1.65530419536613,6.56398866374391,-27.1186552301272));
#41524=CARTESIAN_POINT('Ctrl Pts',(-1.83199864963129,6.51429734873602,-27.1100362416027));
#41525=CARTESIAN_POINT('Ctrl Pts',(-2.00879895964344,6.4645762641958,-27.1014120895349));
#41526=CARTESIAN_POINT('Ctrl Pts',(-2.18350173887581,6.40767367931469,-27.0927879374672));
#41527=CARTESIAN_POINT('Ctrl Pts',(-2.35552729846031,6.34379855813599,-27.0841637853994));
#41528=CARTESIAN_POINT('Ctrl Pts',(-2.53344477974066,6.27773569687258,-27.0752442538031));
#41529=CARTESIAN_POINT('Ctrl Pts',(-2.70849807075692,6.2042143527267,-27.0663247222069));
#41530=CARTESIAN_POINT('Ctrl Pts',(-2.88006970944353,6.12351920620373,-27.0574051906106));
#41531=CARTESIAN_POINT('Ctrl Pts',(-3.04626860909665,6.04535101557425,-27.0487649727514));
#41532=CARTESIAN_POINT('Ctrl Pts',(-3.20920036236136,5.96045169784565,-27.0401247548921));
#41533=CARTESIAN_POINT('Ctrl Pts',(-3.36832956203072,5.86912642235196,-27.0314845370329));
#41534=CARTESIAN_POINT('Ctrl Pts',(-3.53517505522743,5.77337271616397,-27.0224253485681));
#41535=CARTESIAN_POINT('Ctrl Pts',(-3.69783972134989,5.67055456700585,-27.0133661601034));
#41536=CARTESIAN_POINT('Ctrl Pts',(-3.85574103850704,5.56107454040788,-27.0043069716386));
#41537=CARTESIAN_POINT('Ctrl Pts',(-4.01364235566422,5.45159451380989,-26.9952477831738));
#41538=CARTESIAN_POINT('Ctrl Pts',(-4.16678003900837,5.33545286738085,-26.9861885947091));
#41539=CARTESIAN_POINT('Ctrl Pts',(-4.31461139104156,5.21310056917133,-26.9771294062443));
#41540=CARTESIAN_POINT('Ctrl Pts',(-4.46218663562887,5.09096023773449,-26.968085912188));
#41541=CARTESIAN_POINT('Ctrl Pts',(-4.60461041245573,4.96251888607445,-26.9590424181317));
#41542=CARTESIAN_POINT('Ctrl Pts',(-4.74137395223829,4.82821520285046,-26.9499989240754));
#41543=CARTESIAN_POINT('Ctrl Pts',(-4.87801239491148,4.69403436671404,-26.94096370207));
#41544=CARTESIAN_POINT('Ctrl Pts',(-5.00900076750657,4.5540020714474,-26.9319284800646));
#41545=CARTESIAN_POINT('Ctrl Pts',(-5.13386596701775,4.40859492726389,-26.9228932580592));
#41546=CARTESIAN_POINT('Ctrl Pts',(-5.25851118122987,4.26344395881409,-26.913873954148));
#41547=CARTESIAN_POINT('Ctrl Pts',(-5.3770546091405,4.11293723088186,-26.9048546502369));
#41548=CARTESIAN_POINT('Ctrl Pts',(-5.48906244356266,3.95758543693878,-26.8958353463258));
#41549=CARTESIAN_POINT('Ctrl Pts',(-5.60092975633303,3.80242854267219,-26.8868273577614));
#41550=CARTESIAN_POINT('Ctrl Pts',(-5.70627769988811,3.6424389054898,-26.877819369197));
#41551=CARTESIAN_POINT('Ctrl Pts',(-5.8047133411596,3.4781592871753,-26.8688113806326));
#41552=CARTESIAN_POINT('Ctrl Pts',(-5.90292666208736,3.314250700133,-26.8598237369259));
#41553=CARTESIAN_POINT('Ctrl Pts',(-5.99425872091947,3.14607167608885,-26.8508360932191));
#41554=CARTESIAN_POINT('Ctrl Pts',(-6.07836065704107,2.97419244887335,-26.8418484495124));
#41555=CARTESIAN_POINT('Ctrl Pts',(-6.15160761428083,2.82449755495256,-26.8340208347793));
#41556=CARTESIAN_POINT('Ctrl Pts',(-6.21937094682393,2.67199653257325,-26.8261932200462));
#41557=CARTESIAN_POINT('Ctrl Pts',(-6.28144717792786,2.51708369962187,-26.818365605313));
#41558=CARTESIAN_POINT('Ctrl Pts',(-6.34392048509957,2.36117995312011,-26.8104879205543));
#41559=CARTESIAN_POINT('Ctrl Pts',(-6.40061979527873,2.20286322566247,-26.8026102357956));
#41560=CARTESIAN_POINT('Ctrl Pts',(-6.45135507265898,2.04262251198729,-26.7947325510369));
#41561=CARTESIAN_POINT('Ctrl Pts',(-6.50360939287892,1.87758410090503,-26.7866190039503));
#41562=CARTESIAN_POINT('Ctrl Pts',(-6.54953679513948,1.71050508572804,-26.7785054568638));
#41563=CARTESIAN_POINT('Ctrl Pts',(-6.58898439250822,1.54193828517327,-26.7703919097773));
#41564=CARTESIAN_POINT('Ctrl Pts',(-6.62729075844782,1.37824817530526,-26.762513090166));
#41565=CARTESIAN_POINT('Ctrl Pts',(-6.65948699384009,1.21315557237102,-26.7546342705548));
#41566=CARTESIAN_POINT('Ctrl Pts',(-6.68548482724296,1.0471779336408,-26.7467554509435));
#41567=CARTESIAN_POINT('Ctrl Pts',(-6.71264446014735,0.873783033058348,
-26.7385245401193));
#41568=CARTESIAN_POINT('Ctrl Pts',(-6.73303885051885,0.699422635723901,
-26.7302936292952));
#41569=CARTESIAN_POINT('Ctrl Pts',(-6.74662778723258,0.524692767761558,
-26.722062718471));
#41570=CARTESIAN_POINT('Ctrl Pts',(-6.7602167239463,0.349962899799214,-26.7138318076468));
#41571=CARTESIAN_POINT('Ctrl Pts',(-6.76700022565576,0.174864042719825,
-26.7056008968226));
#41572=CARTESIAN_POINT('Ctrl Pts',(-6.76699999999437,-8.73235207390737E-6,
-26.6973699859984));
#41573=CARTESIAN_POINT('Ctrl Pts',(-6.767,2.46159858321081E-13,-26.6971797838101));
#41574=CARTESIAN_POINT('Ctrl Pts',(-6.76700000000001,-0.186007249559863,
-26.6884302719974));
#41575=CARTESIAN_POINT('Ctrl Pts',(-6.75932637294247,-0.372014355816143,
-26.6796807601846));
#41576=CARTESIAN_POINT('Ctrl Pts',(-6.74400518263361,-0.557389537586617,
-26.6709312483719));
#41577=CARTESIAN_POINT('Ctrl Pts',(-6.72868405703726,-0.742763936383156,
-26.6621817735147));
#41578=CARTESIAN_POINT('Ctrl Pts',(-6.70571545643557,-0.927506130405536,
-26.6534322986574));
#41579=CARTESIAN_POINT('Ctrl Pts',(-6.67517739401564,-1.11098864009612,
-26.6446828238002));
#41580=CARTESIAN_POINT('Ctrl Pts',(-6.64463945804373,-1.29447039004625,
-26.6359333851717));
#41581=CARTESIAN_POINT('Ctrl Pts',(-6.60653217002702,-1.47669218339379,
-26.6271839465432));
#41582=CARTESIAN_POINT('Ctrl Pts',(-6.5609849608545,-1.65703510627901,-26.6184345079147));
#41583=CARTESIAN_POINT('Ctrl Pts',(-6.51543793649521,-1.83737729740133,
-26.6096851047881));
#41584=CARTESIAN_POINT('Ctrl Pts',(-6.46245112156856,-2.01584035545082,
-26.6009357016614));
#41585=CARTESIAN_POINT('Ctrl Pts',(-6.40220448361671,-2.19181813797544,
-26.5921862985348));
#41586=CARTESIAN_POINT('Ctrl Pts',(-6.34195808511921,-2.36779522106443,
-26.5834369301833));
#41587=CARTESIAN_POINT('Ctrl Pts',(-6.27445201416296,-2.54128677725889,
-26.5746875618317));
#41588=CARTESIAN_POINT('Ctrl Pts',(-6.19991555052659,-2.71170355428807,
-26.5659381934802));
#41589=CARTESIAN_POINT('Ctrl Pts',(-6.12537937695036,-2.88211966813698,
-26.557188859177));
#41590=CARTESIAN_POINT('Ctrl Pts',(-6.04381298028244,-3.04946076420082,
-26.5484395248738));
#41591=CARTESIAN_POINT('Ctrl Pts',(-5.95549339308748,-3.21315848424745,
-26.5396901905706));
#41592=CARTESIAN_POINT('Ctrl Pts',(-5.86717414225566,-3.37685558085504,
-26.5309408895891));
#41593=CARTESIAN_POINT('Ctrl Pts',(-5.77210188843815,-3.5369090770041,-26.5221915886075));
#41594=CARTESIAN_POINT('Ctrl Pts',(-5.67059953311112,-3.6927753702439,-26.5134422876259));
#41595=CARTESIAN_POINT('Ctrl Pts',(-5.56909755592427,-3.84864108281434,
-26.5046930192393));
#41596=CARTESIAN_POINT('Ctrl Pts',(-5.46116568154663,-4.00031938355243,
-26.4959437508527));
#41597=CARTESIAN_POINT('Ctrl Pts',(-5.34717048488051,-4.14729511918585,
-26.4871944824661));
#41598=CARTESIAN_POINT('Ctrl Pts',(-5.23317570342956,-4.29427031947606,
-26.4784452459477));
#41599=CARTESIAN_POINT('Ctrl Pts',(-5.11311781951174,-4.43654276249987,
-26.4696960094293));
#41600=CARTESIAN_POINT('Ctrl Pts',(-4.98740458928846,-4.57362924412817,
-26.460946772911));
#41601=CARTESIAN_POINT('Ctrl Pts',(-4.86169180652338,-4.71071523781682,
-26.4521975675343));
#41602=CARTESIAN_POINT('Ctrl Pts',(-4.73032391141167,-4.84261509584885,
-26.4434483621576));
#41603=CARTESIAN_POINT('Ctrl Pts',(-4.59374706946921,-4.96888084599974,
-26.4346991567809));
#41604=CARTESIAN_POINT('Ctrl Pts',(-4.45717070231118,-5.09514615721082,
-26.4259499818192));
#41605=CARTESIAN_POINT('Ctrl Pts',(-4.31538563496991,-5.21577720520889,
-26.4172008068575));
#41606=CARTESIAN_POINT('Ctrl Pts',(-4.16887340951689,-5.33036429293749,
-26.4084516318958));
#41607=CARTESIAN_POINT('Ctrl Pts',(-4.02236168122185,-5.44495099183926,
-26.3997024866225));
#41608=CARTESIAN_POINT('Ctrl Pts',(-3.87112305262899,-5.55349359498124,
-26.3909533413493));
#41609=CARTESIAN_POINT('Ctrl Pts',(-3.71567116928734,-5.65562346357383,
-26.3822041960761));
#41610=CARTESIAN_POINT('Ctrl Pts',(-3.56021980053056,-5.75775299409085,
-26.3734550797647));
#41611=CARTESIAN_POINT('Ctrl Pts',(-3.40055544441836,-5.85346967520023,
-26.3647059634533));
#41612=CARTESIAN_POINT('Ctrl Pts',(-3.23722035886603,-5.94244843041514,
-26.355956847142));
#41613=CARTESIAN_POINT('Ctrl Pts',(-3.0738858004326,-6.03142689847567,-26.347207759066));
#41614=CARTESIAN_POINT('Ctrl Pts',(-2.90688078789005,-6.11366734708005,
-26.33845867099));
#41615=CARTESIAN_POINT('Ctrl Pts',(-2.73677250610188,-6.18889047001519,
-26.329709582914));
#41616=CARTESIAN_POINT('Ctrl Pts',(-2.56666475916736,-6.26411335643415,
-26.3209605223468));
#41617=CARTESIAN_POINT('Ctrl Pts',(-2.39345402456902,-6.33231884545328,
-26.3122114617796));
#41618=CARTESIAN_POINT('Ctrl Pts',(-2.21772855943881,-6.39327529804946,
-26.3034624012125));
#41619=CARTESIAN_POINT('Ctrl Pts',(-2.042003632234,-6.45423156404763,-26.2947133674277));
#41620=CARTESIAN_POINT('Ctrl Pts',(-1.86376426060836,-6.5079387441251,-26.2859643336428));
#41621=CARTESIAN_POINT('Ctrl Pts',(-1.68361577621482,-6.55421443943365,
-26.277215299858));
#41622=CARTESIAN_POINT('Ctrl Pts',(-1.50346782833009,-6.60048999692635,
-26.2684662921291));
#41623=CARTESIAN_POINT('Ctrl Pts',(-1.32141105657181,-6.63933404265203,
-26.2597172844003));
#41624=CARTESIAN_POINT('Ctrl Pts',(-1.13806375346329,-6.67061465631564,
-26.2509682766714));
#41625=CARTESIAN_POINT('Ctrl Pts',(-0.954716981168126,-6.70189517941797,
-26.2422192942719));
#41626=CARTESIAN_POINT('Ctrl Pts',(-0.770079967440584,-6.72561226609023,
-26.2334703118725));
#41627=CARTESIAN_POINT('Ctrl Pts',(-0.584779764071559,-6.74168536995998,
-26.2247213294731));
#41628=CARTESIAN_POINT('Ctrl Pts',(-0.391489587591418,-6.75845153117881,
-26.2155950990575));
#41629=CARTESIAN_POINT('Ctrl Pts',(-0.197478091803673,-6.76689985146399,
-26.2064688686419));
#41630=CARTESIAN_POINT('Ctrl Pts',(-0.00346214752944389,-6.76699911434415,
-26.1973426382262));
#41631=CARTESIAN_POINT('Ctrl Pts',(0.184490798486235,-6.76709527525931,
-26.1885016025111));
#41632=CARTESIAN_POINT('Ctrl Pts',(0.372447602156381,-6.75935633790754,
-26.179660566796));
#41633=CARTESIAN_POINT('Ctrl Pts',(0.559756448195821,-6.743809140145,-26.1708195310809));
#41634=CARTESIAN_POINT('Ctrl Pts',(0.745136131044979,-6.72842206873137,
-26.1620695524675));
#41635=CARTESIAN_POINT('Ctrl Pts',(0.929880851946681,-6.70538686355701,
-26.1533195738542));
#41636=CARTESIAN_POINT('Ctrl Pts',(1.11336305057628,-6.67478177303285,-26.1445695952409));
#41637=CARTESIAN_POINT('Ctrl Pts',(1.29684337090296,-6.64417699581227,-26.1358197062009));
#41638=CARTESIAN_POINT('Ctrl Pts',(1.4790609120537,-6.6060025354802,-26.127069817161));
#41639=CARTESIAN_POINT('Ctrl Pts',(1.65939671095408,-6.56038806441165,-26.118319928121));
#41640=CARTESIAN_POINT('Ctrl Pts',(1.83973072369346,-6.51477404513797,-26.1095701257455));
#41641=CARTESIAN_POINT('Ctrl Pts',(2.01818275357222,-6.46172023288603,-26.10082032337));
#41642=CARTESIAN_POINT('Ctrl Pts',(2.1941466403351,-6.40140683918045,-26.0920705209945));
#41643=CARTESIAN_POINT('Ctrl Pts',(2.37010884271446,-6.34109402281428,-26.083320802375));
#41644=CARTESIAN_POINT('Ctrl Pts',(2.54358267847994,-6.27352185699716,-26.0745710837554));
#41645=CARTESIAN_POINT('Ctrl Pts',(2.71397890841932,-6.19891986435178,-26.0658213651359));
#41646=CARTESIAN_POINT('Ctrl Pts',(2.88437356389133,-6.12431856103153,-26.0570717273641));
#41647=CARTESIAN_POINT('Ctrl Pts',(3.05169040787365,-6.0426876758246,-26.0483220895922));
#41648=CARTESIAN_POINT('Ctrl Pts',(3.21536112512248,-5.95430447953841,-26.0395724518204));
#41649=CARTESIAN_POINT('Ctrl Pts',(3.37903038443035,-5.86592207054932,-26.0308228919884));
#41650=CARTESIAN_POINT('Ctrl Pts',(3.53905332980163,-5.77078760703261,-26.0220733321563));
#41651=CARTESIAN_POINT('Ctrl Pts',(3.69488643042079,-5.66922422085177,-26.0133237723242));
#41652=CARTESIAN_POINT('Ctrl Pts',(3.8507181946893,-5.56766170563029,-26.0045742875242));
#41653=CARTESIAN_POINT('Ctrl Pts',(4.00235994599412,-5.45967053456114,-25.9958248027242));
#41654=CARTESIAN_POINT('Ctrl Pts',(4.14929662974488,-5.34561750206539,-25.9870753179242));
#41655=CARTESIAN_POINT('Ctrl Pts',(4.29623210225234,-5.23156540974311,-25.9783259052489));
#41656=CARTESIAN_POINT('Ctrl Pts',(4.43846235842308,-5.11145173172021,-25.9695764925735));
#41657=CARTESIAN_POINT('Ctrl Pts',(4.5755043179762,-4.98568443006386,-25.9608270798981));
#41658=CARTESIAN_POINT('Ctrl Pts',(4.7125451933768,-4.85991812336509,-25.9520777364402));
#41659=CARTESIAN_POINT('Ctrl Pts',(4.84439764315164,-4.72849847630916,-25.9433283929823));
#41660=CARTESIAN_POINT('Ctrl Pts',(4.97061384196861,-4.59187184425155,-25.9345790495245));
#41661=CARTESIAN_POINT('Ctrl Pts',(5.09682908420371,-4.45524624767559,-25.9258297723771));
#41662=CARTESIAN_POINT('Ctrl Pts',(5.21740796650326,-4.31341395556705,-25.9170804952297));
#41663=CARTESIAN_POINT('Ctrl Pts',(5.33194095942397,-4.1668566816267,-25.9083312180824));
#41664=CARTESIAN_POINT('Ctrl Pts',(5.44647312235278,-4.02030046975018,-25.8995820043388));
#41665=CARTESIAN_POINT('Ctrl Pts',(5.55495930712433,-3.86901957035339,-25.8908327905953));
#41666=CARTESIAN_POINT('Ctrl Pts',(5.65703106079939,-3.71352778058156,-25.8820835768518));
#41667=CARTESIAN_POINT('Ctrl Pts',(5.75910210868871,-3.55803706597383,-25.8733344236056));
#41668=CARTESIAN_POINT('Ctrl Pts',(5.85475865698677,-3.39833575880679,-25.8645852703594));
#41669=CARTESIAN_POINT('Ctrl Pts',(5.94367583069183,-3.234966247065,-25.8558361171132));
#41670=CARTESIAN_POINT('Ctrl Pts',(6.03259241910196,-3.07159781069866,-25.847087021458));
#41671=CARTESIAN_POINT('Ctrl Pts',(6.11476958471085,-2.90456146975588,-25.8383379258029));
#41672=CARTESIAN_POINT('Ctrl Pts',(6.189928235745,-2.73442451647998,-25.8295888301478));
#41673=CARTESIAN_POINT('Ctrl Pts',(6.26508641701035,-2.5642886266217,-25.8208397891777));
#41674=CARTESIAN_POINT('Ctrl Pts',(6.33322605570383,-2.39105242531046,-25.8120907482076));
#41675=CARTESIAN_POINT('Ctrl Pts',(6.39411573747842,-2.21530425353513,-25.8033417072375));
#41676=CARTESIAN_POINT('Ctrl Pts',(6.45500505889196,-2.03955712188338,-25.7945927180465));
#41677=CARTESIAN_POINT('Ctrl Pts',(6.50864441544996,-1.86129832025341,-25.7858437288555));
#41678=CARTESIAN_POINT('Ctrl Pts',(6.55485164049968,-1.6811332401207,-25.7770947396645));
#41679=CARTESIAN_POINT('Ctrl Pts',(6.60199852639165,-1.49730435912654,-25.7681678327876));
#41680=CARTESIAN_POINT('Ctrl Pts',(6.64140767441059,-1.31149113173403,-25.7592409259107));
#41681=CARTESIAN_POINT('Ctrl Pts',(6.67293975269645,-1.12435050446178,-25.7503140190338));
#41682=CARTESIAN_POINT('Ctrl Pts',(6.70384664831542,-0.940920291561222,
-25.7415641048498));
#41683=CARTESIAN_POINT('Ctrl Pts',(6.72718585889694,-0.756215114275426,
-25.7328141906658));
#41684=CARTESIAN_POINT('Ctrl Pts',(6.74287810451885,-0.570862389372636,
-25.7240642764818));
#41685=CARTESIAN_POINT('Ctrl Pts',(6.75857004154137,-0.385513309565678,
-25.7153145343712));
#41686=CARTESIAN_POINT('Ctrl Pts',(6.76661529035563,-0.199516993256871,
-25.7065647922607));
#41687=CARTESIAN_POINT('Ctrl Pts',(6.76698652348897,-0.0135052182028017,
-25.6978150501501));
#41688=CARTESIAN_POINT('Ctrl Pts',(6.76735774981518,0.172503146040102,-25.6890654684794));
#41689=CARTESIAN_POINT('Ctrl Pts',(6.76005524147473,0.358526681834634,-25.6803158868088));
#41690=CARTESIAN_POINT('Ctrl Pts',(6.74510380214872,0.543933542115981,-25.6715663051382));
#41691=CARTESIAN_POINT('Ctrl Pts',(6.73015261710967,0.729337249085829,-25.6628168722762));
#41692=CARTESIAN_POINT('Ctrl Pts',(6.7075527844459,0.91412401585576,-25.6540674394143));
#41693=CARTESIAN_POINT('Ctrl Pts',(6.67738106408271,1.09766621749494,-25.6453180065524));
#41694=CARTESIAN_POINT('Ctrl Pts',(6.64720981677234,1.28120554143423,-25.63656871087));
#41695=CARTESIAN_POINT('Ctrl Pts',(6.60946696581502,1.46350005650714,-25.6278194151877));
#41696=CARTESIAN_POINT('Ctrl Pts',(6.56428070010972,1.64393062206621,-25.6190701195053));
#41697=CARTESIAN_POINT('Ctrl Pts',(6.51909508282717,1.82435859844738,-25.6103209493753));
#41698=CARTESIAN_POINT('Ctrl Pts',(6.46646633415635,2.00292240086648,-25.6015717792454));
#41699=CARTESIAN_POINT('Ctrl Pts',(6.40657319597164,2.17901557696537,-25.5928226091154));
#41700=CARTESIAN_POINT('Ctrl Pts',(6.34668083768264,2.35510646007518,-25.5840735529123));
#41701=CARTESIAN_POINT('Ctrl Pts',(6.27952437143852,2.52872650996614,-25.5753244967092));
#41702=CARTESIAN_POINT('Ctrl Pts',(6.205331873351,2.69928607998008,-25.5665754405061));
#41703=CARTESIAN_POINT('Ctrl Pts',(6.12831449784216,2.87633970115475,-25.5574932642173));
#41704=CARTESIAN_POINT('Ctrl Pts',(6.04371489463117,3.05009490562421,-25.5484110879285));
#41705=CARTESIAN_POINT('Ctrl Pts',(5.95184265120455,3.21991584599698,-25.5393289116396));
#41706=CARTESIAN_POINT('Ctrl Pts',(5.8633328133545,3.38352155905374,-25.5305791312852));
#41707=CARTESIAN_POINT('Ctrl Pts',(5.76807337235636,3.54347560903903,-25.5218293509308));
#41708=CARTESIAN_POINT('Ctrl Pts',(5.666387900863,3.69923467178731,-25.5130795705764));
#41709=CARTESIAN_POINT('Ctrl Pts',(5.56470608502682,3.85498813489852,-25.5043301047821));
#41710=CARTESIAN_POINT('Ctrl Pts',(5.45659885766885,4.00654667256353,-25.4955806389878));
#41711=CARTESIAN_POINT('Ctrl Pts',(5.34243340580433,4.15339551506306,-25.4868311731936));
#41712=CARTESIAN_POINT('Ctrl Pts',(5.22827145140514,4.30023985883968,-25.4780819754397));
#41713=CARTESIAN_POINT('Ctrl Pts',(5.10805181978004,4.44237456993141,-25.4693327776858));
#41714=CARTESIAN_POINT('Ctrl Pts',(4.9821828128246,4.57931691626549,-25.4605835799319));
#41715=CARTESIAN_POINT('Ctrl Pts',(4.8563169929615,4.71625579512242,-25.451834603714));
#41716=CARTESIAN_POINT('Ctrl Pts',(4.72480227791772,4.84800236135833,-25.443085627496));
#41717=CARTESIAN_POINT('Ctrl Pts',(4.58808530848063,4.97410918678955,-25.434336651278));
#41718=CARTESIAN_POINT('Ctrl Pts',(4.45135945056915,5.10022421089058,-25.4255871062568));
#41719=CARTESIAN_POINT('Ctrl Pts',(4.30943087207979,5.22069856612037,-25.4168375612356));
#41720=CARTESIAN_POINT('Ctrl Pts',(4.16278164322401,5.33512305301736,-25.4080880162144));
#41721=CARTESIAN_POINT('Ctrl Pts',(4.0161410353432,5.44954081331479,-25.3993389855471));
#41722=CARTESIAN_POINT('Ctrl Pts',(3.86478055833338,5.5579092406839,-25.3905899548798));
#41723=CARTESIAN_POINT('Ctrl Pts',(3.70921425811872,5.65986029751343,-25.3818409242126));
#41724=CARTESIAN_POINT('Ctrl Pts',(3.55364584530041,5.76181273884702,-25.3730917747327));
#41725=CARTESIAN_POINT('Ctrl Pts',(3.39387173464266,5.85734747818108,-25.3643426252529));
#41726=CARTESIAN_POINT('Ctrl Pts',(3.23043456092328,5.9461400544885,-25.355593475773));
#41727=CARTESIAN_POINT('Ctrl Pts',(3.1869076880634,5.96978744811309,-25.35326338704));
#41728=CARTESIAN_POINT('Ctrl Pts',(3.14312114982855,5.99295688499314,-25.350933298307));
#41729=CARTESIAN_POINT('Ctrl Pts',(3.09908550384719,6.01564277861013,-25.348603209574));
#41730=CARTESIAN_POINT('Origin',(0.,0.,-63.6971797838103));
#41731=CARTESIAN_POINT('',(3.09908550384719,6.01564277861013,-22.9543563216829));
#41732=CARTESIAN_POINT('',(3.09908550384722,6.01564277861011,-23.348603209574));
#41733=CARTESIAN_POINT('',(3.09908550384721,6.01564277861012,-63.6971797838103));
#41734=CARTESIAN_POINT('',(-6.76699985752918,-0.0013885964259113,-24.302820216155));
#41735=CARTESIAN_POINT('Ctrl Pts',(-6.76699985752918,-0.00138859642590996,
-24.302820216155));
#41736=CARTESIAN_POINT('Ctrl Pts',(-6.76696126318091,-0.189469124644247,
-24.2940182998959));
#41737=CARTESIAN_POINT('Ctrl Pts',(-6.75907723606001,-0.377334540807269,
-24.2852163836369));
#41738=CARTESIAN_POINT('Ctrl Pts',(-6.74342679625424,-0.564343905398435,
-24.2764144673779));
#41739=CARTESIAN_POINT('Ctrl Pts',(-6.72774331109054,-0.751748133741929,
-24.2675939661796));
#41740=CARTESIAN_POINT('Ctrl Pts',(-6.70426066358534,-0.938292432248802,
-24.2587734649813));
#41741=CARTESIAN_POINT('Ctrl Pts',(-6.67310915788618,-1.12334463408856,
-24.249952963783));
#41742=CARTESIAN_POINT('Ctrl Pts',(-6.6418545809807,-1.30900911945202,-24.2411032781303));
#41743=CARTESIAN_POINT('Ctrl Pts',(-6.60288040506713,-1.49317136165447,
-24.2322535924775));
#41744=CARTESIAN_POINT('Ctrl Pts',(-6.55636800887928,-1.67520969796153,
-24.2234039068248));
#41745=CARTESIAN_POINT('Ctrl Pts',(-6.50977942525895,-1.85754621356254,
-24.2145397253626));
#41746=CARTESIAN_POINT('Ctrl Pts',(-6.45562802879989,-2.03775161692499,
-24.2056755439005));
#41747=CARTESIAN_POINT('Ctrl Pts',(-6.39414431751011,-2.21522176019765,
-24.1968113624384));
#41748=CARTESIAN_POINT('Ctrl Pts',(-6.33249091550744,-2.39318170856659,
-24.1879227164598));
#41749=CARTESIAN_POINT('Ctrl Pts',(-6.26346480114711,-2.56839104029644,
-24.1790340704812));
#41750=CARTESIAN_POINT('Ctrl Pts',(-6.18734493758006,-2.7402648819781,-24.1701454245025));
#41751=CARTESIAN_POINT('Ctrl Pts',(-6.11503594919804,-2.90353400831308,
-24.161701780903));
#41752=CARTESIAN_POINT('Ctrl Pts',(-6.03632618151536,-3.06379328561213,
-24.1532581373035));
#41753=CARTESIAN_POINT('Ctrl Pts',(-5.95149173846921,-3.22056440502791,
-24.144814493704));
#41754=CARTESIAN_POINT('Ctrl Pts',(-5.87040260093117,-3.37041432927839,
-24.1367436235176));
#41755=CARTESIAN_POINT('Ctrl Pts',(-5.78350212677905,-3.51747328255109,
-24.1286727533313));
#41756=CARTESIAN_POINT('Ctrl Pts',(-5.69100705784284,-3.66124673678011,
-24.1206018831449));
#41757=CARTESIAN_POINT('Ctrl Pts',(-5.59862709183042,-3.80484127612065,
-24.1125410565291));
#41758=CARTESIAN_POINT('Ctrl Pts',(-5.50066658303825,-3.94515814187245,
-24.1044802299133));
#41759=CARTESIAN_POINT('Ctrl Pts',(-5.39738937150403,-4.08172475460747,
-24.0964194032975));
#41760=CARTESIAN_POINT('Ctrl Pts',(-5.29421803331549,-4.21815136778222,
-24.0883668401376));
#41761=CARTESIAN_POINT('Ctrl Pts',(-5.18574106188821,-4.35083508368595,
-24.0803142769777));
#41762=CARTESIAN_POINT('Ctrl Pts',(-5.07226699578639,-4.47932991902317,
-24.0722617138178));
#41763=CARTESIAN_POINT('Ctrl Pts',(-4.95888440959649,-4.60772116508556,
-24.06421564243));
#41764=CARTESIAN_POINT('Ctrl Pts',(-4.84051299257633,-4.7319299737604,-24.0561695710421));
#41765=CARTESIAN_POINT('Ctrl Pts',(-4.71750311646949,-4.85154133715262,
-24.0481234996542));
#41766=CARTESIAN_POINT('Ctrl Pts',(-4.59456550079222,-4.97108243652399,
-24.0400821548184));
#41767=CARTESIAN_POINT('Ctrl Pts',(-4.46699511709127,-5.08603120759034,
-24.0320408099825));
#41768=CARTESIAN_POINT('Ctrl Pts',(-4.33518086957777,-5.19600768167706,
-24.0239994651466));
#41769=CARTESIAN_POINT('Ctrl Pts',(-4.20082564896488,-5.30810416378636,
-24.0158031079256));
#41770=CARTESIAN_POINT('Ctrl Pts',(-4.06206154160527,-5.41503439628679,
-24.0076067507045));
#41771=CARTESIAN_POINT('Ctrl Pts',(-3.9193381014415,-5.51643706087444,-23.9994103934834));
#41772=CARTESIAN_POINT('Ctrl Pts',(-3.77935840701377,-5.61589033909452,
-23.9913716047749));
#41773=CARTESIAN_POINT('Ctrl Pts',(-3.63557055703218,-5.71002644174433,
-23.9833328160664));
#41774=CARTESIAN_POINT('Ctrl Pts',(-3.48842989759845,-5.79854687396259,
-23.9752940273579));
#41775=CARTESIAN_POINT('Ctrl Pts',(-3.341273492781,-5.88707677866912,-23.9672543784262));
#41776=CARTESIAN_POINT('Ctrl Pts',(-3.19076388411651,-5.96998962378017,
-23.9592147294945));
#41777=CARTESIAN_POINT('Ctrl Pts',(-3.03738278992653,-6.04703189899459,
-23.9511750805628));
#41778=CARTESIAN_POINT('Ctrl Pts',(-2.8839549125279,-6.12409767309495,-23.9431329794346));
#41779=CARTESIAN_POINT('Ctrl Pts',(-2.72765413979294,-6.19528914557821,
-23.9350908783065));
#41780=CARTESIAN_POINT('Ctrl Pts',(-2.56898387667595,-6.26040021415397,
-23.9270487771783));
#41781=CARTESIAN_POINT('Ctrl Pts',(-2.40495911557534,-6.32770852548052,
-23.9187352867335));
#41782=CARTESIAN_POINT('Ctrl Pts',(-2.23840254812185,-6.38851870702157,
-23.9104217962887));
#41783=CARTESIAN_POINT('Ctrl Pts',(-2.06988818108355,-6.44265876155261,
-23.9021083058439));
#41784=CARTESIAN_POINT('Ctrl Pts',(-1.90658770693222,-6.49512370404318,
-23.8940520376732));
#41785=CARTESIAN_POINT('Ctrl Pts',(-1.7414491532652,-6.54132509649991,-23.8859957695024));
#41786=CARTESIAN_POINT('Ctrl Pts',(-1.57500554275679,-6.5811584497173,-23.8779395013317));
#41787=CARTESIAN_POINT('Ctrl Pts',(-1.40059056081101,-6.62289951482055,
-23.8694973997499));
#41788=CARTESIAN_POINT('Ctrl Pts',(-1.22474292072371,-6.65764748650981,
-23.8610552981681));
#41789=CARTESIAN_POINT('Ctrl Pts',(-1.04808159823491,-6.68534321956931,
-23.8526131965863));
#41790=CARTESIAN_POINT('Ctrl Pts',(-0.871420275746075,-6.71303895262882,
-23.8441710950045));
#41791=CARTESIAN_POINT('Ctrl Pts',(-0.693945738634898,-6.73368247969746,
-23.8357289934227));
#41792=CARTESIAN_POINT('Ctrl Pts',(-0.516275786879578,-6.74727710353457,
-23.8272868918409));
#41793=CARTESIAN_POINT('Ctrl Pts',(-0.340884219412577,-6.76069739413723,
-23.8189530491482));
#41794=CARTESIAN_POINT('Ctrl Pts',(-0.164744669744684,-6.76729175556978,
-23.8106192064555));
#41795=CARTESIAN_POINT('Ctrl Pts',(0.0115772523575617,-6.76699009658119,
-23.8022853637629));
#41796=CARTESIAN_POINT('Ctrl Pts',(0.187691356767948,-6.76668879313588,
-23.7939613435581));
#41797=CARTESIAN_POINT('Ctrl Pts',(0.36398706053264,-6.75950766123828,-23.7856373233533));
#41798=CARTESIAN_POINT('Ctrl Pts',(0.539893785042186,-6.74542835562523,
-23.7773133031486));
#41799=CARTESIAN_POINT('Ctrl Pts',(0.715625433464996,-6.7313630628348,-23.7689975676577));
#41800=CARTESIAN_POINT('Ctrl Pts',(0.89096852936691,-6.71041330247559,-23.7606818321669));
#41801=CARTESIAN_POINT('Ctrl Pts',(1.06535241597644,-6.68261275473697,-23.752366096676));
#41802=CARTESIAN_POINT('Ctrl Pts',(1.23959469377682,-6.65483478249276,-23.744057113996));
#41803=CARTESIAN_POINT('Ctrl Pts',(1.41287897234954,-6.62021716259422,-23.735748131316));
#41804=CARTESIAN_POINT('Ctrl Pts',(1.58463941174141,-6.57884541046192,-23.7274391486359));
#41805=CARTESIAN_POINT('Ctrl Pts',(1.75629182636982,-6.5374996781381,-23.7191353916988));
#41806=CARTESIAN_POINT('Ctrl Pts',(1.92642197456027,-6.48940836033004,-23.7108316347616));
#41807=CARTESIAN_POINT('Ctrl Pts',(2.09447368731141,-6.43470814980448,-23.7025278778244));
#41808=CARTESIAN_POINT('Ctrl Pts',(2.26245717511828,-6.38003014624577,-23.6942274920124));
#41809=CARTESIAN_POINT('Ctrl Pts',(2.42836357859681,-6.3187487036407,-23.6859271062004));
#41810=CARTESIAN_POINT('Ctrl Pts',(2.59165110374154,-6.25105059621783,-23.6776267203883));
#41811=CARTESIAN_POINT('Ctrl Pts',(2.75490419579602,-6.18336676456428,-23.6693280849117));
#41812=CARTESIAN_POINT('Ctrl Pts',(2.91553918865101,-6.10926909693446,-23.6610294494351));
#41813=CARTESIAN_POINT('Ctrl Pts',(3.07303328924743,-6.02899290123791,-23.6527308139584));
#41814=CARTESIAN_POINT('Ctrl Pts',(3.23052032064901,-5.94872030877518,-23.6444325509699));
#41815=CARTESIAN_POINT('Ctrl Pts',(3.38486643097191,-5.86226989897023,-23.6361342879813));
#41816=CARTESIAN_POINT('Ctrl Pts',(3.53557233034882,-5.76992350875398,-23.6278360249927));
#41817=CARTESIAN_POINT('Ctrl Pts',(3.68629647956674,-5.67756593578412,-23.6195367571199));
#41818=CARTESIAN_POINT('Ctrl Pts',(3.83337924325554,-5.57931114192698,-23.6112374892471));
#41819=CARTESIAN_POINT('Ctrl Pts',(3.97634912170628,-5.47548506182838,-23.6029382213743));
#41820=CARTESIAN_POINT('Ctrl Pts',(4.11941938805517,-5.37158607908716,-23.5946331260778));
#41821=CARTESIAN_POINT('Ctrl Pts',(4.25837071686701,-5.2621081979698,-23.5863280307812));
#41822=CARTESIAN_POINT('Ctrl Pts',(4.39276288911597,-5.1474190814432,-23.5780229354847));
#41823=CARTESIAN_POINT('Ctrl Pts',(4.52720406773925,-5.03268814330094,-23.5697148117186));
#41824=CARTESIAN_POINT('Ctrl Pts',(4.65708251649328,-4.91274241357201,-23.5614066879525));
#41825=CARTESIAN_POINT('Ctrl Pts',(4.78199374036426,-4.78798755920658,-23.5530985641864));
#41826=CARTESIAN_POINT('Ctrl Pts',(4.90703774414458,-4.66310009115171,-23.5447816089327));
#41827=CARTESIAN_POINT('Ctrl Pts',(5.02710373249196,-4.5333935357797,-23.5364646536791));
#41828=CARTESIAN_POINT('Ctrl Pts',(5.14182575095762,-4.39930868964535,-23.5281476984254));
#41829=CARTESIAN_POINT('Ctrl Pts',(5.22637413311174,-4.30049019809801,-23.522018228943));
#41830=CARTESIAN_POINT('Ctrl Pts',(5.30802077137017,-4.19929437624894,-23.5158887594606));
#41831=CARTESIAN_POINT('Ctrl Pts',(5.38663401285674,-4.09590808143138,-23.5097592899781));
#41832=CARTESIAN_POINT('Ctrl Pts',(5.49502224369749,-3.9533639326779,-23.501308266453));
#41833=CARTESIAN_POINT('Ctrl Pts',(5.59784060462339,-3.80639422127925,-23.4928572429278));
#41834=CARTESIAN_POINT('Ctrl Pts',(5.69472503408853,-3.65546109076891,-23.4844062194027));
#41835=CARTESIAN_POINT('Ctrl Pts',(5.79152415969299,-3.50466085239416,-23.4759626367526));
#41836=CARTESIAN_POINT('Ctrl Pts',(5.88239958932085,-3.34990442815064,-23.4675190541025));
#41837=CARTESIAN_POINT('Ctrl Pts',(5.96702915765726,-3.19168482649338,-23.4590754714524));
#41838=CARTESIAN_POINT('Ctrl Pts',(6.05159571664363,-3.03358302425849,-23.4506381753126));
#41839=CARTESIAN_POINT('Ctrl Pts',(6.12992552853229,-2.87202347595894,-23.4422008791728));
#41840=CARTESIAN_POINT('Ctrl Pts',(6.20174098034566,-2.70752614257025,-23.433763583033));
#41841=CARTESIAN_POINT('Ctrl Pts',(6.27350519730995,-2.54314616548629,-23.4253323062607));
#41842=CARTESIAN_POINT('Ctrl Pts',(6.33876419210611,-2.37583288696878,-23.4169010294884));
#41843=CARTESIAN_POINT('Ctrl Pts',(6.39728725678751,-2.20612890696444,-23.408469752716));
#41844=CARTESIAN_POINT('Ctrl Pts',(6.45578523636488,-2.03649766822914,-23.4000420898941));
#41845=CARTESIAN_POINT('Ctrl Pts',(6.50755293384692,-1.86447808367463,-23.3916144270723));
#41846=CARTESIAN_POINT('Ctrl Pts',(6.55240832212275,-1.69063129634361,-23.3831867642504));
#41847=CARTESIAN_POINT('Ctrl Pts',(6.59724990213602,-1.51683802592948,-23.3747616957964));
#41848=CARTESIAN_POINT('Ctrl Pts',(6.63518333376086,-1.34121899507468,-23.3663366273425));
#41849=CARTESIAN_POINT('Ctrl Pts',(6.66607677140178,-1.16434937960118,-23.3579115588885));
#41850=CARTESIAN_POINT('Ctrl Pts',(6.67453016156533,-1.1159524389611,-23.3556062022745));
#41851=CARTESIAN_POINT('Ctrl Pts',(6.68245673431267,-1.06746193098025,-23.3533008456605));
#41852=CARTESIAN_POINT('Ctrl Pts',(6.68985445395339,-1.01888978055528,-23.3509954890464));
#41853=CARTESIAN_POINT('Ctrl Pts',(6.71751215354869,-0.837294098318812,
-23.3423765005219));
#41854=CARTESIAN_POINT('Ctrl Pts',(6.73776139366763,-0.654637731083349,
-23.3337575119974));
#41855=CARTESIAN_POINT('Ctrl Pts',(6.75055135896841,-0.471535099361469,
-23.3251385234728));
#41856=CARTESIAN_POINT('Ctrl Pts',(6.76334898659981,-0.288322772822682,
-23.316514371405));
#41857=CARTESIAN_POINT('Ctrl Pts',(6.7686783999153,-0.10466395165724,-23.3078902193371));
#41858=CARTESIAN_POINT('Ctrl Pts',(6.76654088834419,0.078825163280762,-23.2992660672693));
#41859=CARTESIAN_POINT('Ctrl Pts',(6.76433016642674,0.268598829766734,-23.2903465356731));
#41860=CARTESIAN_POINT('Ctrl Pts',(6.75413198765148,0.458190601449416,-23.2814270040769));
#41861=CARTESIAN_POINT('Ctrl Pts',(6.73600618976047,0.64692318826012,-23.2725074724807));
#41862=CARTESIAN_POINT('Ctrl Pts',(6.71844799839546,0.82974564363355,-23.2638672546214));
#41863=CARTESIAN_POINT('Ctrl Pts',(6.69345126546767,1.01176161468065,-23.2552270367621));
#41864=CARTESIAN_POINT('Ctrl Pts',(6.66112278249805,1.19236415431085,-23.2465868189028));
#41865=CARTESIAN_POINT('Ctrl Pts',(6.62722666728823,1.38172424572757,-23.2375276304382));
#41866=CARTESIAN_POINT('Ctrl Pts',(6.58527016512356,1.56953004256572,-23.2284684419736));
#41867=CARTESIAN_POINT('Ctrl Pts',(6.53543587681752,1.75509740470619,-23.2194092535089));
#41868=CARTESIAN_POINT('Ctrl Pts',(6.48560158851148,1.9406647668467,-23.2103500650443));
#41869=CARTESIAN_POINT('Ctrl Pts',(6.42788966055494,2.12399333926707,-23.2012908765797));
#41870=CARTESIAN_POINT('Ctrl Pts',(6.36254168908051,2.30442015585539,-23.1922316881151));
#41871=CARTESIAN_POINT('Ctrl Pts',(6.29730692838156,2.48453439564347,-23.1831881940588));
#41872=CARTESIAN_POINT('Ctrl Pts',(6.2244032583442,2.66192314364162,-23.1741447000026));
#41873=CARTESIAN_POINT('Ctrl Pts',(6.1440721534288,2.8359595154834,-23.1651012059463));
#41874=CARTESIAN_POINT('Ctrl Pts',(6.06381452708134,3.00983669689219,-23.156065983941));
#41875=CARTESIAN_POINT('Ctrl Pts',(5.97614312949107,3.18036740825088,-23.1470307619357));
#41876=CARTESIAN_POINT('Ctrl Pts',(5.88134716121483,3.34694555815752,-23.1379955399304));
#41877=CARTESIAN_POINT('Ctrl Pts',(5.78671820279783,3.51323023362767,-23.1289762360194));
#41878=CARTESIAN_POINT('Ctrl Pts',(5.68498985596708,3.67557604633669,-23.1199569321083));
#41879=CARTESIAN_POINT('Ctrl Pts',(5.57649665749191,3.83340240895494,-23.1109376281972));
#41880=CARTESIAN_POINT('Ctrl Pts',(5.46813957131234,3.99103076737732,-23.1019296396329));
#41881=CARTESIAN_POINT('Ctrl Pts',(5.35303470505299,4.14415079539388,-23.0929216510686));
#41882=CARTESIAN_POINT('Ctrl Pts',(5.23156056683908,4.29220957497352,-23.0839136625042));
#41883=CARTESIAN_POINT('Ctrl Pts',(5.11036078222108,4.43993395861358,-23.0749260187976));
#41884=CARTESIAN_POINT('Ctrl Pts',(4.98282059060928,4.58261972742745,-23.065938375091));
#41885=CARTESIAN_POINT('Ctrl Pts',(4.84935922262927,4.7197461933774,-23.0569507313843));
#41886=CARTESIAN_POINT('Ctrl Pts',(4.73312362134445,4.8391738409656,-23.0491231166506));
#41887=CARTESIAN_POINT('Ctrl Pts',(4.61239739832344,4.95438499555938,-23.041295501917));
#41888=CARTESIAN_POINT('Ctrl Pts',(4.48748318345316,5.06505515056106,-23.0334678871833));
#41889=CARTESIAN_POINT('Ctrl Pts',(4.35785277193138,5.17990371083857,-23.0253447370661));
#41890=CARTESIAN_POINT('Ctrl Pts',(4.22376899574635,5.28980931252195,-23.017221586949));
#41891=CARTESIAN_POINT('Ctrl Pts',(4.0856543433547,5.39441540731031,-23.0090984368318));
#41892=CARTESIAN_POINT('Ctrl Pts',(3.94755721279876,5.49900823130679,-23.0009763172534));
#41893=CARTESIAN_POINT('Ctrl Pts',(3.80543051846155,5.59830266940212,-22.992854197675));
#41894=CARTESIAN_POINT('Ctrl Pts',(3.65972842587266,5.6919835601361,-22.9847320780966));
#41895=CARTESIAN_POINT('Ctrl Pts',(3.51399481055972,5.78568471877986,-22.9766082012934));
#41896=CARTESIAN_POINT('Ctrl Pts',(3.36468456166332,5.87376970914436,-22.9684843244901));
#41897=CARTESIAN_POINT('Ctrl Pts',(3.21227947894243,5.95596755776636,-22.9603604476869));
#41898=CARTESIAN_POINT('Ctrl Pts',(3.17473339339418,5.97621758749729,-22.9583590723522));
#41899=CARTESIAN_POINT('Ctrl Pts',(3.13699959370374,5.99611053399551,-22.9563576970175));
#41900=CARTESIAN_POINT('Ctrl Pts',(3.09908550384719,6.01564277861013,-22.9543563216829));
#41901=CARTESIAN_POINT('Ctrl Pts',(3.09908550384718,6.01564277861014,-24.9542890874699));
#41902=CARTESIAN_POINT('Ctrl Pts',(2.93974250446997,6.09773169207842,-24.9458659075154));
#41903=CARTESIAN_POINT('Ctrl Pts',(2.77713343362295,6.17348699570386,-24.9374427275608));
#41904=CARTESIAN_POINT('Ctrl Pts',(2.61179253161539,6.24266199403733,-24.9290195476063));
#41905=CARTESIAN_POINT('Ctrl Pts',(2.44643071877461,6.31184574100368,-24.9205953023635));
#41906=CARTESIAN_POINT('Ctrl Pts',(2.27833669360101,6.37444739472453,-24.9121710571208));
#41907=CARTESIAN_POINT('Ctrl Pts',(2.10806433798888,6.43026855946931,-24.9037468118781));
#41908=CARTESIAN_POINT('Ctrl Pts',(1.93774669663451,6.48610457044599,-24.8953203261178));
#41909=CARTESIAN_POINT('Ctrl Pts',(1.76524988660969,6.53515639324064,-24.8868938403575));
#41910=CARTESIAN_POINT('Ctrl Pts',(1.59114294713281,6.57727550903788,-24.8784673545972));
#41911=CARTESIAN_POINT('Ctrl Pts',(1.41688211841228,6.61943185298291,-24.870033420854));
#41912=CARTESIAN_POINT('Ctrl Pts',(1.24100864062694,6.65464316526037,-24.8615994871107));
#41913=CARTESIAN_POINT('Ctrl Pts',(1.06410293293535,6.68281182947106,-24.8531655533675));
#41914=CARTESIAN_POINT('Ctrl Pts',(0.887119446636669,6.71099287835546,-24.8447279115493));
#41915=CARTESIAN_POINT('Ctrl Pts',(0.709103155837299,6.73212505908049,-24.8362902697311));
#41916=CARTESIAN_POINT('Ctrl Pts',(0.530640151997714,6.74616261507888,-24.8278526279129));
#41917=CARTESIAN_POINT('Ctrl Pts',(0.351964788015918,6.76021687491685,-24.8194049458131));
#41918=CARTESIAN_POINT('Ctrl Pts',(0.172841981973288,6.76715961762895,-24.8109572637133));
#41919=CARTESIAN_POINT('Ctrl Pts',(-0.00614018145540926,6.76699721428727,
-24.8025095816135));
#41920=CARTESIAN_POINT('Ctrl Pts',(-0.166031593208453,6.76685213335252,
-24.7949629535524));
#41921=CARTESIAN_POINT('Ctrl Pts',(-0.325810607070901,6.76103750980862,
-24.7874163254912));
#41922=CARTESIAN_POINT('Ctrl Pts',(-0.485061296249177,6.74959291653068,
-24.7798696974301));
#41923=CARTESIAN_POINT('Ctrl Pts',(-0.658960047123738,6.73709563638972,
-24.7716289218333));
#41924=CARTESIAN_POINT('Ctrl Pts',(-0.832615606941793,6.71785623257765,
-24.7633881462365));
#41925=CARTESIAN_POINT('Ctrl Pts',(-1.00546700708788,6.69188501826337,-24.7551473706398));
#41926=CARTESIAN_POINT('Ctrl Pts',(-1.17812695556864,6.66594256988461,-24.7469157225954));
#41927=CARTESIAN_POINT('Ctrl Pts',(-1.34998416916725,6.63328321007928,-24.738684074551));
#41928=CARTESIAN_POINT('Ctrl Pts',(-1.52047994699688,6.59396919395142,-24.7304524265066));
#41929=CARTESIAN_POINT('Ctrl Pts',(-1.69081726620803,6.55469171623385,-24.7222284289483));
#41930=CARTESIAN_POINT('Ctrl Pts',(-1.85979532491654,6.50877197895478,-24.7140044313901));
#41931=CARTESIAN_POINT('Ctrl Pts',(-2.0268627052942,6.45632376619137,-24.7057804338318));
#41932=CARTESIAN_POINT('Ctrl Pts',(-2.19378248099232,6.40392189162767,-24.6975637022073));
#41933=CARTESIAN_POINT('Ctrl Pts',(-2.35879460474896,6.34500314383873,-24.6893469705828));
#41934=CARTESIAN_POINT('Ctrl Pts',(-2.5213601055814,6.27973185876456,-24.6811302389583));
#41935=CARTESIAN_POINT('Ctrl Pts',(-2.68384231808897,6.21449401458632,-24.6729177170696));
#41936=CARTESIAN_POINT('Ctrl Pts',(-2.8438800747858,6.14291024732061,-24.6647051951809));
#41937=CARTESIAN_POINT('Ctrl Pts',(-3.00095137062681,6.06519413301281,-24.6564926732923));
#41938=CARTESIAN_POINT('Ctrl Pts',(-3.157970141071,5.98750400734744,-24.6482828977104));
#41939=CARTESIAN_POINT('Ctrl Pts',(-3.3120241083009,5.90368577745693,-24.6400731221286));
#41940=CARTESIAN_POINT('Ctrl Pts',(-3.46261291399464,5.81400041347071,-24.6318633465467));
#41941=CARTESIAN_POINT('Ctrl Pts',(-3.52838619199684,5.77482817652375,-24.6282775298641));
#41942=CARTESIAN_POINT('Ctrl Pts',(-3.5934987167778,5.7345372570846,-24.6246917131814));
#41943=CARTESIAN_POINT('Ctrl Pts',(-3.65791030015089,5.69315213533329,-24.6211058964987));
#41944=CARTESIAN_POINT('Ctrl Pts',(-3.81703835178444,5.59091068362489,-24.612247178977));
#41945=CARTESIAN_POINT('Ctrl Pts',(-3.97172164551044,5.48209412690925,-24.6033884614553));
#41946=CARTESIAN_POINT('Ctrl Pts',(-4.12145293553082,5.36711418736405,-24.5945297439335));
#41947=CARTESIAN_POINT('Ctrl Pts',(-4.27146434874709,5.25191913881842,-24.5856544531741));
#41948=CARTESIAN_POINT('Ctrl Pts',(-4.4165050382828,5.13053782208303,-24.5767791624147));
#41949=CARTESIAN_POINT('Ctrl Pts',(-4.55610228615621,5.00342092553506,-24.5679038716552));
#41950=CARTESIAN_POINT('Ctrl Pts',(-4.69609602160113,4.87594298841948,-24.5590033730745));
#41951=CARTESIAN_POINT('Ctrl Pts',(-4.83061518387692,4.74269704823708,-24.5501028744937));
#41952=CARTESIAN_POINT('Ctrl Pts',(-4.95922314274264,4.60417145863247,-24.541202375913));
#41953=CARTESIAN_POINT('Ctrl Pts',(-5.08800519837498,4.46545834675119,-24.5322898287153));
#41954=CARTESIAN_POINT('Ctrl Pts',(-5.21085989449811,4.32145150324707,-24.5233772815177));
#41955=CARTESIAN_POINT('Ctrl Pts',(-5.32739130261227,4.1726719148348,-24.5144647343201));
#41956=CARTESIAN_POINT('Ctrl Pts',(-5.44418002345574,4.02356380656185,-24.5055325073479));
#41957=CARTESIAN_POINT('Ctrl Pts',(-5.5546173685349,3.86966207927037,-24.4966002803756));
#41958=CARTESIAN_POINT('Ctrl Pts',(-5.6583494813666,3.711518576906,-24.4876680534034));
#41959=CARTESIAN_POINT('Ctrl Pts',(-5.75638830654893,3.56205470541254,-24.479226067458));
#41960=CARTESIAN_POINT('Ctrl Pts',(-5.84843801511981,3.40880228570009,-24.4707840815125));
#41961=CARTESIAN_POINT('Ctrl Pts',(-5.93423791843253,3.25224681219577,-24.462342095567));
#41962=CARTESIAN_POINT('Ctrl Pts',(-6.01993194663376,3.09588452455265,-24.4539105268385));
#41963=CARTESIAN_POINT('Ctrl Pts',(-6.09954851351526,2.93593918572723,-24.4454789581099));
#41964=CARTESIAN_POINT('Ctrl Pts',(-6.17278380768894,2.77290985492374,-24.4370473893814));
#41965=CARTESIAN_POINT('Ctrl Pts',(-6.24592343696218,2.61009348407181,-24.4286268345388));
#41966=CARTESIAN_POINT('Ctrl Pts',(-6.31269826743987,2.4442014499328,-24.4202062796963));
#41967=CARTESIAN_POINT('Ctrl Pts',(-6.37284955307715,2.27575868093354,-24.4117857248537));
#41968=CARTESIAN_POINT('Ctrl Pts',(-6.43293074713882,2.10751219068301,-24.4033749821033));
#41969=CARTESIAN_POINT('Ctrl Pts',(-6.48640366561141,1.93672120074102,-24.3949642393529));
#41970=CARTESIAN_POINT('Ctrl Pts',(-6.53305685168915,1.76393230385905,-24.3865534966025));
#41971=CARTESIAN_POINT('Ctrl Pts',(-6.57964837773527,1.59137177656423,-24.3781538700632));
#41972=CARTESIAN_POINT('Ctrl Pts',(-6.61943806093463,1.41681892897331,-24.3697542435239));
#41973=CARTESIAN_POINT('Ctrl Pts',(-6.65226369345949,1.24083711770753,-24.3613546169845));
#41974=CARTESIAN_POINT('Ctrl Pts',(-6.68506370311208,1.0649926734664,-24.3529615469848));
#41975=CARTESIAN_POINT('Ctrl Pts',(-6.71091043242371,0.887721814446482,
-24.344568476985));
#41976=CARTESIAN_POINT('Ctrl Pts',(-6.72969209734646,0.709600785591848,
-24.3361754069852));
#41977=CARTESIAN_POINT('Ctrl Pts',(-6.74845868258237,0.531622769049905,
-24.3277890757313));
#41978=CARTESIAN_POINT('Ctrl Pts',(-6.76017148011533,0.352796274545456,
-24.3194027444774));
#41979=CARTESIAN_POINT('Ctrl Pts',(-6.764770165924,0.173705504301365,-24.3110164132235));
#41980=CARTESIAN_POINT('Ctrl Pts',(-6.76626830751665,0.115362024680058,
-24.3082843475457));
#41981=CARTESIAN_POINT('Ctrl Pts',(-6.76701183699318,0.0569905504860054,
-24.3055522818678));
#41982=CARTESIAN_POINT('Ctrl Pts',(-6.76699985752934,-0.0013885956796133,
-24.3028202161899));
#41983=CARTESIAN_POINT('',(-6.767,5.12853742065664E-10,-24.6971797838342));
#41984=CARTESIAN_POINT('Ctrl Pts',(3.09908550384719,6.01564277861013,-25.348603209574));
#41985=CARTESIAN_POINT('Ctrl Pts',(2.93373232018326,6.10082796552481,-25.3398537616747));
#41986=CARTESIAN_POINT('Ctrl Pts',(2.76486502144422,6.17919158180192,-25.3311043137754));
#41987=CARTESIAN_POINT('Ctrl Pts',(2.59305716434347,6.25046746591381,-25.3223548658761));
#41988=CARTESIAN_POINT('Ctrl Pts',(2.42125069459279,6.32174277447226,-25.3136054886287));
#41989=CARTESIAN_POINT('Ctrl Pts',(2.24650397871055,6.38593035557827,-25.3048561113813));
#41990=CARTESIAN_POINT('Ctrl Pts',(2.06941053323769,6.44281220003539,-25.2961067341338));
#41991=CARTESIAN_POINT('Ctrl Pts',(1.89231845896684,6.49969360406685,-25.2873574246312));
#41992=CARTESIAN_POINT('Ctrl Pts',(1.71287996431508,6.5492692970088,-25.2786081151286));
#41993=CARTESIAN_POINT('Ctrl Pts',(1.53170449173509,6.59137090065478,-25.269858805626));
#41994=CARTESIAN_POINT('Ctrl Pts',(1.35053036178181,6.63347219230081,-25.2611095609615));
#41995=CARTESIAN_POINT('Ctrl Pts',(1.16761955878861,6.66809944062451,-25.2523603162969));
#41996=CARTESIAN_POINT('Ctrl Pts',(0.983593309310713,6.69513503985388,-25.2436110716323));
#41997=CARTESIAN_POINT('Ctrl Pts',(0.799568362460183,6.72217044771212,-25.2348618888991));
#41998=CARTESIAN_POINT('Ctrl Pts',(0.614428268438772,6.74161427235975,-25.2261127061659));
#41999=CARTESIAN_POINT('Ctrl Pts',(0.428801816330421,6.75340047696801,-25.2173635234328));
#42000=CARTESIAN_POINT('Ctrl Pts',(0.243176616522949,6.76518660206241,-25.2086143997246));
#42001=CARTESIAN_POINT('Ctrl Pts',(0.0570653511656382,6.76931519233997,
-25.1998652760165));
#42002=CARTESIAN_POINT('Ctrl Pts',(-0.12889990079984,6.76577222610796,-25.1911161523084));
#42003=CARTESIAN_POINT('Ctrl Pts',(-0.314863959942008,6.76222928260134,
-25.1823670847191));
#42004=CARTESIAN_POINT('Ctrl Pts',(-0.500681721080844,6.75101488651276,
-25.1736180171298));
#42005=CARTESIAN_POINT('Ctrl Pts',(-0.685722110173637,6.73216712415987,
-25.1648689495405));
#42006=CARTESIAN_POINT('Ctrl Pts',(-0.870761373827949,6.71331947644141,
-25.1561199351642));
#42007=CARTESIAN_POINT('Ctrl Pts',(-1.05502298984377,6.68683858439991,-25.1473709207878));
#42008=CARTESIAN_POINT('Ctrl Pts',(-1.23788117676093,6.6528143813142,-25.1386219064115));
#42009=CARTESIAN_POINT('Ctrl Pts',(-1.43009641450781,6.61704912302565,-25.1294251955244));
#42010=CARTESIAN_POINT('Ctrl Pts',(-1.62076048990655,6.57294837083637,-25.1202284846374));
#42011=CARTESIAN_POINT('Ctrl Pts',(-1.8091579895809,6.52067760042893,-25.1110317737504));
#42012=CARTESIAN_POINT('Ctrl Pts',(-1.98840442999994,6.47094578578336,-25.1022817760439));
#42013=CARTESIAN_POINT('Ctrl Pts',(-2.165598959492,6.41381888475486,-25.0935317783374));
#42014=CARTESIAN_POINT('Ctrl Pts',(-2.3401396623936,6.34949095286326,-25.0847817806309));
#42015=CARTESIAN_POINT('Ctrl Pts',(-2.51467682551077,6.2851643255786,-25.0760319603793));
#42016=CARTESIAN_POINT('Ctrl Pts',(-2.68656000075933,6.21363705880919,-25.0672821401277));
#42017=CARTESIAN_POINT('Ctrl Pts',(-2.85520533838011,6.13515211512198,-25.0585323198761));
#42018=CARTESIAN_POINT('Ctrl Pts',(-3.02384747995483,6.05666865882541,-25.0497826654448));
#42019=CARTESIAN_POINT('Ctrl Pts',(-3.18925164681729,5.97122791041344,-25.0410330110136));
#42020=CARTESIAN_POINT('Ctrl Pts',(-3.35085601826389,5.87912008253486,-25.0322833565824));
#42021=CARTESIAN_POINT('Ctrl Pts',(-3.51245754188701,5.78701387779823,-25.0235338563392));
#42022=CARTESIAN_POINT('Ctrl Pts',(-3.67025915508273,5.68824097062701,-25.0147843560961));
#42023=CARTESIAN_POINT('Ctrl Pts',(-3.82372487926228,5.58313684658639,-25.0060348558529));
#42024=CARTESIAN_POINT('Ctrl Pts',(-3.97718810298238,5.47803443503632,-24.9972854981678));
#42025=CARTESIAN_POINT('Ctrl Pts',(-4.12631534260514,5.36660117498307,-24.9885361404827));
#42026=CARTESIAN_POINT('Ctrl Pts',(-4.27060009883765,5.24921554099352,-24.9797867827976));
#42027=CARTESIAN_POINT('Ctrl Pts',(-4.41488269591803,5.13183166362364,-24.9710375560424));
#42028=CARTESIAN_POINT('Ctrl Pts',(-4.55432273232732,5.00849577141613,-24.9622883292872));
#42029=CARTESIAN_POINT('Ctrl Pts',(-4.68844662477907,4.87962675279552,-24.953539102532));
#42030=CARTESIAN_POINT('Ctrl Pts',(-4.82256868832932,4.75075949142141,-24.9447899950805));
#42031=CARTESIAN_POINT('Ctrl Pts',(-4.95137454635713,4.61635945314831,-24.936040887629));
#42032=CARTESIAN_POINT('Ctrl Pts',(-5.07442674459007,4.47688309136938,-24.9272917801775));
#42033=CARTESIAN_POINT('Ctrl Pts',(-5.19747742836518,4.33740844618772,-24.9185427804052));
#42034=CARTESIAN_POINT('Ctrl Pts',(-5.3147744044896,4.19285781738521,-24.9097937806328));
#42035=CARTESIAN_POINT('Ctrl Pts',(-5.42591931529244,4.04372212001968,-24.9010447808604));
#42036=CARTESIAN_POINT('Ctrl Pts',(-5.5370763646114,3.89457013503419,-24.8922948255799));
#42037=CARTESIAN_POINT('Ctrl Pts',(-5.642079832717,3.74083230919091,-24.8835448702993));
#42038=CARTESIAN_POINT('Ctrl Pts',(-5.74057303467049,3.58303087254548,-24.8747949150187));
#42039=CARTESIAN_POINT('Ctrl Pts',(-5.83906243362146,3.42523552890191,-24.8660452975899));
#42040=CARTESIAN_POINT('Ctrl Pts',(-5.93104191766888,3.26337713159788,-24.8572956801611));
#42041=CARTESIAN_POINT('Ctrl Pts',(-6.016199066982,3.09800545293983,-24.8485460627323));
#42042=CARTESIAN_POINT('Ctrl Pts',(-6.10135338094014,2.93263928042444,-24.8397967366269));
#42043=CARTESIAN_POINT('Ctrl Pts',(-6.17968568351558,2.7637603154309,-24.8310474105215));
#42044=CARTESIAN_POINT('Ctrl Pts',(-6.25092992693692,2.59194213834421,-24.8222980844161));
#42045=CARTESIAN_POINT('Ctrl Pts',(-6.32217217689992,2.42012876883723,-24.8135490031223));
#42046=CARTESIAN_POINT('Ctrl Pts',(-6.38632665482822,2.24537661650595,-24.8047999218285));
#42047=CARTESIAN_POINT('Ctrl Pts',(-6.44317547868406,2.06827917624398,-24.7960508405347));
#42048=CARTESIAN_POINT('Ctrl Pts',(-6.50002944235073,1.8911657242639,-24.7873009682197));
#42049=CARTESIAN_POINT('Ctrl Pts',(-6.54957634249617,1.71170683292186,-24.7785510959048));
#42050=CARTESIAN_POINT('Ctrl Pts',(-6.59164787707697,1.53051209228371,-24.7698012235898));
#42051=CARTESIAN_POINT('Ctrl Pts',(-6.63371649074386,1.34932993151087,-24.761051958755));
#42052=CARTESIAN_POINT('Ctrl Pts',(-6.6683107125658,1.16641244177108,-24.7523026939202));
#42053=CARTESIAN_POINT('Ctrl Pts',(-6.69531304839871,0.982380875191491,
-24.7435534290855));
#42054=CARTESIAN_POINT('Ctrl Pts',(-6.72231677032668,0.798339861827445,
-24.7348037151298));
#42055=CARTESIAN_POINT('Ctrl Pts',(-6.74172778477602,0.613184940761843,
-24.7260540011742));
#42056=CARTESIAN_POINT('Ctrl Pts',(-6.75348015835317,0.427545027722295,
-24.7173042872185));
#42057=CARTESIAN_POINT('Ctrl Pts',(-6.76249038364074,0.285219953738662,
-24.7105961194237));
#42058=CARTESIAN_POINT('Ctrl Pts',(-6.76699999998919,0.142609996109865,
-24.703887951629));
#42059=CARTESIAN_POINT('Ctrl Pts',(-6.767,5.12854570784153E-10,-24.6971797838342));
#42060=CARTESIAN_POINT('Ctrl Pts',(-6.767,2.94242285249967E-13,-24.6971797838101));
#42061=CARTESIAN_POINT('Ctrl Pts',(-6.76700000000001,-0.186007249559716,
-24.6884302719974));
#42062=CARTESIAN_POINT('Ctrl Pts',(-6.75932637294248,-0.3720143558159,-24.6796807601846));
#42063=CARTESIAN_POINT('Ctrl Pts',(-6.74400518263364,-0.557389537586276,
-24.6709312483719));
#42064=CARTESIAN_POINT('Ctrl Pts',(-6.7286840570373,-0.742763936382717,
-24.6621817735147));
#42065=CARTESIAN_POINT('Ctrl Pts',(-6.70571545643564,-0.927506130404996,
-24.6534322986575));
#42066=CARTESIAN_POINT('Ctrl Pts',(-6.67517739401574,-1.11098864009548,
-24.6446828238003));
#42067=CARTESIAN_POINT('Ctrl Pts',(-6.64463945804389,-1.2944703900454,-24.6359333851718));
#42068=CARTESIAN_POINT('Ctrl Pts',(-6.60653217002725,-1.47669218339272,
-24.6271839465433));
#42069=CARTESIAN_POINT('Ctrl Pts',(-6.56098496085482,-1.65703510627773,
-24.6184345079148));
#42070=CARTESIAN_POINT('Ctrl Pts',(-6.51543793649556,-1.83737729740012,
-24.6096851047881));
#42071=CARTESIAN_POINT('Ctrl Pts',(-6.46245112156892,-2.01584035544967,
-24.6009357016615));
#42072=CARTESIAN_POINT('Ctrl Pts',(-6.40220448361708,-2.19181813797436,
-24.5921862985348));
#42073=CARTESIAN_POINT('Ctrl Pts',(-6.34195808511964,-2.36779522106327,
-24.5834369301833));
#42074=CARTESIAN_POINT('Ctrl Pts',(-6.27445201416346,-2.54128677725765,
-24.5746875618318));
#42075=CARTESIAN_POINT('Ctrl Pts',(-6.19991555052717,-2.71170355428676,
-24.5659381934802));
#42076=CARTESIAN_POINT('Ctrl Pts',(-6.12537937695099,-2.88211966813562,
-24.5571888591771));
#42077=CARTESIAN_POINT('Ctrl Pts',(-6.04381298028314,-3.04946076419942,
-24.5484395248739));
#42078=CARTESIAN_POINT('Ctrl Pts',(-5.95549339308826,-3.21315848424601,
-24.5396901905707));
#42079=CARTESIAN_POINT('Ctrl Pts',(-5.86717414225632,-3.3768555808539,-24.5309408895891));
#42080=CARTESIAN_POINT('Ctrl Pts',(-5.77210188843868,-3.53690907700326,
-24.5221915886075));
#42081=CARTESIAN_POINT('Ctrl Pts',(-5.67059953311149,-3.69277537024333,
-24.513442287626));
#42082=CARTESIAN_POINT('Ctrl Pts',(-5.56909755592458,-3.84864108281388,
-24.5046930192393));
#42083=CARTESIAN_POINT('Ctrl Pts',(-5.46116568154688,-4.00031938355209,
-24.4959437508527));
#42084=CARTESIAN_POINT('Ctrl Pts',(-5.3471704848807,-4.14729511918561,-24.4871944824661));
#42085=CARTESIAN_POINT('Ctrl Pts',(-5.23317570342983,-4.29427031947572,
-24.4784452459477));
#42086=CARTESIAN_POINT('Ctrl Pts',(-5.1131178195121,-4.43654276249944,-24.4696960094294));
#42087=CARTESIAN_POINT('Ctrl Pts',(-4.98740458928893,-4.57362924412766,
-24.460946772911));
#42088=CARTESIAN_POINT('Ctrl Pts',(-4.8616918065238,-4.71071523781639,-24.4521975675343));
#42089=CARTESIAN_POINT('Ctrl Pts',(-4.73032391141204,-4.84261509584849,
-24.4434483621576));
#42090=CARTESIAN_POINT('Ctrl Pts',(-4.59374706946951,-4.96888084599946,
-24.4346991567809));
#42091=CARTESIAN_POINT('Ctrl Pts',(-4.45717070231163,-5.09514615721042,
-24.4259499818192));
#42092=CARTESIAN_POINT('Ctrl Pts',(-4.31538563497053,-5.21577720520838,
-24.4172008068575));
#42093=CARTESIAN_POINT('Ctrl Pts',(-4.16887340951768,-5.33036429293688,
-24.4084516318958));
#42094=CARTESIAN_POINT('Ctrl Pts',(-4.0223616812227,-5.44495099183863,-24.3997024866226));
#42095=CARTESIAN_POINT('Ctrl Pts',(-3.87112305262993,-5.55349359498058,
-24.3909533413494));
#42096=CARTESIAN_POINT('Ctrl Pts',(-3.71567116928835,-5.65562346357317,
-24.3822041960761));
#42097=CARTESIAN_POINT('Ctrl Pts',(-3.5602198005318,-5.75775299409007,-24.3734550797648));
#42098=CARTESIAN_POINT('Ctrl Pts',(-3.40055544441984,-5.85346967519936,
-24.3647059634534));
#42099=CARTESIAN_POINT('Ctrl Pts',(-3.23722035886776,-5.94244843041419,
-24.3559568471421));
#42100=CARTESIAN_POINT('Ctrl Pts',(-3.07388580043406,-6.03142689847494,
-24.347207759066));
#42101=CARTESIAN_POINT('Ctrl Pts',(-2.90688078789121,-6.11366734707951,
-24.33845867099));
#42102=CARTESIAN_POINT('Ctrl Pts',(-2.73677250610272,-6.18889047001482,
-24.329709582914));
#42103=CARTESIAN_POINT('Ctrl Pts',(-2.56666475916807,-6.26411335643386,
-24.3209605223468));
#42104=CARTESIAN_POINT('Ctrl Pts',(-2.39345402456959,-6.33231884545306,
-24.3122114617797));
#42105=CARTESIAN_POINT('Ctrl Pts',(-2.21772855943924,-6.39327529804931,
-24.3034624012125));
#42106=CARTESIAN_POINT('Ctrl Pts',(-2.04200363223474,-6.45423156404739,
-24.2947133674277));
#42107=CARTESIAN_POINT('Ctrl Pts',(-1.86376426060941,-6.50793874412479,
-24.2859643336429));
#42108=CARTESIAN_POINT('Ctrl Pts',(-1.6836157762162,-6.5542144394333,-24.2772152998581));
#42109=CARTESIAN_POINT('Ctrl Pts',(-1.50346782833139,-6.60048999692605,
-24.2684662921292));
#42110=CARTESIAN_POINT('Ctrl Pts',(-1.32141105657302,-6.63933404265179,
-24.2597172844003));
#42111=CARTESIAN_POINT('Ctrl Pts',(-1.13806375346441,-6.67061465631545,
-24.2509682766714));
#42112=CARTESIAN_POINT('Ctrl Pts',(-0.95471698116888,-6.70189517941787,
-24.242219294272));
#42113=CARTESIAN_POINT('Ctrl Pts',(-0.770079967440963,-6.7256122660902,
-24.2334703118725));
#42114=CARTESIAN_POINT('Ctrl Pts',(-0.584779764071558,-6.74168536995998,
-24.2247213294731));
#42115=CARTESIAN_POINT('Ctrl Pts',(-0.391489587591418,-6.75845153117881,
-24.2155950990575));
#42116=CARTESIAN_POINT('Ctrl Pts',(-0.19747809180367,-6.76689985146399,
-24.2064688686419));
#42117=CARTESIAN_POINT('Ctrl Pts',(-0.00346214752944239,-6.76699911434415,
-24.1973426382262));
#42118=CARTESIAN_POINT('Ctrl Pts',(0.184490798486235,-6.76709527525931,
-24.1885016025111));
#42119=CARTESIAN_POINT('Ctrl Pts',(0.372447602156376,-6.75935633790754,
-24.179660566796));
#42120=CARTESIAN_POINT('Ctrl Pts',(0.559756448195814,-6.743809140145,-24.1708195310809));
#42121=CARTESIAN_POINT('Ctrl Pts',(0.745136131044969,-6.72842206873137,
-24.1620695524675));
#42122=CARTESIAN_POINT('Ctrl Pts',(0.929880851946669,-6.70538686355701,
-24.1533195738542));
#42123=CARTESIAN_POINT('Ctrl Pts',(1.11336305057626,-6.67478177303285,-24.1445695952409));
#42124=CARTESIAN_POINT('Ctrl Pts',(1.29684337090294,-6.64417699581227,-24.1358197062009));
#42125=CARTESIAN_POINT('Ctrl Pts',(1.47906091205368,-6.6060025354802,-24.127069817161));
#42126=CARTESIAN_POINT('Ctrl Pts',(1.65939671095406,-6.56038806441165,-24.118319928121));
#42127=CARTESIAN_POINT('Ctrl Pts',(1.83973072369344,-6.51477404513798,-24.1095701257455));
#42128=CARTESIAN_POINT('Ctrl Pts',(2.01818275357219,-6.46172023288604,-24.10082032337));
#42129=CARTESIAN_POINT('Ctrl Pts',(2.19414664033507,-6.40140683918046,-24.0920705209945));
#42130=CARTESIAN_POINT('Ctrl Pts',(2.37010884271446,-6.34109402281428,-24.083320802375));
#42131=CARTESIAN_POINT('Ctrl Pts',(2.54358267847997,-6.27352185699714,-24.0745710837554));
#42132=CARTESIAN_POINT('Ctrl Pts',(2.71397890841937,-6.19891986435176,-24.0658213651359));
#42133=CARTESIAN_POINT('Ctrl Pts',(2.88437356389145,-6.12431856103148,-24.0570717273641));
#42134=CARTESIAN_POINT('Ctrl Pts',(3.05169040787381,-6.04268767582452,-24.0483220895922));
#42135=CARTESIAN_POINT('Ctrl Pts',(3.21536112512269,-5.95430447953829,-24.0395724518204));
#42136=CARTESIAN_POINT('Ctrl Pts',(3.37903038443055,-5.8659220705492,-24.0308228919883));
#42137=CARTESIAN_POINT('Ctrl Pts',(3.53905332980183,-5.77078760703248,-24.0220733321563));
#42138=CARTESIAN_POINT('Ctrl Pts',(3.69488643042099,-5.66922422085164,-24.0133237723242));
#42139=CARTESIAN_POINT('Ctrl Pts',(3.85071819468949,-5.56766170563015,-24.0045742875242));
#42140=CARTESIAN_POINT('Ctrl Pts',(4.0023599459943,-5.459670534561,-23.9958248027242));
#42141=CARTESIAN_POINT('Ctrl Pts',(4.14929662974506,-5.34561750206525,-23.9870753179242));
#42142=CARTESIAN_POINT('Ctrl Pts',(4.29623210225248,-5.23156540974299,-23.9783259052488));
#42143=CARTESIAN_POINT('Ctrl Pts',(4.43846235842319,-5.11145173172011,-23.9695764925735));
#42144=CARTESIAN_POINT('Ctrl Pts',(4.57550431797629,-4.98568443006378,-23.9608270798981));
#42145=CARTESIAN_POINT('Ctrl Pts',(4.71254519337698,-4.85991812336492,-23.9520777364402));
#42146=CARTESIAN_POINT('Ctrl Pts',(4.8443976431519,-4.7284984763089,-23.9433283929823));
#42147=CARTESIAN_POINT('Ctrl Pts',(4.97061384196894,-4.59187184425118,-23.9345790495244));
#42148=CARTESIAN_POINT('Ctrl Pts',(5.09682908420408,-4.45524624767517,-23.9258297723771));
#42149=CARTESIAN_POINT('Ctrl Pts',(5.21740796650366,-4.31341395556657,-23.9170804952297));
#42150=CARTESIAN_POINT('Ctrl Pts',(5.33194095942439,-4.16685668162616,-23.9083312180823));
#42151=CARTESIAN_POINT('Ctrl Pts',(5.44647312235317,-4.02030046974965,-23.8995820043388));
#42152=CARTESIAN_POINT('Ctrl Pts',(5.55495930712468,-3.86901957035289,-23.8908327905953));
#42153=CARTESIAN_POINT('Ctrl Pts',(5.6570310607997,-3.71352778058107,-23.8820835768517));
#42154=CARTESIAN_POINT('Ctrl Pts',(5.75910210868896,-3.55803706597342,-23.8733344236055));
#42155=CARTESIAN_POINT('Ctrl Pts',(5.85475865698696,-3.39833575880646,-23.8645852703593));
#42156=CARTESIAN_POINT('Ctrl Pts',(5.94367583069196,-3.23496624706475,-23.8558361171131));
#42157=CARTESIAN_POINT('Ctrl Pts',(6.032592419102,-3.07159781069858,-23.847087021458));
#42158=CARTESIAN_POINT('Ctrl Pts',(6.1147695847108,-2.90456146975597,-23.8383379258029));
#42159=CARTESIAN_POINT('Ctrl Pts',(6.18992823574488,-2.73442451648025,-23.8295888301478));
#42160=CARTESIAN_POINT('Ctrl Pts',(6.26508641701032,-2.56428862662178,-23.8208397891777));
#42161=CARTESIAN_POINT('Ctrl Pts',(6.33322605570389,-2.39105242531033,-23.8120907482076));
#42162=CARTESIAN_POINT('Ctrl Pts',(6.39411573747854,-2.21530425353479,-23.8033417072374));
#42163=CARTESIAN_POINT('Ctrl Pts',(6.45500505889202,-2.03955712188319,-23.7945927180464));
#42164=CARTESIAN_POINT('Ctrl Pts',(6.50864441544996,-1.86129832025337,-23.7858437288555));
#42165=CARTESIAN_POINT('Ctrl Pts',(6.55485164049965,-1.68113324012082,-23.7770947396645));
#42166=CARTESIAN_POINT('Ctrl Pts',(6.60199852639162,-1.49730435912667,-23.7681678327876));
#42167=CARTESIAN_POINT('Ctrl Pts',(6.64140767441057,-1.31149113173415,-23.7592409259107));
#42168=CARTESIAN_POINT('Ctrl Pts',(6.67293975269643,-1.12435050446191,-23.7503140190338));
#42169=CARTESIAN_POINT('Ctrl Pts',(6.7038466483154,-0.940920291561387,-23.7415641048498));
#42170=CARTESIAN_POINT('Ctrl Pts',(6.72718585889692,-0.756215114275625,
-23.7328141906658));
#42171=CARTESIAN_POINT('Ctrl Pts',(6.74287810451883,-0.570862389372871,
-23.7240642764818));
#42172=CARTESIAN_POINT('Ctrl Pts',(6.75857004154136,-0.385513309565883,
-23.7153145343713));
#42173=CARTESIAN_POINT('Ctrl Pts',(6.76661529035562,-0.199516993257048,
-23.7065647922607));
#42174=CARTESIAN_POINT('Ctrl Pts',(6.76698652348897,-0.0135052182029489,
-23.6978150501501));
#42175=CARTESIAN_POINT('Ctrl Pts',(6.76735774981518,0.172503146039984,-23.6890654684794));
#42176=CARTESIAN_POINT('Ctrl Pts',(6.76005524147474,0.358526681834546,-23.6803158868088));
#42177=CARTESIAN_POINT('Ctrl Pts',(6.74510380214873,0.543933542115922,-23.6715663051382));
#42178=CARTESIAN_POINT('Ctrl Pts',(6.73015261710968,0.729337249085736,-23.6628168722762));
#42179=CARTESIAN_POINT('Ctrl Pts',(6.70755278444592,0.914124015855634,-23.6540674394143));
#42180=CARTESIAN_POINT('Ctrl Pts',(6.67738106408274,1.09766621749478,-23.6453180065524));
#42181=CARTESIAN_POINT('Ctrl Pts',(6.64720981677236,1.28120554143416,-23.63656871087));
#42182=CARTESIAN_POINT('Ctrl Pts',(6.60946696581501,1.46350005650716,-23.6278194151877));
#42183=CARTESIAN_POINT('Ctrl Pts',(6.5642807001097,1.64393062206632,-23.6190701195053));
#42184=CARTESIAN_POINT('Ctrl Pts',(6.51909508282715,1.82435859844743,-23.6103209493753));
#42185=CARTESIAN_POINT('Ctrl Pts',(6.46646633415636,2.00292240086646,-23.6015717792454));
#42186=CARTESIAN_POINT('Ctrl Pts',(6.40657319597167,2.17901557696529,-23.5928226091154));
#42187=CARTESIAN_POINT('Ctrl Pts',(6.34668083768268,2.35510646007506,-23.5840735529123));
#42188=CARTESIAN_POINT('Ctrl Pts',(6.27952437143857,2.528726509966,-23.5753244967092));
#42189=CARTESIAN_POINT('Ctrl Pts',(6.20533187335107,2.69928607997991,-23.5665754405061));
#42190=CARTESIAN_POINT('Ctrl Pts',(6.12831449784224,2.87633970115458,-23.5574932642173));
#42191=CARTESIAN_POINT('Ctrl Pts',(6.04371489463125,3.05009490562404,-23.5484110879285));
#42192=CARTESIAN_POINT('Ctrl Pts',(5.95184265120464,3.21991584599681,-23.5393289116396));
#42193=CARTESIAN_POINT('Ctrl Pts',(5.8633328133546,3.38352155905357,-23.5305791312852));
#42194=CARTESIAN_POINT('Ctrl Pts',(5.76807337235647,3.54347560903886,-23.5218293509308));
#42195=CARTESIAN_POINT('Ctrl Pts',(5.66638790086311,3.69923467178715,-23.5130795705764));
#42196=CARTESIAN_POINT('Ctrl Pts',(5.56470608502697,3.85498813489831,-23.5043301047821));
#42197=CARTESIAN_POINT('Ctrl Pts',(5.45659885766904,4.00654667256326,-23.4955806389878));
#42198=CARTESIAN_POINT('Ctrl Pts',(5.34243340580458,4.15339551506275,-23.4868311731936));
#42199=CARTESIAN_POINT('Ctrl Pts',(5.22827145140539,4.30023985883937,-23.4780819754397));
#42200=CARTESIAN_POINT('Ctrl Pts',(5.1080518197803,4.44237456993111,-23.4693327776858));
#42201=CARTESIAN_POINT('Ctrl Pts',(4.98218281282487,4.57931691626519,-23.460583579932));
#42202=CARTESIAN_POINT('Ctrl Pts',(4.8563169929617,4.71625579512222,-23.451834603714));
#42203=CARTESIAN_POINT('Ctrl Pts',(4.72480227791784,4.84800236135822,-23.443085627496));
#42204=CARTESIAN_POINT('Ctrl Pts',(4.58808530848065,4.97410918678953,-23.434336651278));
#42205=CARTESIAN_POINT('Ctrl Pts',(4.45135945056915,5.10022421089058,-23.4255871062568));
#42206=CARTESIAN_POINT('Ctrl Pts',(4.30943087207976,5.22069856612039,-23.4168375612356));
#42207=CARTESIAN_POINT('Ctrl Pts',(4.16278164322396,5.3351230530174,-23.4080880162144));
#42208=CARTESIAN_POINT('Ctrl Pts',(4.01614103534315,5.44954081331483,-23.3993389855471));
#42209=CARTESIAN_POINT('Ctrl Pts',(3.86478055833334,5.55790924068393,-23.3905899548798));
#42210=CARTESIAN_POINT('Ctrl Pts',(3.70921425811868,5.65986029751345,-23.3818409242126));
#42211=CARTESIAN_POINT('Ctrl Pts',(3.5536458453004,5.76181273884703,-23.3730917747327));
#42212=CARTESIAN_POINT('Ctrl Pts',(3.39387173464268,5.85734747818107,-23.3643426252529));
#42213=CARTESIAN_POINT('Ctrl Pts',(3.23043456092332,5.94614005448847,-23.355593475773));
#42214=CARTESIAN_POINT('Ctrl Pts',(3.18690768806344,5.96978744811307,-23.35326338704));
#42215=CARTESIAN_POINT('Ctrl Pts',(3.14312114982858,5.99295688499312,-23.350933298307));
#42216=CARTESIAN_POINT('Ctrl Pts',(3.09908550384722,6.01564277861012,-23.348603209574));
#42217=CARTESIAN_POINT('Origin',(0.,0.,-63.6971797838103));
#42218=CARTESIAN_POINT('',(3.09908550384717,6.01564277861014,-20.9542113918581));
#42219=CARTESIAN_POINT('',(3.09908550384722,6.01564277861012,-21.3487227114526));
#42220=CARTESIAN_POINT('',(3.09908550384721,6.01564277861012,-63.6971797838103));
#42221=CARTESIAN_POINT('',(-6.7669985214907,-0.00447326979864322,-22.3028202162209));
#42222=CARTESIAN_POINT('Ctrl Pts',(-6.76699852149027,-0.00447327045386464,
-22.30282021619));
#42223=CARTESIAN_POINT('Ctrl Pts',(-6.76683979782902,-0.244584569803976,
-22.2915000487806));
#42224=CARTESIAN_POINT('Ctrl Pts',(-6.75389750641668,-0.484287776517787,
-22.2801798813713));
#42225=CARTESIAN_POINT('Ctrl Pts',(-6.72832438920961,-0.722454090975468,
-22.2688597139619));
#42226=CARTESIAN_POINT('Ctrl Pts',(-6.70632789425158,-0.927310780628065,
-22.2591227701499));
#42227=CARTESIAN_POINT('Ctrl Pts',(-6.67498738865535,-1.13103108037173,
-22.2493858263378));
#42228=CARTESIAN_POINT('Ctrl Pts',(-6.63442894834782,-1.33290717205828,
-22.2396488825258));
#42229=CARTESIAN_POINT('Ctrl Pts',(-6.60017265787884,-1.50341486375258,
-22.2314249081082));
#42230=CARTESIAN_POINT('Ctrl Pts',(-6.55929354599552,-1.67282715905326,
-22.2232009336907));
#42231=CARTESIAN_POINT('Ctrl Pts',(-6.51187460497495,-1.8405917877363,-22.2149769592731));
#42232=CARTESIAN_POINT('Ctrl Pts',(-6.46450574295683,-2.00817924069444,
-22.2067616701705));
#42233=CARTESIAN_POINT('Ctrl Pts',(-6.41061090207985,-2.17412214992992,
-22.1985463810678));
#42234=CARTESIAN_POINT('Ctrl Pts',(-6.35032426429631,-2.33787740018367,
-22.1903310919651));
#42235=CARTESIAN_POINT('Ctrl Pts',(-6.29008920283704,-2.50149255481757,
-22.1821228311929));
#42236=CARTESIAN_POINT('Ctrl Pts',(-6.22347335833223,-2.66292344329954,
-22.1739145704208));
#42237=CARTESIAN_POINT('Ctrl Pts',(-6.15066101690496,-2.82164102166197,
-22.1657063096486));
#42238=CARTESIAN_POINT('Ctrl Pts',(-6.07789636732612,-2.98025464052329,
-22.1575034252607));
#42239=CARTESIAN_POINT('Ctrl Pts',(-5.99894345429057,-3.13615816451053,
-22.1493005408728));
#42240=CARTESIAN_POINT('Ctrl Pts',(-5.91403510308101,-3.28884140686741,
-22.141097656485));
#42241=CARTESIAN_POINT('Ctrl Pts',(-5.82916534409085,-3.44145525222029,
-22.1328985004407));
#42242=CARTESIAN_POINT('Ctrl Pts',(-5.73834571358609,-3.59085141920646,
-22.1246993443966));
#42243=CARTESIAN_POINT('Ctrl Pts',(-5.64185554690849,-3.73654318693334,
-22.1165001883523));
#42244=CARTESIAN_POINT('Ctrl Pts',(-5.54537377252907,-3.88222228301916,
-22.1083017454353));
#42245=CARTESIAN_POINT('Ctrl Pts',(-5.44322263509805,-4.02419731815061,
-22.1001033025183));
#42246=CARTESIAN_POINT('Ctrl Pts',(-5.33572567249588,-4.16200919603362,
-22.0919048596013));
#42247=CARTESIAN_POINT('Ctrl Pts',(-5.2282297804362,-4.29981970147346,-22.0837064983311));
#42248=CARTESIAN_POINT('Ctrl Pts',(-5.1153883890271,-4.43346684876428,-22.0755081370609));
#42249=CARTESIAN_POINT('Ctrl Pts',(-4.99756625548406,-4.56252348180774,
-22.0673097757907));
#42250=CARTESIAN_POINT('Ctrl Pts',(-4.87972389207549,-4.69160227366172,
-22.0591100068754));
#42251=CARTESIAN_POINT('Ctrl Pts',(-4.75689932460476,-4.81608871606268,
-22.0509102379601));
#42252=CARTESIAN_POINT('Ctrl Pts',(-4.62949523045415,-4.93559144492353,
-22.0427104690448));
#42253=CARTESIAN_POINT('Ctrl Pts',(-4.50204611712428,-5.05513640095774,
-22.0345078026805));
#42254=CARTESIAN_POINT('Ctrl Pts',(-4.37001451507296,-5.16969389020239,
-22.0263051363162));
#42255=CARTESIAN_POINT('Ctrl Pts',(-4.23383735478326,-5.27891184367024,
-22.0181024699518));
#42256=CARTESIAN_POINT('Ctrl Pts',(-4.09750553127736,-5.38825384143387,
-22.0098904874088));
#42257=CARTESIAN_POINT('Ctrl Pts',(-3.95701902333565,-5.49224396332791,
-22.0016785048658));
#42258=CARTESIAN_POINT('Ctrl Pts',(-3.81284586685571,-5.59057200969645,
-21.9934665223228));
#42259=CARTESIAN_POINT('Ctrl Pts',(-3.66858767509963,-5.6889580512756,-21.9852496962415));
#42260=CARTESIAN_POINT('Ctrl Pts',(-3.52063880381534,-5.7816751702197,-21.9770328701602));
#42261=CARTESIAN_POINT('Ctrl Pts',(-3.369493126046,-5.8684584921024,-21.9688160440789));
#42262=CARTESIAN_POINT('Ctrl Pts',(-3.2181143598121,-5.95537564640125,-21.960586546465));
#42263=CARTESIAN_POINT('Ctrl Pts',(-3.06352925281743,-6.03634055079179,
-21.9523570488512));
#42264=CARTESIAN_POINT('Ctrl Pts',(-2.9062541465771,-6.11113539659395,-21.9441275512373));
#42265=CARTESIAN_POINT('Ctrl Pts',(-2.76606581816127,-6.17780433523132,
-21.9367921277125));
#42266=CARTESIAN_POINT('Ctrl Pts',(-2.62374067824165,-6.23957167109107,
-21.9294567041876));
#42267=CARTESIAN_POINT('Ctrl Pts',(-2.47965458072791,-6.29631655496093,
-21.9221212806628));
#42268=CARTESIAN_POINT('Ctrl Pts',(-2.32112246806096,-6.35875065844598,
-21.9140504104764));
#42269=CARTESIAN_POINT('Ctrl Pts',(-2.15994130847932,-6.41530737282659,
-21.90597954029));
#42270=CARTESIAN_POINT('Ctrl Pts',(-1.99659536623688,-6.46574790287415,
-21.8979086701036));
#42271=CARTESIAN_POINT('Ctrl Pts',(-1.83345269532306,-6.51612566360269,
-21.8898478434878));
#42272=CARTESIAN_POINT('Ctrl Pts',(-1.66815095386152,-6.56040227556719,
-21.881787016872));
#42273=CARTESIAN_POINT('Ctrl Pts',(-1.50119630741602,-6.59838606377351,
-21.8737261902562));
#42274=CARTESIAN_POINT('Ctrl Pts',(-1.33441281244487,-6.63633091337291,
-21.8656736270963));
#42275=CARTESIAN_POINT('Ctrl Pts',(-1.16598014516901,-6.66799569491895,
-21.8576210639364));
#42276=CARTESIAN_POINT('Ctrl Pts',(-0.996421543867331,-6.69323786421169,
-21.8495685007765));
#42277=CARTESIAN_POINT('Ctrl Pts',(-0.826999636405796,-6.71845968390831,
-21.8415224293886));
#42278=CARTESIAN_POINT('Ctrl Pts',(-0.656453968629374,-6.73726914223733,
-21.8334763580008));
#42279=CARTESIAN_POINT('Ctrl Pts',(-0.48531983937667,-6.74957433128249,
-21.8254302866129));
#42280=CARTESIAN_POINT('Ctrl Pts',(-0.314286240472433,-6.7618722918166,
-21.817388941777));
#42281=CARTESIAN_POINT('Ctrl Pts',(-0.142665239355296,-6.76767356261957,
-21.8093475969411));
#42282=CARTESIAN_POINT('Ctrl Pts',(0.0290009467029128,-6.76693785586142,
-21.8013062521052));
#42283=CARTESIAN_POINT('Ctrl Pts',(0.203976328610638,-6.76618796694074,
-21.7931098948842));
#42284=CARTESIAN_POINT('Ctrl Pts',(0.378998263215142,-6.75864644712516,
-21.7849135376631));
#42285=CARTESIAN_POINT('Ctrl Pts',(0.553490139944152,-6.7443263314422,-21.7767171804421));
#42286=CARTESIAN_POINT('Ctrl Pts',(0.724627547763495,-6.73028150870549,
-21.7686783917336));
#42287=CARTESIAN_POINT('Ctrl Pts',(0.895254709047074,-6.70971640581834,
-21.7606396030251));
#42288=CARTESIAN_POINT('Ctrl Pts',(1.0648310349809,-6.68269585324228,-21.7526008143166));
#42289=CARTESIAN_POINT('Ctrl Pts',(1.234425507118,-6.65567240922228,-21.7445611653848));
#42290=CARTESIAN_POINT('Ctrl Pts',(1.40296855114293,-6.62219219871555,-21.7365215164531));
#42291=CARTESIAN_POINT('Ctrl Pts',(1.56992836752977,-6.58237145114322,-21.7284818675214));
#42292=CARTESIAN_POINT('Ctrl Pts',(1.73693910881058,-6.54253855773011,-21.7204397663932));
#42293=CARTESIAN_POINT('Ctrl Pts',(1.90236529815806,-6.4963613643341,-21.7123976652651));
#42294=CARTESIAN_POINT('Ctrl Pts',(2.06568907075119,-6.44400633635467,-21.7043555641369));
#42295=CARTESIAN_POINT('Ctrl Pts',(2.23452437898895,-6.38988453187784,-21.6960420736921));
#42296=CARTESIAN_POINT('Ctrl Pts',(2.40111247499271,-6.32916077531904,-21.6877285832474));
#42297=CARTESIAN_POINT('Ctrl Pts',(2.56490343797082,-6.26207308755539,-21.6794150928026));
#42298=CARTESIAN_POINT('Ctrl Pts',(2.72362665182019,-6.19706111608909,-21.6713588246319));
#42299=CARTESIAN_POINT('Ctrl Pts',(2.87972293892313,-6.12607337260562,-21.6633025564611));
#42300=CARTESIAN_POINT('Ctrl Pts',(3.03271720490066,-6.04937313736717,-21.6552462882903));
#42301=CARTESIAN_POINT('Ctrl Pts',(3.19303872193976,-5.96899954955905,-21.6468041867086));
#42302=CARTESIAN_POINT('Ctrl Pts',(3.34995335952171,-5.88235308065762,-21.6383620851268));
#42303=CARTESIAN_POINT('Ctrl Pts',(3.50294945914151,-5.78978705020316,-21.6299199835451));
#42304=CARTESIAN_POINT('Ctrl Pts',(3.65594555876131,-5.6972210197487,-21.6214778819633));
#42305=CARTESIAN_POINT('Ctrl Pts',(3.80502278354149,-5.59873575392552,-21.6130357803815));
#42306=CARTESIAN_POINT('Ctrl Pts',(3.94971058606822,-5.49473159365411,-21.6045936787998));
#42307=CARTESIAN_POINT('Ctrl Pts',(4.09254295714659,-5.39206115043665,-21.5962598361071));
#42308=CARTESIAN_POINT('Ctrl Pts',(4.23155224880822,-5.28368659903462,-21.5879259934144));
#42309=CARTESIAN_POINT('Ctrl Pts',(4.3662605840787,-5.1699185208203,-21.5795921507217));
#42310=CARTESIAN_POINT('Ctrl Pts',(4.50081014853403,-5.05628453267902,-21.571268130517));
#42311=CARTESIAN_POINT('Ctrl Pts',(4.6310685914594,-4.93726990388134,-21.5629441103122));
#42312=CARTESIAN_POINT('Ctrl Pts',(4.75658755455274,-4.81322800580587,-21.5546200901075));
#42313=CARTESIAN_POINT('Ctrl Pts',(4.88198159138795,-4.68930956389827,-21.5463043546166));
#42314=CARTESIAN_POINT('Ctrl Pts',(5.00264530054966,-4.56037406439998,-21.5379886191258));
#42315=CARTESIAN_POINT('Ctrl Pts',(5.11816376418442,-4.42681473330313,-21.5296728836349));
#42316=CARTESIAN_POINT('Ctrl Pts',(5.23358842080311,-4.29336385934743,-21.5213639009549));
#42317=CARTESIAN_POINT('Ctrl Pts',(5.34387593080243,-4.15529689752791,-21.5130549182748));
#42318=CARTESIAN_POINT('Ctrl Pts',(5.44864843940284,-4.01304363093563,-21.5047459355948));
#42319=CARTESIAN_POINT('Ctrl Pts',(5.55335505375238,-3.87087983125181,-21.4964421786577));
#42320=CARTESIAN_POINT('Ctrl Pts',(5.65255337342312,-3.72453525312796,-21.4881384217205));
#42321=CARTESIAN_POINT('Ctrl Pts',(5.74590589694503,-3.57447260773562,-21.4798346647833));
#42322=CARTESIAN_POINT('Ctrl Pts',(5.83922052159282,-3.4244708841598,-21.4715342789713));
#42323=CARTESIAN_POINT('Ctrl Pts',(5.9266938955467,-3.27075439587046,-21.4632338931593));
#42324=CARTESIAN_POINT('Ctrl Pts',(6.00803176401268,-3.11381491463681,-21.4549335073473));
#42325=CARTESIAN_POINT('Ctrl Pts',(6.08935248043865,-2.95690852785613,-21.4466348718706));
#42326=CARTESIAN_POINT('Ctrl Pts',(6.16454010903527,-2.79678081075611,-21.438336236394));
#42327=CARTESIAN_POINT('Ctrl Pts',(6.23334618431693,-2.63394843276431,-21.4300376009174));
#42328=CARTESIAN_POINT('Ctrl Pts',(6.30214917120639,-2.47112336357837,-21.4217393379288));
#42329=CARTESIAN_POINT('Ctrl Pts',(6.36457104038087,-2.30559419582851,-21.4134410749402));
#42330=CARTESIAN_POINT('Ctrl Pts',(6.42041126945608,-2.13789806376296,-21.4051428119516));
#42331=CARTESIAN_POINT('Ctrl Pts',(6.47625826054463,-1.97018162441175,-21.3968435440788));
#42332=CARTESIAN_POINT('Ctrl Pts',(6.52552191410141,-1.80029802800402,-21.388544276206));
#42333=CARTESIAN_POINT('Ctrl Pts',(6.56805136520168,-1.62880025296914,-21.3802450083332));
#42334=CARTESIAN_POINT('Ctrl Pts',(6.61061067883143,-1.45718205885458,-21.3719399130367));
#42335=CARTESIAN_POINT('Ctrl Pts',(6.64642625782737,-1.28394775932448,-21.3636348177402));
#42336=CARTESIAN_POINT('Ctrl Pts',(6.67539803959756,-1.10966211656387,-21.3553297224437));
#42337=CARTESIAN_POINT('Ctrl Pts',(6.70438038598591,-0.935312920195172,
-21.3470215986776));
#42338=CARTESIAN_POINT('Ctrl Pts',(6.72651391134347,-0.759911960716135,
-21.3387134749115));
#42339=CARTESIAN_POINT('Ctrl Pts',(6.74175035679169,-0.5840300734544,-21.3304053511454));
#42340=CARTESIAN_POINT('Ctrl Pts',(6.7570029984934,-0.407961224762586,-21.3220883958917));
#42341=CARTESIAN_POINT('Ctrl Pts',(6.76534388934378,-0.231410774170983,
-21.3137714406381));
#42342=CARTESIAN_POINT('Ctrl Pts',(6.7667768782302,-0.0549516173484228,
-21.3054544853844));
#42343=CARTESIAN_POINT('Ctrl Pts',(6.76783296923709,0.075096096469244,-21.2993250159018));
#42344=CARTESIAN_POINT('Ctrl Pts',(6.76513814630155,0.205094195796902,-21.2931955464192));
#42345=CARTESIAN_POINT('Ctrl Pts',(6.75871200404309,0.334814943519255,-21.2870660769367));
#42346=CARTESIAN_POINT('Ctrl Pts',(6.74985194208228,0.513667794296063,-21.2786150534115));
#42347=CARTESIAN_POINT('Ctrl Pts',(6.7338807044077,0.692320057028802,-21.2701640298863));
#42348=CARTESIAN_POINT('Ctrl Pts',(6.71081733390735,0.87018372251419,-21.2617130063611));
#42349=CARTESIAN_POINT('Ctrl Pts',(6.68777427001924,1.04789078432853,-21.2532694237109));
#42350=CARTESIAN_POINT('Ctrl Pts',(6.65765156203011,1.22481030563259,-21.2448258410608));
#42351=CARTESIAN_POINT('Ctrl Pts',(6.62052018187237,1.40035764054068,-21.2363822584106));
#42352=CARTESIAN_POINT('Ctrl Pts',(6.58341644718391,1.57577427498913,-21.2279449622708));
#42353=CARTESIAN_POINT('Ctrl Pts',(6.53931451088454,1.74982043637239,-21.219507666131));
#42354=CARTESIAN_POINT('Ctrl Pts',(6.48833678684317,1.92191954579207,-21.2110703699911));
#42355=CARTESIAN_POINT('Ctrl Pts',(6.437395431521,2.09389587561929,-21.2026390932188));
#42356=CARTESIAN_POINT('Ctrl Pts',(6.37958816691832,2.26392760715644,-21.1942078164464));
#42357=CARTESIAN_POINT('Ctrl Pts',(6.31508787128656,2.43145104370404,-21.1857765396741));
#42358=CARTESIAN_POINT('Ctrl Pts',(6.25061522281635,2.59890267364255,-21.1773488768521));
#42359=CARTESIAN_POINT('Ctrl Pts',(6.17945538143675,2.76384784316277,-21.1689212140302));
#42360=CARTESIAN_POINT('Ctrl Pts',(6.10183041101897,2.92574001496443,-21.1604935512083));
#42361=CARTESIAN_POINT('Ctrl Pts',(6.02422933663726,3.08758234995257,-21.1520684827543));
#42362=CARTESIAN_POINT('Ctrl Pts',(5.94016724537731,3.24637326293725,-21.1436434143003));
#42363=CARTESIAN_POINT('Ctrl Pts',(5.84991363060396,3.40158779314513,-21.1352183458463));
#42364=CARTESIAN_POINT('Ctrl Pts',(5.82521747901043,3.44405923960365,-21.1329129892326));
#42365=CARTESIAN_POINT('Ctrl Pts',(5.80005801344589,3.4862630452555,-21.130607632619));
#42366=CARTESIAN_POINT('Ctrl Pts',(5.77444135510304,3.52818877562919,-21.1283022760053));
#42367=CARTESIAN_POINT('Ctrl Pts',(5.67866889066826,3.68493562634545,-21.1196832874808));
#42368=CARTESIAN_POINT('Ctrl Pts',(5.57654527277411,3.83772354106652,-21.1110642989564));
#42369=CARTESIAN_POINT('Ctrl Pts',(5.46842726088112,3.98604971023345,-21.1024453104319));
#42370=CARTESIAN_POINT('Ctrl Pts',(5.36024447665021,4.13446474001282,-21.0938211583641));
#42371=CARTESIAN_POINT('Ctrl Pts',(5.2460603106858,4.27841244399173,-21.0851970062963));
#42372=CARTESIAN_POINT('Ctrl Pts',(5.12627253381604,4.41742220180993,-21.0765728542285));
#42373=CARTESIAN_POINT('Ctrl Pts',(5.0023819933623,4.56119308123083,-21.0676533226323));
#42374=CARTESIAN_POINT('Ctrl Pts',(4.87249743537002,4.69968150795205,-21.058733791036));
#42375=CARTESIAN_POINT('Ctrl Pts',(4.7371007621332,4.83240782316612,-21.0498142594398));
#42376=CARTESIAN_POINT('Ctrl Pts',(4.60594401454381,4.9609778345766,-21.0411740415805));
#42377=CARTESIAN_POINT('Ctrl Pts',(4.46961540632021,5.08414098228172,-21.0325338237213));
#42378=CARTESIAN_POINT('Ctrl Pts',(4.32858746846222,5.20150166085447,-21.023893605862));
#42379=CARTESIAN_POINT('Ctrl Pts',(4.1807209807577,5.32455324622649,-21.0148344173973));
#42380=CARTESIAN_POINT('Ctrl Pts',(4.02768839344572,5.4412254049512,-21.0057752289326));
#42381=CARTESIAN_POINT('Ctrl Pts',(3.87006994481229,5.551112286944,-20.9967160404678));
#42382=CARTESIAN_POINT('Ctrl Pts',(3.71245149617885,5.6609991689368,-20.9876568520031));
#42383=CARTESIAN_POINT('Ctrl Pts',(3.55024752690922,5.76410059690113,-20.9785976635383));
#42384=CARTESIAN_POINT('Ctrl Pts',(3.38406977779038,5.86006490911541,-20.9695384750736));
#42385=CARTESIAN_POINT('Ctrl Pts',(3.29035203109883,5.91418502538377,-20.9644294473351));
#42386=CARTESIAN_POINT('Ctrl Pts',(3.19532225413756,5.96606438296092,-20.9593204195966));
#42387=CARTESIAN_POINT('Ctrl Pts',(3.09908550384717,6.01564277861014,-20.9542113918581));
#42388=CARTESIAN_POINT('Ctrl Pts',(3.09908550384719,6.01564277861013,-22.9543563216829));
#42389=CARTESIAN_POINT('Ctrl Pts',(2.94506750066652,6.09498840775651,-22.9462261559891));
#42390=CARTESIAN_POINT('Ctrl Pts',(2.78807281632298,6.16837786125163,-22.9380959902953));
#42391=CARTESIAN_POINT('Ctrl Pts',(2.62861170812857,6.23559856692919,-22.9299658246015));
#42392=CARTESIAN_POINT('Ctrl Pts',(2.46907887916276,6.30284950644195,-22.9218320022057));
#42393=CARTESIAN_POINT('Ctrl Pts',(2.3070777574783,6.36392603961682,-22.91369817981));
#42394=CARTESIAN_POINT('Ctrl Pts',(2.14313547521938,6.41866491841226,-22.9055643574142));
#42395=CARTESIAN_POINT('Ctrl Pts',(1.97902262328357,6.47346074891498,-22.8974220723848));
#42396=CARTESIAN_POINT('Ctrl Pts',(1.81296492893481,6.52190565783806,-22.8892797873555));
#42397=CARTESIAN_POINT('Ctrl Pts',(1.64550205599884,6.5638869569565,-22.8811375023261));
#42398=CARTESIAN_POINT('Ctrl Pts',(1.60139656903797,6.57494376977958,-22.8789930303014));
#42399=CARTESIAN_POINT('Ctrl Pts',(1.55719365224243,6.58555250370754,-22.8768485582767));
#42400=CARTESIAN_POINT('Ctrl Pts',(1.51290324157315,6.59571169637041,-22.8747040862519));
#42401=CARTESIAN_POINT('Ctrl Pts',(1.33857467565615,6.63569862494095,-22.8662633712739));
#42402=CARTESIAN_POINT('Ctrl Pts',(1.16253102035022,6.66879946415491,-22.8578226562958));
#42403=CARTESIAN_POINT('Ctrl Pts',(0.985343015162563,6.69487775410951,-22.8493819413177));
#42404=CARTESIAN_POINT('Ctrl Pts',(0.8082889370173,6.7209363328639,-22.8409476062297));
#42405=CARTESIAN_POINT('Ctrl Pts',(0.630092561903329,6.73998289511041,-22.8325132711417));
#42406=CARTESIAN_POINT('Ctrl Pts',(0.451334955646914,6.75193200186519,-22.8240789360536));
#42407=CARTESIAN_POINT('Ctrl Pts',(0.272685012540239,6.76387391184386,-22.815649680845));
#42408=CARTESIAN_POINT('Ctrl Pts',(0.0934748440294833,6.76872686639846,
-22.8072204256364));
#42409=CARTESIAN_POINT('Ctrl Pts',(-0.0857088242301413,6.76645719689773,
-22.7987911704278));
#42410=CARTESIAN_POINT('Ctrl Pts',(-0.264812058153802,6.76418854623628,
-22.7903656990548));
#42411=CARTESIAN_POINT('Ctrl Pts',(-0.443888482710617,6.75480365081094,
-22.7819402276818));
#42412=CARTESIAN_POINT('Ctrl Pts',(-0.622350428176236,6.73832092917433,
-22.7735147563087));
#42413=CARTESIAN_POINT('Ctrl Pts',(-0.800759615113575,6.72184308030841,
-22.7650917757495));
#42414=CARTESIAN_POINT('Ctrl Pts',(-0.978554353579318,6.6982716203976,-22.7566687951903));
#42415=CARTESIAN_POINT('Ctrl Pts',(-1.15515075464894,6.66767693683745,-22.748245814631));
#42416=CARTESIAN_POINT('Ctrl Pts',(-1.33175007978853,6.63708174669282,-22.7398226946047));
#42417=CARTESIAN_POINT('Ctrl Pts',(-1.5071506983219,6.59946315094049,-22.7313995745784));
#42418=CARTESIAN_POINT('Ctrl Pts',(-1.68077692221323,6.55494301559941,-22.722976454552));
#42419=CARTESIAN_POINT('Ctrl Pts',(-1.85440915038874,6.51042134067785,-22.7145530432402));
#42420=CARTESIAN_POINT('Ctrl Pts',(-2.02626653847878,6.45899773296964,-22.7061296319283));
#42421=CARTESIAN_POINT('Ctrl Pts',(-2.19578646472837,6.40084453813055,-22.6977062206165));
#42422=CARTESIAN_POINT('Ctrl Pts',(-2.36533589530772,6.34268122193833,-22.6892813432404));
#42423=CARTESIAN_POINT('Ctrl Pts',(-2.5325467375133,6.2777860916801,-22.6808564658643));
#42424=CARTESIAN_POINT('Ctrl Pts',(-2.69687397725934,6.20638056767238,-22.6724315884881));
#42425=CARTESIAN_POINT('Ctrl Pts',(-2.86125274249415,6.13495265416594,-22.6640040694567));
#42426=CARTESIAN_POINT('Ctrl Pts',(-3.02274579686597,6.0570104098419,-22.6555765504253));
#42427=CARTESIAN_POINT('Ctrl Pts',(-3.18083012460513,5.97282250853016,-22.6471490313939));
#42428=CARTESIAN_POINT('Ctrl Pts',(-3.33905621625991,5.88855911076214,-22.6387139548891));
#42429=CARTESIAN_POINT('Ctrl Pts',(-3.49386717869796,5.79803902158271,-22.6302788783843));
#42430=CARTESIAN_POINT('Ctrl Pts',(-3.644765541231,5.70157637407894,-22.6218438018795));
#42431=CARTESIAN_POINT('Ctrl Pts',(-3.79573683393573,5.6050671055428,-22.6134046486467));
#42432=CARTESIAN_POINT('Ctrl Pts',(-3.94279147898377,5.50260973696425,-22.604965495414));
#42433=CARTESIAN_POINT('Ctrl Pts',(-4.08546238809936,5.39456078614612,-22.5965263421812));
#42434=CARTESIAN_POINT('Ctrl Pts',(-4.22829184459585,5.28639176264978,-22.5880778106831));
#42435=CARTESIAN_POINT('Ctrl Pts',(-4.36672757022377,5.17261894862968,-22.579629279185));
#42436=CARTESIAN_POINT('Ctrl Pts',(-4.50033593007315,5.05363883914281,-22.5711807476869));
#42437=CARTESIAN_POINT('Ctrl Pts',(-4.57415888382355,4.98789846833242,-22.5665126599209));
#42438=CARTESIAN_POINT('Ctrl Pts',(-4.64650872167435,4.92056901762265,-22.5618445721549));
#42439=CARTESIAN_POINT('Ctrl Pts',(-4.71731727448002,4.85172203778127,-22.5571764843889));
#42440=CARTESIAN_POINT('Ctrl Pts',(-4.84231865047318,4.73018351069451,-22.5489357087922));
#42441=CARTESIAN_POINT('Ctrl Pts',(-4.96279257189696,4.60364323105405,-22.5406949331954));
#42442=CARTESIAN_POINT('Ctrl Pts',(-5.07831648673242,4.47247030851874,-22.5324541575986));
#42443=CARTESIAN_POINT('Ctrl Pts',(-5.19371244630784,4.34144267421606,-22.5242225095543));
#42444=CARTESIAN_POINT('Ctrl Pts',(-5.30416908320955,4.2057928787383,-22.5159908615099));
#42445=CARTESIAN_POINT('Ctrl Pts',(-5.40929902691201,4.06592831189248,-22.5077592134655));
#42446=CARTESIAN_POINT('Ctrl Pts',(-5.51433126294195,3.92619373504582,-22.4995352159072));
#42447=CARTESIAN_POINT('Ctrl Pts',(-5.61404645257981,3.78225247080156,-22.4913112183489));
#42448=CARTESIAN_POINT('Ctrl Pts',(-5.70809597807009,3.63454664368749,-22.4830872207906));
#42449=CARTESIAN_POINT('Ctrl Pts',(-5.80206241043929,3.48697131524543,-22.4748704891661));
#42450=CARTESIAN_POINT('Ctrl Pts',(-5.89037296505994,3.3356383519811,-22.4666537575416));
#42451=CARTESIAN_POINT('Ctrl Pts',(-5.97272109854002,3.1810205404956,-22.4584370259171));
#42452=CARTESIAN_POINT('Ctrl Pts',(-6.05502704202283,3.02648194543879,-22.4502245040284));
#42453=CARTESIAN_POINT('Ctrl Pts',(-6.13137648142408,2.86866216718532,-22.4420119821396));
#42454=CARTESIAN_POINT('Ctrl Pts',(-6.20150756057124,2.70806074085826,-22.4337994602509));
#42455=CARTESIAN_POINT('Ctrl Pts',(-6.27161518754793,2.54751302042128,-22.425589684669));
#42456=CARTESIAN_POINT('Ctrl Pts',(-6.33550845455604,2.38418583066897,-22.4173799090872));
#42457=CARTESIAN_POINT('Ctrl Pts',(-6.39297258518575,2.21860102881599,-22.4091701335053));
#42458=CARTESIAN_POINT('Ctrl Pts',(-6.41807142451639,2.14627788928947,-22.4055843168226));
#42459=CARTESIAN_POINT('Ctrl Pts',(-6.44194438404629,2.07352432665489,-22.4019985001399));
#42460=CARTESIAN_POINT('Ctrl Pts',(-6.46457647938253,2.00038494850721,-22.3984126834572));
#42461=CARTESIAN_POINT('Ctrl Pts',(-6.51678662117979,1.83165919654648,-22.3901405374326));
#42462=CARTESIAN_POINT('Ctrl Pts',(-6.56236028910773,1.66097445397087,-22.381868391408));
#42463=CARTESIAN_POINT('Ctrl Pts',(-6.60117389750525,1.48888957780469,-22.3735962453834));
#42464=CARTESIAN_POINT('Ctrl Pts',(-6.64000848849303,1.3167116727603,-22.3653196274466));
#42465=CARTESIAN_POINT('Ctrl Pts',(-6.67207566787301,1.14313246732658,-22.3570430095098));
#42466=CARTESIAN_POINT('Ctrl Pts',(-6.69730339989465,0.968718829051837,
-22.3487663915729));
#42467=CARTESIAN_POINT('Ctrl Pts',(-6.72256647596976,0.794060837263601,
-22.3404781780941));
#42468=CARTESIAN_POINT('Ctrl Pts',(-6.74097091645306,0.618566423146213,
-22.3321899646152));
#42469=CARTESIAN_POINT('Ctrl Pts',(-6.75249666487768,0.442806719479055,
-22.3239017511364));
#42470=CARTESIAN_POINT('Ctrl Pts',(-6.76226879363462,0.293788504675128,
-22.3168745728312));
#42471=CARTESIAN_POINT('Ctrl Pts',(-6.76709705177433,0.14457973026869,-22.3098473945261));
#42472=CARTESIAN_POINT('Ctrl Pts',(-6.7669985214907,-0.00447326979873706,
-22.3028202162209));
#42473=CARTESIAN_POINT('',(-6.767,3.46986979080088E-13,-22.6971797838101));
#42474=CARTESIAN_POINT('Ctrl Pts',(3.09908550384722,6.01564277861012,-23.348603209574));
#42475=CARTESIAN_POINT('Ctrl Pts',(2.93373232018332,6.10082796552478,-23.3398537616747));
#42476=CARTESIAN_POINT('Ctrl Pts',(2.76486502144432,6.17919158180188,-23.3311043137754));
#42477=CARTESIAN_POINT('Ctrl Pts',(2.59305716434359,6.25046746591376,-23.3223548658761));
#42478=CARTESIAN_POINT('Ctrl Pts',(2.42125069459294,6.3217427744722,-23.3136054886287));
#42479=CARTESIAN_POINT('Ctrl Pts',(2.24650397871075,6.3859303555782,-23.3048561113813));
#42480=CARTESIAN_POINT('Ctrl Pts',(2.06941053323792,6.44281220003532,-23.2961067341338));
#42481=CARTESIAN_POINT('Ctrl Pts',(1.89231845896707,6.49969360406678,-23.2873574246312));
#42482=CARTESIAN_POINT('Ctrl Pts',(1.71287996431531,6.54926929700874,-23.2786081151286));
#42483=CARTESIAN_POINT('Ctrl Pts',(1.53170449173533,6.59137090065472,-23.2698588056261));
#42484=CARTESIAN_POINT('Ctrl Pts',(1.35053036178202,6.63347219230077,-23.2611095609615));
#42485=CARTESIAN_POINT('Ctrl Pts',(1.16761955878879,6.66809944062448,-23.2523603162969));
#42486=CARTESIAN_POINT('Ctrl Pts',(0.983593309310867,6.69513503985386,-23.2436110716323));
#42487=CARTESIAN_POINT('Ctrl Pts',(0.799568362460278,6.72217044771211,-23.2348618888991));
#42488=CARTESIAN_POINT('Ctrl Pts',(0.614428268438806,6.74161427235975,-23.2261127061659));
#42489=CARTESIAN_POINT('Ctrl Pts',(0.428801816330394,6.75340047696801,-23.2173635234328));
#42490=CARTESIAN_POINT('Ctrl Pts',(0.243176616522861,6.76518660206242,-23.2086143997246));
#42491=CARTESIAN_POINT('Ctrl Pts',(0.0570653511654892,6.76931519233997,
-23.1998652760165));
#42492=CARTESIAN_POINT('Ctrl Pts',(-0.12889990080005,6.76577222610795,-23.1911161523083));
#42493=CARTESIAN_POINT('Ctrl Pts',(-0.314863959942088,6.76222928260133,
-23.1823670847191));
#42494=CARTESIAN_POINT('Ctrl Pts',(-0.500681721080793,6.75101488651276,
-23.1736180171298));
#42495=CARTESIAN_POINT('Ctrl Pts',(-0.685722110173457,6.73216712415989,
-23.1648689495406));
#42496=CARTESIAN_POINT('Ctrl Pts',(-0.870761373827607,6.71331947644145,
-23.1561199351642));
#42497=CARTESIAN_POINT('Ctrl Pts',(-1.05502298984326,6.68683858439999,-23.1473709207878));
#42498=CARTESIAN_POINT('Ctrl Pts',(-1.23788117676027,6.65281438131432,-23.1386219064115));
#42499=CARTESIAN_POINT('Ctrl Pts',(-1.43009641451764,6.61704912302384,-23.129425195524));
#42500=CARTESIAN_POINT('Ctrl Pts',(-1.62076048992671,6.57294837083171,-23.1202284846364));
#42501=CARTESIAN_POINT('Ctrl Pts',(-1.80915798961111,6.52067760042055,-23.1110317737489));
#42502=CARTESIAN_POINT('Ctrl Pts',(-1.98840443002991,6.47094578577415,-23.1022817760424));
#42503=CARTESIAN_POINT('Ctrl Pts',(-2.16559895952171,6.41381888474482,-23.0935317783359));
#42504=CARTESIAN_POINT('Ctrl Pts',(-2.34013966242301,6.34949095285242,-23.0847817806294));
#42505=CARTESIAN_POINT('Ctrl Pts',(-2.51467682553994,6.28516432556693,-23.0760319603778));
#42506=CARTESIAN_POINT('Ctrl Pts',(-2.68656000078822,6.21363705879669,-23.0672821401262));
#42507=CARTESIAN_POINT('Ctrl Pts',(-2.85520533840869,6.13515211510868,-23.0585323198746));
#42508=CARTESIAN_POINT('Ctrl Pts',(-3.0238474799831,6.0566686588113,-23.0497826654433));
#42509=CARTESIAN_POINT('Ctrl Pts',(-3.18925164684522,5.97122791039852,-23.0410330110121));
#42510=CARTESIAN_POINT('Ctrl Pts',(-3.35085601829144,5.87912008251915,-23.0322833565808));
#42511=CARTESIAN_POINT('Ctrl Pts',(-3.51245754191413,5.78701387778178,-23.0235338563377));
#42512=CARTESIAN_POINT('Ctrl Pts',(-3.67025915510938,5.68824097060981,-23.0147843560946));
#42513=CARTESIAN_POINT('Ctrl Pts',(-3.82372487928844,5.58313684656848,-23.0060348558514));
#42514=CARTESIAN_POINT('Ctrl Pts',(-3.97718810300806,5.47803443501767,-22.9972854981663));
#42515=CARTESIAN_POINT('Ctrl Pts',(-4.12631534263033,5.3666011749637,-22.9885361404812));
#42516=CARTESIAN_POINT('Ctrl Pts',(-4.27060009886231,5.24921554097346,-22.9797867827961));
#42517=CARTESIAN_POINT('Ctrl Pts',(-4.41488269594219,5.13183166360286,-22.9710375560409));
#42518=CARTESIAN_POINT('Ctrl Pts',(-4.55432273235094,5.00849577139466,-22.9622883292857));
#42519=CARTESIAN_POINT('Ctrl Pts',(-4.68844662480212,4.87962675277337,-22.9535391025305));
#42520=CARTESIAN_POINT('Ctrl Pts',(-4.8225686883517,4.7507594913987,-22.944789995079));
#42521=CARTESIAN_POINT('Ctrl Pts',(-4.95137454637881,4.61635945312505,-22.9360408876275));
#42522=CARTESIAN_POINT('Ctrl Pts',(-5.07442674461103,4.47688309134563,-22.927291780176));
#42523=CARTESIAN_POINT('Ctrl Pts',(-5.1974774283858,4.33740844616303,-22.9185427804037));
#42524=CARTESIAN_POINT('Ctrl Pts',(-5.31477440450984,4.19285781735958,-22.9097937806313));
#42525=CARTESIAN_POINT('Ctrl Pts',(-5.42591931531223,4.04372211999312,-22.9010447808589));
#42526=CARTESIAN_POINT('Ctrl Pts',(-5.5370763646305,3.89457013500704,-22.8922948255783));
#42527=CARTESIAN_POINT('Ctrl Pts',(-5.64207983273537,3.74083230916319,-22.8835448702977));
#42528=CARTESIAN_POINT('Ctrl Pts',(-5.74057303468812,3.58303087251723,-22.8747949150171));
#42529=CARTESIAN_POINT('Ctrl Pts',(-5.8390624336383,3.4252355288732,-22.8660452975883));
#42530=CARTESIAN_POINT('Ctrl Pts',(-5.9310419176849,3.26337713156875,-22.8572956801595));
#42531=CARTESIAN_POINT('Ctrl Pts',(-6.0161990669972,3.09800545291032,-22.8485460627307));
#42532=CARTESIAN_POINT('Ctrl Pts',(-6.10135338095453,2.93263928039451,-22.8397967366253));
#42533=CARTESIAN_POINT('Ctrl Pts',(-6.17968568352913,2.76376031540059,-22.8310474105199));
#42534=CARTESIAN_POINT('Ctrl Pts',(-6.25092992694964,2.59194213831355,-22.8222980844145));
#42535=CARTESIAN_POINT('Ctrl Pts',(-6.32217217691168,2.4201287688065,-22.8135490031207));
#42536=CARTESIAN_POINT('Ctrl Pts',(-6.38632665483903,2.24537661647518,-22.8047999218269));
#42537=CARTESIAN_POINT('Ctrl Pts',(-6.44317547869393,2.06827917621322,-22.7960508405332));
#42538=CARTESIAN_POINT('Ctrl Pts',(-6.50002944235973,1.89116572423296,-22.7873009682182));
#42539=CARTESIAN_POINT('Ctrl Pts',(-6.54957634250429,1.71170683289078,-22.7785510959032));
#42540=CARTESIAN_POINT('Ctrl Pts',(-6.59164787708421,1.53051209225252,-22.7698012235883));
#42541=CARTESIAN_POINT('Ctrl Pts',(-6.63371649075027,1.34932993147939,-22.7610519587535));
#42542=CARTESIAN_POINT('Ctrl Pts',(-6.66831071257135,1.16641244173934,-22.7523026939187));
#42543=CARTESIAN_POINT('Ctrl Pts',(-6.6953130484034,0.982380875159536,-22.7435534290839));
#42544=CARTESIAN_POINT('Ctrl Pts',(-6.7223167703305,0.798339861795333,-22.7348037151283));
#42545=CARTESIAN_POINT('Ctrl Pts',(-6.74172778477895,0.61318494072961,-22.7260540011726));
#42546=CARTESIAN_POINT('Ctrl Pts',(-6.75348015835522,0.427545027689976,
-22.717304287217));
#42547=CARTESIAN_POINT('Ctrl Pts',(-6.76249038365222,0.285219953546579,
-22.7105961194147));
#42548=CARTESIAN_POINT('Ctrl Pts',(-6.76699999999999,0.142609995757398,
-22.7038879516124));
#42549=CARTESIAN_POINT('Ctrl Pts',(-6.767,3.46987300839874E-13,-22.6971797838101));
#42550=CARTESIAN_POINT('Ctrl Pts',(-6.76699992255766,-0.00102376982859472,
-22.6971797838101));
#42551=CARTESIAN_POINT('Ctrl Pts',(-6.76699274983805,-0.0484346151663659,
-22.6949554495712));
#42552=CARTESIAN_POINT('Ctrl Pts',(-6.7664872992955,-0.0958431546807729,
-22.6927311153323));
#42553=CARTESIAN_POINT('Ctrl Pts',(-6.7654838603425,-0.143238037703361,
-22.6905067810934));
#42554=CARTESIAN_POINT('Ctrl Pts',(-6.76159567273573,-0.326886675463195,
-22.6818877925689));
#42555=CARTESIAN_POINT('Ctrl Pts',(-6.75022687176097,-0.510310039791529,
-22.6732688040444));
#42556=CARTESIAN_POINT('Ctrl Pts',(-6.73143274283991,-0.692894096253327,
-22.6646498155198));
#42557=CARTESIAN_POINT('Ctrl Pts',(-6.7126273545584,-0.875587536859203,
-22.656025663452));
#42558=CARTESIAN_POINT('Ctrl Pts',(-6.68638779175664,-1.05744036356867,
-22.6474015113841));
#42559=CARTESIAN_POINT('Ctrl Pts',(-6.652820978273,-1.23784572182912,-22.6387773593163));
#42560=CARTESIAN_POINT('Ctrl Pts',(-6.61810449239762,-1.42443001214147,
-22.6298578277201));
#42561=CARTESIAN_POINT('Ctrl Pts',(-6.57555002218844,-1.60946557576452,
-22.6209382961239));
#42562=CARTESIAN_POINT('Ctrl Pts',(-6.52533264709187,-1.79229541225689,
-22.6120187645277));
#42563=CARTESIAN_POINT('Ctrl Pts',(-6.47668782124208,-1.96939996101538,
-22.6033785466684));
#42564=CARTESIAN_POINT('Ctrl Pts',(-6.42085288937884,-2.14443455975871,
-22.5947383288091));
#42565=CARTESIAN_POINT('Ctrl Pts',(-6.35803712842322,-2.31681955999853,
-22.5860981109498));
#42566=CARTESIAN_POINT('Ctrl Pts',(-6.29217538438971,-2.49756363741301,
-22.5770389224852));
#42567=CARTESIAN_POINT('Ctrl Pts',(-6.21863911694482,-2.6753944074447,-22.5679797340205));
#42568=CARTESIAN_POINT('Ctrl Pts',(-6.1377255251347,-2.84966916994061,-22.5589205455559));
#42569=CARTESIAN_POINT('Ctrl Pts',(-6.05681193332454,-3.02394393243659,
-22.5498613570913));
#42570=CARTESIAN_POINT('Ctrl Pts',(-5.96852122234264,-3.19466236274906,
-22.5408021686267));
#42571=CARTESIAN_POINT('Ctrl Pts',(-5.87320508241716,-3.3612127364791,-22.5317429801621));
#42572=CARTESIAN_POINT('Ctrl Pts',(-5.7780540710162,-3.52747457337271,-22.5226994861059));
#42573=CARTESIAN_POINT('Ctrl Pts',(-5.67581502940719,-3.68973637230308,
-22.5136559920496));
#42574=CARTESIAN_POINT('Ctrl Pts',(-5.56683334138906,-3.84742193542626,
-22.5046124979934));
#42575=CARTESIAN_POINT('Ctrl Pts',(-5.45795133852264,-4.00496326414118,
-22.4955772759881));
#42576=CARTESIAN_POINT('Ctrl Pts',(-5.34233913788169,-4.15793651845302,
-22.4865420539828));
#42577=CARTESIAN_POINT('Ctrl Pts',(-5.22038557744195,-4.30579416865647,
-22.4775068319775));
#42578=CARTESIAN_POINT('Ctrl Pts',(-5.09864687262647,-4.45339132586882,
-22.4684875280665));
#42579=CARTESIAN_POINT('Ctrl Pts',(-4.97058926859331,-4.59589069254239,
-22.4594682241554));
#42580=CARTESIAN_POINT('Ctrl Pts',(-4.83664189523819,-4.73277763868394,
-22.4504489202443));
#42581=CARTESIAN_POINT('Ctrl Pts',(-4.70286256821907,-4.86949285059011,
-22.44144093168));
#42582=CARTESIAN_POINT('Ctrl Pts',(-4.5632083840568,-5.00060952406196,-22.4324329431157));
#42583=CARTESIAN_POINT('Ctrl Pts',(-4.41814704867377,-5.12564782796236,
-22.4234249545514));
#42584=CARTESIAN_POINT('Ctrl Pts',(-4.27341333939746,-5.25040372847396,
-22.4144373108447));
#42585=CARTESIAN_POINT('Ctrl Pts',(-4.12329703565662,-5.3691085070198,-22.4054496671381));
#42586=CARTESIAN_POINT('Ctrl Pts',(-3.96830043668197,-5.48132106742797,
-22.3964620234314));
#42587=CARTESIAN_POINT('Ctrl Pts',(-3.83330914181043,-5.57905043007564,
-22.3886344086978));
#42588=CARTESIAN_POINT('Ctrl Pts',(-3.6946166839515,-5.67185578121942,-22.3808067939641));
#42589=CARTESIAN_POINT('Ctrl Pts',(-3.55257685114231,-5.75946930860195,
-22.3729791792304));
#42590=CARTESIAN_POINT('Ctrl Pts',(-3.40517408456408,-5.85039082033881,
-22.3648560207851));
#42591=CARTESIAN_POINT('Ctrl Pts',(-3.25423141251924,-5.93567898960228,
-22.3567328623398));
#42592=CARTESIAN_POINT('Ctrl Pts',(-3.10022620198568,-6.01505498699068,
-22.3486097038945));
#42593=CARTESIAN_POINT('Ctrl Pts',(-2.94623184962556,-6.0944253879558,-22.3404871181744));
#42594=CARTESIAN_POINT('Ctrl Pts',(-2.78917571423031,-6.16788427965845,
-22.3323645324543));
#42595=CARTESIAN_POINT('Ctrl Pts',(-2.6295593600824,-6.23519900017658,-22.3242419467342));
#42596=CARTESIAN_POINT('Ctrl Pts',(-2.46992382638634,-6.30252180925137,
-22.3161183850018));
#42597=CARTESIAN_POINT('Ctrl Pts',(-2.30772779907883,-6.36369883591761,
-22.3079948232694));
#42598=CARTESIAN_POINT('Ctrl Pts',(-2.14349234403927,-6.41854575204112,
-22.299871261537));
#42599=CARTESIAN_POINT('Ctrl Pts',(-1.97913726296015,-6.47343261763447,
-22.2917417827538));
#42600=CARTESIAN_POINT('Ctrl Pts',(-1.81274013478251,-6.52198004777808,
-22.2836123039707));
#42601=CARTESIAN_POINT('Ctrl Pts',(-1.64483730910135,-6.56405356670619,
-22.2754828251876));
#42602=CARTESIAN_POINT('Ctrl Pts',(-1.47686603239342,-6.60614423826743,
-22.2673500321591));
#42603=CARTESIAN_POINT('Ctrl Pts',(-1.30738819255101,-6.64175566249123,
-22.2592172391305));
#42604=CARTESIAN_POINT('Ctrl Pts',(-1.13694957416881,-6.67080464905077,
-22.251084446102));
#42605=CARTESIAN_POINT('Ctrl Pts',(-0.966325629645998,-6.69988522197623,
-22.2429428098949));
#42606=CARTESIAN_POINT('Ctrl Pts',(-0.794739182451133,-6.72238905752447,
-22.2348011736877));
#42607=CARTESIAN_POINT('Ctrl Pts',(-0.622741120960248,-6.73828483341757,
-22.2266595374806));
#42608=CARTESIAN_POINT('Ctrl Pts',(-0.535110444863029,-6.74638351532437,
-22.2225114844201));
#42609=CARTESIAN_POINT('Ctrl Pts',(-0.447372942291769,-6.752767737948,-22.2183634313595));
#42610=CARTESIAN_POINT('Ctrl Pts',(-0.35960133187925,-6.75743855925533,
-22.214215378299));
#42611=CARTESIAN_POINT('Ctrl Pts',(-0.180998229206384,-6.76694303540198,
-22.2057746633209));
#42612=CARTESIAN_POINT('Ctrl Pts',(-0.00188612121038587,-6.76936932874372,
-22.1973339483429));
#42613=CARTESIAN_POINT('Ctrl Pts',(0.177149307238839,-6.76468085891307,
-22.1888932333648));
#42614=CARTESIAN_POINT('Ctrl Pts',(0.356049412276157,-6.75999593284881,
-22.1804588982768));
#42615=CARTESIAN_POINT('Ctrl Pts',(0.534872621195459,-6.74820697237735,
-22.1720245631887));
#42616=CARTESIAN_POINT('Ctrl Pts',(0.713031823750875,-6.72932943303555,
-22.1635902281007));
#42617=CARTESIAN_POINT('Ctrl Pts',(0.89108372356648,-6.71046326336572,-22.1551609728921));
#42618=CARTESIAN_POINT('Ctrl Pts',(1.06847208359119,-6.68451706146053,-22.1467317176835));
#42619=CARTESIAN_POINT('Ctrl Pts',(1.2446130940856,-6.6515582569824,-22.1383024624748));
#42620=CARTESIAN_POINT('Ctrl Pts',(1.42067503607245,-6.61861424748854,-22.1298769911018));
#42621=CARTESIAN_POINT('Ctrl Pts',(1.59549041778119,-6.57866397324414,-22.1214515197288));
#42622=CARTESIAN_POINT('Ctrl Pts',(1.76848343022747,-6.53182634161464,-22.1130260483558));
#42623=CARTESIAN_POINT('Ctrl Pts',(1.9414253009206,-6.48500255654785,-22.1046030677966));
#42624=CARTESIAN_POINT('Ctrl Pts',(2.11254555524785,-6.43129556159063,-22.0961800872373));
#42625=CARTESIAN_POINT('Ctrl Pts',(2.28128101958846,-6.37087481509922,-22.0877571066781));
#42626=CARTESIAN_POINT('Ctrl Pts',(2.45001927783838,-6.31045306816555,-22.0793339866518));
#42627=CARTESIAN_POINT('Ctrl Pts',(2.61637235116062,-6.2433174537385,-22.0709108666255));
#42628=CARTESIAN_POINT('Ctrl Pts',(2.77979397187767,-6.16968674033881,-22.0624877465991));
#42629=CARTESIAN_POINT('Ctrl Pts',(2.94322124398679,-6.09605348066632,-22.0540643352873));
#42630=CARTESIAN_POINT('Ctrl Pts',(3.10371655722626,-6.0159248110216,-22.0456409239754));
#42631=CARTESIAN_POINT('Ctrl Pts',(3.26075517191744,-5.92956699167938,-22.0372175126635));
#42632=CARTESIAN_POINT('Ctrl Pts',(3.41782111861132,-5.84319414207116,-22.0287926352874));
#42633=CARTESIAN_POINT('Ctrl Pts',(3.57142887507701,-5.75059014196348,-22.0203677579113));
#42634=CARTESIAN_POINT('Ctrl Pts',(3.72107946287387,-5.65206658055072,-22.0119428805352));
#42635=CARTESIAN_POINT('Ctrl Pts',(3.87077697423446,-5.55351212666583,-22.0035153615038));
#42636=CARTESIAN_POINT('Ctrl Pts',(4.01651456469795,-5.44903459421697,-21.9950878424723));
#42637=CARTESIAN_POINT('Ctrl Pts',(4.15782303043522,-5.33898835432167,-21.9866603234409));
#42638=CARTESIAN_POINT('Ctrl Pts',(4.29925821614311,-5.22884342921164,-21.9782252469361));
#42639=CARTESIAN_POINT('Ctrl Pts',(4.43625607739851,-5.11312002342242,-21.9697901704313));
#42640=CARTESIAN_POINT('Ctrl Pts',(4.56838037158332,-4.99221291418267,-21.9613550939265));
#42641=CARTESIAN_POINT('Ctrl Pts',(4.70056852230911,-4.87124736974125,-21.9529159406938));
#42642=CARTESIAN_POINT('Ctrl Pts',(4.82787816797478,-4.74509335622317,-21.944476787461));
#42643=CARTESIAN_POINT('Ctrl Pts',(4.94991026570973,-4.61418219855063,-21.9360376342282));
#42644=CARTESIAN_POINT('Ctrl Pts',(5.07207797531951,-4.48312556187823,-21.9275891027301));
#42645=CARTESIAN_POINT('Ctrl Pts',(5.18895619684924,-4.34730146728461,-21.919140571232));
#42646=CARTESIAN_POINT('Ctrl Pts',(5.30018569986966,-4.2071748890315,-21.9106920397339));
#42647=CARTESIAN_POINT('Ctrl Pts',(5.36164360913839,-4.12975040812883,-21.9060239519679));
#42648=CARTESIAN_POINT('Ctrl Pts',(5.4213777547571,-4.0510129594965,-21.9013558642019));
#42649=CARTESIAN_POINT('Ctrl Pts',(5.47933324514631,-3.9710447225679,-21.896687776436));
#42650=CARTESIAN_POINT('Ctrl Pts',(5.58164455865225,-3.82987336323727,-21.8884470008392));
#42651=CARTESIAN_POINT('Ctrl Pts',(5.67863786581217,-3.68455059667655,-21.8802062252424));
#42652=CARTESIAN_POINT('Ctrl Pts',(5.76996015947585,-3.53551251702797,-21.8719654496457));
#42653=CARTESIAN_POINT('Ctrl Pts',(5.86118130379875,-3.3866395132103,-21.8637338016013));
#42654=CARTESIAN_POINT('Ctrl Pts',(5.94674375751435,-3.23405969094357,-21.8555021535569));
#42655=CARTESIAN_POINT('Ctrl Pts',(6.02633573746481,-3.0782408254317,-21.8472705055126));
#42656=CARTESIAN_POINT('Ctrl Pts',(6.1058537447027,-2.92256677782938,-21.8390465079543));
#42657=CARTESIAN_POINT('Ctrl Pts',(6.17941216819836,-2.76365999720127,-21.830822510396));
#42658=CARTESIAN_POINT('Ctrl Pts',(6.24674335927927,-2.60201583455989,-21.8225985128377));
#42659=CARTESIAN_POINT('Ctrl Pts',(6.3140150629913,-2.44051448516415,-21.8143817812132));
#42660=CARTESIAN_POINT('Ctrl Pts',(6.37507036364216,-2.27628090123508,-21.8061650495887));
#42661=CARTESIAN_POINT('Ctrl Pts',(6.42968832115496,-2.10983342773869,-21.7979483179642));
#42662=CARTESIAN_POINT('Ctrl Pts',(6.48427829586609,-1.94347123144506,-21.7897357960755));
#42663=CARTESIAN_POINT('Ctrl Pts',(6.53243738527677,-1.77489774179779,-21.7815232741868));
#42664=CARTESIAN_POINT('Ctrl Pts',(6.57399326105277,-1.60464999412108,-21.7733107522981));
#42665=CARTESIAN_POINT('Ctrl Pts',(6.61553524034389,-1.43445917811064,-21.7651009767162));
#42666=CARTESIAN_POINT('Ctrl Pts',(6.65047832061509,-1.26259556467711,-21.7568912011344));
#42667=CARTESIAN_POINT('Ctrl Pts',(6.67870038343357,-1.08961010839855,-21.7486814255525));
#42668=CARTESIAN_POINT('Ctrl Pts',(6.69102704725852,-1.01405455528866,-21.7450956088698));
#42669=CARTESIAN_POINT('Ctrl Pts',(6.70207218499357,-0.938285141900227,
-21.741509792187));
#42670=CARTESIAN_POINT('Ctrl Pts',(6.71182868254411,-0.862348384458541,
-21.7379239755043));
#42671=CARTESIAN_POINT('Ctrl Pts',(6.73593199385336,-0.674747527188622,
-21.7290652579825));
#42672=CARTESIAN_POINT('Ctrl Pts',(6.75214205920244,-0.486319296408045,
-21.7202065404608));
#42673=CARTESIAN_POINT('Ctrl Pts',(6.76044773986345,-0.297716906767592,
-21.711347822939));
#42674=CARTESIAN_POINT('Ctrl Pts',(6.768768959119,-0.108761672347425,-21.7024725321795));
#42675=CARTESIAN_POINT('Ctrl Pts',(6.76915622979846,0.0803681129719283,
-21.6935972414201));
#42676=CARTESIAN_POINT('Ctrl Pts',(6.7616504580941,0.269020598757414,-21.6847219506606));
#42677=CARTESIAN_POINT('Ctrl Pts',(6.75412336831047,0.458208900020156,-21.6758214520799));
#42678=CARTESIAN_POINT('Ctrl Pts',(6.7386583853227,0.646916928190347,-21.6669209534991));
#42679=CARTESIAN_POINT('Ctrl Pts',(6.71534846787936,0.834496228242138,-21.6580204549183));
#42680=CARTESIAN_POINT('Ctrl Pts',(6.69200699576958,1.02232945464346,-21.6491079077207));
#42681=CARTESIAN_POINT('Ctrl Pts',(6.66079941421044,1.20903064421832,-21.6401953605231));
#42682=CARTESIAN_POINT('Ctrl Pts',(6.62186985046744,1.39396150716953,-21.6312828133254));
#42683=CARTESIAN_POINT('Ctrl Pts',(6.58285432644569,1.57930071552714,-21.6223505863532));
#42684=CARTESIAN_POINT('Ctrl Pts',(6.53608276928002,1.76286152368634,-21.6134183593809));
#42685=CARTESIAN_POINT('Ctrl Pts',(6.48174999680389,1.94401799861337,-21.6044861324086));
#42686=CARTESIAN_POINT('Ctrl Pts',(6.43039925269116,2.11523178661635,-21.5960441464634));
#42687=CARTESIAN_POINT('Ctrl Pts',(6.37229498617801,2.28429788968549,-21.5876021605182));
#42688=CARTESIAN_POINT('Ctrl Pts',(6.30764116018565,2.45070438738168,-21.5791601745729));
#42689=CARTESIAN_POINT('Ctrl Pts',(6.24464550963262,2.61284306081242,-21.5709347000798));
#42690=CARTESIAN_POINT('Ctrl Pts',(6.17531061659187,2.77276620515393,-21.5627092255868));
#42691=CARTESIAN_POINT('Ctrl Pts',(6.09981303746284,2.92994366976541,-21.5544837510937));
#42692=CARTESIAN_POINT('Ctrl Pts',(6.02112223576987,3.09376906444736,-21.545910374442));
#42693=CARTESIAN_POINT('Ctrl Pts',(5.93573613715189,3.25461107827148,-21.5373369977903));
#42694=CARTESIAN_POINT('Ctrl Pts',(5.84391203472763,3.41188820601813,-21.5287636211386));
#42695=CARTESIAN_POINT('Ctrl Pts',(5.75600724214319,3.5624523055066,-21.5205561802116));
#42696=CARTESIAN_POINT('Ctrl Pts',(5.66220280499075,3.70974915038927,-21.5123487392847));
#42697=CARTESIAN_POINT('Ctrl Pts',(5.56277293849444,3.85329031280463,-21.5041412983577));
#42698=CARTESIAN_POINT('Ctrl Pts',(5.4634029665276,3.99674500894293,-21.4959388014263));
#42699=CARTESIAN_POINT('Ctrl Pts',(5.35841451651555,4.1364482339894,-21.4877363044948));
#42700=CARTESIAN_POINT('Ctrl Pts',(5.24812630850918,4.27193858218185,-21.4795338075634));
#42701=CARTESIAN_POINT('Ctrl Pts',(5.13788450026496,4.40737192772602,-21.4713347615349));
#42702=CARTESIAN_POINT('Ctrl Pts',(5.0223476010062,4.53859564917111,-21.4631357155065));
#42703=CARTESIAN_POINT('Ctrl Pts',(4.90187602113822,4.66517957568518,-21.454936669478));
#42704=CARTESIAN_POINT('Ctrl Pts',(4.78143324103618,4.79173324122434,-21.4467395835019));
#42705=CARTESIAN_POINT('Ctrl Pts',(4.65605837803892,4.91364906262556,-21.4385424975259));
#42706=CARTESIAN_POINT('Ctrl Pts',(4.52615031160175,5.03053201528301,-21.4303454115498));
#42707=CARTESIAN_POINT('Ctrl Pts',(4.3962239227512,5.1474314532738,-21.4221471694453));
#42708=CARTESIAN_POINT('Ctrl Pts',(4.26176331661265,5.2592963611186,-21.4139489273409));
#42709=CARTESIAN_POINT('Ctrl Pts',(4.12320250774531,5.36577022244922,-21.4057506852365));
#42710=CARTESIAN_POINT('Ctrl Pts',(3.98462975913752,5.47225325859832,-21.3975517366922));
#42711=CARTESIAN_POINT('Ctrl Pts',(3.8419563917584,5.57334410895098,-21.3893527881479));
#42712=CARTESIAN_POINT('Ctrl Pts',(3.69564733064943,5.66872823545668,-21.3811538396036));
#42713=CARTESIAN_POINT('Ctrl Pts',(3.54926196351698,5.76416210859693,-21.3729506149799));
#42714=CARTESIAN_POINT('Ctrl Pts',(3.39923741989362,5.85388312401151,-21.3647473903562));
#42715=CARTESIAN_POINT('Ctrl Pts',(3.24606567045609,5.93762129670514,-21.3565441657325));
#42716=CARTESIAN_POINT('Ctrl Pts',(3.19738457693707,5.96423498905363,-21.3539370143059));
#42717=CARTESIAN_POINT('Ctrl Pts',(3.14838576474938,5.99024470736143,-21.3513298628792));
#42718=CARTESIAN_POINT('Ctrl Pts',(3.09908550384722,6.01564277861012,-21.3487227114526));
#42719=CARTESIAN_POINT('Origin',(0.,0.,-63.6971797838103));
#42720=CARTESIAN_POINT('',(3.09908550384715,6.01564277861015,-18.9542023328983));
#42721=CARTESIAN_POINT('',(3.09908550384723,6.01564277861011,-19.3485039941327));
#42722=CARTESIAN_POINT('',(3.09908550384721,6.01564277861012,-63.6971797838103));
#42723=CARTESIAN_POINT('',(-6.76699815055718,0.00500303464652949,-20.3028202161448));
#42724=CARTESIAN_POINT('Ctrl Pts',(-6.76699815055718,0.00500303464652949,
-20.3028202161448));
#42725=CARTESIAN_POINT('Ctrl Pts',(-6.76712283725175,-0.163645533901148,
-20.2948669119147));
#42726=CARTESIAN_POINT('Ctrl Pts',(-6.76093875946453,-0.332552986580211,
-20.2869136076846));
#42727=CARTESIAN_POINT('Ctrl Pts',(-6.74841442827687,-0.501190287440406,
-20.2789603034545));
#42728=CARTESIAN_POINT('Ctrl Pts',(-6.73590074886688,-0.669684164511485,
-20.2710137634042));
#42729=CARTESIAN_POINT('Ctrl Pts',(-6.71705756938782,-0.837907967772918,
-20.2630672233539));
#42730=CARTESIAN_POINT('Ctrl Pts',(-6.69190542923894,-1.00533115246792,
-20.2551206833037));
#42731=CARTESIAN_POINT('Ctrl Pts',(-6.66677067925789,-1.17263858091856,
-20.2471796374843));
#42732=CARTESIAN_POINT('Ctrl Pts',(-6.6353357071835,-1.3391461155133,-20.2392385916649));
#42733=CARTESIAN_POINT('Ctrl Pts',(-6.59767297846628,-1.50432718157184,
-20.2312975458455));
#42734=CARTESIAN_POINT('Ctrl Pts',(-6.56002526039464,-1.66944241399267,
-20.2233596649647));
#42735=CARTESIAN_POINT('Ctrl Pts',(-6.51615480937113,-1.83323185725992,
-20.2154217840839));
#42736=CARTESIAN_POINT('Ctrl Pts',(-6.46618536754747,-1.99517813553452,
-20.2074839032032));
#42737=CARTESIAN_POINT('Ctrl Pts',(-6.41622188589341,-2.15710509745798,
-20.1995469691234));
#42738=CARTESIAN_POINT('Ctrl Pts',(-6.36016097106077,-2.31718896535845,
-20.1916100350435));
#42739=CARTESIAN_POINT('Ctrl Pts',(-6.29817646049836,-2.47492672061707,
-20.1836731009637));
#42740=CARTESIAN_POINT('Ctrl Pts',(-6.277471492571,-2.52761658029216,-20.1810218907812));
#42741=CARTESIAN_POINT('Ctrl Pts',(-6.25610598230951,-2.58004480419888,
-20.1783706805986));
#42742=CARTESIAN_POINT('Ctrl Pts',(-6.23408762025765,-2.6321931051787,-20.1757194704161));
#42743=CARTESIAN_POINT('Ctrl Pts',(-6.16051576579193,-2.80644072638164,
-20.1668607528943));
#42744=CARTESIAN_POINT('Ctrl Pts',(-6.07970647936697,-2.97743143841342,
-20.1580020353726));
#42745=CARTESIAN_POINT('Ctrl Pts',(-5.99197883434973,-3.14459514861688,
-20.1491433178508));
#42746=CARTESIAN_POINT('Ctrl Pts',(-5.90408706499864,-3.31207159527391,
-20.1402680270914));
#42747=CARTESIAN_POINT('Ctrl Pts',(-5.80925119159497,-3.47570650227465,
-20.1313927363319));
#42748=CARTESIAN_POINT('Ctrl Pts',(-5.70783457661667,-3.63495714499899,
-20.1225174455725));
#42749=CARTESIAN_POINT('Ctrl Pts',(-5.60612991564855,-3.79466009535581,
-20.1136169469917));
#42750=CARTESIAN_POINT('Ctrl Pts',(-5.49780725073439,-3.94995364274463,
-20.1047164484109));
#42751=CARTESIAN_POINT('Ctrl Pts',(-5.38327321796285,-4.10032418971524,
-20.0958159498302));
#42752=CARTESIAN_POINT('Ctrl Pts',(-5.26858414031805,-4.25089829349628,
-20.0869034026326));
#42753=CARTESIAN_POINT('Ctrl Pts',(-5.14766706099953,-4.39653588227203,
-20.0779908554349));
#42754=CARTESIAN_POINT('Ctrl Pts',(-5.02096771915789,-4.53675789117895,
-20.0690783082373));
#42755=CARTESIAN_POINT('Ctrl Pts',(-4.89398861279517,-4.67728952397654,
-20.060146081265));
#42756=CARTESIAN_POINT('Ctrl Pts',(-4.76120188077836,-4.81238146545405,
-20.0512138542928));
#42757=CARTESIAN_POINT('Ctrl Pts',(-4.62309084950618,-4.94159083668531,
-20.0422816273205));
#42758=CARTESIAN_POINT('Ctrl Pts',(-4.49255997646557,-5.06370861306052,
-20.0338396413752));
#42759=CARTESIAN_POINT('Ctrl Pts',(-4.35727364105156,-5.1805720395231,-20.0253976554299));
#42760=CARTESIAN_POINT('Ctrl Pts',(-4.21766570116265,-5.29184136508609,
-20.0169556694847));
#42761=CARTESIAN_POINT('Ctrl Pts',(-4.08166309068968,-5.40023719668545,
-20.0087316950671));
#42762=CARTESIAN_POINT('Ctrl Pts',(-3.94129875731921,-5.5035303789621,-20.0005077206495));
#42763=CARTESIAN_POINT('Ctrl Pts',(-3.79699181587882,-5.60135181453096,
-19.992283746232));
#42764=CARTESIAN_POINT('Ctrl Pts',(-3.65283727656988,-5.6990699411728,-19.9840684571293));
#42765=CARTESIAN_POINT('Ctrl Pts',(-3.50474871503935,-5.79132762888708,
-19.9758531680267));
#42766=CARTESIAN_POINT('Ctrl Pts',(-3.35317851588266,-5.87779574675941,
-19.967637878924));
#42767=CARTESIAN_POINT('Ctrl Pts',(-3.20173798781057,-5.9641898895714,-19.9594296181518));
#42768=CARTESIAN_POINT('Ctrl Pts',(-3.04682206402243,-6.04480415041973,
-19.9512213573797));
#42769=CARTESIAN_POINT('Ctrl Pts',(-2.88891240264724,-6.11935242732685,
-19.9430130966075));
#42770=CARTESIAN_POINT('Ctrl Pts',(-2.73110617159055,-6.19385187535322,
-19.9348102122196));
#42771=CARTESIAN_POINT('Ctrl Pts',(-2.57031043194759,-6.26229310109508,
-19.9266073278317));
#42772=CARTESIAN_POINT('Ctrl Pts',(-2.40703183625131,-6.32443568544046,
-19.9184044434439));
#42773=CARTESIAN_POINT('Ctrl Pts',(-2.24382745331819,-6.38655002497594,
-19.9102052873997));
#42774=CARTESIAN_POINT('Ctrl Pts',(-2.07814279704653,-6.44237129933789,
-19.9020061313554));
#42775=CARTESIAN_POINT('Ctrl Pts',(-1.91050499431835,-6.49170699174606,
-19.8938069753112));
#42776=CARTESIAN_POINT('Ctrl Pts',(-1.74288177200269,-6.54103839314865,
-19.8856085323942));
#42777=CARTESIAN_POINT('Ctrl Pts',(-1.57330608293532,-6.58388522682869,
-19.8774100894772));
#42778=CARTESIAN_POINT('Ctrl Pts',(-1.40232108498669,-6.62010457429501,
-19.8692116465602));
#42779=CARTESIAN_POINT('Ctrl Pts',(-1.23133778984605,-6.65632356105955,
-19.8610132852899));
#42780=CARTESIAN_POINT('Ctrl Pts',(-1.05894556447187,-6.68591511770607,
-19.8528149240197));
#42781=CARTESIAN_POINT('Ctrl Pts',(-0.88569853639518,-6.70878730491789,
-19.8446165627495));
#42782=CARTESIAN_POINT('Ctrl Pts',(-0.712421762090327,-6.73166341924642,
-19.8364167938342));
#42783=CARTESIAN_POINT('Ctrl Pts',(-0.538290248299013,-6.74781781867277,
-19.8282170249189));
#42784=CARTESIAN_POINT('Ctrl Pts',(-0.363864087781422,-6.75721036564816,
-19.8200172560036));
#42785=CARTESIAN_POINT('Ctrl Pts',(-0.189376292490828,-6.76660623154945,
-19.8118145896393));
#42786=CARTESIAN_POINT('Ctrl Pts',(-0.0145940010320489,-6.76923546609791,
-19.8036119232751));
#42787=CARTESIAN_POINT('Ctrl Pts',(0.159921789960391,-6.76511005240091,
-19.7954092569108));
#42788=CARTESIAN_POINT('Ctrl Pts',(0.334635787271743,-6.76097995326509,
-19.7871972743678));
#42789=CARTESIAN_POINT('Ctrl Pts',(0.50908232046455,-6.7500798880267,-19.7789852918248));
#42790=CARTESIAN_POINT('Ctrl Pts',(0.682703554901262,-6.73247390311505,
-19.7707733092818));
#42791=CARTESIAN_POINT('Ctrl Pts',(0.856427193488416,-6.71485753395557,
-19.7625564832005));
#42792=CARTESIAN_POINT('Ctrl Pts',(1.0293242084062,-6.69052741081406,-19.7543396571192));
#42793=CARTESIAN_POINT('Ctrl Pts',(1.20084618305044,-6.65959889517779,-19.7461228310379));
#42794=CARTESIAN_POINT('Ctrl Pts',(1.37263266935201,-6.62862268330349,-19.737893333424));
#42795=CARTESIAN_POINT('Ctrl Pts',(1.54303952781845,-6.59102782148515,-19.7296638358102));
#42796=CARTESIAN_POINT('Ctrl Pts',(1.71153145798003,-6.54698014876666,-19.7214343381963));
#42797=CARTESIAN_POINT('Ctrl Pts',(1.8617179853064,-6.50771793011884,-19.7140989146714));
#42798=CARTESIAN_POINT('Ctrl Pts',(2.01038312910002,-6.46332959546182,-19.7067634911465));
#42799=CARTESIAN_POINT('Ctrl Pts',(2.1571615090825,-6.41396470396688,-19.6994280676216));
#42800=CARTESIAN_POINT('Ctrl Pts',(2.31865583139229,-6.3596505079741,-19.6913571974352));
#42801=CARTESIAN_POINT('Ctrl Pts',(2.47839234892487,-6.29913379034842,-19.6832863272488));
#42802=CARTESIAN_POINT('Ctrl Pts',(2.63584678961586,-6.2325436782803,-19.6752154570624));
#42803=CARTESIAN_POINT('Ctrl Pts',(2.7931052904937,-6.16603643243088,-19.6671546304466));
#42804=CARTESIAN_POINT('Ctrl Pts',(2.94808702594458,-6.09347097388618,-19.6590938038308));
#42805=CARTESIAN_POINT('Ctrl Pts',(3.10028130905614,-6.01502658387452,-19.651032977215));
#42806=CARTESIAN_POINT('Ctrl Pts',(3.25231957209563,-5.93666261015138,-19.6429804140552));
#42807=CARTESIAN_POINT('Ctrl Pts',(3.40157574060937,-5.85243186780364,-19.6349278508953));
#42808=CARTESIAN_POINT('Ctrl Pts',(3.54755770179896,-5.76256222113106,-19.6268752877355));
#42809=CARTESIAN_POINT('Ctrl Pts',(3.69342197603767,-5.67276502508598,-19.6188292163476));
#42810=CARTESIAN_POINT('Ctrl Pts',(3.83601698061662,-5.57733816728854,-19.6107831449597));
#42811=CARTESIAN_POINT('Ctrl Pts',(3.97487398102934,-5.47655601951956,-19.6027370735718));
#42812=CARTESIAN_POINT('Ctrl Pts',(4.11364941184123,-5.3758330748123,-19.5946957287359));
#42813=CARTESIAN_POINT('Ctrl Pts',(4.24869090868095,-5.26976132127368,-19.5866543839));
#42814=CARTESIAN_POINT('Ctrl Pts',(4.37955768302687,-5.15865907974547,-19.5786130390641));
#42815=CARTESIAN_POINT('Ctrl Pts',(4.51294716610432,-5.04541512886285,-19.5704166818431));
#42816=CARTESIAN_POINT('Ctrl Pts',(4.6419989966731,-4.92694497590987,-19.562220324622));
#42817=CARTESIAN_POINT('Ctrl Pts',(4.76628040783076,-4.80362988519397,-19.5540239674009));
#42818=CARTESIAN_POINT('Ctrl Pts',(4.88817260673625,-4.68268542998077,-19.5459851786924));
#42819=CARTESIAN_POINT('Ctrl Pts',(5.00547587849568,-4.55708091549586,-19.5379463899839));
#42820=CARTESIAN_POINT('Ctrl Pts',(5.11781836831975,-4.42721403919994,-19.5299076012754));
#42821=CARTESIAN_POINT('Ctrl Pts',(5.23017287980833,-4.29733326597132,-19.5218679523437));
#42822=CARTESIAN_POINT('Ctrl Pts',(5.33756530793048,-4.16318950515134,-19.513828303412));
#42823=CARTESIAN_POINT('Ctrl Pts',(5.43966361935346,-4.02521411955718,-19.5057886544802));
#42824=CARTESIAN_POINT('Ctrl Pts',(5.54179307207653,-3.88719664969317,-19.497746553352));
#42825=CARTESIAN_POINT('Ctrl Pts',(5.63862497187286,-3.74534552881586,-19.4897044522238));
#42826=CARTESIAN_POINT('Ctrl Pts',(5.72987029471872,-3.60012158207192,-19.4816623510955));
#42827=CARTESIAN_POINT('Ctrl Pts',(5.82419478871754,-3.44999689769468,-19.4733488606508));
#42828=CARTESIAN_POINT('Ctrl Pts',(5.91254882592503,-3.29626813509692,-19.465035370206));
#42829=CARTESIAN_POINT('Ctrl Pts',(5.99466493256604,-3.1394715074775,-19.4567218797613));
#42830=CARTESIAN_POINT('Ctrl Pts',(6.07424033842432,-2.9875262218276,-19.4486656115905));
#42831=CARTESIAN_POINT('Ctrl Pts',(6.14795798087953,-2.83270044954413,-19.4406093434197));
#42832=CARTESIAN_POINT('Ctrl Pts',(6.21562390031658,-2.67550154733898,-19.432553075249));
#42833=CARTESIAN_POINT('Ctrl Pts',(6.28653049793723,-2.51077402426975,-19.4241109736672));
#42834=CARTESIAN_POINT('Ctrl Pts',(6.35079128159519,-2.34344092609721,-19.4156688720855));
#42835=CARTESIAN_POINT('Ctrl Pts',(6.40824229486414,-2.17410204229573,-19.4072267705038));
#42836=CARTESIAN_POINT('Ctrl Pts',(6.46569330813309,-2.00476315849424,-19.398784668922));
#42837=CARTESIAN_POINT('Ctrl Pts',(6.51633450330733,-1.83341895554725,-19.3903425673403));
#42838=CARTESIAN_POINT('Ctrl Pts',(6.56006365577354,-1.66067872636436,-19.3819004657586));
#42839=CARTESIAN_POINT('Ctrl Pts',(6.60323203916829,-1.49015366423727,-19.3735666230659));
#42840=CARTESIAN_POINT('Ctrl Pts',(6.63980242160831,-1.31772619053291,-19.3652327803732));
#42841=CARTESIAN_POINT('Ctrl Pts',(6.66960917268499,-1.14394164345751,-19.3568989376805));
#42842=CARTESIAN_POINT('Ctrl Pts',(6.69938079273463,-0.970361923456567,
-19.3485749174758));
#42843=CARTESIAN_POINT('Ctrl Pts',(6.72240460365799,-0.79542865631812,-19.340250897271));
#42844=CARTESIAN_POINT('Ctrl Pts',(6.73856511291884,-0.619700910886155,
-19.3319268770663));
#42845=CARTESIAN_POINT('Ctrl Pts',(6.75470953798093,-0.444148063406899,
-19.3236111415754));
#42846=CARTESIAN_POINT('Ctrl Pts',(6.76400423914188,-0.267802657257806,
-19.3152954060846));
#42847=CARTESIAN_POINT('Ctrl Pts',(6.76638497210012,-0.0912327207618753,
-19.3069796705937));
#42848=CARTESIAN_POINT('Ctrl Pts',(6.76876377177906,0.0851938317380542,
-19.2986706879137));
#42849=CARTESIAN_POINT('Ctrl Pts',(6.76423978601747,0.261844204963231,-19.2903617052337));
#42850=CARTESIAN_POINT('Ctrl Pts',(6.75280066705504,0.43814626669764,-19.2820527225537));
#42851=CARTESIAN_POINT('Ctrl Pts',(6.74136874246237,0.614337447320704,-19.2737489656165));
#42852=CARTESIAN_POINT('Ctrl Pts',(6.72303037444839,0.790180406891127,-19.2654452086793));
#42853=CARTESIAN_POINT('Ctrl Pts',(6.69782529232956,0.965103804484467,-19.2571414517421));
#42854=CARTESIAN_POINT('Ctrl Pts',(6.6726304428665,1.13995618739502,-19.2488410659301));
#42855=CARTESIAN_POINT('Ctrl Pts',(6.64057448357458,1.31388940847959,-19.240540680118));
#42856=CARTESIAN_POINT('Ctrl Pts',(6.60174894418908,1.48633774018503,-19.232240294306));
#42857=CARTESIAN_POINT('Ctrl Pts',(6.56293159209956,1.65874970702462,-19.2239416588294));
#42858=CARTESIAN_POINT('Ctrl Pts',(6.51734758024701,1.82967706920284,-19.2156430233527));
#42859=CARTESIAN_POINT('Ctrl Pts',(6.46513950353293,1.99856453482442,-19.2073443878761));
#42860=CARTESIAN_POINT('Ctrl Pts',(6.4129337702025,2.16744441985409,-19.1990461248875));
#42861=CARTESIAN_POINT('Ctrl Pts',(6.35410466737922,2.334284258586,-19.1907478618989));
#42862=CARTESIAN_POINT('Ctrl Pts',(6.28884464858707,2.49854397318473,-19.1824495989104));
#42863=CARTESIAN_POINT('Ctrl Pts',(6.22357672708529,2.66282357893356,-19.1741503310376));
#42864=CARTESIAN_POINT('Ctrl Pts',(6.151876466812,2.82452211500237,-19.1658510631648));
#42865=CARTESIAN_POINT('Ctrl Pts',(6.07398451623223,2.9831193567424,-19.157551795292));
#42866=CARTESIAN_POINT('Ctrl Pts',(5.99603787294857,3.14182795930875,-19.1492466999955));
#42867=CARTESIAN_POINT('Ctrl Pts',(5.91189100566273,3.29743060375431,-19.140941604699));
#42868=CARTESIAN_POINT('Ctrl Pts',(5.82183101912393,3.44943076242537,-19.1326365094025));
#42869=CARTESIAN_POINT('Ctrl Pts',(5.73173819203074,3.60148634825858,-19.1243283856364));
#42870=CARTESIAN_POINT('Ctrl Pts',(5.63572813163984,3.74993653463364,-19.1160202618703));
#42871=CARTESIAN_POINT('Ctrl Pts',(5.53413148795322,3.89431350484841,-19.1077121381042));
#42872=CARTESIAN_POINT('Ctrl Pts',(5.43242684762144,4.03884394694823,-19.0993951828505));
#42873=CARTESIAN_POINT('Ctrl Pts',(5.32512396528859,4.17929224173099,-19.0910782275968));
#42874=CARTESIAN_POINT('Ctrl Pts',(5.21259468491312,4.31522254939598,-19.0827612723431));
#42875=CARTESIAN_POINT('Ctrl Pts',(5.12966231736792,4.41540111801554,-19.0766318028606));
#42876=CARTESIAN_POINT('Ctrl Pts',(5.04389210149061,4.51312643698517,-19.070502333378));
#42877=CARTESIAN_POINT('Ctrl Pts',(4.95544567355009,4.60823688372177,-19.0643728638955));
#42878=CARTESIAN_POINT('Ctrl Pts',(4.83347871531932,4.73939347369998,-19.0559203716268));
#42879=CARTESIAN_POINT('Ctrl Pts',(4.70619836508152,4.8658159181396,-19.0474678793582));
#42880=CARTESIAN_POINT('Ctrl Pts',(4.57399803204446,4.98706637241309,-19.0390153870896));
#42881=CARTESIAN_POINT('Ctrl Pts',(4.4419489224322,5.10817812878369,-19.0305725635926));
#42882=CARTESIAN_POINT('Ctrl Pts',(4.30499129864393,5.22412947218761,-19.0221297400956));
#42883=CARTESIAN_POINT('Ctrl Pts',(4.16355581478407,5.33451890775333,-19.0136869165986));
#42884=CARTESIAN_POINT('Ctrl Pts',(4.0222164140432,5.44483335109656,-19.0052498286694));
#42885=CARTESIAN_POINT('Ctrl Pts',(3.87640547584229,5.54959321322586,-18.9968127407403));
#42886=CARTESIAN_POINT('Ctrl Pts',(3.72658789699992,5.64843621243382,-18.9883756528111));
#42887=CARTESIAN_POINT('Ctrl Pts',(3.57686991233555,5.74721350381675,-18.9799441736019));
#42888=CARTESIAN_POINT('Ctrl Pts',(3.42315087482237,5.84008159441289,-18.9715126943926));
#42889=CARTESIAN_POINT('Ctrl Pts',(3.26592606587821,5.92672050397328,-18.9630812151834));
#42890=CARTESIAN_POINT('Ctrl Pts',(3.21073683449655,5.95713259261561,-18.960121587755));
#42891=CARTESIAN_POINT('Ctrl Pts',(3.15511589980604,5.98677753606144,-18.9571619603267));
#42892=CARTESIAN_POINT('Ctrl Pts',(3.09908550384715,6.01564277861015,-18.9542023328983));
#42893=CARTESIAN_POINT('Ctrl Pts',(3.09908550384717,6.01564277861014,-20.9542113918581));
#42894=CARTESIAN_POINT('Ctrl Pts',(2.92882038742808,6.10335845148578,-20.94517233765));
#42895=CARTESIAN_POINT('Ctrl Pts',(2.75477586505623,6.1838690702449,-20.9361332834419));
#42896=CARTESIAN_POINT('Ctrl Pts',(2.57755385392215,6.25687662737017,-20.9270942292338));
#42897=CARTESIAN_POINT('Ctrl Pts',(2.40051490507444,6.32980877100563,-20.9180645119581));
#42898=CARTESIAN_POINT('Ctrl Pts',(2.22030523965799,6.39525323423264,-20.9090347946824));
#42899=CARTESIAN_POINT('Ctrl Pts',(2.03754785581475,6.45295961054032,-20.9000050774067));
#42900=CARTESIAN_POINT('Ctrl Pts',(1.8551275642729,6.51055954860302,-20.890992015262));
#42901=CARTESIAN_POINT('Ctrl Pts',(1.67016916369237,6.56044982527673,-20.8819789531173));
#42902=CARTESIAN_POINT('Ctrl Pts',(1.48331185316542,6.60242947302423,-20.8729658909726));
#42903=CARTESIAN_POINT('Ctrl Pts',(1.29670371392215,6.64435314157194,-20.8639648476045));
#42904=CARTESIAN_POINT('Ctrl Pts',(1.10820194925722,6.67838717830084,-20.8549638042364));
#42905=CARTESIAN_POINT('Ctrl Pts',(0.918459496959166,6.70438074339797,-20.8459627608683));
#42906=CARTESIAN_POINT('Ctrl Pts',(0.729118848265548,6.7303192638384,-20.8369807783462));
#42907=CARTESIAN_POINT('Ctrl Pts',(0.538542991287307,6.74825126235499,-20.8279987958241));
#42908=CARTESIAN_POINT('Ctrl Pts',(0.347393559309,6.75807714627102,-20.8190168133021));
#42909=CARTESIAN_POINT('Ctrl Pts',(0.288925390215197,6.76108265581584,-20.8162694335821));
#42910=CARTESIAN_POINT('Ctrl Pts',(0.230403634598677,6.76333011234689,-20.8135220538621));
#42911=CARTESIAN_POINT('Ctrl Pts',(0.171847416073251,6.76481762249279,-20.8107746741422));
#42912=CARTESIAN_POINT('Ctrl Pts',(-0.00128534660343033,6.7692157333605,
-20.8026515156969));
#42913=CARTESIAN_POINT('Ctrl Pts',(-0.174642473794895,6.76696439773253,
-20.7945283572516));
#42914=CARTESIAN_POINT('Ctrl Pts',(-0.347671132330947,6.75806287213605,
-20.7864051988064));
#42915=CARTESIAN_POINT('Ctrl Pts',(-0.520687591441088,6.74916197414371,
-20.7782826130863));
#42916=CARTESIAN_POINT('Ctrl Pts',(-0.693375262484683,6.73361183893786,
-20.7701600273662));
#42917=CARTESIAN_POINT('Ctrl Pts',(-0.865183633320813,6.71146379567333,
-20.7620374416461));
#42918=CARTESIAN_POINT('Ctrl Pts',(-1.03701264870072,6.68931309109348,-20.7539138799137));
#42919=CARTESIAN_POINT('Ctrl Pts',(-1.20796179062591,6.6605629477761,-20.7457903181814));
#42920=CARTESIAN_POINT('Ctrl Pts',(-1.37748801595936,6.62531627666849,-20.737666756449));
#42921=CARTESIAN_POINT('Ctrl Pts',(-1.5471377210312,6.5900439325435,-20.7295372776659));
#42922=CARTESIAN_POINT('Ctrl Pts',(-1.71536208077116,6.54826568426473,-20.7214077988828));
#42923=CARTESIAN_POINT('Ctrl Pts',(-1.88162993016014,6.50013521443405,-20.7132783200997));
#42924=CARTESIAN_POINT('Ctrl Pts',(-2.04796556402496,6.45198512265793,-20.7051455270712));
#42925=CARTESIAN_POINT('Ctrl Pts',(-2.21234275044118,6.39747776243313,-20.6970127340427));
#42926=CARTESIAN_POINT('Ctrl Pts',(-2.37424797790894,6.33681588334357,-20.6888799410141));
#42927=CARTESIAN_POINT('Ctrl Pts',(-2.53632925274934,6.27608804366336,-20.680738304807));
#42928=CARTESIAN_POINT('Ctrl Pts',(-2.69593286293405,6.20919246016743,-20.6725966685999));
#42929=CARTESIAN_POINT('Ctrl Pts',(-2.85256698655622,6.13637927341601,-20.6644550323927));
#42930=CARTESIAN_POINT('Ctrl Pts',(-2.93236994499914,6.09928194377897,-20.6603069793321));
#42931=CARTESIAN_POINT('Ctrl Pts',(-3.01140249969909,6.0606492768492,-20.6561589262714));
#42932=CARTESIAN_POINT('Ctrl Pts',(-3.0896023418646,6.02051877907085,-20.6520108732108));
#42933=CARTESIAN_POINT('Ctrl Pts',(-3.24872821836542,5.93885875960588,-20.6435701582327));
#42934=CARTESIAN_POINT('Ctrl Pts',(-3.40473220353192,5.85082586380949,-20.6351294432546));
#42935=CARTESIAN_POINT('Ctrl Pts',(-3.55708975953537,5.75668319804109,-20.6266887282765));
#42936=CARTESIAN_POINT('Ctrl Pts',(-3.70933215651976,5.66261168973496,-20.6182543931885));
#42937=CARTESIAN_POINT('Ctrl Pts',(-3.85793333592621,5.56243979189851,-20.6098200581005));
#42938=CARTESIAN_POINT('Ctrl Pts',(-4.00239371274686,5.45647629594085,-20.6013857230125));
#42939=CARTESIAN_POINT('Ctrl Pts',(-4.1467670831485,5.35057662028141,-20.5929564678039));
#42940=CARTESIAN_POINT('Ctrl Pts',(-4.28700435484837,5.23889249745418,-20.5845272125952));
#42941=CARTESIAN_POINT('Ctrl Pts',(-4.42263494853166,5.12177597245588,-20.5760979573866));
#42942=CARTESIAN_POINT('Ctrl Pts',(-4.55820465855936,5.00471202027304,-20.5676724860136));
#42943=CARTESIAN_POINT('Ctrl Pts',(-4.68917156182421,4.88222074571305,-20.5592470146406));
#42944=CARTESIAN_POINT('Ctrl Pts',(-4.81509789671109,4.75469465319157,-20.5508215432676));
#42945=CARTESIAN_POINT('Ctrl Pts',(-4.94098700412073,4.62720626108207,-20.5423985627084));
#42946=CARTESIAN_POINT('Ctrl Pts',(-5.06183828081076,4.49468625628662,-20.5339755821491));
#42947=CARTESIAN_POINT('Ctrl Pts',(-5.17725032162532,4.35756446965854,-20.5255526015899));
#42948=CARTESIAN_POINT('Ctrl Pts',(-5.29266427342344,4.22044041257863,-20.5171294815635));
#42949=CARTESIAN_POINT('Ctrl Pts',(-5.40263858969954,4.07871467219305,-20.5087063615372));
#42950=CARTESIAN_POINT('Ctrl Pts',(-5.50681128787152,3.93285118454421,-20.5002832415109));
#42951=CARTESIAN_POINT('Ctrl Pts',(-5.61098758850913,3.78698265269271,-20.491859830199));
#42952=CARTESIAN_POINT('Ctrl Pts',(-5.70936167704904,3.63697635957528,-20.4834364188871));
#42953=CARTESIAN_POINT('Ctrl Pts',(-5.80161407269013,3.48332644918099,-20.4750130075753));
#42954=CARTESIAN_POINT('Ctrl Pts',(-5.89388252452679,3.3296497965759,-20.4665881301992));
#42955=CARTESIAN_POINT('Ctrl Pts',(-5.98002698759351,3.17232854828038,-20.4581632528231));
#42956=CARTESIAN_POINT('Ctrl Pts',(-6.05977305275952,3.01188305700098,-20.449738375447));
#42957=CARTESIAN_POINT('Ctrl Pts',(-6.1395441226356,2.85138725737118,-20.4413108564155));
#42958=CARTESIAN_POINT('Ctrl Pts',(-6.21291264632887,2.68776556018021,-20.4328833373841));
#42959=CARTESIAN_POINT('Ctrl Pts',(-6.27965147295604,2.52156030627884,-20.4244558183527));
#42960=CARTESIAN_POINT('Ctrl Pts',(-6.34645014838363,2.35520600592923,-20.4160207418479));
#42961=CARTESIAN_POINT('Ctrl Pts',(-6.40660712288565,2.18626382926887,-20.4075856653431));
#42962=CARTESIAN_POINT('Ctrl Pts',(-6.4599440620716,2.01529444868631,-20.3991505888384));
#42963=CARTESIAN_POINT('Ctrl Pts',(-6.51330677935141,1.84424243747654,-20.3907114356056));
#42964=CARTESIAN_POINT('Ctrl Pts',(-6.55984279598541,1.67116158884748,-20.3822722823728));
#42965=CARTESIAN_POINT('Ctrl Pts',(-6.59942431532174,1.49662543956069,-20.37383312914));
#42966=CARTESIAN_POINT('Ctrl Pts',(-6.63904982082356,1.32189533167719,-20.3653845976419));
#42967=CARTESIAN_POINT('Ctrl Pts',(-6.67170532081396,1.1457070186125,-20.3569360661438));
#42968=CARTESIAN_POINT('Ctrl Pts',(-6.6973143557294,0.968643082121012,-20.3484875346457));
#42969=CARTESIAN_POINT('Ctrl Pts',(-6.71146417840731,0.87080951235629,-20.3438194468797));
#42970=CARTESIAN_POINT('Ctrl Pts',(-6.72346369021172,0.772708718850963,
-20.3391513591137));
#42971=CARTESIAN_POINT('Ctrl Pts',(-6.73330680843928,0.674439340063505,
-20.3344832713477));
#42972=CARTESIAN_POINT('Ctrl Pts',(-6.75556168816653,0.452256373728216,
-20.3239289196285));
#42973=CARTESIAN_POINT('Ctrl Pts',(-6.76683268631128,0.22880640812643,-20.3133745679092));
#42974=CARTESIAN_POINT('Ctrl Pts',(-6.76699815055647,0.00500303560476391,
-20.30282021619));
#42975=CARTESIAN_POINT('',(-6.76699940505972,-0.0028375907681064,-20.6971797837861));
#42976=CARTESIAN_POINT('Ctrl Pts',(3.09908550384722,6.01564277861012,-21.3487227114526));
#42977=CARTESIAN_POINT('Ctrl Pts',(2.94376984384265,6.09565692309225,-21.3405091353549));
#42978=CARTESIAN_POINT('Ctrl Pts',(2.78546096918994,6.16959676464732,-21.3322955592572));
#42979=CARTESIAN_POINT('Ctrl Pts',(2.62468011135187,6.23725446916141,-21.3240819831595));
#42980=CARTESIAN_POINT('Ctrl Pts',(2.46379495760027,6.30495606212213,-21.3158630790492));
#42981=CARTESIAN_POINT('Ctrl Pts',(2.3004349593365,6.36636726981934,-21.307644174939));
#42982=CARTESIAN_POINT('Ctrl Pts',(2.13513727481221,6.42132991036183,-21.2994252708288));
#42983=CARTESIAN_POINT('Ctrl Pts',(1.96960157265642,6.47637169343775,-21.2911945320453));
#42984=CARTESIAN_POINT('Ctrl Pts',(1.80212295443262,6.52494626216037,-21.2829637932618));
#42985=CARTESIAN_POINT('Ctrl Pts',(1.63325058337474,6.56694613438439,-21.2747330544783));
#42986=CARTESIAN_POINT('Ctrl Pts',(1.54365516646979,6.58922921146972,-21.2703662272221));
#42987=CARTESIAN_POINT('Ctrl Pts',(1.45366756059266,6.60966248588322,-21.265999399966));
#42988=CARTESIAN_POINT('Ctrl Pts',(1.36337035817647,6.62823583364728,-21.2616325727098));
#42989=CARTESIAN_POINT('Ctrl Pts',(1.19648099980474,6.66256352053254,-21.2535617025234));
#42990=CARTESIAN_POINT('Ctrl Pts',(1.02798955814346,6.69064665127868,-21.245490832337));
#42991=CARTESIAN_POINT('Ctrl Pts',(0.858414069773042,6.71233299865372,-21.2374199621506));
#42992=CARTESIAN_POINT('Ctrl Pts',(0.689049604917057,6.73399235905511,-21.2293591355348));
#42993=CARTESIAN_POINT('Ctrl Pts',(0.518604142883801,6.74927072839133,-21.221298308919));
#42994=CARTESIAN_POINT('Ctrl Pts',(0.347609218017789,6.75806605705723,-21.2132374823032));
#42995=CARTESIAN_POINT('Ctrl Pts',(0.176789586467174,6.7668523693016,-21.2051849191433));
#42996=CARTESIAN_POINT('Ctrl Pts',(0.00542198239936081,6.76916884768676,
-21.1971323559835));
#42997=CARTESIAN_POINT('Ctrl Pts',(-0.165953663895494,6.76496477311151,
-21.1890797928236));
#42998=CARTESIAN_POINT('Ctrl Pts',(-0.33719115149453,6.76076408775447,-21.1810337214357));
#42999=CARTESIAN_POINT('Ctrl Pts',(-0.508436297411776,6.75005332122249,
-21.1729876500478));
#43000=CARTESIAN_POINT('Ctrl Pts',(-0.679145971473218,6.73283370873154,
-21.1649415786599));
#43001=CARTESIAN_POINT('Ctrl Pts',(-0.849755364526388,6.7156242116609,-21.1569002338241));
#43002=CARTESIAN_POINT('Ctrl Pts',(-1.01982954173331,6.69191351756044,-21.1488588889882));
#43003=CARTESIAN_POINT('Ctrl Pts',(-1.18882740769602,6.66175490353036,-21.1408175441523));
#43004=CARTESIAN_POINT('Ctrl Pts',(-1.36108303250737,6.63101492421995,-21.1326211869312));
#43005=CARTESIAN_POINT('Ctrl Pts',(-1.53222003083641,6.59357590825049,-21.1244248297102));
#43006=CARTESIAN_POINT('Ctrl Pts',(-1.70167256602109,6.54954956298914,-21.1162284724891));
#43007=CARTESIAN_POINT('Ctrl Pts',(-1.86786750966858,6.50636958954265,-21.1081896837806));
#43008=CARTESIAN_POINT('Ctrl Pts',(-2.03244179881798,6.4568533803236,-21.1001508950721));
#43009=CARTESIAN_POINT('Ctrl Pts',(-2.19487396594561,6.40115749482968,-21.0921121063636));
#43010=CARTESIAN_POINT('Ctrl Pts',(-2.35732351478699,6.34545564937133,-21.0840724574319));
#43011=CARTESIAN_POINT('Ctrl Pts',(-2.51763013184477,6.28357293197529,-21.0760328085002));
#43012=CARTESIAN_POINT('Ctrl Pts',(-2.67528982156531,6.21571503293298,-21.0679931595685));
#43013=CARTESIAN_POINT('Ctrl Pts',(-2.83299759952107,6.14783643635781,-21.0599510584403));
#43014=CARTESIAN_POINT('Ctrl Pts',(-2.98805650026762,6.07397917800655,-21.0519089573121));
#43015=CARTESIAN_POINT('Ctrl Pts',(-3.13998487003631,5.99439605097487,-21.043866856184));
#43016=CARTESIAN_POINT('Ctrl Pts',(-3.29704022537577,5.91212730607873,-21.0355533657392));
#43017=CARTESIAN_POINT('Ctrl Pts',(-3.45074967952638,5.82373968225327,-21.0272398752944));
#43018=CARTESIAN_POINT('Ctrl Pts',(-3.60061226632843,5.72956196471993,-21.0189263848497));
#43019=CARTESIAN_POINT('Ctrl Pts',(-3.74583805278521,5.63829813838848,-21.0108701166789));
#43020=CARTESIAN_POINT('Ctrl Pts',(-3.88745121120484,5.5415974458643,-21.0028138485082));
#43021=CARTESIAN_POINT('Ctrl Pts',(-4.02502882471039,5.43980072799091,-20.9947575803374));
#43022=CARTESIAN_POINT('Ctrl Pts',(-4.16919534995163,5.33312872865306,-20.9863154787556));
#43023=CARTESIAN_POINT('Ctrl Pts',(-4.30892990245549,5.22086088420463,-20.9778733771739));
#43024=CARTESIAN_POINT('Ctrl Pts',(-4.44378898078276,5.103433010658,-20.9694312755921));
#43025=CARTESIAN_POINT('Ctrl Pts',(-4.57864805911003,4.98600513711137,-20.9609891740104));
#43026=CARTESIAN_POINT('Ctrl Pts',(-4.70863138729938,4.86341761358131,-20.9525470724286));
#43027=CARTESIAN_POINT('Ctrl Pts',(-4.83334402845879,4.73614553224052,-20.9441049708468));
#43028=CARTESIAN_POINT('Ctrl Pts',(-4.9558363074393,4.61113938090659,-20.9358131709738));
#43029=CARTESIAN_POINT('Ctrl Pts',(-5.07364241516591,4.48120821135264,-20.9275213711007));
#43030=CARTESIAN_POINT('Ctrl Pts',(-5.1863463975287,4.34673441158315,-20.9192295712277));
#43031=CARTESIAN_POINT('Ctrl Pts',(-5.29891343238729,4.21242401199591,-20.9109478467865));
#43032=CARTESIAN_POINT('Ctrl Pts',(-5.40639046637114,4.07358224496628,-20.9026661223453));
#43033=CARTESIAN_POINT('Ctrl Pts',(-5.50839779121519,3.9306288013161,-20.8943843979041));
#43034=CARTESIAN_POINT('Ctrl Pts',(-5.61027524080661,3.78785736532699,-20.8861132177161));
#43035=CARTESIAN_POINT('Ctrl Pts',(-5.70669666066461,3.64098497389965,-20.877842037528));
#43036=CARTESIAN_POINT('Ctrl Pts',(-5.79732225400218,3.4904646801323,-20.86957085734));
#43037=CARTESIAN_POINT('Ctrl Pts',(-5.8878808627161,3.34005564130806,-20.8613057906776));
#43038=CARTESIAN_POINT('Ctrl Pts',(-5.97265199587638,3.18600437059106,-20.8530407240153));
#43039=CARTESIAN_POINT('Ctrl Pts',(-6.05133844476635,3.0287938237676,-20.8447756573529));
#43040=CARTESIAN_POINT('Ctrl Pts',(-6.12998036878378,2.87167223482263,-20.8365152674938));
#43041=CARTESIAN_POINT('Ctrl Pts',(-6.20254430962975,2.7113952450136,-20.8282548776346));
#43042=CARTESIAN_POINT('Ctrl Pts',(-6.26877834314064,2.54847151927796,-20.8199944877755));
#43043=CARTESIAN_POINT('Ctrl Pts',(-6.33498637325979,2.38561175717613,-20.8117373409342));
#43044=CARTESIAN_POINT('Ctrl Pts',(-6.39486931500216,2.22010765550495,-20.803480194093));
#43045=CARTESIAN_POINT('Ctrl Pts',(-6.44822280095868,2.0524891495929,-20.7952230472517));
#43046=CARTESIAN_POINT('Ctrl Pts',(-6.50157393681254,1.88487802690407,-20.7869662641194));
#43047=CARTESIAN_POINT('Ctrl Pts',(-6.54839607469187,1.7151530185966,-20.7787094809872));
#43048=CARTESIAN_POINT('Ctrl Pts',(-6.58853415249703,1.54386097864422,-20.7704526978549));
#43049=CARTESIAN_POINT('Ctrl Pts',(-6.62866964037057,1.37257999140522,-20.7621964474961));
#43050=CARTESIAN_POINT('Ctrl Pts',(-6.66212185064965,1.19973251806868,-20.7539401971373));
#43051=CARTESIAN_POINT('Ctrl Pts',(-6.68878650618458,1.02587722203155,-20.7456839467786));
#43052=CARTESIAN_POINT('Ctrl Pts',(-6.71546374862139,0.851939858571766,
-20.7374237991028));
#43053=CARTESIAN_POINT('Ctrl Pts',(-6.73534698013193,0.676994070549397,
-20.7291636514271));
#43054=CARTESIAN_POINT('Ctrl Pts',(-6.74838353860457,0.501606036537511,
-20.7209035037514));
#43055=CARTESIAN_POINT('Ctrl Pts',(-6.76086417350953,0.333697149863501,
-20.7129955971043));
#43056=CARTESIAN_POINT('Ctrl Pts',(-6.7670699447143,0.165383243452747,-20.7050876904571));
#43057=CARTESIAN_POINT('Ctrl Pts',(-6.76699940505994,-0.002837590259075,
-20.69717978381));
#43058=CARTESIAN_POINT('Ctrl Pts',(-6.76699940505972,-0.00283759076810723,
-20.697179783786));
#43059=CARTESIAN_POINT('Ctrl Pts',(-6.76690610989687,-0.225325032808874,
-20.686720853801));
#43060=CARTESIAN_POINT('Ctrl Pts',(-6.75583636494396,-0.447452435014028,
-20.6762619238159));
#43061=CARTESIAN_POINT('Ctrl Pts',(-6.73391989437842,-0.668290248390996,
-20.6658029938309));
#43062=CARTESIAN_POINT('Ctrl Pts',(-6.71173178705549,-0.891865166146056,
-20.6552144339486));
#43063=CARTESIAN_POINT('Ctrl Pts',(-6.67842640940602,-1.11411854687437,
-20.6446258740662));
#43064=CARTESIAN_POINT('Ctrl Pts',(-6.63418845455005,-1.33410365021419,
-20.6340373141839));
#43065=CARTESIAN_POINT('Ctrl Pts',(-6.62379948372796,-1.3857655958745,-20.6315506657839));
#43066=CARTESIAN_POINT('Ctrl Pts',(-6.61280778413403,-1.43730251158528,
-20.6290640173838));
#43067=CARTESIAN_POINT('Ctrl Pts',(-6.60121614522909,-1.48870225497473,
-20.6265773689837));
#43068=CARTESIAN_POINT('Ctrl Pts',(-6.56182126613055,-1.66338736146639,
-20.6181263454585));
#43069=CARTESIAN_POINT('Ctrl Pts',(-6.51545491227376,-1.83665557159931,
-20.6096753219333));
#43070=CARTESIAN_POINT('Ctrl Pts',(-6.46223666432076,-2.00793084898572,
-20.6012242984081));
#43071=CARTESIAN_POINT('Ctrl Pts',(-6.40906527345337,-2.17905532358093,
-20.5927807157579));
#43072=CARTESIAN_POINT('Ctrl Pts',(-6.34905411108343,-2.34819004782845,
-20.5843371331077));
#43073=CARTESIAN_POINT('Ctrl Pts',(-6.28237334123594,-2.51477120258047,
-20.5758935504575));
#43074=CARTESIAN_POINT('Ctrl Pts',(-6.21574221729914,-2.68122833247269,
-20.5674562543177));
#43075=CARTESIAN_POINT('Ctrl Pts',(-6.1424515076189,-2.84513537610459,-20.5590189581778));
#43076=CARTESIAN_POINT('Ctrl Pts',(-6.06272067319979,-3.00594528206284,
-20.550581662038));
#43077=CARTESIAN_POINT('Ctrl Pts',(-5.9830467206515,-3.1666404624151,-20.5421503852656));
#43078=CARTESIAN_POINT('Ctrl Pts',(-5.89694195483159,-3.32424261618742,
-20.5337191084932));
#43079=CARTESIAN_POINT('Ctrl Pts',(-5.80467334503278,-3.47822603599392,
-20.5252878317209));
#43080=CARTESIAN_POINT('Ctrl Pts',(-5.71244428489993,-3.63214345293304,
-20.5168601688989));
#43081=CARTESIAN_POINT('Ctrl Pts',(-5.61405681789739,-3.78244494431092,
-20.5084325060769));
#43082=CARTESIAN_POINT('Ctrl Pts',(-5.50982342841356,-3.92863014137308,
-20.5000048432549));
#43083=CARTESIAN_POINT('Ctrl Pts',(-5.40562212608989,-4.07477033684934,
-20.4915797748009));
#43084=CARTESIAN_POINT('Ctrl Pts',(-5.29557868237724,-4.21679649545947,
-20.4831547063469));
#43085=CARTESIAN_POINT('Ctrl Pts',(-5.18004860928113,-4.35423763769097,
-20.4747296378929));
#43086=CARTESIAN_POINT('Ctrl Pts',(-5.14843604500035,-4.39184574116723,
-20.4724242812794));
#43087=CARTESIAN_POINT('Ctrl Pts',(-5.11641291745343,-4.42911072769324,
-20.4701189246659));
#43088=CARTESIAN_POINT('Ctrl Pts',(-5.08398704627483,-4.46602336685666,
-20.4678135680524));
#43089=CARTESIAN_POINT('Ctrl Pts',(-4.96275712030799,-4.60402787838927,
-20.4591945795279));
#43090=CARTESIAN_POINT('Ctrl Pts',(-4.83594889133726,-4.73704311541802,
-20.4505755910034));
#43091=CARTESIAN_POINT('Ctrl Pts',(-4.70400004711802,-4.8646348842142,-20.441956602479));
#43092=CARTESIAN_POINT('Ctrl Pts',(-4.57197215376572,-4.99230309186642,
-20.4333324504112));
#43093=CARTESIAN_POINT('Ctrl Pts',(-4.43479771769685,-5.11454113556306,
-20.4247082983434));
#43094=CARTESIAN_POINT('Ctrl Pts',(-4.2929493115592,-5.23095356587911,-20.4160841462757));
#43095=CARTESIAN_POINT('Ctrl Pts',(-4.14624255934967,-5.35135315325208,
-20.4071646146794));
#43096=CARTESIAN_POINT('Ctrl Pts',(-3.99453628083196,-5.46552078351104,
-20.3982450830832));
#43097=CARTESIAN_POINT('Ctrl Pts',(-3.83838748395861,-5.57306652777355,
-20.3893255514869));
#43098=CARTESIAN_POINT('Ctrl Pts',(-3.68712846223965,-5.67724449387327,
-20.3806853336277));
#43099=CARTESIAN_POINT('Ctrl Pts',(-3.5317012273828,-5.77520890086533,-20.3720451157685));
#43100=CARTESIAN_POINT('Ctrl Pts',(-3.37263914307193,-5.86665102171751,
-20.3634048979093));
#43101=CARTESIAN_POINT('Ctrl Pts',(-3.20586401970692,-5.96252723918285,
-20.3543457094445));
#43102=CARTESIAN_POINT('Ctrl Pts',(-3.03509311409394,-6.05123272490519,
-20.3452865209797));
#43103=CARTESIAN_POINT('Ctrl Pts',(-2.86096765872771,-6.13246712634598,
-20.336227332515));
#43104=CARTESIAN_POINT('Ctrl Pts',(-2.68684220336148,-6.21370152778676,
-20.3271681440502));
#43105=CARTESIAN_POINT('Ctrl Pts',(-2.50936256428131,-6.28746472868872,
-20.3181089555854));
#43106=CARTESIAN_POINT('Ctrl Pts',(-2.32919171885676,-6.35351516381358,
-20.3090497671206));
#43107=CARTESIAN_POINT('Ctrl Pts',(-2.14933300678128,-6.41945117119363,
-20.3000062730643));
#43108=CARTESIAN_POINT('Ctrl Pts',(-1.96662700198859,-6.4777626523508,-20.290962779008));
#43109=CARTESIAN_POINT('Ctrl Pts',(-1.78170898057334,-6.52823116230916,
-20.2819192849516));
#43110=CARTESIAN_POINT('Ctrl Pts',(-1.59696010299598,-6.57865350890602,
-20.2728840629462));
#43111=CARTESIAN_POINT('Ctrl Pts',(-1.41000347785843,-6.62124714446272,
-20.2638488409408));
#43112=CARTESIAN_POINT('Ctrl Pts',(-1.2214891677209,-6.65584353881163,-20.2548136189355));
#43113=CARTESIAN_POINT('Ctrl Pts',(-1.03330697875866,-6.69037898184526,
-20.2457943150243));
#43114=CARTESIAN_POINT('Ctrl Pts',(-0.843572818697793,-6.71694527552576,
-20.2367750111131));
#43115=CARTESIAN_POINT('Ctrl Pts',(-0.65294639234871,-6.73542500579725,
-20.2277557072019));
#43116=CARTESIAN_POINT('Ctrl Pts',(-0.46255912016646,-6.75388155195632,
-20.2187477186375));
#43117=CARTESIAN_POINT('Ctrl Pts',(-0.27128205192631,-6.76427175805119,
-20.2097397300731));
#43118=CARTESIAN_POINT('Ctrl Pts',(-0.0797819989741408,-6.76652967425989,
-20.2007317415087));
#43119=CARTESIAN_POINT('Ctrl Pts',(0.111285544400721,-6.76878249088575,
-20.1917440978019));
#43120=CARTESIAN_POINT('Ctrl Pts',(0.302574829586595,-6.76293967716026,
-20.1827564540952));
#43121=CARTESIAN_POINT('Ctrl Pts',(0.493417520390925,-6.74898719442935,
-20.1737688103885));
#43122=CARTESIAN_POINT('Ctrl Pts',(0.659628276733426,-6.73683554902031,
-20.1659411956554));
#43123=CARTESIAN_POINT('Ctrl Pts',(0.825500093690068,-6.71853332503442,
-20.1581135809224));
#43124=CARTESIAN_POINT('Ctrl Pts',(0.990589840914559,-6.69410343265451,
-20.1502859661894));
#43125=CARTESIAN_POINT('Ctrl Pts',(1.16191280712198,-6.66875115186773,-20.1421628077441));
#43126=CARTESIAN_POINT('Ctrl Pts',(1.33231670434845,-6.63680942570651,-20.1340396492988));
#43127=CARTESIAN_POINT('Ctrl Pts',(1.50125675876329,-6.59837231021921,-20.1259164908535));
#43128=CARTESIAN_POINT('Ctrl Pts',(1.67018490202014,-6.55993790474971,-20.1177939051335));
#43129=CARTESIAN_POINT('Ctrl Pts',(1.83764905114325,-6.51500910336602,-20.1096713194134));
#43130=CARTESIAN_POINT('Ctrl Pts',(2.00311564730734,-6.4637308656466,-20.1015487336933));
#43131=CARTESIAN_POINT('Ctrl Pts',(2.16860212598614,-6.4124464663191,-20.0934251719609));
#43132=CARTESIAN_POINT('Ctrl Pts',(2.33209022449831,-6.35481122093328,-20.0853016102286));
#43133=CARTESIAN_POINT('Ctrl Pts',(2.49306258660471,-6.291019626362,-20.0771780484962));
#43134=CARTESIAN_POINT('Ctrl Pts',(2.65415219797476,-6.22718156718405,-20.0690485697131));
#43135=CARTESIAN_POINT('Ctrl Pts',(2.81272207249889,-6.15717833774076,-20.06091909093));
#43136=CARTESIAN_POINT('Ctrl Pts',(2.96827526143845,-6.08125241807413,-20.0527896121469));
#43137=CARTESIAN_POINT('Ctrl Pts',(3.12389186667537,-6.00529554474638,-20.0446568191184));
#43138=CARTESIAN_POINT('Ctrl Pts',(3.27648901257774,-5.92341134117101,-20.0365240260899));
#43139=CARTESIAN_POINT('Ctrl Pts',(3.42559555549937,-5.83588760088326,-20.0283912330614));
#43140=CARTESIAN_POINT('Ctrl Pts',(3.57486422916567,-5.74826869180606,-20.0202495968542));
#43141=CARTESIAN_POINT('Ctrl Pts',(3.72063441109514,-5.65499819520947,-20.0121079606471));
#43142=CARTESIAN_POINT('Ctrl Pts',(3.86246445167112,-5.55640687491268,-20.00396632444));
#43143=CARTESIAN_POINT('Ctrl Pts',(3.93472493088678,-5.50617593637372,-19.9998182713792));
#43144=CARTESIAN_POINT('Ctrl Pts',(4.0059631669425,-5.45456449015567,-19.9956702183184));
#43145=CARTESIAN_POINT('Ctrl Pts',(4.07612420460438,-5.4016201707116,-19.9915221652576));
#43146=CARTESIAN_POINT('Ctrl Pts',(4.21889222439334,-5.2938857942257,-19.9830814502795));
#43147=CARTESIAN_POINT('Ctrl Pts',(4.35749189409003,-5.1804081942767,-19.9746407353014));
#43148=CARTESIAN_POINT('Ctrl Pts',(4.49145155575035,-5.06153651793087,-19.9662000203233));
#43149=CARTESIAN_POINT('Ctrl Pts',(4.62530996438702,-4.94275469039855,-19.9577656852353));
#43150=CARTESIAN_POINT('Ctrl Pts',(4.75453510776097,-4.8185871344218,-19.9493313501472));
#43151=CARTESIAN_POINT('Ctrl Pts',(4.87868774436357,-4.68942372717552,-19.9408970150592));
#43152=CARTESIAN_POINT('Ctrl Pts',(5.00276560560868,-4.56033811320223,-19.9324677598506));
#43153=CARTESIAN_POINT('Ctrl Pts',(5.12177682040649,-4.42626288648985,-19.924038504642));
#43154=CARTESIAN_POINT('Ctrl Pts',(5.23531813964038,-4.28762556396339,-19.9156092494333));
#43155=CARTESIAN_POINT('Ctrl Pts',(5.34880849094456,-4.14905047479266,-19.9071837780603));
#43156=CARTESIAN_POINT('Ctrl Pts',(5.45683363158883,-4.00591763061263,-19.8987583066873));
#43157=CARTESIAN_POINT('Ctrl Pts',(5.55902958131697,-3.8586887817033,-19.8903328353143));
#43158=CARTESIAN_POINT('Ctrl Pts',(5.6611953189577,-3.71150345791277,-19.881909854755));
#43159=CARTESIAN_POINT('Ctrl Pts',(5.7575351123742,-3.56022481780452,-19.8734868741958));
#43160=CARTESIAN_POINT('Ctrl Pts',(5.84772719934591,-3.40534515167407,-19.8650638936365));
#43161=CARTESIAN_POINT('Ctrl Pts',(5.93792077971138,-3.25046292105781,-19.8566407736102));
#43162=CARTESIAN_POINT('Ctrl Pts',(6.02196627679717,-3.09197983001042,-19.8482176535838));
#43163=CARTESIAN_POINT('Ctrl Pts',(6.09958661481354,-2.9304150095827,-19.8397945335575));
#43164=CARTESIAN_POINT('Ctrl Pts',(6.17720963707058,-2.76884460197417,-19.8313711222456));
#43165=CARTESIAN_POINT('Ctrl Pts',(6.24840691266008,-2.60419255303586,-19.8229477109338));
#43166=CARTESIAN_POINT('Ctrl Pts',(6.31294841761153,-2.43700046708574,-19.8145242996219));
#43167=CARTESIAN_POINT('Ctrl Pts',(6.37750115577832,-2.26977928195817,-19.8060994222458));
#43168=CARTESIAN_POINT('Ctrl Pts',(6.43539569367677,-2.10001748954333,-19.7976745448697));
#43169=CARTESIAN_POINT('Ctrl Pts',(6.48645090528201,-1.92827478678902,-19.7892496674935));
#43170=CARTESIAN_POINT('Ctrl Pts',(6.53752212546106,-1.7564782333964,-19.7808221484621));
#43171=CARTESIAN_POINT('Ctrl Pts',(6.58174964880295,-1.58269985085183,-19.7723946294307));
#43172=CARTESIAN_POINT('Ctrl Pts',(6.61900267776738,-1.40751289575201,-19.7639671103992));
#43173=CARTESIAN_POINT('Ctrl Pts',(6.65628911380841,-1.23216883976163,-19.7555320338944));
#43174=CARTESIAN_POINT('Ctrl Pts',(6.68658848873907,-1.0554140137599,-19.7470969573896));
#43175=CARTESIAN_POINT('Ctrl Pts',(6.70982124171321,-0.87783136436004,-19.7386618808848));
#43176=CARTESIAN_POINT('Ctrl Pts',(6.73306522322976,-0.700162888097009,
-19.7302227276521));
#43177=CARTESIAN_POINT('Ctrl Pts',(6.74923573608721,-0.521666121963206,
-19.7217835744193));
#43178=CARTESIAN_POINT('Ctrl Pts',(6.75830521449227,-0.342928021261989,
-19.7133444211865));
#43179=CARTESIAN_POINT('Ctrl Pts',(6.76738477163065,-0.163991292417934,
-19.7048958896884));
#43180=CARTESIAN_POINT('Ctrl Pts',(6.76934751775323,0.0151869734734661,
-19.6964473581903));
#43181=CARTESIAN_POINT('Ctrl Pts',(6.76421801476277,0.194019712294481,-19.6879988266921));
#43182=CARTESIAN_POINT('Ctrl Pts',(6.76138379793354,0.292830602730925,-19.6833307389264));
#43183=CARTESIAN_POINT('Ctrl Pts',(6.75638529577431,0.391536068360939,-19.6786626511606));
#43184=CARTESIAN_POINT('Ctrl Pts',(6.74923342816245,0.490037888509266,-19.6739945633948));
#43185=CARTESIAN_POINT('Ctrl Pts',(6.73660792944772,0.663927377405493,-19.6657537877981));
#43186=CARTESIAN_POINT('Ctrl Pts',(6.71724048820842,0.837568704094568,-19.6575130122014));
#43187=CARTESIAN_POINT('Ctrl Pts',(6.69114183123352,1.01040090771779,-19.6492722366046));
#43188=CARTESIAN_POINT('Ctrl Pts',(6.66507208135067,1.18304168093814,-19.6410405885603));
#43189=CARTESIAN_POINT('Ctrl Pts',(6.63228601375324,1.3548747668677,-19.6328089405159));
#43190=CARTESIAN_POINT('Ctrl Pts',(6.59284629547915,1.52534151067453,-19.6245772924716));
#43191=CARTESIAN_POINT('Ctrl Pts',(6.55344323244275,1.69564982284732,-19.6163532949133));
#43192=CARTESIAN_POINT('Ctrl Pts',(6.50739891388341,1.86459397730371,-19.6081292973551));
#43193=CARTESIAN_POINT('Ctrl Pts',(6.4548275304281,2.03162264026257,-19.5999052997968));
#43194=CARTESIAN_POINT('Ctrl Pts',(6.40230259399432,2.19850373274878,-19.5916885681723));
#43195=CARTESIAN_POINT('Ctrl Pts',(6.34326219268906,2.36347236868078,-19.5834718365478));
#43196=CARTESIAN_POINT('Ctrl Pts',(6.27787105981086,2.52598969839335,-19.5752551049234));
#43197=CARTESIAN_POINT('Ctrl Pts',(6.21251342923086,2.68842376446137,-19.5670425830347));
#43198=CARTESIAN_POINT('Ctrl Pts',(6.14081167967596,2.84840869629969,-19.558830061146));
#43199=CARTESIAN_POINT('Ctrl Pts',(6.06297977202706,3.00542264648264,-19.5506175392573));
#43200=CARTESIAN_POINT('Ctrl Pts',(5.98517389174274,3.16238409044484,-19.5424077636755));
#43201=CARTESIAN_POINT('Ctrl Pts',(5.90124209495802,3.31637621352116,-19.5341979880937));
#43202=CARTESIAN_POINT('Ctrl Pts',(5.81144572066407,3.46689884994866,-19.5259882125118));
#43203=CARTESIAN_POINT('Ctrl Pts',(5.77222499729605,3.532643226939,-19.5224023958289));
#43204=CARTESIAN_POINT('Ctrl Pts',(5.73188607893753,3.59772602604172,-19.518816579146));
#43205=CARTESIAN_POINT('Ctrl Pts',(5.69045347539414,3.66210707713124,-19.5152307624631));
#43206=CARTESIAN_POINT('Ctrl Pts',(5.58809472048836,3.82115969911162,-19.5063720449413));
#43207=CARTESIAN_POINT('Ctrl Pts',(5.47916413964674,3.97576271632485,-19.4975133274195));
#43208=CARTESIAN_POINT('Ctrl Pts',(5.36407382894608,4.12540918668872,-19.4886546098977));
#43209=CARTESIAN_POINT('Ctrl Pts',(5.24876820275861,4.27533562156413,-19.4797793191383));
#43210=CARTESIAN_POINT('Ctrl Pts',(5.12727997516108,4.42028677274613,-19.4709040283788));
#43211=CARTESIAN_POINT('Ctrl Pts',(5.00006018296063,4.55979025469064,-19.4620287376193));
#43212=CARTESIAN_POINT('Ctrl Pts',(4.87247905794568,4.69968995789044,-19.4531282390385));
#43213=CARTESIAN_POINT('Ctrl Pts',(4.73913396803678,4.83411083644751,-19.4442277404577));
#43214=CARTESIAN_POINT('Ctrl Pts',(4.60051358868938,4.96261662032081,-19.4353272418769));
#43215=CARTESIAN_POINT('Ctrl Pts',(4.46170555874889,5.09129636264577,-19.4264146946792));
#43216=CARTESIAN_POINT('Ctrl Pts',(4.31760816908561,5.21404484380893,-19.4175021474816));
#43217=CARTESIAN_POINT('Ctrl Pts',(4.16874269820536,5.33046651956088,-19.4085896002839));
#43218=CARTESIAN_POINT('Ctrl Pts',(4.01954851782667,5.44714526574305,-19.3996573733117));
#43219=CARTESIAN_POINT('Ctrl Pts',(3.86556540283638,5.55746910337499,-19.3907251463394));
#43220=CARTESIAN_POINT('Ctrl Pts',(3.70734545794155,5.66108458296466,-19.3817929193671));
#43221=CARTESIAN_POINT('Ctrl Pts',(3.55780933943677,5.75901317626022,-19.373350933422));
#43222=CARTESIAN_POINT('Ctrl Pts',(3.40448908974002,5.85094986113632,-19.3649089474768));
#43223=CARTESIAN_POINT('Ctrl Pts',(3.24787039536178,5.93663430699016,-19.3564669615317));
#43224=CARTESIAN_POINT('Ctrl Pts',(3.19862647078751,5.96357514189857,-19.3538126390654));
#43225=CARTESIAN_POINT('Ctrl Pts',(3.14902628467463,5.98991472998606,-19.351158316599));
#43226=CARTESIAN_POINT('Ctrl Pts',(3.09908550384723,6.01564277861011,-19.3485039941327));
#43227=CARTESIAN_POINT('Origin',(0.,0.,-63.6971797838103));
#43228=CARTESIAN_POINT('',(3.09908550384726,6.0156427786101,-16.9542436419539));
#43229=CARTESIAN_POINT('',(3.09908550384714,6.01564277861016,-17.3484577403131));
#43230=CARTESIAN_POINT('',(3.09908550384721,6.01564277861012,-63.6971797838103));
#43231=CARTESIAN_POINT('',(-6.767,5.61700751015859E-13,-18.30282021619));
#43232=CARTESIAN_POINT('Ctrl Pts',(-6.767,5.61700785041895E-13,-18.30282021619));
#43233=CARTESIAN_POINT('Ctrl Pts',(-6.76700000000002,-0.186007249559512,
-18.2940707043773));
#43234=CARTESIAN_POINT('Ctrl Pts',(-6.75932637294249,-0.372014355815761,
-18.2853211925645));
#43235=CARTESIAN_POINT('Ctrl Pts',(-6.74400518263364,-0.557389537586201,
-18.2765716807518));
#43236=CARTESIAN_POINT('Ctrl Pts',(-6.7286840570373,-0.742763936382802,
-18.2678222058946));
#43237=CARTESIAN_POINT('Ctrl Pts',(-6.70571545643561,-0.927506130405237,
-18.2590727310374));
#43238=CARTESIAN_POINT('Ctrl Pts',(-6.67517739401568,-1.11098864009588,
-18.2503232561801));
#43239=CARTESIAN_POINT('Ctrl Pts',(-6.64463945804381,-1.29447039004583,
-18.2415738175516));
#43240=CARTESIAN_POINT('Ctrl Pts',(-6.60653217002715,-1.47669218339318,
-18.2328243789231));
#43241=CARTESIAN_POINT('Ctrl Pts',(-6.5609849608547,-1.65703510627821,-18.2240749402946));
#43242=CARTESIAN_POINT('Ctrl Pts',(-6.5154379364954,-1.83737729740069,-18.215325537168));
#43243=CARTESIAN_POINT('Ctrl Pts',(-6.46245112156871,-2.01584035545033,
-18.2065761340413));
#43244=CARTESIAN_POINT('Ctrl Pts',(-6.40220448361682,-2.1918181379751,-18.1978267309147));
#43245=CARTESIAN_POINT('Ctrl Pts',(-6.3419580851193,-2.36779522106419,-18.1890773625632));
#43246=CARTESIAN_POINT('Ctrl Pts',(-6.27445201416302,-2.54128677725873,
-18.1803279942116));
#43247=CARTESIAN_POINT('Ctrl Pts',(-6.19991555052662,-2.71170355428801,
-18.1715786258601));
#43248=CARTESIAN_POINT('Ctrl Pts',(-6.12537937695044,-2.8821196681368,-18.1628292915569));
#43249=CARTESIAN_POINT('Ctrl Pts',(-6.04381298028259,-3.04946076420052,
-18.1540799572537));
#43250=CARTESIAN_POINT('Ctrl Pts',(-5.95549339308771,-3.21315848424704,
-18.1453306229505));
#43251=CARTESIAN_POINT('Ctrl Pts',(-5.86717414225596,-3.37685558085452,
-18.136581321969));
#43252=CARTESIAN_POINT('Ctrl Pts',(-5.77210188843853,-3.53690907700348,
-18.1278320209874));
#43253=CARTESIAN_POINT('Ctrl Pts',(-5.67059953311159,-3.69277537024318,
-18.1190827200059));
#43254=CARTESIAN_POINT('Ctrl Pts',(-5.56909755592481,-3.84864108281355,
-18.1103334516192));
#43255=CARTESIAN_POINT('Ctrl Pts',(-5.46116568154725,-4.00031938355158,
-18.1015841832326));
#43256=CARTESIAN_POINT('Ctrl Pts',(-5.34717048488122,-4.14729511918493,
-18.092834914846));
#43257=CARTESIAN_POINT('Ctrl Pts',(-5.23317570343027,-4.29427031947518,
-18.0840856783276));
#43258=CARTESIAN_POINT('Ctrl Pts',(-5.11311781951246,-4.43654276249904,
-18.0753364418093));
#43259=CARTESIAN_POINT('Ctrl Pts',(-4.98740458928918,-4.57362924412738,
-18.0665872052909));
#43260=CARTESIAN_POINT('Ctrl Pts',(-4.86169180652402,-4.71071523781617,
-18.0578379999142));
#43261=CARTESIAN_POINT('Ctrl Pts',(-4.73032391141222,-4.84261509584832,
-18.0490887945375));
#43262=CARTESIAN_POINT('Ctrl Pts',(-4.59374706946965,-4.96888084599933,
-18.0403395891608));
#43263=CARTESIAN_POINT('Ctrl Pts',(-4.45717070231158,-5.09514615721047,
-18.0315904141991));
#43264=CARTESIAN_POINT('Ctrl Pts',(-4.31538563497028,-5.21577720520859,
-18.0228412392374));
#43265=CARTESIAN_POINT('Ctrl Pts',(-4.16887340951722,-5.33036429293724,
-18.0140920642757));
#43266=CARTESIAN_POINT('Ctrl Pts',(-4.02236168122208,-5.44495099183909,
-18.0053429190024));
#43267=CARTESIAN_POINT('Ctrl Pts',(-3.87112305262913,-5.55349359498114,
-17.9965937737292));
#43268=CARTESIAN_POINT('Ctrl Pts',(-3.71567116928738,-5.65562346357381,
-17.9878446284559));
#43269=CARTESIAN_POINT('Ctrl Pts',(-3.56021980053049,-5.75775299409089,
-17.9790955121446));
#43270=CARTESIAN_POINT('Ctrl Pts',(-3.40055544441818,-5.85346967520033,
-17.9703463958332));
#43271=CARTESIAN_POINT('Ctrl Pts',(-3.23722035886573,-5.9424484304153,-17.9615972795218));
#43272=CARTESIAN_POINT('Ctrl Pts',(-3.07388580043242,-6.03142689847576,
-17.9528481914458));
#43273=CARTESIAN_POINT('Ctrl Pts',(-2.90688078788998,-6.11366734708007,
-17.9440991033698));
#43274=CARTESIAN_POINT('Ctrl Pts',(-2.73677250610193,-6.18889047001517,
-17.9353500152938));
#43275=CARTESIAN_POINT('Ctrl Pts',(-2.56666475916757,-6.26411335643406,
-17.9266009547267));
#43276=CARTESIAN_POINT('Ctrl Pts',(-2.39345402456937,-6.33231884545314,
-17.9178518941595));
#43277=CARTESIAN_POINT('Ctrl Pts',(-2.21772855943933,-6.39327529804928,
-17.9091028335924));
#43278=CARTESIAN_POINT('Ctrl Pts',(-2.04200363223431,-6.45423156404754,
-17.9003537998076));
#43279=CARTESIAN_POINT('Ctrl Pts',(-1.86376426060846,-6.50793874412508,
-17.8916047660227));
#43280=CARTESIAN_POINT('Ctrl Pts',(-1.68361577621471,-6.55421443943368,
-17.8828557322379));
#43281=CARTESIAN_POINT('Ctrl Pts',(-1.50346782832989,-6.6004899969264,-17.874106724509));
#43282=CARTESIAN_POINT('Ctrl Pts',(-1.32141105657151,-6.63933404265209,
-17.8653577167801));
#43283=CARTESIAN_POINT('Ctrl Pts',(-1.1380637534629,-6.67061465631571,-17.8566087090512));
#43284=CARTESIAN_POINT('Ctrl Pts',(-0.954716981167104,-6.70189517941813,
-17.8478597266518));
#43285=CARTESIAN_POINT('Ctrl Pts',(-0.770079967438926,-6.72561226609044,
-17.8391107442523));
#43286=CARTESIAN_POINT('Ctrl Pts',(-0.58477976406926,-6.74168536996018,
-17.8303617618529));
#43287=CARTESIAN_POINT('Ctrl Pts',(-0.391489587589147,-6.75845153117895,
-17.8212355314372));
#43288=CARTESIAN_POINT('Ctrl Pts',(-0.19747809180143,-6.76689985146405,
-17.8121093010216));
#43289=CARTESIAN_POINT('Ctrl Pts',(-0.0034621475272351,-6.76699911434415,
-17.802983070606));
#43290=CARTESIAN_POINT('Ctrl Pts',(0.184490798488409,-6.76709527525925,
-17.7941420348909));
#43291=CARTESIAN_POINT('Ctrl Pts',(0.372447602158518,-6.75935633790742,
-17.7853009991758));
#43292=CARTESIAN_POINT('Ctrl Pts',(0.559756448197919,-6.74380914014482,
-17.7764599634606));
#43293=CARTESIAN_POINT('Ctrl Pts',(0.745136131047101,-6.72842206873113,
-17.7677099848473));
#43294=CARTESIAN_POINT('Ctrl Pts',(0.929880851948822,-6.70538686355671,
-17.758960006234));
#43295=CARTESIAN_POINT('Ctrl Pts',(1.11336305057844,-6.67478177303249,-17.7502100276207));
#43296=CARTESIAN_POINT('Ctrl Pts',(1.2968433709051,-6.64417699581185,-17.7414601385807));
#43297=CARTESIAN_POINT('Ctrl Pts',(1.47906091205583,-6.60600253547972,-17.7327102495407));
#43298=CARTESIAN_POINT('Ctrl Pts',(1.65939671095619,-6.56038806441111,-17.7239603605008));
#43299=CARTESIAN_POINT('Ctrl Pts',(1.83973072369562,-6.51477404513736,-17.7152105581253));
#43300=CARTESIAN_POINT('Ctrl Pts',(2.01818275357441,-6.46172023288534,-17.7064607557498));
#43301=CARTESIAN_POINT('Ctrl Pts',(2.19414664033734,-6.40140683917968,-17.6977109533743));
#43302=CARTESIAN_POINT('Ctrl Pts',(2.37010884271667,-6.34109402281345,-17.6889612347547));
#43303=CARTESIAN_POINT('Ctrl Pts',(2.54358267848213,-6.27352185699627,-17.6802115161352));
#43304=CARTESIAN_POINT('Ctrl Pts',(2.71397890842147,-6.19891986435084,-17.6714617975156));
#43305=CARTESIAN_POINT('Ctrl Pts',(2.88437356389346,-6.12431856103053,-17.6627121597438));
#43306=CARTESIAN_POINT('Ctrl Pts',(3.05169040787575,-6.04268767582354,-17.653962521972));
#43307=CARTESIAN_POINT('Ctrl Pts',(3.21536112512454,-5.95430447953729,-17.6452128842002));
#43308=CARTESIAN_POINT('Ctrl Pts',(3.37903038443229,-5.8659220705482,-17.6364633243681));
#43309=CARTESIAN_POINT('Ctrl Pts',(3.53905332980346,-5.77078760703148,-17.6277137645361));
#43310=CARTESIAN_POINT('Ctrl Pts',(3.69488643042251,-5.66922422085065,-17.618964204704));
#43311=CARTESIAN_POINT('Ctrl Pts',(3.85071819469098,-5.56766170562912,-17.610214719904));
#43312=CARTESIAN_POINT('Ctrl Pts',(4.00235994599577,-5.45967053455993,-17.601465235104));
#43313=CARTESIAN_POINT('Ctrl Pts',(4.14929662974649,-5.34561750206414,-17.592715750304));
#43314=CARTESIAN_POINT('Ctrl Pts',(4.29623210225383,-5.23156540974187,-17.5839663376287));
#43315=CARTESIAN_POINT('Ctrl Pts',(4.43846235842447,-5.111451731719,-17.5752169249533));
#43316=CARTESIAN_POINT('Ctrl Pts',(4.57550431797748,-4.98568443006268,-17.5664675122779));
#43317=CARTESIAN_POINT('Ctrl Pts',(4.71254519337812,-4.85991812336382,-17.55771816882));
#43318=CARTESIAN_POINT('Ctrl Pts',(4.84439764315299,-4.72849847630778,-17.5489688253621));
#43319=CARTESIAN_POINT('Ctrl Pts',(4.97061384196998,-4.59187184425006,-17.5402194819042));
#43320=CARTESIAN_POINT('Ctrl Pts',(5.09682908420515,-4.45524624767395,-17.5314702047569));
#43321=CARTESIAN_POINT('Ctrl Pts',(5.21740796650475,-4.31341395556525,-17.5227209276095));
#43322=CARTESIAN_POINT('Ctrl Pts',(5.3319409594255,-4.16685668162473,-17.5139716504621));
#43323=CARTESIAN_POINT('Ctrl Pts',(5.44647312235422,-4.02030046974822,-17.5052224367186));
#43324=CARTESIAN_POINT('Ctrl Pts',(5.55495930712568,-3.86901957035145,-17.4964732229751));
#43325=CARTESIAN_POINT('Ctrl Pts',(5.65703106080064,-3.71352778057964,-17.4877240092315));
#43326=CARTESIAN_POINT('Ctrl Pts',(5.75910210868999,-3.55803706597177,-17.4789748559853));
#43327=CARTESIAN_POINT('Ctrl Pts',(5.85475865698805,-3.39833575880459,-17.4702257027391));
#43328=CARTESIAN_POINT('Ctrl Pts',(5.9436758306931,-3.23496624706266,-17.4614765494929));
#43329=CARTESIAN_POINT('Ctrl Pts',(6.03259241910311,-3.0715978106964,-17.4527274538378));
#43330=CARTESIAN_POINT('Ctrl Pts',(6.11476958471188,-2.9045614697537,-17.4439783581827));
#43331=CARTESIAN_POINT('Ctrl Pts',(6.18992823574592,-2.7344245164779,-17.4352292625276));
#43332=CARTESIAN_POINT('Ctrl Pts',(6.26508641701131,-2.56428862661937,-17.4264802215574));
#43333=CARTESIAN_POINT('Ctrl Pts',(6.33322605570482,-2.39105242530786,-17.4177311805873));
#43334=CARTESIAN_POINT('Ctrl Pts',(6.39411573747941,-2.21530425353227,-17.4089821396172));
#43335=CARTESIAN_POINT('Ctrl Pts',(6.45500505889285,-2.03955712188055,-17.4002331504262));
#43336=CARTESIAN_POINT('Ctrl Pts',(6.50864441545075,-1.86129832025062,-17.3914841612352));
#43337=CARTESIAN_POINT('Ctrl Pts',(6.55485164050038,-1.68113324011795,-17.3827351720442));
#43338=CARTESIAN_POINT('Ctrl Pts',(6.60199852639227,-1.49730435912381,-17.3738082651673));
#43339=CARTESIAN_POINT('Ctrl Pts',(6.64140767441113,-1.31149113173131,-17.3648813582904));
#43340=CARTESIAN_POINT('Ctrl Pts',(6.6729397526969,-1.12435050445909,-17.3559544514136));
#43341=CARTESIAN_POINT('Ctrl Pts',(6.7038466483158,-0.940920291558521,-17.3472045372296));
#43342=CARTESIAN_POINT('Ctrl Pts',(6.72718585889724,-0.756215114272718,
-17.3384546230456));
#43343=CARTESIAN_POINT('Ctrl Pts',(6.74287810451908,-0.570862389369925,
-17.3297047088616));
#43344=CARTESIAN_POINT('Ctrl Pts',(6.75857004154153,-0.385513309562867,
-17.320954966751));
#43345=CARTESIAN_POINT('Ctrl Pts',(6.76661529035571,-0.199516993253964,
-17.3122052246404));
#43346=CARTESIAN_POINT('Ctrl Pts',(6.76698652348897,-0.0135052181998018,
-17.3034554825298));
#43347=CARTESIAN_POINT('Ctrl Pts',(6.7673577498151,0.172503146043099,-17.2947059008592));
#43348=CARTESIAN_POINT('Ctrl Pts',(6.76005524147457,0.358526681837624,-17.2859563191885));
#43349=CARTESIAN_POINT('Ctrl Pts',(6.74510380214848,0.543933542118961,-17.2772067375179));
#43350=CARTESIAN_POINT('Ctrl Pts',(6.73015261710935,0.7293372490888,-17.268457304656));
#43351=CARTESIAN_POINT('Ctrl Pts',(6.7075527844455,0.914124015858719,-17.2597078717941));
#43352=CARTESIAN_POINT('Ctrl Pts',(6.67738106408223,1.09766621749789,-17.2509584389321));
#43353=CARTESIAN_POINT('Ctrl Pts',(6.64720981677177,1.28120554143722,-17.2422091432498));
#43354=CARTESIAN_POINT('Ctrl Pts',(6.60946696581435,1.46350005651017,-17.2334598475674));
#43355=CARTESIAN_POINT('Ctrl Pts',(6.56428070010896,1.64393062206928,-17.2247105518851));
#43356=CARTESIAN_POINT('Ctrl Pts',(6.51909508282631,1.82435859845046,-17.2159613817551));
#43357=CARTESIAN_POINT('Ctrl Pts',(6.4664663341554,2.00292240086956,-17.2072122116251));
#43358=CARTESIAN_POINT('Ctrl Pts',(6.40657319597059,2.17901557696845,-17.1984630414951));
#43359=CARTESIAN_POINT('Ctrl Pts',(6.34668083768153,2.35510646007816,-17.189713985292));
#43360=CARTESIAN_POINT('Ctrl Pts',(6.27952437143735,2.52872650996903,-17.180964929089));
#43361=CARTESIAN_POINT('Ctrl Pts',(6.20533187334978,2.69928607998288,-17.1722158728859));
#43362=CARTESIAN_POINT('Ctrl Pts',(6.1283144978409,2.87633970115742,-17.1631336965971));
#43363=CARTESIAN_POINT('Ctrl Pts',(6.04371489462988,3.05009490562676,-17.1540515203082));
#43364=CARTESIAN_POINT('Ctrl Pts',(5.95184265120324,3.2199158459994,-17.1449693440194));
#43365=CARTESIAN_POINT('Ctrl Pts',(5.86333281335316,3.38352155905606,-17.136219563665));
#43366=CARTESIAN_POINT('Ctrl Pts',(5.76807337235499,3.54347560904126,-17.1274697833105));
#43367=CARTESIAN_POINT('Ctrl Pts',(5.66638790086161,3.69923467178945,-17.1187200029561));
#43368=CARTESIAN_POINT('Ctrl Pts',(5.56470608502536,3.85498813490062,-17.1099705371619));
#43369=CARTESIAN_POINT('Ctrl Pts',(5.45659885766734,4.00654667256559,-17.1012210713676));
#43370=CARTESIAN_POINT('Ctrl Pts',(5.34243340580277,4.15339551506507,-17.0924716055733));
#43371=CARTESIAN_POINT('Ctrl Pts',(5.22827145140352,4.30023985884164,-17.0837224078194));
#43372=CARTESIAN_POINT('Ctrl Pts',(5.10805181977837,4.44237456993333,-17.0749732100656));
#43373=CARTESIAN_POINT('Ctrl Pts',(4.98218281282288,4.57931691626735,-17.0662240123117));
#43374=CARTESIAN_POINT('Ctrl Pts',(4.85631699295956,4.71625579512443,-17.0574750360937));
#43375=CARTESIAN_POINT('Ctrl Pts',(4.72480227791555,4.84800236136045,-17.0487260598757));
#43376=CARTESIAN_POINT('Ctrl Pts',(4.58808530847821,4.97410918679179,-17.0399770836577));
#43377=CARTESIAN_POINT('Ctrl Pts',(4.45135945056669,5.10022421089272,-17.0312275386365));
#43378=CARTESIAN_POINT('Ctrl Pts',(4.3094308720773,5.22069856612243,-17.0224779936153));
#43379=CARTESIAN_POINT('Ctrl Pts',(4.16278164322149,5.33512305301932,-17.0137284485941));
#43380=CARTESIAN_POINT('Ctrl Pts',(4.0161410353407,5.44954081331663,-17.0049794179268));
#43381=CARTESIAN_POINT('Ctrl Pts',(3.86478055833092,5.55790924068561,-16.9962303872596));
#43382=CARTESIAN_POINT('Ctrl Pts',(3.7092142581163,5.65986029751501,-16.9874813565923));
#43383=CARTESIAN_POINT('Ctrl Pts',(3.55364584529801,5.7618127388485,-16.9787322071125));
#43384=CARTESIAN_POINT('Ctrl Pts',(3.39387173464027,5.85734747818247,-16.9699830576326));
#43385=CARTESIAN_POINT('Ctrl Pts',(3.23043456092091,5.94614005448978,-16.9612339081528));
#43386=CARTESIAN_POINT('Ctrl Pts',(3.18690768806183,5.96978744811392,-16.9589038194198));
#43387=CARTESIAN_POINT('Ctrl Pts',(3.14312114982779,5.99295688499353,-16.9565737306868));
#43388=CARTESIAN_POINT('Ctrl Pts',(3.09908550384726,6.0156427786101,-16.9542436419538));
#43389=CARTESIAN_POINT('Ctrl Pts',(3.09908550384715,6.01564277861015,-18.9542023328983));
#43390=CARTESIAN_POINT('Ctrl Pts',(2.93955287157862,6.09782938546984,-18.9457755290877));
#43391=CARTESIAN_POINT('Ctrl Pts',(2.77669907250746,6.17369168653797,-18.937348725277));
#43392=CARTESIAN_POINT('Ctrl Pts',(2.61105431770974,6.24297079521996,-18.9289219214663));
#43393=CARTESIAN_POINT('Ctrl Pts',(2.45830155335587,6.30685796977052,-18.9211509686323));
#43394=CARTESIAN_POINT('Ctrl Pts',(2.30317581700008,6.36514720210411,-18.9133800157982));
#43395=CARTESIAN_POINT('Ctrl Pts',(2.14610905555137,6.41767130053265,-18.9056090629641));
#43396=CARTESIAN_POINT('Ctrl Pts',(1.97190176805378,6.47592729709804,-18.8969900744397));
#43397=CARTESIAN_POINT('Ctrl Pts',(1.79538450031526,6.52706470421298,-18.8883710859152));
#43398=CARTESIAN_POINT('Ctrl Pts',(1.61715397565048,6.5709285507482,-18.8797520973908));
#43399=CARTESIAN_POINT('Ctrl Pts',(1.43881667499724,6.61481867564163,-18.8711279453231));
#43400=CARTESIAN_POINT('Ctrl Pts',(1.25876436438882,6.65142647100605,-18.8625037932554));
#43401=CARTESIAN_POINT('Ctrl Pts',(1.07760441734818,6.68064800148247,-18.8538796411878));
#43402=CARTESIAN_POINT('Ctrl Pts',(0.89023969338103,6.71087037723964,-18.8449601095915));
#43403=CARTESIAN_POINT('Ctrl Pts',(0.701690470581387,6.73319151794819,-18.8360405779952));
#43404=CARTESIAN_POINT('Ctrl Pts',(0.512634310865934,6.74755474696745,-18.8271210463989));
#43405=CARTESIAN_POINT('Ctrl Pts',(0.329498415226465,6.76146819371617,-18.8184808285397));
#43406=CARTESIAN_POINT('Ctrl Pts',(0.145887157616835,6.76791462308545,-18.8098406106805));
#43407=CARTESIAN_POINT('Ctrl Pts',(-0.0375831936387921,6.76689563267795,
-18.8012003928213));
#43408=CARTESIAN_POINT('Ctrl Pts',(-0.229950159010604,6.7658272306659,-18.7921412043565));
#43409=CARTESIAN_POINT('Ctrl Pts',(-0.422161825523465,6.75655142030718,
-18.7830820158916));
#43410=CARTESIAN_POINT('Ctrl Pts',(-0.613512922072761,6.73913131601171,
-18.7740228274268));
#43411=CARTESIAN_POINT('Ctrl Pts',(-0.804864018621992,6.72171121171625,
-18.764963638962));
#43412=CARTESIAN_POINT('Ctrl Pts',(-0.995354170387055,6.69614689720996,
-18.7559044504972));
#43413=CARTESIAN_POINT('Ctrl Pts',(-1.18428889692815,6.66256323111554,-18.7468452620324));
#43414=CARTESIAN_POINT('Ctrl Pts',(-1.37289630730937,6.62903774636671,-18.7378017679761));
#43415=CARTESIAN_POINT('Ctrl Pts',(-1.56012757976248,6.58749062086662,-18.7287582739198));
#43416=CARTESIAN_POINT('Ctrl Pts',(-1.74532380658997,6.53805275369894,-18.7197147798635));
#43417=CARTESIAN_POINT('Ctrl Pts',(-1.93035063510609,6.48866010716755,-18.7106795578582));
#43418=CARTESIAN_POINT('Ctrl Pts',(-2.11334590455118,6.4313911903526,-18.7016443358528));
#43419=CARTESIAN_POINT('Ctrl Pts',(-2.29366304647345,6.36642747773366,-18.6926091138475));
#43420=CARTESIAN_POINT('Ctrl Pts',(-2.47366250884614,6.30157821703395,-18.6835898099363));
#43421=CARTESIAN_POINT('Ctrl Pts',(-2.65099304180712,6.22906131187865,-18.6745705060252));
#43422=CARTESIAN_POINT('Ctrl Pts',(-2.82502546611859,6.14910726169104,-18.6655512021141));
#43423=CARTESIAN_POINT('Ctrl Pts',(-2.99883955459871,6.06925351944366,-18.6565432135496));
#43424=CARTESIAN_POINT('Ctrl Pts',(-3.16936357616707,5.98198135157004,-18.6475352249852));
#43425=CARTESIAN_POINT('Ctrl Pts',(-3.33598810726092,5.88756930729599,-18.6385272364208));
#43426=CARTESIAN_POINT('Ctrl Pts',(-3.50223631101512,5.79337049593079,-18.6295395927141));
#43427=CARTESIAN_POINT('Ctrl Pts',(-3.66460239738049,5.69206411361652,-18.6205519490073));
#43428=CARTESIAN_POINT('Ctrl Pts',(-3.82250174688802,5.58397433688928,-18.6115643053006));
#43429=CARTESIAN_POINT('Ctrl Pts',(-3.96002113627314,5.4898356330842,-18.6037366905674));
#43430=CARTESIAN_POINT('Ctrl Pts',(-4.09415263965759,5.39055234715943,-18.5959090758343));
#43431=CARTESIAN_POINT('Ctrl Pts',(-4.22452484614403,5.28636726158065,-18.5880814611011));
#43432=CARTESIAN_POINT('Ctrl Pts',(-4.35981945711452,5.17824850680777,-18.5799583026558));
#43433=CARTESIAN_POINT('Ctrl Pts',(-4.49100401349823,5.064897837526,-18.5718351442105));
#43434=CARTESIAN_POINT('Ctrl Pts',(-4.61765506804729,4.94667066546149,-18.5637119857652));
#43435=CARTESIAN_POINT('Ctrl Pts',(-4.74429719303384,4.82845182903166,-18.5555894000452));
#43436=CARTESIAN_POINT('Ctrl Pts',(-4.86640618530508,4.70535742444016,-18.5474668143251));
#43437=CARTESIAN_POINT('Ctrl Pts',(-4.983593904042,4.57778120923177,-18.539344228605));
#43438=CARTESIAN_POINT('Ctrl Pts',(-5.10079570409027,4.45018966442718,-18.5312206668726));
#43439=CARTESIAN_POINT('Ctrl Pts',(-5.21307480638164,4.31811550702032,-18.5230971051402));
#43440=CARTESIAN_POINT('Ctrl Pts',(-5.320081999144,4.18198714995443,-18.5149735434078));
#43441=CARTESIAN_POINT('Ctrl Pts',(-5.42716713394764,4.04575963953491,-18.5068440646247));
#43442=CARTESIAN_POINT('Ctrl Pts',(-5.52897246337977,3.90547231958631,-18.4987145858416));
#43443=CARTESIAN_POINT('Ctrl Pts',(-5.62519055643087,3.76158479950153,-18.4905851070585));
#43444=CARTESIAN_POINT('Ctrl Pts',(-5.72144787590491,3.61763861900748,-18.48245231403));
#43445=CARTESIAN_POINT('Ctrl Pts',(-5.81211322713935,3.47008962437107,-18.4743195210015));
#43446=CARTESIAN_POINT('Ctrl Pts',(-5.8969242809301,3.31942359830394,-18.466186727973));
#43447=CARTESIAN_POINT('Ctrl Pts',(-5.98182755387526,3.16859374579081,-18.4580450917659));
#43448=CARTESIAN_POINT('Ctrl Pts',(-6.06086364816737,3.01464041755744,-18.4499034555588));
#43449=CARTESIAN_POINT('Ctrl Pts',(-6.13381734516322,2.8580716884247,-18.4417618193516));
#43450=CARTESIAN_POINT('Ctrl Pts',(-6.17098626286205,2.77830204758421,-18.4376137662909));
#43451=CARTESIAN_POINT('Ctrl Pts',(-6.20657711544618,2.6978538103809,-18.4334657132302));
#43452=CARTESIAN_POINT('Ctrl Pts',(-6.240566382091,2.61679579461518,-18.4293176601694));
#43453=CARTESIAN_POINT('Ctrl Pts',(-6.31738329510644,2.43360188780494,-18.4199429174167));
#43454=CARTESIAN_POINT('Ctrl Pts',(-6.38614096433329,2.24699678707267,-18.4105681746639));
#43455=CARTESIAN_POINT('Ctrl Pts',(-6.44657563827959,2.05765680810483,-18.4011934319112));
#43456=CARTESIAN_POINT('Ctrl Pts',(-6.50687594802183,1.8687377880652,-18.3918395319919));
#43457=CARTESIAN_POINT('Ctrl Pts',(-6.55889016789018,1.67709619195425,-18.3824856320727));
#43458=CARTESIAN_POINT('Ctrl Pts',(-6.60240453971986,1.48342283044539,-18.3731317321535));
#43459=CARTESIAN_POINT('Ctrl Pts',(-6.64583505185042,1.29012271090559,-18.3637958588126));
#43460=CARTESIAN_POINT('Ctrl Pts',(-6.68079837636695,1.0947988041738,-18.3544599854717));
#43461=CARTESIAN_POINT('Ctrl Pts',(-6.70713108362105,0.898154567501827,
-18.3451241121308));
#43462=CARTESIAN_POINT('Ctrl Pts',(-6.73336361908543,0.702258381720841,
-18.3358237532219));
#43463=CARTESIAN_POINT('Ctrl Pts',(-6.75103101770111,0.505052053478654,
-18.326523394313));
#43464=CARTESIAN_POINT('Ctrl Pts',(-6.7600214043759,0.307245199115813,-18.3172230354042));
#43465=CARTESIAN_POINT('Ctrl Pts',(-6.76466233329813,0.205135291651743,
-18.3124220956661));
#43466=CARTESIAN_POINT('Ctrl Pts',(-6.76699188960486,0.102865576435023,
-18.307621155928));
#43467=CARTESIAN_POINT('Ctrl Pts',(-6.76699997885676,0.000534932305956201,
-18.30282021619));
#43468=CARTESIAN_POINT('',(-6.76699999116254,0.000345841369350949,-18.697179783767));
#43469=CARTESIAN_POINT('Ctrl Pts',(3.09908550384723,6.01564277861011,-19.3485039941327));
#43470=CARTESIAN_POINT('Ctrl Pts',(2.94440847816585,6.09532791712462,-19.3402830032412));
#43471=CARTESIAN_POINT('Ctrl Pts',(2.78646210386894,6.16914348376745,-19.3320620123498));
#43472=CARTESIAN_POINT('Ctrl Pts',(2.62573141136858,6.23681197049842,-19.3238410214583));
#43473=CARTESIAN_POINT('Ctrl Pts',(2.46516006366625,6.30441337221169,-19.3156281806726));
#43474=CARTESIAN_POINT('Ctrl Pts',(2.30181022276318,6.3658796917601,-19.3074153398868));
#43475=CARTESIAN_POINT('Ctrl Pts',(2.1361914294365,6.42097930044959,-19.2992024991011));
#43476=CARTESIAN_POINT('Ctrl Pts',(1.97070361066912,6.47603533529808,-19.2909961531894));
#43477=CARTESIAN_POINT('Ctrl Pts',(1.80295075182054,6.5247345746493,-19.2827898072777));
#43478=CARTESIAN_POINT('Ctrl Pts',(1.63346236967899,6.56689345785682,-19.2745834613659));
#43479=CARTESIAN_POINT('Ctrl Pts',(1.4640740386589,6.60902745414589,-19.2663819597633));
#43480=CARTESIAN_POINT('Ctrl Pts',(1.29295257209241,6.64462869882177,-19.2581804581607));
#43481=CARTESIAN_POINT('Ctrl Pts',(1.12064273434524,6.67356343057884,-19.2499789565581));
#43482=CARTESIAN_POINT('Ctrl Pts',(0.94840007031874,6.70248688234392,-19.2417806522505));
#43483=CARTESIAN_POINT('Ctrl Pts',(0.774970311197606,6.72474893997004,-19.2335823479428));
#43484=CARTESIAN_POINT('Ctrl Pts',(0.600908592751125,6.74026689851061,-19.2253840436352));
#43485=CARTESIAN_POINT('Ctrl Pts',(0.426847945465729,6.75578476155499,-19.2171857897792));
#43486=CARTESIAN_POINT('Ctrl Pts',(0.252155702755887,6.76455856672819,-19.2089875359233));
#43487=CARTESIAN_POINT('Ctrl Pts',(0.0773927041020941,6.76655742378292,
-19.2007892820673));
#43488=CARTESIAN_POINT('Ctrl Pts',(-0.0973787949803039,6.76855637806157,
-19.1925906294503));
#43489=CARTESIAN_POINT('Ctrl Pts',(-0.2722206981662,6.763779722904,-19.1843919768333));
#43490=CARTESIAN_POINT('Ctrl Pts',(-0.446571735709607,6.75224871319661,
-19.1761933242164));
#43491=CARTESIAN_POINT('Ctrl Pts',(-0.620962925836858,6.74071504792813,
-19.1679927834713));
#43492=CARTESIAN_POINT('Ctrl Pts',(-0.794862667244472,6.72242395300531,
-19.1597922427263));
#43493=CARTESIAN_POINT('Ctrl Pts',(-0.967714327126197,6.69744861727768,
-19.1515917019812));
#43494=CARTESIAN_POINT('Ctrl Pts',(-1.14063719453846,6.67246299277421,-19.1433877829622));
#43495=CARTESIAN_POINT('Ctrl Pts',(-1.31251076567566,6.64078769346307,-19.1351838639433));
#43496=CARTESIAN_POINT('Ctrl Pts',(-1.48278806505245,6.60254712623379,-19.1269799449243));
#43497=CARTESIAN_POINT('Ctrl Pts',(-1.65326209435543,6.56426237775429,-19.1187665475052));
#43498=CARTESIAN_POINT('Ctrl Pts',(-1.82213581810475,6.5193972894121,-19.110553150086));
#43499=CARTESIAN_POINT('Ctrl Pts',(-1.98887594887905,6.46812658039177,-19.1023397526669));
#43500=CARTESIAN_POINT('Ctrl Pts',(-2.15572319202591,6.41682293552533,-19.0941210790345));
#43501=CARTESIAN_POINT('Ctrl Pts',(-2.32043377276798,6.3591055865086,-19.0859024054021));
#43502=CARTESIAN_POINT('Ctrl Pts',(-2.48249400881984,6.29519757403798,-19.0776837317698));
#43503=CARTESIAN_POINT('Ctrl Pts',(-2.64478933304299,6.23119685518762,-19.0694531359472));
#43504=CARTESIAN_POINT('Ctrl Pts',(-2.8044263051849,6.16098767801956,-19.0612225401246));
#43505=CARTESIAN_POINT('Ctrl Pts',(-2.96091450546015,6.08483970958609,-19.0529919443021));
#43506=CARTESIAN_POINT('Ctrl Pts',(-3.0499750354599,6.041502394599,-19.0483077494243));
#43507=CARTESIAN_POINT('Ctrl Pts',(-3.13801617845152,5.99624234036059,-19.0436235545464));
#43508=CARTESIAN_POINT('Ctrl Pts',(-3.22495178421901,5.94911547958708,-19.0389393596686));
#43509=CARTESIAN_POINT('Ctrl Pts',(-3.37474187771986,5.86791587420853,-19.0308684894822));
#43510=CARTESIAN_POINT('Ctrl Pts',(-3.52173671608847,5.78090699168158,-19.0227976192958));
#43511=CARTESIAN_POINT('Ctrl Pts',(-3.66544193120517,5.68830593841109,-19.0147267491094));
#43512=CARTESIAN_POINT('Ctrl Pts',(-3.80896831635165,5.59582011995366,-19.0066659224936));
#43513=CARTESIAN_POINT('Ctrl Pts',(-3.94921291406009,5.49775617698324,-18.9986050958778));
#43514=CARTESIAN_POINT('Ctrl Pts',(-4.08570333956989,5.39437829791604,-18.990544269262));
#43515=CARTESIAN_POINT('Ctrl Pts',(-4.22205384362153,5.2911063953928,-18.9824917061021));
#43516=CARTESIAN_POINT('Ctrl Pts',(-4.35465753938026,5.18253162084947,-18.9744391429422));
#43517=CARTESIAN_POINT('Ctrl Pts',(-4.48306867116872,5.06896284160631,-18.9663865797824));
#43518=CARTESIAN_POINT('Ctrl Pts',(-4.61137628116239,4.95548561863009,-18.9583405083945));
#43519=CARTESIAN_POINT('Ctrl Pts',(-4.73549777645621,4.83702265004525,-18.9502944370066));
#43520=CARTESIAN_POINT('Ctrl Pts',(-4.85501840760994,4.7139246135008,-18.9422483656187));
#43521=CARTESIAN_POINT('Ctrl Pts',(-4.97446882804233,4.5908988891744,-18.9342070207828));
#43522=CARTESIAN_POINT('Ctrl Pts',(-5.08932350550706,4.46324378417688,-18.9261656759469));
#43523=CARTESIAN_POINT('Ctrl Pts',(-5.19920275818625,4.3313484827786,-18.9181243311111));
#43524=CARTESIAN_POINT('Ctrl Pts',(-5.31120014475798,4.19691064581199,-18.90992797389));
#43525=CARTESIAN_POINT('Ctrl Pts',(-5.41802803229019,4.05806773256378,-18.9017316166689));
#43526=CARTESIAN_POINT('Ctrl Pts',(-5.51932543404989,3.91526956326764,-18.8935352594479));
#43527=CARTESIAN_POINT('Ctrl Pts',(-5.6186754730372,3.77521657631599,-18.8854964707394));
#43528=CARTESIAN_POINT('Ctrl Pts',(-5.71270553000589,3.63135935539557,-18.8774576820309));
#43529=CARTESIAN_POINT('Ctrl Pts',(-5.80111744591931,3.48415346657559,-18.8694188933224));
#43530=CARTESIAN_POINT('Ctrl Pts',(-5.88953882270863,3.336931825392,-18.8613792443907));
#43531=CARTESIAN_POINT('Ctrl Pts',(-5.97234066898833,3.18636112293837,-18.8533395954589));
#43532=CARTESIAN_POINT('Ctrl Pts',(-6.04926982971491,3.03292326432782,-18.8452999465272));
#43533=CARTESIAN_POINT('Ctrl Pts',(-6.12622245482632,2.8794386051942,-18.837257845399));
#43534=CARTESIAN_POINT('Ctrl Pts',(-6.19729866162558,2.72308538284473,-18.8292157442708));
#43535=CARTESIAN_POINT('Ctrl Pts',(-6.26229271905741,2.56436715406366,-18.8211736431427));
#43536=CARTESIAN_POINT('Ctrl Pts',(-6.32948007057329,2.40029280864714,-18.8128601526979));
#43537=CARTESIAN_POINT('Ctrl Pts',(-6.39016742727578,2.23369144887705,-18.8045466622531));
#43538=CARTESIAN_POINT('Ctrl Pts',(-6.44418321522352,2.06513720818533,-18.7962331718084));
#43539=CARTESIAN_POINT('Ctrl Pts',(-6.49652773598207,1.90179809408472,-18.7881769036376));
#43540=CARTESIAN_POINT('Ctrl Pts',(-6.54260735312553,1.73662551931482,-18.7801206354669));
#43541=CARTESIAN_POINT('Ctrl Pts',(-6.58231797049406,1.5701525834488,-18.7720643672961));
#43542=CARTESIAN_POINT('Ctrl Pts',(-6.62393042164316,1.3957068716866,-18.7636222657143));
#43543=CARTESIAN_POINT('Ctrl Pts',(-6.65854872492751,1.21983365843838,-18.7551801641326));
#43544=CARTESIAN_POINT('Ctrl Pts',(-6.68611419154111,1.04315196288582,-18.7467380625508));
#43545=CARTESIAN_POINT('Ctrl Pts',(-6.71367965815473,0.86647026733319,-18.738295960969));
#43546=CARTESIAN_POINT('Ctrl Pts',(-6.73419232108136,0.688980557231193,
-18.7298538593873));
#43547=CARTESIAN_POINT('Ctrl Pts',(-6.74765593860622,0.511300629954842,
-18.7214117578055));
#43548=CARTESIAN_POINT('Ctrl Pts',(-6.76053780325359,0.341298119893798,
-18.7133344331403));
#43549=CARTESIAN_POINT('Ctrl Pts',(-6.76699127607909,0.17087146288988,-18.7052571084752));
#43550=CARTESIAN_POINT('Ctrl Pts',(-6.76699999116249,0.00034584227915461,
-18.6971797838101));
#43551=CARTESIAN_POINT('Ctrl Pts',(-6.76699999116254,0.000345841369450119,
-18.697179783767));
#43552=CARTESIAN_POINT('Ctrl Pts',(-6.76700886075812,-0.173203532875599,
-18.6889592322969));
#43553=CARTESIAN_POINT('Ctrl Pts',(-6.76033706239097,-0.347008637377228,
-18.6807386808267));
#43554=CARTESIAN_POINT('Ctrl Pts',(-6.74695149338562,-0.520513732673331,
-18.6725181293566));
#43555=CARTESIAN_POINT('Ctrl Pts',(-6.73358181676881,-0.693812829226717,
-18.6643073379645));
#43556=CARTESIAN_POINT('Ctrl Pts',(-6.71351426905476,-0.866812270721374,
-18.6560965465724));
#43557=CARTESIAN_POINT('Ctrl Pts',(-6.68676770786251,-1.03895458085862,
-18.6478857551803));
#43558=CARTESIAN_POINT('Ctrl Pts',(-6.6600474945024,-1.21092731492747,-18.6396830521757));
#43559=CARTESIAN_POINT('Ctrl Pts',(-6.62666142542678,-1.38204424617926,
-18.6314803491712));
#43560=CARTESIAN_POINT('Ctrl Pts',(-6.58668028507848,-1.55175121142484,
-18.6232776461667));
#43561=CARTESIAN_POINT('Ctrl Pts',(-6.54673044924656,-1.72132529915803,
-18.6150813657316));
#43562=CARTESIAN_POINT('Ctrl Pts',(-6.50019590959801,-1.88949127127693,
-18.6068850852965));
#43563=CARTESIAN_POINT('Ctrl Pts',(-6.44719884464295,-2.05570330000092,
-18.5986888048614));
#43564=CARTESIAN_POINT('Ctrl Pts',(-6.39423269145756,-2.22181838169672,
-18.5904973050973));
#43565=CARTESIAN_POINT('Ctrl Pts',(-6.33481163146196,-2.38598144875708,
-18.5823058053333));
#43566=CARTESIAN_POINT('Ctrl Pts',(-6.26910820932196,-2.54765995764978,
-18.5741143055692));
#43567=CARTESIAN_POINT('Ctrl Pts',(-6.20342535141963,-2.70928786346617,
-18.5659253696282));
#43568=CARTESIAN_POINT('Ctrl Pts',(-6.13146418170005,-2.86843242670336,
-18.5577364336872));
#43569=CARTESIAN_POINT('Ctrl Pts',(-6.05344614695941,-3.02457910226569,
-18.5495474977462));
#43570=CARTESIAN_POINT('Ctrl Pts',(-5.97543825004887,-3.18070548779542,
-18.541359625893));
#43571=CARTESIAN_POINT('Ctrl Pts',(-5.89137521634352,-3.33383443989974,
-18.5331717540398));
#43572=CARTESIAN_POINT('Ctrl Pts',(-5.80152542174885,-3.4834740964735,-18.5249838821867));
#43573=CARTESIAN_POINT('Ctrl Pts',(-5.71167085621008,-3.63312169877981,
-18.5167955755648));
#43574=CARTESIAN_POINT('Ctrl Pts',(-5.61602910355558,-3.77927932862279,
-18.5086072689429));
#43575=CARTESIAN_POINT('Ctrl Pts',(-5.51491303654802,-3.92148227068703,
-18.500418962321));
#43576=CARTESIAN_POINT('Ctrl Pts',(-5.41372845284464,-4.06378157009599,
-18.4922251072662));
#43577=CARTESIAN_POINT('Ctrl Pts',(-5.30706235095607,-4.2021205333795,-18.4840312522114));
#43578=CARTESIAN_POINT('Ctrl Pts',(-5.19526971211486,-4.33606522303136,
-18.4758373971566));
#43579=CARTESIAN_POINT('Ctrl Pts',(-5.08343967464097,-4.4700547219685,-18.4676408009645));
#43580=CARTESIAN_POINT('Ctrl Pts',(-4.96647992018391,-4.59964674775006,
-18.4594442047724));
#43581=CARTESIAN_POINT('Ctrl Pts',(-4.84478375289696,-4.72444275948664,
-18.4512476085802));
#43582=CARTESIAN_POINT('Ctrl Pts',(-4.72294827922223,-4.84938162602292,
-18.4430416296916));
#43583=CARTESIAN_POINT('Ctrl Pts',(-4.59636581679491,-4.96951325720256,
-18.4348356508029));
#43584=CARTESIAN_POINT('Ctrl Pts',(-4.4654651359907,-5.08447736933222,-18.4266296719143));
#43585=CARTESIAN_POINT('Ctrl Pts',(-4.34452065691637,-5.19069740247753,
-18.419047833257));
#43586=CARTESIAN_POINT('Ctrl Pts',(-4.21989040011406,-5.29250639405488,
-18.4114659945997));
#43587=CARTESIAN_POINT('Ctrl Pts',(-4.09193520383977,-5.38965261288488,
-18.4038841559424));
#43588=CARTESIAN_POINT('Ctrl Pts',(-3.94931117518839,-5.49793571119752,
-18.3954331324173));
#43589=CARTESIAN_POINT('Ctrl Pts',(-3.80226569196563,-5.60064567797856,
-18.3869821088921));
#43590=CARTESIAN_POINT('Ctrl Pts',(-3.65126116601532,-5.69741879253653,
-18.3785310853669));
#43591=CARTESIAN_POINT('Ctrl Pts',(-3.50038959506147,-5.79410670124375,
-18.3700875027167));
#43592=CARTESIAN_POINT('Ctrl Pts',(-3.34556620707401,-5.88486799854257,
-18.3616439200665));
#43593=CARTESIAN_POINT('Ctrl Pts',(-3.18728424791836,-5.96938088271904,
-18.3532003374163));
#43594=CARTESIAN_POINT('Ctrl Pts',(-3.02912013461292,-6.05383084442005,
-18.3447630412765));
#43595=CARTESIAN_POINT('Ctrl Pts',(-2.86750287476671,-6.13204151119479,
-18.3363257451367));
#43596=CARTESIAN_POINT('Ctrl Pts',(-2.70295263390817,-6.20373565352755,
-18.3278884489969));
#43597=CARTESIAN_POINT('Ctrl Pts',(-2.53851978709984,-6.27537864755629,
-18.3194571722245));
#43598=CARTESIAN_POINT('Ctrl Pts',(-2.37115843619585,-6.3405142583537,-18.3110258954521));
#43599=CARTESIAN_POINT('Ctrl Pts',(-2.20141135110492,-6.39891217811484,
-18.3025946186798));
#43600=CARTESIAN_POINT('Ctrl Pts',(-2.03173702575806,-6.45728506641407,
-18.2941669558578));
#43601=CARTESIAN_POINT('Ctrl Pts',(-1.85967931772671,-6.50892591343173,
-18.2857392930358));
#43602=CARTESIAN_POINT('Ctrl Pts',(-1.68579950411636,-6.55365310585791,
-18.2773116302138));
#43603=CARTESIAN_POINT('Ctrl Pts',(-1.51197321759026,-6.59836652948513,
-18.2688865617598));
#43604=CARTESIAN_POINT('Ctrl Pts',(-1.3363262647527,-6.63617046040107,-18.2604614933057));
#43605=CARTESIAN_POINT('Ctrl Pts',(-1.15943391848391,-6.66693347714443,
-18.2520364248517));
#43606=CARTESIAN_POINT('Ctrl Pts',(-1.11103075801335,-6.67535118015643,
-18.2497310682382));
#43607=CARTESIAN_POINT('Ctrl Pts',(-1.06253441866942,-6.68324199690499,
-18.2474257116246));
#43608=CARTESIAN_POINT('Ctrl Pts',(-1.01395682684652,-6.69060390049294,
-18.2451203550111));
#43609=CARTESIAN_POINT('Ctrl Pts',(-0.832340800932257,-6.71812769536696,
-18.2365013664866));
#43610=CARTESIAN_POINT('Ctrl Pts',(-0.649669552838091,-6.73824225069642,
-18.2278823779622));
#43611=CARTESIAN_POINT('Ctrl Pts',(-0.466557540377591,-6.75089720418826,
-18.2192633894377));
#43612=CARTESIAN_POINT('Ctrl Pts',(-0.283335827480763,-6.76355973912656,
-18.21063923737));
#43613=CARTESIAN_POINT('Ctrl Pts',(-0.0996731266688622,-6.76875373256227,
-18.2020150853023));
#43614=CARTESIAN_POINT('Ctrl Pts',(0.0838143623222932,-6.76648092827199,
-18.1933909332346));
#43615=CARTESIAN_POINT('Ctrl Pts',(0.273586347176263,-6.76413027982329,
-18.1844714016383));
#43616=CARTESIAN_POINT('Ctrl Pts',(0.463170547829503,-6.75379231080564,
-18.175551870042));
#43617=CARTESIAN_POINT('Ctrl Pts',(0.651889718517968,-6.73552735833584,
-18.1666323384458));
#43618=CARTESIAN_POINT('Ctrl Pts',(0.834699177889882,-6.7178343699962,-18.1579921205865));
#43619=CARTESIAN_POINT('Ctrl Pts',(1.01669666844332,-6.69270343676662,-18.1493519027273));
#43620=CARTESIAN_POINT('Ctrl Pts',(1.19727532199404,-6.66024179766351,-18.1407116848681));
#43621=CARTESIAN_POINT('Ctrl Pts',(1.38661036908222,-6.62620606947917,-18.1316524964033));
#43622=CARTESIAN_POINT('Ctrl Pts',(1.57438517879334,-6.58411110256957,-18.1225933079385));
#43623=CARTESIAN_POINT('Ctrl Pts',(1.75991574583252,-6.53414000214036,-18.1135341194737));
#43624=CARTESIAN_POINT('Ctrl Pts',(1.9454463128717,-6.48416890171115,-18.1044749310089));
#43625=CARTESIAN_POINT('Ctrl Pts',(2.1287322823246,-6.42632181451492,-18.0954157425442));
#43626=CARTESIAN_POINT('Ctrl Pts',(2.30911086639724,-6.36084082544802,-18.0863565540794));
#43627=CARTESIAN_POINT('Ctrl Pts',(2.48917695722757,-6.2954732776008,-18.0773130600231));
#43628=CARTESIAN_POINT('Ctrl Pts',(2.66651190243871,-6.22243883210547,-18.0682695659668));
#43629=CARTESIAN_POINT('Ctrl Pts',(2.84048899588266,-6.14197942558175,-18.0592260719105));
#43630=CARTESIAN_POINT('Ctrl Pts',(3.01430695311574,-6.06159361498282,-18.0501908499051));
#43631=CARTESIAN_POINT('Ctrl Pts',(3.18477297476097,-5.9737965026322,-18.0411556278997));
#43632=CARTESIAN_POINT('Ctrl Pts',(3.35128118281941,-5.87887773590169,-18.0321204058943));
#43633=CARTESIAN_POINT('Ctrl Pts',(3.51749603966346,-5.7841261953747,-18.0231011019832));
#43634=CARTESIAN_POINT('Ctrl Pts',(3.67976680017574,-5.68227817263267,-18.014081798072));
#43635=CARTESIAN_POINT('Ctrl Pts',(3.83751312385074,-5.57366863244249,-18.0050624941609));
#43636=CARTESIAN_POINT('Ctrl Pts',(3.99506154374408,-5.46519535050687,-17.9960545055965));
#43637=CARTESIAN_POINT('Ctrl Pts',(4.14809665906958,-5.34997761448417,-17.9870465170321));
#43638=CARTESIAN_POINT('Ctrl Pts',(4.29606583103446,-5.2283943400836,-17.9780385284677));
#43639=CARTESIAN_POINT('Ctrl Pts',(4.4437008094418,-5.10708566576675,-17.969050884761));
#43640=CARTESIAN_POINT('Ctrl Pts',(4.58629249937627,-4.97944030133634,-17.9600632410543));
#43641=CARTESIAN_POINT('Ctrl Pts',(4.72332052205592,-4.84587786122653,-17.9510755973476));
#43642=CARTESIAN_POINT('Ctrl Pts',(4.84266243237038,-4.72955423313019,-17.9432479826144));
#43643=CARTESIAN_POINT('Ctrl Pts',(4.95778453973587,-4.60874309349494,-17.9354203678813));
#43644=CARTESIAN_POINT('Ctrl Pts',(5.06836256078318,-4.48374731139606,-17.9275927531481));
#43645=CARTESIAN_POINT('Ctrl Pts',(5.18311562620026,-4.35403212003886,-17.9194695947028));
#43646=CARTESIAN_POINT('Ctrl Pts',(5.29292244058772,-4.21986720072514,-17.9113464362575));
#43647=CARTESIAN_POINT('Ctrl Pts',(5.39742676618268,-4.08167530601036,-17.9032232778122));
#43648=CARTESIAN_POINT('Ctrl Pts',(5.50192372367604,-3.94349315454703,-17.895100692092));
#43649=CARTESIAN_POINT('Ctrl Pts',(5.60111871627963,-3.80128488517399,-17.8869781063719));
#43650=CARTESIAN_POINT('Ctrl Pts',(5.69469686456815,-3.65550497478497,-17.8788555206518));
#43651=CARTESIAN_POINT('Ctrl Pts',(5.7882862572339,-3.50970754743998,-17.8707319589194));
#43652=CARTESIAN_POINT('Ctrl Pts',(5.87625726494517,-3.36033793316674,-17.862608397187));
#43653=CARTESIAN_POINT('Ctrl Pts',(5.95833930282776,-3.20787807629561,-17.8544848354546));
#43654=CARTESIAN_POINT('Ctrl Pts',(6.04048112773466,-3.05530717051045,-17.8463553566715));
#43655=CARTESIAN_POINT('Ctrl Pts',(6.11672524203291,-2.89964184915036,-17.8382258778884));
#43656=CARTESIAN_POINT('Ctrl Pts',(6.18684757181488,-2.74138762730269,-17.8300963991053));
#43657=CARTESIAN_POINT('Ctrl Pts',(6.25699848923641,-2.58306888799438,-17.8219636060768));
#43658=CARTESIAN_POINT('Ctrl Pts',(6.32102251216015,-2.42215948422491,-17.8138308130482));
#43659=CARTESIAN_POINT('Ctrl Pts',(6.37874448824341,-2.25918298367006,-17.8056980200197));
#43660=CARTESIAN_POINT('Ctrl Pts',(6.43652922821884,-2.0960292708955,-17.7975563838126));
#43661=CARTESIAN_POINT('Ctrl Pts',(6.48799812596531,-1.93080432108446,-17.7894147476055));
#43662=CARTESIAN_POINT('Ctrl Pts',(6.53302626424293,-1.76404558634748,-17.7812731113983));
#43663=CARTESIAN_POINT('Ctrl Pts',(6.55596748908339,-1.6790842760636,-17.7771250583377));
#43664=CARTESIAN_POINT('Ctrl Pts',(6.57723766630649,-1.59372499292872,-17.7729770052771));
#43665=CARTESIAN_POINT('Ctrl Pts',(6.59682542287081,-1.50803956850123,-17.7688289522164));
#43666=CARTESIAN_POINT('Ctrl Pts',(6.63668380168188,-1.33368156613357,-17.7603882372383));
#43667=CARTESIAN_POINT('Ctrl Pts',(6.6696548284095,-1.15761355221121,-17.7519475222603));
#43668=CARTESIAN_POINT('Ctrl Pts',(6.69560246401532,-0.980406366703095,
-17.7435068072822));
#43669=CARTESIAN_POINT('Ctrl Pts',(6.72153048717569,-0.803333122734483,
-17.7350724721942));
#43670=CARTESIAN_POINT('Ctrl Pts',(6.74044565347653,-0.625122752326402,
-17.7266381371062));
#43671=CARTESIAN_POINT('Ctrl Pts',(6.75226295239851,-0.446356384144486,
-17.7182038020182));
#43672=CARTESIAN_POINT('Ctrl Pts',(6.76407313393036,-0.267697684389556,
-17.7097745468095));
#43673=CARTESIAN_POINT('Ctrl Pts',(6.76879394889027,-0.0884839863314638,
-17.7013452916009));
#43674=CARTESIAN_POINT('Ctrl Pts',(6.76639216127063,0.0906979597089435,
-17.6929160363923));
#43675=CARTESIAN_POINT('Ctrl Pts',(6.7639914517972,0.269799472186608,-17.6844905650193));
#43676=CARTESIAN_POINT('Ctrl Pts',(6.75447451926184,0.448868928234639,-17.6760650936463));
#43677=CARTESIAN_POINT('Ctrl Pts',(6.73786021552276,0.627318671869125,-17.6676396222733));
#43678=CARTESIAN_POINT('Ctrl Pts',(6.72125082345384,0.805715660582545,-17.659216641714));
#43679=CARTESIAN_POINT('Ctrl Pts',(6.69754827532386,0.983492970610003,-17.6507936611548));
#43680=CARTESIAN_POINT('Ctrl Pts',(6.6668233890321,1.16006676508492,-17.6423706805955));
#43681=CARTESIAN_POINT('Ctrl Pts',(6.63609799400002,1.3366434832552,-17.6339475605692));
#43682=CARTESIAN_POINT('Ctrl Pts',(6.5983500791201,1.51201631652878,-17.6255244405429));
#43683=CARTESIAN_POINT('Ctrl Pts',(6.55370193485421,1.68560966688265,-17.6171013205165));
#43684=CARTESIAN_POINT('Ctrl Pts',(6.50905224658108,1.85920902038388,-17.6086779092047));
#43685=CARTESIAN_POINT('Ctrl Pts',(6.45750193605262,2.03102844523218,-17.6002544978929));
#43686=CARTESIAN_POINT('Ctrl Pts',(6.39922376371957,2.20050544690231,-17.591831086581));
#43687=CARTESIAN_POINT('Ctrl Pts',(6.3409354482813,2.37001194543193,-17.5834062092049));
#43688=CARTESIAN_POINT('Ctrl Pts',(6.27591704493449,2.53717489260836,-17.5749813318287));
#43689=CARTESIAN_POINT('Ctrl Pts',(6.20439037579449,2.70144943775536,-17.5665564544526));
#43690=CARTESIAN_POINT('Ctrl Pts',(6.13284127917035,2.86577549186816,-17.5581289354212));
#43691=CARTESIAN_POINT('Ctrl Pts',(6.05477998124062,3.02721103264571,-17.5497014163898));
#43692=CARTESIAN_POINT('Ctrl Pts',(5.97047554140099,3.18523324256365,-17.5412738973584));
#43693=CARTESIAN_POINT('Ctrl Pts',(5.88609550059781,3.34339716069241,-17.5328388208536));
#43694=CARTESIAN_POINT('Ctrl Pts',(5.79546128818487,3.49814133724314,-17.5244037443488));
#43695=CARTESIAN_POINT('Ctrl Pts',(5.69888740396738,3.64896853328471,-17.515968667844));
#43696=CARTESIAN_POINT('Ctrl Pts',(5.6022668449561,3.79986862510271,-17.5075295146112));
#43697=CARTESIAN_POINT('Ctrl Pts',(5.49970107540827,3.94684768457486,-17.4990903613784));
#43698=CARTESIAN_POINT('Ctrl Pts',(5.39154695743122,4.08943888642612,-17.4906512081456));
#43699=CARTESIAN_POINT('Ctrl Pts',(5.28327264990592,4.23218854708096,-17.4822026766475));
#43700=CARTESIAN_POINT('Ctrl Pts',(5.16939779304018,4.3705403461799,-17.4737541451494));
#43701=CARTESIAN_POINT('Ctrl Pts',(5.05031920151829,4.50406094128129,-17.4653056136513));
#43702=CARTESIAN_POINT('Ctrl Pts',(4.98452441618804,4.57783540216116,-17.4606375258853));
#43703=CARTESIAN_POINT('Ctrl Pts',(4.91714163757313,4.65013557585458,-17.4559694381194));
#43704=CARTESIAN_POINT('Ctrl Pts',(4.84824246668551,4.72089334599155,-17.4513013503534));
#43705=CARTESIAN_POINT('Ctrl Pts',(4.72174813934906,4.85079993879947,-17.4427310495167));
#43706=CARTESIAN_POINT('Ctrl Pts',(4.58984736139188,4.97580553276005,-17.43416074868));
#43707=CARTESIAN_POINT('Ctrl Pts',(4.45295658557858,5.09543586427622,-17.4255904478433));
#43708=CARTESIAN_POINT('Ctrl Pts',(4.32148988795948,5.21032603511549,-17.4173597314791));
#43709=CARTESIAN_POINT('Ctrl Pts',(4.18542130781511,5.32025841659972,-17.4091290151148));
#43710=CARTESIAN_POINT('Ctrl Pts',(4.04515988920989,5.42484750667956,-17.4008982987506));
#43711=CARTESIAN_POINT('Ctrl Pts',(3.90501616407355,5.52934883597,-17.392674488787));
#43712=CARTESIAN_POINT('Ctrl Pts',(3.76068688788923,5.62851558813638,-17.3844506788235));
#43713=CARTESIAN_POINT('Ctrl Pts',(3.61261576397932,5.7220010784557,-17.3762268688599));
#43714=CARTESIAN_POINT('Ctrl Pts',(3.4646649870818,5.81541058704971,-17.3680097429205));
#43715=CARTESIAN_POINT('Ctrl Pts',(3.31297872228734,5.90314784555181,-17.359792616981));
#43716=CARTESIAN_POINT('Ctrl Pts',(3.15803123466129,5.98490833020053,-17.3515754910416));
#43717=CARTESIAN_POINT('Ctrl Pts',(3.13843445406855,5.99524888043058,-17.3505362407988));
#43718=CARTESIAN_POINT('Ctrl Pts',(3.11878554649122,6.00549388532804,-17.3494969905559));
#43719=CARTESIAN_POINT('Ctrl Pts',(3.09908550384714,6.01564277861016,-17.3484577403131));
#43720=CARTESIAN_POINT('Origin',(0.,0.,-63.6971797838103));
#43721=CARTESIAN_POINT('',(3.09908550384715,6.01564277861015,-14.9545069759344));
#43722=CARTESIAN_POINT('',(3.09908550384718,6.01564277861013,-15.3486931990458));
#43723=CARTESIAN_POINT('',(3.09908550384721,6.01564277861012,-63.6971797838103));
#43724=CARTESIAN_POINT('',(-6.76699974845141,-0.0016519250911805,-16.30282021619));
#43725=CARTESIAN_POINT('Ctrl Pts',(-6.76699968617377,-0.00206090370965092,
-16.30282021619));
#43726=CARTESIAN_POINT('Ctrl Pts',(-6.76694375844654,-0.185700202734719,
-16.2942112662645));
#43727=CARTESIAN_POINT('Ctrl Pts',(-6.75940830309195,-0.369187997043884,
-16.2856023163391));
#43728=CARTESIAN_POINT('Ctrl Pts',(-6.74445571692456,-0.551911299434681,
-16.2769933664136));
#43729=CARTESIAN_POINT('Ctrl Pts',(-6.72948741384525,-0.734826665326396,
-16.2683753674777));
#43730=CARTESIAN_POINT('Ctrl Pts',(-6.70708645163332,-0.916975633748548,
-16.2597573685419));
#43731=CARTESIAN_POINT('Ctrl Pts',(-6.67736667878218,-1.0977537233321,-16.2511393696061));
#43732=CARTESIAN_POINT('Ctrl Pts',(-6.64758963169228,-1.27888019806367,
-16.2425047625578));
#43733=CARTESIAN_POINT('Ctrl Pts',(-6.6104656300992,-1.45863021283409,-16.2338701555095));
#43734=CARTESIAN_POINT('Ctrl Pts',(-6.56615938183854,-1.63641069792815,
-16.2252355484613));
#43735=CARTESIAN_POINT('Ctrl Pts',(-6.53432670080435,-1.76414052607361,
-16.2190318480169));
#43736=CARTESIAN_POINT('Ctrl Pts',(-6.49878761153712,-1.8908539874124,-16.2128281475725));
#43737=CARTESIAN_POINT('Ctrl Pts',(-6.45961868919721,-2.01633712215346,
-16.2066244471282));
#43738=CARTESIAN_POINT('Ctrl Pts',(-6.40632570504453,-2.18706866930073,
-16.1981837321501));
#43739=CARTESIAN_POINT('Ctrl Pts',(-6.34622040540474,-2.35581222350463,
-16.189743017172));
#43740=CARTESIAN_POINT('Ctrl Pts',(-6.27947247758363,-2.52200602760376,
-16.1813023021939));
#43741=CARTESIAN_POINT('Ctrl Pts',(-6.21277500099128,-2.68807421459533,
-16.1728679671059));
#43742=CARTESIAN_POINT('Ctrl Pts',(-6.13944502871916,-2.85159618499573,
-16.1644336320179));
#43743=CARTESIAN_POINT('Ctrl Pts',(-6.05970152261526,-3.01202696814194,
-16.1559992969299));
#43744=CARTESIAN_POINT('Ctrl Pts',(-5.98000604488462,-3.17236112612187,
-16.1475700417213));
#43745=CARTESIAN_POINT('Ctrl Pts',(-5.89390488238898,-3.32960751076188,
-16.1391407865127));
#43746=CARTESIAN_POINT('Ctrl Pts',(-5.80166456771601,-3.48324234639345,
-16.1307115313041));
#43747=CARTESIAN_POINT('Ctrl Pts',(-5.70946565909596,-3.63680821638723,
-16.1222860599311));
#43748=CARTESIAN_POINT('Ctrl Pts',(-5.61113326445851,-3.78676548449717,
-16.1138605885581));
#43749=CARTESIAN_POINT('Ctrl Pts',(-5.50697938482385,-3.93261580314238,
-16.1054351171851));
#43750=CARTESIAN_POINT('Ctrl Pts',(-5.40285629609775,-4.07842300420195,
-16.0970121366259));
#43751=CARTESIAN_POINT('Ctrl Pts',(-5.2929153479968,-4.22012540601256,-16.0885891560667));
#43752=CARTESIAN_POINT('Ctrl Pts',(-5.17751152717624,-4.35725411078551,
-16.0801661755074));
#43753=CARTESIAN_POINT('Ctrl Pts',(-5.06210579550756,-4.49438508612563,
-16.0717430554811));
#43754=CARTESIAN_POINT('Ctrl Pts',(-4.94123721996666,-4.62694195382757,
-16.0633199354548));
#43755=CARTESIAN_POINT('Ctrl Pts',(-4.81530112237883,-4.7544888369642,-16.0548968154284));
#43756=CARTESIAN_POINT('Ctrl Pts',(-4.6893606697109,-4.88204013088458,-16.0464734041166));
#43757=CARTESIAN_POINT('Ctrl Pts',(-4.55835257978465,-5.00458085735821,
-16.0380499928047));
#43758=CARTESIAN_POINT('Ctrl Pts',(-4.42270919529753,-5.12171185970381,
-16.0296265814929));
#43759=CARTESIAN_POINT('Ctrl Pts',(-4.28704220257016,-5.23886324827654,
-16.0212017041168));
#43760=CARTESIAN_POINT('Ctrl Pts',(-4.14673855925296,-5.35060281760719,
-16.0127768267407));
#43761=CARTESIAN_POINT('Ctrl Pts',(-4.00226412717075,-5.45657134621753,
-16.0043519493646));
#43762=CARTESIAN_POINT('Ctrl Pts',(-3.85774439452989,-5.56257310170044,
-15.9959244303331));
#43763=CARTESIAN_POINT('Ctrl Pts',(-3.70905153459146,-5.66280001157985,
-15.9874969113017));
#43764=CARTESIAN_POINT('Ctrl Pts',(-3.55668114302472,-5.7569356646442,-15.9790693922703));
#43765=CARTESIAN_POINT('Ctrl Pts',(-3.40417411157982,-5.85115573492395,
-15.9706343157655));
#43766=CARTESIAN_POINT('Ctrl Pts',(-3.24798324287393,-5.93927345827658,
-15.9621992392607));
#43767=CARTESIAN_POINT('Ctrl Pts',(-3.0886305295471,-6.02101739342693,-15.9537641627559));
#43768=CARTESIAN_POINT('Ctrl Pts',(-2.92920080000524,-6.10280083595908,
-15.9453250095232));
#43769=CARTESIAN_POINT('Ctrl Pts',(-2.76660647833734,-6.17820420171611,
-15.9368858562904));
#43770=CARTESIAN_POINT('Ctrl Pts',(-2.60139086113565,-6.24700364875833,
-15.9284467030577));
#43771=CARTESIAN_POINT('Ctrl Pts',(-2.43599164306149,-6.31587955127563,
-15.9199981715596));
#43772=CARTESIAN_POINT('Ctrl Pts',(-2.26796561981151,-6.37813675046467,
-15.9115496400614));
#43773=CARTESIAN_POINT('Ctrl Pts',(-2.09787376510411,-6.43360044342885,
-15.9031011085633));
#43774=CARTESIAN_POINT('Ctrl Pts',(-2.00389249673217,-6.46424593331626,
-15.8984330207972));
#43775=CARTESIAN_POINT('Ctrl Pts',(-1.90928079902951,-6.49281830858076,
-15.8937649330312));
#43776=CARTESIAN_POINT('Ctrl Pts',(-1.81413482365927,-6.51929473498374,
-15.8890968452651));
#43777=CARTESIAN_POINT('Ctrl Pts',(-1.64616955152901,-6.56603470636466,
-15.8808560696683));
#43778=CARTESIAN_POINT('Ctrl Pts',(-1.47616488830859,-6.60634379464391,
-15.8726152940716));
#43779=CARTESIAN_POINT('Ctrl Pts',(-1.30465256828463,-6.64004297245645,
-15.8643745184748));
#43780=CARTESIAN_POINT('Ctrl Pts',(-1.13333021674917,-6.67370482477615,
-15.8561428704304));
#43781=CARTESIAN_POINT('Ctrl Pts',(-0.96050387951586,-6.70077127646936,
-15.8479112223861));
#43782=CARTESIAN_POINT('Ctrl Pts',(-0.78672063134305,-6.72111297689744,
-15.8396795743417));
#43783=CARTESIAN_POINT('Ctrl Pts',(-0.613098897160356,-6.74143577176796,
-15.8314555767834));
#43784=CARTESIAN_POINT('Ctrl Pts',(-0.438522374509828,-6.75504622128248,
-15.8232315792251));
#43785=CARTESIAN_POINT('Ctrl Pts',(-0.263548616740972,-6.76186595006245,
-15.8150075816668));
#43786=CARTESIAN_POINT('Ctrl Pts',(-0.0887294489668274,-6.76867965358555,
-15.8067908500423));
#43787=CARTESIAN_POINT('Ctrl Pts',(0.0864859002690414,-6.76871458046289,
-15.7985741184178));
#43788=CARTESIAN_POINT('Ctrl Pts',(0.261534590517598,-6.76194414779972,
-15.7903573867933));
#43789=CARTESIAN_POINT('Ctrl Pts',(0.436493596841361,-6.75517718387986,
-15.7821448649046));
#43790=CARTESIAN_POINT('Ctrl Pts',(0.611285759586278,-6.74161181814315,
-15.773932343016));
#43791=CARTESIAN_POINT('Ctrl Pts',(0.785347648178865,-6.72127354535582,
-15.7657198211273));
#43792=CARTESIAN_POINT('Ctrl Pts',(0.959351329638174,-6.70094207378478,
-15.7575100455454));
#43793=CARTESIAN_POINT('Ctrl Pts',(1.13262487044065,-6.67384224834337,-15.7493002699636));
#43794=CARTESIAN_POINT('Ctrl Pts',(1.30460927888467,-6.64005147792154,-15.7410904943818));
#43795=CARTESIAN_POINT('Ctrl Pts',(1.37972760030674,-6.62529254729166,-15.7375046776991));
#43796=CARTESIAN_POINT('Ctrl Pts',(1.45460007362233,-6.60925784080126,-15.7339188610164));
#43797=CARTESIAN_POINT('Ctrl Pts',(1.52918061718094,-6.59195689003183,-15.7303330443337));
#43798=CARTESIAN_POINT('Ctrl Pts',(1.71343096416494,-6.54921509665893,-15.721474326812));
#43799=CARTESIAN_POINT('Ctrl Pts',(1.8957078910182,-6.49878607415575,-15.7126156092902));
#43800=CARTESIAN_POINT('Ctrl Pts',(2.07539519919948,-6.44088687737487,-15.7037568917684));
#43801=CARTESIAN_POINT('Ctrl Pts',(2.2554186734751,-6.3828793604959,-15.694881601009));
#43802=CARTESIAN_POINT('Ctrl Pts',(2.43284260030617,-6.31737381980341,-15.6860063102495));
#43803=CARTESIAN_POINT('Ctrl Pts',(2.60707018573707,-6.24463562160683,-15.6771310194901));
#43804=CARTESIAN_POINT('Ctrl Pts',(2.78179261668468,-6.1716908305726,-15.6682305209093));
#43805=CARTESIAN_POINT('Ctrl Pts',(2.95330029856249,-6.09147237476867,-15.6593300223285));
#43806=CARTESIAN_POINT('Ctrl Pts',(3.121017748684,-6.00429323171341,-15.6504295237478));
#43807=CARTESIAN_POINT('Ctrl Pts',(3.28896223814215,-5.91699607413555,-15.6415169765502));
#43808=CARTESIAN_POINT('Ctrl Pts',(3.45310601962957,-5.82271953233222,-15.6326044293525));
#43809=CARTESIAN_POINT('Ctrl Pts',(3.61290095983023,-5.72182100860013,-15.6236918821549));
#43810=CARTESIAN_POINT('Ctrl Pts',(3.77304874286516,-5.62069969107343,-15.6147596551827));
#43811=CARTESIAN_POINT('Ctrl Pts',(3.92882825750772,-5.51292728426395,-15.6058274282104));
#43812=CARTESIAN_POINT('Ctrl Pts',(4.0797206076869,-5.39890440397076,-15.5968952012381));
#43813=CARTESIAN_POINT('Ctrl Pts',(4.22233130302963,-5.29113961520391,-15.5884532152928));
#43814=CARTESIAN_POINT('Ctrl Pts',(4.36057671102482,-5.17779209576435,-15.5800112293474));
#43815=CARTESIAN_POINT('Ctrl Pts',(4.49404799525455,-5.05923132662943,-15.5715692434021));
#43816=CARTESIAN_POINT('Ctrl Pts',(4.62407242719406,-4.9437323506059,-15.5633452689845));
#43817=CARTESIAN_POINT('Ctrl Pts',(4.74981382066025,-4.82306450254085,-15.5551212945669));
#43818=CARTESIAN_POINT('Ctrl Pts',(4.87083694085045,-4.69757772640823,-15.5468973201494));
#43819=CARTESIAN_POINT('Ctrl Pts',(4.99173224888356,-4.57222347648644,-15.5386820310467));
#43820=CARTESIAN_POINT('Ctrl Pts',(5.10791895950427,-4.44206068889404,-15.5304667419441));
#43821=CARTESIAN_POINT('Ctrl Pts',(5.21899553731649,-4.30747891248125,-15.5222514528414));
#43822=CARTESIAN_POINT('Ctrl Pts',(5.32997708707946,-4.17301227324614,-15.5140431920692));
#43823=CARTESIAN_POINT('Ctrl Pts',(5.43585698396787,-4.03413444949387,-15.505834931297));
#43824=CARTESIAN_POINT('Ctrl Pts',(5.5362710917825,-3.89127118025632,-15.4976266705248));
#43825=CARTESIAN_POINT('Ctrl Pts',(5.63661942868097,-3.74850148599851,-15.4894237861369));
#43826=CARTESIAN_POINT('Ctrl Pts',(5.73150890217019,-3.60175183833447,-15.4812209017491));
#43827=CARTESIAN_POINT('Ctrl Pts',(5.82061612079869,-3.45148040329051,-15.4730180173612));
#43828=CARTESIAN_POINT('Ctrl Pts',(5.90968283875454,-3.30127726904522,-15.4648188613169));
#43829=CARTESIAN_POINT('Ctrl Pts',(5.99297235524397,-3.14755584425924,-15.4566197052727));
#43830=CARTESIAN_POINT('Ctrl Pts',(6.07020498216446,-2.99080264720122,-15.4484205492285));
#43831=CARTESIAN_POINT('Ctrl Pts',(6.14743089172441,-2.83406308385969,-15.4402221063115));
#43832=CARTESIAN_POINT('Ctrl Pts',(6.21860079500695,-2.67429259113385,-15.4320236633945));
#43833=CARTESIAN_POINT('Ctrl Pts',(6.28348113694317,-2.51200195097046,-15.4238252204774));
#43834=CARTESIAN_POINT('Ctrl Pts',(6.34836083274802,-2.34971292702967,-15.4156268592072));
#43835=CARTESIAN_POINT('Ctrl Pts',(6.40695095783095,-2.18490413831689,-15.407428497937));
#43836=CARTESIAN_POINT('Ctrl Pts',(6.45906631490303,-2.0181058792058,-15.3992301366667));
#43837=CARTESIAN_POINT('Ctrl Pts',(6.51119062009564,-1.85127898110976,-15.3910303677514));
#43838=CARTESIAN_POINT('Ctrl Pts',(6.55683783545461,-1.68246227445443,-15.3828305988362));
#43839=CARTESIAN_POINT('Ctrl Pts',(6.59587278640836,-1.51220077553138,-15.3746308299209));
#43840=CARTESIAN_POINT('Ctrl Pts',(6.63492153065081,-1.34187911344802,-15.3664281635566));
#43841=CARTESIAN_POINT('Ctrl Pts',(6.66735327604792,-1.17011199152787,-15.3582254971923));
#43842=CARTESIAN_POINT('Ctrl Pts',(6.69308404909215,-0.997454215384487,
-15.350022830828));
#43843=CARTESIAN_POINT('Ctrl Pts',(6.7188440458631,-0.824600343163547,-15.3418108482849));
#43844=CARTESIAN_POINT('Ctrl Pts',(6.73788781280401,-0.650854150958018,
-15.3335988657419));
#43845=CARTESIAN_POINT('Ctrl Pts',(6.75018321515767,-0.476776217741226,
-15.3253868831989));
#43846=CARTESIAN_POINT('Ctrl Pts',(6.76248586950582,-0.302595611006688,
-15.3171700571176));
#43847=CARTESIAN_POINT('Ctrl Pts',(6.76803221378007,-0.128083231145394,
-15.3089532310363));
#43848=CARTESIAN_POINT('Ctrl Pts',(6.76684228280827,0.0462008614439957,
-15.300736404955));
#43849=CARTESIAN_POINT('Ctrl Pts',(6.76565051679105,0.220753725275382,-15.2925069073411));
#43850=CARTESIAN_POINT('Ctrl Pts',(6.75770173226373,0.395077240247219,-15.2842774097272));
#43851=CARTESIAN_POINT('Ctrl Pts',(6.74306793982273,0.568615651327713,-15.2760479121134));
#43852=CARTESIAN_POINT('Ctrl Pts',(6.73002400076775,0.723300396718125,-15.2687124885886));
#43853=CARTESIAN_POINT('Ctrl Pts',(6.71166946035732,0.877361294022358,-15.2613770650638));
#43854=CARTESIAN_POINT('Ctrl Pts',(6.68808929934123,1.03041279302879,-15.2540416415391));
#43855=CARTESIAN_POINT('Ctrl Pts',(6.66214389424629,1.19881635649048,-15.2459704271499));
#43856=CARTESIAN_POINT('Ctrl Pts',(6.6297863745111,1.36654684253158,-15.2378992127606));
#43857=CARTESIAN_POINT('Ctrl Pts',(6.59105446675761,1.53306556162305,-15.2298279983714));
#43858=CARTESIAN_POINT('Ctrl Pts',(6.55237110533006,1.69937556721494,-15.2217669003908));
#43859=CARTESIAN_POINT('Ctrl Pts',(6.50732933721513,1.86447646922579,-15.2137058024102));
#43860=CARTESIAN_POINT('Ctrl Pts',(6.45601863229179,2.0278344161941,-15.2056447044296));
#43861=CARTESIAN_POINT('Ctrl Pts',(6.40476098686464,2.19102343758676,-15.1975919422884));
#43862=CARTESIAN_POINT('Ctrl Pts',(6.34724741661247,2.35247273791885,-15.1895391801472));
#43863=CARTESIAN_POINT('Ctrl Pts',(6.28361843518846,2.51165848812289,-15.181486418006));
#43864=CARTESIAN_POINT('Ctrl Pts',(6.22004131774242,2.6707144860339,-15.1734402196706));
#43865=CARTESIAN_POINT('Ctrl Pts',(6.15035884863705,2.82751026159654,-15.1653940213353));
#43866=CARTESIAN_POINT('Ctrl Pts',(6.07476135706578,2.98153709597923,-15.1573478229999));
#43867=CARTESIAN_POINT('Ctrl Pts',(5.99535398464795,3.14332640863964,-15.1488961210389));
#43868=CARTESIAN_POINT('Ctrl Pts',(5.90942006254912,3.30206005554164,-15.1404444190778));
#43869=CARTESIAN_POINT('Ctrl Pts',(5.81723777276029,3.45717134304491,-15.1319927171167));
#43870=CARTESIAN_POINT('Ctrl Pts',(5.72955553002772,3.60471058938582,-15.1239536004431));
#43871=CARTESIAN_POINT('Ctrl Pts',(5.63622066750068,3.74897236409537,-15.1159144837695));
#43872=CARTESIAN_POINT('Ctrl Pts',(5.53751977969006,3.88949401459127,-15.1078753670959));
#43873=CARTESIAN_POINT('Ctrl Pts',(5.43882850951006,4.03000197234987,-15.0998370337714));
#43874=CARTESIAN_POINT('Ctrl Pts',(5.33477246883049,4.1667702254605,-15.0917987004469));
#43875=CARTESIAN_POINT('Ctrl Pts',(5.22568128450892,4.29936554769808,-15.0837603671225));
#43876=CARTESIAN_POINT('Ctrl Pts',(5.11657913495448,4.4319741976724,-15.0757212258299));
#43877=CARTESIAN_POINT('Ctrl Pts',(5.00244107187347,4.56040879379873,-15.0676820845373));
#43878=CARTESIAN_POINT('Ctrl Pts',(4.88363656133641,4.68426973356342,-15.0596429432447));
#43879=CARTESIAN_POINT('Ctrl Pts',(4.76479658663491,4.80816764688001,-15.0516014021996));
#43880=CARTESIAN_POINT('Ctrl Pts',(4.6412876507134,4.92748891767104,-15.0435598611544));
#43881=CARTESIAN_POINT('Ctrl Pts',(4.51351544708178,5.04187140940288,-15.0355183201093));
#43882=CARTESIAN_POINT('Ctrl Pts',(4.38561739910311,5.15636655779694,-15.0274688588557));
#43883=CARTESIAN_POINT('Ctrl Pts',(4.25344797869773,5.26591296694721,-15.0194193976022));
#43884=CARTESIAN_POINT('Ctrl Pts',(4.117445765198,5.37018895111271,-15.0113699363486));
#43885=CARTESIAN_POINT('Ctrl Pts',(3.98136553561481,5.47452475198027,-15.0033158576155));
#43886=CARTESIAN_POINT('Ctrl Pts',(3.84144843792085,5.57358389181528,-14.9952617788824));
#43887=CARTESIAN_POINT('Ctrl Pts',(3.69816084534254,5.66708879072628,-14.9872077001493));
#43888=CARTESIAN_POINT('Ctrl Pts',(3.55469045356767,5.76071297854489,-14.9791433464224));
#43889=CARTESIAN_POINT('Ctrl Pts',(3.40784130244595,5.84876859034578,-14.9710789926955));
#43890=CARTESIAN_POINT('Ctrl Pts',(3.2581036634238,5.93102432286232,-14.9630146389686));
#43891=CARTESIAN_POINT('Ctrl Pts',(3.20544735148314,5.9599501396348,-14.9601787512905));
#43892=CARTESIAN_POINT('Ctrl Pts',(3.15243401629433,5.98815916502779,-14.9573428636125));
#43893=CARTESIAN_POINT('Ctrl Pts',(3.09908550384716,6.01564277861015,-14.9545069759344));
#43894=CARTESIAN_POINT('Ctrl Pts',(3.09908550384726,6.0156427786101,-16.9542436419538));
#43895=CARTESIAN_POINT('Ctrl Pts',(2.9337323201833,6.1008279655248,-16.9454941940546));
#43896=CARTESIAN_POINT('Ctrl Pts',(2.76486502144424,6.17919158180191,-16.9367447461553));
#43897=CARTESIAN_POINT('Ctrl Pts',(2.59305716434346,6.25046746591382,-16.927995298256));
#43898=CARTESIAN_POINT('Ctrl Pts',(2.42125069459278,6.32174277447227,-16.9192459210085));
#43899=CARTESIAN_POINT('Ctrl Pts',(2.24650397871055,6.38593035557827,-16.9104965437611));
#43900=CARTESIAN_POINT('Ctrl Pts',(2.06941053323769,6.44281220003539,-16.9017471665137));
#43901=CARTESIAN_POINT('Ctrl Pts',(1.89231845896684,6.49969360406685,-16.8929978570111));
#43902=CARTESIAN_POINT('Ctrl Pts',(1.71287996431508,6.5492692970088,-16.8842485475085));
#43903=CARTESIAN_POINT('Ctrl Pts',(1.5317044917351,6.59137090065478,-16.8754992380059));
#43904=CARTESIAN_POINT('Ctrl Pts',(1.35053036178179,6.63347219230081,-16.8667499933413));
#43905=CARTESIAN_POINT('Ctrl Pts',(1.16761955878856,6.66809944062452,-16.8580007486768));
#43906=CARTESIAN_POINT('Ctrl Pts',(0.98359330931063,6.69513503985389,-16.8492515040122));
#43907=CARTESIAN_POINT('Ctrl Pts',(0.799568362460039,6.72217044771214,-16.840502321279));
#43908=CARTESIAN_POINT('Ctrl Pts',(0.614428268438568,6.74161427235978,-16.8317531385458));
#43909=CARTESIAN_POINT('Ctrl Pts',(0.428801816330156,6.75340047696803,-16.8230039558126));
#43910=CARTESIAN_POINT('Ctrl Pts',(0.243176616522558,6.76518660206243,-16.8142548321045));
#43911=CARTESIAN_POINT('Ctrl Pts',(0.0570653511651231,6.76931519233997,
-16.8055057083963));
#43912=CARTESIAN_POINT('Ctrl Pts',(-0.12889990080048,6.76577222610794,-16.7967565846882));
#43913=CARTESIAN_POINT('Ctrl Pts',(-0.314863959942389,6.76222928260131,
-16.788007517099));
#43914=CARTESIAN_POINT('Ctrl Pts',(-0.500681721080966,6.75101488651274,
-16.7792584495097));
#43915=CARTESIAN_POINT('Ctrl Pts',(-0.685722110173501,6.73216712415989,
-16.7705093819204));
#43916=CARTESIAN_POINT('Ctrl Pts',(-0.870761373827683,6.71331947644144,
-16.7617603675441));
#43917=CARTESIAN_POINT('Ctrl Pts',(-1.05502298984337,6.68683858439997,-16.7530113531677));
#43918=CARTESIAN_POINT('Ctrl Pts',(-1.23788117676041,6.65281438131429,-16.7442623387914));
#43919=CARTESIAN_POINT('Ctrl Pts',(-1.43009641451775,6.61704912302381,-16.7350656279038));
#43920=CARTESIAN_POINT('Ctrl Pts',(-1.62076048992678,6.57294837083169,-16.7258689170163));
#43921=CARTESIAN_POINT('Ctrl Pts',(-1.80915798961115,6.52067760042054,-16.7166722061288));
#43922=CARTESIAN_POINT('Ctrl Pts',(-1.98840443003001,6.47094578577412,-16.7079222084223));
#43923=CARTESIAN_POINT('Ctrl Pts',(-2.16559895952187,6.41381888474477,-16.6991722107158));
#43924=CARTESIAN_POINT('Ctrl Pts',(-2.34013966242323,6.34949095285234,-16.6904222130093));
#43925=CARTESIAN_POINT('Ctrl Pts',(-2.51467682554013,6.28516432556686,-16.6816723927577));
#43926=CARTESIAN_POINT('Ctrl Pts',(-2.68656000078838,6.21363705879663,-16.6729225725061));
#43927=CARTESIAN_POINT('Ctrl Pts',(-2.85520533840881,6.13515211510862,-16.6641727522545));
#43928=CARTESIAN_POINT('Ctrl Pts',(-3.02384747998319,6.05666865881125,-16.6554230978232));
#43929=CARTESIAN_POINT('Ctrl Pts',(-3.18925164684528,5.97122791039849,-16.646673443392));
#43930=CARTESIAN_POINT('Ctrl Pts',(-3.35085601829148,5.87912008251913,-16.6379237889607));
#43931=CARTESIAN_POINT('Ctrl Pts',(-3.51245754191405,5.78701387778182,-16.6291742887176));
#43932=CARTESIAN_POINT('Ctrl Pts',(-3.6702591551092,5.68824097060993,-16.6204247884745));
#43933=CARTESIAN_POINT('Ctrl Pts',(-3.82372487928815,5.58313684656868,-16.6116752882313));
#43934=CARTESIAN_POINT('Ctrl Pts',(-3.97718810300776,5.47803443501789,-16.6029259305462));
#43935=CARTESIAN_POINT('Ctrl Pts',(-4.12631534263,5.36660117496396,-16.5941765728611));
#43936=CARTESIAN_POINT('Ctrl Pts',(-4.27060009886196,5.24921554097374,-16.585427215176));
#43937=CARTESIAN_POINT('Ctrl Pts',(-4.41488269594188,5.13183166360313,-16.5766779884208));
#43938=CARTESIAN_POINT('Ctrl Pts',(-4.55432273235066,5.00849577139491,-16.5679287616656));
#43939=CARTESIAN_POINT('Ctrl Pts',(-4.68844662480187,4.87962675277361,-16.5591795349104));
#43940=CARTESIAN_POINT('Ctrl Pts',(-4.82256868835127,4.75075949139912,-16.5504304274589));
#43941=CARTESIAN_POINT('Ctrl Pts',(-4.95137454637822,4.61635945312568,-16.5416813200075));
#43942=CARTESIAN_POINT('Ctrl Pts',(-5.07442674461028,4.47688309134647,-16.532932212556));
#43943=CARTESIAN_POINT('Ctrl Pts',(-5.19747742838496,4.33740844616403,-16.5241832127836));
#43944=CARTESIAN_POINT('Ctrl Pts',(-5.3147744045089,4.19285781736076,-16.5154342130112));
#43945=CARTESIAN_POINT('Ctrl Pts',(-5.42591931531122,4.04372211999448,-16.5066852132388));
#43946=CARTESIAN_POINT('Ctrl Pts',(-5.53707636462956,3.89457013500837,-16.4979352579583));
#43947=CARTESIAN_POINT('Ctrl Pts',(-5.64207983273451,3.74083230916451,-16.4891853026777));
#43948=CARTESIAN_POINT('Ctrl Pts',(-5.74057303468732,3.58303087251851,-16.4804353473971));
#43949=CARTESIAN_POINT('Ctrl Pts',(-5.83906243363747,3.42523552887461,-16.4716857299683));
#43950=CARTESIAN_POINT('Ctrl Pts',(-5.93104191768405,3.2633771315703,-16.4629361125395));
#43951=CARTESIAN_POINT('Ctrl Pts',(-6.01619906699633,3.098005452912,-16.4541864951107));
#43952=CARTESIAN_POINT('Ctrl Pts',(-6.10135338095362,2.93263928039639,-16.4454371690053));
#43953=CARTESIAN_POINT('Ctrl Pts',(-6.1796856835282,2.76376031540267,-16.4366878428999));
#43954=CARTESIAN_POINT('Ctrl Pts',(-6.25092992694869,2.59194213831584,-16.4279385167945));
#43955=CARTESIAN_POINT('Ctrl Pts',(-6.32217217691087,2.42012876880863,-16.4191894355007));
#43956=CARTESIAN_POINT('Ctrl Pts',(-6.38632665483835,2.24537661647715,-16.4104403542069));
#43957=CARTESIAN_POINT('Ctrl Pts',(-6.44317547869335,2.06827917621502,-16.4016912729131));
#43958=CARTESIAN_POINT('Ctrl Pts',(-6.50002944235924,1.89116572423465,-16.3929414005982));
#43959=CARTESIAN_POINT('Ctrl Pts',(-6.54957634250388,1.71170683289237,-16.3841915282832));
#43960=CARTESIAN_POINT('Ctrl Pts',(-6.59164787708387,1.53051209225399,-16.3754416559682));
#43961=CARTESIAN_POINT('Ctrl Pts',(-6.63371649074998,1.34932993148081,-16.3666923911335));
#43962=CARTESIAN_POINT('Ctrl Pts',(-6.66831071257112,1.16641244174071,-16.3579431262987));
#43963=CARTESIAN_POINT('Ctrl Pts',(-6.69531304840321,0.982380875160844,
-16.3491938614639));
#43964=CARTESIAN_POINT('Ctrl Pts',(-6.72231677033033,0.79833986179671,-16.3404441475082));
#43965=CARTESIAN_POINT('Ctrl Pts',(-6.74172778477882,0.613184940731055,
-16.3316944335526));
#43966=CARTESIAN_POINT('Ctrl Pts',(-6.75348015835512,0.427545027691487,
-16.3229447195969));
#43967=CARTESIAN_POINT('Ctrl Pts',(-6.76249038365218,0.285219953547709,
-16.3162365517946));
#43968=CARTESIAN_POINT('Ctrl Pts',(-6.76699999999999,0.142609995758143,
-16.3095283839923));
#43969=CARTESIAN_POINT('Ctrl Pts',(-6.767,7.07605502806519E-13,-16.30282021619));
#43970=CARTESIAN_POINT('',(-6.76699777839932,0.00548335104101128,-16.6971797838448));
#43971=CARTESIAN_POINT('Ctrl Pts',(3.09908550384714,6.01564277861016,-17.3484577403131));
#43972=CARTESIAN_POINT('Ctrl Pts',(2.94341968881325,6.09583731285535,-17.3402457917913));
#43973=CARTESIAN_POINT('Ctrl Pts',(2.78455904321523,6.1700270282288,-17.3320338432694));
#43974=CARTESIAN_POINT('Ctrl Pts',(2.62300731811465,6.23795812819523,-17.3238218947476));
#43975=CARTESIAN_POINT('Ctrl Pts',(2.46150629672237,6.30586790769187,-17.3156125235813));
#43976=CARTESIAN_POINT('Ctrl Pts',(2.29731620634852,6.36752284783082,-17.307403152415));
#43977=CARTESIAN_POINT('Ctrl Pts',(2.13096231121924,6.42271660811554,-17.2991937812488));
#43978=CARTESIAN_POINT('Ctrl Pts',(2.08600190077923,6.43763380686342,-17.2969750373065));
#43979=CARTESIAN_POINT('Ctrl Pts',(2.04088354244671,6.45207931767505,-17.2947562933643));
#43980=CARTESIAN_POINT('Ctrl Pts',(1.99561783376721,6.46604967979293,-17.292537549422));
#43981=CARTESIAN_POINT('Ctrl Pts',(1.81488669171063,6.52182875791112,-17.2836788319002));
#43982=CARTESIAN_POINT('Ctrl Pts',(1.63199268618497,6.56997174407535,-17.2748201143784));
#43983=CARTESIAN_POINT('Ctrl Pts',(1.44757753915087,6.61035613776943,-17.2659613968566));
#43984=CARTESIAN_POINT('Ctrl Pts',(1.26281738099823,6.65081608417739,-17.2570861060972));
#43985=CARTESIAN_POINT('Ctrl Pts',(1.07653064752107,6.68348837523857,-17.2482108153378));
#43986=CARTESIAN_POINT('Ctrl Pts',(0.889366602281064,6.70830202411512,-17.2393355245785));
#43987=CARTESIAN_POINT('Ctrl Pts',(0.701670969067837,6.73318614933396,-17.2304350259977));
#43988=CARTESIAN_POINT('Ctrl Pts',(0.513093296472913,6.75016693239313,-17.221534527417));
#43989=CARTESIAN_POINT('Ctrl Pts',(0.324288389596506,6.75922525444839,-17.2126340288362));
#43990=CARTESIAN_POINT('Ctrl Pts',(0.135227897265158,6.76829583876634,-17.2037214816386));
#43991=CARTESIAN_POINT('Ctrl Pts',(-0.0540601844917341,6.76942253308639,
-17.194808934441));
#43992=CARTESIAN_POINT('Ctrl Pts',(-0.242922330392475,6.76263837133088,
-17.1858963872434));
#43993=CARTESIAN_POINT('Ctrl Pts',(-0.432201502356002,6.75583922948365,
-17.1769641602712));
#43994=CARTESIAN_POINT('Ctrl Pts',(-0.621052597054832,6.74109430213405,
-17.1680319332989));
#43995=CARTESIAN_POINT('Ctrl Pts',(-0.808825609984669,6.71848867920702,
-17.1590997063267));
#43996=CARTESIAN_POINT('Ctrl Pts',(-0.986292790456334,6.6971237551369,-17.1506577203812));
#43997=CARTESIAN_POINT('Ctrl Pts',(-1.16279686929245,6.66873778765191,-17.1422157344357));
#43998=CARTESIAN_POINT('Ctrl Pts',(-1.33779861920414,6.6334443432093,-17.1337737484903));
#43999=CARTESIAN_POINT('Ctrl Pts',(-1.50828100612134,6.59906234043424,-17.1255497740727));
#44000=CARTESIAN_POINT('Ctrl Pts',(-1.67766311369186,6.55805832572131,-17.1173257996551));
#44001=CARTESIAN_POINT('Ctrl Pts',(-1.84539273303507,6.51051569853429,-17.1091018252375));
#44002=CARTESIAN_POINT('Ctrl Pts',(-2.01294521362656,6.46302328097431,-17.1008865361348));
#44003=CARTESIAN_POINT('Ctrl Pts',(-2.17884833909721,6.40900609891225,-17.0926712470321));
#44004=CARTESIAN_POINT('Ctrl Pts',(-2.34255909327287,6.34859873472285,-17.0844559579294));
#44005=CARTESIAN_POINT('Ctrl Pts',(-2.50612978989543,6.28824305014156,-17.0762476971573));
#44006=CARTESIAN_POINT('Ctrl Pts',(-2.66751151617282,6.22150819478933,-17.0680394363851));
#44007=CARTESIAN_POINT('Ctrl Pts',(-2.82617536416221,6.14857884482281,-17.0598311756129));
#44008=CARTESIAN_POINT('Ctrl Pts',(-2.9847352878433,6.07569726334513,-17.0516282912251));
#44009=CARTESIAN_POINT('Ctrl Pts',(-3.14058055455183,5.99662941834599,-17.0434254068372));
#44010=CARTESIAN_POINT('Ctrl Pts',(-3.29320114934089,5.91160851122432,-17.0352225224494));
#44011=CARTESIAN_POINT('Ctrl Pts',(-3.44575237560108,5.82662624748011,-17.0270233664052));
#44012=CARTESIAN_POINT('Ctrl Pts',(-3.59508153730921,5.73569648635172,-17.0188242103609));
#44013=CARTESIAN_POINT('Ctrl Pts',(-3.74070211966927,5.63909892198229,-17.0106250543167));
#44014=CARTESIAN_POINT('Ctrl Pts',(-3.88631003657973,5.54250975925199,-17.0024266113997));
#44015=CARTESIAN_POINT('Ctrl Pts',(-4.02820971331193,5.44025396615212,-16.9942281684826));
#44016=CARTESIAN_POINT('Ctrl Pts',(-4.16594229225302,5.33265541898383,-16.9860297255656));
#44017=CARTESIAN_POINT('Ctrl Pts',(-4.30367349954042,5.2250579433699,-16.9778313642954));
#44018=CARTESIAN_POINT('Ctrl Pts',(-4.43723740837643,5.11211803965734,-16.9696330030252));
#44019=CARTESIAN_POINT('Ctrl Pts',(-4.56620713172781,4.99420077992045,-16.9614346417549));
#44020=CARTESIAN_POINT('Ctrl Pts',(-4.69519899896738,4.87626327398511,-16.9532348728397));
#44021=CARTESIAN_POINT('Ctrl Pts',(-4.81959484443921,4.75334695145079,-16.9450351039244));
#44022=CARTESIAN_POINT('Ctrl Pts',(-4.93900360107153,4.62585477815749,-16.9368353350091));
#44023=CARTESIAN_POINT('Ctrl Pts',(-5.05845455167121,4.49831755456176,-16.9286326686448));
#44024=CARTESIAN_POINT('Ctrl Pts',(-5.17291465799895,4.36620152093371,-16.9204300022805));
#44025=CARTESIAN_POINT('Ctrl Pts',(-5.28203217332817,4.22994386723112,-16.9122273359162));
#44026=CARTESIAN_POINT('Ctrl Pts',(-5.39127361888083,4.09353145889158,-16.9040153533732));
#44027=CARTESIAN_POINT('Ctrl Pts',(-5.49516012661644,3.95296831338133,-16.8958033708302));
#44028=CARTESIAN_POINT('Ctrl Pts',(-5.59338184206356,3.8087226951924,-16.8875913882871));
#44029=CARTESIAN_POINT('Ctrl Pts',(-5.69166149000614,3.66439199898806,-16.8793745622058));
#44030=CARTESIAN_POINT('Ctrl Pts',(-5.78426949558031,3.51637480416475,-16.8711577361245));
#44031=CARTESIAN_POINT('Ctrl Pts',(-5.87094134858256,3.36516517893307,-16.8629409100432));
#44032=CARTESIAN_POINT('Ctrl Pts',(-5.95774686209968,3.2137223666209,-16.8547114124293));
#44033=CARTESIAN_POINT('Ctrl Pts',(-6.03859776317304,3.05907760323322,-16.8464819148154));
#44034=CARTESIAN_POINT('Ctrl Pts',(-6.11327662389944,2.90174739074315,-16.8382524172016));
#44035=CARTESIAN_POINT('Ctrl Pts',(-6.17984217838067,2.76150994296765,-16.8309169936769));
#44036=CARTESIAN_POINT('Ctrl Pts',(-6.24150455586689,2.61913929840205,-16.8235815701522));
#44037=CARTESIAN_POINT('Ctrl Pts',(-6.29814318430964,2.47501139996041,-16.8162461466275));
#44038=CARTESIAN_POINT('Ctrl Pts',(-6.36901475643026,2.29466503512352,-16.8070673756781));
#44039=CARTESIAN_POINT('Ctrl Pts',(-6.43221623805483,2.11106898827689,-16.7978886047287));
#44040=CARTESIAN_POINT('Ctrl Pts',(-6.48746710585673,1.92485312437777,-16.7887098337793));
#44041=CARTESIAN_POINT('Ctrl Pts',(-6.5424239752946,1.73962814372671,-16.7795799044817));
#44042=CARTESIAN_POINT('Ctrl Pts',(-6.58951450754699,1.55181133498299,-16.770449975184));
#44043=CARTESIAN_POINT('Ctrl Pts',(-6.6285078353735,1.36204731062915,-16.7613200458863));
#44044=CARTESIAN_POINT('Ctrl Pts',(-6.66736715134499,1.17293546525917,-16.7522214942327));
#44045=CARTESIAN_POINT('Ctrl Pts',(-6.69818470336403,0.981889947406345,
-16.7431229425791));
#44046=CARTESIAN_POINT('Ctrl Pts',(-6.72077875918299,0.789570687218579,
-16.7340243909255));
#44047=CARTESIAN_POINT('Ctrl Pts',(-6.74325216393855,0.598278401711175,
-16.7249744250566));
#44048=CARTESIAN_POINT('Ctrl Pts',(-6.75758956453549,0.405726136249686,
-16.7159244591878));
#44049=CARTESIAN_POINT('Ctrl Pts',(-6.76366008874744,0.212582228525706,
-16.7068744933189));
#44050=CARTESIAN_POINT('Ctrl Pts',(-6.7658277569075,0.143614230958435,-16.7036429234942));
#44051=CARTESIAN_POINT('Ctrl Pts',(-6.76694179617376,0.0745709569908315,
-16.7004113536695));
#44052=CARTESIAN_POINT('Ctrl Pts',(-6.76699777839932,0.00548335104101361,
-16.6971797838448));
#44053=CARTESIAN_POINT('Ctrl Pts',(-6.76699777839992,0.00548335030004697,
-16.6971797838101));
#44054=CARTESIAN_POINT('Ctrl Pts',(-6.76714103050534,-0.171303946887046,
-16.6889105655165));
#44055=CARTESIAN_POINT('Ctrl Pts',(-6.76035171325591,-0.348144388963959,
-16.680641347223));
#44056=CARTESIAN_POINT('Ctrl Pts',(-6.74664681532118,-0.524448042532959,
-16.6723721289294));
#44057=CARTESIAN_POINT('Ctrl Pts',(-6.7332601547828,-0.696657800915976,
-16.664294927717));
#44058=CARTESIAN_POINT('Ctrl Pts',(-6.71327559157909,-0.868355045356068,
-16.6562177265046));
#44059=CARTESIAN_POINT('Ctrl Pts',(-6.68676157954093,-1.03899402230006,
-16.6481405252923));
#44060=CARTESIAN_POINT('Ctrl Pts',(-6.66024189380405,-1.20966951405535,
-16.6400615956502));
#44061=CARTESIAN_POINT('Ctrl Pts',(-6.62719003316591,-1.37928592273975,
-16.6319826660081));
#44062=CARTESIAN_POINT('Ctrl Pts',(-6.58772579263647,-1.54730665384476,
-16.623903736366));
#44063=CARTESIAN_POINT('Ctrl Pts',(-6.54824546994387,-1.71539585546319,
-16.6158215144608));
#44064=CARTESIAN_POINT('Ctrl Pts',(-6.50234764835162,-1.88188772587341,
-16.6077392925556));
#44065=CARTESIAN_POINT('Ctrl Pts',(-6.45020227626436,-2.04625990413586,
-16.5996570706504));
#44066=CARTESIAN_POINT('Ctrl Pts',(-6.3959321649428,-2.21732966652132,-16.5912455268265));
#44067=CARTESIAN_POINT('Ctrl Pts',(-6.3348948134272,-2.3861029402516,-16.5828339830027));
#44068=CARTESIAN_POINT('Ctrl Pts',(-6.26733703151375,-2.55201401512931,
-16.5744224391789));
#44069=CARTESIAN_POINT('Ctrl Pts',(-6.20229412505351,-2.71174895932588,
-16.5663240196834));
#44070=CARTESIAN_POINT('Ctrl Pts',(-6.13120770860825,-2.86883066175132,
-16.5582256001879));
#44071=CARTESIAN_POINT('Ctrl Pts',(-6.05434470713789,-3.02278003949203,
-16.5501271806924));
#44072=CARTESIAN_POINT('Ctrl Pts',(-5.97741756226229,-3.17685789045306,
-16.5420220029362));
#44073=CARTESIAN_POINT('Ctrl Pts',(-5.89470440723982,-3.32779788958514,
-16.53391682518));
#44074=CARTESIAN_POINT('Ctrl Pts',(-5.80651557822335,-3.47514975790247,
-16.5258116474238));
#44075=CARTESIAN_POINT('Ctrl Pts',(-5.71819348913538,-3.62272428617259,
-16.5176942221236));
#44076=CARTESIAN_POINT('Ctrl Pts',(-5.62437941383026,-3.76669955783019,
-16.5095767968234));
#44077=CARTESIAN_POINT('Ctrl Pts',(-5.52542443370626,-3.90665762863882,
-16.5014593715231));
#44078=CARTESIAN_POINT('Ctrl Pts',(-5.51428713965884,-3.92240978367893,
-16.5005457626036));
#44079=CARTESIAN_POINT('Ctrl Pts',(-5.50308476279341,-3.93811108989045,
-16.499632153684));
#44080=CARTESIAN_POINT('Ctrl Pts',(-5.49181783252863,-3.95376098092949,
-16.4987185447644));
#44081=CARTESIAN_POINT('Ctrl Pts',(-5.38904210163831,-4.09651761047212,
-16.4903847020717));
#44082=CARTESIAN_POINT('Ctrl Pts',(-5.28056508301162,-4.23544695578761,
-16.482050859379));
#44083=CARTESIAN_POINT('Ctrl Pts',(-5.16669771029274,-4.37007136903458,
-16.4737170166864));
#44084=CARTESIAN_POINT('Ctrl Pts',(-5.05296454467821,-4.50453711037893,
-16.4653929964816));
#44085=CARTESIAN_POINT('Ctrl Pts',(-4.93385390387229,-4.63470776401472,
-16.4570689762769));
#44086=CARTESIAN_POINT('Ctrl Pts',(-4.80971948974867,-4.76013523231555,
-16.4487449560721));
#44087=CARTESIAN_POINT('Ctrl Pts',(-4.68570862387184,-4.88543786542126,
-16.4404292205813));
#44088=CARTESIAN_POINT('Ctrl Pts',(-4.55668418961337,-5.00600647287748,
-16.4321134850904));
#44089=CARTESIAN_POINT('Ctrl Pts',(-4.42303971879279,-5.12142642688357,
-16.4237977495995));
#44090=CARTESIAN_POINT('Ctrl Pts',(-4.28950377425102,-5.23675265386877,
-16.4154887669194));
#44091=CARTESIAN_POINT('Ctrl Pts',(-4.15135553090812,-5.34693833201893,
-16.4071797842394));
#44092=CARTESIAN_POINT('Ctrl Pts',(-4.00902505034459,-5.45160592355221,
-16.3988708015593));
#44093=CARTESIAN_POINT('Ctrl Pts',(-3.8667840852522,-5.55620768681925,-16.3905670446222));
#44094=CARTESIAN_POINT('Ctrl Pts',(-3.72036640432536,-5.6552980742625,-16.382263287685));
#44095=CARTESIAN_POINT('Ctrl Pts',(-3.57023496746212,-5.74853992567772,
-16.3739595307479));
#44096=CARTESIAN_POINT('Ctrl Pts',(-3.42016448034264,-5.84174392314928,
-16.3656591449359));
#44097=CARTESIAN_POINT('Ctrl Pts',(-3.26638353648927,-5.92910393248157,
-16.3573587591238));
#44098=CARTESIAN_POINT('Ctrl Pts',(-3.10938412450249,-6.01032606156204,
-16.3490583733118));
#44099=CARTESIAN_POINT('Ctrl Pts',(-2.95241781960651,-6.09153106300892,
-16.3407597378351));
#44100=CARTESIAN_POINT('Ctrl Pts',(-2.79223470741902,-6.1666006030878,-16.3324611023585));
#44101=CARTESIAN_POINT('Ctrl Pts',(-2.62935164042987,-6.23528659734007,
-16.3241624668819));
#44102=CARTESIAN_POINT('Ctrl Pts',(-2.46647588452209,-6.30396950858991,
-16.3158642038933));
#44103=CARTESIAN_POINT('Ctrl Pts',(-2.30090073581917,-6.36626931002763,
-16.3075659409047));
#44104=CARTESIAN_POINT('Ctrl Pts',(-2.13316347627594,-6.42198587537238,
-16.2992676779161));
#44105=CARTESIAN_POINT('Ctrl Pts',(-1.96540590446547,-6.47770918775573,
-16.2909684100433));
#44106=CARTESIAN_POINT('Ctrl Pts',(-1.79548603032544,-6.52684756647184,
-16.2826691421704));
#44107=CARTESIAN_POINT('Ctrl Pts',(-1.6239569433732,-6.56925055436843,-16.2743698742976));
#44108=CARTESIAN_POINT('Ctrl Pts',(-1.4523074153562,-6.61168331599671,-16.2660647790011));
#44109=CARTESIAN_POINT('Ctrl Pts',(-1.27904675476757,-6.64737115321012,
-16.2577596837045));
#44110=CARTESIAN_POINT('Ctrl Pts',(-1.10473979741864,-6.67621441986396,
-16.249454588408));
#44111=CARTESIAN_POINT('Ctrl Pts',(-0.930369278689102,-6.70506820427266,
-16.2411464646419));
#44112=CARTESIAN_POINT('Ctrl Pts',(-0.754952047023796,-6.72707239400851,
-16.2328383408758));
#44113=CARTESIAN_POINT('Ctrl Pts',(-0.579058973178254,-6.74217915110402,
-16.2245302171097));
#44114=CARTESIAN_POINT('Ctrl Pts',(-0.402978926011551,-6.75730196659504,
-16.216213261856));
#44115=CARTESIAN_POINT('Ctrl Pts',(-0.226422373365127,-6.7655126780107,
-16.2078963066023));
#44116=CARTESIAN_POINT('Ctrl Pts',(-0.0499622079141649,-6.76681555665443,
-16.1995793513486));
#44117=CARTESIAN_POINT('Ctrl Pts',(0.0800862492438838,-6.76777575839202,
-16.1934498818662));
#44118=CARTESIAN_POINT('Ctrl Pts',(0.210082326238034,-6.76498508378958,
-16.1873204123838));
#44119=CARTESIAN_POINT('Ctrl Pts',(0.33979830046276,-6.75846329538029,-16.1811909429014));
#44120=CARTESIAN_POINT('Ctrl Pts',(0.518644569769884,-6.74947136101613,
-16.1727399193762));
#44121=CARTESIAN_POINT('Ctrl Pts',(0.697285007755008,-6.73336840077228,
-16.1642888958511));
#44122=CARTESIAN_POINT('Ctrl Pts',(0.875131619415711,-6.71017389109246,
-16.1558378723259));
#44123=CARTESIAN_POINT('Ctrl Pts',(1.052821642421,-6.68699980348899,-16.1473942896758));
#44124=CARTESIAN_POINT('Ctrl Pts',(1.22971890504705,-6.65674665439173,-16.1389507070256));
#44125=CARTESIAN_POINT('Ctrl Pts',(1.40523881389734,-6.61948584679478,-16.1305071243755));
#44126=CARTESIAN_POINT('Ctrl Pts',(1.58062804270633,-6.58225278103012,-16.1220698282358));
#44127=CARTESIAN_POINT('Ctrl Pts',(1.75464163879023,-6.53802252605743,-16.113632532096));
#44128=CARTESIAN_POINT('Ctrl Pts',(1.92670311366764,-6.48691792084526,-16.1051952359562));
#44129=CARTESIAN_POINT('Ctrl Pts',(2.09864183580343,-6.43584977487188,-16.0967639591839));
#44130=CARTESIAN_POINT('Ctrl Pts',(2.26863089768929,-6.37791715530852,-16.0883326824115));
#44131=CARTESIAN_POINT('Ctrl Pts',(2.43610673024851,-6.313293355994,-16.0799014056392));
#44132=CARTESIAN_POINT('Ctrl Pts',(2.60351077660312,-6.24869725677929,-16.0714737428173));
#44133=CARTESIAN_POINT('Ctrl Pts',(2.76840343250652,-6.17741581457886,-16.0630460799954));
#44134=CARTESIAN_POINT('Ctrl Pts',(2.93023832454289,-6.09967149618568,-16.0546184171735));
#44135=CARTESIAN_POINT('Ctrl Pts',(3.09202339739928,-6.02195111056832,-16.0461933487195));
#44136=CARTESIAN_POINT('Ctrl Pts',(3.25075228513535,-5.93777195975516,-16.0377682802655));
#44137=CARTESIAN_POINT('Ctrl Pts',(3.40590022582786,-5.84740392411075,-16.0293432118115));
#44138=CARTESIAN_POINT('Ctrl Pts',(3.44835345136134,-5.82267646346186,-16.0270378551976));
#44139=CARTESIAN_POINT('Ctrl Pts',(3.49053869454235,-5.79748588630927,-16.0247324985836));
#44140=CARTESIAN_POINT('Ctrl Pts',(3.5324455254156,-5.77183832153772,-16.0224271419697));
#44141=CARTESIAN_POINT('Ctrl Pts',(3.68912171694834,-5.67595030789503,-16.0138081534452));
#44142=CARTESIAN_POINT('Ctrl Pts',(3.84183429062203,-5.57371406158912,-16.0051891649207));
#44143=CARTESIAN_POINT('Ctrl Pts',(3.99008070006634,-5.46548671272359,-15.9965701763962));
#44144=CARTESIAN_POINT('Ctrl Pts',(4.13841592234035,-5.35719452601719,-15.9879460243284));
#44145=CARTESIAN_POINT('Ctrl Pts',(4.28227939498782,-5.24290425313291,-15.9793218722606));
#44146=CARTESIAN_POINT('Ctrl Pts',(4.42120079106756,-5.12301401179653,-15.9706977201927));
#44147=CARTESIAN_POINT('Ctrl Pts',(4.56488028233511,-4.99901749744198,-15.9617781885965));
#44148=CARTESIAN_POINT('Ctrl Pts',(4.70327290272848,-4.8690308621258,-15.9528586570003));
#44149=CARTESIAN_POINT('Ctrl Pts',(4.83589934889496,-4.73353636168112,-15.9439391254041));
#44150=CARTESIAN_POINT('Ctrl Pts',(4.96437261864278,-4.60228485032625,-15.9352989075449));
#44151=CARTESIAN_POINT('Ctrl Pts',(5.08743521275111,-4.46586546642328,-15.9266586896856));
#44152=CARTESIAN_POINT('Ctrl Pts',(5.20469187431502,-4.32475103253809,-15.9180184718263));
#44153=CARTESIAN_POINT('Ctrl Pts',(5.32763439881402,-4.17679385455178,-15.9089592833616));
#44154=CARTESIAN_POINT('Ctrl Pts',(5.44419368924396,-4.0236752821493,-15.899900094897));
#44155=CARTESIAN_POINT('Ctrl Pts',(5.55396432346168,-3.86597585270716,-15.8908409064323));
#44156=CARTESIAN_POINT('Ctrl Pts',(5.66373495767941,-3.70827642326501,-15.8817817179677));
#44157=CARTESIAN_POINT('Ctrl Pts',(5.76671675863962,-3.5459964775991,-15.872722529503));
#44158=CARTESIAN_POINT('Ctrl Pts',(5.86255851577539,-3.37974801562327,-15.8636633410384));
#44159=CARTESIAN_POINT('Ctrl Pts',(5.95823423379154,-3.21378756744321,-15.8546198469821));
#44160=CARTESIAN_POINT('Ctrl Pts',(6.04688350104808,-3.04371987375538,-15.8455763529259));
#44161=CARTESIAN_POINT('Ctrl Pts',(6.12818261729637,-2.87013358732074,-15.8365328588696));
#44162=CARTESIAN_POINT('Ctrl Pts',(6.20940736954039,-2.69670607962739,-15.8274976368643));
#44163=CARTESIAN_POINT('Ctrl Pts',(6.28329529268741,-2.51976662024883,-15.818462414859));
#44164=CARTESIAN_POINT('Ctrl Pts',(6.34956934387557,-2.33992695341448,-15.8094271928536));
#44165=CARTESIAN_POINT('Ctrl Pts',(6.41572663461302,-2.16040412492303,-15.8004078889426));
#44166=CARTESIAN_POINT('Ctrl Pts',(6.47429675723077,-1.97799151519004,-15.7913885850315));
#44167=CARTESIAN_POINT('Ctrl Pts',(6.52505138820639,-1.79331909633114,-15.7823692811204));
#44168=CARTESIAN_POINT('Ctrl Pts',(6.57574234395251,-1.60887836192006,-15.7733612925561));
#44169=CARTESIAN_POINT('Ctrl Pts',(6.61863731271837,-1.42218370513725,-15.7643533039917));
#44170=CARTESIAN_POINT('Ctrl Pts',(6.65355746626208,-1.23388088693688,-15.7553453154273));
#44171=CARTESIAN_POINT('Ctrl Pts',(6.68839875141585,-1.04600335724721,-15.7463576717207));
#44172=CARTESIAN_POINT('Ctrl Pts',(6.71530113041781,-0.856525149786348,
-15.737370028014));
#44173=CARTESIAN_POINT('Ctrl Pts',(6.73413666365722,-0.666102390918678,
-15.7283823843074));
#44174=CARTESIAN_POINT('Ctrl Pts',(6.75054110761511,-0.500257366175054,
-15.7205547695738));
#44175=CARTESIAN_POINT('Ctrl Pts',(6.76082741180869,-0.333696197191793,
-15.7127271548403));
#44176=CARTESIAN_POINT('Ctrl Pts',(6.76494249303895,-0.166859419500229,
-15.7048995401067));
#44177=CARTESIAN_POINT('Ctrl Pts',(6.76921294553139,0.00627653900395247,
-15.6967763816614));
#44178=CARTESIAN_POINT('Ctrl Pts',(6.76683378790335,0.179631959079449,-15.688653223216));
#44179=CARTESIAN_POINT('Ctrl Pts',(6.75780468430653,0.35265400715816,-15.6805300647707));
#44180=CARTESIAN_POINT('Ctrl Pts',(6.74877621730882,0.52566385627594,-15.6724074790506));
#44181=CARTESIAN_POINT('Ctrl Pts',(6.73309875733268,0.698340014688396,-15.6642848933305));
#44182=CARTESIAN_POINT('Ctrl Pts',(6.71082403943189,0.870132008251117,-15.6561623076104));
#44183=CARTESIAN_POINT('Ctrl Pts',(6.68854664499442,1.04194464439049,-15.648038745878));
#44184=CARTESIAN_POINT('Ctrl Pts',(6.65967046237651,1.21287254130438,-15.6399151841456));
#44185=CARTESIAN_POINT('Ctrl Pts',(6.62429880290322,1.38237273188348,-15.6317916224132));
#44186=CARTESIAN_POINT('Ctrl Pts',(6.5889013793734,1.55199638323761,-15.6236621436301));
#44187=CARTESIAN_POINT('Ctrl Pts',(6.546999104418,1.72018989260391,-15.615532664847));
#44188=CARTESIAN_POINT('Ctrl Pts',(6.49874605224474,1.8864222084235,-15.6074031860638));
#44189=CARTESIAN_POINT('Ctrl Pts',(6.45047332815091,2.05272229423413,-15.5992703930352));
#44190=CARTESIAN_POINT('Ctrl Pts',(6.39584478137198,2.21705924567967,-15.5911376000066));
#44191=CARTESIAN_POINT('Ctrl Pts',(6.33506354006774,2.37891970089458,-15.583004806978));
#44192=CARTESIAN_POINT('Ctrl Pts',(6.27421620838508,2.54095615479771,-15.5748631707708));
#44193=CARTESIAN_POINT('Ctrl Pts',(6.2072029614369,2.70051039701334,-15.5667215345636));
#44194=CARTESIAN_POINT('Ctrl Pts',(6.13427430235387,2.85709079020618,-15.5585798983564));
#44195=CARTESIAN_POINT('Ctrl Pts',(6.09711814113509,2.93686637371924,-15.5544318452961));
#44196=CARTESIAN_POINT('Ctrl Pts',(6.05842721108827,3.01587042163798,-15.5502837922357));
#44197=CARTESIAN_POINT('Ctrl Pts',(6.01823906458994,3.09404065284275,-15.5461357391753));
#44198=CARTESIAN_POINT('Ctrl Pts',(5.93646814879128,3.25309380534565,-15.5376956858989));
#44199=CARTESIAN_POINT('Ctrl Pts',(5.84832765968676,3.40902085888638,-15.5292556326224));
#44200=CARTESIAN_POINT('Ctrl Pts',(5.75408102651073,3.56129759221962,-15.5208155793459));
#44201=CARTESIAN_POINT('Ctrl Pts',(5.65990187834529,3.71346528826827,-15.5123815695435));
#44202=CARTESIAN_POINT('Ctrl Pts',(5.55962547525091,3.86198759124696,-15.5039475597412));
#44203=CARTESIAN_POINT('Ctrl Pts',(5.45356093673978,4.00636519918816,-15.4955135499388));
#44204=CARTESIAN_POINT('Ctrl Pts',(5.3475575192247,4.15065960775537,-15.4870844003384));
#44205=CARTESIAN_POINT('Ctrl Pts',(5.23577281199732,4.29081381430065,-15.4786552507379));
#44206=CARTESIAN_POINT('Ctrl Pts',(5.11855918845502,4.42635751315714,-15.4702261011375));
#44207=CARTESIAN_POINT('Ctrl Pts',(5.0013967416352,4.5618420321841,-15.4618006317941));
#44208=CARTESIAN_POINT('Ctrl Pts',(4.87881032196602,4.69271980509314,-15.4533751624506));
#44209=CARTESIAN_POINT('Ctrl Pts',(4.75119275114153,4.81855335567639,-15.4449496931071));
#44210=CARTESIAN_POINT('Ctrl Pts',(4.62360288746935,4.94435958643739,-15.436526053024));
#44211=CARTESIAN_POINT('Ctrl Pts',(4.49098428562376,5.06512354239626,-15.4281024129408));
#44212=CARTESIAN_POINT('Ctrl Pts',(4.35376717008197,5.1804440377941,-15.4196787728577));
#44213=CARTESIAN_POINT('Ctrl Pts',(4.21657229000281,5.29574584598549,-15.4112564977904));
#44214=CARTESIAN_POINT('Ctrl Pts',(4.074780638481,5.40560573954111,-15.4028342227231));
#44215=CARTESIAN_POINT('Ctrl Pts',(3.92885627539957,5.50966218267993,-15.3944119476558));
#44216=CARTESIAN_POINT('Ctrl Pts',(3.78290470038821,5.61373803023197,-15.3859881020053));
#44217=CARTESIAN_POINT('Ctrl Pts',(3.63281914390815,5.71200806910145,-15.3775642563547));
#44218=CARTESIAN_POINT('Ctrl Pts',(3.4790940583063,5.80415312801599,-15.3691404107042));
#44219=CARTESIAN_POINT('Ctrl Pts',(3.3547150239598,5.8787077356958,-15.3623246734847));
#44220=CARTESIAN_POINT('Ctrl Pts',(3.22795402870168,5.94925343469849,-15.3555089362653));
#44221=CARTESIAN_POINT('Ctrl Pts',(3.09908550384719,6.01564277861013,-15.3486931990458));
#44222=CARTESIAN_POINT('Origin',(0.,0.,-63.6971797838103));
#44223=CARTESIAN_POINT('',(3.09908550384713,6.01564277861016,-12.9539582652632));
#44224=CARTESIAN_POINT('',(3.09908550384717,6.01564277861014,-13.3487674371071));
#44225=CARTESIAN_POINT('',(3.09908550384721,6.01564277861012,-63.6971797838103));
#44226=CARTESIAN_POINT('',(-6.76699997822088,-0.000542916823992785,-14.302820216237));
#44227=CARTESIAN_POINT('Ctrl Pts',(-6.7669999782208,-0.000542917819759636,
-14.30282021619));
#44228=CARTESIAN_POINT('Ctrl Pts',(-6.76699920699295,-0.010155604417516,
-14.3023664227766));
#44229=CARTESIAN_POINT('Ctrl Pts',(-6.7669779531837,-0.0197681796252492,
-14.3019126293633));
#44230=CARTESIAN_POINT('Ctrl Pts',(-6.76693621826583,-0.0293805704865878,
-14.3014588359501));
#44231=CARTESIAN_POINT('Ctrl Pts',(-6.7661044973316,-0.220942627319672,
-14.2924153418939));
#44232=CARTESIAN_POINT('Ctrl Pts',(-6.75713396258636,-0.412518310869544,
-14.2833718478376));
#44233=CARTESIAN_POINT('Ctrl Pts',(-6.7400410938386,-0.603436039168142,
-14.2743283537814));
#44234=CARTESIAN_POINT('Ctrl Pts',(-6.72296385987539,-0.794179135718705,
-14.2652931317761));
#44235=CARTESIAN_POINT('Ctrl Pts',(-6.69777914608514,-0.984265241636963,
-14.2562579097708));
#44236=CARTESIAN_POINT('Ctrl Pts',(-6.66455537180709,-1.17302629813539,
-14.2472226877655));
#44237=CARTESIAN_POINT('Ctrl Pts',(-6.63139013058659,-1.3614547987451,-14.2382033838545));
#44238=CARTESIAN_POINT('Ctrl Pts',(-6.59021415199377,-1.54856267736042,
-14.2291840799434));
#44239=CARTESIAN_POINT('Ctrl Pts',(-6.54114712940774,-1.73369063890906,
-14.2201647760324));
#44240=CARTESIAN_POINT('Ctrl Pts',(-6.49214166482879,-1.91858634449908,
-14.211156787468));
#44241=CARTESIAN_POINT('Ctrl Pts',(-6.43526497380221,-2.10150686066446,
-14.2021487989037));
#44242=CARTESIAN_POINT('Ctrl Pts',(-6.37068746695663,-2.28180415425202,
-14.1931408103394));
#44243=CARTESIAN_POINT('Ctrl Pts',(-6.30625581067216,-2.46169424008687,
-14.1841531666328));
#44244=CARTESIAN_POINT('Ctrl Pts',(-6.23415813584952,-2.63897270573763,
-14.1751655229261));
#44245=CARTESIAN_POINT('Ctrl Pts',(-6.15461404537522,-2.81300816786409,
-14.1661778792195));
#44246=CARTESIAN_POINT('Ctrl Pts',(-6.08533665578346,-2.9645809929555,-14.1583502644858));
#44247=CARTESIAN_POINT('Ctrl Pts',(-6.01041179618313,-3.11369402552463,
-14.1505226497521));
#44248=CARTESIAN_POINT('Ctrl Pts',(-5.93001527222477,-3.25993985698832,
-14.1426950350184));
#44249=CARTESIAN_POINT('Ctrl Pts',(-5.84658325304866,-3.41170742621089,
-14.1345718765731));
#44250=CARTESIAN_POINT('Ctrl Pts',(-5.75729441569808,-3.56031854822074,
-14.1264487181278));
#44251=CARTESIAN_POINT('Ctrl Pts',(-5.66242665705949,-3.7052953125793,-14.1183255596825));
#44252=CARTESIAN_POINT('Ctrl Pts',(-5.56756558709448,-3.85026185531706,
-14.1102029739623));
#44253=CARTESIAN_POINT('Ctrl Pts',(-5.46712657976063,-3.99159424453248,
-14.1020803882422));
#44254=CARTESIAN_POINT('Ctrl Pts',(-5.36143134271823,-4.12884281092398,
-14.0939578025221));
#44255=CARTESIAN_POINT('Ctrl Pts',(-5.25572340530491,-4.26610786914378,
-14.0858342407897));
#44256=CARTESIAN_POINT('Ctrl Pts',(-5.14475820481112,-4.39928783815394,
-14.0777106790573));
#44257=CARTESIAN_POINT('Ctrl Pts',(-5.02889824193671,-4.52796548929493,
-14.0695871173249));
#44258=CARTESIAN_POINT('Ctrl Pts',(-4.91295388882835,-4.65673686683472,
-14.0614576385417));
#44259=CARTESIAN_POINT('Ctrl Pts',(-4.7921078977559,-4.78099910438522,-14.0533281597586));
#44260=CARTESIAN_POINT('Ctrl Pts',(-4.66676064117878,-4.90037081433075,
-14.0451986809755));
#44261=CARTESIAN_POINT('Ctrl Pts',(-4.54136228273138,-5.01979119002137,
-14.0370658879469));
#44262=CARTESIAN_POINT('Ctrl Pts',(-4.41145927526905,-5.13431682202207,
-14.0289330949184));
#44263=CARTESIAN_POINT('Ctrl Pts',(-4.27748548064466,-5.24360629365651,
-14.0208003018899));
#44264=CARTESIAN_POINT('Ctrl Pts',(-4.14336600984325,-5.35301460101147,
-14.0126586656827));
#44265=CARTESIAN_POINT('Ctrl Pts',(-4.00516720296143,-5.45717515617468,
-14.0045170294756));
#44266=CARTESIAN_POINT('Ctrl Pts',(-3.86335292998348,-5.55578915532151,
-13.9963753932684));
#44267=CARTESIAN_POINT('Ctrl Pts',(-3.79110048415139,-5.60603164842198,
-13.9922273402079));
#44268=CARTESIAN_POINT('Ctrl Pts',(-3.71790997768687,-5.65483510546349,
-13.9880792871475));
#44269=CARTESIAN_POINT('Ctrl Pts',(-3.64384520217837,-5.70216460149667,
-13.983931234087));
#44270=CARTESIAN_POINT('Ctrl Pts',(-3.49313361511055,-5.79847358796571,
-13.9754905191089));
#44271=CARTESIAN_POINT('Ctrl Pts',(-3.33849008577207,-5.88887498709142,
-13.9670498041309));
#44272=CARTESIAN_POINT('Ctrl Pts',(-3.18040616753894,-5.97304826780098,
-13.9586090891528));
#44273=CARTESIAN_POINT('Ctrl Pts',(-3.02244173657929,-6.05715792637918,
-13.9501747540648));
#44274=CARTESIAN_POINT('Ctrl Pts',(-2.86104239372446,-6.13504869453032,
-13.9417404189767));
#44275=CARTESIAN_POINT('Ctrl Pts',(-2.69672658276436,-6.20644461328804,
-13.9333060838887));
#44276=CARTESIAN_POINT('Ctrl Pts',(-2.53250973686716,-6.27779753130499,
-13.9248768286801));
#44277=CARTESIAN_POINT('Ctrl Pts',(-2.36538022983778,-6.34266326606286,
-13.9164475734715));
#44278=CARTESIAN_POINT('Ctrl Pts',(-2.19587925359299,-6.40081270649594,
-13.9080183182628));
#44279=CARTESIAN_POINT('Ctrl Pts',(-2.02645436518907,-6.45893604403883,
-13.8995928468898));
#44280=CARTESIAN_POINT('Ctrl Pts',(-1.85466044499256,-6.51034899063576,
-13.8911673755168));
#44281=CARTESIAN_POINT('Ctrl Pts',(-1.68105709881265,-6.55487116811091,
-13.8827419041438));
#44282=CARTESIAN_POINT('Ctrl Pts',(-1.50750507481849,-6.5993801835387,-13.8743189235846));
#44283=CARTESIAN_POINT('Ctrl Pts',(-1.33214501420962,-6.63700240957085,
-13.8658959430253));
#44284=CARTESIAN_POINT('Ctrl Pts',(-1.15555044746035,-6.66760767917356,
-13.8574729624661));
#44285=CARTESIAN_POINT('Ctrl Pts',(-0.978952956671259,-6.69821345553606,
-13.8490498424398));
#44286=CARTESIAN_POINT('Ctrl Pts',(-0.801121246206729,-6.72180197989719,
-13.8406267224134));
#44287=CARTESIAN_POINT('Ctrl Pts',(-0.622638443870925,-6.73829432187508,
-13.8322036023871));
#44288=CARTESIAN_POINT('Ctrl Pts',(-0.444149469302229,-6.75478723418566,
-13.8237801910752));
#44289=CARTESIAN_POINT('Ctrl Pts',(-0.26500969004412,-6.76418344396783,
-13.8153567797634));
#44290=CARTESIAN_POINT('Ctrl Pts',(-0.0858069133771682,-6.76645595371881,
-13.8069333684515));
#44291=CARTESIAN_POINT('Ctrl Pts',(0.0934270528844234,-6.76872885899189,
-13.7985084910754));
#44292=CARTESIAN_POINT('Ctrl Pts',(0.272723704955782,-6.76387558810306,
-13.7900836136993));
#44293=CARTESIAN_POINT('Ctrl Pts',(0.451495305415063,-6.75192128132343,
-13.7816587363232));
#44294=CARTESIAN_POINT('Ctrl Pts',(0.630322960452874,-6.7399632262212,-13.7732312172917));
#44295=CARTESIAN_POINT('Ctrl Pts',(0.808624903030451,-6.72089971831177,
-13.7648036982603));
#44296=CARTESIAN_POINT('Ctrl Pts',(0.985818212988376,-6.6948077979088,-13.7563761792288));
#44297=CARTESIAN_POINT('Ctrl Pts',(1.1631704230581,-6.66869247928007,-13.7479411027241));
#44298=CARTESIAN_POINT('Ctrl Pts',(1.33941168375111,-6.63553620287084,-13.7395060262193));
#44299=CARTESIAN_POINT('Ctrl Pts',(1.51396783584278,-6.59546741270348,-13.7310709497145));
#44300=CARTESIAN_POINT('Ctrl Pts',(1.68860835207155,-6.55537925702613,-13.7226317964817));
#44301=CARTESIAN_POINT('Ctrl Pts',(1.86156181245422,-6.50837200707619,-13.714192643249));
#44302=CARTESIAN_POINT('Ctrl Pts',(2.03226840845491,-6.45462424281973,-13.7057534900162));
#44303=CARTESIAN_POINT('Ctrl Pts',(2.20316470734511,-6.40081674972782,-13.6973049585181));
#44304=CARTESIAN_POINT('Ctrl Pts',(2.37180883712501,-6.34025388296169,-13.68885642702));
#44305=CARTESIAN_POINT('Ctrl Pts',(2.53765904186203,-6.27316312455335,-13.6804078955219));
#44306=CARTESIAN_POINT('Ctrl Pts',(2.62929666100186,-6.23609330376793,-13.6757398077559));
#44307=CARTESIAN_POINT('Ctrl Pts',(2.72008169611202,-6.19703141223764,-13.6710717199899));
#44308=CARTESIAN_POINT('Ctrl Pts',(2.80992587884462,-6.15602189367447,-13.666403632224));
#44309=CARTESIAN_POINT('Ctrl Pts',(2.96853166898681,-6.08362603122422,-13.6581628566272));
#44310=CARTESIAN_POINT('Ctrl Pts',(3.12455680518312,-6.00499674285417,-13.6499220810305));
#44311=CARTESIAN_POINT('Ctrl Pts',(3.27747918214943,-5.92033945062081,-13.6416813054337));
#44312=CARTESIAN_POINT('Ctrl Pts',(3.43023218100444,-5.83577592551657,-13.6334496573893));
#44313=CARTESIAN_POINT('Ctrl Pts',(3.57988895507602,-5.74519786181873,-13.625218009345));
#44314=CARTESIAN_POINT('Ctrl Pts',(3.72594765005738,-5.64885856691703,-13.6169863613006));
#44315=CARTESIAN_POINT('Ctrl Pts',(3.87187059822284,-5.55260880966682,-13.6087623637423));
#44316=CARTESIAN_POINT('Ctrl Pts',(4.01420183182877,-5.4506086795835,-13.600538366184));
#44317=CARTESIAN_POINT('Ctrl Pts',(4.15246430348639,-5.34315723222434,-13.5923143686257));
#44318=CARTESIAN_POINT('Ctrl Pts',(4.29060461971304,-5.23580071863646,-13.5840976370012));
#44319=CARTESIAN_POINT('Ctrl Pts',(4.42468305888894,-5.12300270457643,-13.5758809053767));
#44320=CARTESIAN_POINT('Ctrl Pts',(4.55425187874156,-5.00510527611348,-13.5676641737522));
#44321=CARTESIAN_POINT('Ctrl Pts',(4.68375431569098,-4.88726825086783,-13.5594516518635));
#44322=CARTESIAN_POINT('Ctrl Pts',(4.80875147230765,-4.76433725338367,-13.5512391299748));
#44323=CARTESIAN_POINT('Ctrl Pts',(4.92882868868712,-4.63669459395104,-13.5430266080861));
#44324=CARTESIAN_POINT('Ctrl Pts',(5.04886575066748,-4.50909461883809,-13.5348168325042));
#44325=CARTESIAN_POINT('Ctrl Pts',(5.16398590643266,-4.37678637942024,-13.5266070569224));
#44326=CARTESIAN_POINT('Ctrl Pts',(5.27381132078866,-4.24018904681399,-13.5183972813405));
#44327=CARTESIAN_POINT('Ctrl Pts',(5.32178020849591,-4.18052688075415,-13.5148114646578));
#44328=CARTESIAN_POINT('Ctrl Pts',(5.36873950156936,-4.12004693476471,-13.511225647975));
#44329=CARTESIAN_POINT('Ctrl Pts',(5.41466008086364,-4.0587861743016,-13.5076398312923));
#44330=CARTESIAN_POINT('Ctrl Pts',(5.52810632655735,-3.90744219324369,-13.4987811137705));
#44331=CARTESIAN_POINT('Ctrl Pts',(5.63509275972133,-3.75148749632004,-13.4899223962488));
#44332=CARTESIAN_POINT('Ctrl Pts',(5.73528769752079,-3.59148493337598,-13.481063678727));
#44333=CARTESIAN_POINT('Ctrl Pts',(5.83567008395668,-3.4311830313345,-13.4721883879676));
#44334=CARTESIAN_POINT('Ctrl Pts',(5.92923544571463,-3.26681834914082,-13.4633130972081));
#44335=CARTESIAN_POINT('Ctrl Pts',(6.01569805499498,-3.09897820436505,-13.4544378064486));
#44336=CARTESIAN_POINT('Ctrl Pts',(6.10240623752637,-2.93066135584009,-13.4455373078679));
#44337=CARTESIAN_POINT('Ctrl Pts',(6.18197117859569,-2.75884952345563,-13.4366368092871));
#44338=CARTESIAN_POINT('Ctrl Pts',(6.25415411332366,-2.58415272899973,-13.4277363107063));
#44339=CARTESIAN_POINT('Ctrl Pts',(6.32643476218699,-2.40921944725936,-13.4188237635087));
#44340=CARTESIAN_POINT('Ctrl Pts',(6.39131335007299,-2.231393644381,-13.4099112163111));
#44341=CARTESIAN_POINT('Ctrl Pts',(6.44860064292124,-2.05130172039996,-13.4009986691135));
#44342=CARTESIAN_POINT('Ctrl Pts',(6.50601443170702,-1.87081213586222,-13.3920664421412));
#44343=CARTESIAN_POINT('Ctrl Pts',(6.55580331910349,-1.68804666991308,-13.3831342151689));
#44344=CARTESIAN_POINT('Ctrl Pts',(6.59782826630241,-1.50364595845598,-13.3742019881967));
#44345=CARTESIAN_POINT('Ctrl Pts',(6.63754669427166,-1.32936599230108,-13.3657600022514));
#44346=CARTESIAN_POINT('Ctrl Pts',(6.67033043952174,-1.15362561833584,-13.3573180163062));
#44347=CARTESIAN_POINT('Ctrl Pts',(6.69610462071256,-0.97697078179025,-13.3488760303609));
#44348=CARTESIAN_POINT('Ctrl Pts',(6.72121319209869,-0.804877998657023,
-13.3406520559434));
#44349=CARTESIAN_POINT('Ctrl Pts',(6.73971650077403,-0.631588486119616,
-13.3324280815258));
#44350=CARTESIAN_POINT('Ctrl Pts',(6.75150688791752,-0.457650240251565,
-13.3242041071083));
#44351=CARTESIAN_POINT('Ctrl Pts',(6.76328482326822,-0.283895690047411,
-13.3159888180056));
#44352=CARTESIAN_POINT('Ctrl Pts',(6.76836393060619,-0.109494125641494,
-13.3077735289029));
#44353=CARTESIAN_POINT('Ctrl Pts',(6.76668783666093,0.0649978552340806,
-13.2995582398003));
#44354=CARTESIAN_POINT('Ctrl Pts',(6.76501317664478,0.239340555020245,-13.2913499790281));
#44355=CARTESIAN_POINT('Ctrl Pts',(6.75659482862921,0.413773160664588,-13.2831417182559));
#44356=CARTESIAN_POINT('Ctrl Pts',(6.74142833678462,0.587735467704081,-13.2749334574838));
#44357=CARTESIAN_POINT('Ctrl Pts',(6.7262717789432,0.761583829994425,-13.2667305730959));
#44358=CARTESIAN_POINT('Ctrl Pts',(6.70437591250843,0.934962151308051,-13.258527688708));
#44359=CARTESIAN_POINT('Ctrl Pts',(6.67578833555443,1.1073116539057,-13.2503248043201));
#44360=CARTESIAN_POINT('Ctrl Pts',(6.64721375211669,1.27958282086594,-13.2421256482759));
#44361=CARTESIAN_POINT('Ctrl Pts',(6.61195357615987,1.45082574768838,-13.2339264922317));
#44362=CARTESIAN_POINT('Ctrl Pts',(6.57010709944948,1.62048810602347,-13.2257273361875));
#44363=CARTESIAN_POINT('Ctrl Pts',(6.52826426236501,1.79013570785894,-13.2175288932705));
#44364=CARTESIAN_POINT('Ctrl Pts',(6.47983634307929,1.9582026650894,-13.2093304503535));
#44365=CARTESIAN_POINT('Ctrl Pts',(6.42497355327282,2.12414779140833,-13.2011320074365));
#44366=CARTESIAN_POINT('Ctrl Pts',(6.37011130983481,2.29009126511018,-13.1929336461663));
#44367=CARTESIAN_POINT('Ctrl Pts',(6.30881443510904,2.4539126090888,-13.184735284896));
#44368=CARTESIAN_POINT('Ctrl Pts',(6.24128270340019,2.61508684678685,-13.1765369236258));
#44369=CARTESIAN_POINT('Ctrl Pts',(6.17373937660476,2.77628875783481,-13.1683371547105));
#44370=CARTESIAN_POINT('Ctrl Pts',(6.09995919866833,2.93484232625759,-13.1601373857953));
#44371=CARTESIAN_POINT('Ctrl Pts',(6.02018969564446,3.09024352251669,-13.15193761688));
#44372=CARTESIAN_POINT('Ctrl Pts',(5.94039200547652,3.2456996309382,-13.1437349505157));
#44373=CARTESIAN_POINT('Ctrl Pts',(5.8546009380752,3.39800082934557,-13.1355322841514));
#44374=CARTESIAN_POINT('Ctrl Pts',(5.76310949658806,3.54666856787275,-13.1273296177871));
#44375=CARTESIAN_POINT('Ctrl Pts',(5.67151414369185,3.69550515579111,-13.1191176352441));
#44376=CARTESIAN_POINT('Ctrl Pts',(5.57420567071083,3.8406997336901,-13.1109056527011));
#44377=CARTESIAN_POINT('Ctrl Pts',(5.47152045981557,3.98180271457786,-13.1026936701581));
#44378=CARTESIAN_POINT('Ctrl Pts',(5.36877468379513,4.12298891991076,-13.0944768440768));
#44379=CARTESIAN_POINT('Ctrl Pts',(5.26064607014841,4.26007843654286,-13.0862600179955));
#44380=CARTESIAN_POINT('Ctrl Pts',(5.14751058168329,4.39265566729952,-13.0780431919142));
#44381=CARTESIAN_POINT('Ctrl Pts',(5.03420062195521,4.52543735129366,-13.0698136943003));
#44382=CARTESIAN_POINT('Ctrl Pts',(4.91586860047096,4.6536925801889,-13.0615841966865));
#44383=CARTESIAN_POINT('Ctrl Pts',(4.79292747399547,4.77704251907176,-13.0533546990726));
#44384=CARTESIAN_POINT('Ctrl Pts',(4.68334299221497,4.88699139881323,-13.0460192755477));
#44385=CARTESIAN_POINT('Ctrl Pts',(4.57009711768723,4.99304337255841,-13.0386838520228));
#44386=CARTESIAN_POINT('Ctrl Pts',(4.45350313218971,5.0949581795709,-13.0313484284979));
#44387=CARTESIAN_POINT('Ctrl Pts',(4.32521708721857,5.2070930161994,-13.0232774077829));
#44388=CARTESIAN_POINT('Ctrl Pts',(4.19245880451748,5.31458421796954,-13.0152063870678));
#44389=CARTESIAN_POINT('Ctrl Pts',(4.05560399409322,5.41704395801761,-13.0071353663528));
#44390=CARTESIAN_POINT('Ctrl Pts',(3.91889938514553,5.51939124601379,-12.9990732037789));
#44391=CARTESIAN_POINT('Ctrl Pts',(3.77810748377986,5.6167178323874,-12.991011041205));
#44392=CARTESIAN_POINT('Ctrl Pts',(3.63364066539739,5.7086727454611,-12.9829488786311));
#44393=CARTESIAN_POINT('Ctrl Pts',(3.48933819013631,5.80052305210954,-12.9748958874433));
#44394=CARTESIAN_POINT('Ctrl Pts',(3.34136943327677,5.88701365279755,-12.9668428962555));
#44395=CARTESIAN_POINT('Ctrl Pts',(3.19017924681859,5.96783422802343,-12.9587899050677));
#44396=CARTESIAN_POINT('Ctrl Pts',(3.15994217896421,5.98399782484398,-12.9571793584662));
#44397=CARTESIAN_POINT('Ctrl Pts',(3.12957636278804,5.99993476827424,-12.9555688118647));
#44398=CARTESIAN_POINT('Ctrl Pts',(3.09908550384713,6.01564277861016,-12.9539582652632));
#44399=CARTESIAN_POINT('Ctrl Pts',(3.09908550384716,6.01564277861015,-14.9545069759344));
#44400=CARTESIAN_POINT('Ctrl Pts',(2.98625823505507,6.07376813046706,-14.948509330515));
#44401=CARTESIAN_POINT('Ctrl Pts',(2.87193152134139,6.12864783471719,-14.9425116850955));
#44402=CARTESIAN_POINT('Ctrl Pts',(2.75631524042156,6.18021158985838,-14.936514039676));
#44403=CARTESIAN_POINT('Ctrl Pts',(2.59566421314202,6.25186041100985,-14.9281801969833));
#44404=CARTESIAN_POINT('Ctrl Pts',(2.43201220990593,6.31733291208247,-14.9198463542906));
#44405=CARTESIAN_POINT('Ctrl Pts',(2.26586828330762,6.37637278730632,-14.9115125115979));
#44406=CARTESIAN_POINT('Ctrl Pts',(2.09992017834578,6.43534307656805,-14.9031884913932));
#44407=CARTESIAN_POINT('Ctrl Pts',(1.93148632585958,6.48789572786059,-14.8948644711884));
#44408=CARTESIAN_POINT('Ctrl Pts',(1.76109786767077,6.53382149285435,-14.8865404509837));
#44409=CARTESIAN_POINT('Ctrl Pts',(1.59087899336004,6.57970154894615,-14.8782247154928));
#44410=CARTESIAN_POINT('Ctrl Pts',(1.41870972295788,6.61896776939942,-14.8699089800019));
#44411=CARTESIAN_POINT('Ctrl Pts',(1.24513877598369,6.65145987197862,-14.8615932445111));
#44412=CARTESIAN_POINT('Ctrl Pts',(1.07170877766893,6.6839255892763,-14.8532842618311));
#44413=CARTESIAN_POINT('Ctrl Pts',(0.89687971125176,6.70962808611324,-14.844975279151));
#44414=CARTESIAN_POINT('Ctrl Pts',(0.721213200343631,6.72845751414469,-14.836666296471));
#44415=CARTESIAN_POINT('Ctrl Pts',(0.545657170832591,6.74727509984202,-14.8283625395338));
#44416=CARTESIAN_POINT('Ctrl Pts',(0.369265091352969,6.75922819436496,-14.8200587825967));
#44417=CARTESIAN_POINT('Ctrl Pts',(0.192606697121493,6.76425839691418,-14.8117550256595));
#44418=CARTESIAN_POINT('Ctrl Pts',(0.0160200219395562,6.76928655732242,
-14.8034546398475));
#44419=CARTESIAN_POINT('Ctrl Pts',(-0.160832405434871,6.76739741606613,
-14.7951542540354));
#44420=CARTESIAN_POINT('Ctrl Pts',(-0.33737753669317,6.75858457058391,-14.7868538682234));
#44421=CARTESIAN_POINT('Ctrl Pts',(-0.513885439177,6.74977358350149,-14.7785552327468));
#44422=CARTESIAN_POINT('Ctrl Pts',(-0.690085827485077,6.73404181825613,
-14.7702565972701));
#44423=CARTESIAN_POINT('Ctrl Pts',(-0.865407217231237,6.71143496939098,
-14.7619579617935));
#44424=CARTESIAN_POINT('Ctrl Pts',(-1.04072073759645,6.6888291352446,-14.7536596988049));
#44425=CARTESIAN_POINT('Ctrl Pts',(-1.21515499313482,6.65934887707142,-14.7453614358164));
#44426=CARTESIAN_POINT('Ctrl Pts',(-1.38814497762178,6.62309161352185,-14.7370631728278));
#44427=CARTESIAN_POINT('Ctrl Pts',(-1.56115591045733,6.58682995937245,-14.728763904955));
#44428=CARTESIAN_POINT('Ctrl Pts',(-1.73272188349723,6.54378973649846,-14.7204646370822));
#44429=CARTESIAN_POINT('Ctrl Pts',(-1.90228922373603,6.49411924045577,-14.7121653692094));
#44430=CARTESIAN_POINT('Ctrl Pts',(-2.07197562757813,6.44441386771908,-14.7038602739129));
#44431=CARTESIAN_POINT('Ctrl Pts',(-2.23966026028805,6.38806901715204,-14.6955551786164));
#44432=CARTESIAN_POINT('Ctrl Pts',(-2.40480486629651,6.32528280435244,-14.6872500833199));
#44433=CARTESIAN_POINT('Ctrl Pts',(-2.57000969261578,6.26247369643479,-14.6789419595538));
#44434=CARTESIAN_POINT('Ctrl Pts',(-2.73267232373408,6.19321867518292,-14.6706338357877));
#44435=CARTESIAN_POINT('Ctrl Pts',(-2.89227535886588,6.11776366399498,-14.6623257120216));
#44436=CARTESIAN_POINT('Ctrl Pts',(-3.05204805110204,6.04222844456603,-14.6540087567679));
#44437=CARTESIAN_POINT('Ctrl Pts',(-3.20875433785463,5.96048022283296,-14.6456918015142));
#44438=CARTESIAN_POINT('Ctrl Pts',(-3.36190129256284,5.87281097082686,-14.6373748462605));
#44439=CARTESIAN_POINT('Ctrl Pts',(-3.47476826810658,5.80820006595472,-14.6312453767781));
#44440=CARTESIAN_POINT('Ctrl Pts',(-3.58570252880072,5.74037412915269,-14.6251159072956));
#44441=CARTESIAN_POINT('Ctrl Pts',(-3.69451722846025,5.66946482911839,-14.6189864378132));
#44442=CARTESIAN_POINT('Ctrl Pts',(-3.84454580586621,5.57169842952086,-14.610535414288));
#44443=CARTESIAN_POINT('Ctrl Pts',(-3.99081822580794,5.46789047907122,-14.6020843907628));
#44444=CARTESIAN_POINT('Ctrl Pts',(-4.13283616202823,5.35835368913175,-14.5936333672377));
#44445=CARTESIAN_POINT('Ctrl Pts',(-4.27472905567653,5.24891334308032,-14.5851897845876));
#44446=CARTESIAN_POINT('Ctrl Pts',(-4.41237467072089,5.13375441284117,-14.5767462019374));
#44447=CARTESIAN_POINT('Ctrl Pts',(-4.54530375002421,5.01323277137776,-14.5683026192873));
#44448=CARTESIAN_POINT('Ctrl Pts',(-4.67813385948723,4.89280086203067,-14.5598653231475));
#44449=CARTESIAN_POINT('Ctrl Pts',(-4.80625418865864,4.76701442265624,-14.5514280270077));
#44450=CARTESIAN_POINT('Ctrl Pts',(-4.92922836711494,4.63626969716274,-14.5429907308679));
#44451=CARTESIAN_POINT('Ctrl Pts',(-5.05211481287109,4.50561824806221,-14.5345594540955));
#44452=CARTESIAN_POINT('Ctrl Pts',(-5.16986220454636,4.37001580957461,-14.5261281773232));
#44453=CARTESIAN_POINT('Ctrl Pts',(-5.28207072526785,4.22989572605145,-14.5176969005509));
#44454=CARTESIAN_POINT('Ctrl Pts',(-5.39423114935557,4.08983570306824,-14.509269237729));
#44455=CARTESIAN_POINT('Ctrl Pts',(-5.50085722866169,3.94526215367283,-14.5008415749071));
#44456=CARTESIAN_POINT('Ctrl Pts',(-5.60158875020747,3.79664226304627,-14.4924139120852));
#44457=CARTESIAN_POINT('Ctrl Pts',(-5.70228926260703,3.6480681234999,-14.4839888436312));
#44458=CARTESIAN_POINT('Ctrl Pts',(-5.79709865021273,3.49545040088813,-14.4755637751773));
#44459=CARTESIAN_POINT('Ctrl Pts',(-5.88569923463785,3.33928637876171,-14.4671387067233));
#44460=CARTESIAN_POINT('Ctrl Pts',(-5.90994306653303,3.29655512224604,-14.4648333501094));
#44461=CARTESIAN_POINT('Ctrl Pts',(-5.9337222751961,3.25355850429868,-14.4625279934954));
#44462=CARTESIAN_POINT('Ctrl Pts',(-5.95703093145548,3.21030706968705,-14.4602226368815));
#44463=CARTESIAN_POINT('Ctrl Pts',(-6.04408268935635,3.04877423086624,-14.4516127306046));
#44464=CARTESIAN_POINT('Ctrl Pts',(-6.12452935516968,2.8837560899616,-14.4430028243278));
#44465=CARTESIAN_POINT('Ctrl Pts',(-6.19811660568511,2.71581286953473,-14.434392918051));
#44466=CARTESIAN_POINT('Ctrl Pts',(-6.27174700067294,2.54777118338742,-14.4257779637549));
#44467=CARTESIAN_POINT('Ctrl Pts',(-6.33850983194855,2.37680127508355,-14.4171630094587));
#44468=CARTESIAN_POINT('Ctrl Pts',(-6.39819923629958,2.20348259185669,-14.4085480551625));
#44469=CARTESIAN_POINT('Ctrl Pts',(-6.45924455656327,2.0262267683098,-14.3997374019187));
#44470=CARTESIAN_POINT('Ctrl Pts',(-6.51289115985987,1.84651451363404,-14.390926748675));
#44471=CARTESIAN_POINT('Ctrl Pts',(-6.55897313549348,1.66498060285243,-14.3821160954312));
#44472=CARTESIAN_POINT('Ctrl Pts',(-6.60411423036851,1.48715316865601,-14.3734853340864));
#44473=CARTESIAN_POINT('Ctrl Pts',(-6.64199658241001,1.30757805290614,-14.3648545727416));
#44474=CARTESIAN_POINT('Ctrl Pts',(-6.67251620037296,1.12686137379909,-14.3562238113968));
#44475=CARTESIAN_POINT('Ctrl Pts',(-6.70399000391936,0.940494648544629,
-14.3473232122035));
#44476=CARTESIAN_POINT('Ctrl Pts',(-6.72763318165452,0.752914176868978,
-14.3384226130102));
#44477=CARTESIAN_POINT('Ctrl Pts',(-6.74338945277686,0.564789950492972,
-14.3295220138169));
#44478=CARTESIAN_POINT('Ctrl Pts',(-6.75914572389919,0.376665724116966,
-14.3206214146236));
#44479=CARTESIAN_POINT('Ctrl Pts',(-6.76701510487806,0.1879980978005,-14.3117208154303));
#44480=CARTESIAN_POINT('Ctrl Pts',(-6.76699997822088,-0.000542916824000972,
-14.302820216237));
#44481=CARTESIAN_POINT('',(-6.76699761007657,-0.00568728563850417,-14.6971797837756));
#44482=CARTESIAN_POINT('Ctrl Pts',(3.09908550384719,6.01564277861013,-15.3486931990458));
#44483=CARTESIAN_POINT('Ctrl Pts',(2.93975348353047,6.09772603598339,-15.3402662756962));
#44484=CARTESIAN_POINT('Ctrl Pts',(2.77719934489261,6.17345415443444,-15.3318393523467));
#44485=CARTESIAN_POINT('Ctrl Pts',(2.61196173671878,6.24259119964755,-15.3234124289971));
#44486=CARTESIAN_POINT('Ctrl Pts',(2.44657711471286,6.31178975689819,-15.3149780081153));
#44487=CARTESIAN_POINT('Ctrl Pts',(2.27850456010173,6.37438539343999,-15.3065435872335));
#44488=CARTESIAN_POINT('Ctrl Pts',(2.10830190077073,6.4301906733165,-15.2981091663517));
#44489=CARTESIAN_POINT('Ctrl Pts',(1.93802114287125,6.48602155979922,-15.2896708752824));
#44490=CARTESIAN_POINT('Ctrl Pts',(1.76560865014932,6.5350557792074,-15.2812325842131));
#44491=CARTESIAN_POINT('Ctrl Pts',(1.59163596375048,6.57715622126281,-15.2727942931438));
#44492=CARTESIAN_POINT('Ctrl Pts',(1.41746237657205,6.61930528021209,-15.2643462576757));
#44493=CARTESIAN_POINT('Ctrl Pts',(1.24172532122487,6.65450448902835,-15.2558982222075));
#44494=CARTESIAN_POINT('Ctrl Pts',(1.06500636527423,6.68266791348526,-15.2474501867393));
#44495=CARTESIAN_POINT('Ctrl Pts',(0.933624842107104,6.70360598197285,-15.2411695035969));
#44496=CARTESIAN_POINT('Ctrl Pts',(0.801700799415876,6.72065632612268,-15.2348888204545));
#44497=CARTESIAN_POINT('Ctrl Pts',(0.669474440955553,6.73380226713758,-15.2286081373122));
#44498=CARTESIAN_POINT('Ctrl Pts',(0.495982525609927,6.75105082871225,-15.2203673617154));
#44499=CARTESIAN_POINT('Ctrl Pts',(0.321584056323243,6.76161406804796,-15.2121265861186));
#44500=CARTESIAN_POINT('Ctrl Pts',(0.146833588963459,6.76540677987304,-15.2038858105218));
#44501=CARTESIAN_POINT('Ctrl Pts',(-0.0277233233071831,6.76919529085856,
-15.1956541624775));
#44502=CARTESIAN_POINT('Ctrl Pts',(-0.202631104760295,6.76622819874597,
-15.1874225144332));
#44503=CARTESIAN_POINT('Ctrl Pts',(-0.377328603778492,6.75647186960551,
-15.1791908663888));
#44504=CARTESIAN_POINT('Ctrl Pts',(-0.551863739105498,6.74672460798817,
-15.1709668688304));
#44505=CARTESIAN_POINT('Ctrl Pts',(-0.726188628068499,6.73020069545278,
-15.1627428712721));
#44506=CARTESIAN_POINT('Ctrl Pts',(-0.899740535828375,6.70691851509971,
-15.1545188737137));
#44507=CARTESIAN_POINT('Ctrl Pts',(-1.07313910980138,6.68365690464371,-15.1463021420892));
#44508=CARTESIAN_POINT('Ctrl Pts',(-1.24576571244587,6.6536489742404,-15.1380854104647));
#44509=CARTESIAN_POINT('Ctrl Pts',(-1.41706128043353,6.61696503901117,-15.1298686788402));
#44510=CARTESIAN_POINT('Ctrl Pts',(-1.588269087361,6.58029989831986,-15.1216561569515));
#44511=CARTESIAN_POINT('Ctrl Pts',(-1.75814687074162,6.53696563914039,-15.1134436350627));
#44512=CARTESIAN_POINT('Ctrl Pts',(-1.92614391507259,6.48708398422811,-15.105231113174));
#44513=CARTESIAN_POINT('Ctrl Pts',(-2.09408478038252,6.43721900998156,-15.0970213375922));
#44514=CARTESIAN_POINT('Ctrl Pts',(-2.26014581884749,6.38081110286614,-15.0888115620103));
#44515=CARTESIAN_POINT('Ctrl Pts',(-2.42378958927283,6.31803236988642,-15.0806017864285));
#44516=CARTESIAN_POINT('Ctrl Pts',(-2.49526493669721,6.29061225032474,-15.0770159697459));
#44517=CARTESIAN_POINT('Ctrl Pts',(-2.56627933281965,6.26197740065527,-15.0734301530634));
#44518=CARTESIAN_POINT('Ctrl Pts',(-2.63678901268566,6.23214511244565,-15.0698443363808));
#44519=CARTESIAN_POINT('Ctrl Pts',(-2.81098233927863,6.15844479877255,-15.060985618859));
#44520=CARTESIAN_POINT('Ctrl Pts',(-2.98191342115986,6.07750945654687,-15.0521269013372));
#44521=CARTESIAN_POINT('Ctrl Pts',(-3.14901240109173,5.98965857939921,-15.0432681838153));
#44522=CARTESIAN_POINT('Ctrl Pts',(-3.316423996375,5.90164334737133,-15.0343928930559));
#44523=CARTESIAN_POINT('Ctrl Pts',(-3.47998893290189,5.80668684568764,-15.0255176022965));
#44524=CARTESIAN_POINT('Ctrl Pts',(-3.63916475412043,5.7051528368982,-15.0166423115371));
#44525=CARTESIAN_POINT('Ctrl Pts',(-3.7987926704622,5.6033304486937,-15.0077418129564));
#44526=CARTESIAN_POINT('Ctrl Pts',(-3.95400630533589,5.49489330955781,-14.9988413143756));
#44527=CARTESIAN_POINT('Ctrl Pts',(-4.1042923612587,5.38024843416301,-14.9899408157948));
#44528=CARTESIAN_POINT('Ctrl Pts',(-4.25478185961625,5.26544836384718,-14.9810282685972));
#44529=CARTESIAN_POINT('Ctrl Pts',(-4.40033025217478,5.14442393342543,-14.9721157213996));
#44530=CARTESIAN_POINT('Ctrl Pts',(-4.54045880286092,5.01762123515943,-14.963203174202));
#44531=CARTESIAN_POINT('Ctrl Pts',(-4.68089677107267,4.89053854415143,-14.9542709472297));
#44532=CARTESIAN_POINT('Ctrl Pts',(-4.81589076726617,4.75765223995337,-14.9453387202575));
#44533=CARTESIAN_POINT('Ctrl Pts',(-4.94499826901006,4.61944597538357,-14.9364064932852));
#44534=CARTESIAN_POINT('Ctrl Pts',(-5.06701976695758,4.48882509587813,-14.9279645073399));
#44535=CARTESIAN_POINT('Ctrl Pts',(-5.18378341004267,4.35345262951812,-14.9195225213945));
#44536=CARTESIAN_POINT('Ctrl Pts',(-5.29494976727013,4.21376268459509,-14.9110805354492));
#44537=CARTESIAN_POINT('Ctrl Pts',(-5.40168110092664,4.07964572248637,-14.9029753457035));
#44538=CARTESIAN_POINT('Ctrl Pts',(-5.50347933923222,3.94126249702449,-14.8948701559579));
#44539=CARTESIAN_POINT('Ctrl Pts',(-5.59997854021005,3.79901689245874,-14.8867649662123));
#44540=CARTESIAN_POINT('Ctrl Pts',(-5.69634300185476,3.65696990174373,-14.878671093533));
#44541=CARTESIAN_POINT('Ctrl Pts',(-5.78742296033443,3.51107157932362,-14.8705772208538));
#44542=CARTESIAN_POINT('Ctrl Pts',(-5.87289225286514,3.36175929927123,-14.8624833481745));
#44543=CARTESIAN_POINT('Ctrl Pts',(-5.95829265641316,3.21256736619695,-14.8543959992261));
#44544=CARTESIAN_POINT('Ctrl Pts',(-6.03809121013814,3.05996727008916,-14.8463086502776));
#44545=CARTESIAN_POINT('Ctrl Pts',(-6.11200434243221,2.90442626315246,-14.8382213013291));
#44546=CARTESIAN_POINT('Ctrl Pts',(-6.18587232017185,2.7489802783674,-14.830138893054));
#44547=CARTESIAN_POINT('Ctrl Pts',(-6.25386187434581,2.59059729164678,-14.8220564847788));
#44548=CARTESIAN_POINT('Ctrl Pts',(-6.31573484108605,2.42977003378752,-14.8139740765036));
#44549=CARTESIAN_POINT('Ctrl Pts',(-6.37758207633992,2.2690096601365,-14.8058950295086));
#44550=CARTESIAN_POINT('Ctrl Pts',(-6.43331765589511,2.10580738396821,-14.7978159825136));
#44551=CARTESIAN_POINT('Ctrl Pts',(-6.48275117260066,1.94067674643275,-14.7897369355187));
#44552=CARTESIAN_POINT('Ctrl Pts',(-6.53218320338001,1.77555107257288,-14.7816581313724));
#44553=CARTESIAN_POINT('Ctrl Pts',(-6.57531343199198,1.60849750413756,-14.7735793272262));
#44554=CARTESIAN_POINT('Ctrl Pts',(-6.61200098781636,1.44004581076973,-14.76550052308));
#44555=CARTESIAN_POINT('Ctrl Pts',(-6.64868681141072,1.27160207097293,-14.7574221003805));
#44556=CARTESIAN_POINT('Ctrl Pts',(-6.67893049380477,1.10176070052763,-14.749343677681));
#44557=CARTESIAN_POINT('Ctrl Pts',(-6.70264216311613,0.931062314358147,
-14.7412652549814));
#44558=CARTESIAN_POINT('Ctrl Pts',(-6.72636607119617,0.760275822284553,
-14.7331826626072));
#44559=CARTESIAN_POINT('Ctrl Pts',(-6.74355118206697,0.588631798153986,
-14.725100070233));
#44560=CARTESIAN_POINT('Ctrl Pts',(-6.75415939711594,0.416677139222255,
-14.7170174778589));
#44561=CARTESIAN_POINT('Ctrl Pts',(-6.76283823491131,0.275996865855036,
-14.7104049131759));
#44562=CARTESIAN_POINT('Ctrl Pts',(-6.76711594140666,0.135108866044254,
-14.703792348493));
#44563=CARTESIAN_POINT('Ctrl Pts',(-6.76699761007719,-0.00568728490314065,
-14.6971797838101));
#44564=CARTESIAN_POINT('Ctrl Pts',(-6.76699761007657,-0.00568728563859448,
-14.6971797837755));
#44565=CARTESIAN_POINT('Ctrl Pts',(-6.76681707131456,-0.220500721906246,
-14.6870909586725));
#44566=CARTESIAN_POINT('Ctrl Pts',(-6.75640429646117,-0.434842481389935,
-14.6770021335695));
#44567=CARTESIAN_POINT('Ctrl Pts',(-6.73591575628249,-0.647864124848208,
-14.6669133084664));
#44568=CARTESIAN_POINT('Ctrl Pts',(-6.71520918628652,-0.863152648698912,
-14.6567171226303));
#44569=CARTESIAN_POINT('Ctrl Pts',(-6.68421135166224,-1.07709290079024,
-14.6465209367942));
#44570=CARTESIAN_POINT('Ctrl Pts',(-6.64313163371893,-1.28883323090414,
-14.636324750958));
#44571=CARTESIAN_POINT('Ctrl Pts',(-6.60159558463147,-1.50292566351396,
-14.626015301512));
#44572=CARTESIAN_POINT('Ctrl Pts',(-6.54975243440539,-1.71476912737992,
-14.6157058520659));
#44573=CARTESIAN_POINT('Ctrl Pts',(-6.48786653253983,-1.9235063961291,-14.6053964026199));
#44574=CARTESIAN_POINT('Ctrl Pts',(-6.46416841085701,-2.00343867545994,
-14.6014485796086));
#44575=CARTESIAN_POINT('Ctrl Pts',(-6.43899814227914,-2.08291570187134,
-14.5975007565974));
#44576=CARTESIAN_POINT('Ctrl Pts',(-6.41237240559593,-2.16189017573786,
-14.5935529335862));
#44577=CARTESIAN_POINT('Ctrl Pts',(-6.35793914863978,-2.32334440628553,
-14.5854820633998));
#44578=CARTESIAN_POINT('Ctrl Pts',(-6.29730466783117,-2.48303625918558,
-14.5774111932134));
#44579=CARTESIAN_POINT('Ctrl Pts',(-6.23059847689061,-2.64044155772637,
-14.569340323027));
#44580=CARTESIAN_POINT('Ctrl Pts',(-6.16397529661965,-2.79765097760813,
-14.5612794964112));
#44581=CARTESIAN_POINT('Ctrl Pts',(-6.09129558404343,-2.95257916573787,
-14.5532186697954));
#44582=CARTESIAN_POINT('Ctrl Pts',(-6.01273899688986,-3.10471556753271,
-14.5451578431796));
#44583=CARTESIAN_POINT('Ctrl Pts',(-5.93426294104238,-3.25669600859168,
-14.5371052800197));
#44584=CARTESIAN_POINT('Ctrl Pts',(-5.84992216950608,-3.40589003009599,
-14.5290527168598));
#44585=CARTESIAN_POINT('Ctrl Pts',(-5.75994490937173,-3.55180568739376,
-14.5210001536999));
#44586=CARTESIAN_POINT('Ctrl Pts',(-5.67004018662044,-3.69760371119268,
-14.5129540823121));
#44587=CARTESIAN_POINT('Ctrl Pts',(-5.57450821420038,-3.84012831526304,
-14.5049080109242));
#44588=CARTESIAN_POINT('Ctrl Pts',(-5.47362370943306,-3.97891096753022,
-14.4968619395363));
#44589=CARTESIAN_POINT('Ctrl Pts',(-5.37279846785594,-4.11761209387093,
-14.4888205947005));
#44590=CARTESIAN_POINT('Ctrl Pts',(-5.26662717206891,-4.25257534338023,
-14.4807792498646));
#44591=CARTESIAN_POINT('Ctrl Pts',(-5.15542846783685,-4.38336016236602,
-14.4727379050287));
#44592=CARTESIAN_POINT('Ctrl Pts',(-5.04208619474571,-4.51666611023683,
-14.4645415478077));
#44593=CARTESIAN_POINT('Ctrl Pts',(-4.92352091931624,-4.6456305533063,-14.4563451905866));
#44594=CARTESIAN_POINT('Ctrl Pts',(-4.80011422484727,-4.76982100590986,
-14.4481488333655));
#44595=CARTESIAN_POINT('Ctrl Pts',(-4.679079926891,-4.89162399486782,-14.440110044657));
#44596=CARTESIAN_POINT('Ctrl Pts',(-4.55338895451524,-5.00883462189334,
-14.4320712559485));
#44597=CARTESIAN_POINT('Ctrl Pts',(-4.42343927925482,-5.12108132553522,
-14.42403246724));
#44598=CARTESIAN_POINT('Ctrl Pts',(-4.29347569820182,-5.23334004059134,
-14.4159928183083));
#44599=CARTESIAN_POINT('Ctrl Pts',(-4.1592527894436,-5.34063353037173,-14.4079531693766));
#44600=CARTESIAN_POINT('Ctrl Pts',(-4.02120216050053,-5.44263007969363,
-14.3999135204449));
#44601=CARTESIAN_POINT('Ctrl Pts',(-3.88310942433789,-5.54465773927653,
-14.3918714193167));
#44602=CARTESIAN_POINT('Ctrl Pts',(-3.74118694428551,-5.64138502068034,
-14.3838293181885));
#44603=CARTESIAN_POINT('Ctrl Pts',(-3.59589575847288,-5.73252323974328,
-14.3757872170603));
#44604=CARTESIAN_POINT('Ctrl Pts',(-3.44570156597138,-5.82673701562805,
-14.3674737266155));
#44605=CARTESIAN_POINT('Ctrl Pts',(-3.29190769846732,-5.91497767892445,
-14.3591602361708));
#44606=CARTESIAN_POINT('Ctrl Pts',(-3.13505056623211,-5.99697815129985,
-14.350846745726));
#44607=CARTESIAN_POINT('Ctrl Pts',(-2.98304664800076,-6.07644150065646,
-14.3427904775552));
#44608=CARTESIAN_POINT('Ctrl Pts',(-2.82816656306412,-6.15004496431317,
-14.3347342093845));
#44609=CARTESIAN_POINT('Ctrl Pts',(-2.67091781100977,-6.21759495680048,
-14.3266779412137));
#44610=CARTESIAN_POINT('Ctrl Pts',(-2.50613805066523,-6.28838007546068,
-14.3182358396319));
#44611=CARTESIAN_POINT('Ctrl Pts',(-2.33875761612971,-6.35251746077792,
-14.3097937380502));
#44612=CARTESIAN_POINT('Ctrl Pts',(-2.16937641760564,-6.40984359861741,
-14.3013516364684));
#44613=CARTESIAN_POINT('Ctrl Pts',(-1.99999521908157,-6.46716973645689,
-14.2929095348866));
#44614=CARTESIAN_POINT('Ctrl Pts',(-1.82861372308746,-6.51768457945689,
-14.2844674333049));
#44615=CARTESIAN_POINT('Ctrl Pts',(-1.65584129774126,-6.561286352286,-14.2760253317231));
#44616=CARTESIAN_POINT('Ctrl Pts',(-1.48528445232515,-6.6043289895204,-14.2676914890304));
#44617=CARTESIAN_POINT('Ctrl Pts',(-1.31283006079866,-6.64077222487531,
-14.2593576463377));
#44618=CARTESIAN_POINT('Ctrl Pts',(-1.13902358334522,-6.67045083008513,
-14.251023803645));
#44619=CARTESIAN_POINT('Ctrl Pts',(-0.965421958813958,-6.70009445530403,
-14.2426997834403));
#44620=CARTESIAN_POINT('Ctrl Pts',(-0.790471762921994,-6.72298927521063,
-14.2343757632355));
#44621=CARTESIAN_POINT('Ctrl Pts',(-0.614732149518258,-6.7390202095222,
-14.2260517430308));
#44622=CARTESIAN_POINT('Ctrl Pts',(-0.439167445879287,-6.7550351885981,
-14.2177360075399));
#44623=CARTESIAN_POINT('Ctrl Pts',(-0.262815234340318,-6.76419986125205,
-14.2094202720491));
#44624=CARTESIAN_POINT('Ctrl Pts',(-0.0862435904396328,-6.76645040202824,
-14.2011045365582));
#44625=CARTESIAN_POINT('Ctrl Pts',(0.0901846680792544,-6.76869911524797,
-14.1927955538782));
#44626=CARTESIAN_POINT('Ctrl Pts',(0.266831657583918,-6.76404487987223,
-14.1844865711981));
#44627=CARTESIAN_POINT('Ctrl Pts',(0.443125236909414,-6.75247576999829,
-14.1761775885181));
#44628=CARTESIAN_POINT('Ctrl Pts',(0.619307940457356,-6.74091393624897,
-14.1678738315809));
#44629=CARTESIAN_POINT('Ctrl Pts',(0.795137330671534,-6.72244591771199,
-14.1595700746438));
#44630=CARTESIAN_POINT('Ctrl Pts',(0.970042096076698,-6.69711186496382,
-14.1512663177066));
#44631=CARTESIAN_POINT('Ctrl Pts',(1.14487585436354,-6.67178809723033,-14.1429659318946));
#44632=CARTESIAN_POINT('Ctrl Pts',(1.3187853921246,-6.63960389926502,-14.1346655460825));
#44633=CARTESIAN_POINT('Ctrl Pts',(1.49120504944879,-6.60065121791013,-14.1263651602705));
#44634=CARTESIAN_POINT('Ctrl Pts',(1.66358834795367,-6.56170675066217,-14.1180665247939));
#44635=CARTESIAN_POINT('Ctrl Pts',(1.83448205289264,-6.51599672014443,-14.1097678893172));
#44636=CARTESIAN_POINT('Ctrl Pts',(2.00333097766183,-6.46366413065689,-14.1014692538406));
#44637=CARTESIAN_POINT('Ctrl Pts',(2.17217232356975,-6.41133389014158,-14.093170990852));
#44638=CARTESIAN_POINT('Ctrl Pts',(2.33896874007954,-6.35238178613532,-14.0848727278634));
#44639=CARTESIAN_POINT('Ctrl Pts',(2.50318029140565,-6.28700067032908,-14.0765744648748));
#44640=CARTESIAN_POINT('Ctrl Pts',(2.66741172804957,-6.22161163714885,-14.068275197002));
#44641=CARTESIAN_POINT('Ctrl Pts',(2.82905735291413,-6.14979217006359,-14.0599759291292));
#44642=CARTESIAN_POINT('Ctrl Pts',(2.98759711893101,-6.07178330105375,-14.0516766612564));
#44643=CARTESIAN_POINT('Ctrl Pts',(3.14624820541665,-5.9937196572446,-14.0433715659599));
#44644=CARTESIAN_POINT('Ctrl Pts',(3.30178876297166,-5.90945808125631,-14.0350664706634));
#44645=CARTESIAN_POINT('Ctrl Pts',(3.45372247577024,-5.81928604386823,-14.0267613753669));
#44646=CARTESIAN_POINT('Ctrl Pts',(3.60571159150095,-5.72908112506642,-14.0184532516007));
#44647=CARTESIAN_POINT('Ctrl Pts',(3.75409094575897,-5.63296163296958,-14.0101451278346));
#44648=CARTESIAN_POINT('Ctrl Pts',(3.89839296576975,-5.53125856242835,-14.0018370040685));
#44649=CARTESIAN_POINT('Ctrl Pts',(4.04284837799412,-5.42944738211072,-13.9935200488149));
#44650=CARTESIAN_POINT('Ctrl Pts',(4.18321751622051,-5.32204097123177,-13.9852030935612));
#44651=CARTESIAN_POINT('Ctrl Pts',(4.31906481494099,-5.20941149500965,-13.9768861383075));
#44652=CARTESIAN_POINT('Ctrl Pts',(4.4191822072307,-5.12640528465051,-13.970756668825));
#44653=CARTESIAN_POINT('Ctrl Pts',(4.51684425808701,-5.04056303560228,-13.9646271993425));
#44654=CARTESIAN_POINT('Ctrl Pts',(4.61188946415114,-4.95204650326021,-13.95849772986));
#44655=CARTESIAN_POINT('Ctrl Pts',(4.742933313002,-4.83000408191801,-13.9500467063348));
#44656=CARTESIAN_POINT('Ctrl Pts',(4.86924074728128,-4.70265360701531,-13.9415956828097));
#44657=CARTESIAN_POINT('Ctrl Pts',(4.9903744377037,-4.57038860180549,-13.9331446592845));
#44658=CARTESIAN_POINT('Ctrl Pts',(5.11140147351199,-4.43824005200161,-13.9247010766344));
#44659=CARTESIAN_POINT('Ctrl Pts',(5.22726362225071,-4.30118583993763,-13.9162574939842));
#44660=CARTESIAN_POINT('Ctrl Pts',(5.33755959374235,-4.15965702711762,-13.9078139113341));
#44661=CARTESIAN_POINT('Ctrl Pts',(5.44777344644726,-4.01823358690768,-13.8993766151943));
#44662=CARTESIAN_POINT('Ctrl Pts',(5.55242918005835,-3.87234244769853,-13.8909393190545));
#44663=CARTESIAN_POINT('Ctrl Pts',(5.65116482608073,-3.7224488053522,-13.8825020229147));
#44664=CARTESIAN_POINT('Ctrl Pts',(5.74983003174796,-3.57266210069074,-13.8740707461424));
#44665=CARTESIAN_POINT('Ctrl Pts',(5.842583392462,-3.41887886478249,-13.8656394693701));
#44666=CARTESIAN_POINT('Ctrl Pts',(5.92910531318734,-3.26159457706406,-13.8572081925977));
#44667=CARTESIAN_POINT('Ctrl Pts',(6.01559014748542,-3.10437770708494,-13.8487805297758));
#44668=CARTESIAN_POINT('Ctrl Pts',(6.09584870711687,-2.94366306687168,-13.8403528669539));
#44669=CARTESIAN_POINT('Ctrl Pts',(6.16960621678527,-2.77997268508245,-13.831925204132));
#44670=CARTESIAN_POINT('Ctrl Pts',(6.24334102097504,-2.6163326936668,-13.8235001356781));
#44671=CARTESIAN_POINT('Ctrl Pts',(6.31057863024381,-2.44971908938091,-13.8150750672241));
#44672=CARTESIAN_POINT('Ctrl Pts',(6.37109133465156,-2.28067626057005,-13.8066499987701));
#44673=CARTESIAN_POINT('Ctrl Pts',(6.38764946282475,-2.23442096833673,-13.8043446421563));
#44674=CARTESIAN_POINT('Ctrl Pts',(6.40370434955022,-2.18798390844266,-13.8020392855424));
#44675=CARTESIAN_POINT('Ctrl Pts',(6.41925196146129,-2.14137648611247,-13.7997339289286));
#44676=CARTESIAN_POINT('Ctrl Pts',(6.47737949272454,-1.96712629167147,-13.7911149404041));
#44677=CARTESIAN_POINT('Ctrl Pts',(6.52838673323858,-1.79057136641632,-13.7824959518796));
#44678=CARTESIAN_POINT('Ctrl Pts',(6.57211915190241,-1.61230854776547,-13.7738769633551));
#44679=CARTESIAN_POINT('Ctrl Pts',(6.61587777018779,-1.43393893377768,-13.7652528112873));
#44680=CARTESIAN_POINT('Ctrl Pts',(6.65235279638334,-1.25385967983139,-13.7566286592195));
#44681=CARTESIAN_POINT('Ctrl Pts',(6.68144074299728,-1.0726782359198,-13.7480045071517));
#44682=CARTESIAN_POINT('Ctrl Pts',(6.71152495960808,-0.885291278812168,
-13.7390849755555));
#44683=CARTESIAN_POINT('Ctrl Pts',(6.73370706994347,-0.696725649066451,
-13.7301654439593));
#44684=CARTESIAN_POINT('Ctrl Pts',(6.74793089696959,-0.507658950204924,
-13.7212459123631));
#44685=CARTESIAN_POINT('Ctrl Pts',(6.76170930707696,-0.324512845448838,
-13.7126056945038));
#44686=CARTESIAN_POINT('Ctrl Pts',(6.76802035133266,-0.140896884559492,
-13.7039654766445));
#44687=CARTESIAN_POINT('Ctrl Pts',(6.76686608173633,0.0425726654844531,
-13.6953252587853));
#44688=CARTESIAN_POINT('Ctrl Pts',(6.76565584074674,0.234938790789733,-13.6862660703206));
#44689=CARTESIAN_POINT('Ctrl Pts',(6.75623830814933,0.427143565653001,-13.6772068818559));
#44690=CARTESIAN_POINT('Ctrl Pts',(6.73867711835929,0.618481765697974,-13.6681476933912));
#44691=CARTESIAN_POINT('Ctrl Pts',(6.72111592856926,0.809819965742948,-13.6590885049265));
#44692=CARTESIAN_POINT('Ctrl Pts',(6.69541116558886,1.00029121621086,-13.6500293164618));
#44693=CARTESIAN_POINT('Ctrl Pts',(6.66168820007291,1.18920112891359,-13.6409701279971));
#44694=CARTESIAN_POINT('Ctrl Pts',(6.62802365722869,1.37778376844662,-13.6319266339408));
#44695=CARTESIAN_POINT('Ctrl Pts',(6.58633849049111,1.56498435577368,-13.6228831398846));
#44696=CARTESIAN_POINT('Ctrl Pts',(6.53676408474523,1.75014407989311,-13.6138396458283));
#44697=CARTESIAN_POINT('Ctrl Pts',(6.48723502452701,1.93513443908993,-13.604804423823));
#44698=CARTESIAN_POINT('Ctrl Pts',(6.42983119410984,2.11808743230304,-13.5957692018176));
#44699=CARTESIAN_POINT('Ctrl Pts',(6.36473454466274,2.29835662506426,-13.5867339798123));
#44700=CARTESIAN_POINT('Ctrl Pts',(6.29975258134059,2.47830822275199,-13.5777146759012));
#44701=CARTESIAN_POINT('Ctrl Pts',(6.22710494354743,2.6555852381161,-13.5686953719901));
#44702=CARTESIAN_POINT('Ctrl Pts',(6.14702259456094,2.82955866204559,-13.559676068079));
#44703=CARTESIAN_POINT('Ctrl Pts',(6.06704071447482,3.00331382416315,-13.5506680795146));
#44704=CARTESIAN_POINT('Ctrl Pts',(5.97964283666695,3.17377345038416,-13.5416600909503));
#44705=CARTESIAN_POINT('Ctrl Pts',(5.88510795963793,3.34032832269619,-13.5326521023859));
#44706=CARTESIAN_POINT('Ctrl Pts',(5.79078659293997,3.50650702499514,-13.5236644586792));
#44707=CARTESIAN_POINT('Ctrl Pts',(5.68936051965363,3.66879837028608,-13.5146768149726));
#44708=CARTESIAN_POINT('Ctrl Pts',(5.58115434728841,3.82661797828627,-13.5056891712659));
#44709=CARTESIAN_POINT('Ctrl Pts',(5.48691427094528,3.96406791835236,-13.4978615565324));
#44710=CARTESIAN_POINT('Ctrl Pts',(5.38753211189394,4.09812618004806,-13.4900339417989));
#44711=CARTESIAN_POINT('Ctrl Pts',(5.28325092638908,4.22842153158942,-13.4822063270654));
#44712=CARTESIAN_POINT('Ctrl Pts',(5.17503689028484,4.36363082948576,-13.4740835024228));
#44713=CARTESIAN_POINT('Ctrl Pts',(5.06159440159116,4.49472655455563,-13.4659606777802));
#44714=CARTESIAN_POINT('Ctrl Pts',(4.94327913949059,4.62128557320116,-13.4578378531375));
#44715=CARTESIAN_POINT('Ctrl Pts',(4.82497424657797,4.74783350017325,-13.4497157403819));
#44716=CARTESIAN_POINT('Ctrl Pts',(4.70179768157302,4.8698452461068,-13.4415936276263));
#44717=CARTESIAN_POINT('Ctrl Pts',(4.57414341672341,4.98693302574297,-13.4334715148706));
#44718=CARTESIAN_POINT('Ctrl Pts',(4.44643674257854,5.10406887653462,-13.4253460675284));
#44719=CARTESIAN_POINT('Ctrl Pts',(4.31424896499503,5.21627647373275,-13.4172206201861));
#44720=CARTESIAN_POINT('Ctrl Pts',(4.17800905335186,5.32320667925921,-13.4090951728438));
#44721=CARTESIAN_POINT('Ctrl Pts',(4.04173783311935,5.43016145786307,-13.4009678582345));
#44722=CARTESIAN_POINT('Ctrl Pts',(3.90141291699111,5.53183620972697,-13.3928405436252));
#44723=CARTESIAN_POINT('Ctrl Pts',(3.75749377382145,5.62792408794691,-13.3847132290159));
#44724=CARTESIAN_POINT('Ctrl Pts',(3.61345871113064,5.7240893600464,-13.3765793682697));
#44725=CARTESIAN_POINT('Ctrl Pts',(3.46582394965658,5.81465857691305,-13.3684455075235));
#44726=CARTESIAN_POINT('Ctrl Pts',(3.31507565523197,5.89936966125096,-13.3603116467773));
#44727=CARTESIAN_POINT('Ctrl Pts',(3.24375774226913,5.93944585423782,-13.3564635768872));
#44728=CARTESIAN_POINT('Ctrl Pts',(3.17174330901091,5.9782115748284,-13.3526155069972));
#44729=CARTESIAN_POINT('Ctrl Pts',(3.09908550384717,6.01564277861014,-13.3487674371071));
#44730=CARTESIAN_POINT('Origin',(0.,0.,-63.6971797838103));
#44731=CARTESIAN_POINT('',(3.0990855038472,6.01564277861013,-10.9542570414832));
#44732=CARTESIAN_POINT('',(3.09908550384727,6.01564277861009,-11.3484335646661));
#44733=CARTESIAN_POINT('',(3.09908550384721,6.01564277861012,-63.6971797838103));
#44734=CARTESIAN_POINT('',(-6.76699969835648,0.00202050572450262,-12.3028202161486));
#44735=CARTESIAN_POINT('Ctrl Pts',(-6.76699969835648,0.00202050572450262,
-12.3028202161486));
#44736=CARTESIAN_POINT('Ctrl Pts',(-6.76705055160899,-0.168295242583025,
-12.294822198901));
#44737=CARTESIAN_POINT('Ctrl Pts',(-6.7606671827498,-0.338707913742557,
-12.2868241816533));
#44738=CARTESIAN_POINT('Ctrl Pts',(-6.74785397761637,-0.508680348319968,
-12.2788261644057));
#44739=CARTESIAN_POINT('Ctrl Pts',(-6.73504188905724,-0.678637971080195,
-12.270828844125));
#44740=CARTESIAN_POINT('Ctrl Pts',(-6.715801100073,-0.84815505553999,-12.2628315238443));
#44741=CARTESIAN_POINT('Ctrl Pts',(-6.69018805542417,-1.01669699668079,
-12.2548342035636));
#44742=CARTESIAN_POINT('Ctrl Pts',(-6.67171402995344,-1.13826193190081,
-12.2490659436558));
#44743=CARTESIAN_POINT('Ctrl Pts',(-6.6499260169178,-1.25931959581929,-12.243297683748));
#44744=CARTESIAN_POINT('Ctrl Pts',(-6.62486185616072,-1.37967184025286,
-12.2375294238403));
#44745=CARTESIAN_POINT('Ctrl Pts',(-6.58741075003943,-1.55950330247109,
-12.2289104353158));
#44746=CARTESIAN_POINT('Ctrl Pts',(-6.54264676604676,-1.73774349421691,
-12.2202914467914));
#44747=CARTESIAN_POINT('Ctrl Pts',(-6.4907366932037,-1.91379888689986,-12.2116724582669));
#44748=CARTESIAN_POINT('Ctrl Pts',(-6.43879552159444,-2.08995975247458,
-12.2030483061991));
#44749=CARTESIAN_POINT('Ctrl Pts',(-6.37969980329426,-2.26393291510661,
-12.1944241541314));
#44750=CARTESIAN_POINT('Ctrl Pts',(-6.313665777883,-2.43514136041198,-12.1858000020636));
#44751=CARTESIAN_POINT('Ctrl Pts',(-6.24537006933625,-2.61221374102931,
-12.1768804704674));
#44752=CARTESIAN_POINT('Ctrl Pts',(-6.16965249749903,-2.78632833563775,
-12.1679609388711));
#44753=CARTESIAN_POINT('Ctrl Pts',(-6.08680548758214,-2.95687131210337,
-12.1590414072748));
#44754=CARTESIAN_POINT('Ctrl Pts',(-6.00655281882438,-3.12207376193214,
-12.1504011894156));
#44755=CARTESIAN_POINT('Ctrl Pts',(-5.9196106539085,-3.28392465112468,-12.1417609715564));
#44756=CARTESIAN_POINT('Ctrl Pts',(-5.82629087306156,-3.44189245364808,
-12.1331207536971));
#44757=CARTESIAN_POINT('Ctrl Pts',(-5.72844594646879,-3.60752023268534,
-12.1240615652324));
#44758=CARTESIAN_POINT('Ctrl Pts',(-5.62358972766744,-3.76887864981842,
-12.1150023767676));
#44759=CARTESIAN_POINT('Ctrl Pts',(-5.51213207804354,-3.92539029323243,
-12.1059431883029));
#44760=CARTESIAN_POINT('Ctrl Pts',(-5.40067442841965,-4.08190193664644,
-12.0968839998381));
#44761=CARTESIAN_POINT('Ctrl Pts',(-5.2826156091448,-4.23356652475674,-12.0878248113733));
#44762=CARTESIAN_POINT('Ctrl Pts',(-5.15841337933328,-4.37984707585955,
-12.0787656229086));
#44763=CARTESIAN_POINT('Ctrl Pts',(-5.0344263211717,-4.52587420616965,-12.0697221288523));
#44764=CARTESIAN_POINT('Ctrl Pts',(-4.90420354310854,-4.66667101399946,
-12.060678634796));
#44765=CARTESIAN_POINT('Ctrl Pts',(-4.76819009904572,-4.80173428870886,
-12.0516351407398));
#44766=CARTESIAN_POINT('Ctrl Pts',(-4.63230106598284,-4.93667402153476,
-12.0425999187344));
#44767=CARTESIAN_POINT('Ctrl Pts',(-4.49063211060068,-5.06589052416948,
-12.0335646967291));
#44768=CARTESIAN_POINT('Ctrl Pts',(-4.34366575669864,-5.18891672645492,
-12.0245294747238));
#44769=CARTESIAN_POINT('Ctrl Pts',(-4.196958325518,-5.3117261833544,-12.0155101708127));
#44770=CARTESIAN_POINT('Ctrl Pts',(-4.0449723147111,-5.42836696512622,-12.0064908669016));
#44771=CARTESIAN_POINT('Ctrl Pts',(-3.88822383432558,-5.53841172306488,
-11.9974715629905));
#44772=CARTESIAN_POINT('Ctrl Pts',(-3.7316720058581,-5.64831842216772,-11.9884635744262));
#44773=CARTESIAN_POINT('Ctrl Pts',(-3.57036982584233,-5.75164547544265,
-11.9794555858618));
#44774=CARTESIAN_POINT('Ctrl Pts',(-3.40486495593366,-5.84800680846516,
-11.9704475972975));
#44775=CARTESIAN_POINT('Ctrl Pts',(-3.23973388457008,-5.94415050604221,
-11.9614599535908));
#44776=CARTESIAN_POINT('Ctrl Pts',(-3.07041927543412,-6.03335976694991,
-11.9524723098842));
#44777=CARTESIAN_POINT('Ctrl Pts',(-2.89749570565441,-6.11529293130871,
-11.9434846661775));
#44778=CARTESIAN_POINT('Ctrl Pts',(-2.74689126173724,-6.18665103866418,
-11.9356570514441));
#44779=CARTESIAN_POINT('Ctrl Pts',(-2.59354989145506,-6.2524906561159,-11.9278294367106));
#44780=CARTESIAN_POINT('Ctrl Pts',(-2.43786844108653,-6.31261328325713,
-11.9200018219772));
#44781=CARTESIAN_POINT('Ctrl Pts',(-2.27630899655625,-6.37500593325907,
-11.9118786635319));
#44782=CARTESIAN_POINT('Ctrl Pts',(-2.11230104511112,-6.43121228452732,
-11.9037555050867));
#44783=CARTESIAN_POINT('Ctrl Pts',(-1.94636493985081,-6.48104563484316,
-11.8956323466414));
#44784=CARTESIAN_POINT('Ctrl Pts',(-1.78044053395428,-6.53087547164702,
-11.8875097609213));
#44785=CARTESIAN_POINT('Ctrl Pts',(-1.61258859558895,-6.57433309724159,
-11.8793871752012));
#44786=CARTESIAN_POINT('Ctrl Pts',(-1.4433448121048,-6.61128162714085,-11.8712645894811));
#44787=CARTESIAN_POINT('Ctrl Pts',(-1.27408069223837,-6.64823459678622,
-11.8631410277488));
#44788=CARTESIAN_POINT('Ctrl Pts',(-1.10342475207964,-6.67867683642486,
-11.8550174660164));
#44789=CARTESIAN_POINT('Ctrl Pts',(-0.931923000236129,-6.7025225491326,
-11.8468939042841));
#44790=CARTESIAN_POINT('Ctrl Pts',(-0.760296329717402,-6.72638563061243,
-11.838764425501));
#44791=CARTESIAN_POINT('Ctrl Pts',(-0.587822979958832,-6.74364253827996,
-11.8306349467179));
#44792=CARTESIAN_POINT('Ctrl Pts',(-0.415054856188062,-6.75425928332298,
-11.8225054679348));
#44793=CARTESIAN_POINT('Ctrl Pts',(-0.242216297894182,-6.7648803566261,
-11.8143726749062));
#44794=CARTESIAN_POINT('Ctrl Pts',(-0.0690830917128784,-6.7688558628985,
-11.8062398818777));
#44795=CARTESIAN_POINT('Ctrl Pts',(0.103792972747499,-6.76620395929714,
-11.7981070888492));
#44796=CARTESIAN_POINT('Ctrl Pts',(0.276857013701378,-6.76354917215292,
-11.7899654526421));
#44797=CARTESIAN_POINT('Ctrl Pts',(0.44966298943481,-6.7542526014934,-11.781823816435));
#44798=CARTESIAN_POINT('Ctrl Pts',(0.621663590627383,-6.73838433009637,
-11.7736821802279));
#44799=CARTESIAN_POINT('Ctrl Pts',(0.709295560672166,-6.73029966135635,
-11.7695341271672));
#44800=CARTESIAN_POINT('Ctrl Pts',(0.796718609205389,-6.72050996055453,
-11.7653860741065));
#44801=CARTESIAN_POINT('Ctrl Pts',(0.883861440874248,-6.70902958357881,
-11.7612380210458));
#44802=CARTESIAN_POINT('Ctrl Pts',(1.06118506565371,-6.68566860230035,-11.7527973060677));
#44803=CARTESIAN_POINT('Ctrl Pts',(1.23771297400534,-6.65525591246259,-11.7443565910896));
#44804=CARTESIAN_POINT('Ctrl Pts',(1.41286268563528,-6.6178627993892,-11.7359158761115));
#44805=CARTESIAN_POINT('Ctrl Pts',(1.5878800108616,-6.58049794979232,-11.7274815410235));
#44806=CARTESIAN_POINT('Ctrl Pts',(1.76152089104537,-6.53616326397663,-11.7190472059354));
#44807=CARTESIAN_POINT('Ctrl Pts',(1.93321097312708,-6.48498144433591,-11.7106128708474));
#44808=CARTESIAN_POINT('Ctrl Pts',(2.10479764872785,-6.43383045077316,-11.7021836156387));
#44809=CARTESIAN_POINT('Ctrl Pts',(2.27443554992023,-6.37584064007484,-11.6937543604301));
#44810=CARTESIAN_POINT('Ctrl Pts',(2.44156308554208,-6.31118520559477,-11.6853251052214));
#44811=CARTESIAN_POINT('Ctrl Pts',(2.60861559874496,-6.24655879450139,-11.6768996338483));
#44812=CARTESIAN_POINT('Ctrl Pts',(2.77315968282938,-6.17527284576334,-11.6684741624753));
#44813=CARTESIAN_POINT('Ctrl Pts',(2.93465103840383,-6.09754969498366,-11.6600486911022));
#44814=CARTESIAN_POINT('Ctrl Pts',(3.09609465244811,-6.01984952142239,-11.6516257105429));
#44815=CARTESIAN_POINT('Ctrl Pts',(3.25448703761365,-5.93571608532095,-11.6432027299837));
#44816=CARTESIAN_POINT('Ctrl Pts',(3.40930557283041,-5.84541910482623,-11.6347797494244));
#44817=CARTESIAN_POINT('Ctrl Pts',(3.56412667152051,-5.75512062920109,-11.6263566293981));
#44818=CARTESIAN_POINT('Ctrl Pts',(3.71537351076483,-5.65865856750349,-11.6179335093717));
#44819=CARTESIAN_POINT('Ctrl Pts',(3.86254911897326,-5.55634801857469,-11.6095103893454));
#44820=CARTESIAN_POINT('Ctrl Pts',(4.00972981675929,-5.45403393157675,-11.6010869780335));
#44821=CARTESIAN_POINT('Ctrl Pts',(4.15283872885666,-5.34587114431071,-11.5926635667217));
#44822=CARTESIAN_POINT('Ctrl Pts',(4.2914087440828,-5.23221750228426,-11.5842401554098));
#44823=CARTESIAN_POINT('Ctrl Pts',(4.43000287691887,-5.11854407925251,-11.5758152780337));
#44824=CARTESIAN_POINT('Ctrl Pts',(4.5640562800505,-4.9993781076363,-11.5673904006576));
#44825=CARTESIAN_POINT('Ctrl Pts',(4.6931354683193,-4.87511727817941,-11.5589655232815));
#44826=CARTESIAN_POINT('Ctrl Pts',(4.82225512990375,-4.7508174862233,-11.55053800425));
#44827=CARTESIAN_POINT('Ctrl Pts',(4.94639722687289,-4.62141988261056,-11.5421104852186));
#44828=CARTESIAN_POINT('Ctrl Pts',(5.06516537921543,-4.48735876448467,-11.5336829661872));
#44829=CARTESIAN_POINT('Ctrl Pts',(5.18404003824691,-4.35317742552917,-11.5252478896824));
#44830=CARTESIAN_POINT('Ctrl Pts',(5.29753090195221,-4.21432446556266,-11.5168128131776));
#44831=CARTESIAN_POINT('Ctrl Pts',(5.40528139314174,-4.07126786897591,-11.5083777366728));
#44832=CARTESIAN_POINT('Ctrl Pts',(5.51308396085323,-3.92814213219398,-11.49993858344));
#44833=CARTESIAN_POINT('Ctrl Pts',(5.61514042889908,-3.78080897796015,-11.4914994302072));
#44834=CARTESIAN_POINT('Ctrl Pts',(5.71113748325057,-3.62976550859836,-11.4830602769744));
#44835=CARTESIAN_POINT('Ctrl Pts',(5.80724121724375,-3.47855418759468,-11.4746117454763));
#44836=CARTESIAN_POINT('Ctrl Pts',(5.89727191068491,-3.3236245984951,-11.4661632139782));
#44837=CARTESIAN_POINT('Ctrl Pts',(5.98096155049406,-3.16549963378796,-11.4577146824801));
#44838=CARTESIAN_POINT('Ctrl Pts',(6.02720279180377,-3.07813046041372,-11.4530465947143));
#44839=CARTESIAN_POINT('Ctrl Pts',(6.07150899249474,-2.98978616490185,-11.4483785069486));
#44840=CARTESIAN_POINT('Ctrl Pts',(6.11384123732871,-2.90055758859207,-11.4437104191828));
#44841=CARTESIAN_POINT('Ctrl Pts',(6.18857216521329,-2.74303855487194,-11.435469643586));
#44842=CARTESIAN_POINT('Ctrl Pts',(6.25731482406535,-2.58241210945067,-11.4272288679892));
#44843=CARTESIAN_POINT('Ctrl Pts',(6.31980203050053,-2.41917161344155,-11.4189880923925));
#44844=CARTESIAN_POINT('Ctrl Pts',(6.38222002558022,-2.25611192397901,-11.4107564443481));
#44845=CARTESIAN_POINT('Ctrl Pts',(6.4383962382608,-2.09044427844205,-11.4025247963037));
#44846=CARTESIAN_POINT('Ctrl Pts',(6.48810981337129,-1.92268563463587,-11.3942931482593));
#44847=CARTESIAN_POINT('Ctrl Pts',(6.53777718473113,-1.75508290555784,-11.386069150701));
#44848=CARTESIAN_POINT('Ctrl Pts',(6.58099377990189,-1.58539338761749,-11.3778451531427));
#44849=CARTESIAN_POINT('Ctrl Pts',(6.61758718147738,-1.41415306651943,-11.3696211555843));
#44850=CARTESIAN_POINT('Ctrl Pts',(6.65414825264026,-1.24306403691103,-11.3614044239598));
#44851=CARTESIAN_POINT('Ctrl Pts',(6.68409771903145,-1.07042728158184,-11.3531876923353));
#44852=CARTESIAN_POINT('Ctrl Pts',(6.70731329259347,-0.896792838396328,
-11.3449709607108));
#44853=CARTESIAN_POINT('Ctrl Pts',(6.73051697195755,-0.723247354565245,
-11.3367584388222));
#44854=CARTESIAN_POINT('Ctrl Pts',(6.74699358254226,-0.548705552672509,
-11.3285459169335));
#44855=CARTESIAN_POINT('Ctrl Pts',(6.75667204855774,-0.373726943420741,
-11.3203333950449));
#44856=CARTESIAN_POINT('Ctrl Pts',(6.76634727804768,-0.19880684785651,-11.312123619463));
#44857=CARTESIAN_POINT('Ctrl Pts',(6.76922887208773,-0.023450590776209,
-11.3039138438811));
#44858=CARTESIAN_POINT('Ctrl Pts',(6.7652976646355,0.151777827357827,-11.2957040682993));
#44859=CARTESIAN_POINT('Ctrl Pts',(6.76358061535384,0.228313047933185,-11.2921182516165));
#44860=CARTESIAN_POINT('Ctrl Pts',(6.76056454762015,0.304823847224531,-11.2885324349338));
#44861=CARTESIAN_POINT('Ctrl Pts',(6.75625098540567,0.381263192827391,-11.2849466182511));
#44862=CARTESIAN_POINT('Ctrl Pts',(6.745594381192,0.570105688180169,-11.2760879007293));
#44863=CARTESIAN_POINT('Ctrl Pts',(6.72702648891292,0.758316202631355,-11.2672291832076));
#44864=CARTESIAN_POINT('Ctrl Pts',(6.70065597101318,0.945250526646458,-11.2583704656858));
#44865=CARTESIAN_POINT('Ctrl Pts',(6.67423611810987,1.13253457475795,-11.2494951749264));
#44866=CARTESIAN_POINT('Ctrl Pts',(6.63998450378622,1.31853740427817,-11.240619884167));
#44867=CARTESIAN_POINT('Ctrl Pts',(6.59806070560644,1.50262567698419,-11.2317445934075));
#44868=CARTESIAN_POINT('Ctrl Pts',(6.55601783441344,1.6872368017762,-11.2228440948268));
#44869=CARTESIAN_POINT('Ctrl Pts',(6.50625923139748,1.86992223365413,-11.213943596246));
#44870=CARTESIAN_POINT('Ctrl Pts',(6.44899502480975,2.05006150395033,-11.2050430976653));
#44871=CARTESIAN_POINT('Ctrl Pts',(6.39165329958869,2.23044462901855,-11.1961305504676));
#44872=CARTESIAN_POINT('Ctrl Pts',(6.3267857597072,2.40827446230105,-11.18721800327));
#44873=CARTESIAN_POINT('Ctrl Pts',(6.25465097536171,2.58294989816039,-11.1783054560723));
#44874=CARTESIAN_POINT('Ctrl Pts',(6.18235691036745,2.75801103444154,-11.1693732291001));
#44875=CARTESIAN_POINT('Ctrl Pts',(6.10276360407996,2.92990360102342,-11.1604410021278));
#44876=CARTESIAN_POINT('Ctrl Pts',(6.01617719747231,3.09804792225915,-11.1515087751555));
#44877=CARTESIAN_POINT('Ctrl Pts',(5.93434304458952,3.25696372243466,-11.1430667892102));
#44878=CARTESIAN_POINT('Ctrl Pts',(5.84626283162006,3.41253148605386,-11.134624803265));
#44879=CARTESIAN_POINT('Ctrl Pts',(5.75223081267895,3.56428529689571,-11.1261828173197));
#44880=CARTESIAN_POINT('Ctrl Pts',(5.66063148459453,3.71211310346517,-11.1179592329599));
#44881=CARTESIAN_POINT('Ctrl Pts',(5.56320847393852,3.8566035721493,-11.1097356486001));
#44882=CARTESIAN_POINT('Ctrl Pts',(5.46023223800644,3.9972681805247,-11.1015120642403));
#44883=CARTESIAN_POINT('Ctrl Pts',(5.35736011285873,4.13779057450879,-11.0932967940688));
#44884=CARTESIAN_POINT('Ctrl Pts',(5.24894615066667,4.27449452244008,-11.0850815238973));
#44885=CARTESIAN_POINT('Ctrl Pts',(5.13530562095612,4.40691787753941,-11.0768662537259));
#44886=CARTESIAN_POINT('Ctrl Pts',(5.02175933092625,4.53923141675941,-11.0686577963037));
#44887=CARTESIAN_POINT('Ctrl Pts',(4.90299533665791,4.66727116144228,-11.0604493388815));
#44888=CARTESIAN_POINT('Ctrl Pts',(4.77937098021986,4.79060560194974,-11.0522408814593));
#44889=CARTESIAN_POINT('Ctrl Pts',(4.65583332537734,4.91385354418871,-11.0440381808829));
#44890=CARTESIAN_POINT('Ctrl Pts',(4.52744235295573,5.03240250484075,-11.0358354803064));
#44891=CARTESIAN_POINT('Ctrl Pts',(4.39459426022936,5.14585564196657,-11.02763277973));
#44892=CARTESIAN_POINT('Ctrl Pts',(4.26180254935955,5.25926062861938,-11.0194335604493));
#44893=CARTESIAN_POINT('Ctrl Pts',(4.12455775784663,5.36757386679171,-11.0112343411685));
#44894=CARTESIAN_POINT('Ctrl Pts',(3.98329151703703,5.47043670014569,-11.0030351218877));
#44895=CARTESIAN_POINT('Ctrl Pts',(3.84203836885357,5.57329000012062,-10.9948366625147));
#44896=CARTESIAN_POINT('Ctrl Pts',(3.69676479861999,5.67069368391839,-10.9866382031417));
#44897=CARTESIAN_POINT('Ctrl Pts',(3.54793421467625,5.76233041471327,-10.9784397437687));
#44898=CARTESIAN_POINT('Ctrl Pts',(3.40160079849206,5.85242961011947,-10.9703788430069));
#44899=CARTESIAN_POINT('Ctrl Pts',(3.25182909134223,5.93695369163598,-10.962317942245));
#44900=CARTESIAN_POINT('Ctrl Pts',(3.0990855038472,6.01564277861013,-10.9542570414832));
#44901=CARTESIAN_POINT('Ctrl Pts',(3.09908550384713,6.01564277861016,-12.9539582652632));
#44902=CARTESIAN_POINT('Ctrl Pts',(2.94677792813768,6.09410724489889,-12.9459132820467));
#44903=CARTESIAN_POINT('Ctrl Pts',(2.7913481699967,6.16685580942879,-12.9378682988301));
#44904=CARTESIAN_POINT('Ctrl Pts',(2.6332745528485,6.23363089453655,-12.9298233156135));
#44905=CARTESIAN_POINT('Ctrl Pts',(2.47528686967876,6.30036967852823,-12.9217827059125));
#44906=CARTESIAN_POINT('Ctrl Pts',(2.31465853174747,6.36114130317295,-12.9137420962114));
#44907=CARTESIAN_POINT('Ctrl Pts',(2.15189080981932,6.41573494952957,-12.9057014865103));
#44908=CARTESIAN_POINT('Ctrl Pts',(1.98915021135736,6.47031949845026,-12.8976622166892));
#44909=CARTESIAN_POINT('Ctrl Pts',(1.82427128925733,6.51872799142564,-12.8896229468681));
#44910=CARTESIAN_POINT('Ctrl Pts',(1.65777370470937,6.56079837702502,-12.8815836770469));
#44911=CARTESIAN_POINT('Ctrl Pts',(1.49128530389774,6.60286644209027,-12.8735448506589));
#44912=CARTESIAN_POINT('Ctrl Pts',(1.32317878006311,6.63859700283098,-12.8655060242708));
#44913=CARTESIAN_POINT('Ctrl Pts',(1.15398703298249,6.66787844278135,-12.8574671978827));
#44914=CARTESIAN_POINT('Ctrl Pts',(0.984771124091398,6.69716406433405,-12.8494272234919));
#44915=CARTESIAN_POINT('Ctrl Pts',(0.814470051410564,6.71999866778069,-12.841387249101));
#44916=CARTESIAN_POINT('Ctrl Pts',(0.643624789566233,6.73632215160883,-12.8333472747101));
#44917=CARTESIAN_POINT('Ctrl Pts',(0.472721299876386,6.75265119884145,-12.8253045601181));
#44918=CARTESIAN_POINT('Ctrl Pts',(0.301273623332456,6.76246467383177,-12.8172618455261));
#44919=CARTESIAN_POINT('Ctrl Pts',(0.129825561801393,6.76575452728688,-12.809219130934));
#44920=CARTESIAN_POINT('Ctrl Pts',(-0.0418248302162636,6.76904826318689,
-12.8011669249174));
#44921=CARTESIAN_POINT('Ctrl Pts',(-0.213475234481144,6.76580299376193,
-12.7931147189007));
#44922=CARTESIAN_POINT('Ctrl Pts',(-0.384583255898232,6.75606281196991,
-12.785062512884));
#44923=CARTESIAN_POINT('Ctrl Pts',(-0.555794869911432,6.74631673325552,
-12.777005431883));
#44924=CARTESIAN_POINT('Ctrl Pts',(-0.726463076460481,6.73006794642621,
-12.7689483508819));
#44925=CARTESIAN_POINT('Ctrl Pts',(-0.896053401502798,6.70741211658083,
-12.7608912698809));
#44926=CARTESIAN_POINT('Ctrl Pts',(-1.06592357492262,6.68471890136442,-12.7528208935398));
#44927=CARTESIAN_POINT('Ctrl Pts',(-1.23471194646283,6.65559758535737,-12.7447505171987));
#44928=CARTESIAN_POINT('Ctrl Pts',(-1.40189580009872,6.62019464711315,-12.7366801408576));
#44929=CARTESIAN_POINT('Ctrl Pts',(-1.55974503709853,6.58676841205595,-12.72906036945));
#44930=CARTESIAN_POINT('Ctrl Pts',(-1.71616380877214,6.54774295278436,-12.7214405980424));
#44931=CARTESIAN_POINT('Ctrl Pts',(-1.87072815952014,6.50328110673208,-12.7138208266348));
#44932=CARTESIAN_POINT('Ctrl Pts',(-2.03977719211289,6.45465260975944,-12.7054869839421));
#44933=CARTESIAN_POINT('Ctrl Pts',(-2.20714519044762,6.39936626702175,-12.6971531412494));
#44934=CARTESIAN_POINT('Ctrl Pts',(-2.37227764169204,6.33755377024354,-12.6888192985568));
#44935=CARTESIAN_POINT('Ctrl Pts',(-2.53721546345172,6.27581412731269,-12.680495278352));
#44936=CARTESIAN_POINT('Ctrl Pts',(-2.69992266403518,6.20756377420348,-12.6721712581472));
#44937=CARTESIAN_POINT('Ctrl Pts',(-2.85985813155339,6.13298462963898,-12.6638472379425));
#44938=CARTESIAN_POINT('Ctrl Pts',(-3.01963441882481,6.05847971205377,-12.6555315024516));
#44939=CARTESIAN_POINT('Ctrl Pts',(-3.17664415587532,5.97765869862999,-12.6472157669608));
#44940=CARTESIAN_POINT('Ctrl Pts',(-3.33036431251776,5.89075229031981,-12.6389000314699));
#44941=CARTESIAN_POINT('Ctrl Pts',(-3.48395964037755,5.80391645454476,-12.6305910487899));
#44942=CARTESIAN_POINT('Ctrl Pts',(-3.63427040917541,5.71100524105929,-12.6222820661099));
#44943=CARTESIAN_POINT('Ctrl Pts',(-3.78079619131092,5.612296246615,-12.6139730834298));
#44944=CARTESIAN_POINT('Ctrl Pts',(-3.92722981943772,5.51364933291447,-12.6056693264927));
#44945=CARTESIAN_POINT('Ctrl Pts',(-4.06988291727517,5.40921209889775,-12.5973655695555));
#44946=CARTESIAN_POINT('Ctrl Pts',(-4.2082819792181,5.2993067266755,-12.5890618126184));
#44947=CARTESIAN_POINT('Ctrl Pts',(-4.34662485447842,5.18944597338477,-12.5807614268064));
#44948=CARTESIAN_POINT('Ctrl Pts',(-4.48071686314835,5.07412172123556,-12.5724610409943));
#44949=CARTESIAN_POINT('Ctrl Pts',(-4.61011544752674,4.95369806916765,-12.5641606551823));
#44950=CARTESIAN_POINT('Ctrl Pts',(-4.73948674511074,4.83329981131445,-12.5558620197057));
#44951=CARTESIAN_POINT('Ctrl Pts',(-4.86416633571904,4.70780453266443,-12.547563384229));
#44952=CARTESIAN_POINT('Ctrl Pts',(-4.9837464045838,4.57761518421962,-12.5392647487524));
#44953=CARTESIAN_POINT('Ctrl Pts',(-5.1033211060424,4.44743167938335,-12.5309664857638));
#44954=CARTESIAN_POINT('Ctrl Pts',(-5.21779650676553,4.31255478085536,-12.5226682227752));
#44955=CARTESIAN_POINT('Ctrl Pts',(-5.32680305458562,4.17342284194369,-12.5143699597866));
#44956=CARTESIAN_POINT('Ctrl Pts',(-5.43582280263355,4.03427405474785,-12.5060706919138));
#44957=CARTESIAN_POINT('Ctrl Pts',(-5.53937216415358,3.8908694745588,-12.497771424041));
#44958=CARTESIAN_POINT('Ctrl Pts',(-5.63712301861594,3.74367908253236,-12.4894721561681));
#44959=CARTESIAN_POINT('Ctrl Pts',(-5.7349425099331,3.59638533912734,-12.4811670608716));
#44960=CARTESIAN_POINT('Ctrl Pts',(-5.82695516600972,3.44530076230277,-12.4728619655751));
#44961=CARTESIAN_POINT('Ctrl Pts',(-5.9128767422217,3.29092352255317,-12.4645568702786));
#44962=CARTESIAN_POINT('Ctrl Pts',(-5.99882964990834,3.13648998883422,-12.4562487465125));
#44963=CARTESIAN_POINT('Ctrl Pts',(-6.07868688808047,2.97876170651755,-12.4479406227464));
#44964=CARTESIAN_POINT('Ctrl Pts',(-6.15221095237008,2.81825999466651,-12.4396324989803));
#44965=CARTESIAN_POINT('Ctrl Pts',(-6.22581317231511,2.65758767042335,-12.4313155437266));
#44966=CARTESIAN_POINT('Ctrl Pts',(-6.2930686295534,2.49413634575469,-12.4229985884729));
#44967=CARTESIAN_POINT('Ctrl Pts',(-6.35378819641643,2.32844681173507,-12.4146816332192));
#44968=CARTESIAN_POINT('Ctrl Pts',(-6.39853759336842,2.20633614606845,-12.4085521637367));
#44969=CARTESIAN_POINT('Ctrl Pts',(-6.43973806006985,2.0830101980983,-12.4024226942542));
#44970=CARTESIAN_POINT('Ctrl Pts',(-6.47733142606586,1.95869002062594,-12.3962932247717));
#44971=CARTESIAN_POINT('Ctrl Pts',(-6.53293815762291,1.77480016259717,-12.3872267377714));
#44972=CARTESIAN_POINT('Ctrl Pts',(-6.58073898742956,1.5884447635909,-12.378160250771));
#44973=CARTESIAN_POINT('Ctrl Pts',(-6.62053851835857,1.40027094768494,-12.3690937637707));
#44974=CARTESIAN_POINT('Ctrl Pts',(-6.66028028210385,1.21237025739489,-12.3600404363581));
#44975=CARTESIAN_POINT('Ctrl Pts',(-6.69204387419446,1.0226566416069,-12.3509871089456));
#44976=CARTESIAN_POINT('Ctrl Pts',(-6.71568417086439,0.831790308432012,
-12.341933781533));
#44977=CARTESIAN_POINT('Ctrl Pts',(-6.73926725371455,0.641385906515465,
-12.3329023648202));
#44978=CARTESIAN_POINT('Ctrl Pts',(-6.75476624873634,0.449834583210811,
-12.3238709481074));
#44979=CARTESIAN_POINT('Ctrl Pts',(-6.7620873952382,0.257804303999635,-12.3148395313947));
#44980=CARTESIAN_POINT('Ctrl Pts',(-6.76533513846844,0.172617504479535,
-12.3108330929931));
#44981=CARTESIAN_POINT('Ctrl Pts',(-6.7669742244786,0.0873365959912321,
-12.3068266545915));
#44982=CARTESIAN_POINT('Ctrl Pts',(-6.76699969835621,0.00202050660550186,
-12.30282021619));
#44983=CARTESIAN_POINT('',(-6.76699999341342,0.000298567942575067,-12.6971797837809));
#44984=CARTESIAN_POINT('Ctrl Pts',(3.09908550384717,6.01564277861014,-13.3487674371071));
#44985=CARTESIAN_POINT('Ctrl Pts',(2.93969369619203,6.09775683669425,-13.3403258001161));
#44986=CARTESIAN_POINT('Ctrl Pts',(2.77720452294419,6.17344477825237,-13.3318841631251));
#44987=CARTESIAN_POINT('Ctrl Pts',(2.6121936832283,6.24249414587648,-13.323442526134));
#44988=CARTESIAN_POINT('Ctrl Pts',(2.44720086633562,6.31153597178669,-13.315001811156));
#44989=CARTESIAN_POINT('Ctrl Pts',(2.27934724675824,6.37408352589492,-13.3065610961779));
#44990=CARTESIAN_POINT('Ctrl Pts',(2.10917205664407,6.42990530532696,-13.2981203811998));
#44991=CARTESIAN_POINT('Ctrl Pts',(1.93912549295624,6.48568489202812,-13.2896860461118));
#44992=CARTESIAN_POINT('Ctrl Pts',(1.76676117239651,6.53474873447013,-13.2812517110237));
#44993=CARTESIAN_POINT('Ctrl Pts',(1.59263717699892,6.57691385244181,-13.2728173759357));
#44994=CARTESIAN_POINT('Ctrl Pts',(1.41861805399358,6.61905357496594,-13.2643881207271));
#44995=CARTESIAN_POINT('Ctrl Pts',(1.24284169231492,6.65430277836938,-13.2559588655185));
#44996=CARTESIAN_POINT('Ctrl Pts',(1.06588055273195,6.68252853696173,-13.2475296103098));
#44997=CARTESIAN_POINT('Ctrl Pts',(0.888998849806665,6.71074162520211,-13.2391041389368));
#44998=CARTESIAN_POINT('Ctrl Pts',(0.710933758113983,6.73193750250743,-13.2306786675638));
#44999=CARTESIAN_POINT('Ctrl Pts',(0.532267523909018,6.74603441163709,-13.2222531961908));
#45000=CARTESIAN_POINT('Ctrl Pts',(0.353654108626332,6.76012715331144,-13.2138302156315));
#45001=CARTESIAN_POINT('Ctrl Pts',(0.174440237263183,6.76712508582163,-13.2054072350723));
#45002=CARTESIAN_POINT('Ctrl Pts',(-0.00478673464667945,6.76699830701704,
-13.1969842545131));
#45003=CARTESIAN_POINT('Ctrl Pts',(-0.184016674183397,6.76687152611325,
-13.1885611344867));
#45004=CARTESIAN_POINT('Ctrl Pts',(-0.363259381365447,6.75961979181696,
-13.1801380144604));
#45005=CARTESIAN_POINT('Ctrl Pts',(-0.541926830466349,6.74526532542796,
-13.1717148944341));
#45006=CARTESIAN_POINT('Ctrl Pts',(-0.720600458185537,6.73091036263757,
-13.1632914831222));
#45007=CARTESIAN_POINT('Ctrl Pts',(-0.898698455710701,6.70945220455209,
-13.1548680718104));
#45008=CARTESIAN_POINT('Ctrl Pts',(-1.07563709152317,6.68096503862575,-13.1464446604985));
#45009=CARTESIAN_POINT('Ctrl Pts',(-1.25260652286495,6.65247291461126,-13.1380197831224));
#45010=CARTESIAN_POINT('Ctrl Pts',(-1.42841586095319,6.61694939672042,-13.1295949057463));
#45011=CARTESIAN_POINT('Ctrl Pts',(-1.60249038261121,6.5745200261037,-13.1211700283702));
#45012=CARTESIAN_POINT('Ctrl Pts',(-1.77661948605881,6.53207735158152,-13.1127425093387));
#45013=CARTESIAN_POINT('Ctrl Pts',(-1.94901236469206,6.48272458613518,-13.1043149903073));
#45014=CARTESIAN_POINT('Ctrl Pts',(-2.11910794001518,6.42663757641308,-13.0958874712759));
#45015=CARTESIAN_POINT('Ctrl Pts',(-2.28935605047631,6.37050027002835,-13.0874523947711));
#45016=CARTESIAN_POINT('Ctrl Pts',(-2.45730242416982,6.30761675709199,-13.0790173182663));
#45017=CARTESIAN_POINT('Ctrl Pts',(-2.62240342745077,6.23821202458641,-13.0705822417615));
#45018=CARTESIAN_POINT('Ctrl Pts',(-2.78758422513324,6.16877374831681,-13.0621430885287));
#45019=CARTESIAN_POINT('Ctrl Pts',(-2.94991660570296,6.09280810328691,-13.053703935296));
#45020=CARTESIAN_POINT('Ctrl Pts',(-3.10887966997177,6.01058700940567,-13.0452647820632));
#45021=CARTESIAN_POINT('Ctrl Pts',(-3.26801938677344,5.92827454483681,-13.0368162505651));
#45022=CARTESIAN_POINT('Ctrl Pts',(-3.42378201332264,5.83969290164503,-13.028367719067));
#45023=CARTESIAN_POINT('Ctrl Pts',(-3.57567282042132,5.74515908233186,-13.0199191875689));
#45024=CARTESIAN_POINT('Ctrl Pts',(-3.65959741945254,5.69292608000412,-13.0152510998029));
#45025=CARTESIAN_POINT('Ctrl Pts',(-3.74234050073199,5.63887669082813,-13.0105830120369));
#45026=CARTESIAN_POINT('Ctrl Pts',(-3.82382272336077,5.58306983480503,-13.005914924271));
#45027=CARTESIAN_POINT('Ctrl Pts',(-3.96766678659879,5.48455159772313,-12.9976741486742));
#45028=CARTESIAN_POINT('Ctrl Pts',(-4.10789963213892,5.38033472218766,-12.9894333730775));
#45029=CARTESIAN_POINT('Ctrl Pts',(-4.24404210803553,5.27071110811637,-12.9811925974807));
#45030=CARTESIAN_POINT('Ctrl Pts',(-4.38003379138044,5.16120891408231,-12.9729609494363));
#45031=CARTESIAN_POINT('Ctrl Pts',(-4.51194385150957,5.0463121269841,-12.964729301392));
#45032=CARTESIAN_POINT('Ctrl Pts',(-4.63932129795759,4.92635635072385,-12.9564976533476));
#45033=CARTESIAN_POINT('Ctrl Pts',(-4.7665803599245,4.80651206125127,-12.9482736557893));
#45034=CARTESIAN_POINT('Ctrl Pts',(-4.88931494026081,4.68161838892821,-12.940049658231));
#45035=CARTESIAN_POINT('Ctrl Pts',(-5.00710633201655,4.55205175496498,-12.9318256606727));
#45036=CARTESIAN_POINT('Ctrl Pts',(-5.12479365462031,4.42259959362595,-12.9236089290482));
#45037=CARTESIAN_POINT('Ctrl Pts',(-5.23754625476821,4.28848296159373,-12.9153921974237));
#45038=CARTESIAN_POINT('Ctrl Pts',(-5.34498167464297,4.15011564871762,-12.9071754657992));
#45039=CARTESIAN_POINT('Ctrl Pts',(-5.45236205137442,4.01181922653882,-12.8989629439105));
#45040=CARTESIAN_POINT('Ctrl Pts',(-5.55443045567882,3.8692767411272,-12.8907504220219));
#45041=CARTESIAN_POINT('Ctrl Pts',(-5.65084391902132,3.72293593859199,-12.8825379001332));
#45042=CARTESIAN_POINT('Ctrl Pts',(-5.74722514123779,3.57664407312525,-12.8743281245513));
#45043=CARTESIAN_POINT('Ctrl Pts',(-5.83795499414237,3.42655671765138,-12.8661183489695));
#45044=CARTESIAN_POINT('Ctrl Pts',(-5.92273310871932,3.27315161929294,-12.8579085733877));
#45045=CARTESIAN_POINT('Ctrl Pts',(-5.95976198661663,3.20614825782064,-12.8543227567049));
#45046=CARTESIAN_POINT('Ctrl Pts',(-5.99565600464417,3.13851233139998,-12.8507369400221));
#45047=CARTESIAN_POINT('Ctrl Pts',(-6.03039281295659,3.07028525082631,-12.8471511233393));
#45048=CARTESIAN_POINT('Ctrl Pts',(-6.11507093287449,2.90396769918182,-12.8384099571292));
#45049=CARTESIAN_POINT('Ctrl Pts',(-6.19279029492635,2.73429120459534,-12.8296687909191));
#45050=CARTESIAN_POINT('Ctrl Pts',(-6.26332310264359,2.56184947096645,-12.820927624709));
#45051=CARTESIAN_POINT('Ctrl Pts',(-6.33396409351821,2.38914324636079,-12.812173051306));
#45052=CARTESIAN_POINT('Ctrl Pts',(-6.39739640571944,2.21366356988124,-12.8034184779029));
#45053=CARTESIAN_POINT('Ctrl Pts',(-6.45344171234111,2.03602039906673,-12.7946639044999));
#45054=CARTESIAN_POINT('Ctrl Pts',(-6.50962377189001,1.85794377137464,-12.7858879695661));
#45055=CARTESIAN_POINT('Ctrl Pts',(-6.55838268520997,1.67769335789036,-12.7771120346324));
#45056=CARTESIAN_POINT('Ctrl Pts',(-6.59959037899519,1.49589298730698,-12.7683360996986));
#45057=CARTESIAN_POINT('Ctrl Pts',(-6.6408491657772,1.31386720430911,-12.7595492835732));
#45058=CARTESIAN_POINT('Ctrl Pts',(-6.6745379815588,1.13028790139143,-12.7507624674477));
#45059=CARTESIAN_POINT('Ctrl Pts',(-6.70058035367453,0.94578640503599,-12.7419756513222));
#45060=CARTESIAN_POINT('Ctrl Pts',(-6.72667643939347,0.760904365766798,
-12.73317071198));
#45061=CARTESIAN_POINT('Ctrl Pts',(-6.74509450769083,0.575096608282414,
-12.7243657726378));
#45062=CARTESIAN_POINT('Ctrl Pts',(-6.75580998387632,0.388999308170436,
-12.7155608332956));
#45063=CARTESIAN_POINT('Ctrl Pts',(-6.76326646901383,0.259501399874452,
-12.7094338168004));
#45064=CARTESIAN_POINT('Ctrl Pts',(-6.76699427685383,0.129863310485216,
-12.7033068003053));
#45065=CARTESIAN_POINT('Ctrl Pts',(-6.76699999341339,0.000298568560796373,
-12.6971797838101));
#45066=CARTESIAN_POINT('Ctrl Pts',(-6.76699999341342,0.000298567942480405,
-12.6971797837809));
#45067=CARTESIAN_POINT('Ctrl Pts',(-6.76700272788868,-0.061677925269276,
-12.6942489633232));
#45068=CARTESIAN_POINT('Ctrl Pts',(-6.76615404016013,-0.123652304761972,
-12.6913181428656));
#45069=CARTESIAN_POINT('Ctrl Pts',(-6.76445405791803,-0.185607915553967,
-12.6883873224079));
#45070=CARTESIAN_POINT('Ctrl Pts',(-6.75968385425956,-0.359457308767372,
-12.6801633479904));
#45071=CARTESIAN_POINT('Ctrl Pts',(-6.74820101348188,-0.533353174028972,
-12.6719393735728));
#45072=CARTESIAN_POINT('Ctrl Pts',(-6.72999343021052,-0.706737171318463,
-12.6637153991552));
#45073=CARTESIAN_POINT('Ctrl Pts',(-6.71180507591366,-0.879938058284459,
-12.6555001100526));
#45074=CARTESIAN_POINT('Ctrl Pts',(-6.68690615869465,-1.05262780007581,
-12.6472848209499));
#45075=CARTESIAN_POINT('Ctrl Pts',(-6.65533657408663,-1.22424837579018,
-12.6390695318473));
#45076=CARTESIAN_POINT('Ctrl Pts',(-6.62379399783722,-1.39572212695454,
-12.6308612710751));
#45077=CARTESIAN_POINT('Ctrl Pts',(-6.58559218453351,-1.56612818305414,
-12.622653010303));
#45078=CARTESIAN_POINT('Ctrl Pts',(-6.54082279672109,-1.73491387160682,
-12.6144447495308));
#45079=CARTESIAN_POINT('Ctrl Pts',(-6.49608273271306,-1.90358900607873,
-12.6062418651429));
#45080=CARTESIAN_POINT('Ctrl Pts',(-6.44478375441965,-2.07064554170197,
-12.598038980755));
#45081=CARTESIAN_POINT('Ctrl Pts',(-6.38706856280714,-2.23554113672747,
-12.5898360963672));
#45082=CARTESIAN_POINT('Ctrl Pts',(-6.32937960368294,-2.40036178403733,
-12.581636940323));
#45083=CARTESIAN_POINT('Ctrl Pts',(-6.26528035943658,-2.56302310974894,
-12.5734377842788));
#45084=CARTESIAN_POINT('Ctrl Pts',(-6.19496335339311,-2.72299798937062,
-12.5652386282345));
#45085=CARTESIAN_POINT('Ctrl Pts',(-6.12465246321934,-2.88295895506771,
-12.5570401853175));
#45086=CARTESIAN_POINT('Ctrl Pts',(-6.04812502480654,-3.04023360861682,
-12.5488417424005));
#45087=CARTESIAN_POINT('Ctrl Pts',(-5.96562181692079,-3.19431453327293,
-12.5406432994835));
#45088=CARTESIAN_POINT('Ctrl Pts',(-5.8831194306693,-3.34839392346549,-12.5324449382133));
#45089=CARTESIAN_POINT('Ctrl Pts',(-5.79464156186918,-3.49927933139718,
-12.5242465769431));
#45090=CARTESIAN_POINT('Ctrl Pts',(-5.70047503863014,-3.64648780800851,
-12.5160482156728));
#45091=CARTESIAN_POINT('Ctrl Pts',(-5.60629234715482,-3.79372156007178,
-12.5078484467576));
#45092=CARTESIAN_POINT('Ctrl Pts',(-5.50641924859686,-3.93727682086154,
-12.4996486778423));
#45093=CARTESIAN_POINT('Ctrl Pts',(-5.40118602410122,-4.07669946562825,
-12.491448908927));
#45094=CARTESIAN_POINT('Ctrl Pts',(-5.29591561466701,-4.21617137641819,
-12.4832462425627));
#45095=CARTESIAN_POINT('Ctrl Pts',(-5.18528152229535,-4.35150747613821,
-12.4750435761983));
#45096=CARTESIAN_POINT('Ctrl Pts',(-5.06965446303003,-4.48228653986776,
-12.466840909834));
#45097=CARTESIAN_POINT('Ctrl Pts',(-4.95389608032675,-4.61321413592504,
-12.458628927291));
#45098=CARTESIAN_POINT('Ctrl Pts',(-4.83313363948699,-4.73957408704741,
-12.450416944748));
#45099=CARTESIAN_POINT('Ctrl Pts',(-4.70777562722417,-4.86098114002863,
-12.442204962205));
#45100=CARTESIAN_POINT('Ctrl Pts',(-4.5823436771115,-4.98245980053052,-12.4339881361237));
#45101=CARTESIAN_POINT('Ctrl Pts',(-4.45231101921201,-5.09897950075,-12.4257713100424));
#45102=CARTESIAN_POINT('Ctrl Pts',(-4.3181193068555,-5.21019526042564,-12.417554483961));
#45103=CARTESIAN_POINT('Ctrl Pts',(-4.18372065149776,-5.32158253086515,
-12.4093249863472));
#45104=CARTESIAN_POINT('Ctrl Pts',(-4.04515040909436,-5.42764929742197,
-12.4010954887333));
#45105=CARTESIAN_POINT('Ctrl Pts',(-3.90288037585503,-5.5280931406558,-12.3928659911195));
#45106=CARTESIAN_POINT('Ctrl Pts',(-3.77606693016552,-5.61762450273365,
-12.3855305675946));
#45107=CARTESIAN_POINT('Ctrl Pts',(-3.64631447432866,-5.702688886801,-12.3781951440698));
#45108=CARTESIAN_POINT('Ctrl Pts',(-3.51397284577488,-5.78310330524683,
-12.3708597205449));
#45109=CARTESIAN_POINT('Ctrl Pts',(-3.3683626978814,-5.87158004148336,-12.3627888503585));
#45110=CARTESIAN_POINT('Ctrl Pts',(-3.21914287105219,-5.95471530131142,
-12.3547179801721));
#45111=CARTESIAN_POINT('Ctrl Pts',(-3.06674998333667,-6.03219143758755,
-12.3466471099857));
#45112=CARTESIAN_POINT('Ctrl Pts',(-2.91454673672493,-6.10957116083403,
-12.3385862833699));
#45113=CARTESIAN_POINT('Ctrl Pts',(-2.75917861433286,-6.18130560612759,
-12.3305254567541));
#45114=CARTESIAN_POINT('Ctrl Pts',(-2.60111182744723,-6.24711983726214,
-12.3224646301383));
#45115=CARTESIAN_POINT('Ctrl Pts',(-2.44320708075705,-6.31286659975836,
-12.3144120669784));
#45116=CARTESIAN_POINT('Ctrl Pts',(-2.28260951646843,-6.37270508353508,
-12.3063595038185));
#45117=CARTESIAN_POINT('Ctrl Pts',(-2.11981052260914,-6.426405865508,-12.2983069406586));
#45118=CARTESIAN_POINT('Ctrl Pts',(-1.95714277316589,-6.48006335527373,
-12.2902608692707));
#45119=CARTESIAN_POINT('Ctrl Pts',(-1.79227747893726,-6.5275928753536,-12.2822147978828));
#45120=CARTESIAN_POINT('Ctrl Pts',(-1.62572652144183,-6.56881285145807,
-12.2741687264949));
#45121=CARTESIAN_POINT('Ctrl Pts',(-1.45927340197547,-6.61000861346446,
-12.266127381659));
#45122=CARTESIAN_POINT('Ctrl Pts',(-1.29113695165918,-6.64490212063055,
-12.2580860368232));
#45123=CARTESIAN_POINT('Ctrl Pts',(-1.12184464548294,-6.67336149113783,
-12.2500446919873));
#45124=CARTESIAN_POINT('Ctrl Pts',(-0.949288904556731,-6.70236947073888,
-12.2418483347662));
#45125=CARTESIAN_POINT('Ctrl Pts',(-0.775532667203259,-6.72469259987832,
-12.2336519775452));
#45126=CARTESIAN_POINT('Ctrl Pts',(-0.601146366280044,-6.74024569628647,
-12.2254556203241));
#45127=CARTESIAN_POINT('Ctrl Pts',(-0.430112504654712,-6.75549979666497,
-12.2174168316156));
#45128=CARTESIAN_POINT('Ctrl Pts',(-0.258472971865798,-6.7642417877685,
-12.2093780429071));
#45129=CARTESIAN_POINT('Ctrl Pts',(-0.0867715089438693,-6.76644365270528,
-12.2013392541986));
#45130=CARTESIAN_POINT('Ctrl Pts',(0.0849483275902528,-6.76864575326156,
-12.1932996052669));
#45131=CARTESIAN_POINT('Ctrl Pts',(0.25672973398804,-6.76430632924852,-12.1852599563352));
#45132=CARTESIAN_POINT('Ctrl Pts',(0.428028892403548,-6.75344950875238,
-12.1772203074034));
#45133=CARTESIAN_POINT('Ctrl Pts',(0.599380299268728,-6.74258937678616,
-12.1691782062752));
#45134=CARTESIAN_POINT('Ctrl Pts',(0.770248792854648,-6.72520791505771,
-12.1611361051471));
#45135=CARTESIAN_POINT('Ctrl Pts',(0.940095746729051,-6.70138112533394,
-12.1530940040189));
#45136=CARTESIAN_POINT('Ctrl Pts',(1.11567436798678,-6.67675027506981,-12.1447805135741));
#45137=CARTESIAN_POINT('Ctrl Pts',(1.29016086458142,-6.64523153704258,-12.1364670231294));
#45138=CARTESIAN_POINT('Ctrl Pts',(1.46297285585442,-6.60696597713604,-12.1281535326846));
#45139=CARTESIAN_POINT('Ctrl Pts',(1.63043798425864,-6.56988436690748,-12.1200972645139));
#45140=CARTESIAN_POINT('Ctrl Pts',(1.79633034633245,-6.52646737970495,-12.1120409963431));
#45141=CARTESIAN_POINT('Ctrl Pts',(1.96013700431782,-6.47689369407156,-12.1039847281724));
#45142=CARTESIAN_POINT('Ctrl Pts',(2.13178874395328,-6.4249458093899,-12.0955426265906));
#45143=CARTESIAN_POINT('Ctrl Pts',(2.30114962883959,-6.36623716666166,-12.0871005250089));
#45144=CARTESIAN_POINT('Ctrl Pts',(2.46765538209628,-6.30102895686183,-12.0786584234271));
#45145=CARTESIAN_POINT('Ctrl Pts',(2.63416113535291,-6.23582074706202,-12.0702163218454));
#45146=CARTESIAN_POINT('Ctrl Pts',(2.79781136955294,-6.16411323435529,-12.0617742202636));
#45147=CARTESIAN_POINT('Ctrl Pts',(2.95807432651015,-6.08622093575657,-12.0533321186819));
#45148=CARTESIAN_POINT('Ctrl Pts',(3.11628212107551,-6.00932750380635,-12.0449982759892));
#45149=CARTESIAN_POINT('Ctrl Pts',(3.27169222448777,-5.92616305035882,-12.0366644332965));
#45150=CARTESIAN_POINT('Ctrl Pts',(3.42378091540367,-5.8369523934428,-12.0283305906038));
#45151=CARTESIAN_POINT('Ctrl Pts',(3.5756903505566,-5.74784688257198,-12.0200065703991));
#45152=CARTESIAN_POINT('Ctrl Pts',(3.72428587417744,-5.65270953879435,-12.0116825501943));
#45153=CARTESIAN_POINT('Ctrl Pts',(3.86906557931096,-5.5518123656146,-12.0033585299896));
#45154=CARTESIAN_POINT('Ctrl Pts',(4.01370118839411,-5.45101561316809,-11.9950427944987));
#45155=CARTESIAN_POINT('Ctrl Pts',(4.15452826186678,-5.34447065028088,-11.9867270590079));
#45156=CARTESIAN_POINT('Ctrl Pts',(4.29107107088441,-5.23249443999886,-11.978411323517));
#45157=CARTESIAN_POINT('Ctrl Pts',(4.42750300002168,-5.12060916023809,-11.970102340837));
#45158=CARTESIAN_POINT('Ctrl Pts',(4.55965732922994,-5.00330164095815,-11.9617933581569));
#45159=CARTESIAN_POINT('Ctrl Pts',(4.68708863826475,-4.88093117110347,-11.9534843754769));
#45160=CARTESIAN_POINT('Ctrl Pts',(4.81443980231853,-4.75863766333182,-11.9451806185397));
#45161=CARTESIAN_POINT('Ctrl Pts',(4.9370736157764,-4.63128779105709,-11.9368768616026));
#45162=CARTESIAN_POINT('Ctrl Pts',(5.05457882629018,-4.49928015229314,-11.9285731046654));
#45163=CARTESIAN_POINT('Ctrl Pts',(5.17203633252132,-4.36732610544808,-11.9202727188534));
#45164=CARTESIAN_POINT('Ctrl Pts',(5.28436915363902,-4.23071831935014,-11.9119723330414));
#45165=CARTESIAN_POINT('Ctrl Pts',(5.39120371393617,-4.08989138179009,-11.9036719472294));
#45166=CARTESIAN_POINT('Ctrl Pts',(5.49801574560448,-3.94909414096674,-11.8953733117527));
#45167=CARTESIAN_POINT('Ctrl Pts',(5.59933161625974,-3.80407979812098,-11.8870746762761));
#45168=CARTESIAN_POINT('Ctrl Pts',(5.69481864018185,-3.65531526074528,-11.8787760407995));
#45169=CARTESIAN_POINT('Ctrl Pts',(5.79030137812491,-3.50655740073435,-11.8704777778109));
#45170=CARTESIAN_POINT('Ctrl Pts',(5.87995560299437,-3.35404997439035,-11.8621795148224));
#45171=CARTESIAN_POINT('Ctrl Pts',(5.96349239510832,-3.19828820675769,-11.8538812518338));
#45172=CARTESIAN_POINT('Ctrl Pts',(6.04703930317096,-3.0425075770403,-11.8455819839611));
#45173=CARTESIAN_POINT('Ctrl Pts',(6.12446713852243,-2.88347212752461,-11.8372827160883));
#45174=CARTESIAN_POINT('Ctrl Pts',(6.19553322246003,-2.72170113888245,-11.8289834482155));
#45175=CARTESIAN_POINT('Ctrl Pts',(6.26664920624323,-2.55981656093146,-11.820678352919));
#45176=CARTESIAN_POINT('Ctrl Pts',(6.33139437276218,-2.39519292458183,-11.8123732576225));
#45177=CARTESIAN_POINT('Ctrl Pts',(6.38957410279937,-2.228369759451,-11.804068162326));
#45178=CARTESIAN_POINT('Ctrl Pts',(6.44777504819142,-2.06148576191948,-11.7957600385599));
#45179=CARTESIAN_POINT('Ctrl Pts',(6.49940567781079,-1.89240096775964,-11.7874519147938));
#45180=CARTESIAN_POINT('Ctrl Pts',(6.54432138956985,-1.72166969829247,-11.7791437910277));
#45181=CARTESIAN_POINT('Ctrl Pts',(6.58928484647106,-1.55075694247213,-11.770826835774));
#45182=CARTESIAN_POINT('Ctrl Pts',(6.62751904274004,-1.37819455288503,-11.7625098805203));
#45183=CARTESIAN_POINT('Ctrl Pts',(6.65893037524787,-1.20454773985977,-11.7541929252666));
#45184=CARTESIAN_POINT('Ctrl Pts',(6.68208004939455,-1.07657268063102,-11.748063455784));
#45185=CARTESIAN_POINT('Ctrl Pts',(6.7015249770888,-0.948008833898331,-11.7419339863014));
#45186=CARTESIAN_POINT('Ctrl Pts',(6.71724575092009,-0.819083952807052,
-11.7358045168188));
#45187=CARTESIAN_POINT('Ctrl Pts',(6.73892081266221,-0.641328405418721,
-11.7273534932936));
#45188=CARTESIAN_POINT('Ctrl Pts',(6.7535541152242,-0.462561580005216,-11.7189024697684));
#45189=CARTESIAN_POINT('Ctrl Pts',(6.76106445889872,-0.283366163499842,
-11.7104514462432));
#45190=CARTESIAN_POINT('Ctrl Pts',(6.76856818993887,-0.104328523232263,
-11.7020078635931));
#45191=CARTESIAN_POINT('Ctrl Pts',(6.76896144866933,0.0751366263168869,
-11.6935642809429));
#45192=CARTESIAN_POINT('Ctrl Pts',(6.76221478027886,0.254441084296753,-11.6851206982927));
#45193=CARTESIAN_POINT('Ctrl Pts',(6.75547313499325,0.433612044520193,-11.676683402153));
#45194=CARTESIAN_POINT('Ctrl Pts',(6.74160217200139,0.612622221501215,-11.6682461060132));
#45195=CARTESIAN_POINT('Ctrl Pts',(6.72062450102552,0.790882618481051,-11.6598088098734));
#45196=CARTESIAN_POINT('Ctrl Pts',(6.69966179601826,0.969015840260736,-11.6513775331011));
#45197=CARTESIAN_POINT('Ctrl Pts',(6.67160253482747,1.1464000205918,-11.6429462563287));
#45198=CARTESIAN_POINT('Ctrl Pts',(6.63652124700247,1.3224502781144,-11.6345149795564));
#45199=CARTESIAN_POINT('Ctrl Pts',(6.60145499628745,1.49842507412315,-11.6260873167345));
#45200=CARTESIAN_POINT('Ctrl Pts',(6.55937278396115,1.67306676267044,-11.6176596539126));
#45201=CARTESIAN_POINT('Ctrl Pts',(6.51040052640408,1.84579901013016,-11.6092319910907));
#45202=CARTESIAN_POINT('Ctrl Pts',(6.46144334444441,2.01847808377374,-11.6008069226367));
#45203=CARTESIAN_POINT('Ctrl Pts',(6.40560043743466,2.18924857001311,-11.5923818541827));
#45204=CARTESIAN_POINT('Ctrl Pts',(6.34304812896488,2.35754733433609,-11.5839567857287));
#45205=CARTESIAN_POINT('Ctrl Pts',(6.32593190269042,2.40359902774811,-11.5816514291149));
#45206=CARTESIAN_POINT('Ctrl Pts',(6.30831360625685,2.4494657428033,-11.5793460725012));
#45207=CARTESIAN_POINT('Ctrl Pts',(6.29019749782231,2.49513615628286,-11.5770407158874));
#45208=CARTESIAN_POINT('Ctrl Pts',(6.22246718235915,2.66588317535046,-11.5684217273629));
#45209=CARTESIAN_POINT('Ctrl Pts',(6.14780512269873,2.83380862626157,-11.5598027388385));
#45210=CARTESIAN_POINT('Ctrl Pts',(6.06647740403953,2.99835636745832,-11.551183750314));
#45211=CARTESIAN_POINT('Ctrl Pts',(5.98510096281952,3.16300268743556,-11.5425595982463));
#45212=CARTESIAN_POINT('Ctrl Pts',(5.89705102790888,3.32426698664446,-11.5339354461786));
#45213=CARTESIAN_POINT('Ctrl Pts',(5.80263957124182,3.48161787194668,-11.5253112941109));
#45214=CARTESIAN_POINT('Ctrl Pts',(5.70499449678336,3.64435806740434,-11.5163917625147));
#45215=CARTESIAN_POINT('Ctrl Pts',(5.60054460875648,3.80291172908376,-11.5074722309184));
#45216=CARTESIAN_POINT('Ctrl Pts',(5.48968324925971,3.95672425407651,-11.4985526993221));
#45217=CARTESIAN_POINT('Ctrl Pts',(5.38229349589826,4.10572016390346,-11.4899124814629));
#45218=CARTESIAN_POINT('Ctrl Pts',(5.26888796700644,4.25026716798676,-11.4812722636037));
#45219=CARTESIAN_POINT('Ctrl Pts',(5.14986505942818,4.38989508640934,-11.4726320457444));
#45220=CARTESIAN_POINT('Ctrl Pts',(5.0250706423261,4.53629366669326,-11.4635728572796));
#45221=CARTESIAN_POINT('Ctrl Pts',(4.89410078483449,4.67728395653573,-11.4545136688149));
#45222=CARTESIAN_POINT('Ctrl Pts',(4.75745828152374,4.81236736955536,-11.4454544803501));
#45223=CARTESIAN_POINT('Ctrl Pts',(4.62081577821295,4.94745078257504,-11.4363952918853));
#45224=CARTESIAN_POINT('Ctrl Pts',(4.47850093466733,5.07662708613753,-11.4273361034205));
#45225=CARTESIAN_POINT('Ctrl Pts',(4.33105680174849,5.1994457377713,-11.4182769149557));
#45226=CARTESIAN_POINT('Ctrl Pts',(4.18385813299746,5.32205992160078,-11.4092328081772));
#45227=CARTESIAN_POINT('Ctrl Pts',(4.03141216534033,5.43845122077355,-11.4001887013987));
#45228=CARTESIAN_POINT('Ctrl Pts',(3.87424375000041,5.54820010143675,-11.3911445946202));
#45229=CARTESIAN_POINT('Ctrl Pts',(3.71725952241186,5.65782036593047,-11.3821110867505));
#45230=CARTESIAN_POINT('Ctrl Pts',(3.55556409441686,5.7608136214315,-11.3730775788807));
#45231=CARTESIAN_POINT('Ctrl Pts',(3.38971261093798,5.85680266145685,-11.3640440710109));
#45232=CARTESIAN_POINT('Ctrl Pts',(3.29417845549221,5.91209449049882,-11.358840568896));
#45233=CARTESIAN_POINT('Ctrl Pts',(3.19726589331876,5.96506307616248,-11.353637066781));
#45234=CARTESIAN_POINT('Ctrl Pts',(3.09908550384727,6.01564277861009,-11.3484335646661));
#45235=CARTESIAN_POINT('Origin',(0.,0.,-63.6971797838103));
#45236=CARTESIAN_POINT('',(3.09908550384723,6.01564277861011,-8.95438620791578));
#45237=CARTESIAN_POINT('',(3.09908550384716,6.01564277861014,-9.34860320957392));
#45238=CARTESIAN_POINT('',(3.09908550384721,6.01564277861012,-63.6971797838103));
#45239=CARTESIAN_POINT('',(-6.76699998098446,0.000507303006826857,-10.3028202161471));
#45240=CARTESIAN_POINT('Ctrl Pts',(-6.76699998098446,0.000507303006836547,
-10.302820216147));
#45241=CARTESIAN_POINT('Ctrl Pts',(-6.76701416573043,-0.188705404997191,
-10.2939567430814));
#45242=CARTESIAN_POINT('Ctrl Pts',(-6.75908815674408,-0.377745891299328,
-10.2850932700157));
#45243=CARTESIAN_POINT('Ctrl Pts',(-6.74329100385126,-0.565964166161285,
-10.27622979695));
#45244=CARTESIAN_POINT('Ctrl Pts',(-6.72744985035007,-0.754706694897294,
-10.2673416360048));
#45245=CARTESIAN_POINT('Ctrl Pts',(-6.70369370392128,-0.942622170167142,
-10.2584534750596));
#45246=CARTESIAN_POINT('Ctrl Pts',(-6.6721434554764,-1.12906629988833,-10.2495653141144));
#45247=CARTESIAN_POINT('Ctrl Pts',(-6.64055091653122,-1.31576034255509,
-10.2406652393241));
#45248=CARTESIAN_POINT('Ctrl Pts',(-6.60114345573103,-1.50097884609136,
-10.2317651645338));
#45249=CARTESIAN_POINT('Ctrl Pts',(-6.55409264275158,-1.68408985218415,
-10.2228650897435));
#45250=CARTESIAN_POINT('Ctrl Pts',(-6.5069417445632,-1.86759036702593,-10.2139460829563));
#45251=CARTESIAN_POINT('Ctrl Pts',(-6.45211504091601,-2.04897416683534,
-10.2050270761691));
#45252=CARTESIAN_POINT('Ctrl Pts',(-6.38983416972207,-2.22762390978644,
-10.1961080693819));
#45253=CARTESIAN_POINT('Ctrl Pts',(-6.33744337954934,-2.37790442157022,
-10.1886053834981));
#45254=CARTESIAN_POINT('Ctrl Pts',(-6.27977875266993,-2.52625051222462,
-10.1811026976143));
#45255=CARTESIAN_POINT('Ctrl Pts',(-6.21699811996086,-2.67230675192859,
-10.1736000117305));
#45256=CARTESIAN_POINT('Ctrl Pts',(-6.1462820307936,-2.83682446423335,-10.1651489882053));
#45257=CARTESIAN_POINT('Ctrl Pts',(-6.06897179667702,-2.99867266197861,
-10.1566979646801));
#45258=CARTESIAN_POINT('Ctrl Pts',(-5.98529045676721,-3.15730694550456,
-10.1482469411549));
#45259=CARTESIAN_POINT('Ctrl Pts',(-5.90168279578987,-3.31580155625909,
-10.1398033585047));
#45260=CARTESIAN_POINT('Ctrl Pts',(-5.81171536389781,-3.47108760120228,
-10.1313597758545));
#45261=CARTESIAN_POINT('Ctrl Pts',(-5.71565869118012,-3.62264195386974,
-10.1229161932043));
#45262=CARTESIAN_POINT('Ctrl Pts',(-5.61967353564768,-3.77408346960033,
-10.1144788970645));
#45263=CARTESIAN_POINT('Ctrl Pts',(-5.5176083537432,-3.92179855251581,-10.1060416009246));
#45264=CARTESIAN_POINT('Ctrl Pts',(-5.40977906859614,-4.06528958734542,
-10.0976043047847));
#45265=CARTESIAN_POINT('Ctrl Pts',(-5.30202671142249,-4.20867825226229,
-10.0891730280123));
#45266=CARTESIAN_POINT('Ctrl Pts',(-5.18851865223275,-4.34784861573657,
-10.0807417512399));
#45267=CARTESIAN_POINT('Ctrl Pts',(-5.06961361076516,-4.482332745072,-10.0723104744675));
#45268=CARTESIAN_POINT('Ctrl Pts',(-4.95075953630283,-4.61675922964112,
-10.0638828116456));
#45269=CARTESIAN_POINT('Ctrl Pts',(-4.82651331048086,-4.7465032366021,-10.0554551488237));
#45270=CARTESIAN_POINT('Ctrl Pts',(-4.69727375868692,-4.87113007791327,
-10.0470274860017));
#45271=CARTESIAN_POINT('Ctrl Pts',(-4.56807399193894,-4.9957185541532,-10.0386024175477));
#45272=CARTESIAN_POINT('Ctrl Pts',(-4.43388420300839,-5.11519277639464,
-10.0301773490938));
#45273=CARTESIAN_POINT('Ctrl Pts',(-4.29514013578894,-5.22915482787945,
-10.0217522806398));
#45274=CARTESIAN_POINT('Ctrl Pts',(-4.2571755121538,-5.2603383334521,-10.0194469240262));
#45275=CARTESIAN_POINT('Ctrl Pts',(-4.21887009675871,-5.2911093436752,-10.0171415674127));
#45276=CARTESIAN_POINT('Ctrl Pts',(-4.18023326724005,-5.32146021609291,
-10.0148362107991));
#45277=CARTESIAN_POINT('Ctrl Pts',(-4.03578256131235,-5.43493238761628,
-10.0062172222747));
#45278=CARTESIAN_POINT('Ctrl Pts',(-3.88676147890056,-5.54247817885556,
-9.9975982337502));
#45279=CARTESIAN_POINT('Ctrl Pts',(-3.73367981419581,-5.64375088439123,
-9.98897924522574));
#45280=CARTESIAN_POINT('Ctrl Pts',(-3.58050643991341,-5.74508426131475,
-9.98035509315803));
#45281=CARTESIAN_POINT('Ctrl Pts',(-3.42326788217518,-5.84013688462208,
-9.97173094109032));
#45282=CARTESIAN_POINT('Ctrl Pts',(-3.26250113558949,-5.92860652601244,
-9.9631067890226));
#45283=CARTESIAN_POINT('Ctrl Pts',(-3.09622808468068,-6.02010627642222,
-9.95418725742634));
#45284=CARTESIAN_POINT('Ctrl Pts',(-2.92618120058117,-6.1045639578302,-9.94526772583007));
#45285=CARTESIAN_POINT('Ctrl Pts',(-2.7529794746539,-6.18169823043267,-9.9363481942338));
#45286=CARTESIAN_POINT('Ctrl Pts',(-2.58520153368723,-6.25641705535153,
-9.92770797637456));
#45287=CARTESIAN_POINT('Ctrl Pts',(-2.41446364764021,-6.32426412338664,
-9.91906775851531));
#45288=CARTESIAN_POINT('Ctrl Pts',(-2.24134669418592,-6.38503359399634,
-9.91042754065607));
#45289=CARTESIAN_POINT('Ctrl Pts',(-2.05983517059483,-6.44874982154134,
-9.90136835219129));
#45290=CARTESIAN_POINT('Ctrl Pts',(-1.8757084891318,-6.50468487829986,-9.89230916372652));
#45291=CARTESIAN_POINT('Ctrl Pts',(-1.6896520389102,-6.55266090892903,-9.88324997526175));
#45292=CARTESIAN_POINT('Ctrl Pts',(-1.50359558868855,-6.60063693955821,
-9.87419078679697));
#45293=CARTESIAN_POINT('Ctrl Pts',(-1.31560975084686,-6.64065389679344,
-9.86513159833219));
#45294=CARTESIAN_POINT('Ctrl Pts',(-1.12639052691803,-6.67259570039047,
-9.85607240986742));
#45295=CARTESIAN_POINT('Ctrl Pts',(-0.937499112019785,-6.70448216705367,
-9.8470289158111));
#45296=CARTESIAN_POINT('Ctrl Pts',(-0.747204705913315,-6.72835164602761,
-9.83798542175478));
#45297=CARTESIAN_POINT('Ctrl Pts',(-0.556171843592307,-6.74410571391012,
-9.82894192769847));
#45298=CARTESIAN_POINT('Ctrl Pts',(-0.365313718332193,-6.75984537160433,
-9.81990670569311));
#45299=CARTESIAN_POINT('Ctrl Pts',(-0.173718722500571,-6.76748441897586,
-9.81087148368774));
#45300=CARTESIAN_POINT('Ctrl Pts',(0.0179432125647909,-6.76697621106524,
-9.80183626168238));
#45301=CARTESIAN_POINT('Ctrl Pts',(0.209267481025032,-6.76646889850632,
-9.79281695777124));
#45302=CARTESIAN_POINT('Ctrl Pts',(0.400658215445884,-6.75784299382939,
-9.78379765386011));
#45303=CARTESIAN_POINT('Ctrl Pts',(0.591445365356354,-6.74110386953046,
-9.77477834994897));
#45304=CARTESIAN_POINT('Ctrl Pts',(0.781993159461948,-6.72438574563208,
-9.76577036138454));
#45305=CARTESIAN_POINT('Ctrl Pts',(0.971938643774609,-6.69957473584734,
-9.75676237282008));
#45306=CARTESIAN_POINT('Ctrl Pts',(1.16061420527621,-6.66672810803854,-9.74775438425564));
#45307=CARTESIAN_POINT('Ctrl Pts',(1.34886363641287,-6.63395566548926,-9.73876674054892));
#45308=CARTESIAN_POINT('Ctrl Pts',(1.53584863573185,-6.59318387219167,-9.72977909684219));
#45309=CARTESIAN_POINT('Ctrl Pts',(1.72090959681955,-6.54452130866532,-9.72079145313548));
#45310=CARTESIAN_POINT('Ctrl Pts',(1.88208486731399,-6.50213958864607,-9.71296383840234));
#45311=CARTESIAN_POINT('Ctrl Pts',(2.04180067145334,-6.45377335070993,-9.70513622366922));
#45312=CARTESIAN_POINT('Ctrl Pts',(2.19962556666777,-6.39952626109633,-9.69730860893608));
#45313=CARTESIAN_POINT('Ctrl Pts',(2.36340938512926,-6.3432309886346,-9.68918545049079));
#45314=CARTESIAN_POINT('Ctrl Pts',(2.52508305395478,-6.28062598189569,-9.68106229204549));
#45315=CARTESIAN_POINT('Ctrl Pts',(2.68412823352618,-6.21190346238475,-9.6729391336002));
#45316=CARTESIAN_POINT('Ctrl Pts',(2.84316219958018,-6.14318578817104,-9.66481654788009));
#45317=CARTESIAN_POINT('Ctrl Pts',(2.99956770952428,-6.06835160550946,-9.65669396216));
#45318=CARTESIAN_POINT('Ctrl Pts',(3.15284677027445,-5.98764112511513,-9.64857137643989));
#45319=CARTESIAN_POINT('Ctrl Pts',(3.3061442490806,-5.90692094652629,-9.64044781470754));
#45320=CARTESIAN_POINT('Ctrl Pts',(3.45631420733181,-5.82032323579165,-9.63232425297518));
#45321=CARTESIAN_POINT('Ctrl Pts',(3.60288365155014,-5.72813393640483,-9.62420069124283));
#45322=CARTESIAN_POINT('Ctrl Pts',(3.74955985421652,-5.63587748805268,-9.61607121245971));
#45323=CARTESIAN_POINT('Ctrl Pts',(3.89262999478622,-5.53802151165535,-9.6079417336766));
#45324=CARTESIAN_POINT('Ctrl Pts',(4.0316499286213,-5.43489538565812,-9.59981225489348));
#45325=CARTESIAN_POINT('Ctrl Pts',(4.17072653843616,-5.33172721695471,-9.59167946186497));
#45326=CARTESIAN_POINT('Ctrl Pts',(4.30574936501194,-5.22328484499509,-9.58354666883644));
#45327=CARTESIAN_POINT('Ctrl Pts',(4.43630793002299,-5.10993747026469,-9.57541387580793));
#45328=CARTESIAN_POINT('Ctrl Pts',(4.56700845766692,-4.99646684745981,-9.56727223960079));
#45329=CARTESIAN_POINT('Ctrl Pts',(4.69323476170268,-4.87808081937901,-9.55913060339365));
#45330=CARTESIAN_POINT('Ctrl Pts',(4.81461322760548,-4.75518542946186,-9.55098896718652));
#45331=CARTESIAN_POINT('Ctrl Pts',(4.87645390731439,-4.69257189757183,-9.54684091412581));
#45332=CARTESIAN_POINT('Ctrl Pts',(4.93703683782887,-4.62878838726588,-9.54269286106512));
#45333=CARTESIAN_POINT('Ctrl Pts',(4.9963167156584,-4.56389179065767,-9.53854480800441));
#45334=CARTESIAN_POINT('Ctrl Pts',(5.11694307828481,-4.43183618119447,-9.53010409302633));
#45335=CARTESIAN_POINT('Ctrl Pts',(5.23241990530334,-4.29489774045607,-9.52166337804825));
#45336=CARTESIAN_POINT('Ctrl Pts',(5.34234744748511,-4.15350607924791,-9.51322266307017));
#45337=CARTESIAN_POINT('Ctrl Pts',(5.45219190125168,-4.01222128851841,-9.50478832798213));
#45338=CARTESIAN_POINT('Ctrl Pts',(5.55649522757408,-3.86649024942434,-9.49635399289409));
#45339=CARTESIAN_POINT('Ctrl Pts',(5.65489700380936,-3.71677667829371,-9.48791965780605));
#45340=CARTESIAN_POINT('Ctrl Pts',(5.75323951406211,-3.56715327750583,-9.4794904025974));
#45341=CARTESIAN_POINT('Ctrl Pts',(5.84568737782654,-3.41355240462048,-9.47106114738875));
#45342=CARTESIAN_POINT('Ctrl Pts',(5.93192244865042,-3.25646818857443,-9.4626318921801));
#45343=CARTESIAN_POINT('Ctrl Pts',(6.01811880913471,-3.09945448656969,-9.45420642080706));
#45344=CARTESIAN_POINT('Ctrl Pts',(6.09810777723121,-2.9389608509411,-9.44578094943403));
#45345=CARTESIAN_POINT('Ctrl Pts',(6.17161607998804,-2.77550787446785,-9.43735547806099));
#45346=CARTESIAN_POINT('Ctrl Pts',(6.24510265155741,-2.61210321943776,-9.42893249750179));
#45347=CARTESIAN_POINT('Ctrl Pts',(6.31211224186913,-2.44574127200291,-9.4205095169426));
#45348=CARTESIAN_POINT('Ctrl Pts',(6.37241867447862,-2.27696491785802,-9.4120865363834));
#45349=CARTESIAN_POINT('Ctrl Pts',(6.43272610563781,-2.10818576912604,-9.40366341635707));
#45350=CARTESIAN_POINT('Ctrl Pts',(6.48633003895352,-1.936992445479,-9.39524029633074));
#45351=CARTESIAN_POINT('Ctrl Pts',(6.53305314376033,-1.76394603681726,-9.38681717630442));
#45352=CARTESIAN_POINT('Ctrl Pts',(6.57977786433003,-1.59089364392205,-9.37839376499256));
#45353=CARTESIAN_POINT('Ctrl Pts',(6.61962119485132,-1.41598836017141,-9.36997035368069));
#45354=CARTESIAN_POINT('Ctrl Pts',(6.65245617608273,-1.23980475289408,-9.36154694236883));
#45355=CARTESIAN_POINT('Ctrl Pts',(6.68529687212382,-1.06359048149737,-9.3531220649927));
#45356=CARTESIAN_POINT('Ctrl Pts',(6.71112672590027,-0.886097770840552,
-9.34469718761657));
#45357=CARTESIAN_POINT('Ctrl Pts',(6.72987016234946,-0.707910021060919,
-9.33627231024044));
#45358=CARTESIAN_POINT('Ctrl Pts',(6.74861947588111,-0.529666399771182,
-9.32784479120897));
#45359=CARTESIAN_POINT('Ctrl Pts',(6.76027790719262,-0.350727636390128,
-9.31941727217751));
#45360=CARTESIAN_POINT('Ctrl Pts',(6.76482184169824,-0.171681245575883,
-9.31098975314604));
#45361=CARTESIAN_POINT('Ctrl Pts',(6.76936985102868,0.00752570712074452,
-9.30255467664126));
#45362=CARTESIAN_POINT('Ctrl Pts',(6.76679060691772,0.186840146404907,-9.29411960013649));
#45363=CARTESIAN_POINT('Ctrl Pts',(6.75711263952535,0.365674413606876,-9.28568452363171));
#45364=CARTESIAN_POINT('Ctrl Pts',(6.7474299947076,0.544595112587973,-9.2772453703989));
#45365=CARTESIAN_POINT('Ctrl Pts',(6.73064181025444,0.723034844344235,-9.26880621716608));
#45366=CARTESIAN_POINT('Ctrl Pts',(6.70682846627655,0.900411530325205,-9.26036706393327));
#45367=CARTESIAN_POINT('Ctrl Pts',(6.68298865899698,1.07798533153518,-9.25191853243515));
#45368=CARTESIAN_POINT('Ctrl Pts',(6.65210814530788,1.25449339711444,-9.24347000093703));
#45369=CARTESIAN_POINT('Ctrl Pts',(6.61431857154867,1.42936308685597,-9.23502146943891));
#45370=CARTESIAN_POINT('Ctrl Pts',(6.59343860596157,1.5259842640964,-9.23035338167305));
#45371=CARTESIAN_POINT('Ctrl Pts',(6.57045025428671,1.62210548785427,-9.2256852939072));
#45372=CARTESIAN_POINT('Ctrl Pts',(6.54538223735837,1.71763219778671,-9.22101720614135));
#45373=CARTESIAN_POINT('Ctrl Pts',(6.50112859164225,1.88626959698187,-9.2127764305446));
#45374=CARTESIAN_POINT('Ctrl Pts',(6.45029244045929,2.05342848501208,-9.20453565494785));
#45375=CARTESIAN_POINT('Ctrl Pts',(6.39298704908826,2.21855935016168,-9.19629487935111));
#45376=CARTESIAN_POINT('Ctrl Pts',(6.33574512965081,2.38350731497582,-9.18806323130674));
#45377=CARTESIAN_POINT('Ctrl Pts',(6.27204835323481,2.54643139644607,-9.17983158326238));
#45378=CARTESIAN_POINT('Ctrl Pts',(6.20206062487855,2.70679386088619,-9.171599935218));
#45379=CARTESIAN_POINT('Ctrl Pts',(6.13213794305246,2.86700728459976,-9.16337593765974));
#45380=CARTESIAN_POINT('Ctrl Pts',(6.05593609486273,3.02466350848271,-9.15515194010147));
#45381=CARTESIAN_POINT('Ctrl Pts',(5.97366829717051,3.17924143081019,-9.1469279425432));
#45382=CARTESIAN_POINT('Ctrl Pts',(5.8914731833971,3.33368278294286,-9.13871121091872));
#45383=CARTESIAN_POINT('Ctrl Pts',(5.8032229682675,3.48505094127598,-9.13049447929424));
#45384=CARTESIAN_POINT('Ctrl Pts',(5.70917827070372,3.6328463321925,-9.12227774766976));
#45385=CARTESIAN_POINT('Ctrl Pts',(5.61518175571999,3.78056600205895,-9.11406522578107));
#45386=CARTESIAN_POINT('Ctrl Pts',(5.51539686137002,3.92471625063394,-9.10585270389237));
#45387=CARTESIAN_POINT('Ctrl Pts',(5.4101294884512,4.06482323332649,-9.09764018200368));
#45388=CARTESIAN_POINT('Ctrl Pts',(5.30489731744878,4.20488336356935,-9.08943040642185));
#45389=CARTESIAN_POINT('Ctrl Pts',(5.19418653364245,4.34090263731415,-9.08122063084003));
#45390=CARTESIAN_POINT('Ctrl Pts',(5.07834564463575,4.47243720063335,-9.07301085525821));
#45391=CARTESIAN_POINT('Ctrl Pts',(5.02774935388386,4.52988808060059,-9.06942503857545));
#45392=CARTESIAN_POINT('Ctrl Pts',(4.97617491922371,4.58648381155589,-9.06583922189268));
#45393=CARTESIAN_POINT('Ctrl Pts',(4.92365379175857,4.64218939067564,-9.06225340520992));
#45394=CARTESIAN_POINT('Ctrl Pts',(4.79199371448726,4.78183225832386,-9.05326447210208));
#45395=CARTESIAN_POINT('Ctrl Pts',(4.65452043799943,4.9157320726033,-9.04427553899425));
#45396=CARTESIAN_POINT('Ctrl Pts',(4.51175443477957,5.04344732501955,-9.0352866058864));
#45397=CARTESIAN_POINT('Ctrl Pts',(4.37074449949692,5.16959163859321,-9.02640823955821));
#45398=CARTESIAN_POINT('Ctrl Pts',(4.22457154299096,5.28970256620136,-9.01752987323002));
#45399=CARTESIAN_POINT('Ctrl Pts',(4.0737664341739,5.40339856384832,-9.00865150690183));
#45400=CARTESIAN_POINT('Ctrl Pts',(3.92014424708681,5.51921843201182,-8.99960729040415));
#45401=CARTESIAN_POINT('Ctrl Pts',(3.76171540559239,5.62838120861716,-8.99056307390648));
#45402=CARTESIAN_POINT('Ctrl Pts',(3.59906836988956,5.73053190104204,-8.98151885740881));
#45403=CARTESIAN_POINT('Ctrl Pts',(3.43642133418668,5.83268259346696,-8.97247464091113));
#45404=CARTESIAN_POINT('Ctrl Pts',(3.2695563726811,5.9278211080299,-8.96343042441345));
#45405=CARTESIAN_POINT('Ctrl Pts',(3.09908550384723,6.01564277861011,-8.95438620791577));
#45406=CARTESIAN_POINT('Ctrl Pts',(3.0990855038472,6.01564277861013,-10.9542570414832));
#45407=CARTESIAN_POINT('Ctrl Pts',(2.94371122680837,6.0956871208962,-10.9460573085275));
#45408=CARTESIAN_POINT('Ctrl Pts',(2.78526207069075,6.16969346450379,-10.9378575755718));
#45409=CARTESIAN_POINT('Ctrl Pts',(2.62425162136487,6.23743476340746,-10.9296578426161));
#45410=CARTESIAN_POINT('Ctrl Pts',(2.46318476932544,6.305199792405,-10.9214552372556));
#45411=CARTESIAN_POINT('Ctrl Pts',(2.29955516720259,6.36669526584841,-10.9132526318951));
#45412=CARTESIAN_POINT('Ctrl Pts',(2.13389486804937,6.42174288586148,-10.9050500265346));
#45413=CARTESIAN_POINT('Ctrl Pts',(1.96804659819913,6.47685296706506,-10.896838113878));
#45414=CARTESIAN_POINT('Ctrl Pts',(1.80016336871473,6.52550046506747,-10.8886262012215));
#45415=CARTESIAN_POINT('Ctrl Pts',(1.63079185720553,6.56755714999665,-10.880414288565));
#45416=CARTESIAN_POINT('Ctrl Pts',(1.4613209119989,6.60963852533361,-10.8721975549038));
#45417=CARTESIAN_POINT('Ctrl Pts',(1.29036029374117,6.64512130188961,-10.8639808212426));
#45418=CARTESIAN_POINT('Ctrl Pts',(1.11846516112074,6.67392872926878,-10.8557640875815));
#45419=CARTESIAN_POINT('Ctrl Pts',(0.946304103210026,6.70278072232803,-10.8475346424651));
#45420=CARTESIAN_POINT('Ctrl Pts',(0.77320599739447,6.72493668341888,-10.8393051973487));
#45421=CARTESIAN_POINT('Ctrl Pts',(0.599730732672557,6.74037180341619,-10.8310757522323));
#45422=CARTESIAN_POINT('Ctrl Pts',(0.442190400473157,6.75438909824962,-10.8236022399737));
#45423=CARTESIAN_POINT('Ctrl Pts',(0.284339235273718,6.76286421240504,-10.8161287277152));
#45424=CARTESIAN_POINT('Ctrl Pts',(0.126594363644664,6.76581575769644,-10.8086552154566));
#45425=CARTESIAN_POINT('Ctrl Pts',(-0.0437590575373766,6.76900322003972,
-10.8005843452702));
#45426=CARTESIAN_POINT('Ctrl Pts',(-0.214544006950354,6.76575834722171,
-10.7925134750838));
#45427=CARTESIAN_POINT('Ctrl Pts',(-0.3852233321942,6.75602634574002,-10.7844426048974));
#45428=CARTESIAN_POINT('Ctrl Pts',(-0.555690260284677,6.7463064549777,-10.7763817782816));
#45429=CARTESIAN_POINT('Ctrl Pts',(-0.726051458031113,6.73011551924833,
-10.7683209516657));
#45430=CARTESIAN_POINT('Ctrl Pts',(-0.89576569172678,6.70745054588741,-10.7602601250499));
#45431=CARTESIAN_POINT('Ctrl Pts',(-1.06530594499202,6.6848088072413,-10.75220756189));
#45432=CARTESIAN_POINT('Ctrl Pts',(-1.23420018744348,6.65570628736731,-10.7441549987301));
#45433=CARTESIAN_POINT('Ctrl Pts',(-1.40190833073111,6.62019199360764,-10.7361024355702));
#45434=CARTESIAN_POINT('Ctrl Pts',(-1.56948127196993,6.58470633057028,-10.7280563641823));
#45435=CARTESIAN_POINT('Ctrl Pts',(-1.73586965415927,6.5428192586714,-10.7200102927945));
#45436=CARTESIAN_POINT('Ctrl Pts',(-1.90053975673978,6.49463144705314,-10.7119642214066));
#45437=CARTESIAN_POINT('Ctrl Pts',(-2.06511312617447,6.44647194269001,-10.7039228765707));
#45438=CARTESIAN_POINT('Ctrl Pts',(-2.22796986830822,6.39201917132693,-10.6958815317348));
#45439=CARTESIAN_POINT('Ctrl Pts',(-2.38858779255754,6.33142459145216,-10.6878401868989));
#45440=CARTESIAN_POINT('Ctrl Pts',(-2.55230193616371,6.26966193452742,-10.6796438296778));
#45441=CARTESIAN_POINT('Ctrl Pts',(-2.71368967910526,6.20151834684661,-10.6714474724568));
#45442=CARTESIAN_POINT('Ctrl Pts',(-2.87221520727613,6.12720725968134,-10.6632511152357));
#45443=CARTESIAN_POINT('Ctrl Pts',(-3.02769320701448,6.05432474464323,-10.6552123265272));
#45444=CARTESIAN_POINT('Ctrl Pts',(-3.18041770050255,5.9755098938006,-10.6471735378187));
#45445=CARTESIAN_POINT('Ctrl Pts',(-3.32990470562327,5.8910121075642,-10.6391347491102));
#45446=CARTESIAN_POINT('Ctrl Pts',(-3.47940770720776,5.8065052792992,-10.6310951001785));
#45447=CARTESIAN_POINT('Ctrl Pts',(-3.62567220541206,5.71631448847311,-10.6230554512467));
#45448=CARTESIAN_POINT('Ctrl Pts',(-3.76824039120981,5.62073423620571,-10.615015802315));
#45449=CARTESIAN_POINT('Ctrl Pts',(-3.91085206214143,5.52512483072967,-10.6069737011867));
#45450=CARTESIAN_POINT('Ctrl Pts',(-4.04976486650263,5.42412289957467,-10.5989316000585));
#45451=CARTESIAN_POINT('Ctrl Pts',(-4.18455158447879,5.31806515913787,-10.5908894989302));
#45452=CARTESIAN_POINT('Ctrl Pts',(-4.32388682462316,5.20842838665154,-10.5825760084855));
#45453=CARTESIAN_POINT('Ctrl Pts',(-4.45881228399271,5.09338887711495,-10.5742625180408));
#45454=CARTESIAN_POINT('Ctrl Pts',(-4.5888956721546,4.97336159052213,-10.5659490275961));
#45455=CARTESIAN_POINT('Ctrl Pts',(-4.71495423522875,4.8570479897513,-10.5578927594253));
#45456=CARTESIAN_POINT('Ctrl Pts',(-4.83646568675954,4.73605097442007,-10.5498364912546));
#45457=CARTESIAN_POINT('Ctrl Pts',(-4.95307667346797,4.61078306437719,-10.5417802230838));
#45458=CARTESIAN_POINT('Ctrl Pts',(-5.07527243141323,4.47951578291441,-10.5333381215021));
#45459=CARTESIAN_POINT('Ctrl Pts',(-5.19208647558606,4.3435588296383,-10.5248960199204));
#45460=CARTESIAN_POINT('Ctrl Pts',(-5.30316260749174,4.20342186301844,-10.5164539183387));
#45461=CARTESIAN_POINT('Ctrl Pts',(-5.41423873939742,4.06328489639858,-10.508011816757));
#45462=CARTESIAN_POINT('Ctrl Pts',(-5.51957675716195,3.91896833967192,-10.4995697151753));
#45463=CARTESIAN_POINT('Ctrl Pts',(-5.61887539771207,3.77101157051872,-10.4911276135935));
#45464=CARTESIAN_POINT('Ctrl Pts',(-5.7203506356957,3.61981163184953,-10.4825004635909));
#45465=CARTESIAN_POINT('Ctrl Pts',(-5.81582121332627,3.46436145607391,-10.4738733135882));
#45466=CARTESIAN_POINT('Ctrl Pts',(-5.90493347073066,3.30515502000206,-10.4652461635856));
#45467=CARTESIAN_POINT('Ctrl Pts',(-5.9939235529799,3.1461668599743,-10.4566308416234));
#45468=CARTESIAN_POINT('Ctrl Pts',(-6.07657254515671,2.98343297541944,-10.4480155196613));
#45469=CARTESIAN_POINT('Ctrl Pts',(-6.1525698941479,2.8174762993901,-10.4394001976991));
#45470=CARTESIAN_POINT('Ctrl Pts',(-6.22846946782509,2.65173313694149,-10.4307959598843));
#45471=CARTESIAN_POINT('Ctrl Pts',(-6.29773433308201,2.48277572998217,-10.4221917220694));
#45472=CARTESIAN_POINT('Ctrl Pts',(-6.36009942576228,2.31115215734887,-10.4135874842545));
#45473=CARTESIAN_POINT('Ctrl Pts',(-6.4223895239155,2.13973496344615,-10.4049935931051));
#45474=CARTESIAN_POINT('Ctrl Pts',(-6.47779628827751,1.96565828633327,-10.3963997019556));
#45475=CARTESIAN_POINT('Ctrl Pts',(-6.52610218492109,1.78949134447982,-10.3878058108061));
#45476=CARTESIAN_POINT('Ctrl Pts',(-6.57433558199768,1.61358880154843,-10.3792248177381));
#45477=CARTESIAN_POINT('Ctrl Pts',(-6.61548929352954,1.43560255063745,-10.37064382467));
#45478=CARTESIAN_POINT('Ctrl Pts',(-6.64939518380052,1.2561181033846,-10.3620628316019));
#45479=CARTESIAN_POINT('Ctrl Pts',(-6.68326992107623,1.07679856783558,-10.3534897228169));
#45480=CARTESIAN_POINT('Ctrl Pts',(-6.70991005583626,0.895983883167295,
-10.3449166140319));
#45481=CARTESIAN_POINT('Ctrl Pts',(-6.72919786552631,0.714272417636402,
-10.3363435052469));
#45482=CARTESIAN_POINT('Ctrl Pts',(-6.74846454119377,0.532760056839584,
-10.3277797901814));
#45483=CARTESIAN_POINT('Ctrl Pts',(-6.76039493087367,0.350353182417493,
-10.319216075116));
#45484=CARTESIAN_POINT('Ctrl Pts',(-6.76492274477394,0.167658155901406,
-10.3106523600505));
#45485=CARTESIAN_POINT('Ctrl Pts',(-6.76630308378061,0.111962167289865,
-10.3080416454303));
#45486=CARTESIAN_POINT('Ctrl Pts',(-6.76699580289412,0.0562394508427558,
-10.3054309308102));
#45487=CARTESIAN_POINT('Ctrl Pts',(-6.76699998098439,0.000507303923607805,
-10.30282021619));
#45488=CARTESIAN_POINT('',(-6.76699933288377,0.00183566786179907,-10.6971797838101));
#45489=CARTESIAN_POINT('Ctrl Pts',(3.09908550384727,6.01564277861009,-11.3484335646661));
#45490=CARTESIAN_POINT('Ctrl Pts',(2.92902828004936,6.10325135120861,-11.3394206331789));
#45491=CARTESIAN_POINT('Ctrl Pts',(2.7551659932718,6.1836904247374,-11.3304077016917));
#45492=CARTESIAN_POINT('Ctrl Pts',(2.57809464427906,6.25665381854707,-11.3213947702044));
#45493=CARTESIAN_POINT('Ctrl Pts',(2.40125969901093,6.32951980067408,-11.3123938716666));
#45494=CARTESIAN_POINT('Ctrl Pts',(2.2212244602406,6.39492992811433,-11.3033929731287));
#45495=CARTESIAN_POINT('Ctrl Pts',(2.03860694960393,6.45262510185014,-11.2943920745908));
#45496=CARTESIAN_POINT('Ctrl Pts',(1.85637556106118,6.51019828629142,-11.2854102073374));
#45497=CARTESIAN_POINT('Ctrl Pts',(1.67157302439807,6.56008900143514,-11.2764283400839));
#45498=CARTESIAN_POINT('Ctrl Pts',(1.48483461019973,6.60208718363769,-11.2674464728305));
#45499=CARTESIAN_POINT('Ctrl Pts',(1.4298548455648,6.61445234258211,-11.2648020198951));
#45500=CARTESIAN_POINT('Ctrl Pts',(1.37470739957853,6.62613366495919,-11.2621575669598));
#45501=CARTESIAN_POINT('Ctrl Pts',(1.31940879332319,6.63712659485273,-11.2595131140244));
#45502=CARTESIAN_POINT('Ctrl Pts',(1.14954404193941,6.67089437725803,-11.2513899555791));
#45503=CARTESIAN_POINT('Ctrl Pts',(0.97832774299963,6.69814765297914,-11.2432667971338));
#45504=CARTESIAN_POINT('Ctrl Pts',(0.806304555653694,6.71879170413342,-11.2351436386886));
#45505=CARTESIAN_POINT('Ctrl Pts',(0.634293496844222,6.73943429977388,-11.2270210529685));
#45506=CARTESIAN_POINT('Ctrl Pts',(0.461476026364602,6.75346855543135,-11.2188984672485));
#45507=CARTESIAN_POINT('Ctrl Pts',(0.288403368807972,6.76085146241657,-11.2107758815285));
#45508=CARTESIAN_POINT('Ctrl Pts',(0.115309914790117,6.76823525653405,-11.2026523197962));
#45509=CARTESIAN_POINT('Ctrl Pts',(-0.0580384216276527,6.76896609612683,
-11.1945287580639));
#45510=CARTESIAN_POINT('Ctrl Pts',(-0.231089006889341,6.76305307319815,
-11.1864051963316));
#45511=CARTESIAN_POINT('Ctrl Pts',(-0.404265638968567,6.75713574333389,
-11.1782757175485));
#45512=CARTESIAN_POINT('Ctrl Pts',(-0.577143720549638,6.74456489817517,
-11.1701462387654));
#45513=CARTESIAN_POINT('Ctrl Pts',(-0.749173691772695,6.72540168165112,
-11.1620167599823));
#45514=CARTESIAN_POINT('Ctrl Pts',(-0.921273796586807,6.70623065262101,
-11.1538839669538));
#45515=CARTESIAN_POINT('Ctrl Pts',(-1.09252474014897,6.68046194947762,-11.1457511739253));
#45516=CARTESIAN_POINT('Ctrl Pts',(-1.26238601742938,6.64820807007413,-11.1376183808968));
#45517=CARTESIAN_POINT('Ctrl Pts',(-1.43243199307947,6.61591911946997,-11.1294767446897));
#45518=CARTESIAN_POINT('Ctrl Pts',(-1.60108492812652,6.57713099016385,-11.1213351084826));
#45519=CARTESIAN_POINT('Ctrl Pts',(-1.76781763462296,6.53200656848385,-11.1131934722755));
#45520=CARTESIAN_POINT('Ctrl Pts',(-1.85276568387851,6.50901628855588,-11.1090454192145));
#45521=CARTESIAN_POINT('Ctrl Pts',(-1.93721556152399,6.48438204768635,-11.1048973661536));
#45522=CARTESIAN_POINT('Ctrl Pts',(-2.02109948946135,6.45813021343632,-11.1007493130927));
#45523=CARTESIAN_POINT('Ctrl Pts',(-2.19179169531306,6.40471135709549,-11.0923085981146));
#45524=CARTESIAN_POINT('Ctrl Pts',(-2.36049088578999,6.34448165293996,-11.0838678831365));
#45525=CARTESIAN_POINT('Ctrl Pts',(-2.52663542900019,6.2776112024337,-11.0754271681584));
#45526=CARTESIAN_POINT('Ctrl Pts',(-2.69265439233694,6.21079129576444,-11.0669928330703));
#45527=CARTESIAN_POINT('Ctrl Pts',(-2.85612224939063,6.13734077263783,-11.0585584979823));
#45528=CARTESIAN_POINT('Ctrl Pts',(-3.01649419109503,6.05747899666932,-11.0501241628943));
#45529=CARTESIAN_POINT('Ctrl Pts',(-3.17676954307263,5.97766532030627,-11.0416949076856));
#45530=CARTESIAN_POINT('Ctrl Pts',(-3.3339523994017,5.89144823764874,-11.033265652477));
#45531=CARTESIAN_POINT('Ctrl Pts',(-3.48751918108041,5.79909466741114,-11.0248363972683));
#45532=CARTESIAN_POINT('Ctrl Pts',(-3.64101702767104,5.70678255406563,-11.0164109258952));
#45533=CARTESIAN_POINT('Ctrl Pts',(-3.79090175091294,5.60833961712535,-11.0079854545222));
#45534=CARTESIAN_POINT('Ctrl Pts',(-3.93667523341055,5.50407822497573,-10.9995599831491));
#45535=CARTESIAN_POINT('Ctrl Pts',(-4.08240562103731,5.39984765551864,-10.9911370025898));
#45536=CARTESIAN_POINT('Ctrl Pts',(-4.22402692080827,5.28980225488819,-10.9827140220305));
#45537=CARTESIAN_POINT('Ctrl Pts',(-4.36107049680697,5.17429735537878,-10.9742910414712));
#45538=CARTESIAN_POINT('Ctrl Pts',(-4.49811634196246,5.05879054334829,-10.9658679214449));
#45539=CARTESIAN_POINT('Ctrl Pts',(-4.63058405276663,4.93782426158901,-10.9574448014186));
#45540=CARTESIAN_POINT('Ctrl Pts',(-4.75803804389615,4.81179415320699,-10.9490216813922));
#45541=CARTESIAN_POINT('Ctrl Pts',(-4.88549644259733,4.68575968649355,-10.9405982700803));
#45542=CARTESIAN_POINT('Ctrl Pts',(-5.00794053865764,4.55466127837574,-10.9321748587685));
#45543=CARTESIAN_POINT('Ctrl Pts',(-5.12497149428656,4.41893156574643,-10.9237514474566));
#45544=CARTESIAN_POINT('Ctrl Pts',(-5.24202281872921,4.2831782298525,-10.9153265700805));
#45545=CARTESIAN_POINT('Ctrl Pts',(-5.35365890662719,4.14279223496335,-10.9069016927044));
#45546=CARTESIAN_POINT('Ctrl Pts',(-5.45952088009703,3.99823970764443,-10.8984768153283));
#45547=CARTESIAN_POINT('Ctrl Pts',(-5.56541604702837,3.85364185528013,-10.8900492962969));
#45548=CARTESIAN_POINT('Ctrl Pts',(-5.66553329292517,3.70487513475965,-10.8816217772655));
#45549=CARTESIAN_POINT('Ctrl Pts',(-5.75955657208287,3.55243537491916,-10.8731942582341));
#45550=CARTESIAN_POINT('Ctrl Pts',(-5.85366416768367,3.39985891299328,-10.8647591817293));
#45551=CARTESIAN_POINT('Ctrl Pts',(-5.94166670178693,3.24360311429356,-10.8563241052246));
#45552=CARTESIAN_POINT('Ctrl Pts',(-6.0232931180757,3.08419017146186,-10.8478890287198));
#45553=CARTESIAN_POINT('Ctrl Pts',(-6.10495898494882,2.92470018330546,-10.8394498754871));
#45554=CARTESIAN_POINT('Ctrl Pts',(-6.18024244341045,2.7620503081495,-10.8310107222543));
#45555=CARTESIAN_POINT('Ctrl Pts',(-6.24892005217444,2.59678400748547,-10.8225715690215));
#45556=CARTESIAN_POINT('Ctrl Pts',(-6.31767398101696,2.43133404962553,-10.8141230375234));
#45557=CARTESIAN_POINT('Ctrl Pts',(-6.37980727148993,2.26326216751822,-10.8056745060253));
#45558=CARTESIAN_POINT('Ctrl Pts',(-6.43514553437091,2.09312946361809,-10.7972259745272));
#45559=CARTESIAN_POINT('Ctrl Pts',(-6.46572172006557,1.99912562474853,-10.7925578867614));
#45560=CARTESIAN_POINT('Ctrl Pts',(-6.49422432686232,1.90449288530371,-10.7878897989957));
#45561=CARTESIAN_POINT('Ctrl Pts',(-6.52063059142497,1.80932741375709,-10.7832217112299));
#45562=CARTESIAN_POINT('Ctrl Pts',(-6.57219902465109,1.6234800647978,-10.774105466421));
#45563=CARTESIAN_POINT('Ctrl Pts',(-6.61586758024389,1.43524805792121,-10.764989221612));
#45564=CARTESIAN_POINT('Ctrl Pts',(-6.65143297376662,1.24528245610789,-10.7558729768031));
#45565=CARTESIAN_POINT('Ctrl Pts',(-6.68690764314078,1.05580143961126,-10.746779986722));
#45566=CARTESIAN_POINT('Ctrl Pts',(-6.71432033728555,0.864595860334953,
-10.737686996641));
#45567=CARTESIAN_POINT('Ctrl Pts',(-6.73351772814808,0.672330279487316,
-10.72859400656));
#45568=CARTESIAN_POINT('Ctrl Pts',(-6.75264138544654,0.480803154538571,
-10.7195359409419));
#45569=CARTESIAN_POINT('Ctrl Pts',(-6.763612642134,0.288224363417974,-10.7104778753239));
#45570=CARTESIAN_POINT('Ctrl Pts',(-6.76632938619459,0.0952661404672239,
-10.7014198097059));
#45571=CARTESIAN_POINT('Ctrl Pts',(-6.76675328336554,0.0651586135911492,
-10.7000064677406));
#45572=CARTESIAN_POINT('Ctrl Pts',(-6.76697631772227,0.0350418758827705,
-10.6985931257754));
#45573=CARTESIAN_POINT('Ctrl Pts',(-6.76699821252111,0.00491850953762435,
-10.6971797838101));
#45574=CARTESIAN_POINT('Ctrl Pts',(-6.767,1.02749929591548E-12,-10.6971797838101));
#45575=CARTESIAN_POINT('Ctrl Pts',(-6.76700000000003,-0.186007249559046,
-10.6884302719974));
#45576=CARTESIAN_POINT('Ctrl Pts',(-6.75932637294252,-0.372014355815296,
-10.6796807601846));
#45577=CARTESIAN_POINT('Ctrl Pts',(-6.74400518263368,-0.557389537585737,
-10.6709312483719));
#45578=CARTESIAN_POINT('Ctrl Pts',(-6.72868405703735,-0.742763936382339,
-10.6621817735147));
#45579=CARTESIAN_POINT('Ctrl Pts',(-6.70571545643567,-0.927506130404779,
-10.6534322986574));
#45580=CARTESIAN_POINT('Ctrl Pts',(-6.67517739401575,-1.11098864009542,
-10.6446828238002));
#45581=CARTESIAN_POINT('Ctrl Pts',(-6.64463945804388,-1.2944703900455,-10.6359333851717));
#45582=CARTESIAN_POINT('Ctrl Pts',(-6.6065321700272,-1.47669218339297,-10.6271839465432));
#45583=CARTESIAN_POINT('Ctrl Pts',(-6.56098496085472,-1.65703510627813,
-10.6184345079147));
#45584=CARTESIAN_POINT('Ctrl Pts',(-6.51543793649544,-1.83737729740055,
-10.609685104788));
#45585=CARTESIAN_POINT('Ctrl Pts',(-6.46245112156878,-2.01584035545013,
-10.6009357016614));
#45586=CARTESIAN_POINT('Ctrl Pts',(-6.40220448361691,-2.19181813797484,
-10.5921862985348));
#45587=CARTESIAN_POINT('Ctrl Pts',(-6.34195808511944,-2.36779522106381,
-10.5834369301833));
#45588=CARTESIAN_POINT('Ctrl Pts',(-6.27445201416322,-2.54128677725824,
-10.5746875618317));
#45589=CARTESIAN_POINT('Ctrl Pts',(-6.19991555052688,-2.7117035542874,-10.5659381934802));
#45590=CARTESIAN_POINT('Ctrl Pts',(-6.12537937695072,-2.8821196681362,-10.557188859177));
#45591=CARTESIAN_POINT('Ctrl Pts',(-6.04381298028289,-3.04946076419993,
-10.5484395248738));
#45592=CARTESIAN_POINT('Ctrl Pts',(-5.95549339308802,-3.21315848424646,
-10.5396901905706));
#45593=CARTESIAN_POINT('Ctrl Pts',(-5.86717414225629,-3.37685558085395,
-10.5309408895891));
#45594=CARTESIAN_POINT('Ctrl Pts',(-5.77210188843887,-3.53690907700292,
-10.5221915886075));
#45595=CARTESIAN_POINT('Ctrl Pts',(-5.67059953311195,-3.69277537024263,
-10.513442287626));
#45596=CARTESIAN_POINT('Ctrl Pts',(-5.56909755592501,-3.84864108281328,
-10.5046930192393));
#45597=CARTESIAN_POINT('Ctrl Pts',(-5.46116568154727,-4.00031938355157,
-10.4959437508527));
#45598=CARTESIAN_POINT('Ctrl Pts',(-5.34717048488103,-4.14729511918517,
-10.4871944824661));
#45599=CARTESIAN_POINT('Ctrl Pts',(-5.2331757034302,-4.29427031947526,-10.4784452459477));
#45600=CARTESIAN_POINT('Ctrl Pts',(-5.11311781951251,-4.43654276249897,
-10.4696960094294));
#45601=CARTESIAN_POINT('Ctrl Pts',(-4.98740458928937,-4.57362924412718,
-10.460946772911));
#45602=CARTESIAN_POINT('Ctrl Pts',(-4.86169180652416,-4.71071523781602,
-10.4521975675343));
#45603=CARTESIAN_POINT('Ctrl Pts',(-4.73032391141232,-4.84261509584822,
-10.4434483621576));
#45604=CARTESIAN_POINT('Ctrl Pts',(-4.59374706946971,-4.96888084599928,
-10.4346991567809));
#45605=CARTESIAN_POINT('Ctrl Pts',(-4.45717070231174,-5.09514615721033,
-10.4259499818192));
#45606=CARTESIAN_POINT('Ctrl Pts',(-4.31538563497053,-5.21577720520837,
-10.4172008068575));
#45607=CARTESIAN_POINT('Ctrl Pts',(-4.16887340951759,-5.33036429293695,
-10.4084516318958));
#45608=CARTESIAN_POINT('Ctrl Pts',(-4.02236168122231,-5.44495099183894,
-10.3997024866225));
#45609=CARTESIAN_POINT('Ctrl Pts',(-3.8711230526292,-5.5534935949811,-10.3909533413493));
#45610=CARTESIAN_POINT('Ctrl Pts',(-3.71567116928729,-5.65562346357387,
-10.382204196076));
#45611=CARTESIAN_POINT('Ctrl Pts',(-3.56021980053062,-5.75775299409081,
-10.3734550797647));
#45612=CARTESIAN_POINT('Ctrl Pts',(-3.40055544441853,-5.85346967520012,
-10.3647059634533));
#45613=CARTESIAN_POINT('Ctrl Pts',(-3.23722035886631,-5.94244843041498,
-10.3559568471419));
#45614=CARTESIAN_POINT('Ctrl Pts',(-3.07388580043301,-6.03142689847546,
-10.3472077590659));
#45615=CARTESIAN_POINT('Ctrl Pts',(-2.90688078789058,-6.11366734707979,
-10.33845867099));
#45616=CARTESIAN_POINT('Ctrl Pts',(-2.73677250610253,-6.1888904700149,-10.329709582914));
#45617=CARTESIAN_POINT('Ctrl Pts',(-2.56666475916788,-6.26411335643394,
-10.3209605223468));
#45618=CARTESIAN_POINT('Ctrl Pts',(-2.39345402456939,-6.33231884545314,
-10.3122114617796));
#45619=CARTESIAN_POINT('Ctrl Pts',(-2.21772855943905,-6.39327529804938,
-10.3034624012124));
#45620=CARTESIAN_POINT('Ctrl Pts',(-2.04200363223433,-6.45423156404753,
-10.2947133674276));
#45621=CARTESIAN_POINT('Ctrl Pts',(-1.86376426060878,-6.50793874412498,
-10.2859643336428));
#45622=CARTESIAN_POINT('Ctrl Pts',(-1.68361577621535,-6.55421443943352,
-10.277215299858));
#45623=CARTESIAN_POINT('Ctrl Pts',(-1.50346782833053,-6.60048999692625,
-10.2684662921291));
#45624=CARTESIAN_POINT('Ctrl Pts',(-1.32141105657216,-6.63933404265196,
-10.2597172844002));
#45625=CARTESIAN_POINT('Ctrl Pts',(-1.13806375346355,-6.6706146563156,-10.2509682766713));
#45626=CARTESIAN_POINT('Ctrl Pts',(-0.954716981168329,-6.70189517941794,
-10.2422192942719));
#45627=CARTESIAN_POINT('Ctrl Pts',(-0.770079967440725,-6.72561226609021,
-10.2334703118725));
#45628=CARTESIAN_POINT('Ctrl Pts',(-0.58477976407164,-6.74168536995997,
-10.224721329473));
#45629=CARTESIAN_POINT('Ctrl Pts',(-0.391489587591469,-6.75845153117881,
-10.2155950990574));
#45630=CARTESIAN_POINT('Ctrl Pts',(-0.197478091803694,-6.76689985146399,
-10.2064688686418));
#45631=CARTESIAN_POINT('Ctrl Pts',(-0.00346214752943487,-6.76699911434415,
-10.1973426382262));
#45632=CARTESIAN_POINT('Ctrl Pts',(0.18449079848621,-6.76709527525931,-10.1885016025111));
#45633=CARTESIAN_POINT('Ctrl Pts',(0.372447602156321,-6.75935633790754,
-10.1796605667959));
#45634=CARTESIAN_POINT('Ctrl Pts',(0.559756448195727,-6.74380914014501,
-10.1708195310808));
#45635=CARTESIAN_POINT('Ctrl Pts',(0.74513613104485,-6.72842206873138,-10.1620695524675));
#45636=CARTESIAN_POINT('Ctrl Pts',(0.929880851946518,-6.70538686355703,
-10.1533195738542));
#45637=CARTESIAN_POINT('Ctrl Pts',(1.11336305057608,-6.67478177303288,-10.1445695952409));
#45638=CARTESIAN_POINT('Ctrl Pts',(1.29684337090276,-6.64417699581231,-10.1358197062009));
#45639=CARTESIAN_POINT('Ctrl Pts',(1.47906091205349,-6.60600253548024,-10.1270698171609));
#45640=CARTESIAN_POINT('Ctrl Pts',(1.65939671095387,-6.5603880644117,-10.1183199281209));
#45641=CARTESIAN_POINT('Ctrl Pts',(1.83973072369326,-6.51477404513803,-10.1095701257455));
#45642=CARTESIAN_POINT('Ctrl Pts',(2.01818275357201,-6.46172023288609,-10.10082032337));
#45643=CARTESIAN_POINT('Ctrl Pts',(2.1941466403349,-6.40140683918052,-10.0920705209945));
#45644=CARTESIAN_POINT('Ctrl Pts',(2.37010884271419,-6.34109402281438,-10.0833208023749));
#45645=CARTESIAN_POINT('Ctrl Pts',(2.54358267847961,-6.27352185699729,-10.0745710837554));
#45646=CARTESIAN_POINT('Ctrl Pts',(2.71397890841893,-6.19891986435195,-10.0658213651359));
#45647=CARTESIAN_POINT('Ctrl Pts',(2.88437356389095,-6.12431856103171,-10.057071727364));
#45648=CARTESIAN_POINT('Ctrl Pts',(3.05169040787327,-6.04268767582479,-10.0483220895922));
#45649=CARTESIAN_POINT('Ctrl Pts',(3.2153611251221,-5.95430447953861,-10.0395724518204));
#45650=CARTESIAN_POINT('Ctrl Pts',(3.37903038442994,-5.86592207054955,-10.0308228919883));
#45651=CARTESIAN_POINT('Ctrl Pts',(3.5390533298012,-5.77078760703287,-10.0220733321563));
#45652=CARTESIAN_POINT('Ctrl Pts',(3.69488643042035,-5.66922422085206,-10.0133237723242));
#45653=CARTESIAN_POINT('Ctrl Pts',(3.85071819468886,-5.56766170563059,-10.0045742875242));
#45654=CARTESIAN_POINT('Ctrl Pts',(4.00235994599368,-5.45967053456146,-9.9958248027242));
#45655=CARTESIAN_POINT('Ctrl Pts',(4.14929662974445,-5.34561750206572,-9.9870753179242));
#45656=CARTESIAN_POINT('Ctrl Pts',(4.29623210225178,-5.23156540974356,-9.97832590524885));
#45657=CARTESIAN_POINT('Ctrl Pts',(4.43846235842242,-5.11145173172078,-9.96957649257349));
#45658=CARTESIAN_POINT('Ctrl Pts',(4.57550431797543,-4.98568443006456,-9.96082707989814));
#45659=CARTESIAN_POINT('Ctrl Pts',(4.71254519337612,-4.85991812336575,-9.95207773644024));
#45660=CARTESIAN_POINT('Ctrl Pts',(4.84439764315105,-4.72849847630977,-9.94332839298234));
#45661=CARTESIAN_POINT('Ctrl Pts',(4.9706138419681,-4.5918718442521,-9.93457904952444));
#45662=CARTESIAN_POINT('Ctrl Pts',(5.09682908420336,-4.45524624767599,-9.92582977237707));
#45663=CARTESIAN_POINT('Ctrl Pts',(5.21740796650306,-4.31341395556729,-9.91708049522971));
#45664=CARTESIAN_POINT('Ctrl Pts',(5.33194095942391,-4.16685668162677,-9.90833121808234));
#45665=CARTESIAN_POINT('Ctrl Pts',(5.44647312235277,-4.0203004697502,-9.89958200433879));
#45666=CARTESIAN_POINT('Ctrl Pts',(5.55495930712435,-3.86901957035337,-9.89083279059525));
#45667=CARTESIAN_POINT('Ctrl Pts',(5.65703106079944,-3.71352778058148,-9.88208357685171));
#45668=CARTESIAN_POINT('Ctrl Pts',(5.75910210868873,-3.55803706597381,-9.87333442360551));
#45669=CARTESIAN_POINT('Ctrl Pts',(5.85475865698675,-3.39833575880683,-9.86458527035931));
#45670=CARTESIAN_POINT('Ctrl Pts',(5.94367583069178,-3.2349662470651,-9.85583611711312));
#45671=CARTESIAN_POINT('Ctrl Pts',(6.03259241910188,-3.07159781069882,-9.847087021458));
#45672=CARTESIAN_POINT('Ctrl Pts',(6.11476958471074,-2.90456146975609,-9.83833792580288));
#45673=CARTESIAN_POINT('Ctrl Pts',(6.18992823574488,-2.73442451648026,-9.82958883014776));
#45674=CARTESIAN_POINT('Ctrl Pts',(6.26508641701031,-2.56428862662182,-9.82083978917764));
#45675=CARTESIAN_POINT('Ctrl Pts',(6.33322605570386,-2.3910524253104,-9.81209074820753));
#45676=CARTESIAN_POINT('Ctrl Pts',(6.3941157374785,-2.21530425353489,-9.80334170723741));
#45677=CARTESIAN_POINT('Ctrl Pts',(6.45500505889206,-2.03955712188307,-9.79459271804641));
#45678=CARTESIAN_POINT('Ctrl Pts',(6.50864441545006,-1.86129832025304,-9.7858437288554));
#45679=CARTESIAN_POINT('Ctrl Pts',(6.55485164049979,-1.68113324012027,-9.7770947396644));
#45680=CARTESIAN_POINT('Ctrl Pts',(6.60199852639174,-1.49730435912615,-9.76816783278752));
#45681=CARTESIAN_POINT('Ctrl Pts',(6.64140767441066,-1.31149113173366,-9.75924092591062));
#45682=CARTESIAN_POINT('Ctrl Pts',(6.6729397526965,-1.12435050446145,-9.75031401903374));
#45683=CARTESIAN_POINT('Ctrl Pts',(6.70384664831547,-0.940920291560891,
-9.74156410484975));
#45684=CARTESIAN_POINT('Ctrl Pts',(6.72718585889698,-0.756215114275096,
-9.73281419066575));
#45685=CARTESIAN_POINT('Ctrl Pts',(6.74287810451888,-0.570862389372309,
-9.72406427648176));
#45686=CARTESIAN_POINT('Ctrl Pts',(6.75857004154139,-0.385513309565321,
-9.71531453437118));
#45687=CARTESIAN_POINT('Ctrl Pts',(6.76661529035564,-0.199516993256485,
-9.7065647922606));
#45688=CARTESIAN_POINT('Ctrl Pts',(6.76698652348897,-0.0135052182023869,
-9.69781505015002));
#45689=CARTESIAN_POINT('Ctrl Pts',(6.76735774981517,0.172503146040514,-9.68906546847938));
#45690=CARTESIAN_POINT('Ctrl Pts',(6.76005524147471,0.358526681835042,-9.68031588680874));
#45691=CARTESIAN_POINT('Ctrl Pts',(6.74510380214869,0.543933542116385,-9.6715663051381));
#45692=CARTESIAN_POINT('Ctrl Pts',(6.73015261710963,0.729337249086165,-9.66281687227618));
#45693=CARTESIAN_POINT('Ctrl Pts',(6.70755278444587,0.914124015856029,-9.65406743941425));
#45694=CARTESIAN_POINT('Ctrl Pts',(6.67738106408268,1.09766621749515,-9.64531800655233));
#45695=CARTESIAN_POINT('Ctrl Pts',(6.6472098167723,1.28120554143443,-9.63656871086998));
#45696=CARTESIAN_POINT('Ctrl Pts',(6.60946696581497,1.46350005650733,-9.62781941518764));
#45697=CARTESIAN_POINT('Ctrl Pts',(6.56428070010968,1.6439306220664,-9.6190701195053));
#45698=CARTESIAN_POINT('Ctrl Pts',(6.51909508282712,1.82435859844753,-9.61032094937531));
#45699=CARTESIAN_POINT('Ctrl Pts',(6.46646633415632,2.00292240086659,-9.60157177924532));
#45700=CARTESIAN_POINT('Ctrl Pts',(6.40657319597161,2.17901557696546,-9.59282260911533));
#45701=CARTESIAN_POINT('Ctrl Pts',(6.34668083768265,2.35510646007513,-9.58407355291226));
#45702=CARTESIAN_POINT('Ctrl Pts',(6.27952437143858,2.52872650996598,-9.57532449670918));
#45703=CARTESIAN_POINT('Ctrl Pts',(6.20533187335112,2.6992860799798,-9.56657544050611));
#45704=CARTESIAN_POINT('Ctrl Pts',(6.12831449784227,2.8763397011545,-9.55749326421726));
#45705=CARTESIAN_POINT('Ctrl Pts',(6.04371489463128,3.05009490562399,-9.54841108792844));
#45706=CARTESIAN_POINT('Ctrl Pts',(5.95184265120465,3.21991584599679,-9.53932891163959));
#45707=CARTESIAN_POINT('Ctrl Pts',(5.86333281335461,3.38352155905355,-9.53057913128517));
#45708=CARTESIAN_POINT('Ctrl Pts',(5.76807337235648,3.54347560903884,-9.52182935093074));
#45709=CARTESIAN_POINT('Ctrl Pts',(5.66638790086312,3.69923467178713,-9.51307957057632));
#45710=CARTESIAN_POINT('Ctrl Pts',(5.56470608502698,3.85498813489829,-9.50433010478206));
#45711=CARTESIAN_POINT('Ctrl Pts',(5.45659885766906,4.00654667256325,-9.49558063898779));
#45712=CARTESIAN_POINT('Ctrl Pts',(5.34243340580459,4.15339551506273,-9.48683117319353));
#45713=CARTESIAN_POINT('Ctrl Pts',(5.22827145140537,4.3002398588394,-9.47808197543966));
#45714=CARTESIAN_POINT('Ctrl Pts',(5.10805181978023,4.44237456993119,-9.46933277768577));
#45715=CARTESIAN_POINT('Ctrl Pts',(4.98218281282476,4.57931691626531,-9.4605835799319));
#45716=CARTESIAN_POINT('Ctrl Pts',(4.85631699296158,4.71625579512234,-9.4518346037139));
#45717=CARTESIAN_POINT('Ctrl Pts',(4.72480227791772,4.84800236135833,-9.44308562749591));
#45718=CARTESIAN_POINT('Ctrl Pts',(4.58808530848053,4.97410918678964,-9.43433665127791));
#45719=CARTESIAN_POINT('Ctrl Pts',(4.45135945056902,5.10022421089068,-9.42558710625671));
#45720=CARTESIAN_POINT('Ctrl Pts',(4.30943087207964,5.22069856612049,-9.41683756123551));
#45721=CARTESIAN_POINT('Ctrl Pts',(4.16278164322383,5.3351230530175,-9.40808801621431));
#45722=CARTESIAN_POINT('Ctrl Pts',(4.01614103534304,5.4495408133149,-9.39933898554705));
#45723=CARTESIAN_POINT('Ctrl Pts',(3.86478055833326,5.55790924068398,-9.39058995487979));
#45724=CARTESIAN_POINT('Ctrl Pts',(3.70921425811863,5.65986029751349,-9.38184092421253));
#45725=CARTESIAN_POINT('Ctrl Pts',(3.55364584530037,5.76181273884705,-9.37309177473269));
#45726=CARTESIAN_POINT('Ctrl Pts',(3.39387173464268,5.85734747818107,-9.36434262525284));
#45727=CARTESIAN_POINT('Ctrl Pts',(3.23043456092335,5.94614005448846,-9.355593475773));
#45728=CARTESIAN_POINT('Ctrl Pts',(3.18690768806344,5.96978744811307,-9.35326338703997));
#45729=CARTESIAN_POINT('Ctrl Pts',(3.14312114982855,5.99295688499314,-9.35093329830694));
#45730=CARTESIAN_POINT('Ctrl Pts',(3.09908550384716,6.01564277861015,-9.34860320957391));
#45731=CARTESIAN_POINT('Origin',(0.,0.,-63.6971797838103));
#45732=CARTESIAN_POINT('',(3.09908550384728,6.01564277861009,-6.95401477785999));
#45733=CARTESIAN_POINT('',(3.09908550384714,6.01564277861016,-7.34868366182765));
#45734=CARTESIAN_POINT('',(3.09908550384721,6.01564277861012,-63.6971797838103));
#45735=CARTESIAN_POINT('',(-6.76699555771448,-0.00775382954289589,-8.30282021621437));
#45736=CARTESIAN_POINT('Ctrl Pts',(-6.76699555771388,-0.0077538300588502,
-8.30282021618999));
#45737=CARTESIAN_POINT('Ctrl Pts',(-6.76671757908296,-0.250353957523485,
-8.2913582776441));
#45738=CARTESIAN_POINT('Ctrl Pts',(-6.75339413019389,-0.492429368534453,
-8.27989633909821));
#45739=CARTESIAN_POINT('Ctrl Pts',(-6.72719065642958,-0.732935789852377,
-8.26843440055233));
#45740=CARTESIAN_POINT('Ctrl Pts',(-6.70813841430844,-0.907805221739758,
-8.26010055785963));
#45741=CARTESIAN_POINT('Ctrl Pts',(-6.68223907331561,-1.08215501582084,
-8.25176671516695));
#45742=CARTESIAN_POINT('Ctrl Pts',(-6.64952771791692,-1.25541631686646,
-8.24343287247425));
#45743=CARTESIAN_POINT('Ctrl Pts',(-6.61685491698888,-1.42847340754959,
-8.23510885226948));
#45744=CARTESIAN_POINT('Ctrl Pts',(-6.57738615977623,-1.60044422200792,
-8.2267848320647));
#45745=CARTESIAN_POINT('Ctrl Pts',(-6.53120830826043,-1.77076453378476,
-8.21846081185993));
#45746=CARTESIAN_POINT('Ctrl Pts',(-6.48507641654277,-1.94091532950809,
-8.21014507636905));
#45747=CARTESIAN_POINT('Ctrl Pts',(-6.43224882461589,-2.10941856173476,
-8.20182934087818));
#45748=CARTESIAN_POINT('Ctrl Pts',(-6.37286354758082,-2.275719491483,-8.1935136053873));
#45749=CARTESIAN_POINT('Ctrl Pts',(-6.3135264944873,-2.44188537620464,-8.18520462270727));
#45750=CARTESIAN_POINT('Ctrl Pts',(-6.24764248369236,-2.60585219580411,
-8.17689564002723));
#45751=CARTESIAN_POINT('Ctrl Pts',(-6.17539959654923,-2.76707947535658,
-8.1685866573472));
#45752=CARTESIAN_POINT('Ctrl Pts',(-6.10320214490235,-2.92820535473328,
-8.16028290041002));
#45753=CARTESIAN_POINT('Ctrl Pts',(-6.02465392885783,-3.08659481122614,
-8.15197914347284));
#45754=CARTESIAN_POINT('Ctrl Pts',(-5.93999155697001,-3.24172628442394,
-8.14367538653566));
#45755=CARTESIAN_POINT('Ctrl Pts',(-5.85536355596431,-3.39679477798321,
-8.13537500072362));
#45756=CARTESIAN_POINT('Ctrl Pts',(-5.76462651144932,-3.54860761892777,
-8.12707461491158));
#45757=CARTESIAN_POINT('Ctrl Pts',(-5.66806361718742,-3.69666658376384,
-8.11877422909955));
#45758=CARTESIAN_POINT('Ctrl Pts',(-5.57152108552739,-3.84469432681668,
-8.11047559362291));
#45759=CARTESIAN_POINT('Ctrl Pts',(-5.46915534151305,-3.98896947966734,
-8.10217695814627));
#45760=CARTESIAN_POINT('Ctrl Pts',(-5.36129379228389,-4.12902141830462,
-8.09387832266963));
#45761=CARTESIAN_POINT('Ctrl Pts',(-5.25343708446977,-4.26906707064649,
-8.08558005968105));
#45762=CARTESIAN_POINT('Ctrl Pts',(-5.14008527535029,-4.40488961110492,
-8.07728179669246));
#45763=CARTESIAN_POINT('Ctrl Pts',(-5.02160718726101,-4.53605007212757,
-8.06898353370387));
#45764=CARTESIAN_POINT('Ctrl Pts',(-4.90311475198104,-4.66722641612214,
-8.06068426583106));
#45765=CARTESIAN_POINT('Ctrl Pts',(-4.77949503433162,-4.79373929806913,
-8.05238499795825));
#45766=CARTESIAN_POINT('Ctrl Pts',(-4.65115509386475,-4.91518517380739,
-8.04408573008544));
#45767=CARTESIAN_POINT('Ctrl Pts',(-4.52272503807419,-5.03671632412474,
-8.03578063478893));
#45768=CARTESIAN_POINT('Ctrl Pts',(-4.38956838971817,-5.15317311968058,
-8.02747553949242));
#45769=CARTESIAN_POINT('Ctrl Pts',(-4.2521274748599,-5.2641904351516,-8.01917044419591));
#45770=CARTESIAN_POINT('Ctrl Pts',(-4.1146364418973,-5.37524823330862,-8.0108623204298));
#45771=CARTESIAN_POINT('Ctrl Pts',(-3.97285830377808,-5.48086238521259,
-8.00255419666371));
#45772=CARTESIAN_POINT('Ctrl Pts',(-3.82726617535817,-5.58070986729818,
-7.9942460728976));
#45773=CARTESIAN_POINT('Ctrl Pts',(-3.68151928334678,-5.68066348668044,
-7.98592911764392));
#45774=CARTESIAN_POINT('Ctrl Pts',(-3.53195059187763,-5.7748379980757,-7.97761216239025));
#45775=CARTESIAN_POINT('Ctrl Pts',(-3.37906066141835,-5.86295471980255,
-7.96929520713657));
#45776=CARTESIAN_POINT('Ctrl Pts',(-3.26638310883645,-5.92789540305026,
-7.96316573765416));
#45777=CARTESIAN_POINT('Ctrl Pts',(-3.15190219783778,-5.98954675271497,
-7.95703626817173));
#45778=CARTESIAN_POINT('Ctrl Pts',(-3.03582580395668,-6.04781371141926,
-7.95090679868932));
#45779=CARTESIAN_POINT('Ctrl Pts',(-2.87578514493605,-6.12814944686357,
-7.94245577516412));
#45780=CARTESIAN_POINT('Ctrl Pts',(-2.71241830995243,-6.20219665234776,
-7.9340047516389));
#45781=CARTESIAN_POINT('Ctrl Pts',(-2.54624649463297,-6.26968243123759,
-7.92555372811368));
#45782=CARTESIAN_POINT('Ctrl Pts',(-2.38022098865794,-6.33710879090492,
-7.9171101454635));
#45783=CARTESIAN_POINT('Ctrl Pts',(-2.21139573062863,-6.39798511476414,
-7.90866656281331));
#45784=CARTESIAN_POINT('Ctrl Pts',(-2.04031455288437,-6.45208536252337,
-7.90022298016313));
#45785=CARTESIAN_POINT('Ctrl Pts',(-1.86936075040631,-6.50614533096285,
-7.89178568402326));
#45786=CARTESIAN_POINT('Ctrl Pts',(-1.69615469144868,-6.55343918065076,
-7.88334838788341));
#45787=CARTESIAN_POINT('Ctrl Pts',(-1.52125851104757,-6.59378961922242,
-7.87491109174353));
#45788=CARTESIAN_POINT('Ctrl Pts',(-1.34648710573618,-6.63411127083269,
-7.86647981497115));
#45789=CARTESIAN_POINT('Ctrl Pts',(-1.17002830631589,-6.66749931776143,
-7.85804853819875));
#45790=CARTESIAN_POINT('Ctrl Pts',(-0.992457877972095,-6.69382673516809,
-7.84961726142637));
#45791=CARTESIAN_POINT('Ctrl Pts',(-0.814963562742269,-6.72014286769056,
-7.84118959860444));
#45792=CARTESIAN_POINT('Ctrl Pts',(-0.636358895781466,-6.73940435551116,
-7.8327619357825));
#45793=CARTESIAN_POINT('Ctrl Pts',(-0.457228919895582,-6.75153543387066,
-7.82433427296057));
#45794=CARTESIAN_POINT('Ctrl Pts',(-0.278154087300592,-6.76366277780448,
-7.81590920450656));
#45795=CARTESIAN_POINT('Ctrl Pts',(-0.0985545986133285,-6.76866406733705,
-7.80748413605254));
#45796=CARTESIAN_POINT('Ctrl Pts',(0.0809799350677422,-6.76651544372112,
-7.79905906759853));
#45797=CARTESIAN_POINT('Ctrl Pts',(0.130106078891218,-6.76592751453216,
-7.79675371098491));
#45798=CARTESIAN_POINT('Ctrl Pts',(0.179227345766093,-6.76480454548256,
-7.7944483543713));
#45799=CARTESIAN_POINT('Ctrl Pts',(0.228331639799978,-6.76314672783803,
-7.79214299775768));
#45800=CARTESIAN_POINT('Ctrl Pts',(0.411916836239953,-6.75694867970556,
-7.78352400923331));
#45801=CARTESIAN_POINT('Ctrl Pts',(0.595182676320826,-6.74327344386702,
-7.77490502070893));
#45802=CARTESIAN_POINT('Ctrl Pts',(0.777515869642375,-6.72218402548266,
-7.76628603218456));
#45803=CARTESIAN_POINT('Ctrl Pts',(0.959958296818278,-6.70108197265465,
-7.7576618801169));
#45804=CARTESIAN_POINT('Ctrl Pts',(1.14146666002476,-6.67255690783578,-7.74903772804925));
#45805=CARTESIAN_POINT('Ctrl Pts',(1.32143549775019,-6.63672338019943,-7.74041357598159));
#45806=CARTESIAN_POINT('Ctrl Pts',(1.50756831658762,-6.59966254460066,-7.73149404438532));
#45807=CARTESIAN_POINT('Ctrl Pts',(1.69205393505231,-6.5547838266985,-7.72257451278904));
#45808=CARTESIAN_POINT('Ctrl Pts',(1.87423760706012,-6.50227055668107,-7.71365498119277));
#45809=CARTESIAN_POINT('Ctrl Pts',(2.05071622586826,-6.4514017315024,-7.70501476333362));
#45810=CARTESIAN_POINT('Ctrl Pts',(2.22503461206296,-6.39336940769518,-7.69637454547447));
#45811=CARTESIAN_POINT('Ctrl Pts',(2.39661579557263,-6.32839013718432,-7.68773432761533));
#45812=CARTESIAN_POINT('Ctrl Pts',(2.57651707859292,-6.26025997340115,-7.67867513915049));
#45813=CARTESIAN_POINT('Ctrl Pts',(2.75340874473678,-6.18449254074994,-7.66961595068564));
#45814=CARTESIAN_POINT('Ctrl Pts',(2.92665188325398,-6.10139309946884,-7.66055676222079));
#45815=CARTESIAN_POINT('Ctrl Pts',(3.09989502177124,-6.01829365818771,-7.65149757375595));
#45816=CARTESIAN_POINT('Ctrl Pts',(3.26948931062098,-5.92786241753779,-7.64243838529112));
#45817=CARTESIAN_POINT('Ctrl Pts',(3.43482749781613,-5.83045873497499,-7.63337919682628));
#45818=CARTESIAN_POINT('Ctrl Pts',(3.59987924820414,-5.73322379745719,-7.62433570276974));
#45819=CARTESIAN_POINT('Ctrl Pts',(3.76084211478365,-5.62895170816136,-7.61529220871318));
#45820=CARTESIAN_POINT('Ctrl Pts',(3.91714428998133,-5.5179950717146,-7.60624871465665));
#45821=CARTESIAN_POINT('Ctrl Pts',(4.07330349615089,-5.40713992689748,-7.59721349265107));
#45822=CARTESIAN_POINT('Ctrl Pts',(4.22481032829184,-5.2896125799144,-7.5881782706455));
#45823=CARTESIAN_POINT('Ctrl Pts',(4.37112219132356,-5.16580872550647,-7.57914304863991));
#45824=CARTESIAN_POINT('Ctrl Pts',(4.51717628470422,-5.04222298653832,-7.57012374472856));
#45825=CARTESIAN_POINT('Ctrl Pts',(4.65805350367384,-4.91238297486737,-7.5611044408172));
#45826=CARTESIAN_POINT('Ctrl Pts',(4.79324465710423,-4.77672426011192,-7.55208513690585));
#45827=CARTESIAN_POINT('Ctrl Pts',(4.92826620378978,-4.64123573868965,-7.54307714834124));
#45828=CARTESIAN_POINT('Ctrl Pts',(5.05761575351991,-4.49994325055495,-7.53406915977664));
#45829=CARTESIAN_POINT('Ctrl Pts',(5.18081939652793,-4.35332050055587,-7.52506117121203));
#45830=CARTESIAN_POINT('Ctrl Pts',(5.30374477979261,-4.2070289031736,-7.51607352750513));
#45831=CARTESIAN_POINT('Ctrl Pts',(5.42055181069141,-4.0554312559849,-7.5070858837982));
#45832=CARTESIAN_POINT('Ctrl Pts',(5.53080574651703,-3.89903536715098,-7.49809824009129));
#45833=CARTESIAN_POINT('Ctrl Pts',(5.62682928288425,-3.76282538782762,-7.49027062535915));
#45834=CARTESIAN_POINT('Ctrl Pts',(5.71788263937237,-3.62297647889661,-7.48244301062701));
#45835=CARTESIAN_POINT('Ctrl Pts',(5.80370247531395,-3.47984576928845,-7.47461539589487));
#45836=CARTESIAN_POINT('Ctrl Pts',(5.89276257202811,-3.33131093814352,-7.46649223744977));
#45837=CARTESIAN_POINT('Ctrl Pts',(5.97614524251994,-3.17930734502623,-7.45836907900467));
#45838=CARTESIAN_POINT('Ctrl Pts',(6.05357768438367,-3.02431582661798,-7.45024592055957));
#45839=CARTESIAN_POINT('Ctrl Pts',(6.13100466685498,-2.869335235923,-7.44212333483966));
#45840=CARTESIAN_POINT('Ctrl Pts',(6.20248209276141,-2.71136746699568,-7.43400074911974));
#45841=CARTESIAN_POINT('Ctrl Pts',(6.26778362790867,-2.5509169711537,-7.42587816339983));
#45842=CARTESIAN_POINT('Ctrl Pts',(6.33309300970753,-2.39044719553316,-7.41775460166764));
#45843=CARTESIAN_POINT('Ctrl Pts',(6.39222488619314,-2.22749443842895,-7.40963103993543));
#45844=CARTESIAN_POINT('Ctrl Pts',(6.44500149845093,-2.06258204320829,-7.40150747820324));
#45845=CARTESIAN_POINT('Ctrl Pts',(6.49781655220792,-1.89754952887733,-7.39337799942033));
#45846=CARTESIAN_POINT('Ctrl Pts',(6.54426698461811,-1.73055487457134,-7.38524852063744));
#45847=CARTESIAN_POINT('Ctrl Pts',(6.58422507744907,-1.56213607905675,-7.37711904185452));
#45848=CARTESIAN_POINT('Ctrl Pts',(6.62419946049119,-1.39364862216351,-7.36898624882619));
#45849=CARTESIAN_POINT('Ctrl Pts',(6.65767615736533,-1.2237362256238,-7.36085345579785));
#45850=CARTESIAN_POINT('Ctrl Pts',(6.68457884990569,-1.05294567732319,-7.35272066276952));
#45851=CARTESIAN_POINT('Ctrl Pts',(6.71151079504283,-0.881969420211572,
-7.34457902656258));
#45852=CARTESIAN_POINT('Ctrl Pts',(6.73185441557633,-0.710113467223356,
-7.33643739035563));
#45853=CARTESIAN_POINT('Ctrl Pts',(6.74558532148725,-0.537929057158783,
-7.32829575414868));
#45854=CARTESIAN_POINT('Ctrl Pts',(6.75258103154576,-0.450203438964313,
-7.32414770108685));
#45855=CARTESIAN_POINT('Ctrl Pts',(6.75786107417153,-0.362392569416437,
-7.31999964802502));
#45856=CARTESIAN_POINT('Ctrl Pts',(6.76142742199599,-0.274569148085876,
-7.31585159496318));
#45857=CARTESIAN_POINT('Ctrl Pts',(6.76868444717152,-0.095860617407945,
-7.30741087998507));
#45858=CARTESIAN_POINT('Ctrl Pts',(6.76885744666228,0.0832678398555202,
-7.29897016500697));
#45859=CARTESIAN_POINT('Ctrl Pts',(6.7619172104908,0.262230125020561,-7.29052945002885));
#45860=CARTESIAN_POINT('Ctrl Pts',(6.75498222007681,0.441057142058771,-7.28209511494079));
#45861=CARTESIAN_POINT('Ctrl Pts',(6.74094472464119,0.619717905404618,-7.2736607798527));
#45862=CARTESIAN_POINT('Ctrl Pts',(6.71982756392381,0.797625545685325,-7.26522644476464));
#45863=CARTESIAN_POINT('Ctrl Pts',(6.69872312177031,0.975426034738707,-7.25679718955598));
#45864=CARTESIAN_POINT('Ctrl Pts',(6.67054755442464,1.15247397477357,-7.24836793434734));
#45865=CARTESIAN_POINT('Ctrl Pts',(6.63537563012189,1.32818645045964,-7.23993867913868));
#45866=CARTESIAN_POINT('Ctrl Pts',(6.60021949425791,1.50382005000461,-7.23151320776563));
#45867=CARTESIAN_POINT('Ctrl Pts',(6.55807332882956,1.6781190541158,-7.22308773639258));
#45868=CARTESIAN_POINT('Ctrl Pts',(6.50906327505818,1.85050919513761,-7.21466226501953));
#45869=CARTESIAN_POINT('Ctrl Pts',(6.46006771008052,2.02284837263255,-7.20623928446025));
#45870=CARTESIAN_POINT('Ctrl Pts',(6.40421239445543,2.19327949204761,-7.19781630390098));
#45871=CARTESIAN_POINT('Ctrl Pts',(6.3416738574515,2.36124155598623,-7.1893933233417));
#45872=CARTESIAN_POINT('Ctrl Pts',(6.27913428493913,2.52920640102819,-7.18097020331533));
#45873=CARTESIAN_POINT('Ctrl Pts',(6.20991138006599,2.69470179422524,-7.17254708328897));
#45874=CARTESIAN_POINT('Ctrl Pts',(6.13423076569902,2.85718426307293,-7.1641239632626));
#45875=CARTESIAN_POINT('Ctrl Pts',(6.05854753417025,3.01967235083525,-7.15570055195071));
#45876=CARTESIAN_POINT('Ctrl Pts',(5.97640628854111,3.17914700411167,-7.1472771406388));
#45877=CARTESIAN_POINT('Ctrl Pts',(5.88807986886808,3.33508687410546,-7.1388537293269));
#45878=CARTESIAN_POINT('Ctrl Pts',(5.79973807630137,3.49105388486925,-7.13042885195075));
#45879=CARTESIAN_POINT('Ctrl Pts',(5.70520912781137,3.64348459561988,-7.1220039745746));
#45880=CARTESIAN_POINT('Ctrl Pts',(5.60481086472979,3.7918839869657,-7.11357909719845));
#45881=CARTESIAN_POINT('Ctrl Pts',(5.50438112135551,3.9403299095575,-7.10515157816698));
#45882=CARTESIAN_POINT('Ctrl Pts',(5.3980785810301,4.08474171648936,-7.09672405913553));
#45883=CARTESIAN_POINT('Ctrl Pts',(5.28626348908012,4.22465469879119,-7.08829654010406));
#45884=CARTESIAN_POINT('Ctrl Pts',(5.17434812567725,4.36469314964802,-7.07986146359924));
#45885=CARTESIAN_POINT('Ctrl Pts',(5.05691054133703,4.50022445385707,-7.07142638709441));
#45886=CARTESIAN_POINT('Ctrl Pts',(4.93435096967174,4.6308173693312,-7.0629913105896));
#45887=CARTESIAN_POINT('Ctrl Pts',(4.81173216415882,4.7614734012209,-7.05455215735678));
#45888=CARTESIAN_POINT('Ctrl Pts',(4.68398666818812,4.88718604682869,-7.04611300412398));
#45889=CARTESIAN_POINT('Ctrl Pts',(4.55155079222759,5.00756172061538,-7.03767385089117));
#45890=CARTESIAN_POINT('Ctrl Pts',(4.4189677428777,5.12807116552548,-7.02922531939302));
#45891=CARTESIAN_POINT('Ctrl Pts',(4.28168415078579,5.2432315696701,-7.02077678789487));
#45892=CARTESIAN_POINT('Ctrl Pts',(4.14016947228494,5.35268958008587,-7.01232825639672));
#45893=CARTESIAN_POINT('Ctrl Pts',(4.06197802096618,5.41316868220828,-7.00766016863119));
#45894=CARTESIAN_POINT('Ctrl Pts',(3.98249538951366,5.47190764087666,-7.00299208086567));
#45895=CARTESIAN_POINT('Ctrl Pts',(3.90180444135521,5.52885260261302,-6.99832399310014));
#45896=CARTESIAN_POINT('Ctrl Pts',(3.75936801179357,5.6293723909705,-6.99008384015391));
#45897=CARTESIAN_POINT('Ctrl Pts',(3.61284801776542,5.72452318394757,-6.98184368720769));
#45898=CARTESIAN_POINT('Ctrl Pts',(3.46268485834673,5.81395756535738,-6.97360353426146));
#45899=CARTESIAN_POINT('Ctrl Pts',(3.34369396220178,5.88482632725157,-6.9670739487943));
#45900=CARTESIAN_POINT('Ctrl Pts',(3.22241623088389,5.95210634827264,-6.96054436332713));
#45901=CARTESIAN_POINT('Ctrl Pts',(3.09908550384728,6.01564277861009,-6.95401477785997));
#45902=CARTESIAN_POINT('Ctrl Pts',(3.09908550384723,6.01564277861011,-8.95438620791577));
#45903=CARTESIAN_POINT('Ctrl Pts',(2.93072002576928,6.10237981264993,-8.94545369149881));
#45904=CARTESIAN_POINT('Ctrl Pts',(2.75883745800324,6.18197965111236,-8.93652117508186));
#45905=CARTESIAN_POINT('Ctrl Pts',(2.58404611684415,6.2541981633158,-8.92758865866489));
#45906=CARTESIAN_POINT('Ctrl Pts',(2.42685614408101,6.31914432077974,-8.91955564053608));
#45907=CARTESIAN_POINT('Ctrl Pts',(2.26731409375055,6.37812149969473,-8.9115226224073));
#45908=CARTESIAN_POINT('Ctrl Pts',(2.10587265006943,6.43098665693606,-8.9034896042785));
#45909=CARTESIAN_POINT('Ctrl Pts',(1.94059351320184,6.48510849430313,-8.89526562986093));
#45910=CARTESIAN_POINT('Ctrl Pts',(1.77300748142415,6.53292637318214,-8.88704165544333));
#45911=CARTESIAN_POINT('Ctrl Pts',(1.60363612383975,6.57424065442666,-8.87881768102576));
#45912=CARTESIAN_POINT('Ctrl Pts',(1.43444363884181,6.61551130378176,-8.87060239192308));
#45913=CARTESIAN_POINT('Ctrl Pts',(1.26346992815423,6.65029194857872,-8.86238710282042));
#45914=CARTESIAN_POINT('Ctrl Pts',(1.09125379238239,6.67843201362498,-8.85417181371775));
#45915=CARTESIAN_POINT('Ctrl Pts',(0.919184990673696,6.70654800432942,-8.8459635529456));
#45916=CARTESIAN_POINT('Ctrl Pts',(0.745876232693255,6.72803467234293,-8.83775529217344));
#45917=CARTESIAN_POINT('Ctrl Pts',(0.571878736844368,6.74279198183848,-8.82954703140128));
#45918=CARTESIAN_POINT('Ctrl Pts',(0.397995208792228,6.75753962534407,-8.82134414701337));
#45919=CARTESIAN_POINT('Ctrl Pts',(0.223424197492965,6.76556665982803,-8.81314126262547));
#45920=CARTESIAN_POINT('Ctrl Pts',(0.048724402896398,6.76682458266523,-8.80493837823756));
#45921=CARTESIAN_POINT('Ctrl Pts',(-0.125895987817598,6.76808193375615,
-8.79673922219329));
#45922=CARTESIAN_POINT('Ctrl Pts',(-0.300644687367139,6.7625763001542,-8.78854006614903));
#45923=CARTESIAN_POINT('Ctrl Pts',(-0.474960524675801,6.75031121504777,
-8.78034091010476));
#45924=CARTESIAN_POINT('Ctrl Pts',(-0.649261200744174,6.73804719670559,
-8.77214246718775));
#45925=CARTESIAN_POINT('Ctrl Pts',(-0.823128731524467,6.71902491452393,
-8.76394402427075));
#45926=CARTESIAN_POINT('Ctrl Pts',(-0.996004230675472,6.6932999762805,-8.75574558135374));
#45927=CARTESIAN_POINT('Ctrl Pts',(-1.16887800819147,6.66757529422696,-8.74754722008351));
#45928=CARTESIAN_POINT('Ctrl Pts',(-1.34075941880886,6.63514814081499,-8.73934885881327));
#45929=CARTESIAN_POINT('Ctrl Pts',(-1.51109708595469,6.59612572627442,-8.73115049754303));
#45930=CARTESIAN_POINT('Ctrl Pts',(-1.68146399979623,6.55709661164982,-8.72295072862773));
#45931=CARTESIAN_POINT('Ctrl Pts',(-1.8502862924431,6.51147005993338,-8.71475095971243));
#45932=CARTESIAN_POINT('Ctrl Pts',(-2.01702507398081,6.45940390832875,-8.70655119079712));
#45933=CARTESIAN_POINT('Ctrl Pts',(-2.18382277389909,6.40731935876471,-8.69834852443288));
#45934=CARTESIAN_POINT('Ctrl Pts',(-2.34853515395549,6.34879078336805,-8.69014585806862));
#45935=CARTESIAN_POINT('Ctrl Pts',(-2.5106406653547,6.28402517893327,-8.68194319170438));
#45936=CARTESIAN_POINT('Ctrl Pts',(-2.6729302880974,6.21918601695969,-8.67373120916136));
#45937=CARTESIAN_POINT('Ctrl Pts',(-2.83260679374606,6.14809580730292,-8.66551922661835));
#45938=CARTESIAN_POINT('Ctrl Pts',(-2.98916976489375,6.07100923378025,-8.65730724407533));
#45939=CARTESIAN_POINT('Ctrl Pts',(-3.14582507899738,5.99387719355488,-8.64909041799404));
#45940=CARTESIAN_POINT('Ctrl Pts',(-3.29936288309264,5.910741909992,-8.64087359191275));
#45941=CARTESIAN_POINT('Ctrl Pts',(-3.44930949280502,5.82190286958183,-8.63265676583146));
#45942=CARTESIAN_POINT('Ctrl Pts',(-3.59948734184626,5.73292682654039,-8.62442726821761));
#45943=CARTESIAN_POINT('Ctrl Pts',(-3.74606262823561,5.63822964354398,-8.61619777060375));
#45944=CARTESIAN_POINT('Ctrl Pts',(-3.88859157399989,5.5381535344027,-8.6079682729899));
#45945=CARTESIAN_POINT('Ctrl Pts',(-4.01563580328179,5.44894995482657,-8.60063284946506));
#45946=CARTESIAN_POINT('Ctrl Pts',(-4.13946546436669,5.3554734108814,-8.59329742594022));
#45947=CARTESIAN_POINT('Ctrl Pts',(-4.25979033663362,5.25799156407871,-8.58596200241539));
#45948=CARTESIAN_POINT('Ctrl Pts',(-4.39058181114603,5.15203014279224,-8.57798849834336));
#45949=CARTESIAN_POINT('Ctrl Pts',(-4.51767880598209,5.04097313569127,-8.57001499427135));
#45950=CARTESIAN_POINT('Ctrl Pts',(-4.64064040705468,4.92511376644351,-8.56204149019932));
#45951=CARTESIAN_POINT('Ctrl Pts',(-4.76344931244249,4.80939827321535,-8.5540778877523));
#45952=CARTESIAN_POINT('Ctrl Pts',(-4.88213276429453,4.6888925373059,-8.54611428530528));
#45953=CARTESIAN_POINT('Ctrl Pts',(-4.99627964831274,4.56393236977236,-8.53815068285827));
#45954=CARTESIAN_POINT('Ctrl Pts',(-5.11031082616481,4.43909886940131,-8.53019515279899));
#45955=CARTESIAN_POINT('Ctrl Pts',(-5.21981432897755,4.30982019869699,-8.52223962273972));
#45956=CARTESIAN_POINT('Ctrl Pts',(-5.32441308937246,4.17647150759097,-8.51428409268045));
#45957=CARTESIAN_POINT('Ctrl Pts',(-5.42892960616438,4.04322766549818,-8.50633481787175));
#45958=CARTESIAN_POINT('Ctrl Pts',(-5.5285488193977,3.90592046881269,-8.49838554306304));
#45959=CARTESIAN_POINT('Ctrl Pts',(-5.62293159514742,3.7649607270585,-8.49043626825434));
#45960=CARTESIAN_POINT('Ctrl Pts',(-5.71726578799842,3.62407354338288,-8.48249108528136));
#45961=CARTESIAN_POINT('Ctrl Pts',(-5.80636869352626,3.47953787092645,-8.47454590230839));
#45962=CARTESIAN_POINT('Ctrl Pts',(-5.88994255353325,3.33179616964757,-8.46660071933541));
#45963=CARTESIAN_POINT('Ctrl Pts',(-5.97349419453688,3.18409374707804,-8.45865764867419));
#45964=CARTESIAN_POINT('Ctrl Pts',(-6.05151952528861,3.0331873225431,-8.45071457801297));
#45965=CARTESIAN_POINT('Ctrl Pts',(-6.12376519705261,2.87954663295581,-8.44277150735175));
#45966=CARTESIAN_POINT('Ctrl Pts',(-6.19600647268141,2.72591529237488,-8.43482892002485));
#45967=CARTESIAN_POINT('Ctrl Pts',(-6.26246862651552,2.56955036320333,-8.42688633269795));
#45968=CARTESIAN_POINT('Ctrl Pts',(-6.32294531131199,2.41094412837747,-8.41894374537105));
#45969=CARTESIAN_POINT('Ctrl Pts',(-6.38343071629526,2.25231502397794,-8.41100001279543));
#45970=CARTESIAN_POINT('Ctrl Pts',(-6.43792880016635,2.09144432801209,-8.4030562802198));
#45971=CARTESIAN_POINT('Ctrl Pts',(-6.48628229156297,1.92884188936176,-8.39511254764418));
#45972=CARTESIAN_POINT('Ctrl Pts',(-6.53467837228234,1.76609623193776,-8.38716181829996));
#45973=CARTESIAN_POINT('Ctrl Pts',(-6.57691894305228,1.60161615197891,-8.37921108895577));
#45974=CARTESIAN_POINT('Ctrl Pts',(-6.61289718464963,1.4359247282685,-8.37126035961155));
#45975=CARTESIAN_POINT('Ctrl Pts',(-6.64889153959868,1.27015909736887,-8.36330606942354));
#45976=CARTESIAN_POINT('Ctrl Pts',(-6.67861791486571,1.10318141787854,-8.35535177923551));
#45977=CARTESIAN_POINT('Ctrl Pts',(-6.70202119829351,0.935521703449177,
-8.3473974890475));
#45978=CARTESIAN_POINT('Ctrl Pts',(-6.72545661367217,0.767631797657053,
-8.33943227787645));
#45979=CARTESIAN_POINT('Ctrl Pts',(-6.742551560049,0.599058365788259,-8.33146706670544));
#45980=CARTESIAN_POINT('Ctrl Pts',(-6.75330301016183,0.430334117795963,
-8.32350185553439));
#45981=CARTESIAN_POINT('Ctrl Pts',(-6.76260837606804,0.284303503474789,
-8.31660797576105));
#45982=CARTESIAN_POINT('Ctrl Pts',(-6.76716275029939,0.138160066701469,
-8.30971409598767));
#45983=CARTESIAN_POINT('Ctrl Pts',(-6.76699555771448,-0.0077538295429859,
-8.30282021621433));
#45984=CARTESIAN_POINT('',(-6.76715677348915,-0.000698709272743195,-8.69690852530228));
#45985=CARTESIAN_POINT('Ctrl Pts',(3.09908550384716,6.01564277861015,-9.34860320957391));
#45986=CARTESIAN_POINT('Ctrl Pts',(2.93373232018315,6.10082796552487,-9.33985376167461));
#45987=CARTESIAN_POINT('Ctrl Pts',(2.76486502144403,6.17919158180201,-9.33110431377533));
#45988=CARTESIAN_POINT('Ctrl Pts',(2.59305716434318,6.25046746591393,-9.32235486587604));
#45989=CARTESIAN_POINT('Ctrl Pts',(2.4212506945925,6.32174277447237,-9.31360548862862));
#45990=CARTESIAN_POINT('Ctrl Pts',(2.24650397871026,6.38593035557837,-9.30485611138119));
#45991=CARTESIAN_POINT('Ctrl Pts',(2.0694105332374,6.44281220003549,-9.29610673413378));
#45992=CARTESIAN_POINT('Ctrl Pts',(1.89231845896649,6.49969360406696,-9.28735742463118));
#45993=CARTESIAN_POINT('Ctrl Pts',(1.71287996431467,6.54926929700891,-9.27860811512858));
#45994=CARTESIAN_POINT('Ctrl Pts',(1.53170449173462,6.59137090065489,-9.26985880562599));
#45995=CARTESIAN_POINT('Ctrl Pts',(1.35053036178131,6.63347219230091,-9.2611095609614));
#45996=CARTESIAN_POINT('Ctrl Pts',(1.16761955878807,6.66809944062461,-9.2523603162968));
#45997=CARTESIAN_POINT('Ctrl Pts',(0.983593309310145,6.69513503985396,-9.24361107163221));
#45998=CARTESIAN_POINT('Ctrl Pts',(0.79956836245968,6.72217044771218,-9.23486188889904));
#45999=CARTESIAN_POINT('Ctrl Pts',(0.614428268438334,6.74161427235979,-9.22611270616587));
#46000=CARTESIAN_POINT('Ctrl Pts',(0.428801816330049,6.75340047696803,-9.2173635234327));
#46001=CARTESIAN_POINT('Ctrl Pts',(0.24317661652258,6.76518660206243,-9.20861439972456));
#46002=CARTESIAN_POINT('Ctrl Pts',(0.0570653511652714,6.76931519233997,
-9.19986527601643));
#46003=CARTESIAN_POINT('Ctrl Pts',(-0.128899900800203,6.76577222610795,
-9.1911161523083));
#46004=CARTESIAN_POINT('Ctrl Pts',(-0.314863959942112,6.76222928260132,
-9.18236708471904));
#46005=CARTESIAN_POINT('Ctrl Pts',(-0.50068172108069,6.75101488651276,-9.17361801712978));
#46006=CARTESIAN_POINT('Ctrl Pts',(-0.685722110173226,6.73216712415992,
-9.16486894954052));
#46007=CARTESIAN_POINT('Ctrl Pts',(-0.8707613738276,6.71331947644145,-9.15611993516416));
#46008=CARTESIAN_POINT('Ctrl Pts',(-1.05502298984348,6.68683858439996,-9.14737092078779));
#46009=CARTESIAN_POINT('Ctrl Pts',(-1.2378811767607,6.65281438131424,-9.13862190641143));
#46010=CARTESIAN_POINT('Ctrl Pts',(-1.43009641451804,6.61704912302375,-9.1294251955239));
#46011=CARTESIAN_POINT('Ctrl Pts',(-1.62076048992708,6.57294837083162,-9.12022848463638));
#46012=CARTESIAN_POINT('Ctrl Pts',(-1.80915798961144,6.52067760042046,-9.11103177374885));
#46013=CARTESIAN_POINT('Ctrl Pts',(-1.98840443003024,6.47094578577405,-9.10228177604234));
#46014=CARTESIAN_POINT('Ctrl Pts',(-2.16559895952203,6.41381888474472,-9.09353177833584));
#46015=CARTESIAN_POINT('Ctrl Pts',(-2.34013966242333,6.3494909528523,-9.08478178062933));
#46016=CARTESIAN_POINT('Ctrl Pts',(-2.51467682554023,6.28516432556682,-9.07603196037774));
#46017=CARTESIAN_POINT('Ctrl Pts',(-2.68656000078848,6.21363705879658,-9.06728214012614));
#46018=CARTESIAN_POINT('Ctrl Pts',(-2.85520533840891,6.13515211510858,-9.05853231987454));
#46019=CARTESIAN_POINT('Ctrl Pts',(-3.02384747998335,6.05666865881118,-9.0497826654433));
#46020=CARTESIAN_POINT('Ctrl Pts',(-3.18925164684549,5.97122791039838,-9.04103301101204));
#46021=CARTESIAN_POINT('Ctrl Pts',(-3.35085601829174,5.87912008251899,-9.03228335658079));
#46022=CARTESIAN_POINT('Ctrl Pts',(-3.51245754191436,5.78701387778163,-9.02353385633765));
#46023=CARTESIAN_POINT('Ctrl Pts',(-3.67025915510956,5.6882409706097,-9.01478435609451));
#46024=CARTESIAN_POINT('Ctrl Pts',(-3.82372487928856,5.5831368465684,-9.00603485585137));
#46025=CARTESIAN_POINT('Ctrl Pts',(-3.97718810300831,5.47803443501749,-8.99728549816624));
#46026=CARTESIAN_POINT('Ctrl Pts',(-4.1263153426307,5.36660117496342,-8.98853614048113));
#46027=CARTESIAN_POINT('Ctrl Pts',(-4.2706000988628,5.24921554097306,-8.979786782796));
#46028=CARTESIAN_POINT('Ctrl Pts',(-4.41488269594284,5.13183166360231,-8.97103755604081));
#46029=CARTESIAN_POINT('Ctrl Pts',(-4.55432273235174,5.00849577139394,-8.96228832928563));
#46030=CARTESIAN_POINT('Ctrl Pts',(-4.68844662480306,4.87962675277247,-8.95353910253043));
#46031=CARTESIAN_POINT('Ctrl Pts',(-4.82256868835247,4.75075949139791,-8.94478999507895));
#46032=CARTESIAN_POINT('Ctrl Pts',(-4.95137454637943,4.61635945312439,-8.93604088762745));
#46033=CARTESIAN_POINT('Ctrl Pts',(-5.0744267446115,4.47688309134509,-8.92729178017596));
#46034=CARTESIAN_POINT('Ctrl Pts',(-5.19747742838613,4.33740844616262,-8.91854278040359));
#46035=CARTESIAN_POINT('Ctrl Pts',(-5.31477440451004,4.19285781735932,-8.90979378063122));
#46036=CARTESIAN_POINT('Ctrl Pts',(-5.42591931531231,4.04372211999301,-8.90104478085884));
#46037=CARTESIAN_POINT('Ctrl Pts',(-5.53707636463062,3.89457013500687,-8.89229482557826));
#46038=CARTESIAN_POINT('Ctrl Pts',(-5.64207983273552,3.74083230916297,-8.88354487029768));
#46039=CARTESIAN_POINT('Ctrl Pts',(-5.7405730346883,3.58303087251695,-8.8747949150171));
#46040=CARTESIAN_POINT('Ctrl Pts',(-5.83906243363843,3.42523552887297,-8.86604529758829));
#46041=CARTESIAN_POINT('Ctrl Pts',(-5.931041917685,3.26337713156858,-8.85729568015948));
#46042=CARTESIAN_POINT('Ctrl Pts',(-6.01619906699726,3.0980054529102,-8.84854606273067));
#46043=CARTESIAN_POINT('Ctrl Pts',(-6.1013533809545,2.93263928039456,-8.83979673662528));
#46044=CARTESIAN_POINT('Ctrl Pts',(-6.17968568352903,2.76376031540081,-8.83104741051989));
#46045=CARTESIAN_POINT('Ctrl Pts',(-6.25092992694947,2.59194213831396,-8.8222980844145));
#46046=CARTESIAN_POINT('Ctrl Pts',(-6.32217217691157,2.42012876880679,-8.81354900312071));
#46047=CARTESIAN_POINT('Ctrl Pts',(-6.38632665483898,2.24537661647535,-8.80479992182692));
#46048=CARTESIAN_POINT('Ctrl Pts',(-6.44317547869392,2.06827917621327,-8.79605084053313));
#46049=CARTESIAN_POINT('Ctrl Pts',(-6.50002944235971,1.89116572423301,-8.78730096821817));
#46050=CARTESIAN_POINT('Ctrl Pts',(-6.54957634250428,1.71170683289083,-8.77855109590321));
#46051=CARTESIAN_POINT('Ctrl Pts',(-6.5916478770842,1.53051209225258,-8.76980122358825));
#46052=CARTESIAN_POINT('Ctrl Pts',(-6.63371649075031,1.3493299314792,-8.76105195875345));
#46053=CARTESIAN_POINT('Ctrl Pts',(-6.66831071257144,1.1664124417389,-8.75230269391866));
#46054=CARTESIAN_POINT('Ctrl Pts',(-6.6953130484035,0.982380875158835,-8.74355342908387));
#46055=CARTESIAN_POINT('Ctrl Pts',(-6.72231677033057,0.798339861794692,
-8.73480371512821));
#46056=CARTESIAN_POINT('Ctrl Pts',(-6.741727784779,0.613184940729031,-8.72605400117256));
#46057=CARTESIAN_POINT('Ctrl Pts',(-6.75348015835525,0.42754502768946,-8.7173042872169));
#46058=CARTESIAN_POINT('Ctrl Pts',(-6.76249038365221,0.285219953546511,
-8.71059611941464));
#46059=CARTESIAN_POINT('Ctrl Pts',(-6.76699999999998,0.142609995757779,
-8.70388795161236));
#46060=CARTESIAN_POINT('Ctrl Pts',(-6.767,1.17640916536316E-12,-8.69717978381009));
#46061=CARTESIAN_POINT('Ctrl Pts',(-6.76699937553265,-0.00290715337751525,
-8.69717978381009));
#46062=CARTESIAN_POINT('Ctrl Pts',(-6.76691524467507,-0.198739084742533,
-8.68799239733351));
#46063=CARTESIAN_POINT('Ctrl Pts',(-6.75832612228008,-0.394331070678668,
-8.67880501085691));
#46064=CARTESIAN_POINT('Ctrl Pts',(-6.74131915260648,-0.588986487706674,
-8.66961762438032));
#46065=CARTESIAN_POINT('Ctrl Pts',(-6.72423368363483,-0.784540378354171,
-8.66038783156073));
#46066=CARTESIAN_POINT('Ctrl Pts',(-6.69865254006024,-0.979148843300637,
-8.65115803874112));
#46067=CARTESIAN_POINT('Ctrl Pts',(-6.66471496962178,-1.17211918067205,
-8.64192824592153));
#46068=CARTESIAN_POINT('Ctrl Pts',(-6.63070812902098,-1.36548339086417,
-8.63267961412088));
#46069=CARTESIAN_POINT('Ctrl Pts',(-6.58831079808566,-1.55720259933329,
-8.62343098232023));
#46070=CARTESIAN_POINT('Ctrl Pts',(-6.53771293764988,-1.74659627415308,
-8.61418235051957));
#46071=CARTESIAN_POINT('Ctrl Pts',(-6.48698320754632,-1.93648355247235,
-8.60490961465616));
#46072=CARTESIAN_POINT('Ctrl Pts',(-6.42801022788074,-2.12403298150376,
-8.59563687879274));
#46073=CARTESIAN_POINT('Ctrl Pts',(-6.361034284994,-2.30857787937312,-8.58636414292933));
#46074=CARTESIAN_POINT('Ctrl Pts',(-6.29883161931191,-2.47997053307438,
-8.57775226134902));
#46075=CARTESIAN_POINT('Ctrl Pts',(-6.22972660763097,-2.64877173829918,
-8.5691403797687));
#46076=CARTESIAN_POINT('Ctrl Pts',(-6.15394835814301,-2.81446417730071,
-8.56052849818839));
#46077=CARTESIAN_POINT('Ctrl Pts',(-6.0814355694657,-2.97301654418608,-8.55228772259161));
#46078=CARTESIAN_POINT('Ctrl Pts',(-6.00269125937446,-3.12898366169191,
-8.54404694699483));
#46079=CARTESIAN_POINT('Ctrl Pts',(-5.91792123483746,-3.28184357614129,
-8.53580617139805));
#46080=CARTESIAN_POINT('Ctrl Pts',(-5.83324510229286,-3.43453418166333,
-8.52757452335366));
#46081=CARTESIAN_POINT('Ctrl Pts',(-5.74255671575046,-3.58412412850215,
-8.51934287530926));
#46082=CARTESIAN_POINT('Ctrl Pts',(-5.64610975256684,-3.73011174926028,
-8.51111122726487));
#46083=CARTESIAN_POINT('Ctrl Pts',(-5.5497524271015,-3.87596368925887,-8.50288722970655));
#46084=CARTESIAN_POINT('Ctrl Pts',(-5.44764737866993,-4.01821967571203,
-8.49466323214823));
#46085=CARTESIAN_POINT('Ctrl Pts',(-5.34009401449279,-4.15640288186531,
-8.48643923458991));
#46086=CARTESIAN_POINT('Ctrl Pts',(-5.23263567413076,-4.2944640026191,-8.47822250296538));
#46087=CARTESIAN_POINT('Ctrl Pts',(-5.11973882974768,-4.42845923520702,
-8.47000577134084));
#46088=CARTESIAN_POINT('Ctrl Pts',(-5.00174589745669,-4.55794108971092,
-8.46178903971632));
#46089=CARTESIAN_POINT('Ctrl Pts',(-4.88381341731307,-4.68735660586728,
-8.45357651782759));
#46090=CARTESIAN_POINT('Ctrl Pts',(-4.76079028822517,-4.8122630869417,-8.44536399593886));
#46091=CARTESIAN_POINT('Ctrl Pts',(-4.63305912612318,-4.93224615503391,
-8.43715147405013));
#46092=CARTESIAN_POINT('Ctrl Pts',(-4.50537067793673,-5.05218910021051,
-8.42894169846826));
#46093=CARTESIAN_POINT('Ctrl Pts',(-4.37297759214175,-5.16721166893132,
-8.42073192288636));
#46094=CARTESIAN_POINT('Ctrl Pts',(-4.23629931833264,-5.27693633517541,
-8.41252214730448));
#46095=CARTESIAN_POINT('Ctrl Pts',(-4.17660179926291,-5.32486121872108,
-8.408936330622));
#46096=CARTESIAN_POINT('Ctrl Pts',(-4.11608724489742,-5.3717759049282,-8.40535051393954));
#46097=CARTESIAN_POINT('Ctrl Pts',(-4.05479264215265,-5.41765130191532,
-8.40176469725706));
#46098=CARTESIAN_POINT('Ctrl Pts',(-3.90336505412913,-5.53098592526393,
-8.39290597973533));
#46099=CARTESIAN_POINT('Ctrl Pts',(-3.74733151455158,-5.63785733818777,
-8.38404726221361));
#46100=CARTESIAN_POINT('Ctrl Pts',(-3.5872551176743,-5.7379342729522,-8.37518854469188));
#46101=CARTESIAN_POINT('Ctrl Pts',(-3.42687924356829,-5.83819843558826,
-8.36631325393246));
#46102=CARTESIAN_POINT('Ctrl Pts',(-3.26244561685854,-5.93164257976171,
-8.35743796317304));
#46103=CARTESIAN_POINT('Ctrl Pts',(-3.09454176563316,-6.01798141080147,
-8.34856267241363));
#46104=CARTESIAN_POINT('Ctrl Pts',(-2.92616102971802,-6.1045654635342,-8.33966217383289));
#46105=CARTESIAN_POINT('Ctrl Pts',(-2.75429057786916,-6.18400369976604,
-8.33076167525215));
#46106=CARTESIAN_POINT('Ctrl Pts',(-2.57954060775898,-6.25605780447419,
-8.32186117667141));
#46107=CARTESIAN_POINT('Ctrl Pts',(-2.40455407838045,-6.3282094489203,-8.31294862947384));
#46108=CARTESIAN_POINT('Ctrl Pts',(-2.22668048646314,-6.39295690163863,
-8.30403608227627));
#46109=CARTESIAN_POINT('Ctrl Pts',(-2.04654637140133,-6.45011139048808,
-8.29512353507869));
#46110=CARTESIAN_POINT('Ctrl Pts',(-1.86601450262073,-6.50739208203088,
-8.28619130810647));
#46111=CARTESIAN_POINT('Ctrl Pts',(-1.68321237516878,-6.55704619616572,
-8.27725908113423));
#46112=CARTESIAN_POINT('Ctrl Pts',(-1.49878072729321,-6.59893516648667,
-8.268326854162));
#46113=CARTESIAN_POINT('Ctrl Pts',(-1.32447152264319,-6.63852508060585,
-8.25988486821644));
#46114=CARTESIAN_POINT('Ctrl Pts',(-1.14870702377738,-6.6711792370778,-8.25144288227087));
#46115=CARTESIAN_POINT('Ctrl Pts',(-0.972033230990177,-6.69682315712837,
-8.24300089632531));
#46116=CARTESIAN_POINT('Ctrl Pts',(-0.799921981160285,-6.72180483132471,
-8.23477692190774));
#46117=CARTESIAN_POINT('Ctrl Pts',(-0.626618872555658,-6.740180362213,-8.22655294749019));
#46118=CARTESIAN_POINT('Ctrl Pts',(-0.452671980481697,-6.75184249505917,
-8.21832897307262));
#46119=CARTESIAN_POINT('Ctrl Pts',(-0.278908793202929,-6.76349231156153,
-8.21011368396996));
#46120=CARTESIAN_POINT('Ctrl Pts',(-0.104503531191567,-6.76844282480463,
-8.20189839486732));
#46121=CARTESIAN_POINT('Ctrl Pts',(0.0699871664054911,-6.7666380719334,
-8.19368310576466));
#46122=CARTESIAN_POINT('Ctrl Pts',(0.244328584011008,-6.76483486306134,
-8.18547484499248));
#46123=CARTESIAN_POINT('Ctrl Pts',(0.41875493508005,-6.7562879017321,-8.1772665842203));
#46124=CARTESIAN_POINT('Ctrl Pts',(0.592706012016421,-6.74099314517673,
-8.16905832344812));
#46125=CARTESIAN_POINT('Ctrl Pts',(0.766543151559387,-6.72570840663748,
-8.16085543906023));
#46126=CARTESIAN_POINT('Ctrl Pts',(0.939905281112293,-6.70368470791542,
-8.15265255467232));
#46127=CARTESIAN_POINT('Ctrl Pts',(1.11223365818358,-6.67497005907918,-8.14444967028443));
#46128=CARTESIAN_POINT('Ctrl Pts',(1.28448370921923,-6.64626846151545,-8.13625051424022));
#46129=CARTESIAN_POINT('Ctrl Pts',(1.45570059086233,-6.61088203140942,-8.12805135819602));
#46130=CARTESIAN_POINT('Ctrl Pts',(1.62533204812493,-6.56891046775171,-8.11985220215181));
#46131=CARTESIAN_POINT('Ctrl Pts',(1.79494875157561,-6.52694255459943,-8.1116537592348));
#46132=CARTESIAN_POINT('Ctrl Pts',(1.96297995542665,-6.47839072650358,-8.10345531631777));
#46133=CARTESIAN_POINT('Ctrl Pts',(2.12888458427527,-6.42340559414047,-8.09525687340076));
#46134=CARTESIAN_POINT('Ctrl Pts',(2.29478756091017,-6.3684210093642,-8.08705851213053));
#46135=CARTESIAN_POINT('Ctrl Pts',(2.45856366390742,-6.3070033597739,-8.0788601508603));
#46136=CARTESIAN_POINT('Ctrl Pts',(2.61968806415335,-6.23935280670459,-8.07066178959007));
#46137=CARTESIAN_POINT('Ctrl Pts',(2.78084012919206,-6.17169063814732,-8.06246202067478));
#46138=CARTESIAN_POINT('Ctrl Pts',(2.93933925366482,-6.09779357286524,-8.05426225175951));
#46139=CARTESIAN_POINT('Ctrl Pts',(3.09468159068023,-6.01790950848423,-8.04606248284423));
#46140=CARTESIAN_POINT('Ctrl Pts',(3.25007881905982,-5.937997216478,-8.03785981647993));
#46141=CARTESIAN_POINT('Ctrl Pts',(3.40231671914451,-5.85209387509924,-8.02965715011561));
#46142=CARTESIAN_POINT('Ctrl Pts',(3.55091695724035,-5.76049284026835,-8.02145448375131));
#46143=CARTESIAN_POINT('Ctrl Pts',(3.69968596806375,-5.66878776955776,-8.01324250120829));
#46144=CARTESIAN_POINT('Ctrl Pts',(3.84480875736337,-5.57137226570385,-8.00503051866528));
#46145=CARTESIAN_POINT('Ctrl Pts',(3.98583598629654,-5.46858304228284,-7.99681853612226));
#46146=CARTESIAN_POINT('Ctrl Pts',(4.12694639499528,-5.3657331923887,-7.98860171004095));
#46147=CARTESIAN_POINT('Ctrl Pts',(4.26395614714185,-5.25750352697139,-7.98038488395965));
#46148=CARTESIAN_POINT('Ctrl Pts',(4.39644992288586,-5.14427031517172,-7.97216805787834));
#46149=CARTESIAN_POINT('Ctrl Pts',(4.52914802316771,-5.03086248140555,-7.96393856026449));
#46150=CARTESIAN_POINT('Ctrl Pts',(4.65731596662949,-4.91243592477088,-7.95570906265064));
#46151=CARTESIAN_POINT('Ctrl Pts',(4.78057522294897,-4.78940388124936,-7.94747956503679));
#46152=CARTESIAN_POINT('Ctrl Pts',(4.89044327211488,-4.6797383598903,-7.94014414151203));
#46153=CARTESIAN_POINT('Ctrl Pts',(4.99641171666389,-4.56641432011216,-7.93280871798728));
#46154=CARTESIAN_POINT('Ctrl Pts',(5.09824052691913,-4.44974522076032,-7.92547329446253));
#46155=CARTESIAN_POINT('Ctrl Pts',(5.21027865342028,-4.32137892364666,-7.91740242427613));
#46156=CARTESIAN_POINT('Ctrl Pts',(5.31767002221868,-4.18854398075456,-7.90933155408973));
#46157=CARTESIAN_POINT('Ctrl Pts',(5.42002710494732,-4.05161636654266,-7.90126068390332));
#46158=CARTESIAN_POINT('Ctrl Pts',(5.52225681224249,-3.91485914810358,-7.89319985728754));
#46159=CARTESIAN_POINT('Ctrl Pts',(5.61946447830822,-3.77401968717285,-7.88513903067177));
#46160=CARTESIAN_POINT('Ctrl Pts',(5.71129960605998,-3.62951040910742,-7.87707820405598));
#46161=CARTESIAN_POINT('Ctrl Pts',(5.80304059017546,-3.48514927292676,-7.86902564089611));
#46162=CARTESIAN_POINT('Ctrl Pts',(5.88941979791398,-3.33712611843255,-7.86097307773622));
#46163=CARTESIAN_POINT('Ctrl Pts',(5.97012727855626,-3.18588594865517,-7.85292051457634));
#46164=CARTESIAN_POINT('Ctrl Pts',(6.05076969487639,-3.03476770486344,-7.84487444318847));
#46165=CARTESIAN_POINT('Ctrl Pts',(6.12574931006339,-2.88043793512903,-7.8368283718006));
#46166=CARTESIAN_POINT('Ctrl Pts',(6.19479982072789,-2.72337000444481,-7.82878230041273));
#46167=CARTESIAN_POINT('Ctrl Pts',(6.26380976863658,-2.56639434111758,-7.82074095557686));
#46168=CARTESIAN_POINT('Ctrl Pts',(6.32689739591313,-2.40668405950758,-7.81269961074098));
#46169=CARTESIAN_POINT('Ctrl Pts',(6.3838426996995,-2.24473637327269,-7.8046582659051));
#46170=CARTESIAN_POINT('Ctrl Pts',(6.44188573372201,-2.07966683396069,-7.79646190868403));
#46171=CARTESIAN_POINT('Ctrl Pts',(6.49354703322238,-1.91227309976545,-7.78826555146296));
#46172=CARTESIAN_POINT('Ctrl Pts',(6.53864527488889,-1.74310268463255,-7.78006919424189));
#46173=CARTESIAN_POINT('Ctrl Pts',(6.58287653837624,-1.57718443750134,-7.7720304055334));
#46174=CARTESIAN_POINT('Ctrl Pts',(6.62079471588866,-1.40955757975313,-7.76399161682492));
#46175=CARTESIAN_POINT('Ctrl Pts',(6.65227936732864,-1.24075308543387,-7.75595282811643));
#46176=CARTESIAN_POINT('Ctrl Pts',(6.6837673879116,-1.07193052750424,-7.74791317918471));
#46177=CARTESIAN_POINT('Ctrl Pts',(6.70882044304195,-0.901930449229639,
-7.73987353025298));
#46178=CARTESIAN_POINT('Ctrl Pts',(6.72736945885729,-0.731292803215058,
-7.73183388132126));
#46179=CARTESIAN_POINT('Ctrl Pts',(6.74592413236132,-0.560603110521183,
-7.7237917801931));
#46180=CARTESIAN_POINT('Ctrl Pts',(6.75797077743414,-0.3892758340752,-7.71574967906493));
#46181=CARTESIAN_POINT('Ctrl Pts',(6.76349231859536,-0.217854667844397,
-7.70770757793677));
#46182=CARTESIAN_POINT('Ctrl Pts',(6.76920019007729,-0.0406487107467705,
-7.69939408749199));
#46183=CARTESIAN_POINT('Ctrl Pts',(6.76793484465814,0.13665714714267,-7.69108059704721));
#46184=CARTESIAN_POINT('Ctrl Pts',(6.75973584536604,0.313464991463971,-7.68276710660243));
#46185=CARTESIAN_POINT('Ctrl Pts',(6.75179052595205,0.484802339838399,-7.67471083843168));
#46186=CARTESIAN_POINT('Ctrl Pts',(6.73733432666607,0.655671672588204,-7.66665457026091));
#46187=CARTESIAN_POINT('Ctrl Pts',(6.71645572713968,0.825537076921797,-7.65859830209016));
#46188=CARTESIAN_POINT('Ctrl Pts',(6.69457720294565,1.00353773035373,-7.65015620050837));
#46189=CARTESIAN_POINT('Ctrl Pts',(6.66564606210925,1.18043544981528,-7.64171409892659));
#46190=CARTESIAN_POINT('Ctrl Pts',(6.62982331990504,1.35562964958847,-7.6332719973448));
#46191=CARTESIAN_POINT('Ctrl Pts',(6.59400057770082,1.53082384936166,-7.62482989576301));
#46192=CARTESIAN_POINT('Ctrl Pts',(6.55128642826821,1.70431410260632,-7.61638779418121));
#46193=CARTESIAN_POINT('Ctrl Pts',(6.50189998196866,1.87552276031936,-7.60794569259942));
#46194=CARTESIAN_POINT('Ctrl Pts',(6.45314010446022,2.04455928357593,-7.59961069646413));
#46195=CARTESIAN_POINT('Ctrl Pts',(6.39772177856541,2.21190939702059,-7.59127570032886));
#46196=CARTESIAN_POINT('Ctrl Pts',(6.33577716324021,2.37701845549501,-7.58294070419358));
#46197=CARTESIAN_POINT('Ctrl Pts',(6.27390699817602,2.54192907198325,-7.57461572575935));
#46198=CARTESIAN_POINT('Ctrl Pts',(6.20552629156955,2.70460367639919,-7.5662907473251));
#46199=CARTESIAN_POINT('Ctrl Pts',(6.13081743388125,2.86450110707218,-7.55796576889087));
#46200=CARTESIAN_POINT('Ctrl Pts',(6.05256284100748,3.0319873828105,-7.54924568109657));
#46201=CARTESIAN_POINT('Ctrl Pts',(5.96736484040027,3.19642607303085,-7.54052559330226));
#46202=CARTESIAN_POINT('Ctrl Pts',(5.87549126295921,3.35721483061332,-7.53180550550796));
#46203=CARTESIAN_POINT('Ctrl Pts',(5.78796009492851,3.51040389921607,-7.52349757311625));
#46204=CARTESIAN_POINT('Ctrl Pts',(5.69437002363127,3.66027974671692,-7.51518964072453));
#46205=CARTESIAN_POINT('Ctrl Pts',(5.59500117228749,3.80634350553147,-7.50688170833281));
#46206=CARTESIAN_POINT('Ctrl Pts',(5.495688731653,3.95232434540187,-7.49857849227175));
#46207=CARTESIAN_POINT('Ctrl Pts',(5.39060424171314,4.09449712128488,-7.49027527621069));
#46208=CARTESIAN_POINT('Ctrl Pts',(5.2800723035603,4.23239004218367,-7.48197206014962));
#46209=CARTESIAN_POINT('Ctrl Pts',(5.1695847597814,4.37022757936263,-7.47367217901676));
#46210=CARTESIAN_POINT('Ctrl Pts',(5.05365434478513,4.50378841599753,-7.4653722978839));
#46211=CARTESIAN_POINT('Ctrl Pts',(4.93264739987986,4.63263193319505,-7.45707241675104));
#46212=CARTESIAN_POINT('Ctrl Pts',(4.81166896840162,4.7614450903977,-7.44877449135762));
#46213=CARTESIAN_POINT('Ctrl Pts',(4.68561662948535,4.88554289072229,-7.44047656596422));
#46214=CARTESIAN_POINT('Ctrl Pts',(4.55489534294085,5.00451969871793,-7.4321786405708));
#46215=CARTESIAN_POINT('Ctrl Pts',(4.42415951349688,5.12350974302575,-7.42387979202327));
#46216=CARTESIAN_POINT('Ctrl Pts',(4.28875395277039,5.23737741924336,-7.41558094347571));
#46217=CARTESIAN_POINT('Ctrl Pts',(4.14911900494689,5.34575537064582,-7.40728209492817));
#46218=CARTESIAN_POINT('Ctrl Pts',(4.00947544449892,5.45414000675443,-7.39898273451117));
#46219=CARTESIAN_POINT('Ctrl Pts',(3.86560225478318,5.5570340338487,-7.39068337409417));
#46220=CARTESIAN_POINT('Ctrl Pts',(3.71797109773611,5.65411177077346,-7.38238401367717));
#46221=CARTESIAN_POINT('Ctrl Pts',(3.5702711685822,5.75123473013384,-7.37408078710811));
#46222=CARTESIAN_POINT('Ctrl Pts',(3.41881006875823,5.84253580051775,-7.36577756053905));
#46223=CARTESIAN_POINT('Ctrl Pts',(3.26408704510001,5.92773352656901,-7.35747433396999));
#46224=CARTESIAN_POINT('Ctrl Pts',(3.20948500324953,5.9577999620188,-7.35454410992254));
#46225=CARTESIAN_POINT('Ctrl Pts',(3.15447694539446,5.98710670692936,-7.35161388587509));
#46226=CARTESIAN_POINT('Ctrl Pts',(3.09908550384714,6.01564277861016,-7.34868366182764));
#46227=CARTESIAN_POINT('Origin',(0.,0.,-63.6971797838103));
#46228=CARTESIAN_POINT('',(3.09908550384723,6.01564277861011,-4.95428495819038));
#46229=CARTESIAN_POINT('',(3.09908550384725,6.0156427786101,-5.34860320957391));
#46230=CARTESIAN_POINT('',(3.09908550384721,6.01564277861012,-63.6971797838103));
#46231=CARTESIAN_POINT('',(-6.76699461023805,0.00854078504219338,-6.30282021615864));
#46232=CARTESIAN_POINT('Ctrl Pts',(-6.76699461023805,0.00854078504218888,
-6.30282021615862));
#46233=CARTESIAN_POINT('Ctrl Pts',(-6.76720711237283,-0.159827906309611,
-6.29489054746016));
#46234=CARTESIAN_POINT('Ctrl Pts',(-6.76113188488697,-0.328457192148686,
-6.28696087876169));
#46235=CARTESIAN_POINT('Ctrl Pts',(-6.74873761255546,-0.496819521435291,
-6.27903121006323));
#46236=CARTESIAN_POINT('Ctrl Pts',(-6.73635391184144,-0.665038247120448,
-6.27110830492636));
#46237=CARTESIAN_POINT('Ctrl Pts',(-6.71766191538891,-0.832990088934394,
-6.2631853997895));
#46238=CARTESIAN_POINT('Ctrl Pts',(-6.69268233672883,-1.00014605915232,
-6.25526249465262));
#46239=CARTESIAN_POINT('Ctrl Pts',(-6.66771834284764,-1.16719774062817,
-6.24734453262253));
#46240=CARTESIAN_POINT('Ctrl Pts',(-6.63647462801936,-1.33345416009714,
-6.23942657059243));
#46241=CARTESIAN_POINT('Ctrl Pts',(-6.59902383464015,-1.49839027955045,
-6.23150860856234));
#46242=CARTESIAN_POINT('Ctrl Pts',(-6.5615829075879,-1.66328294695544,-6.22359273250146));
#46243=CARTESIAN_POINT('Ctrl Pts',(-6.51793823272174,-1.82685563078568,
-6.21567685644061));
#46244=CARTESIAN_POINT('Ctrl Pts',(-6.4682137653419,-1.98859238805783,-6.20776098037973));
#46245=CARTESIAN_POINT('Ctrl Pts',(-6.41849483366338,-2.15031113957894,
-6.19984598557366));
#46246=CARTESIAN_POINT('Ctrl Pts',(-6.3626975674472,-2.31019400355646,-6.19193099076755));
#46247=CARTESIAN_POINT('Ctrl Pts',(-6.30099600942057,-2.46773951001033,
-6.18401599596148));
#46248=CARTESIAN_POINT('Ctrl Pts',(-6.23928856251318,-2.62530005282199,
-6.17610024573752));
#46249=CARTESIAN_POINT('Ctrl Pts',(-6.17167584289126,-2.78052243652897,
-6.16818449551357));
#46250=CARTESIAN_POINT('Ctrl Pts',(-6.09838020600375,-2.93292479668704,
-6.16026874528961));
#46251=CARTESIAN_POINT('Ctrl Pts',(-6.02506240823449,-3.08537323558628,
-6.1523506017444));
#46252=CARTESIAN_POINT('Ctrl Pts',(-5.94605844226286,-3.23499960916278,
-6.1444324581992));
#46253=CARTESIAN_POINT('Ctrl Pts',(-5.86163666280367,-3.38134657100922,
-6.13651431465399));
#46254=CARTESIAN_POINT('Ctrl Pts',(-5.77712022036392,-3.52785763315885,
-6.12858729241572));
#46255=CARTESIAN_POINT('Ctrl Pts',(-5.68717402701725,-3.67108160870135,
-6.12066027017744));
#46256=CARTESIAN_POINT('Ctrl Pts',(-5.5921101966152,-3.81058952773876,-6.11273324793917));
#46257=CARTESIAN_POINT('Ctrl Pts',(-5.49699055219573,-3.95017935487298,
-6.10480157157581));
#46258=CARTESIAN_POINT('Ctrl Pts',(-5.3967475187954,-4.08604847600277,-6.09686989521247));
#46259=CARTESIAN_POINT('Ctrl Pts',(-5.29173303922776,-4.21780161239778,
-6.08893821884911));
#46260=CARTESIAN_POINT('Ctrl Pts',(-5.18655314231556,-4.34976228449692,
-6.08099404861969));
#46261=CARTESIAN_POINT('Ctrl Pts',(-5.07658704153737,-4.47759373644785,
-6.07304987839026));
#46262=CARTESIAN_POINT('Ctrl Pts',(-4.9622236475352,-4.60093745576295,-6.06510570816084));
#46263=CARTESIAN_POINT('Ctrl Pts',(-4.86930048330324,-4.70115736255132,
-6.05865086794422));
#46264=CARTESIAN_POINT('Ctrl Pts',(-4.77347497316505,-4.79841515873253,
-6.0521960277276));
#46265=CARTESIAN_POINT('Ctrl Pts',(-4.67497079558671,-4.89253891761847,
-6.04574118751098));
#46266=CARTESIAN_POINT('Ctrl Pts',(-4.54779207501027,-5.01406208064819,
-6.03740734482067));
#46267=CARTESIAN_POINT('Ctrl Pts',(-4.41570929584349,-5.13077868610561,
-6.02907350213037));
#46268=CARTESIAN_POINT('Ctrl Pts',(-4.27911559842972,-5.24227609872615,
-6.02073965944007));
#46269=CARTESIAN_POINT('Ctrl Pts',(-4.14268289396909,-5.35364209754015,
-6.01241563923771));
#46270=CARTESIAN_POINT('Ctrl Pts',(-4.00175012975998,-5.45980093973423,
-6.00409161903534));
#46271=CARTESIAN_POINT('Ctrl Pts',(-3.85674708017347,-5.56037687208101,
-5.99576759883298));
#46272=CARTESIAN_POINT('Ctrl Pts',(-3.71188834892672,-5.66085270341876,
-5.98745186334448));
#46273=CARTESIAN_POINT('Ctrl Pts',(-3.56296768742227,-5.75575649838763,
-5.97913612785599));
#46274=CARTESIAN_POINT('Ctrl Pts',(-3.4104478977206,-5.84475270109294,-5.9708203923675));
#46275=CARTESIAN_POINT('Ctrl Pts',(-3.25805196204173,-5.93367663424069,
-5.96251140968987));
#46276=CARTESIAN_POINT('Ctrl Pts',(-3.10206302102442,-6.01670235959786,
-5.95420242701225));
#46277=CARTESIAN_POINT('Ctrl Pts',(-2.94297299712593,-6.09353747327344,
-5.94589344433462));
#46278=CARTESIAN_POINT('Ctrl Pts',(-2.78398302922535,-6.17032426327803,
-5.93758968739983));
#46279=CARTESIAN_POINT('Ctrl Pts',(-2.62189617763117,-6.24092804996952,
-5.92928593046504));
#46280=CARTESIAN_POINT('Ctrl Pts',(-2.45722931315714,-6.30510214846368,
-5.92098217353026));
#46281=CARTESIAN_POINT('Ctrl Pts',(-2.29262929946001,-6.36925019382108,
-5.91268178772058));
#46282=CARTESIAN_POINT('Ctrl Pts',(-2.12545168351879,-6.42697362610326,
-5.90438140191092));
#46283=CARTESIAN_POINT('Ctrl Pts',(-1.95623395102337,-6.47807361249187,
-5.89608101610124));
#46284=CARTESIAN_POINT('Ctrl Pts',(-1.78705190214475,-6.52916282322296,
-5.88778238062696));
#46285=CARTESIAN_POINT('Ctrl Pts',(-1.61583092653991,-6.5736312701686,-5.87948374515266));
#46286=CARTESIAN_POINT('Ctrl Pts',(-1.44312456535219,-6.6113297065626,-5.87118510967838));
#46287=CARTESIAN_POINT('Ctrl Pts',(-1.27042595616791,-6.64902645084516,
-5.86288684669212));
#46288=CARTESIAN_POINT('Ctrl Pts',(-1.09624243406426,-6.67995371612954,
-5.85458858370586));
#46289=CARTESIAN_POINT('Ctrl Pts',(-0.921138842400919,-6.70401314385796,
-5.8462903207196));
#46290=CARTESIAN_POINT('Ctrl Pts',(-0.746014046440189,-6.72807548508036,
-5.83799105284912));
#46291=CARTESIAN_POINT('Ctrl Pts',(-0.56996930351817,-6.7452682848114,-5.82969178497865));
#46292=CARTESIAN_POINT('Ctrl Pts',(-0.393575902158023,-6.75554490838752,
-5.82139251710817));
#46293=CARTESIAN_POINT('Ctrl Pts',(-0.217058644198134,-6.76582874780982,
-5.81308742181393));
#46294=CARTESIAN_POINT('Ctrl Pts',(-0.0401925862366737,-6.76918668714386,
-5.80478232651967));
#46295=CARTESIAN_POINT('Ctrl Pts',(0.136448739733167,-6.76562419451637,
-5.79647723122542));
#46296=CARTESIAN_POINT('Ctrl Pts',(0.313154478316598,-6.76206040281879,
-5.78816910746153));
#46297=CARTESIAN_POINT('Ctrl Pts',(0.489634974060889,-6.75157116378814,
-5.77986098369766));
#46298=CARTESIAN_POINT('Ctrl Pts',(0.665320248879113,-6.73421398282171,
-5.77155285993377));
#46299=CARTESIAN_POINT('Ctrl Pts',(0.841192276130339,-6.71683835127211,
-5.76323590468228));
#46300=CARTESIAN_POINT('Ctrl Pts',(1.01626704799254,-6.69258023296174,-5.7549189494308));
#46301=CARTESIAN_POINT('Ctrl Pts',(1.18998214059048,-6.66154873171965,-5.7466019941793));
#46302=CARTESIAN_POINT('Ctrl Pts',(1.31800752143857,-6.63867898732732,-5.74047252466894));
#46303=CARTESIAN_POINT('Ctrl Pts',(1.44529456930429,-6.61213137919877,-5.73434305515856));
#46304=CARTESIAN_POINT('Ctrl Pts',(1.57162303078922,-6.58196703494426,-5.72821358564819));
#46305=CARTESIAN_POINT('Ctrl Pts',(1.74579875685357,-6.54037785939326,-5.71976256210363));
#46306=CARTESIAN_POINT('Ctrl Pts',(1.91847000250474,-6.49183558419278,-5.71131153855909));
#46307=CARTESIAN_POINT('Ctrl Pts',(2.08906228116901,-6.43646702666897,-5.70286051501453));
#46308=CARTESIAN_POINT('Ctrl Pts',(2.25950435839969,-6.38114721951524,-5.69441693234514));
#46309=CARTESIAN_POINT('Ctrl Pts',(2.4278708032841,-6.31901321164062,-5.68597334967575));
#46310=CARTESIAN_POINT('Ctrl Pts',(2.59359998182422,-6.25024224604786,-5.67752976700637));
#46311=CARTESIAN_POINT('Ctrl Pts',(2.75920576982523,-6.18152248258253,-5.66909247084747));
#46312=CARTESIAN_POINT('Ctrl Pts',(2.92217790050786,-6.10617573852384,-5.66065517468856));
#46313=CARTESIAN_POINT('Ctrl Pts',(3.08197212640254,-6.02442833902752,-5.65221787852966));
#46314=CARTESIAN_POINT('Ctrl Pts',(3.2416523512941,-5.9427392600712,-5.64378660173861));
#46315=CARTESIAN_POINT('Ctrl Pts',(3.39815889929805,-5.85465878469378,-5.63535532494755));
#46316=CARTESIAN_POINT('Ctrl Pts',(3.5509694629037,-5.76046047408759,-5.6269240481565));
#46317=CARTESIAN_POINT('Ctrl Pts',(3.70371452636554,-5.66630254029009,-5.61849638531613));
#46318=CARTESIAN_POINT('Ctrl Pts',(3.85276648200666,-5.56603217261552,-5.61006872247578));
#46319=CARTESIAN_POINT('Ctrl Pts',(3.99762893149013,-5.45996812500889,-5.60164105963542));
#46320=CARTESIAN_POINT('Ctrl Pts',(4.14244678657624,-5.35393672811541,-5.59321599116335));
#46321=CARTESIAN_POINT('Ctrl Pts',(4.28307744033944,-5.24211540368635,-5.58479092269128));
#46322=CARTESIAN_POINT('Ctrl Pts',(4.419054422616,-5.1248655601838,-5.57636585421921));
#46323=CARTESIAN_POINT('Ctrl Pts',(4.45626188521486,-5.09278241571475,-5.57406049771829));
#46324=CARTESIAN_POINT('Ctrl Pts',(4.49312109345409,-5.06029305666917,-5.57175514121737));
#46325=CARTESIAN_POINT('Ctrl Pts',(4.5296229160184,-5.02740541817358,-5.56944978471645));
#46326=CARTESIAN_POINT('Ctrl Pts',(4.66609152203814,-4.9044490870789,-5.56083079623976));
#46327=CARTESIAN_POINT('Ctrl Pts',(4.79750107732584,-4.77597765589931,-5.55221180776308));
#46328=CARTESIAN_POINT('Ctrl Pts',(4.92342292830874,-4.64243423959928,-5.5435928192864));
#46329=CARTESIAN_POINT('Ctrl Pts',(5.04942021771019,-4.50881081888339,-5.53496866726698));
#46330=CARTESIAN_POINT('Ctrl Pts',(5.16992303305106,-4.37010957027606,-5.52634451524756));
#46331=CARTESIAN_POINT('Ctrl Pts',(5.28454190082363,-4.22680800349855,-5.51772036322813));
#46332=CARTESIAN_POINT('Ctrl Pts',(5.40308649663685,-4.07859831827684,-5.50880083160788));
#46333=CARTESIAN_POINT('Ctrl Pts',(5.5153367379354,-3.9254678958385,-5.49988129998763));
#46334=CARTESIAN_POINT('Ctrl Pts',(5.62090973344387,-3.76797860509796,-5.49096176836738));
#46335=CARTESIAN_POINT('Ctrl Pts',(5.72317672625415,-3.61542106814178,-5.48232155055708));
#46336=CARTESIAN_POINT('Ctrl Pts',(5.81917821852534,-3.45877381000802,-5.47368133274678));
#46337=CARTESIAN_POINT('Ctrl Pts',(5.90861221698887,-3.29857403573876,-5.46504111493648));
#46338=CARTESIAN_POINT('Ctrl Pts',(6.00238293787045,-3.13060605290927,-5.45598192641126));
#46339=CARTESIAN_POINT('Ctrl Pts',(6.0889332302011,-2.95873280659627,-5.44692273788604));
#46340=CARTESIAN_POINT('Ctrl Pts',(6.16797083144579,-2.78359925679577,-5.43786354936081));
#46341=CARTESIAN_POINT('Ctrl Pts',(6.2470084326905,-2.60846570699522,-5.42880436083559));
#46342=CARTESIAN_POINT('Ctrl Pts',(6.31853323120567,-2.43007222117997,-5.41974517231035));
#46343=CARTESIAN_POINT('Ctrl Pts',(6.38231202064313,-2.24908476299898,-5.41068598378512));
#46344=CARTESIAN_POINT('Ctrl Pts',(6.44598031801662,-2.06841085228392,-5.40164248963802));
#46345=CARTESIAN_POINT('Ctrl Pts',(6.50198887538156,-1.88498578516538,-5.39259899549091));
#46346=CARTESIAN_POINT('Ctrl Pts',(6.55012725636153,-1.69944753536844,-5.38355550134381));
#46347=CARTESIAN_POINT('Ctrl Pts',(6.59822160533842,-1.51407899673791,-5.37452027924812));
#46348=CARTESIAN_POINT('Ctrl Pts',(6.63846009066339,-1.32660136477124,-5.36548505715244));
#46349=CARTESIAN_POINT('Ctrl Pts',(6.6706823728222,-1.13766677059639,-5.35644983505675));
#46350=CARTESIAN_POINT('Ctrl Pts',(6.70284788632655,-0.949065038092803,
-5.34743053105769));
#46351=CARTESIAN_POINT('Ctrl Pts',(6.72702535817801,-0.759011703455649,
-5.33841122705862));
#46352=CARTESIAN_POINT('Ctrl Pts',(6.74310568222232,-0.56816789629568,-5.32939192305955));
#46353=CARTESIAN_POINT('Ctrl Pts',(6.75916583237354,-0.377563516062186,
-5.32038393440925));
#46354=CARTESIAN_POINT('Ctrl Pts',(6.7671490875398,-0.186170878945884,-5.31137594575893));
#46355=CARTESIAN_POINT('Ctrl Pts',(6.7669978911239,0.00534242685262255,
-5.30236795710862));
#46356=CARTESIAN_POINT('Ctrl Pts',(6.76684703619048,0.196423193049244,-5.29338031332056));
#46357=CARTESIAN_POINT('Ctrl Pts',(6.75859840195246,0.38762384627601,-5.2843926695325));
#46358=CARTESIAN_POINT('Ctrl Pts',(6.74224635805464,0.578275926612022,-5.27540502574443));
#46359=CARTESIAN_POINT('Ctrl Pts',(6.72800486210553,0.744320663695759,-5.26757741144743));
#46360=CARTESIAN_POINT('Ctrl Pts',(6.70761753852657,0.909949118378983,-5.25974979715043));
#46361=CARTESIAN_POINT('Ctrl Pts',(6.68111286994208,1.07471848364786,-5.25192218285343));
#46362=CARTESIAN_POINT('Ctrl Pts',(6.65360747519168,1.24570897990876,-5.24379902445563));
#46363=CARTESIAN_POINT('Ctrl Pts',(6.61952471774068,1.41569758942989,-5.23567586605784));
#46364=CARTESIAN_POINT('Ctrl Pts',(6.57896549905707,1.5841407646471,-5.22755270766005));
#46365=CARTESIAN_POINT('Ctrl Pts',(6.53840914001137,1.7525720637359,-5.21943012198757));
#46366=CARTESIAN_POINT('Ctrl Pts',(6.49137731497009,1.91945778970711,-5.21130753631509));
#46367=CARTESIAN_POINT('Ctrl Pts',(6.43802168382705,2.08426624944434,-5.20318495064262));
#46368=CARTESIAN_POINT('Ctrl Pts',(6.38465964145645,2.24909451261215,-5.19506138895799));
#46369=CARTESIAN_POINT('Ctrl Pts',(6.3249723937789,2.41184466467059,-5.18693782727336));
#46370=CARTESIAN_POINT('Ctrl Pts',(6.25916093024621,2.57200183695103,-5.17881426558873));
#46371=CARTESIAN_POINT('Ctrl Pts',(6.19330153087195,2.73227566472615,-5.1706847868534));
#46372=CARTESIAN_POINT('Ctrl Pts',(6.12130914558339,2.88995240163682,-5.16255530811808));
#46373=CARTESIAN_POINT('Ctrl Pts',(6.04343248649321,3.04453818849402,-5.15442582938275));
#46374=CARTESIAN_POINT('Ctrl Pts',(5.96552407846039,3.19918699725454,-5.14629303640209));
#46375=CARTESIAN_POINT('Ctrl Pts',(5.88172679186075,3.35074202406299,-5.1381602434214));
#46376=CARTESIAN_POINT('Ctrl Pts',(5.79233432410532,3.49873578279233,-5.13002745044074));
#46377=CARTESIAN_POINT('Ctrl Pts',(5.70284465560015,3.64689046228675,-5.12188581428129));
#46378=CARTESIAN_POINT('Ctrl Pts',(5.60774785532039,3.79147583397952,-5.11374417812184));
#46379=CARTESIAN_POINT('Ctrl Pts',(5.50738021654732,3.93205444397495,-5.10560254196239));
#46380=CARTESIAN_POINT('Ctrl Pts',(5.45624426404744,4.00367734166491,-5.10145448861561));
#46381=CARTESIAN_POINT('Ctrl Pts',(5.40374077199387,4.07426071113786,-5.09730643526883));
#46382=CARTESIAN_POINT('Ctrl Pts',(5.34991806237872,4.14375020070394,-5.09315838192204));
#46383=CARTESIAN_POINT('Ctrl Pts',(5.24039083725283,4.28515874408661,-5.0847172466467));
#46384=CARTESIAN_POINT('Ctrl Pts',(5.12517271087284,4.42232659902459,-5.07627611137136));
#46385=CARTESIAN_POINT('Ctrl Pts',(5.00461878989457,4.55478646786369,-5.06783497609601));
#46386=CARTESIAN_POINT('Ctrl Pts',(4.88415430102167,4.68714807225107,-5.05940010281939));
#46387=CARTESIAN_POINT('Ctrl Pts',(4.75836213143086,4.81480840661897,-5.05096522954278));
#46388=CARTESIAN_POINT('Ctrl Pts',(4.62763773171091,4.93733308822136,-5.04253035626616));
#46389=CARTESIAN_POINT('Ctrl Pts',(4.49700434453506,5.05977246606248,-5.03410135549136));
#46390=CARTESIAN_POINT('Ctrl Pts',(4.36144581882315,5.17708309505497,-5.02567235471656));
#46391=CARTESIAN_POINT('Ctrl Pts',(4.22139467466584,5.28886717555876,-5.01724335394176));
#46392=CARTESIAN_POINT('Ctrl Pts',(4.08140243801101,5.40060423808895,-5.00881789852453));
#46393=CARTESIAN_POINT('Ctrl Pts',(3.93692161000627,5.50681917839115,-5.00039244310729));
#46394=CARTESIAN_POINT('Ctrl Pts',(3.78841848304066,5.60715385889811,-4.99196698769006));
#46395=CARTESIAN_POINT('Ctrl Pts',(3.6399552691467,5.70746157252985,-4.98354379677603));
#46396=CARTESIAN_POINT('Ctrl Pts',(3.48747218749065,5.80189199062351,-4.97512060586202));
#46397=CARTESIAN_POINT('Ctrl Pts',(3.33146557681007,5.89012954955403,-4.96669741494799));
#46398=CARTESIAN_POINT('Ctrl Pts',(3.25483486647963,5.93347198734671,-4.96255992936213));
#46399=CARTESIAN_POINT('Ctrl Pts',(3.17735444124636,5.97532088147924,-4.95842244377625));
#46400=CARTESIAN_POINT('Ctrl Pts',(3.09908550384723,6.01564277861011,-4.95428495819038));
#46401=CARTESIAN_POINT('Ctrl Pts',(3.09908550384728,6.01564277861009,-6.95401477785997));
#46402=CARTESIAN_POINT('Ctrl Pts',(2.94372312579465,6.09568099088196,-6.94578931815296));
#46403=CARTESIAN_POINT('Ctrl Pts',(2.78510216617008,6.16977702221691,-6.93756385844597));
#46404=CARTESIAN_POINT('Ctrl Pts',(2.62371606615217,6.23766005840451,-6.92933839873896));
#46405=CARTESIAN_POINT('Ctrl Pts',(2.46248089378075,6.30547961064345,-6.92112063144954));
#46406=CARTESIAN_POINT('Ctrl Pts',(2.29848606155289,6.36709761084517,-6.91290286416012));
#46407=CARTESIAN_POINT('Ctrl Pts',(2.13224832484289,6.42228978489796,-6.90468509687069));
#46408=CARTESIAN_POINT('Ctrl Pts',(1.9661012565253,6.47745185636518,-6.89647181166677));
#46409=CARTESIAN_POINT('Ctrl Pts',(1.79771405661862,6.52619496945636,-6.88825852646284));
#46410=CARTESIAN_POINT('Ctrl Pts',(1.62762253474435,6.56834331352986,-6.88004524125892));
#46411=CARTESIAN_POINT('Ctrl Pts',(1.45759198929683,6.61047654776492,-6.87183490045092));
#46412=CARTESIAN_POINT('Ctrl Pts',(1.28585868366744,6.64601963619481,-6.86362455964293));
#46413=CARTESIAN_POINT('Ctrl Pts',(1.11297273894915,6.67484686583565,-6.85541421883494));
#46414=CARTESIAN_POINT('Ctrl Pts',(1.00169281192937,6.69340182711861,-6.85012954327956));
#46415=CARTESIAN_POINT('Ctrl Pts',(0.889935635221197,6.70917542902428,-6.84484486772417));
#46416=CARTESIAN_POINT('Ctrl Pts',(0.777850161710652,6.722145351443,-6.83956019216879));
#46417=CARTESIAN_POINT('Ctrl Pts',(0.589960945506097,6.74388687138455,-6.83070147464816));
#46418=CARTESIAN_POINT('Ctrl Pts',(0.401343712628413,6.75772536213437,-6.82184275712753));
#46419=CARTESIAN_POINT('Ctrl Pts',(0.212651766161567,6.7636579028177,-6.8129840396069));
#46420=CARTESIAN_POINT('Ctrl Pts',(0.0236068073694866,6.76960154233181,
-6.80410874884863));
#46421=CARTESIAN_POINT('Ctrl Pts',(-0.165512885127531,6.76760966529908,
-6.79523345809037));
#46422=CARTESIAN_POINT('Ctrl Pts',(-0.354056027043083,6.75773137448615,
-6.7863581673321));
#46423=CARTESIAN_POINT('Ctrl Pts',(-0.543134673873633,6.74782502710628,
-6.77745766875256));
#46424=CARTESIAN_POINT('Ctrl Pts',(-0.731633232608158,6.72998745607991,
-6.76855717017301));
#46425=CARTESIAN_POINT('Ctrl Pts',(-0.918904468882634,6.70431976989967,
-6.75965667159348));
#46426=CARTESIAN_POINT('Ctrl Pts',(-1.10642921447976,6.67861733733836,-6.75074412439712));
#46427=CARTESIAN_POINT('Ctrl Pts',(-1.29272306280434,6.64506365792602,-6.74183157720076));
#46428=CARTESIAN_POINT('Ctrl Pts',(-1.47714958757996,6.60381087675233,-6.7329190300044));
#46429=CARTESIAN_POINT('Ctrl Pts',(-1.6619833441341,6.5624670054089,-6.7239868030334));
#46430=CARTESIAN_POINT('Ctrl Pts',(-1.84494127586665,6.51339008559803,-6.71505457606242));
#46431=CARTESIAN_POINT('Ctrl Pts',(-2.02539994993796,6.45678279352739,-6.70612234909142));
#46432=CARTESIAN_POINT('Ctrl Pts',(-2.19595423570235,6.40328236569897,-6.69768036313999));
#46433=CARTESIAN_POINT('Ctrl Pts',(-2.36427605199081,6.34305596615075,-6.68923837718855));
#46434=CARTESIAN_POINT('Ctrl Pts',(-2.52985608457464,6.27631398125848,-6.68079639123712));
#46435=CARTESIAN_POINT('Ctrl Pts',(-2.69116006683436,6.21129558635274,-6.67257241681886));
#46436=CARTESIAN_POINT('Ctrl Pts',(-2.85016978965994,6.1399686234312,-6.66434844240058));
#46437=CARTESIAN_POINT('Ctrl Pts',(-3.00635765272632,6.06251619906239,-6.6561244679823));
#46438=CARTESIAN_POINT('Ctrl Pts',(-3.16238056625533,5.98514557196846,-6.64790917887894));
#46439=CARTESIAN_POINT('Ctrl Pts',(-3.31558723591539,5.90166252353698,-6.63969388977555));
#46440=CARTESIAN_POINT('Ctrl Pts',(-3.46546847096888,5.81229879451501,-6.63147860067218));
#46441=CARTESIAN_POINT('Ctrl Pts',(-3.61522147987744,5.72301151780187,-6.62327033989929));
#46442=CARTESIAN_POINT('Ctrl Pts',(-3.76165441395981,5.62785376290883,-6.61506207912641));
#46443=CARTESIAN_POINT('Ctrl Pts',(-3.9042811250425,5.5271039339456,-6.60685381835351));
#46444=CARTESIAN_POINT('Ctrl Pts',(-4.04681441609006,5.42642009579495,-6.59865093396491));
#46445=CARTESIAN_POINT('Ctrl Pts',(-4.18554615821571,5.32015168562442,-6.59044804957631));
#46446=CARTESIAN_POINT('Ctrl Pts',(-4.32001766245039,5.20862135273017,-6.58224516518771));
#46447=CARTESIAN_POINT('Ctrl Pts',(-4.454428047211,5.09714171217649,-6.57404600914276));
#46448=CARTESIAN_POINT('Ctrl Pts',(-4.58458177634407,4.98040514210116,-6.56584685309781));
#46449=CARTESIAN_POINT('Ctrl Pts',(-4.71005177716155,4.85877569521966,-6.55764769705286));
#46450=CARTESIAN_POINT('Ctrl Pts',(-4.83551086513983,4.73715682714256,-6.54944925413513));
#46451=CARTESIAN_POINT('Ctrl Pts',(-4.95628677300689,4.61064617319267,-6.54125081121741));
#46452=CARTESIAN_POINT('Ctrl Pts',(-5.07198770799842,4.47964615677544,-6.53305236829967));
#46453=CARTESIAN_POINT('Ctrl Pts',(-5.1876874907456,4.3486474449633,-6.52485400702872));
#46454=CARTESIAN_POINT('Ctrl Pts',(-5.29831216303947,4.21315972788572,-6.51665564575777));
#46455=CARTESIAN_POINT('Ctrl Pts',(-5.40350890565426,4.07362007390418,-6.50845728448682));
#46456=CARTESIAN_POINT('Ctrl Pts',(-5.50872371037568,3.93405646119497,-6.5002575155708));
#46457=CARTESIAN_POINT('Ctrl Pts',(-5.60850851273157,3.79043981195242,-6.49205774665481));
#46458=CARTESIAN_POINT('Ctrl Pts',(-5.70255264668566,3.64323788844188,-6.48385797773879));
#46459=CARTESIAN_POINT('Ctrl Pts',(-5.79663001183018,3.49598395004272,-6.47565531137377));
#46460=CARTESIAN_POINT('Ctrl Pts',(-5.8849624747538,3.34514251581136,-6.46745264500874));
#46461=CARTESIAN_POINT('Ctrl Pts',(-5.96728429184347,3.19120779334693,-6.45924997864372));
#46462=CARTESIAN_POINT('Ctrl Pts',(-6.04969960594082,3.03709823951412,-6.45103799609998));
#46463=CARTESIAN_POINT('Ctrl Pts',(-6.12609046668072,2.87988869538403,-6.44282601355628));
#46464=CARTESIAN_POINT('Ctrl Pts',(-6.1962380045632,2.72009624660722,-6.43461403101254));
#46465=CARTESIAN_POINT('Ctrl Pts',(-6.26642691641151,2.56020955008465,-6.42639720493053));
#46466=CARTESIAN_POINT('Ctrl Pts',(-6.33036503393945,2.39773724539352,-6.41818037884849));
#46467=CARTESIAN_POINT('Ctrl Pts',(-6.38788279024429,2.2332134824286,-6.40996355276648));
#46468=CARTESIAN_POINT('Ctrl Pts',(-6.44548924723638,2.06843600005976,-6.40173405515192));
#46469=CARTESIAN_POINT('Ctrl Pts',(-6.49665545189059,1.90160107999209,-6.39350455753737));
#46470=CARTESIAN_POINT('Ctrl Pts',(-6.54126223146,1.73325630513059,-6.38527505992281));
#46471=CARTESIAN_POINT('Ctrl Pts',(-6.58102281408157,1.58320094595872,-6.37793963640657));
#46472=CARTESIAN_POINT('Ctrl Pts',(-6.61557250581569,1.43194629982475,-6.37060421289033));
#46473=CARTESIAN_POINT('Ctrl Pts',(-6.64486161374839,1.27988403151738,-6.36326878937409));
#46474=CARTESIAN_POINT('Ctrl Pts',(-6.6917400058292,1.0365022716225,-6.35152814980036));
#46475=CARTESIAN_POINT('Ctrl Pts',(-6.7252771074405,0.790369188616169,-6.33978751022664));
#46476=CARTESIAN_POINT('Ctrl Pts',(-6.74520470436182,0.542680841982831,
-6.32804687065291));
#46477=CARTESIAN_POINT('Ctrl Pts',(-6.75947725452555,0.365281411120508,
-6.31963798583193));
#46478=CARTESIAN_POINT('Ctrl Pts',(-6.7667692658776,0.187084554290086,-6.31122910101097));
#46479=CARTESIAN_POINT('Ctrl Pts',(-6.76699461023721,0.0085407857079797,
-6.30282021618999));
#46480=CARTESIAN_POINT('',(-6.767,1.31899902783804E-12,-6.69717978381011));
#46481=CARTESIAN_POINT('Ctrl Pts',(3.09908550384714,6.01564277861016,-7.34868366182764));
#46482=CARTESIAN_POINT('Ctrl Pts',(2.94200344356414,6.09656692152444,-7.34037397322581));
#46483=CARTESIAN_POINT('Ctrl Pts',(2.7818368468515,6.17128969279476,-7.33206428462395));
#46484=CARTESIAN_POINT('Ctrl Pts',(2.61911520635259,6.23959329891401,-7.32375459602213));
#46485=CARTESIAN_POINT('Ctrl Pts',(2.4562330644433,6.30796427668145,-7.31543671111197));
#46486=CARTESIAN_POINT('Ctrl Pts',(2.29079116923637,6.36990331782327,-7.30711882620181));
#46487=CARTESIAN_POINT('Ctrl Pts',(2.12333635217102,6.42524176475478,-7.29880094129163));
#46488=CARTESIAN_POINT('Ctrl Pts',(2.06708211921916,6.44383198472835,-7.29600665777322));
#46489=CARTESIAN_POINT('Ctrl Pts',(2.01060083010719,6.46167772582537,-7.29321237425482));
#46490=CARTESIAN_POINT('Ctrl Pts',(1.95391351252487,6.47877387979954,-7.29041809073641));
#46491=CARTESIAN_POINT('Ctrl Pts',(1.78246854235173,6.53047944169917,-7.28196706721121));
#46492=CARTESIAN_POINT('Ctrl Pts',(1.60882488134752,6.57541929489793,-7.273516043686));
#46493=CARTESIAN_POINT('Ctrl Pts',(1.43354279756602,6.61341394799589,-7.2650650201608));
#46494=CARTESIAN_POINT('Ctrl Pts',(1.25841504444962,6.65137514793107,-7.25662143751063));
#46495=CARTESIAN_POINT('Ctrl Pts',(1.08165206635396,6.68240326630607,-7.24817785486046));
#46496=CARTESIAN_POINT('Ctrl Pts',(0.903828398855612,6.7063688554554,-7.23973427221029));
#46497=CARTESIAN_POINT('Ctrl Pts',(0.726137126617511,6.73031660147699,-7.23129697607045));
#46498=CARTESIAN_POINT('Ctrl Pts',(0.547387066681654,6.74721225626119,-7.22285967993061));
#46499=CARTESIAN_POINT('Ctrl Pts',(0.368162427983455,6.75697753634133,-7.21442238379078));
#46500=CARTESIAN_POINT('Ctrl Pts',(0.189065652399561,6.76673584963871,-7.20599110701841));
#46501=CARTESIAN_POINT('Ctrl Pts',(0.00949530359264483,6.76937391707232,
-7.19755983024603));
#46502=CARTESIAN_POINT('Ctrl Pts',(-0.169959600044876,6.76486531531505,
-7.18912855347367));
#46503=CARTESIAN_POINT('Ctrl Pts',(-0.34933758281461,6.7603586461077,-7.18070089065173));
#46504=CARTESIAN_POINT('Ctrl Pts',(-0.528599888290563,6.74871142288825,
-7.17227322782982));
#46505=CARTESIAN_POINT('Ctrl Pts',(-0.707157146879609,6.72994931404517,
-7.16384556500788));
#46506=CARTESIAN_POINT('Ctrl Pts',(-0.885659438482283,6.71119298092127,
-7.15542049655389));
#46507=CARTESIAN_POINT('Ctrl Pts',(-1.06345678674942,6.68532616467469,-7.14699542809988));
#46508=CARTESIAN_POINT('Ctrl Pts',(-1.23996422122642,6.65242645431563,-7.13857035964589));
#46509=CARTESIAN_POINT('Ctrl Pts',(-1.28826205805277,6.64342408652718,-7.13626500303217));
#46510=CARTESIAN_POINT('Ctrl Pts',(-1.3364633524736,6.63389543839418,-7.13395964641846));
#46511=CARTESIAN_POINT('Ctrl Pts',(-1.38455622051691,6.62384277230581,-7.13165428980474));
#46512=CARTESIAN_POINT('Ctrl Pts',(-1.56436001976624,6.58625907998689,-7.12303530128034));
#46513=CARTESIAN_POINT('Ctrl Pts',(-1.74256715692082,6.54136368508706,-7.11441631275595));
#46514=CARTESIAN_POINT('Ctrl Pts',(-1.91858422653124,6.48932381421251,-7.10579732423155));
#46515=CARTESIAN_POINT('Ctrl Pts',(-2.09470674607431,6.4372527668112,-7.09717317216385));
#46516=CARTESIAN_POINT('Ctrl Pts',(-2.26863628795792,6.3780287877381,-7.08854902009614));
#46517=CARTESIAN_POINT('Ctrl Pts',(-2.43979599739637,6.31186854196827,-7.07992486802844));
#46518=CARTESIAN_POINT('Ctrl Pts',(-2.61681797293183,6.2434422899811,-7.07100533643219));
#46519=CARTESIAN_POINT('Ctrl Pts',(-2.79087669084853,6.16759635760581,-7.06208580483594));
#46520=CARTESIAN_POINT('Ctrl Pts',(-2.96135853479528,6.08462362257479,-7.05316627323968));
#46521=CARTESIAN_POINT('Ctrl Pts',(-3.12650176645941,6.00424916576569,-7.04452605538049));
#46522=CARTESIAN_POINT('Ctrl Pts',(-3.28828850598584,5.91718768584641,-7.03588583752132));
#46523=CARTESIAN_POINT('Ctrl Pts',(-3.44618745744697,5.82375145487298,-7.02724561966213));
#46524=CARTESIAN_POINT('Ctrl Pts',(-3.61174304678404,5.72578443139944,-7.01818643119735));
#46525=CARTESIAN_POINT('Ctrl Pts',(-3.77302410569276,5.62080926558137,-7.00912724273256));
#46526=CARTESIAN_POINT('Ctrl Pts',(-3.92945352472115,5.50923624444047,-7.00006805426778));
#46527=CARTESIAN_POINT('Ctrl Pts',(-4.08588294374954,5.39766322329956,-6.991008865803));
#46528=CARTESIAN_POINT('Ctrl Pts',(-4.2374604415056,5.27949260821497,-6.9819496773382));
#46529=CARTESIAN_POINT('Ctrl Pts',(-4.38364937395421,5.15518255411299,-6.97289048887341));
#46530=CARTESIAN_POINT('Ctrl Pts',(-4.52958504433626,5.03108785845619,-6.9638469948169));
#46531=CARTESIAN_POINT('Ctrl Pts',(-4.67028579583294,4.90076130110252,-6.95480350076039));
#46532=CARTESIAN_POINT('Ctrl Pts',(-4.80524874609557,4.76464830686872,-6.94576000670389));
#46533=CARTESIAN_POINT('Ctrl Pts',(-4.9400882462411,4.62865981469304,-6.93672478469832));
#46534=CARTESIAN_POINT('Ctrl Pts',(-5.06920025600074,4.48689562171797,-6.92768956269277));
#46535=CARTESIAN_POINT('Ctrl Pts',(-5.19211806112594,4.33983859599984,-6.91865434068721));
#46536=CARTESIAN_POINT('Ctrl Pts',(-5.31481931183733,4.19304065274716,-6.90963503677588));
#46537=CARTESIAN_POINT('Ctrl Pts',(-5.4313479970059,4.04096867969486,-6.90061573286456));
#46538=CARTESIAN_POINT('Ctrl Pts',(-5.54127714858927,3.88413910185029,-6.89159642895323));
#46539=CARTESIAN_POINT('Ctrl Pts',(-5.65106838637363,3.72750627766539,-6.88258844038864));
#46540=CARTESIAN_POINT('Ctrl Pts',(-5.75427647750861,3.56612795463913,-6.87358045182403));
#46541=CARTESIAN_POINT('Ctrl Pts',(-5.85051575148578,3.40055207894495,-6.86457246325944));
#46542=CARTESIAN_POINT('Ctrl Pts',(-5.94653766569161,3.23535016216579,-6.85558481955256));
#46543=CARTESIAN_POINT('Ctrl Pts',(-6.03562206043584,3.06596982176754,-6.84659717584569));
#46544=CARTESIAN_POINT('Ctrl Pts',(-6.11742769958871,2.89298588664113,-6.83760953213881));
#46545=CARTESIAN_POINT('Ctrl Pts',(-6.18867474131694,2.7423288687156,-6.82978191740645));
#46546=CARTESIAN_POINT('Ctrl Pts',(-6.25440127660616,2.58893899415625,-6.82195430267408));
#46547=CARTESIAN_POINT('Ctrl Pts',(-6.31440909771308,2.43321325549535,-6.81412668794172));
#46548=CARTESIAN_POINT('Ctrl Pts',(-6.37465596804438,2.27686716241471,-6.80626789085354));
#46549=CARTESIAN_POINT('Ctrl Pts',(-6.42912601522734,2.11819375689573,-6.79840909376536));
#46550=CARTESIAN_POINT('Ctrl Pts',(-6.47763603090721,1.95768241834388,-6.79055029667717));
#46551=CARTESIAN_POINT('Ctrl Pts',(-6.52615098102859,1.79715475256967,-6.7826907001917));
#46552=CARTESIAN_POINT('Ctrl Pts',(-6.56870456311595,1.63478914977025,-6.77483110370624));
#46553=CARTESIAN_POINT('Ctrl Pts',(-6.60516308027976,1.47109132378285,-6.76697150722077));
#46554=CARTESIAN_POINT('Ctrl Pts',(-6.64162179949535,1.30739259058809,-6.7591118671777));
#46555=CARTESIAN_POINT('Ctrl Pts',(-6.67198530883263,1.14236200194392,-6.75125222713463));
#46556=CARTESIAN_POINT('Ctrl Pts',(-6.69617098524394,0.976515814709235,
-6.74339258709157));
#46557=CARTESIAN_POINT('Ctrl Pts',(-6.720373904881,0.810551387107869,-6.73552734350262));
#46558=CARTESIAN_POINT('Ctrl Pts',(-6.73839014284395,0.643770586544007,
-6.72766209991364));
#46559=CARTESIAN_POINT('Ctrl Pts',(-6.75018891372674,0.4766955307118,-6.71979685632468));
#46560=CARTESIAN_POINT('Ctrl Pts',(-6.76140225160766,0.31791042748965,-6.71232187145086));
#46561=CARTESIAN_POINT('Ctrl Pts',(-6.76700020687108,0.158859864586206,
-6.70484688657703));
#46562=CARTESIAN_POINT('Ctrl Pts',(-6.76699999999426,-8.81190322315926E-6,
-6.6973719017032));
#46563=CARTESIAN_POINT('Ctrl Pts',(-6.767,1.31899900917185E-12,-6.6971797838101));
#46564=CARTESIAN_POINT('Ctrl Pts',(-6.76700000000004,-0.186007249558627,
-6.68843027199736));
#46565=CARTESIAN_POINT('Ctrl Pts',(-6.75932637294254,-0.372014355814748,
-6.67968076018463));
#46566=CARTESIAN_POINT('Ctrl Pts',(-6.74400518263374,-0.557389537585063,
-6.67093124837189));
#46567=CARTESIAN_POINT('Ctrl Pts',(-6.72868405703741,-0.742763936381794,
-6.66218177351468));
#46568=CARTESIAN_POINT('Ctrl Pts',(-6.70571545643574,-0.927506130404363,
-6.65343229865747));
#46569=CARTESIAN_POINT('Ctrl Pts',(-6.6751773940158,-1.11098864009513,-6.64468282380025));
#46570=CARTESIAN_POINT('Ctrl Pts',(-6.64463945804395,-1.29447039004509,
-6.63593338517174));
#46571=CARTESIAN_POINT('Ctrl Pts',(-6.60653217002731,-1.47669218339244,
-6.62718394654323));
#46572=CARTESIAN_POINT('Ctrl Pts',(-6.56098496085489,-1.65703510627748,
-6.61843450791471));
#46573=CARTESIAN_POINT('Ctrl Pts',(-6.51543793649563,-1.83737729739984,
-6.60968510478808));
#46574=CARTESIAN_POINT('Ctrl Pts',(-6.46245112156901,-2.01584035544936,
-6.60093570166145));
#46575=CARTESIAN_POINT('Ctrl Pts',(-6.40220448361719,-2.19181813797402,
-6.59218629853481));
#46576=CARTESIAN_POINT('Ctrl Pts',(-6.34195808511981,-2.36779522106281,
-6.58343693018329));
#46577=CARTESIAN_POINT('Ctrl Pts',(-6.27445201416368,-2.54128677725708,
-6.57468756183176));
#46578=CARTESIAN_POINT('Ctrl Pts',(-6.19991555052746,-2.71170355428608,
-6.56593819348024));
#46579=CARTESIAN_POINT('Ctrl Pts',(-6.12537937695139,-2.88211966813477,
-6.55718885917705));
#46580=CARTESIAN_POINT('Ctrl Pts',(-6.04381298028365,-3.04946076419841,
-6.54843952487388));
#46581=CARTESIAN_POINT('Ctrl Pts',(-5.95549339308889,-3.21315848424485,
-6.5396901905707));
#46582=CARTESIAN_POINT('Ctrl Pts',(-5.86717414225711,-3.37685558085253,
-6.53094088958914));
#46583=CARTESIAN_POINT('Ctrl Pts',(-5.77210188843963,-3.53690907700169,
-6.52219158860758));
#46584=CARTESIAN_POINT('Ctrl Pts',(-5.67059953311263,-3.69277537024158,
-6.51344228762603));
#46585=CARTESIAN_POINT('Ctrl Pts',(-5.56909755592579,-3.84864108281213,
-6.5046930192394));
#46586=CARTESIAN_POINT('Ctrl Pts',(-5.46116568154816,-4.00031938355035,
-6.49594375085278));
#46587=CARTESIAN_POINT('Ctrl Pts',(-5.34717048488204,-4.14729511918388,
-6.48719448246615));
#46588=CARTESIAN_POINT('Ctrl Pts',(-5.2331757034312,-4.29427031947405,-6.4784452459478));
#46589=CARTESIAN_POINT('Ctrl Pts',(-5.1131178195135,-4.43654276249783,-6.46969600942943));
#46590=CARTESIAN_POINT('Ctrl Pts',(-4.98740458929035,-4.57362924412612,
-6.46094677291107));
#46591=CARTESIAN_POINT('Ctrl Pts',(-4.86169180652517,-4.71071523781498,
-6.45219756753435));
#46592=CARTESIAN_POINT('Ctrl Pts',(-4.73032391141336,-4.84261509584721,
-6.44344836215764));
#46593=CARTESIAN_POINT('Ctrl Pts',(-4.59374706947077,-4.9688808459983,-6.43469915678092));
#46594=CARTESIAN_POINT('Ctrl Pts',(-4.45717070231283,-5.09514615720938,
-6.42594998181922));
#46595=CARTESIAN_POINT('Ctrl Pts',(-4.31538563497165,-5.21577720520745,
-6.41720080685753));
#46596=CARTESIAN_POINT('Ctrl Pts',(-4.16887340951873,-5.33036429293606,
-6.40845163189584));
#46597=CARTESIAN_POINT('Ctrl Pts',(-4.02236168122362,-5.44495099183796,
-6.39970248662259));
#46598=CARTESIAN_POINT('Ctrl Pts',(-3.8711230526307,-5.55349359498005,-6.39095334134935));
#46599=CARTESIAN_POINT('Ctrl Pts',(-3.71567116928898,-5.65562346357276,
-6.3822041960761));
#46600=CARTESIAN_POINT('Ctrl Pts',(-3.56021980053228,-5.75775299408978,
-6.37345507976474));
#46601=CARTESIAN_POINT('Ctrl Pts',(-3.40055544442016,-5.85346967519918,
-6.36470596345339));
#46602=CARTESIAN_POINT('Ctrl Pts',(-3.23722035886792,-5.94244843041411,
-6.35595684714203));
#46603=CARTESIAN_POINT('Ctrl Pts',(-3.0738858004343,-6.03142689847482,-6.34720775906601));
#46604=CARTESIAN_POINT('Ctrl Pts',(-2.90688078789154,-6.11366734707935,
-6.33845867098999));
#46605=CARTESIAN_POINT('Ctrl Pts',(-2.73677250610315,-6.18889047001463,
-6.32970958291397));
#46606=CARTESIAN_POINT('Ctrl Pts',(-2.56666475916863,-6.26411335643363,
-6.32096052234681));
#46607=CARTESIAN_POINT('Ctrl Pts',(-2.39345402457027,-6.33231884545281,
-6.31221146177964));
#46608=CARTESIAN_POINT('Ctrl Pts',(-2.21772855944005,-6.39327529804903,
-6.30346240121247));
#46609=CARTESIAN_POINT('Ctrl Pts',(-2.0420036322354,-6.45423156404718,-6.29471336742767));
#46610=CARTESIAN_POINT('Ctrl Pts',(-1.86376426060992,-6.50793874412465,
-6.28596433364288));
#46611=CARTESIAN_POINT('Ctrl Pts',(-1.68361577621656,-6.5542144394332,-6.27721529985808));
#46612=CARTESIAN_POINT('Ctrl Pts',(-1.50346782833206,-6.60048999692589,
-6.26846629212919));
#46613=CARTESIAN_POINT('Ctrl Pts',(-1.32141105657402,-6.63933404265158,
-6.25971728440031));
#46614=CARTESIAN_POINT('Ctrl Pts',(-1.13806375346573,-6.67061465631523,
-6.25096827667143));
#46615=CARTESIAN_POINT('Ctrl Pts',(-0.954716981170584,-6.70189517941762,
-6.24221929427201));
#46616=CARTESIAN_POINT('Ctrl Pts',(-0.770079967443055,-6.72561226608995,
-6.23347031187258));
#46617=CARTESIAN_POINT('Ctrl Pts',(-0.58477976407404,-6.74168536995976,
-6.22472132947316));
#46618=CARTESIAN_POINT('Ctrl Pts',(-0.391489587593874,-6.75845153117867,
-6.21559509905754));
#46619=CARTESIAN_POINT('Ctrl Pts',(-0.1974780918061,-6.76689985146392,-6.20646886864193));
#46620=CARTESIAN_POINT('Ctrl Pts',(-0.0034621475318405,-6.76699911434415,
-6.19734263822631));
#46621=CARTESIAN_POINT('Ctrl Pts',(0.184490798483868,-6.76709527525937,
-6.18850160251118));
#46622=CARTESIAN_POINT('Ctrl Pts',(0.372447602154045,-6.75935633790767,
-6.17966056679605));
#46623=CARTESIAN_POINT('Ctrl Pts',(0.55975644819352,-6.74380914014519,-6.17081953108092));
#46624=CARTESIAN_POINT('Ctrl Pts',(0.745136131042648,-6.72842206873162,
-6.16206955246761));
#46625=CARTESIAN_POINT('Ctrl Pts',(0.929880851944321,-6.70538686355733,
-6.15331957385431));
#46626=CARTESIAN_POINT('Ctrl Pts',(1.11336305057389,-6.67478177303324,-6.144569595241));
#46627=CARTESIAN_POINT('Ctrl Pts',(1.29684337090052,-6.64417699581275,-6.13581970620102));
#46628=CARTESIAN_POINT('Ctrl Pts',(1.47906091205121,-6.60600253548075,-6.12706981716103));
#46629=CARTESIAN_POINT('Ctrl Pts',(1.65939671095154,-6.56038806441229,-6.11831992812105));
#46630=CARTESIAN_POINT('Ctrl Pts',(1.83973072369088,-6.5147740451387,-6.10957012574556));
#46631=CARTESIAN_POINT('Ctrl Pts',(2.01818275356959,-6.46172023288685,-6.10082032337007));
#46632=CARTESIAN_POINT('Ctrl Pts',(2.19414664033244,-6.40140683918136,-6.09207052099458));
#46633=CARTESIAN_POINT('Ctrl Pts',(2.37010884271175,-6.34109402281529,-6.08332080237505));
#46634=CARTESIAN_POINT('Ctrl Pts',(2.54358267847721,-6.27352185699826,-6.07457108375552));
#46635=CARTESIAN_POINT('Ctrl Pts',(2.71397890841655,-6.19891986435299,-6.06582136513599));
#46636=CARTESIAN_POINT('Ctrl Pts',(2.88437356388866,-6.12431856103279,-6.05707172736416));
#46637=CARTESIAN_POINT('Ctrl Pts',(3.05169040787107,-6.0426876758259,-6.04832208959234));
#46638=CARTESIAN_POINT('Ctrl Pts',(3.21536112511998,-5.95430447953975,-6.03957245182052));
#46639=CARTESIAN_POINT('Ctrl Pts',(3.37903038442792,-5.86592207055072,-6.03082289198845));
#46640=CARTESIAN_POINT('Ctrl Pts',(3.53905332979926,-5.77078760703406,-6.02207333215635));
#46641=CARTESIAN_POINT('Ctrl Pts',(3.69488643041849,-5.66922422085327,-6.01332377232428));
#46642=CARTESIAN_POINT('Ctrl Pts',(3.85071819468698,-5.56766170563189,-6.00457428752429));
#46643=CARTESIAN_POINT('Ctrl Pts',(4.00235994599179,-5.45967053456284,-5.9958248027243));
#46644=CARTESIAN_POINT('Ctrl Pts',(4.14929662974255,-5.3456175020672,-5.9870753179243));
#46645=CARTESIAN_POINT('Ctrl Pts',(4.29623210225003,-5.231565409745,-5.97832590524894));
#46646=CARTESIAN_POINT('Ctrl Pts',(4.43846235842079,-5.11145173172219,-5.96957649257358));
#46647=CARTESIAN_POINT('Ctrl Pts',(4.57550431797394,-4.98568443006593,-5.96082707989822));
#46648=CARTESIAN_POINT('Ctrl Pts',(4.71254519337467,-4.85991812336716,-5.95207773644033));
#46649=CARTESIAN_POINT('Ctrl Pts',(4.84439764314964,-4.72849847631122,-5.94332839298243));
#46650=CARTESIAN_POINT('Ctrl Pts',(4.97061384196672,-4.59187184425359,-5.93457904952453));
#46651=CARTESIAN_POINT('Ctrl Pts',(5.09682908420199,-4.45524624767756,-5.92582977237716));
#46652=CARTESIAN_POINT('Ctrl Pts',(5.21740796650169,-4.31341395556895,-5.9170804952298));
#46653=CARTESIAN_POINT('Ctrl Pts',(5.33194095942255,-4.16685668162851,-5.90833121808243));
#46654=CARTESIAN_POINT('Ctrl Pts',(5.44647312235137,-4.02030046975208,-5.89958200433889));
#46655=CARTESIAN_POINT('Ctrl Pts',(5.55495930712293,-3.86901957035539,-5.89083279059536));
#46656=CARTESIAN_POINT('Ctrl Pts',(5.65703106079801,-3.71352778058365,-5.88208357685183));
#46657=CARTESIAN_POINT('Ctrl Pts',(5.7591021086874,-3.55803706597597,-5.87333442360563));
#46658=CARTESIAN_POINT('Ctrl Pts',(5.85475865698551,-3.39833575880897,-5.86458527035943));
#46659=CARTESIAN_POINT('Ctrl Pts',(5.94367583069063,-3.23496624706721,-5.85583611711323));
#46660=CARTESIAN_POINT('Ctrl Pts',(6.03259241910076,-3.07159781070102,-5.84708702145811));
#46661=CARTESIAN_POINT('Ctrl Pts',(6.11476958470965,-2.90456146975838,-5.83833792580299));
#46662=CARTESIAN_POINT('Ctrl Pts',(6.18992823574383,-2.73442451648264,-5.82958883014787));
#46663=CARTESIAN_POINT('Ctrl Pts',(6.26508641700938,-2.5642886266241,-5.82083978917775));
#46664=CARTESIAN_POINT('Ctrl Pts',(6.33322605570304,-2.39105242531259,-5.81209074820762));
#46665=CARTESIAN_POINT('Ctrl Pts',(6.39411573747778,-2.21530425353698,-5.8033417072375));
#46666=CARTESIAN_POINT('Ctrl Pts',(6.45500505889137,-2.03955712188525,-5.7945927180465));
#46667=CARTESIAN_POINT('Ctrl Pts',(6.50864441544941,-1.8612983202553,-5.7858437288555));
#46668=CARTESIAN_POINT('Ctrl Pts',(6.55485164049919,-1.6811332401226,-5.7770947396645));
#46669=CARTESIAN_POINT('Ctrl Pts',(6.60199852639122,-1.49730435912843,-5.76816783278761));
#46670=CARTESIAN_POINT('Ctrl Pts',(6.64140767441022,-1.3114911317359,-5.75924092591072));
#46671=CARTESIAN_POINT('Ctrl Pts',(6.67293975269614,-1.12435050446364,-5.75031401903384));
#46672=CARTESIAN_POINT('Ctrl Pts',(6.70384664831516,-0.940920291563085,
-5.74156410484984));
#46673=CARTESIAN_POINT('Ctrl Pts',(6.72718585889673,-0.756215114277297,
-5.73281419066585));
#46674=CARTESIAN_POINT('Ctrl Pts',(6.7428781045187,-0.570862389374515,-5.72406427648186));
#46675=CARTESIAN_POINT('Ctrl Pts',(6.75857004154126,-0.385513309567596,
-5.71531453437128));
#46676=CARTESIAN_POINT('Ctrl Pts',(6.76661529035557,-0.199516993258827,
-5.7065647922607));
#46677=CARTESIAN_POINT('Ctrl Pts',(6.76698652348896,-0.0135052182047926,
-5.69781505015012));
#46678=CARTESIAN_POINT('Ctrl Pts',(6.76735774981523,0.172503146038172,-5.68906546847948));
#46679=CARTESIAN_POINT('Ctrl Pts',(6.76005524147483,0.358526681832767,-5.68031588680884));
#46680=CARTESIAN_POINT('Ctrl Pts',(6.74510380214887,0.543933542114178,-5.67156630513819));
#46681=CARTESIAN_POINT('Ctrl Pts',(6.73015261710987,0.729337249084028,-5.66281687227627));
#46682=CARTESIAN_POINT('Ctrl Pts',(6.70755278444615,0.914124015853962,-5.65406743941434));
#46683=CARTESIAN_POINT('Ctrl Pts',(6.67738106408301,1.09766621749315,-5.64531800655242));
#46684=CARTESIAN_POINT('Ctrl Pts',(6.64720981677268,1.28120554143251,-5.63656871087007));
#46685=CARTESIAN_POINT('Ctrl Pts',(6.60946696581539,1.46350005650549,-5.62781941518771));
#46686=CARTESIAN_POINT('Ctrl Pts',(6.56428070011012,1.64393062206462,-5.61907011950536));
#46687=CARTESIAN_POINT('Ctrl Pts',(6.51909508282762,1.82435859844577,-5.61032094937537));
#46688=CARTESIAN_POINT('Ctrl Pts',(6.46646633415686,2.00292240086485,-5.60157177924539));
#46689=CARTESIAN_POINT('Ctrl Pts',(6.4065731959722,2.17901557696373,-5.5928226091154));
#46690=CARTESIAN_POINT('Ctrl Pts',(6.34668083768323,2.3551064600736,-5.58407355291232));
#46691=CARTESIAN_POINT('Ctrl Pts',(6.27952437143912,2.52872650996464,-5.57532449670924));
#46692=CARTESIAN_POINT('Ctrl Pts',(6.20533187335162,2.69928607997866,-5.56657544050616));
#46693=CARTESIAN_POINT('Ctrl Pts',(6.12831449784278,2.87633970115342,-5.55749326421731));
#46694=CARTESIAN_POINT('Ctrl Pts',(6.04371489463178,3.05009490562299,-5.54841108792846));
#46695=CARTESIAN_POINT('Ctrl Pts',(5.95184265120515,3.21991584599586,-5.53932891163961));
#46696=CARTESIAN_POINT('Ctrl Pts',(5.86333281335517,3.38352155905257,-5.5305791312852));
#46697=CARTESIAN_POINT('Ctrl Pts',(5.7680733723571,3.54347560903783,-5.52182935093079));
#46698=CARTESIAN_POINT('Ctrl Pts',(5.66638790086381,3.69923467178608,-5.51307957057637));
#46699=CARTESIAN_POINT('Ctrl Pts',(5.56470608502773,3.8549881348972,-5.50433010478211));
#46700=CARTESIAN_POINT('Ctrl Pts',(5.45659885766987,4.00654667256213,-5.49558063898784));
#46701=CARTESIAN_POINT('Ctrl Pts',(5.34243340580548,4.15339551506159,-5.48683117319358));
#46702=CARTESIAN_POINT('Ctrl Pts',(5.22827145140633,4.30023985883823,-5.47808197543971));
#46703=CARTESIAN_POINT('Ctrl Pts',(5.10805181978127,4.44237456993,-5.46933277768583));
#46704=CARTESIAN_POINT('Ctrl Pts',(4.98218281282587,4.5793169162641,-5.46058357993196));
#46705=CARTESIAN_POINT('Ctrl Pts',(4.85631699296259,4.71625579512131,-5.45183460371396));
#46706=CARTESIAN_POINT('Ctrl Pts',(4.72480227791862,4.84800236135746,-5.44308562749596));
#46707=CARTESIAN_POINT('Ctrl Pts',(4.58808530848131,4.97410918678892,-5.43433665127795));
#46708=CARTESIAN_POINT('Ctrl Pts',(4.45135945056987,5.10022421088994,-5.42558710625675));
#46709=CARTESIAN_POINT('Ctrl Pts',(4.30943087208055,5.22069856611974,-5.41683756123554));
#46710=CARTESIAN_POINT('Ctrl Pts',(4.16278164322482,5.33512305301673,-5.40808801621434));
#46711=CARTESIAN_POINT('Ctrl Pts',(4.01614103534405,5.44954081331416,-5.39933898554708));
#46712=CARTESIAN_POINT('Ctrl Pts',(3.86478055833429,5.55790924068327,-5.39058995487984));
#46713=CARTESIAN_POINT('Ctrl Pts',(3.70921425811968,5.6598602975128,-5.38184092421258));
#46714=CARTESIAN_POINT('Ctrl Pts',(3.55364584530144,5.76181273884639,-5.37309177473274));
#46715=CARTESIAN_POINT('Ctrl Pts',(3.39387173464376,5.85734747818045,-5.36434262525288));
#46716=CARTESIAN_POINT('Ctrl Pts',(3.23043456092445,5.94614005448786,-5.35559347577304));
#46717=CARTESIAN_POINT('Ctrl Pts',(3.1869076880642,5.96978744811267,-5.35326338703999));
#46718=CARTESIAN_POINT('Ctrl Pts',(3.14312114982898,5.99295688499292,-5.35093329830695));
#46719=CARTESIAN_POINT('Ctrl Pts',(3.09908550384725,6.0156427786101,-5.3486032095739));
#46720=CARTESIAN_POINT('Origin',(0.,0.,-63.6971797838103));
#46721=CARTESIAN_POINT('',(3.09908550384716,6.01564277861015,-2.95434584629073));
#46722=CARTESIAN_POINT('',(3.09908550384726,6.0156427786101,-3.34860320957391));
#46723=CARTESIAN_POINT('',(3.09908550384721,6.01564277861012,-63.6971797838103));
#46724=CARTESIAN_POINT('',(-6.76699993702048,-0.000923236083376258,-4.30282021616649));
#46725=CARTESIAN_POINT('Ctrl Pts',(-6.76699993702048,-0.000923236083286258,
-4.30282021616649));
#46726=CARTESIAN_POINT('Ctrl Pts',(-6.7669744401561,-0.187806399292575,
-4.29407494551509));
#46727=CARTESIAN_POINT('Ctrl Pts',(-6.75920300097723,-0.374494000220519,
-4.2853296748637));
#46728=CARTESIAN_POINT('Ctrl Pts',(-6.74375962059959,-0.560352727815666,
-4.27658440421229));
#46729=CARTESIAN_POINT('Ctrl Pts',(-6.72828782458872,-0.746553433223164,
-4.26782304236859));
#46730=CARTESIAN_POINT('Ctrl Pts',(-6.70511590738353,-0.931921941745487,
-4.2590616805249));
#46731=CARTESIAN_POINT('Ctrl Pts',(-6.6743692209328,-1.11583354612812,-4.2503003186812));
#46732=CARTESIAN_POINT('Ctrl Pts',(-6.64228067589974,-1.30777149068659,
-4.24115659015217));
#46733=CARTESIAN_POINT('Ctrl Pts',(-6.60194150520994,-1.49812216265994,
-4.23201286162312));
#46734=CARTESIAN_POINT('Ctrl Pts',(-6.55355158142941,-1.68619413756071,
-4.22286913309409));
#46735=CARTESIAN_POINT('Ctrl Pts',(-6.50697258852339,-1.86722775985893,
-4.21406759688544));
#46736=CARTESIAN_POINT('Ctrl Pts',(-6.45293460916008,-2.04614991837855,
-4.20526606067679));
#46737=CARTESIAN_POINT('Ctrl Pts',(-6.39166523521518,-2.2223646237604,-4.19646452446813));
#46738=CARTESIAN_POINT('Ctrl Pts',(-6.33030499424766,-2.39884066861074,
-4.18764993492894));
#46739=CARTESIAN_POINT('Ctrl Pts',(-6.26169203660224,-2.57260098166927,
-4.17883534538975));
#46740=CARTESIAN_POINT('Ctrl Pts',(-6.18610139645694,-2.74307100031215,
-4.17002075585056));
#46741=CARTESIAN_POINT('Ctrl Pts',(-6.11035348030401,-2.9138957036607,-4.16118782642896));
#46742=CARTESIAN_POINT('Ctrl Pts',(-6.02759897279409,-3.08141617416001,
-4.15235489700738));
#46743=CARTESIAN_POINT('Ctrl Pts',(-5.93815896279803,-3.24508199165159,
-4.14352196758578));
#46744=CARTESIAN_POINT('Ctrl Pts',(-5.92821415851176,-3.26327993822358,
-4.14253983716812));
#46745=CARTESIAN_POINT('Ctrl Pts',(-5.91818674397737,-3.28143025942478,
-4.14155770675046));
#46746=CARTESIAN_POINT('Ctrl Pts',(-5.90807719298252,-3.29953222165807,
-4.14057557633281));
#46747=CARTESIAN_POINT('Ctrl Pts',(-5.82499975830413,-3.44828903447326,
-4.13250470595885));
#46748=CARTESIAN_POINT('Ctrl Pts',(-5.73614866817978,-3.59417773654744,
-4.12443383558491));
#46749=CARTESIAN_POINT('Ctrl Pts',(-5.64174723066037,-3.73670672990752,
-4.11636296521097));
#46750=CARTESIAN_POINT('Ctrl Pts',(-5.54746326837892,-3.87905835703406,
-4.10830213840673));
#46751=CARTESIAN_POINT('Ctrl Pts',(-5.44764290525162,-4.01805828733157,
-4.10024131160252));
#46752=CARTESIAN_POINT('Ctrl Pts',(-5.3425562510797,-4.15323749670655,-4.09218048479828));
#46753=CARTESIAN_POINT('Ctrl Pts',(-5.23757732516842,-4.28827812881672,
-4.08412792144917));
#46754=CARTESIAN_POINT('Ctrl Pts',(-5.12734307878022,-4.41950554250522,
-4.07607535810006));
#46755=CARTESIAN_POINT('Ctrl Pts',(-5.01216796210952,-4.54647790268499,
-4.06802279475095));
#46756=CARTESIAN_POINT('Ctrl Pts',(-4.89708569668207,-4.67334790098451,
-4.05997672317315));
#46757=CARTESIAN_POINT('Ctrl Pts',(-4.77707073828189,-4.79596939842845,
-4.05193065159535));
#46758=CARTESIAN_POINT('Ctrl Pts',(-4.65247895408675,-4.91393208965894,
-4.04388458001755));
#46759=CARTESIAN_POINT('Ctrl Pts',(-4.52796035958034,-5.03182548536798,
-4.03584323499117));
#46760=CARTESIAN_POINT('Ctrl Pts',(-4.39887056169622,-5.14506526717237,
-4.02780188996477));
#46761=CARTESIAN_POINT('Ctrl Pts',(-4.26560349006025,-5.25327667894866,
-4.01976054493839));
#46762=CARTESIAN_POINT('Ctrl Pts',(-4.12976744452351,-5.36357406957334,
-4.01156418783554));
#46763=CARTESIAN_POINT('Ctrl Pts',(-3.989591700041,-5.46864695758852,-4.00336783073271));
#46764=CARTESIAN_POINT('Ctrl Pts',(-3.84553058218129,-5.56814004327373,
-3.99517147362985));
#46765=CARTESIAN_POINT('Ctrl Pts',(-3.70423892045861,-5.6657204564708,-3.98713268473011));
#46766=CARTESIAN_POINT('Ctrl Pts',(-3.55921024720981,-5.75793345376984,
-3.97909389583036));
#46767=CARTESIAN_POINT('Ctrl Pts',(-3.41090384310648,-5.84448663041344,
-3.97105510693062));
#46768=CARTESIAN_POINT('Ctrl Pts',(-3.26258156887137,-5.9310490690328,-3.96301545780748));
#46769=CARTESIAN_POINT('Ctrl Pts',(-3.11098118792053,-6.01195029270372,
-3.95497580868433));
#46770=CARTESIAN_POINT('Ctrl Pts',(-2.95658775176706,-6.08694322842763,
-3.94693615956119));
#46771=CARTESIAN_POINT('Ctrl Pts',(-2.8021472236272,-6.16195903796274,-3.93889405824153));
#46772=CARTESIAN_POINT('Ctrl Pts',(-2.64491228029246,-6.23106280938724,
-3.93085195692187));
#46773=CARTESIAN_POINT('Ctrl Pts',(-2.48538902667397,-6.29405516230106,
-3.92280985560221));
#46774=CARTESIAN_POINT('Ctrl Pts',(-2.32048250087141,-6.3591732553409,-3.91449636550785));
#46775=CARTESIAN_POINT('Ctrl Pts',(-2.15313092619656,-6.41776008038371,
-3.90618287541348));
#46776=CARTESIAN_POINT('Ctrl Pts',(-1.98391054883965,-6.46965129927439,
-3.89786938531912));
#46777=CARTESIAN_POINT('Ctrl Pts',(-1.81992589778733,-6.51993698918583,
-3.88981311695804));
#46778=CARTESIAN_POINT('Ctrl Pts',(-1.65418673905913,-6.56393520726695,
-3.88175684859694));
#46779=CARTESIAN_POINT('Ctrl Pts',(-1.48722743952302,-6.60154857159514,
-3.87370058023586));
#46780=CARTESIAN_POINT('Ctrl Pts',(-1.31227208800184,-6.64096332355095,
-3.86525847927485));
#46781=CARTESIAN_POINT('Ctrl Pts',(-1.13597732951258,-6.67336652512646,
-3.85681637831386));
#46782=CARTESIAN_POINT('Ctrl Pts',(-0.958962872365025,-6.69870727897745,
-3.84837427735285));
#46783=CARTESIAN_POINT('Ctrl Pts',(-0.781948415217469,-6.72404803282843,
-3.83993217639185));
#46784=CARTESIAN_POINT('Ctrl Pts',(-0.604214726714419,-6.74232637782005,
-3.83149007543084));
#46785=CARTESIAN_POINT('Ctrl Pts',(-0.426379507918857,-6.75355384336476,
-3.82304797446984));
#46786=CARTESIAN_POINT('Ctrl Pts',(-0.250824807746037,-6.76463733043077,
-3.81471413310211));
#46787=CARTESIAN_POINT('Ctrl Pts',(-0.0746130893532963,-6.76888553519746,
-3.8063802917344));
#46788=CARTESIAN_POINT('Ctrl Pts',(0.101689154437278,-6.76623590453879,
-3.79804645036667));
#46789=CARTESIAN_POINT('Ctrl Pts',(0.277783603723323,-6.76358939680515,
-3.7897224314856));
#46790=CARTESIAN_POINT('Ctrl Pts',(0.453968021015937,-6.75406125446949,
-3.78139841260451));
#46791=CARTESIAN_POINT('Ctrl Pts',(0.629671634160306,-6.73764073197242,
-3.77307439372344));
#46792=CARTESIAN_POINT('Ctrl Pts',(0.805200373409075,-6.72123655245594,
-3.7647586595531));
#46793=CARTESIAN_POINT('Ctrl Pts',(0.980248917723264,-6.69795369201965,
-3.75644292538275));
#46794=CARTESIAN_POINT('Ctrl Pts',(1.1542471095858,-6.66783342698457,-3.7481271912124));
#46795=CARTESIAN_POINT('Ctrl Pts',(1.32810400592666,-6.63773762116092,-3.73981820984785));
#46796=CARTESIAN_POINT('Ctrl Pts',(1.50091190811382,-6.6008155333522,-3.73150922848331));
#46797=CARTESIAN_POINT('Ctrl Pts',(1.67210616528295,-6.55716020637156,-3.72320024711875));
#46798=CARTESIAN_POINT('Ctrl Pts',(1.8431927539021,-6.51353233536891,-3.7148964914901));
#46799=CARTESIAN_POINT('Ctrl Pts',(2.01266738391637,-6.46317975023025,-3.70659273586143));
#46800=CARTESIAN_POINT('Ctrl Pts',(2.17997575605842,-6.40624653779399,-3.69828898023278));
#46801=CARTESIAN_POINT('Ctrl Pts',(2.34721620534498,-6.3493364387639,-3.68998859571334));
#46802=CARTESIAN_POINT('Ctrl Pts',(2.51229182036566,-6.28585114760582,-3.68168821119389));
#46803=CARTESIAN_POINT('Ctrl Pts',(2.674663342484,-6.21598463675485,-3.67338782667445));
#46804=CARTESIAN_POINT('Ctrl Pts',(2.83700062487769,-6.14613285884512,-3.66508919247967));
#46805=CARTESIAN_POINT('Ctrl Pts',(2.9966346310973,-6.06990267944113,-3.65679055828492));
#46806=CARTESIAN_POINT('Ctrl Pts',(3.15304574806969,-5.98753634732848,-3.64849192409014));
#46807=CARTESIAN_POINT('Ctrl Pts',(3.30944984469072,-5.90517371214353,-3.64019366237099));
#46808=CARTESIAN_POINT('Ctrl Pts',(3.46263103270155,-5.81667563527687,-3.63189540065179));
#46809=CARTESIAN_POINT('Ctrl Pts',(3.61209381974494,-5.72233057742738,-3.62359713893263));
#46810=CARTESIAN_POINT('Ctrl Pts',(3.76157470635164,-5.62797409463139,-3.61529787231509));
#46811=CARTESIAN_POINT('Ctrl Pts',(3.90733600098045,-5.5277694061083,-3.60699860569756));
#46812=CARTESIAN_POINT('Ctrl Pts',(4.04891058620135,-5.42204869629061,-3.59869933908002));
#46813=CARTESIAN_POINT('Ctrl Pts',(4.19058458010979,-5.31625375311391,-3.59039424500976));
#46814=CARTESIAN_POINT('Ctrl Pts',(4.32806571145238,-5.20493525774109,-3.58208915093949));
#46815=CARTESIAN_POINT('Ctrl Pts',(4.46091869638858,-5.0884667026729,-3.57378405686923));
#46816=CARTESIAN_POINT('Ctrl Pts',(4.59382012668081,-4.97195567689455,-3.56547593431421));
#46817=CARTESIAN_POINT('Ctrl Pts',(4.72208979020483,-4.8502910831247,-3.5571678117592));
#46818=CARTESIAN_POINT('Ctrl Pts',(4.84532863005262,-4.72388393875129,-3.54885968920418));
#46819=CARTESIAN_POINT('Ctrl Pts',(4.96869847261396,-4.59734242376107,-3.54054273512656));
#46820=CARTESIAN_POINT('Ctrl Pts',(5.08702656919703,-4.46604854002439,-3.53222578104894));
#46821=CARTESIAN_POINT('Ctrl Pts',(5.19995286785108,-4.33044791818668,-3.52390882697133));
#46822=CARTESIAN_POINT('Ctrl Pts',(5.28317805141306,-4.23051205932944,-3.51777934218314));
#46823=CARTESIAN_POINT('Ctrl Pts',(5.36347007604982,-4.1282377104919,-3.51164985739497));
#46824=CARTESIAN_POINT('Ctrl Pts',(5.44069978791588,-4.02381346706979,-3.50552037260679));
#46825=CARTESIAN_POINT('Ctrl Pts',(5.54718029662547,-3.8798384826689,-3.49706934200465));
#46826=CARTESIAN_POINT('Ctrl Pts',(5.64803248650558,-3.7315124930526,-3.48861831140253));
#46827=CARTESIAN_POINT('Ctrl Pts',(5.74289848198448,-3.57930244958712,-3.4801672808004));
#46828=CARTESIAN_POINT('Ctrl Pts',(5.83768095012316,-3.42722642358515,-3.47172369113752));
#46829=CARTESIAN_POINT('Ctrl Pts',(5.92648755485924,-3.27127344009668,-3.46328010147462));
#46830=CARTESIAN_POINT('Ctrl Pts',(6.00900272415619,-3.11194075475154,-3.45483651181173));
#46831=CARTESIAN_POINT('Ctrl Pts',(6.09145645761784,-2.95272669894683,-3.44639920873819));
#46832=CARTESIAN_POINT('Ctrl Pts',(6.16762794147849,-2.79013825084872,-3.43796190566463));
#46833=CARTESIAN_POINT('Ctrl Pts',(6.23724651100191,-2.62469902293472,-3.42952460259108));
#46834=CARTESIAN_POINT('Ctrl Pts',(6.30681541179301,-2.45937782612629,-3.42109331903432));
#46835=CARTESIAN_POINT('Ctrl Pts',(6.3698405952902,-2.29121021117695,-3.41266203547756));
#46836=CARTESIAN_POINT('Ctrl Pts',(6.4260985991014,-2.12074180291404,-3.4042307519208));
#46837=CARTESIAN_POINT('Ctrl Pts',(6.4823324880812,-1.95034646544364,-3.39580308240947));
#46838=CARTESIAN_POINT('Ctrl Pts',(6.53180487642007,-1.77765261495826,-3.38737541289814));
#46839=CARTESIAN_POINT('Ctrl Pts',(6.57434122516572,-1.60322376949896,-3.3789477433868));
#46840=CARTESIAN_POINT('Ctrl Pts',(6.61686447872655,-1.42884862347647,-3.37052266840681));
#46841=CARTESIAN_POINT('Ctrl Pts',(6.65245587262219,-1.25273986934714,-3.36209759342683));
#46842=CARTESIAN_POINT('Ctrl Pts',(6.68099123182748,-1.0754743884651,-3.35367251844684));
#46843=CARTESIAN_POINT('Ctrl Pts',(6.68879923455886,-1.02697002764914,-3.35136720285636));
#46844=CARTESIAN_POINT('Ctrl Pts',(6.69607923934458,-0.978379126285159,
-3.34906188726589));
#46845=CARTESIAN_POINT('Ctrl Pts',(6.70282936956514,-0.92971363467198,-3.34675657167541));
#46846=CARTESIAN_POINT('Ctrl Pts',(6.72806635269987,-0.747766005373889,
-3.3381375956296));
#46847=CARTESIAN_POINT('Ctrl Pts',(6.74588142968121,-0.564856441547501,
-3.32951861958377));
#46848=CARTESIAN_POINT('Ctrl Pts',(6.75623197145129,-0.381599984197407,
-3.32089964353796));
#46849=CARTESIAN_POINT('Ctrl Pts',(6.766588713977,-0.198233742399754,-3.31227550407507));
#46850=CARTESIAN_POINT('Ctrl Pts',(6.76947197975218,-0.0145204960127364,
-3.3036513646122));
#46851=CARTESIAN_POINT('Ctrl Pts',(6.76489126357795,0.168923627615384,-3.2950272251493));
#46852=CARTESIAN_POINT('Ctrl Pts',(6.76015364638722,0.358651172519226,-3.28610768728216));
#46853=CARTESIAN_POINT('Ctrl Pts',(6.74743169061268,0.548090474372401,-3.27718814941503));
#46854=CARTESIAN_POINT('Ctrl Pts',(6.72679424816834,0.73656509746889,-3.26826861154789));
#46855=CARTESIAN_POINT('Ctrl Pts',(6.70680310738943,0.919137271018851,-3.25962840636424));
#46856=CARTESIAN_POINT('Ctrl Pts',(6.67938484532721,1.10080397853448,-3.25098820118059));
#46857=CARTESIAN_POINT('Ctrl Pts',(6.64465432640456,1.28095975057503,-3.24234799599694));
#46858=CARTESIAN_POINT('Ctrl Pts',(6.60823958201906,1.46985201570466,-3.23328879178807));
#46859=CARTESIAN_POINT('Ctrl Pts',(6.5637858348098,1.6570827815149,-3.22422958757919));
#46860=CARTESIAN_POINT('Ctrl Pts',(6.51148478162744,1.84197039569973,-3.21517038337031));
#46861=CARTESIAN_POINT('Ctrl Pts',(6.45918372844511,2.02685800988449,-3.20611117916144));
#46862=CARTESIAN_POINT('Ctrl Pts',(6.39903552049933,2.20940211939612,-3.19705197495256));
#46863=CARTESIAN_POINT('Ctrl Pts',(6.33129056347372,2.38894303005924,-3.18799277074368));
#46864=CARTESIAN_POINT('Ctrl Pts',(6.26366301495595,2.56817277910472,-3.17894926700456));
#46865=CARTESIAN_POINT('Ctrl Pts',(6.18840351584211,2.74457514840907,-3.16990576326542));
#46866=CARTESIAN_POINT('Ctrl Pts',(6.10576186767639,2.91752652348337,-3.16086225952629));
#46867=CARTESIAN_POINT('Ctrl Pts',(6.0231958127705,3.09031969795877,-3.15182702798336));
#46868=CARTESIAN_POINT('Ctrl Pts',(5.93326119283621,3.25966796585851,-3.14279179644043));
#46869=CARTESIAN_POINT('Ctrl Pts',(5.836255254385,3.42496913937389,-3.1337565648975));
#46870=CARTESIAN_POINT('Ctrl Pts',(5.73942022348833,3.589979081035,-3.12473725185763));
#46871=CARTESIAN_POINT('Ctrl Pts',(5.63553887235576,3.7509559615117,-3.11571793881776));
#46872=CARTESIAN_POINT('Ctrl Pts',(5.52495344003932,3.90732369856885,-3.10669862577788));
#46873=CARTESIAN_POINT('Ctrl Pts',(5.41450674835925,4.06349525644675,-3.09769062838062));
#46874=CARTESIAN_POINT('Ctrl Pts',(5.29737289792351,4.21506901725398,-3.08868263098338));
#46875=CARTESIAN_POINT('Ctrl Pts',(5.17393772677935,4.3614971511408,-3.07967463358612));
#46876=CARTESIAN_POINT('Ctrl Pts',(5.05078134635042,4.50759456239973,-3.07068698165454));
#46877=CARTESIAN_POINT('Ctrl Pts',(4.92135220708575,4.64856936344266,-3.06169932972296));
#46878=CARTESIAN_POINT('Ctrl Pts',(4.78607643669927,4.78390649386796,-3.05271167779137));
#46879=CARTESIAN_POINT('Ctrl Pts',(4.66826140793107,4.90177496261819,-3.044884108465));
#46880=CARTESIAN_POINT('Ctrl Pts',(4.54601235635552,5.01536756173044,-3.03705653913864));
#46881=CARTESIAN_POINT('Ctrl Pts',(4.4196362004456,5.12436384888025,-3.02922896981227));
#46882=CARTESIAN_POINT('Ctrl Pts',(4.28848975550654,5.23747439151649,-3.02110593519172));
#46883=CARTESIAN_POINT('Ctrl Pts',(4.15295629101846,5.34558325009788,-3.01298290057119));
#46884=CARTESIAN_POINT('Ctrl Pts',(4.01346298745678,5.44833954965313,-3.00485986595064));
#46885=CARTESIAN_POINT('Ctrl Pts',(3.86888714423837,5.55483984948749,-2.99644086267399));
#46886=CARTESIAN_POINT('Ctrl Pts',(3.72005776986405,5.65558990884324,-2.98802185939734));
#46887=CARTESIAN_POINT('Ctrl Pts',(3.56748588484631,5.75024638267112,-2.97960285612069));
#46888=CARTESIAN_POINT('Ctrl Pts',(3.41491399982863,5.84490285649897,-2.97118385284403));
#46889=CARTESIAN_POINT('Ctrl Pts',(3.2585999821917,5.93346552412804,-2.96276484956737));
#46890=CARTESIAN_POINT('Ctrl Pts',(3.09908550384716,6.01564277861015,-2.95434584629072));
#46891=CARTESIAN_POINT('Ctrl Pts',(3.09908550384723,6.01564277861011,-4.95428495819038));
#46892=CARTESIAN_POINT('Ctrl Pts',(2.93974516298852,6.09773032248641,-4.94586184187556));
#46893=CARTESIAN_POINT('Ctrl Pts',(2.77713547189578,6.17348621254161,-4.93743872556074));
#46894=CARTESIAN_POINT('Ctrl Pts',(2.61179029507344,6.24266292975684,-4.92901560924592));
#46895=CARTESIAN_POINT('Ctrl Pts',(2.44642807142854,6.31184677898067,-4.92059162452131));
#46896=CARTESIAN_POINT('Ctrl Pts',(2.27833010742088,6.3744499742426,-4.9121676397967));
#46897=CARTESIAN_POINT('Ctrl Pts',(2.10805000452703,6.43027325845594,-4.9037436550721));
#46898=CARTESIAN_POINT('Ctrl Pts',(1.93772859501676,6.48611008430421,-4.89531762685386));
#46899=CARTESIAN_POINT('Ctrl Pts',(1.76522430811125,6.53516361624418,-4.88689159863562));
#46900=CARTESIAN_POINT('Ctrl Pts',(1.59110600155887,6.57728444662411,-4.87846557041738));
#46901=CARTESIAN_POINT('Ctrl Pts',(1.41402158440019,6.62012280662058,-4.86989600455419));
#46902=CARTESIAN_POINT('Ctrl Pts',(1.23526800822187,6.65579004345812,-4.86132643869098));
#46903=CARTESIAN_POINT('Ctrl Pts',(1.05545426470397,6.68418321824875,-4.85275687282779));
#46904=CARTESIAN_POINT('Ctrl Pts',(0.878421895293671,6.71213720502377,-4.84431986173009));
#46905=CARTESIAN_POINT('Ctrl Pts',(0.700362257308595,6.73304053449834,-4.8358828506324));
#46906=CARTESIAN_POINT('Ctrl Pts',(0.521861552053374,6.74684737640392,-4.8274458395347));
#46907=CARTESIAN_POINT('Ctrl Pts',(0.339154181869231,6.76097959941957,-4.81880999628876));
#46908=CARTESIAN_POINT('Ctrl Pts',(0.155985072554053,6.76767670853061,-4.81017415304279));
#46909=CARTESIAN_POINT('Ctrl Pts',(-0.0270172230871244,6.76694606670222,
-4.80153830979685));
#46910=CARTESIAN_POINT('Ctrl Pts',(-0.210019518728302,6.76621542487383,
-4.7929024665509));
#46911=CARTESIAN_POINT('Ctrl Pts',(-0.392854630975622,6.75805708424938,
-4.78426662330496));
#46912=CARTESIAN_POINT('Ctrl Pts',(-0.574899632783152,6.74253508794918,
-4.77563078005902));
#46913=CARTESIAN_POINT('Ctrl Pts',(-0.748616549970566,6.72772318254615,
-4.7673900041459));
#46914=CARTESIAN_POINT('Ctrl Pts',(-0.922000515700265,6.70617298925634,
-4.75914922823277));
#46915=CARTESIAN_POINT('Ctrl Pts',(-1.09449074839643,6.67790229051568,-4.75090845231965));
#46916=CARTESIAN_POINT('Ctrl Pts',(-1.26678992941556,6.64966290464603,-4.74267680396137));
#46917=CARTESIAN_POINT('Ctrl Pts',(-1.43819700046978,6.61471789211129,-4.7344451556031));
#46918=CARTESIAN_POINT('Ctrl Pts',(-1.60815413919947,6.5731369424785,-4.72621350724482));
#46919=CARTESIAN_POINT('Ctrl Pts',(-1.77795331987167,6.53159463815406,-4.71798950937533));
#46920=CARTESIAN_POINT('Ctrl Pts',(-1.94630490837617,6.48342876343106,-4.70976551150581));
#46921=CARTESIAN_POINT('Ctrl Pts',(-2.11265905095506,6.42876043529526,-4.70154151363632));
#46922=CARTESIAN_POINT('Ctrl Pts',(-2.27886621890777,6.37414040687095,-4.69332478170559));
#46923=CARTESIAN_POINT('Ctrl Pts',(-2.4430791215607,6.31302948597131,-4.68510804977489));
#46924=CARTESIAN_POINT('Ctrl Pts',(-2.60476102407502,6.24559917121325,-4.67689131784416));
#46925=CARTESIAN_POINT('Ctrl Pts',(-2.76636009090852,6.17820340352536,-4.66867879565226));
#46926=CARTESIAN_POINT('Ctrl Pts',(-2.92543041260506,6.10449482673665,-4.66046627346035));
#46927=CARTESIAN_POINT('Ctrl Pts',(-3.08145287446718,6.02469394927559,-4.65225375126845));
#46928=CARTESIAN_POINT('Ctrl Pts',(-3.23742316157219,5.9449197576606,-4.6440439753885));
#46929=CARTESIAN_POINT('Ctrl Pts',(-3.39034730284099,5.85905748574763,-4.63583419950854));
#46930=CARTESIAN_POINT('Ctrl Pts',(-3.53972845950541,5.7673747435872,-4.62762442362858));
#46931=CARTESIAN_POINT('Ctrl Pts',(-3.60497423177531,5.72733012584791,-4.62403860879483));
#46932=CARTESIAN_POINT('Ctrl Pts',(-3.66954441310266,5.68617572491462,-4.62045279396108));
#46933=CARTESIAN_POINT('Ctrl Pts',(-3.73339914491863,5.64393655392412,-4.61686697912732));
#46934=CARTESIAN_POINT('Ctrl Pts',(-3.89115157019759,5.53958513820244,-4.60800826230965));
#46935=CARTESIAN_POINT('Ctrl Pts',(-4.04437207474734,5.4287183903029,-4.599149545492));
#46936=CARTESIAN_POINT('Ctrl Pts',(-4.19255894052685,5.31175475057051,-4.59029082867433));
#46937=CARTESIAN_POINT('Ctrl Pts',(-4.3410230397332,5.19457229096844,-4.58141553864413));
#46938=CARTESIAN_POINT('Ctrl Pts',(-4.4844344771304,5.07127030552435,-4.57254024861391));
#46939=CARTESIAN_POINT('Ctrl Pts',(-4.62232657832742,4.94230573753668,-4.56366495858371));
#46940=CARTESIAN_POINT('Ctrl Pts',(-4.76061032371742,4.81297488153313,-4.55476446075864));
#46941=CARTESIAN_POINT('Ctrl Pts',(-4.89334317243053,4.67794943720698,-4.54586396293358));
#46942=CARTESIAN_POINT('Ctrl Pts',(-5.02009503618959,4.53772352921866,-4.53696346510851));
#46943=CARTESIAN_POINT('Ctrl Pts',(-5.14701848396949,4.3973077973934,-4.52805091867792));
#46944=CARTESIAN_POINT('Ctrl Pts',(-5.26794460461904,4.25167773611181,-4.51913837224735));
#46945=CARTESIAN_POINT('Ctrl Pts',(-5.38248444255352,4.10135955820376,-4.51022582581677));
#46946=CARTESIAN_POINT('Ctrl Pts',(-5.49727719558463,3.9507094631464,-4.50129359961728));
#46947=CARTESIAN_POINT('Ctrl Pts',(-5.60565530267525,3.79535075324253,-4.49236137341778));
#46948=CARTESIAN_POINT('Ctrl Pts',(-5.7072722874395,3.63583993556167,-4.48342914721828));
#46949=CARTESIAN_POINT('Ctrl Pts',(-5.80331212307908,3.48508371357432,-4.47498715754416));
#46950=CARTESIAN_POINT('Ctrl Pts',(-5.89331291743969,3.33061903030178,-4.46654516787004));
#46951=CARTESIAN_POINT('Ctrl Pts',(-5.97702046976212,3.17293480929638,-4.45810317819592));
#46952=CARTESIAN_POINT('Ctrl Pts',(-6.06103424403036,3.01467374226404,-4.44963030573483));
#46953=CARTESIAN_POINT('Ctrl Pts',(-6.13886019197762,2.85288229057625,-4.44115743327376));
#46954=CARTESIAN_POINT('Ctrl Pts',(-6.2101993575957,2.68806862615483,-4.43268456081268));
#46955=CARTESIAN_POINT('Ctrl Pts',(-6.28144175108267,2.52347853274668,-4.42422318186877));
#46956=CARTESIAN_POINT('Ctrl Pts',(-6.34621476874222,2.355874695178,-4.41576180292485));
#46957=CARTESIAN_POINT('Ctrl Pts',(-6.40426491590136,2.18579044900352,-4.40730042398094));
#46958=CARTESIAN_POINT('Ctrl Pts',(-6.46399800312121,2.0107752662924,-4.39859373999837));
#46959=CARTESIAN_POINT('Ctrl Pts',(-6.51661233897661,1.83313396935372,-4.38988705601582));
#46960=CARTESIAN_POINT('Ctrl Pts',(-6.56188355911143,1.65347305894686,-4.38118037203324));
#46961=CARTESIAN_POINT('Ctrl Pts',(-6.60576150047129,1.47934143916692,-4.37274164720787));
#46962=CARTESIAN_POINT('Ctrl Pts',(-6.64274148190805,1.30331301880828,-4.3643029223825));
#46963=CARTESIAN_POINT('Ctrl Pts',(-6.67266859811752,1.1259586047881,-4.35586419755713));
#46964=CARTESIAN_POINT('Ctrl Pts',(-6.70402115093086,0.940156752269966,
-4.34702353399594));
#46965=CARTESIAN_POINT('Ctrl Pts',(-6.72763241147778,0.752899831740139,
-4.33818287043475));
#46966=CARTESIAN_POINT('Ctrl Pts',(-6.74338357278951,0.564860151039709,
-4.32934220687356));
#46967=CARTESIAN_POINT('Ctrl Pts',(-6.75913473410124,0.376820470339342,
-4.32050154331238));
#46968=CARTESIAN_POINT('Ctrl Pts',(-6.76702571198923,0.187998438435085,
-4.31166087975119));
#46969=CARTESIAN_POINT('Ctrl Pts',(-6.76699993702055,-0.000923235581007906,
-4.30282021619));
#46970=CARTESIAN_POINT('',(-6.767,-8.1208758347662E-10,-4.69717978377183));
#46971=CARTESIAN_POINT('Ctrl Pts',(3.09908550384725,6.0156427786101,-5.3486032095739));
#46972=CARTESIAN_POINT('Ctrl Pts',(2.93373232018335,6.10082796552477,-5.33985376167461));
#46973=CARTESIAN_POINT('Ctrl Pts',(2.76486502144435,6.17919158180187,-5.33110431377533));
#46974=CARTESIAN_POINT('Ctrl Pts',(2.59305716434362,6.25046746591375,-5.32235486587604));
#46975=CARTESIAN_POINT('Ctrl Pts',(2.42125069459295,6.3217427744722,-5.31360548862862));
#46976=CARTESIAN_POINT('Ctrl Pts',(2.24650397871072,6.38593035557821,-5.30485611138121));
#46977=CARTESIAN_POINT('Ctrl Pts',(2.06941053323786,6.44281220003534,-5.29610673413379));
#46978=CARTESIAN_POINT('Ctrl Pts',(1.89231845896701,6.4996936040668,-5.2873574246312));
#46979=CARTESIAN_POINT('Ctrl Pts',(1.71287996431525,6.54926929700875,-5.2786081151286));
#46980=CARTESIAN_POINT('Ctrl Pts',(1.53170449173527,6.59137090065473,-5.269858805626));
#46981=CARTESIAN_POINT('Ctrl Pts',(1.35053036178197,6.63347219230078,-5.26110956096141));
#46982=CARTESIAN_POINT('Ctrl Pts',(1.16761955878874,6.66809944062449,-5.25236031629683));
#46983=CARTESIAN_POINT('Ctrl Pts',(0.983593309310811,6.69513503985387,-5.24361107163224));
#46984=CARTESIAN_POINT('Ctrl Pts',(0.799568362460158,6.72217044771213,-5.23486188889906));
#46985=CARTESIAN_POINT('Ctrl Pts',(0.614428268438623,6.74161427235977,-5.22611270616587));
#46986=CARTESIAN_POINT('Ctrl Pts',(0.428801816330147,6.75340047696803,-5.21736352343269));
#46987=CARTESIAN_POINT('Ctrl Pts',(0.243176616522549,6.76518660206243,-5.20861439972455));
#46988=CARTESIAN_POINT('Ctrl Pts',(0.0570653511651141,6.76931519233997,
-5.19986527601641));
#46989=CARTESIAN_POINT('Ctrl Pts',(-0.128899900800489,6.76577222610794,
-5.19111615230827));
#46990=CARTESIAN_POINT('Ctrl Pts',(-0.314863959942398,6.76222928260131,
-5.18236708471901));
#46991=CARTESIAN_POINT('Ctrl Pts',(-0.500681721080975,6.75101488651274,
-5.17361801712975));
#46992=CARTESIAN_POINT('Ctrl Pts',(-0.68572211017351,6.73216712415989,-5.1648689495405));
#46993=CARTESIAN_POINT('Ctrl Pts',(-0.870761373827884,6.71331947644142,
-5.15611993516413));
#46994=CARTESIAN_POINT('Ctrl Pts',(-1.05502298984376,6.68683858439991,-5.14737092078777));
#46995=CARTESIAN_POINT('Ctrl Pts',(-1.23788117676098,6.65281438131419,-5.13862190641141));
#46996=CARTESIAN_POINT('Ctrl Pts',(-1.43009641451832,6.61704912302369,-5.12942519552388));
#46997=CARTESIAN_POINT('Ctrl Pts',(-1.62076048992735,6.57294837083155,-5.12022848463636));
#46998=CARTESIAN_POINT('Ctrl Pts',(-1.80915798961171,6.52067760042038,-5.11103177374883));
#46999=CARTESIAN_POINT('Ctrl Pts',(-1.98840443003051,6.47094578577397,-5.10228177604233));
#47000=CARTESIAN_POINT('Ctrl Pts',(-2.1655989595223,6.41381888474463,-5.09353177833581));
#47001=CARTESIAN_POINT('Ctrl Pts',(-2.3401396624236,6.3494909528522,-5.08478178062931));
#47002=CARTESIAN_POINT('Ctrl Pts',(-2.51467682554049,6.28516432556671,-5.07603196037771));
#47003=CARTESIAN_POINT('Ctrl Pts',(-2.68656000078874,6.21363705879647,-5.06728214012612));
#47004=CARTESIAN_POINT('Ctrl Pts',(-2.85520533840917,6.13515211510846,-5.05853231987452));
#47005=CARTESIAN_POINT('Ctrl Pts',(-3.02384747998354,6.05666865881108,-5.04978266544328));
#47006=CARTESIAN_POINT('Ctrl Pts',(-3.18925164684563,5.9712279103983,-5.04103301101203));
#47007=CARTESIAN_POINT('Ctrl Pts',(-3.35085601829182,5.87912008251894,-5.03228335658078));
#47008=CARTESIAN_POINT('Ctrl Pts',(-3.51245754191444,5.78701387778158,-5.02353385633764));
#47009=CARTESIAN_POINT('Ctrl Pts',(-3.67025915510964,5.68824097060965,-5.0147843560945));
#47010=CARTESIAN_POINT('Ctrl Pts',(-3.82372487928863,5.58313684656835,-5.00603485585136));
#47011=CARTESIAN_POINT('Ctrl Pts',(-3.97718810300823,5.47803443501755,-4.99728549816624));
#47012=CARTESIAN_POINT('Ctrl Pts',(-4.12631534263046,5.3666011749636,-4.98853614048114));
#47013=CARTESIAN_POINT('Ctrl Pts',(-4.27060009886242,5.24921554097337,-4.97978678279602));
#47014=CARTESIAN_POINT('Ctrl Pts',(-4.41488269594247,5.13183166360263,-4.97103755604083));
#47015=CARTESIAN_POINT('Ctrl Pts',(-4.55432273235138,5.00849577139426,-4.96228832928563));
#47016=CARTESIAN_POINT('Ctrl Pts',(-4.68844662480271,4.87962675277281,-4.95353910253044));
#47017=CARTESIAN_POINT('Ctrl Pts',(-4.82256868835227,4.75075949139812,-4.94478999507895));
#47018=CARTESIAN_POINT('Ctrl Pts',(-4.95137454637936,4.61635945312446,-4.93604088762745));
#47019=CARTESIAN_POINT('Ctrl Pts',(-5.07442674461156,4.47688309134502,-4.92729178017596));
#47020=CARTESIAN_POINT('Ctrl Pts',(-5.19747742838615,4.3374084461626,-4.91854278040358));
#47021=CARTESIAN_POINT('Ctrl Pts',(-5.31477440451002,4.19285781735935,-4.9097937806312));
#47022=CARTESIAN_POINT('Ctrl Pts',(-5.42591931531225,4.04372211999309,-4.90104478085883));
#47023=CARTESIAN_POINT('Ctrl Pts',(-5.53707636463048,3.89457013500706,-4.89229482557825));
#47024=CARTESIAN_POINT('Ctrl Pts',(-5.64207983273532,3.74083230916327,-4.88354487029767));
#47025=CARTESIAN_POINT('Ctrl Pts',(-5.74057303468804,3.58303087251736,-4.8747949150171));
#47026=CARTESIAN_POINT('Ctrl Pts',(-5.83906243363822,3.42523552887333,-4.86604529758829));
#47027=CARTESIAN_POINT('Ctrl Pts',(-5.93104191768483,3.26337713156889,-4.85729568015948));
#47028=CARTESIAN_POINT('Ctrl Pts',(-6.01619906699712,3.09800545291046,-4.84854606273067));
#47029=CARTESIAN_POINT('Ctrl Pts',(-6.10135338095431,2.93263928039494,-4.83979673662528));
#47030=CARTESIAN_POINT('Ctrl Pts',(-6.1796856835288,2.76376031540131,-4.83104741051991));
#47031=CARTESIAN_POINT('Ctrl Pts',(-6.25092992694921,2.59194213831458,-4.82229808441453));
#47032=CARTESIAN_POINT('Ctrl Pts',(-6.32217217691145,2.42012876880713,-4.81354900312072));
#47033=CARTESIAN_POINT('Ctrl Pts',(-6.38632665483897,2.24537661647539,-4.80479992182691));
#47034=CARTESIAN_POINT('Ctrl Pts',(-6.443175478694,2.068279176213,-4.79605084053311));
#47035=CARTESIAN_POINT('Ctrl Pts',(-6.50002944235977,1.8911657242328,-4.78730096821815));
#47036=CARTESIAN_POINT('Ctrl Pts',(-6.54957634250432,1.71170683289068,-4.77855109590318));
#47037=CARTESIAN_POINT('Ctrl Pts',(-6.59164787708422,1.53051209225249,-4.76980122358822));
#47038=CARTESIAN_POINT('Ctrl Pts',(-6.63371649075029,1.34932993147929,-4.76105195875344));
#47039=CARTESIAN_POINT('Ctrl Pts',(-6.66831071257138,1.16641244173919,-4.75230269391867));
#47040=CARTESIAN_POINT('Ctrl Pts',(-6.69531304840343,0.982380875159316,
-4.74355342908389));
#47041=CARTESIAN_POINT('Ctrl Pts',(-6.72231677033051,0.798339861795239,
-4.73480371512824));
#47042=CARTESIAN_POINT('Ctrl Pts',(-6.74172778477894,0.61318494072964,-4.72605400117257));
#47043=CARTESIAN_POINT('Ctrl Pts',(-6.75348015835521,0.427545027690135,
-4.71730428721692));
#47044=CARTESIAN_POINT('Ctrl Pts',(-6.76249038365219,0.285219953547058,
-4.71059611941464));
#47045=CARTESIAN_POINT('Ctrl Pts',(-6.76699999999997,0.142609995758198,
-4.70388795161237));
#47046=CARTESIAN_POINT('Ctrl Pts',(-6.767,1.46790887861953E-12,-4.6971797838101));
#47047=CARTESIAN_POINT('Ctrl Pts',(-6.767,-8.12088412195109E-10,-4.69717978377182));
#47048=CARTESIAN_POINT('Ctrl Pts',(-6.76699999997768,-0.186007250372196,
-4.68843027195908));
#47049=CARTESIAN_POINT('Ctrl Pts',(-6.75932637289781,-0.372014356627555,
-4.67968076014633));
#47050=CARTESIAN_POINT('Ctrl Pts',(-6.7440051825667,-0.557389538396189,
-4.67093124833359));
#47051=CARTESIAN_POINT('Ctrl Pts',(-6.72868405694809,-0.742763937190855,
-4.66218177347638));
#47052=CARTESIAN_POINT('Ctrl Pts',(-6.70571545632424,-0.927506131210442,
-4.6534322986192));
#47053=CARTESIAN_POINT('Ctrl Pts',(-6.67517739388229,-1.11098864089732,
-4.644682823762));
#47054=CARTESIAN_POINT('Ctrl Pts',(-6.64463945788839,-1.29447039084364,
-4.63593338513348));
#47055=CARTESIAN_POINT('Ctrl Pts',(-6.60653216984984,-1.47669218418644,
-4.62718394650495));
#47056=CARTESIAN_POINT('Ctrl Pts',(-6.56098496065573,-1.65703510706604,
-4.61843450787644));
#47057=CARTESIAN_POINT('Ctrl Pts',(-6.51543793627481,-1.83737729818289,
-4.60968510474981));
#47058=CARTESIAN_POINT('Ctrl Pts',(-6.46245112132675,-2.01584035622603,
-4.60093570162319));
#47059=CARTESIAN_POINT('Ctrl Pts',(-6.40220448335379,-2.19181813874342,
-4.59218629849656));
#47060=CARTESIAN_POINT('Ctrl Pts',(-6.34195808483518,-2.36779522182518,
-4.58343693014502));
#47061=CARTESIAN_POINT('Ctrl Pts',(-6.27445201385812,-2.54128677801154,
-4.57468756179349));
#47062=CARTESIAN_POINT('Ctrl Pts',(-6.19991555020131,-2.71170355503178,
-4.56593819344195));
#47063=CARTESIAN_POINT('Ctrl Pts',(-6.1253793766047,-2.8821196688716,-4.55718885913876));
#47064=CARTESIAN_POINT('Ctrl Pts',(-6.04381297991678,-3.04946076492552,
-4.54843952483557));
#47065=CARTESIAN_POINT('Ctrl Pts',(-5.95549339270228,-3.21315848496141,
-4.53969019053238));
#47066=CARTESIAN_POINT('Ctrl Pts',(-5.86717414185079,-3.3768555815585,-4.53094088955082));
#47067=CARTESIAN_POINT('Ctrl Pts',(-5.77210188801403,-3.53690907769625,
-4.52219158856927));
#47068=CARTESIAN_POINT('Ctrl Pts',(-5.67059953266826,-3.69277537092395,
-4.51344228758771));
#47069=CARTESIAN_POINT('Ctrl Pts',(-5.56909755546278,-3.84864108348211,
-4.5046930192011));
#47070=CARTESIAN_POINT('Ctrl Pts',(-5.46116568106704,-4.00031938420715,
-4.49594375081448));
#47071=CARTESIAN_POINT('Ctrl Pts',(-5.34717048438338,-4.1472951198268,-4.48719448242787));
#47072=CARTESIAN_POINT('Ctrl Pts',(-5.23317570291497,-4.29427032010314,
-4.47844524590952));
#47073=CARTESIAN_POINT('Ctrl Pts',(-5.11311781898027,-4.43654276311237,
-4.46969600939117));
#47074=CARTESIAN_POINT('Ctrl Pts',(-4.98740458874075,-4.57362924472543,
-4.46094677287282));
#47075=CARTESIAN_POINT('Ctrl Pts',(-4.8616918059593,-4.71071523839898,-4.45219756749611));
#47076=CARTESIAN_POINT('Ctrl Pts',(-4.73032391083184,-4.84261509641523,
-4.4434483621194));
#47077=CARTESIAN_POINT('Ctrl Pts',(-4.5937470688743,-4.96888084654973,-4.4346991567427));
#47078=CARTESIAN_POINT('Ctrl Pts',(-4.45717070170109,-5.09514615774453,
-4.425949981781));
#47079=CARTESIAN_POINT('Ctrl Pts',(-4.3153856343453,-5.21577720572568,-4.4172008068193));
#47080=CARTESIAN_POINT('Ctrl Pts',(-4.16887340887849,-5.33036429343679,
-4.4084516318576));
#47081=CARTESIAN_POINT('Ctrl Pts',(-4.02236168056949,-5.44495099232119,
-4.39970248658434));
#47082=CARTESIAN_POINT('Ctrl Pts',(-3.8711230519634,-5.5534935954452,-4.3909533413111));
#47083=CARTESIAN_POINT('Ctrl Pts',(-3.71567116860927,-5.65562346401932,
-4.38220419603785));
#47084=CARTESIAN_POINT('Ctrl Pts',(-3.56021979984027,-5.75775299451768,
-4.37345507972648));
#47085=CARTESIAN_POINT('Ctrl Pts',(-3.40055544371662,-5.8534696756079,-4.36470596341512));
#47086=CARTESIAN_POINT('Ctrl Pts',(-3.23722035815365,-5.94244843080321,
-4.35595684710376));
#47087=CARTESIAN_POINT('Ctrl Pts',(-3.07388579970981,-6.03142689884403,
-4.34720775902776));
#47088=CARTESIAN_POINT('Ctrl Pts',(-2.90688078715767,-6.11366734742827,
-4.33845867095178));
#47089=CARTESIAN_POINT('Ctrl Pts',(-2.73677250536075,-6.18889047034292,
-4.32970958287579));
#47090=CARTESIAN_POINT('Ctrl Pts',(-2.56666475841723,-6.26411335674151,
-4.32096052230863));
#47091=CARTESIAN_POINT('Ctrl Pts',(-2.39345402381071,-6.3323188457399,-4.31221146174146));
#47092=CARTESIAN_POINT('Ctrl Pts',(-2.21772855867322,-6.39327529831504,
-4.30346240117429));
#47093=CARTESIAN_POINT('Ctrl Pts',(-2.04200363146135,-6.45423156429208,
-4.2947133673895));
#47094=CARTESIAN_POINT('Ctrl Pts',(-1.86376425982952,-6.50793874434814,
-4.28596433360469));
#47095=CARTESIAN_POINT('Ctrl Pts',(-1.6836157754307,-6.55421443963507,-4.27721529981989));
#47096=CARTESIAN_POINT('Ctrl Pts',(-1.50346782754062,-6.60048999710617,
-4.26846629209101));
#47097=CARTESIAN_POINT('Ctrl Pts',(-1.32141105577788,-6.63933404281004,
-4.25971728436212));
#47098=CARTESIAN_POINT('Ctrl Pts',(-1.13806375266581,-6.6706146564517,-4.25096827663324));
#47099=CARTESIAN_POINT('Ctrl Pts',(-0.954716980367006,-6.70189517953209,
-4.24221929423382));
#47100=CARTESIAN_POINT('Ctrl Pts',(-0.770079966636729,-6.72561226618227,
-4.2334703118344));
#47101=CARTESIAN_POINT('Ctrl Pts',(-0.58477976326588,-6.74168537002986,
-4.22472132943498));
#47102=CARTESIAN_POINT('Ctrl Pts',(-0.391489586792104,-6.75845153122487,
-4.21559509901976));
#47103=CARTESIAN_POINT('Ctrl Pts',(-0.197478091011775,-6.76689985148686,
-4.20646886860455));
#47104=CARTESIAN_POINT('Ctrl Pts',(-0.00346214674593483,-6.76699911434455,
-4.19734263818933));
#47105=CARTESIAN_POINT('Ctrl Pts',(0.184490799261612,-6.76709527523794,
-4.18850160247459));
#47106=CARTESIAN_POINT('Ctrl Pts',(0.372447602922716,-6.75935633786509,
-4.17966056675984));
#47107=CARTESIAN_POINT('Ctrl Pts',(0.559756448952297,-6.74380914008221,
-4.17081953104509));
#47108=CARTESIAN_POINT('Ctrl Pts',(0.745136131799664,-6.72842206864779,
-4.16206955243179));
#47109=CARTESIAN_POINT('Ctrl Pts',(0.929880852698716,-6.70538686345272,
-4.15331957381849));
#47110=CARTESIAN_POINT('Ctrl Pts',(1.11336305132482,-6.67478177290799,-4.14456959520518));
#47111=CARTESIAN_POINT('Ctrl Pts',(1.29684337164803,-6.64417699566684,-4.1358197061652));
#47112=CARTESIAN_POINT('Ctrl Pts',(1.47906091279446,-6.60600253531434,-4.12706981712522));
#47113=CARTESIAN_POINT('Ctrl Pts',(1.65939671168969,-6.56038806422558,-4.11831992808523));
#47114=CARTESIAN_POINT('Ctrl Pts',(1.83973072442393,-6.51477404493169,-4.10957012570974));
#47115=CARTESIAN_POINT('Ctrl Pts',(2.0181827542967,-6.46172023265975,-4.10082032333425));
#47116=CARTESIAN_POINT('Ctrl Pts',(2.1941466410528,-6.40140683893445,-4.09207052095876));
#47117=CARTESIAN_POINT('Ctrl Pts',(2.37010884342536,-6.34109402254856,-4.08332080233923));
#47118=CARTESIAN_POINT('Ctrl Pts',(2.54358267918324,-6.27352185671201,-4.07457108371969));
#47119=CARTESIAN_POINT('Ctrl Pts',(2.71397890911422,-6.19891986404754,-4.06582136510015));
#47120=CARTESIAN_POINT('Ctrl Pts',(2.88437356457784,-6.12431856070821,-4.05707172732833));
#47121=CARTESIAN_POINT('Ctrl Pts',(3.05169040855098,-6.04268767548253,-4.0483220895565));
#47122=CARTESIAN_POINT('Ctrl Pts',(3.21536112578986,-5.95430447917801,-4.03957245178468));
#47123=CARTESIAN_POINT('Ctrl Pts',(3.37903038508777,-5.86592207017061,-4.03082289195261));
#47124=CARTESIAN_POINT('Ctrl Pts',(3.53905333044834,-5.770787606636,-4.02207333212056));
#47125=CARTESIAN_POINT('Ctrl Pts',(3.69488643105606,-5.66922422043773,-4.01332377228849));
#47126=CARTESIAN_POINT('Ctrl Pts',(3.85071819531322,-5.56766170519877,-4.00457428748849));
#47127=CARTESIAN_POINT('Ctrl Pts',(4.00235994660596,-5.45967053411261,-3.99582480268849));
#47128=CARTESIAN_POINT('Ctrl Pts',(4.14929663034396,-5.34561750160038,-3.98707531788849));
#47129=CARTESIAN_POINT('Ctrl Pts',(4.29623210283858,-5.23156540926167,-3.97832590521313));
#47130=CARTESIAN_POINT('Ctrl Pts',(4.43846235899581,-5.11145173122288,-3.96957649253777));
#47131=CARTESIAN_POINT('Ctrl Pts',(4.57550431853479,-4.98568442955122,-3.96082707986241));
#47132=CARTESIAN_POINT('Ctrl Pts',(4.7125451939213,-4.8599181228371,-3.95207773640452));
#47133=CARTESIAN_POINT('Ctrl Pts',(4.84439764368142,-4.72849847576639,-3.94332839294662));
#47134=CARTESIAN_POINT('Ctrl Pts',(4.97061384248308,-4.59187184369464,-3.93457904948873));
#47135=CARTESIAN_POINT('Ctrl Pts',(5.09682908470292,-4.45524624710449,-3.92582977234136));
#47136=CARTESIAN_POINT('Ctrl Pts',(5.21740796698661,-4.31341395498239,-3.91708049519402));
#47137=CARTESIAN_POINT('Ctrl Pts',(5.33194095989094,-4.16685668102916,-3.90833121804665));
#47138=CARTESIAN_POINT('Ctrl Pts',(5.44647312280323,-4.02030046913993,-3.89958200430312));
#47139=CARTESIAN_POINT('Ctrl Pts',(5.55495930755774,-3.86901956973112,-3.89083279055957));
#47140=CARTESIAN_POINT('Ctrl Pts',(5.65703106121529,-3.71352777994799,-3.88208357681604));
#47141=CARTESIAN_POINT('Ctrl Pts',(5.75910210908722,-3.55803706532881,-3.87333442356984));
#47142=CARTESIAN_POINT('Ctrl Pts',(5.8547586573674,-3.39833575815103,-3.86458527032366));
#47143=CARTESIAN_POINT('Ctrl Pts',(5.94367583105418,-3.23496624639925,-3.85583611707746));
#47144=CARTESIAN_POINT('Ctrl Pts',(6.03259241944603,-3.07159781002292,-3.84708702142233));
#47145=CARTESIAN_POINT('Ctrl Pts',(6.11476958503622,-2.9045614690709,-3.8383379257672));
#47146=CARTESIAN_POINT('Ctrl Pts',(6.18992823605133,-2.73442451578656,-3.82958883011207));
#47147=CARTESIAN_POINT('Ctrl Pts',(6.26508641729767,-2.56428862591972,-3.82083978914196));
#47148=CARTESIAN_POINT('Ctrl Pts',(6.33322605597181,-2.39105242460069,-3.81209074817183));
#47149=CARTESIAN_POINT('Ctrl Pts',(6.39411573772674,-2.21530425281839,-3.80334170720171));
#47150=CARTESIAN_POINT('Ctrl Pts',(6.4550050591206,-2.03955712115978,-3.79459271801071));
#47151=CARTESIAN_POINT('Ctrl Pts',(6.50864441565861,-1.86129831952377,-3.78584372881972));
#47152=CARTESIAN_POINT('Ctrl Pts',(6.55485164068815,-1.68113323938585,-3.77709473962872));
#47153=CARTESIAN_POINT('Ctrl Pts',(6.60199852655558,-1.49730435840175,-3.76816783275258));
#47154=CARTESIAN_POINT('Ctrl Pts',(6.64140767455104,-1.31149113102048,-3.75924092587644));
#47155=CARTESIAN_POINT('Ctrl Pts',(6.6729397528146,-1.12435050376054,-3.7503140190003));
#47156=CARTESIAN_POINT('Ctrl Pts',(6.70384664841429,-0.940920290856767,
-3.74156410481631));
#47157=CARTESIAN_POINT('Ctrl Pts',(6.7271858589764,-0.756215113568551,-3.73281419063232));
#47158=CARTESIAN_POINT('Ctrl Pts',(6.74287810457884,-0.570862388664146,
-3.72406427644832));
#47159=CARTESIAN_POINT('Ctrl Pts',(6.75857004158188,-0.38551330885554,-3.71531453433774));
#47160=CARTESIAN_POINT('Ctrl Pts',(6.76661529037659,-0.199516992545889,
-3.70656479222716));
#47161=CARTESIAN_POINT('Ctrl Pts',(6.76698652349039,-0.0135052174917819,
-3.69781505011657));
#47162=CARTESIAN_POINT('Ctrl Pts',(6.76735774979706,0.172503146751192,-3.68906546844593));
#47163=CARTESIAN_POINT('Ctrl Pts',(6.76005524143706,0.358526682544987,-3.68031588677528));
#47164=CARTESIAN_POINT('Ctrl Pts',(6.74510380209157,0.543933542824793,-3.67156630510464));
#47165=CARTESIAN_POINT('Ctrl Pts',(6.73015261703303,0.729337249793037,-3.66281687224272));
#47166=CARTESIAN_POINT('Ctrl Pts',(6.70755278434985,0.914124016560562,-3.6540674393808));
#47167=CARTESIAN_POINT('Ctrl Pts',(6.67738106396738,1.09766621819654,-3.64531800651888));
#47168=CARTESIAN_POINT('Ctrl Pts',(6.64720981663772,1.28120554213269,-3.63656871083653));
#47169=CARTESIAN_POINT('Ctrl Pts',(6.60946696566123,1.46350005720166,-3.62781941515418));
#47170=CARTESIAN_POINT('Ctrl Pts',(6.56428069993697,1.64393062275601,-3.61907011947183));
#47171=CARTESIAN_POINT('Ctrl Pts',(6.51909508263546,1.82435859913243,-3.61032094934184));
#47172=CARTESIAN_POINT('Ctrl Pts',(6.46646633394588,2.002922401546,-3.60157177921185));
#47173=CARTESIAN_POINT('Ctrl Pts',(6.40657319574266,2.1790155776386,-3.59282260908186));
#47174=CARTESIAN_POINT('Ctrl Pts',(6.34668083743517,2.35510646074208,-3.58407355287879));
#47175=CARTESIAN_POINT('Ctrl Pts',(6.27952437117281,2.52872651062595,-3.57532449667571));
#47176=CARTESIAN_POINT('Ctrl Pts',(6.20533187306738,2.69928608063207,-3.56657544047263));
#47177=CARTESIAN_POINT('Ctrl Pts',(6.12831449755176,2.87633970177148,-3.55749326418519));
#47178=CARTESIAN_POINT('Ctrl Pts',(6.04371489433665,3.0500949062059,-3.54841108789775));
#47179=CARTESIAN_POINT('Ctrl Pts',(5.95184265090852,3.21991584654418,-3.5393289116103));
#47180=CARTESIAN_POINT('Ctrl Pts',(5.86333281304345,3.38352155959277,-3.53057913125588));
#47181=CARTESIAN_POINT('Ctrl Pts',(5.76807337203062,3.54347560956928,-3.52182935090146));
#47182=CARTESIAN_POINT('Ctrl Pts',(5.66638790052296,3.69923467230818,-3.51307957054704));
#47183=CARTESIAN_POINT('Ctrl Pts',(5.56470608467248,3.85498813541002,-3.50433010475277));
#47184=CARTESIAN_POINT('Ctrl Pts',(5.45659885730059,4.00654667306507,-3.4955806389585));
#47185=CARTESIAN_POINT('Ctrl Pts',(5.3424334054226,4.15339551555407,-3.48683117316423));
#47186=CARTESIAN_POINT('Ctrl Pts',(5.22827145100989,4.30023985932022,-3.47808197541036));
#47187=CARTESIAN_POINT('Ctrl Pts',(5.10805181937171,4.44237457040093,-3.46933277765649));
#47188=CARTESIAN_POINT('Ctrl Pts',(4.98218281240366,4.57931691672346,-3.46058357990262));
#47189=CARTESIAN_POINT('Ctrl Pts',(4.85631699252778,4.71625579556903,-3.45183460368461));
#47190=CARTESIAN_POINT('Ctrl Pts',(4.72480227747168,4.84800236179304,-3.4430856274666));
#47191=CARTESIAN_POINT('Ctrl Pts',(4.58808530802277,4.97410918721188,-3.43433665124859));
#47192=CARTESIAN_POINT('Ctrl Pts',(4.45135945009968,5.10022421130032,-3.42558710622739));
#47193=CARTESIAN_POINT('Ctrl Pts',(4.30943087159923,5.22069856651705,-3.4168375612062));
#47194=CARTESIAN_POINT('Ctrl Pts',(4.16278164273292,5.33512305340054,-3.408088016185));
#47195=CARTESIAN_POINT('Ctrl Pts',(4.01614103484162,5.44954081368443,-3.39933898551774));
#47196=CARTESIAN_POINT('Ctrl Pts',(3.86478055782189,5.55790924103957,-3.39058995485048));
#47197=CARTESIAN_POINT('Ctrl Pts',(3.70921425759791,5.65986029785475,-3.38184092418322));
#47198=CARTESIAN_POINT('Ctrl Pts',(3.55364584477024,5.76181273917401,-3.37309177470338));
#47199=CARTESIAN_POINT('Ctrl Pts',(3.39387173410373,5.85734747849335,-3.36434262522353));
#47200=CARTESIAN_POINT('Ctrl Pts',(3.2304345603762,5.94614005478571,-3.35559347574369));
#47201=CARTESIAN_POINT('Ctrl Pts',(3.18690768769653,5.96978744830722,-3.35326338702042));
#47202=CARTESIAN_POINT('Ctrl Pts',(3.1431211496441,5.99295688508816,-3.35093329829716));
#47203=CARTESIAN_POINT('Ctrl Pts',(3.09908550384726,6.0156427786101,-3.34860320957389));
#47204=CARTESIAN_POINT('Origin',(0.,0.,-63.6971797838103));
#47205=CARTESIAN_POINT('',(3.0990855038472,6.01564277861013,-0.95422544671683));
#47206=CARTESIAN_POINT('',(3.09908550384728,6.01564277861008,-1.34871979865156));
#47207=CARTESIAN_POINT('',(3.09908550384721,6.01564277861012,-63.6971797838103));
#47208=CARTESIAN_POINT('',(-6.76699839382599,-0.00466239815280736,-2.30282021621694));
#47209=CARTESIAN_POINT('Ctrl Pts',(-6.76699839382559,-0.0046623987238019,
-2.30282021619001));
#47210=CARTESIAN_POINT('Ctrl Pts',(-6.76683414407748,-0.243054232521557,
-2.29158517435079));
#47211=CARTESIAN_POINT('Ctrl Pts',(-6.75406843836986,-0.481031945011058,
-2.28035013251158));
#47212=CARTESIAN_POINT('Ctrl Pts',(-6.72885664862788,-0.7174797573565,-2.26911509067237));
#47213=CARTESIAN_POINT('Ctrl Pts',(-6.70364485888591,-0.953927569701941,
-2.25788004883316));
#47214=CARTESIAN_POINT('Ctrl Pts',(-6.66598706078046,-1.18884602160625,
-2.24664500699395));
#47215=CARTESIAN_POINT('Ctrl Pts',(-6.61609060837904,-1.42113829788612,
-2.23540996515474));
#47216=CARTESIAN_POINT('Ctrl Pts',(-6.57956666468819,-1.59117503617786,
-2.22718597295188));
#47217=CARTESIAN_POINT('Ctrl Pts',(-6.53643504805841,-1.760028269909,-2.21896198074902));
#47218=CARTESIAN_POINT('Ctrl Pts',(-6.4867860993046,-1.92714688123885,-2.21073798854616));
#47219=CARTESIAN_POINT('Ctrl Pts',(-6.43718958452491,-2.09408899954798,
-2.20252268165498));
#47220=CARTESIAN_POINT('Ctrl Pts',(-6.38108954510199,-2.25929980253373,
-2.19430737476378));
#47221=CARTESIAN_POINT('Ctrl Pts',(-6.31862738505078,-2.42223800830686,
-2.18609206787259));
#47222=CARTESIAN_POINT('Ctrl Pts',(-6.25621866251127,-2.58503681748739,
-2.17788378932557));
#47223=CARTESIAN_POINT('Ctrl Pts',(-6.18745878708354,-2.74556656867843,
-2.16967551077858));
#47224=CARTESIAN_POINT('Ctrl Pts',(-6.1125390750994,-2.9033007173531,-2.16146723223156));
#47225=CARTESIAN_POINT('Ctrl Pts',(-6.03766843545712,-3.06093155030669,
-2.15326433009937));
#47226=CARTESIAN_POINT('Ctrl Pts',(-5.95664614923389,-3.2157701053826,-2.14506142796716));
#47227=CARTESIAN_POINT('Ctrl Pts',(-5.86971181647224,-3.36730934004676,
-2.13685852583498));
#47228=CARTESIAN_POINT('Ctrl Pts',(-5.78281699718807,-3.5187796969506,-2.12865935209385));
#47229=CARTESIAN_POINT('Ctrl Pts',(-5.69001566293867,-3.66695341065426,
-2.12046017835272));
#47230=CARTESIAN_POINT('Ctrl Pts',(-5.59159360718813,-3.81134752181599,
-2.11226100461159));
#47231=CARTESIAN_POINT('Ctrl Pts',(-5.49318011331474,-3.95572907192489,
-2.10406254412846));
#47232=CARTESIAN_POINT('Ctrl Pts',(-5.38914706663194,-4.09633137351286,
-2.09586408364533));
#47233=CARTESIAN_POINT('Ctrl Pts',(-5.27982409132891,-4.23269967805688,
-2.0876656231622));
#47234=CARTESIAN_POINT('Ctrl Pts',(-5.17050220583707,-4.36906662318216,
-2.0794672444073));
#47235=CARTESIAN_POINT('Ctrl Pts',(-5.05589072029722,-4.50119937480523,
-2.07126886565242));
#47236=CARTESIAN_POINT('Ctrl Pts',(-4.93636004923348,-4.62867567067856,
-2.06307048689752));
#47237=CARTESIAN_POINT('Ctrl Pts',(-4.81680885640397,-4.75617385247173,
-2.0548707005942));
#47238=CARTESIAN_POINT('Ctrl Pts',(-4.69233704080369,-4.87901372411103,
-2.04667091429086));
#47239=CARTESIAN_POINT('Ctrl Pts',(-4.56335245713835,-4.99680931714723,
-2.03847112798753));
#47240=CARTESIAN_POINT('Ctrl Pts',(-4.43432229767364,-5.11464653243132,
-2.03026844434714));
#47241=CARTESIAN_POINT('Ctrl Pts',(-4.30077645846428,-5.227435676881,-2.02206576070675));
#47242=CARTESIAN_POINT('Ctrl Pts',(-4.16315652102638,-5.33483052977651,
-2.01386307706635));
#47243=CARTESIAN_POINT('Ctrl Pts',(-4.02538028656725,-5.44234735261269,
-2.00565107751547));
#47244=CARTESIAN_POINT('Ctrl Pts',(-3.88352099307658,-5.54445742369008,
-1.9974390779646));
#47245=CARTESIAN_POINT('Ctrl Pts',(-3.73805076719158,-5.64085680210892,
-1.98922707841372));
#47246=CARTESIAN_POINT('Ctrl Pts',(-3.5924947433204,-5.73731303664719,-1.98101023544543));
#47247=CARTESIAN_POINT('Ctrl Pts',(-3.44332384770358,-5.82805167849745,
-1.97279339247713));
#47248=CARTESIAN_POINT('Ctrl Pts',(-3.29103543832631,-5.91281445199157,
-1.96457654950884));
#47249=CARTESIAN_POINT('Ctrl Pts',(-3.13851218547216,-5.99770793789197,
-1.95634703537287));
#47250=CARTESIAN_POINT('Ctrl Pts',(-2.98286213142457,-6.07660697774788,
-1.94811752123689));
#47251=CARTESIAN_POINT('Ctrl Pts',(-2.82460447394779,-6.14930065664008,
-1.93988800710091));
#47252=CARTESIAN_POINT('Ctrl Pts',(-2.6835446421044,-6.21409472906666,-1.93255279249783));
#47253=CARTESIAN_POINT('Ctrl Pts',(-2.54041358176544,-6.27395945691981,
-1.92521757789475));
#47254=CARTESIAN_POINT('Ctrl Pts',(-2.39558868938805,-6.32877901583521,
-1.91788236329167));
#47255=CARTESIAN_POINT('Ctrl Pts',(-2.23623556789188,-6.38909784424109,
-1.90981131055579));
#47256=CARTESIAN_POINT('Ctrl Pts',(-2.07431185801297,-6.44350422937888,
-1.9017402578199));
#47257=CARTESIAN_POINT('Ctrl Pts',(-1.91030498556335,-6.49176585083996,
-1.89366920508402));
#47258=CARTESIAN_POINT('Ctrl Pts',(-1.74650219917809,-6.53996741674216,
-1.88560819576501));
#47259=CARTESIAN_POINT('Ctrl Pts',(-1.58062176144763,-6.58203932943863,
-1.87754718644599));
#47260=CARTESIAN_POINT('Ctrl Pts',(-1.41317236866547,-6.61779667687369,
-1.86948617712698));
#47261=CARTESIAN_POINT('Ctrl Pts',(-1.24589462961894,-6.65351736916082,
-1.86143343121424));
#47262=CARTESIAN_POINT('Ctrl Pts',(-1.07705149789421,-6.68293630070154,
-1.85338068530152));
#47263=CARTESIAN_POINT('Ctrl Pts',(-0.907168085471193,-6.70591791365675,
-1.84532793938877));
#47264=CARTESIAN_POINT('Ctrl Pts',(-0.737421626671457,-6.7288809996992,
-1.83728168529718));
#47265=CARTESIAN_POINT('Ctrl Pts',(-0.566636924103956,-6.74541704638878,
-1.82923543120557));
#47266=CARTESIAN_POINT('Ctrl Pts',(-0.395350473852723,-6.7554412885336,
-1.82118917711398));
#47267=CARTESIAN_POINT('Ctrl Pts',(-0.224164644211534,-6.76545964203189,
-1.81314764971848));
#47268=CARTESIAN_POINT('Ctrl Pts',(-0.0524780250569159,-6.76897378436333,
-1.80510612232298));
#47269=CARTESIAN_POINT('Ctrl Pts',(0.119166657993148,-6.76595065808366,
-1.79706459492748));
#47270=CARTESIAN_POINT('Ctrl Pts',(0.294113713877558,-6.76286936810255,
-1.78886835186502));
#47271=CARTESIAN_POINT('Ctrl Pts',(0.469016810825393,-6.75299664798575,
-1.78067210880258));
#47272=CARTESIAN_POINT('Ctrl Pts',(0.64329960582345,-6.73635321350858,-1.77247586574013));
#47273=CARTESIAN_POINT('Ctrl Pts',(0.814238192715004,-6.72002913992128,
-1.76443689547384));
#47274=CARTESIAN_POINT('Ctrl Pts',(0.984579684449283,-6.69719189655806,
-1.75639792520754));
#47275=CARTESIAN_POINT('Ctrl Pts',(1.1537843844718,-6.6679135112979,-1.74835895494125));
#47276=CARTESIAN_POINT('Ctrl Pts',(1.32300718046266,-6.63863199479651,-1.74031912492963));
#47277=CARTESIAN_POINT('Ctrl Pts',(1.49109257463482,-6.60290802834851,-1.73227929491801));
#47278=CARTESIAN_POINT('Ctrl Pts',(1.65751034340853,-6.56086491718079,-1.72423946490639));
#47279=CARTESIAN_POINT('Ctrl Pts',(1.82397885896552,-6.51880898555126,-1.71619718326046));
#47280=CARTESIAN_POINT('Ctrl Pts',(1.98877837504448,-6.47043016506247,-1.7081549016145));
#47281=CARTESIAN_POINT('Ctrl Pts',(2.151393270295,-6.41590180695819,-1.70011261996857));
#47282=CARTESIAN_POINT('Ctrl Pts',(2.31948522096978,-6.35953687146615,-1.69179946509024));
#47283=CARTESIAN_POINT('Ctrl Pts',(2.4852424055632,-6.29660105568209,-1.68348631021192));
#47284=CARTESIAN_POINT('Ctrl Pts',(2.64811820204749,-6.22733963968441,-1.67517315533359));
#47285=CARTESIAN_POINT('Ctrl Pts',(2.80596442074268,-6.16021700481359,-1.66711670930971));
#47286=CARTESIAN_POINT('Ctrl Pts',(2.96110425850402,-6.08715385393473,-1.65906026328583));
#47287=CARTESIAN_POINT('Ctrl Pts',(3.1130661472397,-6.0084197725284,-1.65100381726195));
#47288=CARTESIAN_POINT('Ctrl Pts',(3.27229115713246,-5.9259225424984,-1.64256230795639));
#47289=CARTESIAN_POINT('Ctrl Pts',(3.42802655569584,-5.83719922644851,-1.63412079865084));
#47290=CARTESIAN_POINT('Ctrl Pts',(3.57976554674399,-5.74260982745169,-1.62567928934529));
#47291=CARTESIAN_POINT('Ctrl Pts',(3.73150453779209,-5.6480204284549,-1.61723778003973));
#47292=CARTESIAN_POINT('Ctrl Pts',(3.87924678897198,-5.54756527697109,-1.60879627073416));
#47293=CARTESIAN_POINT('Ctrl Pts',(4.02252722040997,-5.44165083049812,-1.6003547614286));
#47294=CARTESIAN_POINT('Ctrl Pts',(4.16397288302205,-5.33709266500959,-1.5920213493556));
#47295=CARTESIAN_POINT('Ctrl Pts',(4.30152031993196,-5.22688229002238,-1.58368793728259));
#47296=CARTESIAN_POINT('Ctrl Pts',(4.43469586182674,-5.1113365779507,-1.57535452520958));
#47297=CARTESIAN_POINT('Ctrl Pts',(4.56771445692495,-4.99592703599787,-1.56703093402644));
#47298=CARTESIAN_POINT('Ctrl Pts',(4.69637116022414,-4.87519490859631,-1.5587073428433));
#47299=CARTESIAN_POINT('Ctrl Pts',(4.82022238645935,-4.74949946258299,-1.55038375166016));
#47300=CARTESIAN_POINT('Ctrl Pts',(4.94395037254816,-4.6239290918365,-1.54206844299975));
#47301=CARTESIAN_POINT('Ctrl Pts',(5.06288216577888,-4.49340548852718,-1.53375313433935));
#47302=CARTESIAN_POINT('Ctrl Pts',(5.1766081478372,-4.35832732636565,-1.52543782567894));
#47303=CARTESIAN_POINT('Ctrl Pts',(5.2902418118422,-4.223358815075,-1.51712926704252));
#47304=CARTESIAN_POINT('Ctrl Pts',(5.39867786200226,-4.08384337692888,-1.50882070840609));
#47305=CARTESIAN_POINT('Ctrl Pts',(5.50154422585003,-3.9402157467601,-1.50051214976968));
#47306=CARTESIAN_POINT('Ctrl Pts',(5.60434593288425,-3.79667839396242,-1.49220881349076));
#47307=CARTESIAN_POINT('Ctrl Pts',(5.70158472839756,-3.64903428224829,-1.48390547721187));
#47308=CARTESIAN_POINT('Ctrl Pts',(5.7929293278183,-3.49775053468693,-1.47560214093295));
#47309=CARTESIAN_POINT('Ctrl Pts',(5.88423691686185,-3.34652808323496,-1.46730216894277));
#47310=CARTESIAN_POINT('Ctrl Pts',(5.96965488888101,-3.19166923166052,-1.45900219695258));
#47311=CARTESIAN_POINT('Ctrl Pts',(6.04889558886728,-3.03366958566387,-1.45070222496241));
#47312=CARTESIAN_POINT('Ctrl Pts',(6.12811962113046,-2.87570317377984,-1.44240399881288));
#47313=CARTESIAN_POINT('Ctrl Pts',(6.20116881411983,-2.71459759438054,-1.43410577266335));
#47314=CARTESIAN_POINT('Ctrl Pts',(6.26780162997457,-2.55087273835607,-1.42580754651382));
#47315=CARTESIAN_POINT('Ctrl Pts',(6.3344314952917,-2.38715513215795,-1.4175096878143));
#47316=CARTESIAN_POINT('Ctrl Pts',(6.39464541870508,-2.22081880267863,-1.40921182911477));
#47317=CARTESIAN_POINT('Ctrl Pts',(6.44825007422594,-2.0524034642938,-1.40091397041524));
#47318=CARTESIAN_POINT('Ctrl Pts',(6.50186125743187,-1.88396761719982,-1.39261510124735));
#47319=CARTESIAN_POINT('Ctrl Pts',(6.54886146408816,-1.71345258833752,-1.38431623207946));
#47320=CARTESIAN_POINT('Ctrl Pts',(6.58910723279088,-1.5414132718979,-1.37601736291158));
#47321=CARTESIAN_POINT('Ctrl Pts',(6.62938131468486,-1.36925292454671,-1.36771265542881));
#47322=CARTESIAN_POINT('Ctrl Pts',(6.66289138438381,-1.19556648598138,-1.35940794794606));
#47323=CARTESIAN_POINT('Ctrl Pts',(6.68954493557173,-1.02091995522011,-1.3511032404633));
#47324=CARTESIAN_POINT('Ctrl Pts',(6.7162082249102,-0.846209615542786,-1.34279549876978));
#47325=CARTESIAN_POINT('Ctrl Pts',(6.73600995759143,-0.670538829432128,
-1.33448775707625));
#47326=CARTESIAN_POINT('Ctrl Pts',(6.74890950767273,-0.494478975533438,
-1.32618001538273));
#47327=CARTESIAN_POINT('Ctrl Pts',(6.76182279011761,-0.318231695103592,
-1.31786342958776));
#47328=CARTESIAN_POINT('Ctrl Pts',(6.76781919118983,-0.141594866962051,
-1.3095468437928));
#47329=CARTESIAN_POINT('Ctrl Pts',(6.7669102156302,0.034858766468189,-1.30123025799784));
#47330=CARTESIAN_POINT('Ctrl Pts',(6.76623974952352,0.165012079571077,-1.29509589185374));
#47331=CARTESIAN_POINT('Ctrl Pts',(6.76181341237456,0.295065708862492,-1.28896152570965));
#47332=CARTESIAN_POINT('Ctrl Pts',(6.75365390418925,0.424791645903411,-1.28282715956554));
#47333=CARTESIAN_POINT('Ctrl Pts',(6.74241150413655,0.603531693502222,-1.2743750572212));
#47334=CARTESIAN_POINT('Ctrl Pts',(6.72405955500997,0.781976433371651,-1.26592295487685));
#47335=CARTESIAN_POINT('Ctrl Pts',(6.69862491618937,0.959538030620478,-1.25747085253251));
#47336=CARTESIAN_POINT('Ctrl Pts',(6.67321272079666,1.13694294819584,-1.24902620829091));
#47337=CARTESIAN_POINT('Ctrl Pts',(6.64073033942457,1.31346594993434,-1.2405815640493));
#47338=CARTESIAN_POINT('Ctrl Pts',(6.6012565110271,1.48852325330251,-1.2321369198077));
#47339=CARTESIAN_POINT('Ctrl Pts',(6.56181215926768,1.66344983459537,-1.22369858150935));
#47340=CARTESIAN_POINT('Ctrl Pts',(6.51538684054236,1.83691257716809,-1.215260243211));
#47341=CARTESIAN_POINT('Ctrl Pts',(6.46211062418777,2.00833644610648,-1.20682190491265));
#47342=CARTESIAN_POINT('Ctrl Pts',(6.40887262314128,2.17963735180879,-1.19838961947841));
#47343=CARTESIAN_POINT('Ctrl Pts',(6.34879362477254,2.34890198542799,-1.18995733404419));
#47344=CARTESIAN_POINT('Ctrl Pts',(6.28205398723239,2.51556886240423,-1.18152504860995));
#47345=CARTESIAN_POINT('Ctrl Pts',(6.21534311734696,2.68216389878695,-1.17309639785347));
#47346=CARTESIAN_POINT('Ctrl Pts',(6.14197745474585,2.84616310375001,-1.16466774709697));
#47347=CARTESIAN_POINT('Ctrl Pts',(6.06218631264873,3.00702279850593,-1.15623909634049));
#47348=CARTESIAN_POINT('Ctrl Pts',(5.98242004989309,3.16783233627485,-1.14781307368625));
#47349=CARTESIAN_POINT('Ctrl Pts',(5.89623245022907,3.32550401957339,-1.13938705103205));
#47350=CARTESIAN_POINT('Ctrl Pts',(5.80389996755179,3.47951636964857,-1.13096102837782));
#47351=CARTESIAN_POINT('Ctrl Pts',(5.77870504470176,3.52154198366415,-1.12866180512994));
#47352=CARTESIAN_POINT('Ctrl Pts',(5.75305284538321,3.56329526650867,-1.12636258188204));
#47353=CARTESIAN_POINT('Ctrl Pts',(5.7269495768861,3.60476594854702,-1.12406335863416));
#47354=CARTESIAN_POINT('Ctrl Pts',(5.62909068991299,3.76023593448914,-1.11544377032609));
#47355=CARTESIAN_POINT('Ctrl Pts',(5.52493312005685,3.91166182871268,-1.10682418201804));
#47356=CARTESIAN_POINT('Ctrl Pts',(5.41484041301644,4.05854558944013,-1.09820459370997));
#47357=CARTESIAN_POINT('Ctrl Pts',(5.30468141757354,4.20551779099271,-1.0895798154238));
#47358=CARTESIAN_POINT('Ctrl Pts',(5.18858033539406,4.34794215774012,-1.0809550371376));
#47359=CARTESIAN_POINT('Ctrl Pts',(5.06694128655958,4.48535338614004,-1.07233025885143));
#47360=CARTESIAN_POINT('Ctrl Pts',(4.94114952461637,4.62745578415146,-1.06341103375568));
#47361=CARTESIAN_POINT('Ctrl Pts',(4.80943523720456,4.76419644679313,-1.05449180865994));
#47362=CARTESIAN_POINT('Ctrl Pts',(4.67228663297741,4.89510230938033,-1.04557258356419));
#47363=CARTESIAN_POINT('Ctrl Pts',(4.53941781836711,5.02192319017247,-1.03693168727223));
#47364=CARTESIAN_POINT('Ctrl Pts',(4.40144899293313,5.1432677689271,-1.02829079098026));
#47365=CARTESIAN_POINT('Ctrl Pts',(4.25885802004751,5.2587467485207,-1.01964989468829));
#47366=CARTESIAN_POINT('Ctrl Pts',(4.10937762731945,5.37980520595427,-1.01059150519065));
#47367=CARTESIAN_POINT('Ctrl Pts',(3.95481768651747,5.49441698771944,-1.00153311569303));
#47368=CARTESIAN_POINT('Ctrl Pts',(3.79576360793486,5.60218418410867,-0.99247472619539));
#47369=CARTESIAN_POINT('Ctrl Pts',(3.63670952935225,5.7099513804979,-0.983416336697754));
#47370=CARTESIAN_POINT('Ctrl Pts',(3.47316165563625,5.81087381904181,-0.974357947200104));
#47371=CARTESIAN_POINT('Ctrl Pts',(3.30573614850423,5.90460815943552,-0.965299557702465));
#47372=CARTESIAN_POINT('Ctrl Pts',(3.23750883840348,5.94280569587234,-0.961608187373922));
#47373=CARTESIAN_POINT('Ctrl Pts',(3.16861202014468,5.97982472446026,-0.957916817045377));
#47374=CARTESIAN_POINT('Ctrl Pts',(3.0990855038472,6.01564277861013,-0.954225446716826));
#47375=CARTESIAN_POINT('Ctrl Pts',(3.09908550384716,6.01564277861015,-2.95434584629072));
#47376=CARTESIAN_POINT('Ctrl Pts',(2.94505279430701,6.0949959840484,-2.94621616489886));
#47377=CARTESIAN_POINT('Ctrl Pts',(2.78803629944485,6.16839524135199,-2.938086483507));
#47378=CARTESIAN_POINT('Ctrl Pts',(2.6285457489766,6.23562637154737,-2.92995680211514));
#47379=CARTESIAN_POINT('Ctrl Pts',(2.46898819084288,6.30288574793708,-2.92182370515433));
#47380=CARTESIAN_POINT('Ctrl Pts',(2.30695484747266,6.36397170294264,-2.91369060819352));
#47381=CARTESIAN_POINT('Ctrl Pts',(2.14297252482312,6.4187193238101,-2.90555751123271));
#47382=CARTESIAN_POINT('Ctrl Pts',(1.9788142104859,6.47352570178039,-2.89741568554166));
#47383=CARTESIAN_POINT('Ctrl Pts',(1.81270309031937,6.52198005798384,-2.88927385985062));
#47384=CARTESIAN_POINT('Ctrl Pts',(1.64517880988649,6.56396798312579,-2.88113203415956));
#47385=CARTESIAN_POINT('Ctrl Pts',(1.57201917722354,6.58230455601975,-2.87757641239999));
#47386=CARTESIAN_POINT('Ctrl Pts',(1.49859014298685,6.5994085385298,-2.87402079064042));
#47387=CARTESIAN_POINT('Ctrl Pts',(1.42493704901875,6.61527349444706,-2.87046516888085));
#47388=CARTESIAN_POINT('Ctrl Pts',(1.25009215240008,6.65293527384785,-2.86202448722753));
#47389=CARTESIAN_POINT('Ctrl Pts',(1.07362401827726,6.68368879323515,-2.85358380557422));
#47390=CARTESIAN_POINT('Ctrl Pts',(0.896105147946706,6.70740520349139,-2.8451431239209));
#47391=CARTESIAN_POINT('Ctrl Pts',(0.718720460886934,6.73110368694643,-2.83670882242462));
#47392=CARTESIAN_POINT('Ctrl Pts',(0.540286950172614,6.7477756208244,-2.82827452092834));
#47393=CARTESIAN_POINT('Ctrl Pts',(0.361386763349121,6.75734330985751,-2.81984021943207));
#47394=CARTESIAN_POINT('Ctrl Pts',(0.182594330036346,6.7669052361684,-2.81141099800649));
#47395=CARTESIAN_POINT('Ctrl Pts',(0.00333611310928791,6.76937143062896,
-2.80298177658091));
#47396=CARTESIAN_POINT('Ctrl Pts',(-0.175800769736442,6.76471603907807,
-2.79455255515533));
#47397=CARTESIAN_POINT('Ctrl Pts',(-0.354857236466523,6.76006273737323,
-2.78612711768108));
#47398=CARTESIAN_POINT('Ctrl Pts',(-0.533792144965517,6.74829423267054,
-2.77770168020682));
#47399=CARTESIAN_POINT('Ctrl Pts',(-0.712018126993741,6.72943676594352,
-2.76927624273257));
#47400=CARTESIAN_POINT('Ctrl Pts',(-0.890191419189449,6.71058487414307,
-2.76085329611226));
#47401=CARTESIAN_POINT('Ctrl Pts',(-1.06765587165717,6.6846482347562,-2.75243034949195));
#47402=CARTESIAN_POINT('Ctrl Pts',(-1.24382858853427,6.65170500265495,-2.74400740287164));
#47403=CARTESIAN_POINT('Ctrl Pts',(-1.42000422530965,6.61876122455039,-2.73558431664885));
#47404=CARTESIAN_POINT('Ctrl Pts',(-1.59488775484884,6.57881067648143,-2.72716123042605));
#47405=CARTESIAN_POINT('Ctrl Pts',(-1.76790516686299,6.53198287819091,-2.71873814420326));
#47406=CARTESIAN_POINT('Ctrl Pts',(-1.94092856479743,6.48515345978906,-2.71031476656517));
#47407=CARTESIAN_POINT('Ctrl Pts',(-2.11208539450655,6.43144640372495,-2.7018913889271));
#47408=CARTESIAN_POINT('Ctrl Pts',(-2.28081538299629,6.37104153091843,-2.69346801128901));
#47409=CARTESIAN_POINT('Ctrl Pts',(-2.44957474239012,6.31062614340886,-2.68504316738982));
#47410=CARTESIAN_POINT('Ctrl Pts',(-2.61590610436534,6.24351072711649,-2.67661832349062));
#47411=CARTESIAN_POINT('Ctrl Pts',(-2.77926745554553,6.16992393879742,-2.66819347959143));
#47412=CARTESIAN_POINT('Ctrl Pts',(-2.94268003467798,6.09631407463788,-2.65976599377298));
#47413=CARTESIAN_POINT('Ctrl Pts',(-3.10312044219389,6.01622892941827,-2.65133850795452));
#47414=CARTESIAN_POINT('Ctrl Pts',(-3.26006929038381,5.92994411625408,-2.64291102213607));
#47415=CARTESIAN_POINT('Ctrl Pts',(-3.4171588965251,5.84358191944755,-2.63447597821411));
#47416=CARTESIAN_POINT('Ctrl Pts',(-3.57075039389726,5.7510091056195,-2.62604093429216));
#47417=CARTESIAN_POINT('Ctrl Pts',(-3.72035054300453,5.65254640292018,-2.61760589037021));
#47418=CARTESIAN_POINT('Ctrl Pts',(-3.87002300130549,5.55403610829878,-2.60916676937194));
#47419=CARTESIAN_POINT('Ctrl Pts',(-4.01569998984316,5.44963043701574,-2.60072764837366));
#47420=CARTESIAN_POINT('Ctrl Pts',(-4.15691921338945,5.33969209349693,-2.59228852737539));
#47421=CARTESIAN_POINT('Ctrl Pts',(-4.29829538564324,5.22963156632291,-2.58384002727774));
#47422=CARTESIAN_POINT('Ctrl Pts',(-4.43520363545698,5.11402629175641,-2.57539152718009));
#47423=CARTESIAN_POINT('Ctrl Pts',(-4.56721565045773,4.99327850236836,-2.56694302708243));
#47424=CARTESIAN_POINT('Ctrl Pts',(-4.64016307634304,4.92655548161036,-2.56227454039421));
#47425=CARTESIAN_POINT('Ctrl Pts',(-4.71161610343265,4.85826286943379,-2.55760605370602));
#47426=CARTESIAN_POINT('Ctrl Pts',(-4.78150750434896,4.7884731372176,-2.5529375670178));
#47427=CARTESIAN_POINT('Ctrl Pts',(-4.90488130088784,4.66527880844385,-2.54469665441244));
#47428=CARTESIAN_POINT('Ctrl Pts',(-5.02366127589653,4.53714331615842,-2.5364557418071));
#47429=CARTESIAN_POINT('Ctrl Pts',(-5.13742982010061,4.40444137701264,-2.52821482920175));
#47430=CARTESIAN_POINT('Ctrl Pts',(-5.25107233795084,4.27188643756399,-2.51998304541295));
#47431=CARTESIAN_POINT('Ctrl Pts',(-5.35971424928701,4.13477539128512,-2.51175126162414));
#47432=CARTESIAN_POINT('Ctrl Pts',(-5.46297363312294,3.99352076291129,-2.50351947783533));
#47433=CARTESIAN_POINT('Ctrl Pts',(-5.56613703177179,3.85239743836116,-2.49529534593518));
#47434=CARTESIAN_POINT('Ctrl Pts',(-5.66392765853334,3.70713848799727,-2.48707121403503));
#47435=CARTESIAN_POINT('Ctrl Pts',(-5.75600280431726,3.55819065210001,-2.47884708213488));
#47436=CARTESIAN_POINT('Ctrl Pts',(-5.84799657513271,3.40937445460903,-2.47063021862912));
#47437=CARTESIAN_POINT('Ctrl Pts',(-5.9342847463501,3.25687617096491,-2.46241335512337));
#47438=CARTESIAN_POINT('Ctrl Pts',(-6.01456708783003,3.10117264046873,-2.45419649161762));
#47439=CARTESIAN_POINT('Ctrl Pts',(-6.09480828430846,2.94554890861666,-2.44598383928527));
#47440=CARTESIAN_POINT('Ctrl Pts',(-6.16904961859227,2.78672351696052,-2.4377711869529));
#47441=CARTESIAN_POINT('Ctrl Pts',(-6.23703589978149,2.62519945620078,-2.42955853462055));
#47442=CARTESIAN_POINT('Ctrl Pts',(-6.30499942553193,2.4637294585669,-2.42134863111493));
#47443=CARTESIAN_POINT('Ctrl Pts',(-6.36671193103798,2.29956291878483,-2.41313872760933));
#47444=CARTESIAN_POINT('Ctrl Pts',(-6.42196559806087,2.13322452107665,-2.40492882410371));
#47445=CARTESIAN_POINT('Ctrl Pts',(-6.44609322205822,2.06058951723948,-2.40134380476453));
#47446=CARTESIAN_POINT('Ctrl Pts',(-6.46898988947276,1.98754063857672,-2.39775878542533));
#47447=CARTESIAN_POINT('Ctrl Pts',(-6.49064122044032,1.91412265738666,-2.39417376608615));
#47448=CARTESIAN_POINT('Ctrl Pts',(-6.54045949825669,1.7451927477602,-2.38592487415039));
#47449=CARTESIAN_POINT('Ctrl Pts',(-6.58365384022403,1.57440063720012,-2.37767598221462));
#47450=CARTESIAN_POINT('Ctrl Pts',(-6.62010824159231,1.40230377222685,-2.36942709027886));
#47451=CARTESIAN_POINT('Ctrl Pts',(-6.65658155097781,1.2301176447677,-2.36117391984216));
#47452=CARTESIAN_POINT('Ctrl Pts',(-6.68630788869608,1.05662575944793,-2.35292074940546));
#47453=CARTESIAN_POINT('Ctrl Pts',(-6.70922288550451,0.882392924168423,
-2.34466757896875));
#47454=CARTESIAN_POINT('Ctrl Pts',(-6.73216758693566,0.707934231531007,
-2.33640370997878));
#47455=CARTESIAN_POINT('Ctrl Pts',(-6.74828327122341,0.532733019499745,
-2.32813984098882));
#47456=CARTESIAN_POINT('Ctrl Pts',(-6.75755759151857,0.357357520292742,
-2.31987597199884));
#47457=CARTESIAN_POINT('Ctrl Pts',(-6.76393799849216,0.236705329886858,
-2.31419072007154));
#47458=CARTESIAN_POINT('Ctrl Pts',(-6.76708150887763,0.115970675755758,
-2.30850546814425));
#47459=CARTESIAN_POINT('Ctrl Pts',(-6.76699839382599,-0.00466239815271638,
-2.30282021621695));
#47460=CARTESIAN_POINT('',(-6.767,1.61215658878167E-12,-2.69717978381011));
#47461=CARTESIAN_POINT('Ctrl Pts',(3.09908550384726,6.0156427786101,-3.34860320957389));
#47462=CARTESIAN_POINT('Ctrl Pts',(2.93373232018333,6.10082796552478,-3.3398537616746));
#47463=CARTESIAN_POINT('Ctrl Pts',(2.76486502144429,6.17919158180189,-3.33110431377531));
#47464=CARTESIAN_POINT('Ctrl Pts',(2.59305716434354,6.25046746591378,-3.32235486587602));
#47465=CARTESIAN_POINT('Ctrl Pts',(2.42125069459283,6.32174277447225,-3.31360548862861));
#47466=CARTESIAN_POINT('Ctrl Pts',(2.24650397871057,6.38593035557826,-3.30485611138118));
#47467=CARTESIAN_POINT('Ctrl Pts',(2.06941053323768,6.4428122000354,-3.29610673413377));
#47468=CARTESIAN_POINT('Ctrl Pts',(1.89231845896679,6.49969360406686,-3.28735742463117));
#47469=CARTESIAN_POINT('Ctrl Pts',(1.712879964315,6.54926929700882,-3.27860811512858));
#47470=CARTESIAN_POINT('Ctrl Pts',(1.53170449173499,6.5913709006548,-3.26985880562598));
#47471=CARTESIAN_POINT('Ctrl Pts',(1.35053036178164,6.63347219230084,-3.26110956096139));
#47472=CARTESIAN_POINT('Ctrl Pts',(1.16761955878838,6.66809944062455,-3.2523603162968));
#47473=CARTESIAN_POINT('Ctrl Pts',(0.983593309310419,6.69513503985392,-3.24361107163221));
#47474=CARTESIAN_POINT('Ctrl Pts',(0.799568362459921,6.72217044771215,-3.23486188889903));
#47475=CARTESIAN_POINT('Ctrl Pts',(0.614428268438543,6.74161427235978,-3.22611270616587));
#47476=CARTESIAN_POINT('Ctrl Pts',(0.428801816330225,6.75340047696802,-3.2173635234327));
#47477=CARTESIAN_POINT('Ctrl Pts',(0.243176616522786,6.76518660206242,-3.20861439972456));
#47478=CARTESIAN_POINT('Ctrl Pts',(0.0570653511655087,6.76931519233997,
-3.19986527601642));
#47479=CARTESIAN_POINT('Ctrl Pts',(-0.128899900799936,6.76577222610795,
-3.19111615230829));
#47480=CARTESIAN_POINT('Ctrl Pts',(-0.314863959942007,6.76222928260133,
-3.18236708471902));
#47481=CARTESIAN_POINT('Ctrl Pts',(-0.500681721080748,6.75101488651276,
-3.17361801712977));
#47482=CARTESIAN_POINT('Ctrl Pts',(-0.685722110173445,6.73216712415989,
-3.16486894954051));
#47483=CARTESIAN_POINT('Ctrl Pts',(-0.870761373827916,6.71331947644142,
-3.15611993516414));
#47484=CARTESIAN_POINT('Ctrl Pts',(-1.05502298984389,6.6868385843999,-3.14737092078778));
#47485=CARTESIAN_POINT('Ctrl Pts',(-1.23788117676121,6.65281438131415,-3.13862190641141));
#47486=CARTESIAN_POINT('Ctrl Pts',(-1.43009641451851,6.61704912302365,-3.12942519552388));
#47487=CARTESIAN_POINT('Ctrl Pts',(-1.62076048992751,6.57294837083151,-3.12022848463634));
#47488=CARTESIAN_POINT('Ctrl Pts',(-1.80915798961184,6.52067760042035,-3.11103177374881));
#47489=CARTESIAN_POINT('Ctrl Pts',(-1.98840443003061,6.47094578577394,-3.10228177604231));
#47490=CARTESIAN_POINT('Ctrl Pts',(-2.16559895952237,6.4138188847446,-3.09353177833581));
#47491=CARTESIAN_POINT('Ctrl Pts',(-2.34013966242364,6.34949095285219,-3.0847817806293));
#47492=CARTESIAN_POINT('Ctrl Pts',(-2.51467682554056,6.28516432556668,-3.0760319603777));
#47493=CARTESIAN_POINT('Ctrl Pts',(-2.68656000078884,6.21363705879643,-3.0672821401261));
#47494=CARTESIAN_POINT('Ctrl Pts',(-2.8552053384093,6.1351521151084,-3.05853231987451));
#47495=CARTESIAN_POINT('Ctrl Pts',(-3.02384747998358,6.05666865881105,-3.04978266544327));
#47496=CARTESIAN_POINT('Ctrl Pts',(-3.18925164684558,5.97122791039832,-3.04103301101202));
#47497=CARTESIAN_POINT('Ctrl Pts',(-3.3508560182917,5.87912008251901,-3.03228335658078));
#47498=CARTESIAN_POINT('Ctrl Pts',(-3.5124575419143,5.78701387778167,-3.02353385633764));
#47499=CARTESIAN_POINT('Ctrl Pts',(-3.67025915510947,5.68824097060975,-3.01478435609451));
#47500=CARTESIAN_POINT('Ctrl Pts',(-3.82372487928845,5.58313684656848,-3.00603485585137));
#47501=CARTESIAN_POINT('Ctrl Pts',(-3.97718810300807,5.47803443501766,-2.99728549816625));
#47502=CARTESIAN_POINT('Ctrl Pts',(-4.12631534263033,5.3666011749637,-2.98853614048113));
#47503=CARTESIAN_POINT('Ctrl Pts',(-4.27060009886232,5.24921554097345,-2.97978678279601));
#47504=CARTESIAN_POINT('Ctrl Pts',(-4.41488269594215,5.13183166360289,-2.97103755604083));
#47505=CARTESIAN_POINT('Ctrl Pts',(-4.55432273235086,5.00849577139473,-2.96228832928566));
#47506=CARTESIAN_POINT('Ctrl Pts',(-4.688446624802,4.87962675277349,-2.95353910253048));
#47507=CARTESIAN_POINT('Ctrl Pts',(-4.82256868835142,4.75075949139897,-2.944789995079));
#47508=CARTESIAN_POINT('Ctrl Pts',(-4.95137454637838,4.61635945312551,-2.93604088762752));
#47509=CARTESIAN_POINT('Ctrl Pts',(-5.07442674461046,4.47688309134626,-2.92729178017603));
#47510=CARTESIAN_POINT('Ctrl Pts',(-5.19747742838464,4.33740844616438,-2.91854278040369));
#47511=CARTESIAN_POINT('Ctrl Pts',(-5.31477440450814,4.19285781736169,-2.90979378063135));
#47512=CARTESIAN_POINT('Ctrl Pts',(-5.42591931531006,4.04372211999603,-2.901044780859));
#47513=CARTESIAN_POINT('Ctrl Pts',(-5.53707636462847,3.89457013500993,-2.89229482557842));
#47514=CARTESIAN_POINT('Ctrl Pts',(-5.64207983273348,3.74083230916606,-2.88354487029784));
#47515=CARTESIAN_POINT('Ctrl Pts',(-5.74057303468636,3.58303087252006,-2.87479491501725));
#47516=CARTESIAN_POINT('Ctrl Pts',(-5.83906243363663,3.42523552887605,-2.86604529758844));
#47517=CARTESIAN_POINT('Ctrl Pts',(-5.93104191768333,3.26337713157162,-2.85729568015964));
#47518=CARTESIAN_POINT('Ctrl Pts',(-6.01619906699572,3.0980054529132,-2.84854606273083));
#47519=CARTESIAN_POINT('Ctrl Pts',(-6.10135338095293,2.9326392803978,-2.83979673662545));
#47520=CARTESIAN_POINT('Ctrl Pts',(-6.17968568352746,2.7637603154043,-2.83104741052006));
#47521=CARTESIAN_POINT('Ctrl Pts',(-6.25092992694792,2.59194213831769,-2.82229808441468));
#47522=CARTESIAN_POINT('Ctrl Pts',(-6.32217217691024,2.4201287688103,-2.81354900312087));
#47523=CARTESIAN_POINT('Ctrl Pts',(-6.38632665483784,2.24537661647862,-2.80479992182707));
#47524=CARTESIAN_POINT('Ctrl Pts',(-6.44317547869295,2.06827917621629,-2.79605084053326));
#47525=CARTESIAN_POINT('Ctrl Pts',(-6.50002944235886,1.89116572423596,-2.7873009682183));
#47526=CARTESIAN_POINT('Ctrl Pts',(-6.54957634250353,1.71170683289371,-2.77855109590334));
#47527=CARTESIAN_POINT('Ctrl Pts',(-6.59164787708355,1.53051209225538,-2.76980122358837));
#47528=CARTESIAN_POINT('Ctrl Pts',(-6.6337164907497,1.34932993148217,-2.76105195875359));
#47529=CARTESIAN_POINT('Ctrl Pts',(-6.66831071257088,1.16641244174204,-2.7523026939188));
#47530=CARTESIAN_POINT('Ctrl Pts',(-6.69531304840301,0.982380875162153,
-2.74355342908402));
#47531=CARTESIAN_POINT('Ctrl Pts',(-6.72231677033017,0.798339861798054,
-2.73480371512836));
#47532=CARTESIAN_POINT('Ctrl Pts',(-6.74172778477869,0.613184940732429,
-2.72605400117271));
#47533=CARTESIAN_POINT('Ctrl Pts',(-6.75348015835503,0.427545027692894,
-2.71730428721705));
#47534=CARTESIAN_POINT('Ctrl Pts',(-6.76249038365213,0.285219953548949,
-2.71059611941474));
#47535=CARTESIAN_POINT('Ctrl Pts',(-6.76699999999997,0.142609995759217,
-2.70388795161242));
#47536=CARTESIAN_POINT('Ctrl Pts',(-6.767,1.61215615940619E-12,-2.69717978381011));
#47537=CARTESIAN_POINT('Ctrl Pts',(-6.76699995433269,-0.000786168808179289,
-2.69717978381012));
#47538=CARTESIAN_POINT('Ctrl Pts',(-6.76699094693078,-0.0783179758107126,
-2.6935424771142));
#47539=CARTESIAN_POINT('Ctrl Pts',(-6.76564930093462,-0.155845262926331,
-2.6899051704183));
#47540=CARTESIAN_POINT('Ctrl Pts',(-6.76297653321342,-0.23331826161836,
-2.68626786372241));
#47541=CARTESIAN_POINT('Ctrl Pts',(-6.7566431324609,-0.41689857962518,-2.67764888767665));
#47542=CARTESIAN_POINT('Ctrl Pts',(-6.7428328025016,-0.60015403054839,-2.6690299116309));
#47543=CARTESIAN_POINT('Ctrl Pts',(-6.72160900020107,-0.782471372266058,
-2.66041093558513));
#47544=CARTESIAN_POINT('Ctrl Pts',(-6.70037248324128,-0.964897935830279,
-2.65178679612227));
#47545=CARTESIAN_POINT('Ctrl Pts',(-6.67171366577148,-1.14638496649781,
-2.64316265665942));
#47546=CARTESIAN_POINT('Ctrl Pts',(-6.63574754288657,-1.32632708902249,
-2.63453851719656));
#47547=CARTESIAN_POINT('Ctrl Pts',(-6.59854949009672,-1.51243268050393,
-2.62561897932941));
#47548=CARTESIAN_POINT('Ctrl Pts',(-6.55353475948872,-1.69688530660009,
-2.61669944146222));
#47549=CARTESIAN_POINT('Ctrl Pts',(-6.50088716470291,-1.87903035414573,
-2.60777990359508));
#47550=CARTESIAN_POINT('Ctrl Pts',(-6.4498883317872,-2.05547117511759,-2.59913969841149));
#47551=CARTESIAN_POINT('Ctrl Pts',(-6.39172761537296,-2.22974648828572,
-2.5904994932279));
#47552=CARTESIAN_POINT('Ctrl Pts',(-6.32662199237576,-2.40127948510527,
-2.58185928804431));
#47553=CARTESIAN_POINT('Ctrl Pts',(-6.25835913040098,-2.58113082124127,
-2.57280008383537));
#47554=CARTESIAN_POINT('Ctrl Pts',(-6.18246119374536,-2.7579668993438,-2.56374087962646));
#47555=CARTESIAN_POINT('Ctrl Pts',(-6.09923391623129,-2.93114902983351,
-2.55468167541753));
#47556=CARTESIAN_POINT('Ctrl Pts',(-6.01600663871724,-3.10433116032317,
-2.54562247120861));
#47557=CARTESIAN_POINT('Ctrl Pts',(-5.92545022984855,-3.27385902130687,
-2.53656326699969));
#47558=CARTESIAN_POINT('Ctrl Pts',(-5.82792449794053,-3.43912562235005,
-2.52750406279076));
#47559=CARTESIAN_POINT('Ctrl Pts',(-5.73056778747931,-3.60410580052341,
-2.51846055905157));
#47560=CARTESIAN_POINT('Ctrl Pts',(-5.62617692789581,-3.76499189855237,
-2.50941705531238));
#47561=CARTESIAN_POINT('Ctrl Pts',(-5.51510494610675,-3.92121236780525,
-2.50037355157318));
#47562=CARTESIAN_POINT('Ctrl Pts',(-5.40413456312874,-4.07728994040966,
-2.49133832003021));
#47563=CARTESIAN_POINT('Ctrl Pts',(-5.2864953970188,-4.22871021085151,-2.48230308848723));
#47564=CARTESIAN_POINT('Ctrl Pts',(-5.16258354324788,-4.37493087476661,
-2.47326785694426));
#47565=CARTESIAN_POINT('Ctrl Pts',(-5.03889000056429,-4.52089392335956,
-2.46424854390434));
#47566=CARTESIAN_POINT('Ctrl Pts',(-4.90894599217956,-4.66167547700369,
-2.45522923086442));
#47567=CARTESIAN_POINT('Ctrl Pts',(-4.77318746376898,-4.79676666471475,
-2.4462099178245));
#47568=CARTESIAN_POINT('Ctrl Pts',(-4.63759925819609,-4.93168836683468,
-2.4372019204272));
#47569=CARTESIAN_POINT('Ctrl Pts',(-4.49621125898455,-5.06093378285568,
-2.4281939230299));
#47570=CARTESIAN_POINT('Ctrl Pts',(-4.34949752101403,-5.18402935125688,
-2.4191859256326));
#47571=CARTESIAN_POINT('Ctrl Pts',(-4.20311515073677,-5.30684689596981,
-2.41019827370098));
#47572=CARTESIAN_POINT('Ctrl Pts',(-4.05143123417201,-5.42354216612182,
-2.40121062176937));
#47573=CARTESIAN_POINT('Ctrl Pts',(-3.89495390058917,-5.53368079240981,
-2.39222296983774));
#47574=CARTESIAN_POINT('Ctrl Pts',(-3.75867390377791,-5.62960325795577,
-2.38439540051164));
#47575=CARTESIAN_POINT('Ctrl Pts',(-3.61875868543511,-5.72055291907881,
-2.37656783118552));
#47576=CARTESIAN_POINT('Ctrl Pts',(-3.47556556181662,-5.80626670292662,
-2.36874026185942));
#47577=CARTESIAN_POINT('Ctrl Pts',(-3.3269649527174,-5.89521734640807,-2.36061709546545));
#47578=CARTESIAN_POINT('Ctrl Pts',(-3.17489976460162,-5.97848799426903,
-2.35249392907148));
#47579=CARTESIAN_POINT('Ctrl Pts',(-3.01985103637224,-6.05580619885755,
-2.34437076267751));
#47580=CARTESIAN_POINT('Ctrl Pts',(-2.86481323790383,-6.13311895309827,
-2.33624816890524));
#47581=CARTESIAN_POINT('Ctrl Pts',(-2.70679264580833,-6.20447993653089,
-2.32812557513295));
#47582=CARTESIAN_POINT('Ctrl Pts',(-2.5462938792863,-6.26966318715042,-2.32000298136068));
#47583=CARTESIAN_POINT('Ctrl Pts',(-2.38577582527473,-6.33485427098444,
-2.31187941147847));
#47584=CARTESIAN_POINT('Ctrl Pts',(-2.22277934339818,-6.39386600711472,
-2.30375584159626));
#47585=CARTESIAN_POINT('Ctrl Pts',(-2.0578279090229,-6.44652102275688,-2.29563227171405));
#47586=CARTESIAN_POINT('Ctrl Pts',(-1.89275632476716,-6.49921439207484,
-2.28750278466019));
#47587=CARTESIAN_POINT('Ctrl Pts',(-1.72572729299683,-6.54554168174518,
-2.27937329760633));
#47588=CARTESIAN_POINT('Ctrl Pts',(-1.55727890752929,-6.58537557047162,
-2.27124381055247));
#47589=CARTESIAN_POINT('Ctrl Pts',(-1.388761847141,-6.62522569912309,-2.26311100917845));
#47590=CARTESIAN_POINT('Ctrl Pts',(-1.21882463853448,-6.65857707953059,
-2.25497820780443));
#47591=CARTESIAN_POINT('Ctrl Pts',(-1.0480141266985,-6.68535379693853,-2.24684540643041));
#47592=CARTESIAN_POINT('Ctrl Pts',(-0.877017882973423,-6.7121596301793,
-2.23870376180344));
#47593=CARTESIAN_POINT('Ctrl Pts',(-0.705146802449887,-6.73237647888262,
-2.23056211717648));
#47594=CARTESIAN_POINT('Ctrl Pts',(-0.532952142707695,-6.74598035970928,
-2.22242047254951));
#47595=CARTESIAN_POINT('Ctrl Pts',(-0.445222433489368,-6.75291126285662,
-2.21827246867557));
#47596=CARTESIAN_POINT('Ctrl Pts',(-0.357408740641188,-6.7581264770849,
-2.21412446480163));
#47597=CARTESIAN_POINT('Ctrl Pts',(-0.269583759570994,-6.76162802855759,
-2.20997646092768));
#47598=CARTESIAN_POINT('Ctrl Pts',(-0.0908706414179498,-6.76875325846862,
-2.20153577927436));
#47599=CARTESIAN_POINT('Ctrl Pts',(0.0882571890225949,-6.76879421211967,
-2.19309509762102));
#47600=CARTESIAN_POINT('Ctrl Pts',(0.267213616123141,-6.76172210929719,
-2.18465441596769));
#47601=CARTESIAN_POINT('Ctrl Pts',(0.44603477332994,-6.75465535214802,-2.17622011447142));
#47602=CARTESIAN_POINT('Ctrl Pts',(0.624684453502308,-6.74048626963007,
-2.16778581297514));
#47603=CARTESIAN_POINT('Ctrl Pts',(0.802575808428136,-6.71923813179187,
-2.15935151147887));
#47604=CARTESIAN_POINT('Ctrl Pts',(0.980360017473445,-6.69800279193613,
-2.15092229005329));
#47605=CARTESIAN_POINT('Ctrl Pts',(1.15738648162811,-6.66969693671389,-2.14249306862772));
#47606=CARTESIAN_POINT('Ctrl Pts',(1.33307234478328,-6.63439576175359,-2.13406384720214));
#47607=CARTESIAN_POINT('Ctrl Pts',(1.50867934101614,-6.59911043379984,-2.12563840972788));
#47608=CARTESIAN_POINT('Ctrl Pts',(1.68294660984761,-6.5568361130292,-2.11721297225361));
#47609=CARTESIAN_POINT('Ctrl Pts',(1.85529998054192,-6.50769936169467,-2.10878753477935));
#47610=CARTESIAN_POINT('Ctrl Pts',(2.02760239755298,-6.45857713690205,-2.10036458815902));
#47611=CARTESIAN_POINT('Ctrl Pts',(2.19799172449061,-6.40259661869964,-2.09194164153869));
#47612=CARTESIAN_POINT('Ctrl Pts',(2.36590709789767,-6.339934747623,-2.08351869491836));
#47613=CARTESIAN_POINT('Ctrl Pts',(2.53382525434494,-6.27727183798446,-2.07509560869557));
#47614=CARTESIAN_POINT('Ctrl Pts',(2.69926906072849,-6.20792746456873,-2.06667252247277));
#47615=CARTESIAN_POINT('Ctrl Pts',(2.86169521457616,-6.13212764861201,-2.05824943624999));
#47616=CARTESIAN_POINT('Ctrl Pts',(3.02412698791627,-6.05632521019282,-2.04982605861188));
#47617=CARTESIAN_POINT('Ctrl Pts',(3.18354059826417,-5.97406702480634,-2.0414026809738));
#47618=CARTESIAN_POINT('Ctrl Pts',(3.33941490162489,-5.88562631457398,-2.03297930333569));
#47619=CARTESIAN_POINT('Ctrl Pts',(3.49531633809476,-5.79717020942794,-2.0245544594365));
#47620=CARTESIAN_POINT('Ctrl Pts',(3.64767694922484,-5.70252959839476,-2.01612961553731));
#47621=CARTESIAN_POINT('Ctrl Pts',(3.79600195360329,-5.60202268544497,-2.00770477163812));
#47622=CARTESIAN_POINT('Ctrl Pts',(3.94437347073541,-5.50148425486061,-1.99927728581965));
#47623=CARTESIAN_POINT('Ctrl Pts',(4.08870658205265,-5.39507604170789,-1.99084980000117));
#47624=CARTESIAN_POINT('Ctrl Pts',(4.22853684786533,-5.28315863156172,-1.9824223141827));
#47625=CARTESIAN_POINT('Ctrl Pts',(4.36849251900562,-5.17114084944386,-1.97398727026074));
#47626=CARTESIAN_POINT('Ctrl Pts',(4.50393701486435,-5.05360420636309,-1.96555222633878));
#47627=CARTESIAN_POINT('Ctrl Pts',(4.6344393921433,-4.93094925146776,-1.95711718241682));
#47628=CARTESIAN_POINT('Ctrl Pts',(4.76500484771274,-4.80823501133154,-1.94867806141855));
#47629=CARTESIAN_POINT('Ctrl Pts',(4.89062318330465,-4.68039775952832,-1.94023894042027));
#47630=CARTESIAN_POINT('Ctrl Pts',(5.01090113887212,-4.54787409417302,-1.931799819422));
#47631=CARTESIAN_POINT('Ctrl Pts',(5.13131276936844,-4.41520314420971,-1.92335131932434));
#47632=CARTESIAN_POINT('Ctrl Pts',(5.24637194241103,-4.27783562594789,-1.9149028192267));
#47633=CARTESIAN_POINT('Ctrl Pts',(5.35572565503845,-4.13624125359765,-1.90645431912905));
#47634=CARTESIAN_POINT('Ctrl Pts',(5.41615251729663,-4.05799879224021,-1.901785832441));
#47635=CARTESIAN_POINT('Ctrl Pts',(5.47483798966932,-3.97846621218753,-1.89711734575295));
#47636=CARTESIAN_POINT('Ctrl Pts',(5.53172826624605,-3.8977264383759,-1.89244885906491));
#47637=CARTESIAN_POINT('Ctrl Pts',(5.63215219988649,-3.75520286184755,-1.88420794645958));
#47638=CARTESIAN_POINT('Ctrl Pts',(5.72720313160569,-3.60859894912544,-1.87596703385426));
#47639=CARTESIAN_POINT('Ctrl Pts',(5.81653388517389,-3.45835547083061,-1.86772612124894));
#47640=CARTESIAN_POINT('Ctrl Pts',(5.90576568318962,-3.30827842375688,-1.85949433746014));
#47641=CARTESIAN_POINT('Ctrl Pts',(5.9892897399464,-3.15457014208908,-1.85126255367135));
#47642=CARTESIAN_POINT('Ctrl Pts',(6.06680052155676,-2.99770252554163,-1.84303076988255));
#47643=CARTESIAN_POINT('Ctrl Pts',(6.14423925269989,-2.84098072593513,-1.83480663798238));
#47644=CARTESIAN_POINT('Ctrl Pts',(6.21567568402042,-2.68110575721418,-1.82658250608222));
#47645=CARTESIAN_POINT('Ctrl Pts',(6.28084877942527,-2.51857650469311,-1.81835837418205));
#47646=CARTESIAN_POINT('Ctrl Pts',(6.34596427558815,-2.3561908936806,-1.8101415106763));
#47647=CARTESIAN_POINT('Ctrl Pts',(6.40482733670172,-2.19115600330071,-1.80192464717055));
#47648=CARTESIAN_POINT('Ctrl Pts',(6.4572239373238,-2.02399308873637,-1.7937077836648));
#47649=CARTESIAN_POINT('Ctrl Pts',(6.50959368449124,-1.85691584579362,-1.78549513133246));
#47650=CARTESIAN_POINT('Ctrl Pts',(6.55550346537122,-1.68771308940238,-1.77728247900012));
#47651=CARTESIAN_POINT('Ctrl Pts',(6.59478811068874,-1.51692411646675,-1.76906982666778));
#47652=CARTESIAN_POINT('Ctrl Pts',(6.63405960718674,-1.34619230768174,-1.76085992316218));
#47653=CARTESIAN_POINT('Ctrl Pts',(6.66671030593745,-1.17387568633946,-1.75265001965659));
#47654=CARTESIAN_POINT('Ctrl Pts',(6.69262542835401,-1.00052679911601,-1.74444011615099));
#47655=CARTESIAN_POINT('Ctrl Pts',(6.70394178730754,-0.924830524157983,
-1.74085509681171));
#47656=CARTESIAN_POINT('Ctrl Pts',(6.71397445593086,-0.848937562605707,
-1.73727007747243));
#47657=CARTESIAN_POINT('Ctrl Pts',(6.72271694394573,-0.77289448929655,-1.73368505813315));
#47658=CARTESIAN_POINT('Ctrl Pts',(6.74431934565474,-0.584994544336063,
-1.72482659269746));
#47659=CARTESIAN_POINT('Ctrl Pts',(6.75801862979966,-0.396372405831646,
-1.71596812726178));
#47660=CARTESIAN_POINT('Ctrl Pts',(6.7638123466204,-0.207681341736289,-1.70710966182609));
#47661=CARTESIAN_POINT('Ctrl Pts',(6.76961689746334,-0.0186374327851885,
-1.69823463140904));
#47662=CARTESIAN_POINT('Ctrl Pts',(6.76748633003523,0.170475400059,-1.68935960099199));
#47663=CARTESIAN_POINT('Ctrl Pts',(6.75747021679043,0.359005945898372,-1.68048457057494));
#47664=CARTESIAN_POINT('Ctrl Pts',(6.74742566410994,0.548071799416485,-1.67158434067677));
#47665=CARTESIAN_POINT('Ctrl Pts',(6.72945077441733,0.736551796775352,-1.66268411077861));
#47666=CARTESIAN_POINT('Ctrl Pts',(6.70364712284126,0.9237988159887,-1.65378388088044));
#47667=CARTESIAN_POINT('Ctrl Pts',(6.67780854976143,1.11129924691262,-1.64487160581064));
#47668=CARTESIAN_POINT('Ctrl Pts',(6.64412009238467,1.29756311042424,-1.63595933074085));
#47669=CARTESIAN_POINT('Ctrl Pts',(6.60273435444023,1.48195413042873,-1.62704705567105));
#47670=CARTESIAN_POINT('Ctrl Pts',(6.56125723488288,1.66675229428643,-1.61811510188798));
#47671=CARTESIAN_POINT('Ctrl Pts',(6.51204889709496,1.84966908917597,-1.60918314810491));
#47672=CARTESIAN_POINT('Ctrl Pts',(6.4553124662422,2.03008127009192,-1.60025119432184));
#47673=CARTESIAN_POINT('Ctrl Pts',(6.4016799217538,2.20062362134301,-1.59180788194849));
#47674=CARTESIAN_POINT('Ctrl Pts',(6.34132091572155,2.36892787838849,-1.58336456957514));
#47675=CARTESIAN_POINT('Ctrl Pts',(6.27444632298704,2.53448463004896,-1.57492125720179));
#47676=CARTESIAN_POINT('Ctrl Pts',(6.20929631430771,2.69577194959081,-1.56669568375285));
#47677=CARTESIAN_POINT('Ctrl Pts',(6.13783698063295,2.85475945785251,-1.55847011030391));
#47678=CARTESIAN_POINT('Ctrl Pts',(6.06025193000832,3.01091938530916,-1.55024453685496));
#47679=CARTESIAN_POINT('Ctrl Pts',(5.9810512360148,3.17033121180112,-1.54184767276315));
#47680=CARTESIAN_POINT('Ctrl Pts',(5.89546697102152,3.32679603403316,-1.53345080867134));
#47681=CARTESIAN_POINT('Ctrl Pts',(5.80374756332198,3.4797705702006,-1.52505394457953));
#47682=CARTESIAN_POINT('Ctrl Pts',(5.71409531493739,3.6292973874466,-1.51684632784833));
#47683=CARTESIAN_POINT('Ctrl Pts',(5.61858168015793,3.77548921626075,-1.50863871111713));
#47684=CARTESIAN_POINT('Ctrl Pts',(5.51748638254428,3.91786077068067,-1.50043109438593));
#47685=CARTESIAN_POINT('Ctrl Pts',(5.41645265011226,4.06014562343577,-1.49222847594275));
#47686=CARTESIAN_POINT('Ctrl Pts',(5.30984423053164,4.19861454334708,-1.48402585749956));
#47687=CARTESIAN_POINT('Ctrl Pts',(5.19798504347307,4.33280976824858,-1.47582323905637));
#47688=CARTESIAN_POINT('Ctrl Pts',(5.08617365571423,4.46694764928814,-1.46762412572912));
#47689=CARTESIAN_POINT('Ctrl Pts',(4.96911619876696,4.59681519798083,-1.45942501240185));
#47690=CARTESIAN_POINT('Ctrl Pts',(4.84717792625352,4.72198635652843,-1.45122589907459));
#47691=CARTESIAN_POINT('Ctrl Pts',(4.72013759570419,4.85239484132451,-1.44268372403934));
#47692=CARTESIAN_POINT('Ctrl Pts',(4.58779944702644,4.97770512743408,-1.4341415490041));
#47693=CARTESIAN_POINT('Ctrl Pts',(4.4506207720848,5.09747621309676,-1.42559937396885));
#47694=CARTESIAN_POINT('Ctrl Pts',(4.31896857378499,5.21242211651037,-1.41740133500885));
#47695=CARTESIAN_POINT('Ctrl Pts',(4.18285854295231,5.32226616906058,-1.40920329604884));
#47696=CARTESIAN_POINT('Ctrl Pts',(4.04273003568223,5.42665853528603,-1.40100525708883));
#47697=CARTESIAN_POINT('Ctrl Pts',(3.90258913388723,5.53106013513433,-1.39280649300302));
#47698=CARTESIAN_POINT('Ctrl Pts',(3.75842933855136,5.63000887862587,-1.3846077289172));
#47699=CARTESIAN_POINT('Ctrl Pts',(3.61072026394537,5.72319737345606,-1.37640896483138));
#47700=CARTESIAN_POINT('Ctrl Pts',(3.4629419197733,5.81642956991133,-1.36820635585768));
#47701=CARTESIAN_POINT('Ctrl Pts',(3.31161128004421,5.90389593936438,-1.36000374688397));
#47702=CARTESIAN_POINT('Ctrl Pts',(3.15722423136878,5.98533408865853,-1.35180113791027));
#47703=CARTESIAN_POINT('Ctrl Pts',(3.13789221657325,5.99553159888094,-1.35077402482403));
#47704=CARTESIAN_POINT('Ctrl Pts',(3.11851230807468,6.00563464987257,-1.34974691173779));
#47705=CARTESIAN_POINT('Ctrl Pts',(3.09908550384728,6.01564277861008,-1.34871979865154));
#47706=CARTESIAN_POINT('Origin',(0.,0.,-63.6971797838103));
#47707=CARTESIAN_POINT('',(3.09908550384726,6.0156427786101,1.04588102939736));
#47708=CARTESIAN_POINT('',(3.09908550384723,6.01564277861011,0.651473025530853));
#47709=CARTESIAN_POINT('',(3.09908550384721,6.01564277861012,-63.6971797838103));
#47710=CARTESIAN_POINT('',(-6.76699833344662,0.00474922421608585,-0.30282021614616));
#47711=CARTESIAN_POINT('Ctrl Pts',(-6.76699833344662,0.00474922421608134,
-0.302820216146117));
#47712=CARTESIAN_POINT('Ctrl Pts',(-6.76711739371051,-0.164895452611073,
-0.294814773799422));
#47713=CARTESIAN_POINT('Ctrl Pts',(-6.76085299225617,-0.334804302025666,
-0.286809331452755));
#47714=CARTESIAN_POINT('Ctrl Pts',(-6.74817206586946,-0.50444302891323,
-0.278803889106058));
#47715=CARTESIAN_POINT('Ctrl Pts',(-6.73550285360902,-0.673925050414571,
-0.270805841862813));
#47716=CARTESIAN_POINT('Ctrl Pts',(-6.71642893600105,-0.843137071533396,
-0.26280779461959));
#47717=CARTESIAN_POINT('Ctrl Pts',(-6.6909692592208,-1.0115430649074,-0.254809747376342));
#47718=CARTESIAN_POINT('Ctrl Pts',(-6.66553007862698,-1.17981348387234,
-0.246818138921328));
#47719=CARTESIAN_POINT('Ctrl Pts',(-6.63371543035107,-1.34727879468629,
-0.238826530466301));
#47720=CARTESIAN_POINT('Ctrl Pts',(-6.59559619156139,-1.51340671263905,
-0.23083492201129));
#47721=CARTESIAN_POINT('Ctrl Pts',(-6.55749478096564,-1.67945693332309,
-0.222847051195066));
#47722=CARTESIAN_POINT('Ctrl Pts',(-6.51309473124773,-1.84417063787405,
-0.214859180378844));
#47723=CARTESIAN_POINT('Ctrl Pts',(-6.46251825217731,-2.00702437460911,
-0.206871309562622));
#47724=CARTESIAN_POINT('Ctrl Pts',(-6.4119521146099,-2.16984481222097,-0.19888507204693));
#47725=CARTESIAN_POINT('Ctrl Pts',(-6.35521217029182,-2.33080567695449,
-0.190898834531245));
#47726=CARTESIAN_POINT('Ctrl Pts',(-6.29247083559223,-2.48939747393245,
-0.182912597015552));
#47727=CARTESIAN_POINT('Ctrl Pts',(-6.26253342991367,-2.56507050489605,
-0.179101915692029));
#47728=CARTESIAN_POINT('Ctrl Pts',(-6.23123036841646,-2.64020438570276,
-0.175291234368502));
#47729=CARTESIAN_POINT('Ctrl Pts',(-6.1985843025168,-2.71474522646092,-0.171480553044979));
#47730=CARTESIAN_POINT('Ctrl Pts',(-6.12300021659017,-2.88732655158057,
-0.16265784021088));
#47731=CARTESIAN_POINT('Ctrl Pts',(-6.04027740399832,-3.05658346159284,
-0.153835127376766));
#47732=CARTESIAN_POINT('Ctrl Pts',(-5.950739396998,-3.22195431826957,-0.145012414542663));
#47733=CARTESIAN_POINT('Ctrl Pts',(-5.86104116092577,-3.38762110758734,
-0.136173913384289));
#47734=CARTESIAN_POINT('Ctrl Pts',(-5.7645034872635,-3.54938771430167,-0.127335412225904));
#47735=CARTESIAN_POINT('Ctrl Pts',(-5.66149380543021,-3.70672050350109,
-0.118496911067531));
#47736=CARTESIAN_POINT('Ctrl Pts',(-5.55819742015028,-3.86449119185844,
-0.109633810000682));
#47737=CARTESIAN_POINT('Ctrl Pts',(-5.44839312850079,-4.01780314579878,
-0.100770708933852));
#47738=CARTESIAN_POINT('Ctrl Pts',(-5.33249117548759,-4.166152525214,-0.0919076078670003));
#47739=CARTESIAN_POINT('Ctrl Pts',(-5.21643407329633,-4.3147004887228,-0.0830326424371255));
#47740=CARTESIAN_POINT('Ctrl Pts',(-5.09426317499926,-4.45827240387543,
-0.0741576770072431));
#47741=CARTESIAN_POINT('Ctrl Pts',(-4.96642729574578,-4.59639956009824,
-0.0652827115773675));
#47742=CARTESIAN_POINT('Ctrl Pts',(-4.83830328111168,-4.73483804770128,
-0.0563877424399488));
#47743=CARTESIAN_POINT('Ctrl Pts',(-4.7044889277927,-4.86780703436492,-0.0474927733025496));
#47744=CARTESIAN_POINT('Ctrl Pts',(-4.56547008504128,-4.99487456324913,
-0.0385978041651356));
#47745=CARTESIAN_POINT('Ctrl Pts',(-4.43063904179203,-5.11811431365618,
-0.0299707868146038));
#47746=CARTESIAN_POINT('Ctrl Pts',(-4.29091269533491,-5.23580287374704,
-0.021343769464066));
#47747=CARTESIAN_POINT('Ctrl Pts',(-4.14676186211144,-5.34758403944605,
-0.0127167521135334));
#47748=CARTESIAN_POINT('Ctrl Pts',(-4.00982403171967,-5.45377191201807,
-0.00452141246605009));
#47749=CARTESIAN_POINT('Ctrl Pts',(-3.86861282731891,-5.55484528617162,
0.00367392718142589));
#47750=CARTESIAN_POINT('Ctrl Pts',(-3.72354778978322,-5.65044076663056,
0.01186926682891));
#47751=CARTESIAN_POINT('Ctrl Pts',(-3.57863977833541,-5.74593276947304,
0.020055735406248));
#47752=CARTESIAN_POINT('Ctrl Pts',(-3.42988653875487,-5.83595848762258,
0.0282422039835867));
#47753=CARTESIAN_POINT('Ctrl Pts',(-3.27774058002029,-5.92019473413572,
0.0364286725609233));
#47754=CARTESIAN_POINT('Ctrl Pts',(-3.12572818164929,-6.00435703439484,
0.0446079546988116));
#47755=CARTESIAN_POINT('Ctrl Pts',(-2.97032930915141,-6.0827398094413,0.0527872368366991));
#47756=CARTESIAN_POINT('Ctrl Pts',(-2.81202539050201,-6.15506313559593,
0.0609665189745883));
#47757=CARTESIAN_POINT('Ctrl Pts',(-2.65382805791667,-6.22733776643879,
0.0691402939999721));
#47758=CARTESIAN_POINT('Ctrl Pts',(-2.49272990224806,-6.29356092426462,
0.0773140690253551));
#47759=CARTESIAN_POINT('Ctrl Pts',(-2.32923693719625,-6.35349858663718,
0.0854878440507392));
#47760=CARTESIAN_POINT('Ctrl Pts',(-2.16582061799092,-6.41340815010734,
0.0936577871931698));
#47761=CARTESIAN_POINT('Ctrl Pts',(-2.00001206442768,-6.46703796370879,
0.101827730335612));
#47762=CARTESIAN_POINT('Ctrl Pts',(-1.83233730168922,-6.5142021010127,0.109997673478041));
#47763=CARTESIAN_POINT('Ctrl Pts',(-1.66467846498493,-6.56136175858663,
0.118166840625374));
#47764=CARTESIAN_POINT('Ctrl Pts',(-1.49515411740455,-6.60205685664008,
0.126336007772689));
#47765=CARTESIAN_POINT('Ctrl Pts',(-1.32430580213373,-6.63615122962361,
0.134505174920022));
#47766=CARTESIAN_POINT('Ctrl Pts',(-1.15345997221496,-6.67024510663199,
0.142674223229448));
#47767=CARTESIAN_POINT('Ctrl Pts',(-0.981290567314751,-6.69773837790576,
0.150843271538878));
#47768=CARTESIAN_POINT('Ctrl Pts',(-0.808349536187398,-6.71854597568147,
0.159012319848301));
#47769=CARTESIAN_POINT('Ctrl Pts',(-0.635378980098935,-6.73935712578661,
0.167182762799772));
#47770=CARTESIAN_POINT('Ctrl Pts',(-0.461636894350587,-6.75348028543297,
0.175353205751246));
#47771=CARTESIAN_POINT('Ctrl Pts',(-0.287680581486563,-6.76088225626179,
0.183523648702717));
#47772=CARTESIAN_POINT('Ctrl Pts',(-0.113662340719825,-6.76828686216906,
0.191697000306298));
#47773=CARTESIAN_POINT('Ctrl Pts',(0.0605699180535765,-6.76896549814052,
0.199870351909894));
#47774=CARTESIAN_POINT('Ctrl Pts',(0.234458642070341,-6.76293709457352,
0.208043703513475));
#47775=CARTESIAN_POINT('Ctrl Pts',(0.408549242425096,-6.75690169232364,
0.216226543980122));
#47776=CARTESIAN_POINT('Ctrl Pts',(0.582295149546237,-6.74414370742732,
0.224409384446751));
#47777=CARTESIAN_POINT('Ctrl Pts',(0.755142638418673,-6.7247340910732,0.232592224913397));
#47778=CARTESIAN_POINT('Ctrl Pts',(0.928093459013221,-6.70531287125816,
0.240779957247449));
#47779=CARTESIAN_POINT('Ctrl Pts',(1.10014443411077,-6.67923214884072,0.24896768958151));
#47780=CARTESIAN_POINT('Ctrl Pts',(1.27075197801329,-6.64661405607211,0.257155421915563));
#47781=CARTESIAN_POINT('Ctrl Pts',(1.44163107605683,-6.61394404544593,0.26535618657263));
#47782=CARTESIAN_POINT('Ctrl Pts',(1.61106179982824,-6.57471595244428,0.273556951229701));
#47783=CARTESIAN_POINT('Ctrl Pts',(1.77851437334723,-6.52910220656694,0.281757715886769));
#47784=CARTESIAN_POINT('Ctrl Pts',(1.93542277373969,-6.48636067234556,0.289442093841041));
#47785=CARTESIAN_POINT('Ctrl Pts',(2.09059423390549,-6.43801290758808,0.2971264717953));
#47786=CARTESIAN_POINT('Ctrl Pts',(2.24360986589362,-6.38423869930196,0.304810849749572));
#47787=CARTESIAN_POINT('Ctrl Pts',(2.40603247148264,-6.32715860291028,0.312967641793932));
#47788=CARTESIAN_POINT('Ctrl Pts',(2.56654333132276,-6.26378195897024,0.321124433838292));
#47789=CARTESIAN_POINT('Ctrl Pts',(2.72461256508535,-6.19425341507587,0.329281225882653));
#47790=CARTESIAN_POINT('Ctrl Pts',(2.88248672069836,-6.12481067851644,0.337427951376676));
#47791=CARTESIAN_POINT('Ctrl Pts',(3.03792491751405,-6.04923130013865,0.345574676870704));
#47792=CARTESIAN_POINT('Ctrl Pts',(3.19041215785423,-5.96770971671846,0.353721402364727));
#47793=CARTESIAN_POINT('Ctrl Pts',(3.34274326961125,-5.88627160158904,0.361859786592254));
#47794=CARTESIAN_POINT('Ctrl Pts',(3.49212912016178,-5.79890356470488,0.369998170819779));
#47795=CARTESIAN_POINT('Ctrl Pts',(3.63807444548162,-5.70584816912732,0.378136555047305));
#47796=CARTESIAN_POINT('Ctrl Pts',(3.78390100651039,-5.6128684981957,0.386268316593145));
#47797=CARTESIAN_POINT('Ctrl Pts',(3.92629231027381,-5.51421087925476,0.394400078138987));
#47798=CARTESIAN_POINT('Ctrl Pts',(4.06477748702086,-5.41016385897954,0.402531839684826));
#47799=CARTESIAN_POINT('Ctrl Pts',(4.2031790566202,-5.30617965463017,0.4106586918721));
#47800=CARTESIAN_POINT('Ctrl Pts',(4.33767890412596,-5.1968127475801,0.41878554405939));
#47801=CARTESIAN_POINT('Ctrl Pts',(4.46783497657259,-5.08239506749668,0.426912396246664));
#47802=CARTESIAN_POINT('Ctrl Pts',(4.59824569830731,-4.96775353016073,0.435055148553578));
#47803=CARTESIAN_POINT('Ctrl Pts',(4.72429532883956,-4.84804164851499,0.443197900860493));
#47804=CARTESIAN_POINT('Ctrl Pts',(4.84557192025978,-4.72363438102379,0.451340653167406));
#47805=CARTESIAN_POINT('Ctrl Pts',(4.96656198496555,-4.5995210367472,0.459464167499062));
#47806=CARTESIAN_POINT('Ctrl Pts',(5.08280128871719,-4.47073473738736,0.467587681830721));
#47807=CARTESIAN_POINT('Ctrl Pts',(5.19391741158416,-4.33768497261419,0.475711196162379));
#47808=CARTESIAN_POINT('Ctrl Pts',(5.30504043323385,-4.20462694728084,0.48383521485253));
#47809=CARTESIAN_POINT('Ctrl Pts',(5.41103940589524,-4.06730520998406,0.491959233542661));
#47810=CARTESIAN_POINT('Ctrl Pts',(5.51158212918542,-3.92616243082783,0.500083252232812));
#47811=CARTESIAN_POINT('Ctrl Pts',(5.61215021905236,-3.78498404184303,0.50820932058441));
#47812=CARTESIAN_POINT('Ctrl Pts',(5.70725910641704,-3.63998298928229,0.516335388936017));
#47813=CARTESIAN_POINT('Ctrl Pts',(5.79661988945616,-3.49163097379452,0.524461457287615));
#47814=CARTESIAN_POINT('Ctrl Pts',(5.88631440177505,-3.34272491872029,0.532617873481364));
#47815=CARTESIAN_POINT('Ctrl Pts',(5.97021760322336,-3.19044314194321,0.540774289675092));
#47816=CARTESIAN_POINT('Ctrl Pts',(6.04808420343757,-3.03528688399119,0.548930705868841));
#47817=CARTESIAN_POINT('Ctrl Pts',(6.12578114329155,-2.88046868968318,0.55706935037992));
#47818=CARTESIAN_POINT('Ctrl Pts',(6.19746765311683,-2.72278888060113,0.565207994891024));
#47819=CARTESIAN_POINT('Ctrl Pts',(6.26294878048974,-2.56276443961635,0.573346639402104));
#47820=CARTESIAN_POINT('Ctrl Pts',(6.32864438641896,-2.40221585049219,0.581511941437192));
#47821=CARTESIAN_POINT('Ctrl Pts',(6.38809378152727,-2.23930759778346,0.589677243472273));
#47822=CARTESIAN_POINT('Ctrl Pts',(6.44115090277373,-2.0745756307489,0.597842545507362));
#47823=CARTESIAN_POINT('Ctrl Pts',(6.49420802402017,-1.9098436637144,0.606007847542448));
#47824=CARTESIAN_POINT('Ctrl Pts',(6.54087282947605,-1.74328834989732,0.614173149577535));
#47825=CARTESIAN_POINT('Ctrl Pts',(6.58105109452538,-1.5754540587546,0.62233845161262));
#47826=CARTESIAN_POINT('Ctrl Pts',(6.62169554697867,-1.40567239053157,0.630598495442894));
#47827=CARTESIAN_POINT('Ctrl Pts',(6.65581859810969,-1.23409558594309,0.638858539273176));
#47828=CARTESIAN_POINT('Ctrl Pts',(6.68326332567506,-1.06126354864695,0.647118583103449));
#47829=CARTESIAN_POINT('Ctrl Pts',(6.71067819738982,-0.888619527335835,
0.655369641213821));
#47830=CARTESIAN_POINT('Ctrl Pts',(6.73142915937007,-0.714723340715225,
0.663620699324172));
#47831=CARTESIAN_POINT('Ctrl Pts',(6.74540960430284,-0.540128012770085,
0.671871757434545));
#47832=CARTESIAN_POINT('Ctrl Pts',(6.75937757270251,-0.365688498491826,
0.680115452073999));
#47833=CARTESIAN_POINT('Ctrl Pts',(6.76658703108541,-0.190551437647277,
0.688359146713446));
#47834=CARTESIAN_POINT('Ctrl Pts',(6.76698275302029,-0.0152780995526872,
0.696602841352899));
#47835=CARTESIAN_POINT('Ctrl Pts',(6.76737819911042,0.159873061259471,0.704840789583804));
#47836=CARTESIAN_POINT('Ctrl Pts',(6.76096936991359,0.335159956271986,0.713078737814734));
#47837=CARTESIAN_POINT('Ctrl Pts',(6.74775300467988,0.51001802696937,0.72131668604564));
#47838=CARTESIAN_POINT('Ctrl Pts',(6.73454327084701,0.684788361444416,0.729550500830175));
#47839=CARTESIAN_POINT('Ctrl Pts',(6.71453283348665,0.859129946988257,0.7377843156147));
#47840=CARTESIAN_POINT('Ctrl Pts',(6.68777049571708,1.03247992552696,0.746018130399236));
#47841=CARTESIAN_POINT('Ctrl Pts',(6.6610128684915,1.20579939205632,0.754250495917751));
#47842=CARTESIAN_POINT('Ctrl Pts',(6.62750575669221,1.37812724775876,0.762482861436278));
#47843=CARTESIAN_POINT('Ctrl Pts',(6.58734968078777,1.54890709309026,0.770715226954792));
#47844=CARTESIAN_POINT('Ctrl Pts',(6.54719622948158,1.71967577626327,0.778947054406483));
#47845=CARTESIAN_POINT('Ctrl Pts',(6.50039476023779,1.88889630470125,0.78717888185817));
#47846=CARTESIAN_POINT('Ctrl Pts',(6.44709664380496,2.05602379982304,0.795410709309863));
#47847=CARTESIAN_POINT('Ctrl Pts',(6.39379257744239,2.22316995220555,0.803643455720766));
#47848=CARTESIAN_POINT('Ctrl Pts',(6.33399052677082,2.38822226729607,0.811876202131666));
#47849=CARTESIAN_POINT('Ctrl Pts',(6.26789136840603,2.55065222910948,0.820108948542568));
#47850=CARTESIAN_POINT('Ctrl Pts',(6.2017731318378,2.71312907309105,0.828344071171487));
#47851=CARTESIAN_POINT('Ctrl Pts',(6.12935430059118,2.87298172707546,0.836579193800416));
#47852=CARTESIAN_POINT('Ctrl Pts',(6.05088344068903,3.0297027225778,0.844814316429336));
#47853=CARTESIAN_POINT('Ctrl Pts',(5.97233329027532,3.18658207607343,0.853057760199208));
#47854=CARTESIAN_POINT('Ctrl Pts',(5.88771905286392,3.3403231310681,0.861301203969076));
#47855=CARTESIAN_POINT('Ctrl Pts',(5.79733520580429,3.49044316835874,0.869544647738948));
#47856=CARTESIAN_POINT('Ctrl Pts',(5.70690374895223,3.64064228154674,0.877792433752036));
#47857=CARTESIAN_POINT('Ctrl Pts',(5.61069681733334,3.78721627718881,0.886040219765133));
#47858=CARTESIAN_POINT('Ctrl Pts',(5.50905157702439,3.92971242226261,0.894288005778222));
#47859=CARTESIAN_POINT('Ctrl Pts',(5.40726414965501,4.07240789893255,0.902547329256762));
#47860=CARTESIAN_POINT('Ctrl Pts',(5.30002342783129,4.2110138442777,0.910806652735291));
#47861=CARTESIAN_POINT('Ctrl Pts',(5.18770691809457,4.34511057764399,0.91906597621383));
#47862=CARTESIAN_POINT('Ctrl Pts',(5.09342187217554,4.45767921686428,0.925999335301106));
#47863=CARTESIAN_POINT('Ctrl Pts',(4.99556072735516,4.56707079875741,0.932932694388378));
#47864=CARTESIAN_POINT('Ctrl Pts',(4.89436596278416,4.67305797335534,0.939866053475654));
#47865=CARTESIAN_POINT('Ctrl Pts',(4.77535419221126,4.79770593671977,0.948020144692652));
#47866=CARTESIAN_POINT('Ctrl Pts',(4.65139416642594,4.91799660289649,0.956174235909639));
#47867=CARTESIAN_POINT('Ctrl Pts',(4.52283974904205,5.03350867730307,0.964328327126637));
#47868=CARTESIAN_POINT('Ctrl Pts',(4.39446997400465,5.14885484204353,0.972470706645458));
#47869=CARTESIAN_POINT('Ctrl Pts',(4.261519223839,5.25943584696624,0.980613086164297));
#47870=CARTESIAN_POINT('Ctrl Pts',(4.12437998102941,5.36486521471731,0.988755465683113));
#47871=CARTESIAN_POINT('Ctrl Pts',(3.98735447350243,5.47020714550512,0.99689109238766));
#47872=CARTESIAN_POINT('Ctrl Pts',(3.84614767331955,5.57040571944288,1.00502671909223));
#47873=CARTESIAN_POINT('Ctrl Pts',(3.70118757133341,5.6651124933056,1.01316234579679));
#47874=CARTESIAN_POINT('Ctrl Pts',(3.55634029040894,5.75974555779153,1.02129164062085));
#47875=CARTESIAN_POINT('Ctrl Pts',(3.40774583104385,5.84889513669293,1.02942093544488));
#47876=CARTESIAN_POINT('Ctrl Pts',(3.25586358768148,5.93225431841976,1.03755023026893));
#47877=CARTESIAN_POINT('Ctrl Pts',(3.20398124987265,5.9607294655474,1.04032716331174));
#47878=CARTESIAN_POINT('Ctrl Pts',(3.15171552704348,5.98852930994894,1.04310409635457));
#47879=CARTESIAN_POINT('Ctrl Pts',(3.09908550384726,6.0156427786101,1.04588102939738));
#47880=CARTESIAN_POINT('Ctrl Pts',(3.0990855038472,6.01564277861013,-0.954225446716826));
#47881=CARTESIAN_POINT('Ctrl Pts',(2.92900571023975,6.10326297852299,-0.945195402684114));
#47882=CARTESIAN_POINT('Ctrl Pts',(2.75515599357988,6.18369314046508,-0.936165358651385));
#47883=CARTESIAN_POINT('Ctrl Pts',(2.57813708152171,6.2566363318386,-0.927135314618674));
#47884=CARTESIAN_POINT('Ctrl Pts',(2.40129499313276,6.32950666047336,-0.918114290670318));
#47885=CARTESIAN_POINT('Ctrl Pts',(2.22129025081137,6.39490485694901,-0.909093266721976));
#47886=CARTESIAN_POINT('Ctrl Pts',(2.03874463708718,6.45258160000695,-0.900072242773618));
#47887=CARTESIAN_POINT('Ctrl Pts',(1.85652788528628,6.51015443651647,-0.891067470496419));
#47888=CARTESIAN_POINT('Ctrl Pts',(1.67177963047401,6.56003352206036,-0.882062698219208));
#47889=CARTESIAN_POINT('Ctrl Pts',(1.48513782241612,6.60201898273771,-0.873057925942007));
#47890=CARTESIAN_POINT('Ctrl Pts',(1.29873687580939,6.64395026113356,-0.864064774332975));
#47891=CARTESIAN_POINT('Ctrl Pts',(1.1104474857551,6.67800818943961,-0.855071622723939));
#47892=CARTESIAN_POINT('Ctrl Pts',(0.920921277242054,6.70404303395517,-0.846078471114907));
#47893=CARTESIAN_POINT('Ctrl Pts',(0.731796195377596,6.7300227764877,-0.837104353246874));
#47894=CARTESIAN_POINT('Ctrl Pts',(0.541439757278538,6.74801329436519,-0.828130235378856));
#47895=CARTESIAN_POINT('Ctrl Pts',(0.350512111891381,6.75791611811048,-0.819156117510822));
#47896=CARTESIAN_POINT('Ctrl Pts',(0.261011179120108,6.76255825340983,-0.814949330597593));
#47897=CARTESIAN_POINT('Ctrl Pts',(0.171384886256927,6.76542389053578,-0.810742543684355));
#47898=CARTESIAN_POINT('Ctrl Pts',(0.0817019711920329,6.76650676404771,
-0.806535756771126));
#47899=CARTESIAN_POINT('Ctrl Pts',(-0.0917704497586113,6.76860135128945,
-0.798398627087806));
#47900=CARTESIAN_POINT('Ctrl Pts',(-0.265375328847117,6.76402127081696,
-0.790261497404494));
#47901=CARTESIAN_POINT('Ctrl Pts',(-0.438558221892025,6.75277392528514,
-0.782124367721174));
#47902=CARTESIAN_POINT('Ctrl Pts',(-0.61173098952734,6.74152723734704,-0.773987713787909));
#47903=CARTESIAN_POINT('Ctrl Pts',(-0.784481456414752,6.72361408456344,
-0.765851059854628));
#47904=CARTESIAN_POINT('Ctrl Pts',(-0.956258271735937,6.69909390274063,
-0.757714405921362));
#47905=CARTESIAN_POINT('Ctrl Pts',(-1.12805752486441,6.67457051804602,-0.749576689163218));
#47906=CARTESIAN_POINT('Ctrl Pts',(-1.298882512385,6.64343843838427,-0.741438972405071));
#47907=CARTESIAN_POINT('Ctrl Pts',(-1.46819009767355,6.60580856800236,-0.733301255646928));
#47908=CARTESIAN_POINT('Ctrl Pts',(-1.63762256907882,6.56815094075192,-0.725157536276185));
#47909=CARTESIAN_POINT('Ctrl Pts',(-1.80553504645514,6.52398602910561,-0.717013816905453));
#47910=CARTESIAN_POINT('Ctrl Pts',(-1.97139698273959,6.4734753368222,-0.708870097534707));
#47911=CARTESIAN_POINT('Ctrl Pts',(-2.13732761100616,6.42294372545602,-0.700723005429758));
#47912=CARTESIAN_POINT('Ctrl Pts',(-2.30120566108843,6.36606121397866,-0.692575913324796));
#47913=CARTESIAN_POINT('Ctrl Pts',(-2.46251891230449,6.30303812510624,-0.684428821219846));
#47914=CARTESIAN_POINT('Ctrl Pts',(-2.62400769448509,6.23994645846047,-0.676272863960146));
#47915=CARTESIAN_POINT('Ctrl Pts',(-2.78292576961112,6.17070101395603,-0.668116906700458));
#47916=CARTESIAN_POINT('Ctrl Pts',(-2.93878324221061,6.09555920775954,-0.659960949440759));
#47917=CARTESIAN_POINT('Ctrl Pts',(-3.01642570140689,6.05812632421383,-0.655897951573662));
#47918=CARTESIAN_POINT('Ctrl Pts',(-3.09330902488021,6.01923086615666,-0.651834953706578));
#47919=CARTESIAN_POINT('Ctrl Pts',(-3.16937523825415,5.97890872978853,-0.647771955839481));
#47920=CARTESIAN_POINT('Ctrl Pts',(-3.32713024121956,5.89528397103979,-0.639345636030166));
#47921=CARTESIAN_POINT('Ctrl Pts',(-3.48169452813347,5.80534763426989,-0.630919316220838));
#47922=CARTESIAN_POINT('Ctrl Pts',(-3.63254823534196,5.70936794381953,-0.622492996411523));
#47923=CARTESIAN_POINT('Ctrl Pts',(-3.78328574887108,5.61346218084225,-0.614073166897478));
#47924=CARTESIAN_POINT('Ctrl Pts',(-3.93031809795312,5.51152252199718,-0.605653337383427));
#47925=CARTESIAN_POINT('Ctrl Pts',(-4.07315087405494,5.40386259606825,-0.597233507869383));
#47926=CARTESIAN_POINT('Ctrl Pts',(-4.2158961409155,5.29626863005895,-0.588818836925468));
#47927=CARTESIAN_POINT('Ctrl Pts',(-4.35444669709763,5.18296158477958,-0.580404165981556));
#47928=CARTESIAN_POINT('Ctrl Pts',(-4.4883376319278,5.06429800681405,-0.571989495037641));
#47929=CARTESIAN_POINT('Ctrl Pts',(-4.62216761181995,4.94568845140838,-0.563578654941174));
#47930=CARTESIAN_POINT('Ctrl Pts',(-4.75134194942648,4.82172744728789,-0.555167814844717));
#47931=CARTESIAN_POINT('Ctrl Pts',(-4.87542902751879,4.69281160900661,-0.546756974748249));
#47932=CARTESIAN_POINT('Ctrl Pts',(-4.99947913152118,4.5639341836356,-0.538348640820536));
#47933=CARTESIAN_POINT('Ctrl Pts',(-5.11844476660789,4.43010510941468,-0.529940306892819));
#47934=CARTESIAN_POINT('Ctrl Pts',(-5.23193112488908,4.29175788045143,-0.521531972965107));
#47935=CARTESIAN_POINT('Ctrl Pts',(-5.34542017002875,4.15340737603347,-0.51312343996498));
#47936=CARTESIAN_POINT('Ctrl Pts',(-5.45342946142394,4.01053875793179,-0.504714906964856));
#47937=CARTESIAN_POINT('Ctrl Pts',(-5.55560403496423,3.86361913323366,-0.496306373964728));
#47938=CARTESIAN_POINT('Ctrl Pts',(-5.65778282591142,3.71669344421036,-0.487897493889944));
#47939=CARTESIAN_POINT('Ctrl Pts',(-5.75412622721796,3.56571669032804,-0.479488613815146));
#47940=CARTESIAN_POINT('Ctrl Pts',(-5.84432216496291,3.41118563436868,-0.47107973374036));
#47941=CARTESIAN_POINT('Ctrl Pts',(-5.9345347280865,3.25662609445114,-0.462669303697597));
#47942=CARTESIAN_POINT('Ctrl Pts',(-6.01859739958445,3.09851123585628,-0.454258873654861));
#47943=CARTESIAN_POINT('Ctrl Pts',(-6.09624352368068,2.93736342660922,-0.4458484436121));
#47944=CARTESIAN_POINT('Ctrl Pts',(-6.17391507030227,2.77616285511141,-0.437435259866257));
#47945=CARTESIAN_POINT('Ctrl Pts',(-6.24516573563743,2.61192765508278,-0.42902207612041));
#47946=CARTESIAN_POINT('Ctrl Pts',(-6.30977642014614,2.44520153111513,-0.420608892374567));
#47947=CARTESIAN_POINT('Ctrl Pts',(-6.3744472030143,2.27832032495629,-0.412187883010642));
#47948=CARTESIAN_POINT('Ctrl Pts',(-6.43246554287891,2.10894387818012,-0.403766873646707));
#47949=CARTESIAN_POINT('Ctrl Pts',(-6.48366140323119,1.93763355881604,-0.395345864282781));
#47950=CARTESIAN_POINT('Ctrl Pts',(-6.53488294260128,1.76623731295888,-0.386920631076383));
#47951=CARTESIAN_POINT('Ctrl Pts',(-6.57927509001139,1.59290558337106,-0.378495397869984));
#47952=CARTESIAN_POINT('Ctrl Pts',(-6.61671853072273,1.4182118618847,-0.370070164663588));
#47953=CARTESIAN_POINT('Ctrl Pts',(-6.65420523124043,1.2433163102134,-0.361635197470407));
#47954=CARTESIAN_POINT('Ctrl Pts',(-6.68472712177001,1.06705595191768,-0.353200230277231));
#47955=CARTESIAN_POINT('Ctrl Pts',(-6.70821634980292,0.890012586560914,
-0.344765263084049));
#47956=CARTESIAN_POINT('Ctrl Pts',(-6.72169535679295,0.788418410888559,
-0.339924960048193));
#47957=CARTESIAN_POINT('Ctrl Pts',(-6.73285953853334,0.686566488305788,
-0.335084657012332));
#47958=CARTESIAN_POINT('Ctrl Pts',(-6.74170381834428,0.5845670412555,-0.330244353976475));
#47959=CARTESIAN_POINT('Ctrl Pts',(-6.75840709403868,0.391931244878789,
-0.321102974714318));
#47960=CARTESIAN_POINT('Ctrl Pts',(-6.76686237902982,0.198465732430607,
-0.311961595452164));
#47961=CARTESIAN_POINT('Ctrl Pts',(-6.76699833344597,0.00474922514552044,
-0.302820216190007));
#47962=CARTESIAN_POINT('',(-6.76699942930229,-0.00277917658345995,-0.697179783782191));
#47963=CARTESIAN_POINT('Ctrl Pts',(3.09908550384728,6.01564277861008,-1.34871979865154));
#47964=CARTESIAN_POINT('Ctrl Pts',(2.94374847892273,6.09566792968225,-1.34050698664135));
#47965=CARTESIAN_POINT('Ctrl Pts',(2.78541162564976,6.16962008736427,-1.33229417463114));
#47966=CARTESIAN_POINT('Ctrl Pts',(2.62459578153322,6.23728995506526,-1.32408136262094));
#47967=CARTESIAN_POINT('Ctrl Pts',(2.46368013222434,6.30500181989781,-1.31586345359256));
#47968=CARTESIAN_POINT('Ctrl Pts',(2.30028276042722,6.36642349734732,-1.30764554456416));
#47969=CARTESIAN_POINT('Ctrl Pts',(2.1349406106516,6.42139529923136,-1.29942763553576));
#47970=CARTESIAN_POINT('Ctrl Pts',(1.96935243679418,6.47644889748191,-1.29119749850909));
#47971=CARTESIAN_POINT('Ctrl Pts',(1.80181404729578,6.52503334608869,-1.28296736148243));
#47972=CARTESIAN_POINT('Ctrl Pts',(1.63287470142026,6.5670396077275,-1.27473722445576));
#47973=CARTESIAN_POINT('Ctrl Pts',(1.51420469579376,6.5965465486902,-1.26895603475006));
#47974=CARTESIAN_POINT('Ctrl Pts',(1.39484363862823,6.62280872975009,-1.26317484504439));
#47975=CARTESIAN_POINT('Ctrl Pts',(1.27498338669229,6.64580366574718,-1.2573936553387));
#47976=CARTESIAN_POINT('Ctrl Pts',(1.10764786172967,6.67790663253063,-1.24932260260283));
#47977=CARTESIAN_POINT('Ctrl Pts',(0.938793560500144,6.70374396058503,-1.24125154986695));
#47978=CARTESIAN_POINT('Ctrl Pts',(0.768940524153764,6.72317034369308,-1.23318049713107));
#47979=CARTESIAN_POINT('Ctrl Pts',(0.599298848692328,6.74257255309419,-1.22511948781206));
#47980=CARTESIAN_POINT('Ctrl Pts',(0.428661276890571,6.75557964920356,-1.21705847849305));
#47981=CARTESIAN_POINT('Ctrl Pts',(0.257560676775405,6.76209667912098,-1.20899746917404));
#47982=CARTESIAN_POINT('Ctrl Pts',(0.0866354732782866,6.76860702837798,
-1.20094472326129));
#47983=CARTESIAN_POINT('Ctrl Pts',(-0.0847514443693596,6.76864053714096,
-1.19289197734856));
#47984=CARTESIAN_POINT('Ctrl Pts',(-0.256059497801806,6.76215369047358,
-1.18483923143582));
#47985=CARTESIAN_POINT('Ctrl Pts',(-0.427229449118924,6.75567207325823,
-1.17679297734423));
#47986=CARTESIAN_POINT('Ctrl Pts',(-0.598320291927199,6.74268057687285,
-1.16874672325262));
#47987=CARTESIAN_POINT('Ctrl Pts',(-0.768788941225106,6.72318767876147,
-1.16070046916104));
#47988=CARTESIAN_POINT('Ctrl Pts',(-0.9391574503223,6.70370623156928,-1.15265894176555));
#47989=CARTESIAN_POINT('Ctrl Pts',(-1.10890412388516,6.67773102786735,-1.14461741437007));
#47990=CARTESIAN_POINT('Ctrl Pts',(-1.27748860541604,6.64532255522877,-1.13657588697458));
#47991=CARTESIAN_POINT('Ctrl Pts',(-1.44931658276778,6.61229055695717,-1.12837964391212));
#47992=CARTESIAN_POINT('Ctrl Pts',(-1.61993679679775,6.57257523889413,-1.12018340084964));
#47993=CARTESIAN_POINT('Ctrl Pts',(-1.78878499137808,6.52629582953612,-1.11198715778718));
#47994=CARTESIAN_POINT('Ctrl Pts',(-1.95439325914239,6.48090444802929,-1.10394818752089));
#47995=CARTESIAN_POINT('Ctrl Pts',(-2.1182965290554,6.4291987268512,-1.0959092172546));
#47996=CARTESIAN_POINT('Ctrl Pts',(-2.27997544670536,6.37134216334523,-1.0878702469883));
#47997=CARTESIAN_POINT('Ctrl Pts',(-2.44167165546222,6.31347941224203,-1.07983041697668));
#47998=CARTESIAN_POINT('Ctrl Pts',(-2.6011426866065,6.24946463474063,-1.07179058696506));
#47999=CARTESIAN_POINT('Ctrl Pts',(-2.75788731040707,6.17951022194281,-1.06375075695344));
#48000=CARTESIAN_POINT('Ctrl Pts',(-2.91467973129993,6.10953447752006,-1.05570847530751));
#48001=CARTESIAN_POINT('Ctrl Pts',(-3.06874374914964,6.03361564470674,-1.04766619366157));
#48002=CARTESIAN_POINT('Ctrl Pts',(-3.21960110107852,5.95201291580705,-1.03962391201564));
#48003=CARTESIAN_POINT('Ctrl Pts',(-3.37553950094233,5.86766171378452,-1.03131075713731));
#48004=CARTESIAN_POINT('Ctrl Pts',(-3.52805106989464,5.77723725642645,-1.02299760225897));
#48005=CARTESIAN_POINT('Ctrl Pts',(-3.67663933634794,5.68107491505076,-1.01468444738064));
#48006=CARTESIAN_POINT('Ctrl Pts',(-3.82063922158787,5.58788205095032,-1.00662800135676));
#48007=CARTESIAN_POINT('Ctrl Pts',(-3.96095424620564,5.48930067774289,-0.998571555332877));
#48008=CARTESIAN_POINT('Ctrl Pts',(-4.09716604848102,5.38567724350192,-0.990515109309001));
#48009=CARTESIAN_POINT('Ctrl Pts',(-4.23988818588854,5.27710105719995,-0.982073600003433));
#48010=CARTESIAN_POINT('Ctrl Pts',(-4.37810486731001,5.16298931304757,-0.973632090697874));
#48011=CARTESIAN_POINT('Ctrl Pts',(-4.51137852757536,5.04378357792362,-0.965190581392307));
#48012=CARTESIAN_POINT('Ctrl Pts',(-4.64465218784067,4.92457784279971,-0.956749072086742));
#48013=CARTESIAN_POINT('Ctrl Pts',(-4.77298255617914,4.80027849925549,-0.94830756278117));
#48014=CARTESIAN_POINT('Ctrl Pts',(-4.89598113101639,4.67136572799984,-0.939866053475605));
#48015=CARTESIAN_POINT('Ctrl Pts',(-5.01696362412722,4.54456597864526,-0.931562909778558));
#48016=CARTESIAN_POINT('Ctrl Pts',(-5.13317976522407,4.41289279758091,-0.923259766081505));
#48017=CARTESIAN_POINT('Ctrl Pts',(-5.24421808414461,4.27673540050477,-0.914956622384459));
#48018=CARTESIAN_POINT('Ctrl Pts',(-5.35512072254373,4.14074437758496,-0.906663624508037));
#48019=CARTESIAN_POINT('Ctrl Pts',(-5.46085792174848,4.00028032354014,-0.898370626631615));
#48020=CARTESIAN_POINT('Ctrl Pts',(-5.56105499227057,3.8557692323248,-0.890077628755193));
#48021=CARTESIAN_POINT('Ctrl Pts',(-5.66112294863427,3.71144435840927,-0.881795317253492));
#48022=CARTESIAN_POINT('Ctrl Pts',(-5.75566480980538,3.56308313093797,-0.873513005751797));
#48023=CARTESIAN_POINT('Ctrl Pts',(-5.84434627259084,3.41114433087396,-0.865230694250094));
#48024=CARTESIAN_POINT('Ctrl Pts',(-5.93296115248566,3.25931960791458,-0.856954601187101));
#48025=CARTESIAN_POINT('Ctrl Pts',(-6.01572422155528,3.10392296416771,-0.848678508124099));
#48026=CARTESIAN_POINT('Ctrl Pts',(-6.09234417361033,2.94544249142235,-0.840402415061106));
#48027=CARTESIAN_POINT('Ctrl Pts',(-6.16891973497529,2.78705383624359,-0.832131116852098));
#48028=CARTESIAN_POINT('Ctrl Pts',(-6.2393591169355,2.6255852264934,-0.823859818643093));
#48029=CARTESIAN_POINT('Ctrl Pts',(-6.30341664058509,2.46154984820437,-0.815588520434083));
#48030=CARTESIAN_POINT('Ctrl Pts',(-6.36744803186293,2.29758138841675,-0.807320596514733));
#48031=CARTESIAN_POINT('Ctrl Pts',(-6.42510262495094,2.13104857317411,-0.79905267259539));
#48032=CARTESIAN_POINT('Ctrl Pts',(-6.47618257374036,1.96248522837287,-0.790784748676039));
#48033=CARTESIAN_POINT('Ctrl Pts',(-6.52725782163957,1.79393739646454,-0.782517585654132));
#48034=CARTESIAN_POINT('Ctrl Pts',(-6.57175952260472,1.62335974133626,-0.774250422632216));
#48035=CARTESIAN_POINT('Ctrl Pts',(-6.60953936200882,1.45130231931742,-0.765983259610309));
#48036=CARTESIAN_POINT('Ctrl Pts',(-6.64731619469459,1.27925859053315,-0.757716754532716));
#48037=CARTESIAN_POINT('Ctrl Pts',(-6.67837215988471,1.10573567334515,-0.74945024945513));
#48038=CARTESIAN_POINT('Ctrl Pts',(-6.70260986472482,0.931294798274735,
-0.741183744377537));
#48039=CARTESIAN_POINT('Ctrl Pts',(-6.72685689179225,0.756786830321425,
-0.732914059863605));
#48040=CARTESIAN_POINT('Ctrl Pts',(-6.74428037073407,0.581360547257899,
-0.724644375349675));
#48041=CARTESIAN_POINT('Ctrl Pts',(-6.75483461391262,0.405583947769132,
-0.716374690835742));
#48042=CARTESIAN_POINT('Ctrl Pts',(-6.76300049239713,0.269584584521214,
-0.709976388493866));
#48043=CARTESIAN_POINT('Ctrl Pts',(-6.76705534748704,0.133375685775319,
-0.70357808615199));
#48044=CARTESIAN_POINT('Ctrl Pts',(-6.76699942930254,-0.00277917598916038,
-0.697179783810114));
#48045=CARTESIAN_POINT('Ctrl Pts',(-6.76699942930229,-0.00277917658345176,
-0.697179783782168));
#48046=CARTESIAN_POINT('Ctrl Pts',(-6.76690970559949,-0.221246851251606,
-0.686913369374764));
#48047=CARTESIAN_POINT('Ctrl Pts',(-6.75623640357004,-0.439364788743829,
-0.676646954967357));
#48048=CARTESIAN_POINT('Ctrl Pts',(-6.7351046007485,-0.656243108136276,
-0.666380540559935));
#48049=CARTESIAN_POINT('Ctrl Pts',(-6.7137419144094,-0.875491013772146,
-0.656001956552447));
#48050=CARTESIAN_POINT('Ctrl Pts',(-6.68169095530472,-1.09347220153135,
-0.645623372544961));
#48051=CARTESIAN_POINT('Ctrl Pts',(-6.63913111398288,-1.30928493894359,
-0.63524478853747));
#48052=CARTESIAN_POINT('Ctrl Pts',(-6.62148928374299,-1.39874325360786,
-0.630942676229158));
#48053=CARTESIAN_POINT('Ctrl Pts',(-6.60204235066164,-1.48782916916932,
-0.62664056392084));
#48054=CARTESIAN_POINT('Ctrl Pts',(-6.58080558754353,-1.5764792478672,-0.622338451612528));
#48055=CARTESIAN_POINT('Ctrl Pts',(-6.53908299118297,-1.75064474711359,
-0.613886349268152));
#48056=CARTESIAN_POINT('Ctrl Pts',(-6.49040676320739,-1.92330031190699,
-0.605434246923772));
#48057=CARTESIAN_POINT('Ctrl Pts',(-6.4349041551301,-2.09387141780229,-0.5969821445794));
#48058=CARTESIAN_POINT('Ctrl Pts',(-6.3794505223416,-2.26429201240706,-0.588537500337764));
#48059=CARTESIAN_POINT('Ctrl Pts',(-6.31718261765681,-2.43263150061118,
-0.580092856096124));
#48060=CARTESIAN_POINT('Ctrl Pts',(-6.24827810907183,-2.59832824556363,
-0.571648211854487));
#48061=CARTESIAN_POINT('Ctrl Pts',(-6.17942505415503,-2.7639012583321,-0.563209873556128));
#48062=CARTESIAN_POINT('Ctrl Pts',(-6.10394540134535,-2.92683515686584,
-0.554771535257758));
#48063=CARTESIAN_POINT('Ctrl Pts',(-6.02206588901574,-3.08658572347393,
-0.546333196959402));
#48064=CARTESIAN_POINT('Ctrl Pts',(-5.94024510928763,-3.24622170016688,
-0.537900911525146));
#48065=CARTESIAN_POINT('Ctrl Pts',(-5.85203377767385,-3.40267860546137,
-0.529468626090902));
#48066=CARTESIAN_POINT('Ctrl Pts',(-5.75770585330553,-3.55543419385189,
-0.521036340656643));
#48067=CARTESIAN_POINT('Ctrl Pts',(-5.66341858833023,-3.70812393801288,
-0.51260768990013));
#48068=CARTESIAN_POINT('Ctrl Pts',(-5.56302016037904,-3.85711526441339,
-0.504179039143616));
#48069=CARTESIAN_POINT('Ctrl Pts',(-5.45682970571519,-4.0019118634503,-0.495750388387101));
#48070=CARTESIAN_POINT('Ctrl Pts',(-5.3506723618518,-4.14666331406674,-0.487324365732841));
#48071=CARTESIAN_POINT('Ctrl Pts',(-5.23872678862464,-4.2872223788229,-0.478898343078576));
#48072=CARTESIAN_POINT('Ctrl Pts',(-5.12135475846663,-4.42312270211118,
-0.470472320424314));
#48073=CARTESIAN_POINT('Ctrl Pts',(-5.08932725136838,-4.4602060563218,-0.468173097176611));
#48074=CARTESIAN_POINT('Ctrl Pts',(-5.05689593330575,-4.49694270786391,
-0.465873873928905));
#48075=CARTESIAN_POINT('Ctrl Pts',(-5.02406868047268,-4.53332360348272,
-0.463574650681203));
#48076=CARTESIAN_POINT('Ctrl Pts',(-4.901002160078,-4.66971242210901,-0.454955062373151));
#48077=CARTESIAN_POINT('Ctrl Pts',(-4.77242363098732,-4.80103706814503,
-0.446335474065095));
#48078=CARTESIAN_POINT('Ctrl Pts',(-4.63877664921645,-4.92686920860339,
-0.437715885757044));
#48079=CARTESIAN_POINT('Ctrl Pts',(-4.50504919667541,-5.05277711440356,
-0.429091107470883));
#48080=CARTESIAN_POINT('Ctrl Pts',(-4.36624742236036,-5.17318570617981,
-0.420466329184711));
#48081=CARTESIAN_POINT('Ctrl Pts',(-4.22284924252844,-5.28770586122914,
-0.411841550898551));
#48082=CARTESIAN_POINT('Ctrl Pts',(-4.07455550072935,-5.4061356929298,-0.402922325802797));
#48083=CARTESIAN_POINT('Ctrl Pts',(-3.92134625974652,-5.5182677169265,-0.394003100707058));
#48084=CARTESIAN_POINT('Ctrl Pts',(-3.76378360987677,-5.6237195820936,-0.385083875611301));
#48085=CARTESIAN_POINT('Ctrl Pts',(-3.611137779954,-5.72588076996802,-0.376442979319348));
#48086=CARTESIAN_POINT('Ctrl Pts',(-3.45440642855516,-5.82177230803757,
-0.367802083027394));
#48087=CARTESIAN_POINT('Ctrl Pts',(-3.29412709115138,-5.91109259844088,
-0.359161186735442));
#48088=CARTESIAN_POINT('Ctrl Pts',(-3.12610370357964,-6.00472848448555,
-0.350102797237785));
#48089=CARTESIAN_POINT('Ctrl Pts',(-2.95418133405112,-6.09114222573036,
-0.341044407740149));
#48090=CARTESIAN_POINT('Ctrl Pts',(-2.77900494902321,-6.170042179216,-0.331986018242496));
#48091=CARTESIAN_POINT('Ctrl Pts',(-2.60382856399525,-6.24894213270166,
-0.32292762874484));
#48092=CARTESIAN_POINT('Ctrl Pts',(-2.42539853061243,-6.32032818726296,
-0.313869239247172));
#48093=CARTESIAN_POINT('Ctrl Pts',(-2.24438075491975,-6.38396773385846,
-0.304810849749515));
#48094=CARTESIAN_POINT('Ctrl Pts',(-2.06386608615943,-6.44743040557555,
-0.295777636445384));
#48095=CARTESIAN_POINT('Ctrl Pts',(-1.88061033434157,-6.50324941191704,
-0.286744423141259));
#48096=CARTESIAN_POINT('Ctrl Pts',(-1.69524999163123,-6.55121488472744,
-0.277711209837129));
#48097=CARTESIAN_POINT('Ctrl Pts',(-1.510059729892,-6.59913634588963,-0.268686285132753));
#48098=CARTESIAN_POINT('Ctrl Pts',(-1.32276896481906,-6.63921860024135,
-0.259661360428383));
#48099=CARTESIAN_POINT('Ctrl Pts',(-1.1340283502408,-6.67130187451071,-0.250636435724005));
#48100=CARTESIAN_POINT('Ctrl Pts',(-0.945616935672086,-6.70332918936604,
-0.241627252227767));
#48101=CARTESIAN_POINT('Ctrl Pts',(-0.755760957629054,-6.72738534371772,
-0.232618068731527));
#48102=CARTESIAN_POINT('Ctrl Pts',(-0.565120088508994,-6.74336179405818,
-0.223608885235294));
#48103=CARTESIAN_POINT('Ctrl Pts',(-0.374714945004879,-6.75931848967022,
-0.214610841508506));
#48104=CARTESIAN_POINT('Ctrl Pts',(-0.18352708569595,-6.76721539860972,
-0.205612797781702));
#48105=CARTESIAN_POINT('Ctrl Pts',(0.00777736804904949,-6.7669955307024,
-0.196614754054913));
#48106=CARTESIAN_POINT('Ctrl Pts',(0.198658389228101,-6.76677614944989,
-0.187636626564621));
#48107=CARTESIAN_POINT('Ctrl Pts',(0.389655250132718,-6.75847585301212,
-0.178658499074348));
#48108=CARTESIAN_POINT('Ctrl Pts',(0.580100937286119,-6.74208957983797,
-0.169680371584057));
#48109=CARTESIAN_POINT('Ctrl Pts',(0.747205729784349,-6.72771159722512,
-0.161802597328769));
#48110=CARTESIAN_POINT('Ctrl Pts',(0.913885991250512,-6.70710894989072,
-0.153924823073464));
#48111=CARTESIAN_POINT('Ctrl Pts',(1.07968995621285,-6.68031126508736,-0.146047048818176));
#48112=CARTESIAN_POINT('Ctrl Pts',(1.25095258969113,-6.65263133552967,-0.137909919134849));
#48113=CARTESIAN_POINT('Ctrl Pts',(1.42120128441979,-6.61835287109931,-0.129772789451537));
#48114=CARTESIAN_POINT('Ctrl Pts',(1.58989107614523,-6.57757822956092,-0.121635659768209));
#48115=CARTESIAN_POINT('Ctrl Pts',(1.75857100515743,-6.5368059719759,-0.113499005834931));
#48116=CARTESIAN_POINT('Ctrl Pts',(1.9256918583268,-6.48953837960548,-0.105362351901639));
#48117=CARTESIAN_POINT('Ctrl Pts',(2.09072064053307,-6.43592854242875,-0.0972256979683621));
#48118=CARTESIAN_POINT('Ctrl Pts',(2.25577097910605,-6.38231170263529,-0.0890879812102037));
#48119=CARTESIAN_POINT('Ctrl Pts',(2.41872835612831,-6.32235108206134,-0.0809502644520282));
#48120=CARTESIAN_POINT('Ctrl Pts',(2.57907669378534,-6.25624906853726,-0.0728125476938715));
#48121=CARTESIAN_POINT('Ctrl Pts',(2.73954330896164,-6.19009829627771,-0.0646688283231229));
#48122=CARTESIAN_POINT('Ctrl Pts',(2.8973967035762,-6.11779722237087,-0.0565251089523754));
#48123=CARTESIAN_POINT('Ctrl Pts',(3.05214187870714,-6.03959592623894,-0.0483813895816212));
#48124=CARTESIAN_POINT('Ctrl Pts',(3.20695114179602,-5.96136224291709,-0.040234297476667));
#48125=CARTESIAN_POINT('Ctrl Pts',(3.35864930069323,-5.8772236429884,-0.032087205371719));
#48126=CARTESIAN_POINT('Ctrl Pts',(3.50676778194066,-5.78747515964803,-0.023940113266768));
#48127=CARTESIAN_POINT('Ctrl Pts',(3.6550474364314,-5.6976290176359,-0.0157841560070632));
#48128=CARTESIAN_POINT('Ctrl Pts',(3.79973932923221,-5.6021610002471,-0.00762819874735902));
#48129=CARTESIAN_POINT('Ctrl Pts',(3.94040495610507,-5.50140870885836,0.000527758512347987));
#48130=CARTESIAN_POINT('Ctrl Pts',(4.01047939663398,-5.45121762374378,0.00459075637939762));
#48131=CARTESIAN_POINT('Ctrl Pts',(4.07955517102849,-5.39971578419021,0.0086537542464415));
#48132=CARTESIAN_POINT('Ctrl Pts',(4.14758131819055,-5.34694849507611,0.0127167521134908));
#48133=CARTESIAN_POINT('Ctrl Pts',(4.28866189222471,-5.23751352412726,0.0211430719227959));
#48134=CARTESIAN_POINT('Ctrl Pts',(4.42551682084227,-5.12240752092213,0.0295693917321155));
#48135=CARTESIAN_POINT('Ctrl Pts',(4.55767992858152,-5.0019838732852,0.0379957115414271));
#48136=CARTESIAN_POINT('Ctrl Pts',(4.68974123890343,-4.8816529808545,0.04641554105546));
#48137=CARTESIAN_POINT('Ctrl Pts',(4.81711768504375,-4.75601283324789,0.0548353705694841));
#48138=CARTESIAN_POINT('Ctrl Pts',(4.93937595472497,-4.62545718582334,0.0632552000835176));
#48139=CARTESIAN_POINT('Ctrl Pts',(5.06155932053113,-4.49498152582156,0.0716698710274222));
#48140=CARTESIAN_POINT('Ctrl Pts',(5.17863053259408,-4.35959661368453,0.0800845419713343));
#48141=CARTESIAN_POINT('Ctrl Pts',(5.29019269833248,-4.21973342931869,0.088499212915238));
#48142=CARTESIAN_POINT('Ctrl Pts',(5.4017040744868,-4.07993391880605,0.0969100530116977));
#48143=CARTESIAN_POINT('Ctrl Pts',(5.5077111961529,-3.93566046249943,0.105320893108149));
#48144=CARTESIAN_POINT('Ctrl Pts',(5.60785684119223,-3.78737780643726,0.113731733204609));
#48145=CARTESIAN_POINT('Ctrl Pts',(5.70797264594431,-3.63913933399435,0.122140067132336));
#48146=CARTESIAN_POINT('Ctrl Pts',(5.80223026949453,-3.48689432146133,0.130548401060059));
#48147=CARTESIAN_POINT('Ctrl Pts',(5.89031507729034,-3.33113753697534,0.138956734987786));
#48148=CARTESIAN_POINT('Ctrl Pts',(5.9784019705473,-3.17537706485317,0.14736526798791));
#48149=CARTESIAN_POINT('Ctrl Pts',(6.06031558521371,-3.01610494300437,0.155773800988043));
#48150=CARTESIAN_POINT('Ctrl Pts',(6.13578630374197,-2.85384222318132,0.164182333988165));
#48151=CARTESIAN_POINT('Ctrl Pts',(6.21126013743586,-2.69157280572429,0.172591214062936));
#48152=CARTESIAN_POINT('Ctrl Pts',(6.28029040316456,-2.52631284807733,0.181000094137698));
#48153=CARTESIAN_POINT('Ctrl Pts',(6.34265482316743,-2.35860526458986,0.189408974212469));
#48154=CARTESIAN_POINT('Ctrl Pts',(6.40503073850055,-2.19086676837908,0.197819404255213));
#48155=CARTESIAN_POINT('Ctrl Pts',(6.4607382416948,-2.02068006109688,0.206229834297953));
#48156=CARTESIAN_POINT('Ctrl Pts',(6.50960419080739,-1.84860549577862,0.214640264340694));
#48157=CARTESIAN_POINT('Ctrl Pts',(6.55848613937721,-1.67647459062251,0.223053448086541));
#48158=CARTESIAN_POINT('Ctrl Pts',(6.60052197647211,-1.50245491748494,0.231466631832394));
#48159=CARTESIAN_POINT('Ctrl Pts',(6.63558907049047,-1.32711969602874,0.239879815578242));
#48160=CARTESIAN_POINT('Ctrl Pts',(6.67068878256316,-1.15162138453218,0.248300824942154));
#48161=CARTESIAN_POINT('Ctrl Pts',(6.69880673379692,-0.974805408722592,
0.256721834306079));
#48162=CARTESIAN_POINT('Ctrl Pts',(6.71987165761963,-0.797253977801603,
0.265142843669992));
#48163=CARTESIAN_POINT('Ctrl Pts',(6.7409471472684,-0.619613489946317,0.273568076876392));
#48164=CARTESIAN_POINT('Ctrl Pts',(6.75496252317796,-0.441237144900999,
0.281993310082783));
#48165=CARTESIAN_POINT('Ctrl Pts',(6.76189856815725,-0.262710399400144,
0.290418543289185));
#48166=CARTESIAN_POINT('Ctrl Pts',(6.7688426266085,-0.0839773952787056,
0.298853510482359));
#48167=CARTESIAN_POINT('Ctrl Pts',(6.76869100669955,0.0949060212790336,
0.307288477675536));
#48168=CARTESIAN_POINT('Ctrl Pts',(6.76147661581355,0.273355032524567,0.315723444868709));
#48169=CARTESIAN_POINT('Ctrl Pts',(6.75733672560317,0.375755820946249,0.320563747904648));
#48170=CARTESIAN_POINT('Ctrl Pts',(6.75087209684535,0.478013640515783,0.325404050940573));
#48171=CARTESIAN_POINT('Ctrl Pts',(6.7420966267274,0.580019030611108,0.330244353976511));
#48172=CARTESIAN_POINT('Ctrl Pts',(6.72709792733164,0.754362759462393,0.338517215628905));
#48173=CARTESIAN_POINT('Ctrl Pts',(6.70531184881675,0.928363414331154,0.346790077281274));
#48174=CARTESIAN_POINT('Ctrl Pts',(6.67675688288832,1.10145654785085,0.355062938933656));
#48175=CARTESIAN_POINT('Ctrl Pts',(6.64823478984464,1.27435041408216,0.363326276749506));
#48176=CARTESIAN_POINT('Ctrl Pts',(6.61295938424434,1.44633849500936,0.371589614565336));
#48177=CARTESIAN_POINT('Ctrl Pts',(6.57100105581381,1.61685933973668,0.379852952381185));
#48178=CARTESIAN_POINT('Ctrl Pts',(6.52908375851575,1.78721343179226,0.388108209462619));
#48179=CARTESIAN_POINT('Ctrl Pts',(6.48049663861083,1.95610280542443,0.396363466544053));
#48180=CARTESIAN_POINT('Ctrl Pts',(6.42536150878182,2.12297397098151,0.404618723625489));
#48181=CARTESIAN_POINT('Ctrl Pts',(6.37027977715849,2.28968352232187,0.412865985515531));
#48182=CARTESIAN_POINT('Ctrl Pts',(6.3086627871622,2.45437842876475,0.421113247405568));
#48183=CARTESIAN_POINT('Ctrl Pts',(6.24068272489409,2.61651832158853,0.429360509295606));
#48184=CARTESIAN_POINT('Ctrl Pts',(6.17274088431909,2.7785670514887,0.437603134174403));
#48185=CARTESIAN_POINT('Ctrl Pts',(6.09844323291158,2.93806330498765,0.445845759053206));
#48186=CARTESIAN_POINT('Ctrl Pts',(6.01801099791469,3.09448422664874,0.454088383932003));
#48187=CARTESIAN_POINT('Ctrl Pts',(5.93761260647178,3.25083933091827,0.46232754055308));
#48188=CARTESIAN_POINT('Ctrl Pts',(5.85108493604182,3.40412136909221,0.470566697174174));
#48189=CARTESIAN_POINT('Ctrl Pts',(5.7586963544244,3.55382966636545,0.478805853795251));
#48190=CARTESIAN_POINT('Ctrl Pts',(5.72056234903276,3.61562276801768,0.482206620832802));
#48191=CARTESIAN_POINT('Ctrl Pts',(5.68143037765305,3.676807299254,0.485607387870354));
#48192=CARTESIAN_POINT('Ctrl Pts',(5.64132157314919,3.73734931580146,0.489008154907907));
#48193=CARTESIAN_POINT('Ctrl Pts',(5.53726608791621,3.89441530135636,0.497830867741997));
#48194=CARTESIAN_POINT('Ctrl Pts',(5.42674759486663,4.04698209985476,0.506653580576097));
#48195=CARTESIAN_POINT('Ctrl Pts',(5.31018113334372,4.19455186296229,0.515476293410202));
#48196=CARTESIAN_POINT('Ctrl Pts',(5.19340607508605,4.34238570349254,0.524314794568539));
#48197=CARTESIAN_POINT('Ctrl Pts',(5.07056158678431,4.48520443187774,0.533153295726877));
#48198=CARTESIAN_POINT('Ctrl Pts',(4.94210115344296,4.6225453149902,0.541991796885213));
#48199=CARTESIAN_POINT('Ctrl Pts',(4.81328318041853,4.76026845444839,0.550854897952025));
#48200=CARTESIAN_POINT('Ctrl Pts',(4.67881816800654,4.89248304563406,0.559717999018851));
#48201=CARTESIAN_POINT('Ctrl Pts',(4.53919667414657,5.01876305013663,0.568581100085666));
#48202=CARTESIAN_POINT('Ctrl Pts',(4.39938827955337,5.14521209612974,0.577456065515498));
#48203=CARTESIAN_POINT('Ctrl Pts',(4.25440981792345,5.26571051468527,0.5863310309453));
#48204=CARTESIAN_POINT('Ctrl Pts',(4.10478382286784,5.379873489918,0.595205996375128));
#48205=CARTESIAN_POINT('Ctrl Pts',(3.95482057865104,5.49429378252144,0.604100965512506));
#48206=CARTESIAN_POINT('Ctrl Pts',(3.80018906105163,5.6023499083688,0.612995934649882));
#48207=CARTESIAN_POINT('Ctrl Pts',(3.64144198757417,5.70369961087818,0.621890903787261));
#48208=CARTESIAN_POINT('Ctrl Pts',(3.48747700623195,5.80199625795376,0.630517921138043));
#48209=CARTESIAN_POINT('Ctrl Pts',(3.32964101985645,5.89398457502353,0.639144938488834));
#48210=CARTESIAN_POINT('Ctrl Pts',(3.16845894722699,5.97939435894115,0.647771955839616));
#48211=CARTESIAN_POINT('Ctrl Pts',(3.14540941730174,5.99160821956599,0.649005645736694));
#48212=CARTESIAN_POINT('Ctrl Pts',(3.12228440987943,6.00369137191337,0.650239335633784));
#48213=CARTESIAN_POINT('Ctrl Pts',(3.09908550384723,6.01564277861011,0.651473025530862));
#48214=CARTESIAN_POINT('Origin',(0.,0.,-63.6971797838103));
#48215=CARTESIAN_POINT('',(3.09908550384731,6.01564277861007,3.04562247039131));
#48216=CARTESIAN_POINT('',(3.09908550384727,6.01564277861009,2.6515053192028));
#48217=CARTESIAN_POINT('',(3.09908550384721,6.01564277861012,-63.6971797838103));
#48218=CARTESIAN_POINT('',(-6.76699874199977,0.004126229935696,1.69717978377767));
#48219=CARTESIAN_POINT('Ctrl Pts',(-6.7669987420002,0.0041262292468995,
1.69717978380999));
#48220=CARTESIAN_POINT('Ctrl Pts',(-6.76710297099132,-0.166808881138621,
1.70519840959001));
#48221=CARTESIAN_POINT('Ctrl Pts',(-6.76072618644486,-0.337884134911409,
1.71321703537002));
#48222=CARTESIAN_POINT('Ctrl Pts',(-6.74786314866394,-0.508558675968804,
1.72123566115003));
#48223=CARTESIAN_POINT('Ctrl Pts',(-6.74120626970332,-0.596886159789519,
1.72538546014442));
#48224=CARTESIAN_POINT('Ctrl Pts',(-6.7328130489101,-0.685106279448968,
1.72953525913879));
#48225=CARTESIAN_POINT('Ctrl Pts',(-6.72268824459125,-0.773144078445009,
1.73368505813318));
#48226=CARTESIAN_POINT('Ctrl Pts',(-6.70258469082633,-0.947949691445093,
1.74192479339818));
#48227=CARTESIAN_POINT('Ctrl Pts',(-6.67566140789129,-1.12194795613973,
1.75016452866318));
#48228=CARTESIAN_POINT('Ctrl Pts',(-6.64201440311397,-1.29457856803925,
1.75840426392818));
#48229=CARTESIAN_POINT('Ctrl Pts',(-6.60835701093335,-1.46726247394813,
1.76664654293977));
#48230=CARTESIAN_POINT('Ctrl Pts',(-6.56797182808259,-1.63857753976916,
1.77488882195136));
#48231=CARTESIAN_POINT('Ctrl Pts',(-6.52100572584818,-1.807974923348,1.78313110096295));
#48232=CARTESIAN_POINT('Ctrl Pts',(-6.4740169939614,-1.97745392757924,1.7913773513475));
#48233=CARTESIAN_POINT('Ctrl Pts',(-6.4204411183472,-2.14501306905879,1.79962360173205));
#48234=CARTESIAN_POINT('Ctrl Pts',(-6.36047448242523,-2.31011977144421,
1.8078698521166));
#48235=CARTESIAN_POINT('Ctrl Pts',(-6.30043566332169,-2.47542521646204,
1.81612602869727));
#48236=CARTESIAN_POINT('Ctrl Pts',(-6.23399083852102,-2.63827199441728,
1.82438220527795));
#48237=CARTESIAN_POINT('Ctrl Pts',(-6.16138450155594,-2.79814760582538,
1.83263838185863));
#48238=CARTESIAN_POINT('Ctrl Pts',(-6.08872815499652,-2.95813333592013,
1.84090024510605));
#48239=CARTESIAN_POINT('Ctrl Pts',(-6.00990199294824,-3.11514350533717,
1.84916210835345));
#48240=CARTESIAN_POINT('Ctrl Pts',(-5.92519591535356,-3.26869123116232,
1.85742397160087));
#48241=CARTESIAN_POINT('Ctrl Pts',(-5.84036956708222,-3.42245697308987,
1.8656975655282));
#48242=CARTESIAN_POINT('Ctrl Pts',(-5.74964680847141,-3.57275015056186,
1.87397115945553));
#48243=CARTESIAN_POINT('Ctrl Pts',(-5.65336077724304,-3.71911292142763,
1.88224475338286));
#48244=CARTESIAN_POINT('Ctrl Pts',(-5.61377649472611,-3.77928432114158,
1.88564612194351));
#48245=CARTESIAN_POINT('Ctrl Pts',(-5.57325242186237,-3.83879182045804,
1.88904749050416));
#48246=CARTESIAN_POINT('Ctrl Pts',(-5.53181362420354,-3.89760529390498,
1.89244885906481));
#48247=CARTESIAN_POINT('Ctrl Pts',(-5.42905042189326,-4.04345558908385,
1.90088384138278));
#48248=CARTESIAN_POINT('Ctrl Pts',(-5.32042193225358,-4.18537206677828,
1.90931882370074));
#48249=CARTESIAN_POINT('Ctrl Pts',(-5.20625440608239,-4.32286988690935,
1.91775380601871));
#48250=CARTESIAN_POINT('Ctrl Pts',(-5.09219484559422,-4.46023767841879,
1.92618081156204));
#48251=CARTESIAN_POINT('Ctrl Pts',(-4.97260690208883,-4.5931948844967,1.93460781710537));
#48252=CARTESIAN_POINT('Ctrl Pts',(-4.84785902237663,-4.72128710196294,
1.9430348226487));
#48253=CARTESIAN_POINT('Ctrl Pts',(-4.72320942905771,-4.84927839809814,
1.95145518872061));
#48254=CARTESIAN_POINT('Ctrl Pts',(-4.59340823641803,-4.97241210706217,
1.95987555479253));
#48255=CARTESIAN_POINT('Ctrl Pts',(-4.45886316091591,-5.09026800003958,
1.96829592086445));
#48256=CARTESIAN_POINT('Ctrl Pts',(-4.32440288737786,-5.20804961002177,
1.97671097969209));
#48257=CARTESIAN_POINT('Ctrl Pts',(-4.18520494336179,-5.32055981555433,
1.98512603851973));
#48258=CARTESIAN_POINT('Ctrl Pts',(-4.04171305541096,-5.42741601295871,
1.99354109734738));
#48259=CARTESIAN_POINT('Ctrl Pts',(-3.89828901883082,-5.5342216824931,2.00195217704223));
#48260=CARTESIAN_POINT('Ctrl Pts',(-3.75057535512656,-5.63537847480804,
2.01036325673709));
#48261=CARTESIAN_POINT('Ctrl Pts',(-3.59904823634381,-5.73054454589357,
2.01877433643195));
#48262=CARTESIAN_POINT('Ctrl Pts',(-3.44755742646226,-5.8256878133021,2.02718340066539));
#48263=CARTESIAN_POINT('Ctrl Pts',(-3.29225526556584,-5.91484304125412,
2.03559246489883));
#48264=CARTESIAN_POINT('Ctrl Pts',(-3.13364664840334,-5.99771187061787,
2.04400152913227));
#48265=CARTESIAN_POINT('Ctrl Pts',(-2.97505735390578,-6.08057060439758,
2.05240956892245));
#48266=CARTESIAN_POINT('Ctrl Pts',(-2.81316270309042,-6.15714431105671,
2.06081760871261));
#48267=CARTESIAN_POINT('Ctrl Pts',(-2.64849218286932,-6.22718059456124,
2.06922564850278));
#48268=CARTESIAN_POINT('Ctrl Pts',(-2.48381817102483,-6.29721836309373,
2.07763386657446));
#48269=CARTESIAN_POINT('Ctrl Pts',(-2.31636848099018,-6.36071830128286,
2.08604208464614));
#48270=CARTESIAN_POINT('Ctrl Pts',(-2.14669288550721,-6.41747603465044,
2.09445030271782));
#48271=CARTESIAN_POINT('Ctrl Pts',(-1.97698942264425,-6.47424308986137,
2.1028599017483));
#48272=CARTESIAN_POINT('Ctrl Pts',(-1.80505964350623,-6.52426562694529,
2.11126950077879));
#48273=CARTESIAN_POINT('Ctrl Pts',(-1.63146912695812,-6.56738893988947,
2.11967909980928));
#48274=CARTESIAN_POINT('Ctrl Pts',(-1.45776002175846,-6.61054171259696,
2.1280944438714));
#48275=CARTESIAN_POINT('Ctrl Pts',(-1.28238823770533,-6.64678576226753,
2.13650978793351));
#48276=CARTESIAN_POINT('Ctrl Pts',(-1.10593119819516,-6.67601716481156,
2.14492513199563));
#48277=CARTESIAN_POINT('Ctrl Pts',(-0.929410368622567,-6.7052591346472,
2.15334351824482));
#48278=CARTESIAN_POINT('Ctrl Pts',(-0.751803832989001,-6.72748335415473,
2.16176190449402));
#48279=CARTESIAN_POINT('Ctrl Pts',(-0.573695352906521,-6.74263766207658,
2.1701802907432));
#48280=CARTESIAN_POINT('Ctrl Pts',(-0.395419202031871,-6.75780623621872,
2.17860660203611));
#48281=CARTESIAN_POINT('Ctrl Pts',(-0.216640497220458,-6.76589157901934,
2.187032913329));
#48282=CARTESIAN_POINT('Ctrl Pts',(-0.0379453377691904,-6.76689361164645,
2.1954592246219));
#48283=CARTESIAN_POINT('Ctrl Pts',(0.0646760729647106,-6.76746906093177,
2.20029830339055));
#48284=CARTESIAN_POINT('Ctrl Pts',(0.167269944912153,-6.76570939935171,
2.2051373821592));
#48285=CARTESIAN_POINT('Ctrl Pts',(0.269725823615944,-6.76162236301871,
2.20997646092785));
#48286=CARTESIAN_POINT('Ctrl Pts',(0.442402428732244,-6.75473417302027,
2.2181321246558));
#48287=CARTESIAN_POINT('Ctrl Pts',(0.615031731835564,-6.74121836881216,
2.22628778838376));
#48288=CARTESIAN_POINT('Ctrl Pts',(0.787061651744364,-6.72107305096094,
2.23444345211172));
#48289=CARTESIAN_POINT('Ctrl Pts',(0.958941008873126,-6.70094536454885,
2.24259197789876));
#48290=CARTESIAN_POINT('Ctrl Pts',(1.13022166734705,-6.67419975683062,2.2507405036858));
#48291=CARTESIAN_POINT('Ctrl Pts',(1.30035287488392,-6.64088634150451,2.25888902947284));
#48292=CARTESIAN_POINT('Ctrl Pts',(1.47036736483711,-6.60759578066463,2.26703196500837));
#48293=CARTESIAN_POINT('Ctrl Pts',(1.63923361758765,-6.56774645349893,2.27517490054391));
#48294=CARTESIAN_POINT('Ctrl Pts',(1.80640734694751,-6.52144013979229,2.28331783607943));
#48295=CARTESIAN_POINT('Ctrl Pts',(1.97349951886859,-6.47515641710136,2.29145679899935));
#48296=CARTESIAN_POINT('Ctrl Pts',(2.13890046121281,-6.42242207865703,2.29959576191926));
#48297=CARTESIAN_POINT('Ctrl Pts',(2.30207741597558,-6.36338970760515,2.30773472483918));
#48298=CARTESIAN_POINT('Ctrl Pts',(2.46520773901468,-6.30437420646741,2.31587136185548));
#48299=CARTESIAN_POINT('Ctrl Pts',(2.62611499811908,-6.23906438240821,2.32400799887178));
#48300=CARTESIAN_POINT('Ctrl Pts',(2.78428290701581,-6.16766225515791,2.33214463588808));
#48301=CARTESIAN_POINT('Ctrl Pts',(2.94245684475139,-6.09625740629411,2.34028158304614));
#48302=CARTESIAN_POINT('Ctrl Pts',(3.09789088966155,-6.01875993661228,2.34841853020418));
#48303=CARTESIAN_POINT('Ctrl Pts',(3.25008982849438,-5.93541953923372,2.35655547736224));
#48304=CARTESIAN_POINT('Ctrl Pts',(3.32606063320038,-5.89381979417688,2.36061707219455));
#48305=CARTESIAN_POINT('Ctrl Pts',(3.40122575489734,-5.85076498187504,2.36467866702688));
#48306=CARTESIAN_POINT('Ctrl Pts',(3.47552596350473,-5.80629040584473,2.3687402618592));
#48307=CARTESIAN_POINT('Ctrl Pts',(3.63969370392998,-5.70802297443215,2.37771443378472));
#48308=CARTESIAN_POINT('Ctrl Pts',(3.7995540908287,-5.60287161391884,2.38668860571026));
#48309=CARTESIAN_POINT('Ctrl Pts',(3.95457002635816,-5.49123528057482,2.39566277763578));
#48310=CARTESIAN_POINT('Ctrl Pts',(4.10984646873757,-5.3794113405216,2.40465203080602));
#48311=CARTESIAN_POINT('Ctrl Pts',(4.26026199279593,-5.2610807871186,2.41364128397626));
#48312=CARTESIAN_POINT('Ctrl Pts',(4.40531210531596,-5.13668319587228,2.4226305371465));
#48313=CARTESIAN_POINT('Ctrl Pts',(4.5506972519056,-5.01199827336838,2.43164055352761));
#48314=CARTESIAN_POINT('Ctrl Pts',(4.69069200782386,-4.88121843270496,2.44065056990872));
#48315=CARTESIAN_POINT('Ctrl Pts',(4.82482635548035,-4.74482240336372,2.44966058628982));
#48316=CARTESIAN_POINT('Ctrl Pts',(4.95909489252592,-4.60828992202363,2.45867961638453));
#48317=CARTESIAN_POINT('Ctrl Pts',(5.08749114456103,-4.46613020390667,2.46769864647925));
#48318=CARTESIAN_POINT('Ctrl Pts',(5.20958400989011,-4.31885672879957,2.47671767657395));
#48319=CARTESIAN_POINT('Ctrl Pts',(5.33184918371774,-4.17137540803904,2.48574943513998));
#48320=CARTESIAN_POINT('Ctrl Pts',(5.44779302950886,-4.01876608561737,2.494781193706));
#48321=CARTESIAN_POINT('Ctrl Pts',(5.5570251635486,-3.86157485123462,2.50381295227203));
#48322=CARTESIAN_POINT('Ctrl Pts',(5.65253371598365,-3.72413262891281,2.51170998911167));
#48323=CARTESIAN_POINT('Ctrl Pts',(5.74291168395272,-3.58318802975742,2.51960702595129));
#48324=CARTESIAN_POINT('Ctrl Pts',(5.82792588108913,-3.4391232784725,2.52750406279092));
#48325=CARTESIAN_POINT('Ctrl Pts',(5.92109086185467,-3.28124623870097,2.53615823244789));
#48326=CARTESIAN_POINT('Ctrl Pts',(6.00789619768168,-3.11948068244951,2.54481240210485));
#48327=CARTESIAN_POINT('Ctrl Pts',(6.08802720130508,-2.9543550558742,2.55346657176182));
#48328=CARTESIAN_POINT('Ctrl Pts',(6.16808425728699,-2.78938181289679,2.56211275505388));
#48329=CARTESIAN_POINT('Ctrl Pts',(6.24147913375015,-2.62105495666394,2.57075893834593));
#48330=CARTESIAN_POINT('Ctrl Pts',(6.30794276905849,-2.4499279626721,2.57940512163799));
#48331=CARTESIAN_POINT('Ctrl Pts',(6.37639769764787,-2.27367389382561,2.58831035014502));
#48332=CARTESIAN_POINT('Ctrl Pts',(6.43749942211724,-2.09444956361584,2.59721557865208));
#48333=CARTESIAN_POINT('Ctrl Pts',(6.49100618115909,-1.91288466880639,2.6061208071591));
#48334=CARTESIAN_POINT('Ctrl Pts',(6.54285762426688,-1.73693677021995,2.61475053838488));
#48335=CARTESIAN_POINT('Ctrl Pts',(6.5875768975266,-1.55879127692548,2.62338026961067));
#48336=CARTESIAN_POINT('Ctrl Pts',(6.62499347012686,-1.37903970964452,2.63201000083646));
#48337=CARTESIAN_POINT('Ctrl Pts',(6.66420178404938,-1.19068050439851,2.64105297798411));
#48338=CARTESIAN_POINT('Ctrl Pts',(6.69539069388701,-1.00055794336212,2.65009595513175));
#48339=CARTESIAN_POINT('Ctrl Pts',(6.71842324907516,-0.809368918532445,
2.6591389322794));
#48340=CARTESIAN_POINT('Ctrl Pts',(6.7414558042633,-0.618179893702837,2.66818190942705));
#48341=CARTESIAN_POINT('Ctrl Pts',(6.75633192426425,-0.425924783021438,
2.6772248865747));
#48342=CARTESIAN_POINT('Ctrl Pts',(6.76297676298404,-0.233311601378899,
2.68626786372235));
#48343=CARTESIAN_POINT('Ctrl Pts',(6.76916879388631,-0.0538239082668467,
2.69469461361171));
#48344=CARTESIAN_POINT('Ctrl Pts',(6.76821062399756,0.125895236555421,2.70312136350109));
#48345=CARTESIAN_POINT('Ctrl Pts',(6.76011154818979,0.30525539476169,2.71154811339045));
#48346=CARTESIAN_POINT('Ctrl Pts',(6.75201056628867,0.484657764846474,2.71997684649028));
#48347=CARTESIAN_POINT('Ctrl Pts',(6.73676534253674,0.66370064882653,2.7284055795901));
#48348=CARTESIAN_POINT('Ctrl Pts',(6.71443720104782,0.841796931085577,2.73683431268992));
#48349=CARTESIAN_POINT('Ctrl Pts',(6.69210078749759,1.0199591939086,2.74526616844091));
#48350=CARTESIAN_POINT('Ctrl Pts',(6.66267626524027,1.19717382711612,2.75369802419192));
#48351=CARTESIAN_POINT('Ctrl Pts',(6.62627645457056,1.37286173652115,2.76212987994292));
#48352=CARTESIAN_POINT('Ctrl Pts',(6.58984306320376,1.54871172705679,2.77056951451442));
#48353=CARTESIAN_POINT('Ctrl Pts',(6.54642159402834,1.72303185506663,2.77900914908593));
#48354=CARTESIAN_POINT('Ctrl Pts',(6.49617561294783,1.89525497116927,2.78744878365744));
#48355=CARTESIAN_POINT('Ctrl Pts',(6.44590318059714,2.06756875164107,2.79589286115253));
#48356=CARTESIAN_POINT('Ctrl Pts',(6.38879917133256,2.23778300296788,2.8043369386476));
#48357=CARTESIAN_POINT('Ctrl Pts',(6.32507629851579,2.40534796192855,2.81278101614269));
#48358=CARTESIAN_POINT('Ctrl Pts',(6.2612863409453,2.57308932621288,2.82123398320654));
#48359=CARTESIAN_POINT('Ctrl Pts',(6.19086372552568,2.73817552016933,2.82968695027037));
#48360=CARTESIAN_POINT('Ctrl Pts',(6.11406878487783,2.90007791167454,2.83813991733422));
#48361=CARTESIAN_POINT('Ctrl Pts',(6.09319834879832,2.94407786120928,2.84043716644073));
#48362=CARTESIAN_POINT('Ctrl Pts',(6.07185752517465,2.98784280561122,2.84273441554726));
#48363=CARTESIAN_POINT('Ctrl Pts',(6.05005211393966,3.03136246902514,2.84503166465377));
#48364=CARTESIAN_POINT('Ctrl Pts',(5.97071873144858,3.18969757521933,2.85338961489284));
#48365=CARTESIAN_POINT('Ctrl Pts',(5.88508860599053,3.34507034491326,2.8617475651319));
#48366=CARTESIAN_POINT('Ctrl Pts',(5.79340883242674,3.49695626228866,2.87010551537097));
#48367=CARTESIAN_POINT('Ctrl Pts',(5.70226108570057,3.64796077059028,2.87841496359414));
#48368=CARTESIAN_POINT('Ctrl Pts',(5.60513388527962,3.79551847850857,2.88672441181733));
#48369=CARTESIAN_POINT('Ctrl Pts',(5.50231710724092,3.93913638395066,2.8950338600405));
#48370=CARTESIAN_POINT('Ctrl Pts',(5.39956497794379,4.08266398587391,2.90333808348051));
#48371=CARTESIAN_POINT('Ctrl Pts',(5.29113060003837,4.22225643876606,2.91164230692051));
#48372=CARTESIAN_POINT('Ctrl Pts',(5.1773477978745,4.35744865487181,2.91994653036052));
#48373=CARTESIAN_POINT('Ctrl Pts',(5.06361763577753,4.49257832613627,2.92824691196442));
#48374=CARTESIAN_POINT('Ctrl Pts',(4.9445442035622,4.62331155151054,2.93654729356831));
#48375=CARTESIAN_POINT('Ctrl Pts',(4.8205024599883,4.74921520182512,2.94484767517221));
#48376=CARTESIAN_POINT('Ctrl Pts',(4.69500339757764,4.87659804580412,2.95324557477381));
#48377=CARTESIAN_POINT('Ctrl Pts',(4.56441876193443,4.99903682580213,2.96164347437542));
#48378=CARTESIAN_POINT('Ctrl Pts',(4.42917678438174,5.11611982000948,2.97004137397701));
#48379=CARTESIAN_POINT('Ctrl Pts',(4.29554593048381,5.23180801664768,2.97833923027147));
#48380=CARTESIAN_POINT('Ctrl Pts',(4.15736837259501,5.34226711638402,2.98663708656591));
#48381=CARTESIAN_POINT('Ctrl Pts',(4.01509197128691,5.44713919981007,2.99493494286037));
#48382=CARTESIAN_POINT('Ctrl Pts',(3.87024253161636,5.55390787249001,3.00338286411553));
#48383=CARTESIAN_POINT('Ctrl Pts',(3.72114486015774,5.65488527325917,3.0118307853707));
#48384=CARTESIAN_POINT('Ctrl Pts',(3.56830396325748,5.74973876152656,3.02027870662586));
#48385=CARTESIAN_POINT('Ctrl Pts',(3.41546306635722,5.84459224979395,3.02872662788102));
#48386=CARTESIAN_POINT('Ctrl Pts',(3.25887927574339,5.93332164015267,3.03717454913619));
#48387=CARTESIAN_POINT('Ctrl Pts',(3.0990855038473,6.01564277861008,3.04562247039135));
#48388=CARTESIAN_POINT('Ctrl Pts',(3.09908550384726,6.0156427786101,1.04588102939738));
#48389=CARTESIAN_POINT('Ctrl Pts',(2.94511050341158,6.09496625398363,1.05400525660668));
#48390=CARTESIAN_POINT('Ctrl Pts',(2.78801560534586,6.16841149912689,1.06212948381596));
#48391=CARTESIAN_POINT('Ctrl Pts',(2.62829577678531,6.23573173811482,1.07025371102526));
#48392=CARTESIAN_POINT('Ctrl Pts',(2.46858314112875,6.30304894536888,1.07837757236398));
#48393=CARTESIAN_POINT('Ctrl Pts',(2.30624614327927,6.36424154462215,1.08650143370269));
#48394=CARTESIAN_POINT('Ctrl Pts',(2.14180121197924,6.41911026298538,1.09462529504141));
#48395=CARTESIAN_POINT('Ctrl Pts',(1.97735210139803,6.47398037580814,1.10274936284378));
#48396=CARTESIAN_POINT('Ctrl Pts',(1.81079529740787,6.52252617097112,1.11087343064615));
#48397=CARTESIAN_POINT('Ctrl Pts',(1.64266370095001,6.56459785254064,1.11899749844852));
#48398=CARTESIAN_POINT('Ctrl Pts',(1.47449585096053,6.60667860585558,1.12712331801056));
#48399=CARTESIAN_POINT('Ctrl Pts',(1.30475288709302,6.64228237665215,1.13524913757259));
#48400=CARTESIAN_POINT('Ctrl Pts',(1.13397920245994,6.67131022876229,1.14337495713463));
#48401=CARTESIAN_POINT('Ctrl Pts',(0.96313620896442,6.70034986188783,1.15150407457778));
#48402=CARTESIAN_POINT('Ctrl Pts',(0.791262021954657,6.72280820051437,1.15963319202093));
#48403=CARTESIAN_POINT('Ctrl Pts',(0.618907432297392,6.73863803674356,1.16776230946408));
#48404=CARTESIAN_POINT('Ctrl Pts',(0.446347403748565,6.75448674142305,1.17590111644831));
#48405=CARTESIAN_POINT('Ctrl Pts',(0.273306193277052,6.76369113041661,1.18403992343255));
#48406=CARTESIAN_POINT('Ctrl Pts',(0.100336820484199,6.7662560934726,1.19217873041679));
#48407=CARTESIAN_POINT('Ctrl Pts',(-0.0727451131579683,6.76882272569358,
1.20032283377813));
#48408=CARTESIAN_POINT('Ctrl Pts',(-0.245754751500726,6.76474133226017,
1.20846693713949));
#48409=CARTESIAN_POINT('Ctrl Pts',(-0.418143228922062,6.75406879148463,
1.21661104050084));
#48410=CARTESIAN_POINT('Ctrl Pts',(-0.590796825776929,6.74337983721089,
1.22476766882964));
#48411=CARTESIAN_POINT('Ctrl Pts',(-0.762826990860979,6.7260795249096,1.2329242971584));
#48412=CARTESIAN_POINT('Ctrl Pts',(-0.933693007081257,6.70227620801527,
1.2410809254872));
#48413=CARTESIAN_POINT('Ctrl Pts',(-1.04760000602917,6.68640784254145,1.24651850210436));
#48414=CARTESIAN_POINT('Ctrl Pts',(-1.16098986786002,6.66765049645239,1.25195607872154));
#48415=CARTESIAN_POINT('Ctrl Pts',(-1.27370620471547,6.64604856317416,1.2573936553387));
#48416=CARTESIAN_POINT('Ctrl Pts',(-1.44372401441086,6.61346488024396,1.26559552644534));
#48417=CARTESIAN_POINT('Ctrl Pts',(-1.61275339964681,6.57430259382322,1.27379739755197));
#48418=CARTESIAN_POINT('Ctrl Pts',(-1.78024430706333,6.52863072988269,1.28199926865861));
#48419=CARTESIAN_POINT('Ctrl Pts',(-1.9475318094701,6.48301433095859,1.29019117921456));
#48420=CARTESIAN_POINT('Ctrl Pts',(-2.11328420892936,6.43090418777637,1.29838308977052));
#48421=CARTESIAN_POINT('Ctrl Pts',(-2.27695920292253,6.37242071651161,1.30657500032648));
#48422=CARTESIAN_POINT('Ctrl Pts',(-2.44046892556389,6.31399629912014,1.31475863907439));
#48423=CARTESIAN_POINT('Ctrl Pts',(-2.6019050818716,6.24921148879263,1.3229422778223));
#48424=CARTESIAN_POINT('Ctrl Pts',(-2.76073810189435,6.17823713795034,1.33112591657022));
#48425=CARTESIAN_POINT('Ctrl Pts',(-2.91944323475257,6.10731993333925,1.33930296611926));
#48426=CARTESIAN_POINT('Ctrl Pts',(-3.0755490771151,6.0302232598561,1.34748001566831));
#48427=CARTESIAN_POINT('Ctrl Pts',(-3.22854365472601,5.9471669616321,1.35565706521736));
#48428=CARTESIAN_POINT('Ctrl Pts',(-3.3814463376797,5.86416055033988,1.36382920330368));
#48429=CARTESIAN_POINT('Ctrl Pts',(-3.53124116147165,5.77520181624719,1.37200134139002));
#48430=CARTESIAN_POINT('Ctrl Pts',(-3.67743844357896,5.68055767453228,1.38017347947634));
#48431=CARTESIAN_POINT('Ctrl Pts',(-3.82359233340284,5.58594162380075,1.38834319202009));
#48432=CARTESIAN_POINT('Ctrl Pts',(-3.96615050295292,5.48564371890684,1.39651290456383));
#48433=CARTESIAN_POINT('Ctrl Pts',(-4.10464990705188,5.37997566356382,1.40468261710758));
#48434=CARTESIAN_POINT('Ctrl Pts',(-4.24313025833367,5.27432214455873,1.41285120577617));
#48435=CARTESIAN_POINT('Ctrl Pts',(-4.37755266819308,5.16330016469292,1.42101979444476));
#48436=CARTESIAN_POINT('Ctrl Pts',(-4.50748503267875,5.04726338525909,1.42918838311336));
#48437=CARTESIAN_POINT('Ctrl Pts',(-4.63742359469937,4.93122107108418,1.43735736140861));
#48438=CARTESIAN_POINT('Ctrl Pts',(-4.76287141501455,4.81016372158861,1.44552633970388));
#48439=CARTESIAN_POINT('Ctrl Pts',(-4.88343129243093,4.68448372951666,1.45369531799913));
#48440=CARTESIAN_POINT('Ctrl Pts',(-5.00401925598966,4.55877445849866,1.46186619937435));
#48441=CARTESIAN_POINT('Ctrl Pts',(-5.11971675875143,4.42844066108668,1.47003708074955));
#48442=CARTESIAN_POINT('Ctrl Pts',(-5.23016511913173,4.29390985310798,1.47820796212477));
#48443=CARTESIAN_POINT('Ctrl Pts',(-5.34072043420266,4.15924876975989,1.48638675592247));
#48444=CARTESIAN_POINT('Ctrl Pts',(-5.44601622193107,4.02038283582922,1.49456554972017));
#48445=CARTESIAN_POINT('Ctrl Pts',(-5.54573504425719,3.87777150163566,1.50274434351788));
#48446=CARTESIAN_POINT('Ctrl Pts',(-5.64550296165731,3.73508995488,1.51092716402264));
#48447=CARTESIAN_POINT('Ctrl Pts',(-5.73968824483146,3.58865963579089,1.51910998452742));
#48448=CARTESIAN_POINT('Ctrl Pts',(-5.82801821818632,3.43896679956181,1.52729280503219));
#48449=CARTESIAN_POINT('Ctrl Pts',(-5.91647344082183,3.28906170333373,1.53548722853357));
#48450=CARTESIAN_POINT('Ctrl Pts',(-5.99905658974666,3.1358851631107,1.54368165203496));
#48451=CARTESIAN_POINT('Ctrl Pts',(-6.07554161380753,2.97994682819895,1.55187607553634));
#48452=CARTESIAN_POINT('Ctrl Pts',(-6.14724123871581,2.83376500686494,1.55955780275815));
#48453=CARTESIAN_POINT('Ctrl Pts',(-6.21358230576481,2.68515659461769,1.56723952997996));
#48454=CARTESIAN_POINT('Ctrl Pts',(-6.27441812645904,2.53455443310303,1.57492125720177));
#48455=CARTESIAN_POINT('Ctrl Pts',(-6.34885486612547,2.35028250643317,1.58432036981129));
#48456=CARTESIAN_POINT('Ctrl Pts',(-6.4152027678741,2.16264824857119,1.59371948242081));
#48457=CARTESIAN_POINT('Ctrl Pts',(-6.47319209011458,1.97232684017583,1.60311859503034));
#48458=CARTESIAN_POINT('Ctrl Pts',(-6.53096545521913,1.7827142047869,1.61248270455031));
#48459=CARTESIAN_POINT('Ctrl Pts',(-6.580442309698,1.59043454498714,1.62184681407032));
#48460=CARTESIAN_POINT('Ctrl Pts',(-6.62140321499279,1.39617637298556,1.63121092359029));
#48461=CARTESIAN_POINT('Ctrl Pts',(-6.66224919727079,1.20246322641746,1.64054876045569));
#48462=CARTESIAN_POINT('Ctrl Pts',(-6.6946268655054,1.00678280225882,1.64988659732106));
#48463=CARTESIAN_POINT('Ctrl Pts',(-6.71836691624296,0.809836390101164,
1.65922443418647));
#48464=CARTESIAN_POINT('Ctrl Pts',(-6.74199049957226,0.613856186417202,
1.66851646012795));
#48465=CARTESIAN_POINT('Ctrl Pts',(-6.75706093789863,0.416622543517127,
1.67780848606946));
#48466=CARTESIAN_POINT('Ctrl Pts',(-6.76346042492071,0.218842593046833,
1.68710051201094));
#48467=CARTESIAN_POINT('Ctrl Pts',(-6.76577431460309,0.147330456965178,
1.69046026926653));
#48468=CARTESIAN_POINT('Ctrl Pts',(-6.76695507065543,0.0757470404218229,
1.69382002652209));
#48469=CARTESIAN_POINT('Ctrl Pts',(-6.76699874199978,0.00412622993574791,
1.69717978377767));
#48470=CARTESIAN_POINT('',(-6.76699985285232,0.0014112039775177,1.30282021622242));
#48471=CARTESIAN_POINT('Ctrl Pts',(3.09908550384723,6.01564277861011,0.651473025530862));
#48472=CARTESIAN_POINT('Ctrl Pts',(2.94500347134394,6.09502139381515,0.659666922542915));
#48473=CARTESIAN_POINT('Ctrl Pts',(2.78765915579723,6.16858476961951,0.667860819554956));
#48474=CARTESIAN_POINT('Ctrl Pts',(2.62753232127271,6.23605347160103,0.676054716567009));
#48475=CARTESIAN_POINT('Ctrl Pts',(2.46757388614715,6.30345121927376,0.68423999636424));
#48476=CARTESIAN_POINT('Ctrl Pts',(2.30483908880748,6.36476691599561,0.692425276161489));
#48477=CARTESIAN_POINT('Ctrl Pts',(2.13983261521718,6.41976676981749,0.700610555958718));
#48478=CARTESIAN_POINT('Ctrl Pts',(1.97496591280073,6.47472003519975,0.708788902293637));
#48479=CARTESIAN_POINT('Ctrl Pts',(1.80783170699304,6.523367997734,0.716967248628545));
#48480=CARTESIAN_POINT('Ctrl Pts',(1.63895505841475,6.56552475560764,0.725145594963465));
#48481=CARTESIAN_POINT('Ctrl Pts',(1.47018691803207,6.60765442652895,0.733318686471199));
#48482=CARTESIAN_POINT('Ctrl Pts',(1.29967891415012,6.64330111242377,0.741491777978916));
#48483=CARTESIAN_POINT('Ctrl Pts',(1.12797173330277,6.6723285866982,0.749664869486651));
#48484=CARTESIAN_POINT('Ctrl Pts',(0.956339766498883,6.70134334587416,0.757834380880514));
#48485=CARTESIAN_POINT('Ctrl Pts',(0.783510024817833,6.72374460921029,0.76600389227438));
#48486=CARTESIAN_POINT('Ctrl Pts',(0.610033917780788,6.739447130081,0.774173403668243));
#48487=CARTESIAN_POINT('Ctrl Pts',(0.436567554066994,6.75514876901622,0.782342456219724));
#48488=CARTESIAN_POINT('Ctrl Pts',(0.262455256200104,6.76415237287407,0.790511508771234));
#48489=CARTESIAN_POINT('Ctrl Pts',(0.0882544452816943,6.7664244733011,0.798680561322712));
#48490=CARTESIAN_POINT('Ctrl Pts',(-0.0859486866819264,6.76869660400151,
0.806849722718346));
#48491=CARTESIAN_POINT('Ctrl Pts',(-0.260239972500771,6.76423704688248,
0.815018884113973));
#48492=CARTESIAN_POINT('Ctrl Pts',(-0.434061269699222,6.7530644757878,0.82318804550961));
#48493=CARTESIAN_POINT('Ctrl Pts',(-0.60791708683003,6.74188968588331,0.831358829254771));
#48494=CARTESIAN_POINT('Ctrl Pts',(-0.781302368596437,6.72399924954581,
0.839529612999922));
#48495=CARTESIAN_POINT('Ctrl Pts',(-0.953663358242854,6.69946379937566,
0.847700396745083));
#48496=CARTESIAN_POINT('Ctrl Pts',(-1.12609051198966,6.6749189307983,0.855874317003656));
#48497=CARTESIAN_POINT('Ctrl Pts',(-1.29749223279426,6.64372401867423,0.864048237262222));
#48498=CARTESIAN_POINT('Ctrl Pts',(-1.46732421200396,6.6060009579826,0.872222157520795));
#48499=CARTESIAN_POINT('Ctrl Pts',(-1.63735500078733,6.56823373773015,0.880405646375398));
#48500=CARTESIAN_POINT('Ctrl Pts',(-1.80581202409021,6.5239231819788,0.888589135230002));
#48501=CARTESIAN_POINT('Ctrl Pts',(-1.97216443620976,6.47324157100208,0.896772624084605));
#48502=CARTESIAN_POINT('Ctrl Pts',(-2.13862045505929,6.42252839477231,0.904961209736478));
#48503=CARTESIAN_POINT('Ctrl Pts',(-2.30296890969443,6.36543637371573,0.913149795388368));
#48504=CARTESIAN_POINT('Ctrl Pts',(-2.46469843567633,6.3021861779207,0.921338381040243));
#48505=CARTESIAN_POINT('Ctrl Pts',(-2.62667820868644,6.23883811395078,0.929539637039182));
#48506=CARTESIAN_POINT('Ctrl Pts',(-2.78603062590047,6.16931298165621,0.937740893038129));
#48507=CARTESIAN_POINT('Ctrl Pts',(-2.94226734446068,6.09387822931508,0.945942149037066));
#48508=CARTESIAN_POINT('Ctrl Pts',(-3.06518908596394,6.0345287293186,0.952394618592198));
#48509=CARTESIAN_POINT('Ctrl Pts',(-3.18618266288592,5.97152211066172,0.958847088147319));
#48510=CARTESIAN_POINT('Ctrl Pts',(-3.30502313505015,5.90500728846149,0.965299557702451));
#48511=CARTESIAN_POINT('Ctrl Pts',(-3.45525352507588,5.82092357943833,0.973456349746807));
#48512=CARTESIAN_POINT('Ctrl Pts',(-3.60252087704555,5.73096435441098,0.981613141791164));
#48513=CARTESIAN_POINT('Ctrl Pts',(-3.74632795874808,5.63536297193912,0.989769933835518));
#48514=CARTESIAN_POINT('Ctrl Pts',(-3.8899575636659,5.53987957410176,0.997916659329544));
#48515=CARTESIAN_POINT('Ctrl Pts',(-4.03013509782365,5.43876807929148,1.00606338482358));
#48516=CARTESIAN_POINT('Ctrl Pts',(-4.16638652809531,5.33230834615797,1.01421011031761));
#48517=CARTESIAN_POINT('Ctrl Pts',(-4.30249845329929,5.2259576149795,1.02234849454513));
#48518=CARTESIAN_POINT('Ctrl Pts',(-4.43469199163253,5.11426977035619,1.03048687877263));
#48519=CARTESIAN_POINT('Ctrl Pts',(-4.56252080310049,4.99756870100605,1.03862526300016));
#48520=CARTESIAN_POINT('Ctrl Pts',(-4.6902455927495,4.8809625981769,1.04675702454598));
#48521=CARTESIAN_POINT('Ctrl Pts',(-4.81361245903754,4.75935163870093,1.0548887860918));
#48522=CARTESIAN_POINT('Ctrl Pts',(-4.93220697932092,4.63310083131568,1.06302054763762));
#48523=CARTESIAN_POINT('Ctrl Pts',(-5.05072990096972,4.50692624486713,1.07114739982488));
#48524=CARTESIAN_POINT('Ctrl Pts',(-5.16448596484937,4.37611765467796,1.07927425201212));
#48525=CARTESIAN_POINT('Ctrl Pts',(-5.27309657678577,4.2410778691142,1.08740110419939));
#48526=CARTESIAN_POINT('Ctrl Pts',(-5.38191968449378,4.10577387931734,1.09554385650631));
#48527=CARTESIAN_POINT('Ctrl Pts',(-5.48557692486534,3.96622238171489,1.10368660881325));
#48528=CARTESIAN_POINT('Ctrl Pts',(-5.58372674065851,3.82286341446501,1.11182936112017));
#48529=CARTESIAN_POINT('Ctrl Pts',(-5.68164466879755,3.67984314550352,1.11995287545181));
#48530=CARTESIAN_POINT('Ctrl Pts',(-5.77408096657034,3.53303368568106,1.12807638978344));
#48531=CARTESIAN_POINT('Ctrl Pts',(-5.86073894005466,3.38290231554608,1.13619990411507));
#48532=CARTESIAN_POINT('Ctrl Pts',(-5.94740229380722,3.23276162431794,1.14432392280522));
#48533=CARTESIAN_POINT('Ctrl Pts',(-6.02828642574991,3.07929892872288,1.15244794149537));
#48534=CARTESIAN_POINT('Ctrl Pts',(-6.10313995500485,2.92300730235547,1.16057196018551));
#48535=CARTESIAN_POINT('Ctrl Pts',(-6.17801236954316,2.7666762441579,1.16869802853712));
#48536=CARTESIAN_POINT('Ctrl Pts',(-6.24685099393633,2.60751516382964,1.17682409688876));
#48537=CARTESIAN_POINT('Ctrl Pts',(-6.30945208222826,2.44603831165121,1.18495016524038));
#48538=CARTESIAN_POINT('Ctrl Pts',(-6.37228696229546,2.28395840350418,1.19310658143415));
#48539=CARTESIAN_POINT('Ctrl Pts',(-6.42883749442711,2.11954573955337,1.20126299762787));
#48540=CARTESIAN_POINT('Ctrl Pts',(-6.47894796318552,1.95333619490711,1.20941941382164));
#48541=CARTESIAN_POINT('Ctrl Pts',(-6.52894924828666,1.78748879746097,1.21755805833271));
#48542=CARTESIAN_POINT('Ctrl Pts',(-6.57253845972189,1.61985270788154,1.2256967028438));
#48543=CARTESIAN_POINT('Ctrl Pts',(-6.60961217372183,1.45097067957562,1.23383534735487));
#48544=CARTESIAN_POINT('Ctrl Pts',(-6.64680731991122,1.28153549076212,1.24200064938998));
#48545=CARTESIAN_POINT('Ctrl Pts',(-6.67744416759231,1.11084655455454,1.25016595142508));
#48546=CARTESIAN_POINT('Ctrl Pts',(-6.70147071035139,0.939456927326899,
1.25833125346018));
#48547=CARTESIAN_POINT('Ctrl Pts',(-6.72549725311047,0.768067300099262,
1.26649655549529));
#48548=CARTESIAN_POINT('Ctrl Pts',(-6.74291351265852,0.595977351140993,
1.27466185753042));
#48549=CARTESIAN_POINT('Ctrl Pts',(-6.75371999706329,0.423739544139386,
1.28282715956553));
#48550=CARTESIAN_POINT('Ctrl Pts',(-6.7625400282018,0.283162575341534,1.28949151177365));
#48551=CARTESIAN_POINT('Ctrl Pts',(-6.76697046679597,0.1423230389344,1.29615586398178));
#48552=CARTESIAN_POINT('Ctrl Pts',(-6.76699985285218,0.00141120466605954,
1.30282021618987));
#48553=CARTESIAN_POINT('Ctrl Pts',(-6.76699985285232,0.00141120397761236,
1.30282021622243));
#48554=CARTESIAN_POINT('Ctrl Pts',(-6.76703593212785,-0.171595998423697,
1.31100250224065));
#48555=CARTESIAN_POINT('Ctrl Pts',(-6.76043302341163,-0.344846684814409,
1.31918478825889));
#48556=CARTESIAN_POINT('Ctrl Pts',(-6.74716121089084,-0.517788175077523,
1.32736707427711));
#48557=CARTESIAN_POINT('Ctrl Pts',(-6.7339035463615,-0.690545306593661,
1.33554063783089));
#48558=CARTESIAN_POINT('Ctrl Pts',(-6.71399116002272,-0.862993539468723,
1.34371420138467));
#48559=CARTESIAN_POINT('Ctrl Pts',(-6.68744612489619,-1.03457881604588,
1.35188776493845));
#48560=CARTESIAN_POINT('Ctrl Pts',(-6.66092390272815,-1.20601663123258,
1.36005430408391));
#48561=CARTESIAN_POINT('Ctrl Pts',(-6.62778043765355,-1.37659261032166,
1.36822084322936));
#48562=CARTESIAN_POINT('Ctrl Pts',(-6.58808971705167,-1.54575641033057,
1.37638738237482));
#48563=CARTESIAN_POINT('Ctrl Pts',(-6.54842490917863,-1.71480976901683,
1.38454858986311));
#48564=CARTESIAN_POINT('Ctrl Pts',(-6.50222144160911,-1.8824524327505,1.39270979735142));
#48565=CARTESIAN_POINT('Ctrl Pts',(-6.44960463395322,-2.04814283332223,
1.40087100483971));
#48566=CARTESIAN_POINT('Ctrl Pts',(-6.39601677912313,-2.21689106279759,
1.40918282803092));
#48567=CARTESIAN_POINT('Ctrl Pts',(-6.33577661045198,-2.38361388714914,
1.41749465122212));
#48568=CARTESIAN_POINT('Ctrl Pts',(-6.26907034096874,-2.54775313953022,
1.42580647441332));
#48569=CARTESIAN_POINT('Ctrl Pts',(-6.20360850721721,-2.70883029966387,
1.43396323677059));
#48570=CARTESIAN_POINT('Ctrl Pts',(-6.13191986236707,-2.86741909194896,
1.44211999912783));
#48571=CARTESIAN_POINT('Ctrl Pts',(-6.05422965113859,-3.02301047488663,
1.4502767614851));
#48572=CARTESIAN_POINT('Ctrl Pts',(-5.97653869147967,-3.17860335671747,
1.45843360242072));
#48573=CARTESIAN_POINT('Ctrl Pts',(-5.89284621213306,-3.33119844676367,
1.46659044335637));
#48574=CARTESIAN_POINT('Ctrl Pts',(-5.80342409808935,-3.48031000597875,
1.47474728429199));
#48575=CARTESIAN_POINT('Ctrl Pts',(-5.71398439523565,-3.62945089457071,
1.48290572963081));
#48576=CARTESIAN_POINT('Ctrl Pts',(-5.61881300015372,-3.77510657663525,
1.49106417496961));
#48577=CARTESIAN_POINT('Ctrl Pts',(-5.51822591717691,-3.91681908275032,
1.49922262030843));
#48578=CARTESIAN_POINT('Ctrl Pts',(-5.41431940631598,-4.06320817785083,
1.50765029873511));
#48579=CARTESIAN_POINT('Ctrl Pts',(-5.30463388482756,-4.20538904208645,
1.51607797716176));
#48580=CARTESIAN_POINT('Ctrl Pts',(-5.18956329734131,-4.34289325022939,
1.52450565558844));
#48581=CARTESIAN_POINT('Ctrl Pts',(-5.07800877693082,-4.47619591539258,
1.53267582005531));
#48582=CARTESIAN_POINT('Ctrl Pts',(-4.96139372600185,-4.60510328713949,
1.54084598452221));
#48583=CARTESIAN_POINT('Ctrl Pts',(-4.84011482850923,-4.72922588240878,
1.54901614898908));
#48584=CARTESIAN_POINT('Ctrl Pts',(-4.71310207903707,-4.85921677466381,
1.55757258439566));
#48585=CARTESIAN_POINT('Ctrl Pts',(-4.58097411048328,-4.98395914907564,
1.56612901980223));
#48586=CARTESIAN_POINT('Ctrl Pts',(-4.44422528968739,-5.10305306404931,
1.57468545520881));
#48587=CARTESIAN_POINT('Ctrl Pts',(-4.30747646889149,-5.22214697902299,
1.58324189061539));
#48588=CARTESIAN_POINT('Ctrl Pts',(-4.16610718824954,-5.33559220394104,
1.59179832602198));
#48589=CARTESIAN_POINT('Ctrl Pts',(-4.02064581935871,-5.4430410796974,1.60035476142856));
#48590=CARTESIAN_POINT('Ctrl Pts',(-3.88205876894149,-5.54541205884647,
1.60850683062828));
#48591=CARTESIAN_POINT('Ctrl Pts',(-3.73934588974453,-5.6426443928679,1.61665889982797));
#48592=CARTESIAN_POINT('Ctrl Pts',(-3.59292772261526,-5.73438395820011,
1.62481096902769));
#48593=CARTESIAN_POINT('Ctrl Pts',(-3.44667627812929,-5.82601906202233,
1.63295375567353));
#48594=CARTESIAN_POINT('Ctrl Pts',(-3.29672825103698,-5.91217365526322,
1.64109654231937));
#48595=CARTESIAN_POINT('Ctrl Pts',(-3.14353663765987,-5.99253422248802,
1.64923932896521));
#48596=CARTESIAN_POINT('Ctrl Pts',(-2.99048726144911,-6.07282017558013,
1.65737455509991));
#48597=CARTESIAN_POINT('Ctrl Pts',(-2.83420061636461,-6.14732264439639,
1.6655097812346));
#48598=CARTESIAN_POINT('Ctrl Pts',(-2.67515802192827,-6.21577175881747,
1.6736450073693));
#48599=CARTESIAN_POINT('Ctrl Pts',(-2.51622968654349,-6.28417169816743,
1.68177438901168));
#48600=CARTESIAN_POINT('Ctrl Pts',(-2.35454967862933,-6.34652679859568,
1.68990377065407));
#48601=CARTESIAN_POINT('Ctrl Pts',(-2.19062322316334,-6.40261344250436,
1.69803315229645));
#48602=CARTESIAN_POINT('Ctrl Pts',(-2.02678011070006,-6.45867157100774,
1.7061584008227));
#48603=CARTESIAN_POINT('Ctrl Pts',(-1.86069317044212,-6.50846747201788,
1.71428364934896));
#48604=CARTESIAN_POINT('Ctrl Pts',(-1.69288687471926,-6.551825930945,1.72240889787521));
#48605=CARTESIAN_POINT('Ctrl Pts',(-1.52467828578781,-6.59528833599336,
1.7305536256009));
#48606=CARTESIAN_POINT('Ctrl Pts',(-1.35474243399278,-6.63228226671296,
1.73869835332659));
#48607=CARTESIAN_POINT('Ctrl Pts',(-1.18362257516338,-6.66268163726616,
1.74684308105228));
#48608=CARTESIAN_POINT('Ctrl Pts',(-1.01294189042843,-6.69300298872721,
1.75496690557334));
#48609=CARTESIAN_POINT('Ctrl Pts',(-0.841083633217064,-6.71676353994614,
1.76309073009443));
#48610=CARTESIAN_POINT('Ctrl Pts',(-0.668596442072254,-6.73388949995828,
1.7712145546155));
#48611=CARTESIAN_POINT('Ctrl Pts',(-0.496083192992632,-6.75101804721847,
1.77933960641662));
#48612=CARTESIAN_POINT('Ctrl Pts',(-0.322941184776123,-6.76150997075938,
1.78746465821772));
#48613=CARTESIAN_POINT('Ctrl Pts',(-0.149723408568824,-6.76534344293965,
1.79558971001885));
#48614=CARTESIAN_POINT('Ctrl Pts',(0.0235534855205549,-6.76917822345421,
1.80371753483706));
#48615=CARTESIAN_POINT('Ctrl Pts',(0.196905833599724,-6.76635001921679,
1.81184535965528));
#48616=CARTESIAN_POINT('Ctrl Pts',(0.369781457612505,-6.7568891269286,1.8199731844735));
#48617=CARTESIAN_POINT('Ctrl Pts',(0.543322254846379,-6.74739183198253,
1.82813228270834));
#48618=CARTESIAN_POINT('Ctrl Pts',(0.71638228217314,-6.73121073379521,1.83629138094319));
#48619=CARTESIAN_POINT('Ctrl Pts',(0.888409896509298,-6.70842879188446,
1.84445047917804));
#48620=CARTESIAN_POINT('Ctrl Pts',(1.06008050677724,-6.68569412869681,1.85259264506586));
#48621=CARTESIAN_POINT('Ctrl Pts',(1.23072263383571,-6.65638610654844,1.86073481095369));
#48622=CARTESIAN_POINT('Ctrl Pts',(1.39980035596695,-6.62063803295685,1.86887697684152));
#48623=CARTESIAN_POINT('Ctrl Pts',(1.56940549599356,-6.58477844749073,1.87704454124987));
#48624=CARTESIAN_POINT('Ctrl Pts',(1.73743610402486,-6.54243868313282,1.88521210565824));
#48625=CARTESIAN_POINT('Ctrl Pts',(1.90336891080001,-6.49380287577318,1.89337967006659));
#48626=CARTESIAN_POINT('Ctrl Pts',(2.06930171757522,-6.44516706841352,1.90154723447495));
#48627=CARTESIAN_POINT('Ctrl Pts',(2.23313639867561,-6.39023539501033,1.90971479888331));
#48628=CARTESIAN_POINT('Ctrl Pts',(2.3943724109838,-6.32923927162812,1.91788236329167));
#48629=CARTESIAN_POINT('Ctrl Pts',(2.55628567234072,-6.26798694266289,1.9260842343983));
#48630=CARTESIAN_POINT('Ctrl Pts',(2.71609718244165,-6.20042290644401,1.93428610550492));
#48631=CARTESIAN_POINT('Ctrl Pts',(2.87327686873585,-6.12670947863431,1.94248797661156));
#48632=CARTESIAN_POINT('Ctrl Pts',(3.03026567221649,-6.05308557019464,1.9506798871675));
#48633=CARTESIAN_POINT('Ctrl Pts',(3.18462869154788,-5.97332729029976,1.95887179772344));
#48634=CARTESIAN_POINT('Ctrl Pts',(3.33585230157968,-5.88764625483271,1.96706370827938));
#48635=CARTESIAN_POINT('Ctrl Pts',(3.48692321308562,-5.80205173606637,1.97524734702734));
#48636=CARTESIAN_POINT('Ctrl Pts',(3.63486071542537,-5.71054654706401,1.9834309857753));
#48637=CARTESIAN_POINT('Ctrl Pts',(3.77917237523593,-5.61338980993246,1.99161462452325));
#48638=CARTESIAN_POINT('Ctrl Pts',(3.9233678400085,-5.51631130023436,1.99979167407241));
#48639=CARTESIAN_POINT('Ctrl Pts',(4.06394297796849,-5.4135905055032,2.00796872362158));
#48640=CARTESIAN_POINT('Ctrl Pts',(4.20043109097176,-5.30553179709611,2.01614577317073));
#48641=CARTESIAN_POINT('Ctrl Pts',(4.33683722375847,-5.19753799306875,2.02431791125707));
#48642=CARTESIAN_POINT('Ctrl Pts',(4.4691609387328,-5.08421288525191,2.03249004934339));
#48643=CARTESIAN_POINT('Ctrl Pts',(4.59696557014832,-4.96590339685248,2.04066218742972));
#48644=CARTESIAN_POINT('Ctrl Pts',(4.72473226833609,-4.84762902346193,2.04883189997347));
#48645=CARTESIAN_POINT('Ctrl Pts',(4.84798228667743,-4.72437345802782,2.05700161251722));
#48646=CARTESIAN_POINT('Ctrl Pts',(4.96631288172423,-4.59652318179948,2.06517132506097));
#48647=CARTESIAN_POINT('Ctrl Pts',(5.08462719849755,-4.46869049342963,2.07333991372958));
#48648=CARTESIAN_POINT('Ctrl Pts',(5.19802319349817,-4.33626461754554,2.08150850239818));
#48649=CARTESIAN_POINT('Ctrl Pts',(5.30613580032696,-4.19966806646533,2.08967709106679));
#48650=CARTESIAN_POINT('Ctrl Pts',(5.41425356392816,-4.06306499998096,2.09784606936205));
#48651=CARTESIAN_POINT('Ctrl Pts',(5.51708721291567,-3.92229114543175,2.10601504765731));
#48652=CARTESIAN_POINT('Ctrl Pts',(5.61431270765535,-3.77780118860954,2.11418402595257));
#48653=CARTESIAN_POINT('Ctrl Pts',(5.71156085246089,-3.63327757079085,2.12235490732784));
#48654=CARTESIAN_POINT('Ctrl Pts',(5.80319803940902,-3.48503642649626,2.13052578870311));
#48655=CARTESIAN_POINT('Ctrl Pts',(5.888944200231,-3.33356043991492,2.13869667007839));
#48656=CARTESIAN_POINT('Ctrl Pts',(5.97477339491605,-3.18193776879156,2.14687546387608));
#48657=CARTESIAN_POINT('Ctrl Pts',(6.05469998805779,-3.0270743120676,2.15505425767378));
#48658=CARTESIAN_POINT('Ctrl Pts',(6.12849001961643,-2.86947714391696,2.16323305147148));
#48659=CARTESIAN_POINT('Ctrl Pts',(6.20231638059613,-2.711802385152,2.17141587197627));
#48660=CARTESIAN_POINT('Ctrl Pts',(6.27000001694408,-2.5513915648,2.17959869248106));
#48661=CARTESIAN_POINT('Ctrl Pts',(6.33135566415787,-2.38877049000863,2.18778151298585));
#48662=CARTESIAN_POINT('Ctrl Pts',(6.39279831185822,-2.22591882336021,2.19597593648723));
#48663=CARTESIAN_POINT('Ctrl Pts',(6.44789492419247,-2.06085098194257,2.20417035998862));
#48664=CARTESIAN_POINT('Ctrl Pts',(6.49651018178799,-1.89410782637236,2.21236478349));
#48665=CARTESIAN_POINT('Ctrl Pts',(6.54208375357042,-1.7377972040399,2.22004651071159));
#48666=CARTESIAN_POINT('Ctrl Pts',(6.58196205937282,-1.58001470154794,2.22772823793315));
#48667=CARTESIAN_POINT('Ctrl Pts',(6.61607479780713,-1.42121190180121,2.23540996515473));
#48668=CARTESIAN_POINT('Ctrl Pts',(6.65558914655382,-1.23726333891385,2.2443080619462));
#48669=CARTESIAN_POINT('Ctrl Pts',(6.68745532321374,-1.05153737755717,2.25320615873768));
#48670=CARTESIAN_POINT('Ctrl Pts',(6.71153051444414,-0.864665920275071,
2.26210425552915));
#48671=CARTESIAN_POINT('Ctrl Pts',(6.73556882002407,-0.678080769140777,
2.27098871952805));
#48672=CARTESIAN_POINT('Ctrl Pts',(6.75183992159552,-0.490353885417766,
2.27987318352692));
#48673=CARTESIAN_POINT('Ctrl Pts',(6.76025210269091,-0.302126642425282,
2.28875764752581));
#48674=CARTESIAN_POINT('Ctrl Pts',(6.76864382875009,-0.114357092274315,
2.29762050808671));
#48675=CARTESIAN_POINT('Ctrl Pts',(6.76921476013823,0.0739101251375437,
2.30648336864763));
#48676=CARTESIAN_POINT('Ctrl Pts',(6.76192497390255,0.262029859582791,2.31534622920853));
#48677=CARTESIAN_POINT('Ctrl Pts',(6.75464621330479,0.449865067155732,2.32419568489193));
#48678=CARTESIAN_POINT('Ctrl Pts',(6.73953045916144,0.637552973558179,2.33304514057532));
#48679=CARTESIAN_POINT('Ctrl Pts',(6.71658963936422,0.82444685479736,2.34189459625873));
#48680=CARTESIAN_POINT('Ctrl Pts',(6.69370541990664,1.01087962535048,2.35072221827612));
#48681=CARTESIAN_POINT('Ctrl Pts',(6.66303469078023,1.19652201798138,2.35954984029351));
#48682=CARTESIAN_POINT('Ctrl Pts',(6.6246410713492,1.38073157267928,2.3683774623109));
#48683=CARTESIAN_POINT('Ctrl Pts',(6.58724279776656,1.56016553658314,2.37697623023597));
#48684=CARTESIAN_POINT('Ctrl Pts',(6.54251707201548,1.73823975977284,2.38557499816104));
#48685=CARTESIAN_POINT('Ctrl Pts',(6.49057015165411,1.91436362963172,2.3941737660861));
#48686=CARTESIAN_POINT('Ctrl Pts',(6.44079222121798,2.08313362948909,2.40241350135111));
#48687=CARTESIAN_POINT('Ctrl Pts',(6.38443398140809,2.24993892942386,2.41065323661612));
#48688=CARTESIAN_POINT('Ctrl Pts',(6.32168608733571,2.41424398377341,2.41889297188114));
#48689=CARTESIAN_POINT('Ctrl Pts',(6.25891882191981,2.57859976189143,2.42713525089275));
#48690=CARTESIAN_POINT('Ctrl Pts',(6.18975809724076,2.74045342707464,2.43537752990436));
#48691=CARTESIAN_POINT('Ctrl Pts',(6.11444271380599,2.89928944736205,2.44361980891597));
#48692=CARTESIAN_POINT('Ctrl Pts',(6.03909104120139,3.05820199952183,2.45186605930035));
#48693=CARTESIAN_POINT('Ctrl Pts',(5.957578951542,3.21409369134424,2.46011230968473));
#48694=CARTESIAN_POINT('Ctrl Pts',(5.87019123532304,3.36647350512915,2.46835856006911));
#48695=CARTESIAN_POINT('Ctrl Pts',(5.78269832855263,3.51903674190916,2.47661473664978));
#48696=CARTESIAN_POINT('Ctrl Pts',(5.68931584344398,3.66807935094485,2.48487091323046));
#48697=CARTESIAN_POINT('Ctrl Pts',(5.59037252578222,3.81313834301607,2.49312708981114));
#48698=CARTESIAN_POINT('Ctrl Pts',(5.4913610582128,3.95829724842301,2.50138895305854));
#48699=CARTESIAN_POINT('Ctrl Pts',(5.38678133114394,4.09946678412285,2.50965081630594));
#48700=CARTESIAN_POINT('Ctrl Pts',(5.2770024321496,4.23621698347561,2.51791267955333));
#48701=CARTESIAN_POINT('Ctrl Pts',(5.16706766260978,4.3731613488144,2.5261862734807));
#48702=CARTESIAN_POINT('Ctrl Pts',(5.05191920593846,4.50567357863123,2.53445986740805));
#48703=CARTESIAN_POINT('Ctrl Pts',(4.93196376787249,4.63335973051878,2.54273346133542));
#48704=CARTESIAN_POINT('Ctrl Pts',(4.88264872300639,4.68585295975988,2.54613482989619));
#48705=CARTESIAN_POINT('Ctrl Pts',(4.83252163703819,4.73753098419086,2.54953619845697));
#48706=CARTESIAN_POINT('Ctrl Pts',(4.78161236962705,4.78836842219034,2.55293756701775));
#48707=CARTESIAN_POINT('Ctrl Pts',(4.65537813259575,4.91442455155208,2.56137157494924));
#48708=CARTESIAN_POINT('Ctrl Pts',(4.5240411366395,5.03560058765171,2.56980558288074));
#48709=CARTESIAN_POINT('Ctrl Pts',(4.38800578918041,5.15147495326525,2.57823959081223));
#48710=CARTESIAN_POINT('Ctrl Pts',(4.25208352366071,5.26725299613449,2.58666658781611));
#48711=CARTESIAN_POINT('Ctrl Pts',(4.11147094151205,5.37773793266703,2.59509358481999));
#48712=CARTESIAN_POINT('Ctrl Pts',(3.96660893953291,5.48254525934968,2.60352058182387));
#48713=CARTESIAN_POINT('Ctrl Pts',(3.82187371122521,5.58726086557137,2.61194020407568));
#48714=CARTESIAN_POINT('Ctrl Pts',(3.67289674888787,5.68630857373254,2.62035982632747));
#48715=CARTESIAN_POINT('Ctrl Pts',(3.52015165274744,5.77934436953358,2.62877944857928));
#48716=CARTESIAN_POINT('Ctrl Pts',(3.38272405843464,5.86305039954687,2.63635473878712));
#48717=CARTESIAN_POINT('Ctrl Pts',(3.2422467575683,5.94189023337968,2.64393002899497));
#48718=CARTESIAN_POINT('Ctrl Pts',(3.09908550384727,6.01564277861009,2.65150531920281));
#48719=CARTESIAN_POINT('Origin',(0.,0.,-63.6971797838103));
#48720=CARTESIAN_POINT('',(3.09908550384713,6.01564277861016,5.04570102894007));
#48721=CARTESIAN_POINT('',(3.09908550384716,6.01564277861015,4.65139679042609));
#48722=CARTESIAN_POINT('',(3.09908550384721,6.01564277861012,-63.6971797838103));
#48723=CARTESIAN_POINT('',(-6.76699851873671,-0.00447743399645792,3.6971797838519));
#48724=CARTESIAN_POINT('Ctrl Pts',(-6.76699851873671,-0.00447743399636642,
3.69717978385191));
#48725=CARTESIAN_POINT('Ctrl Pts',(-6.76686776413152,-0.202094243171143,
3.70644559443041));
#48726=CARTESIAN_POINT('Ctrl Pts',(-6.75807649647211,-0.399395897026799,
3.71571140500891));
#48727=CARTESIAN_POINT('Ctrl Pts',(-6.74073150822531,-0.595674184448696,
3.7249772155874));
#48728=CARTESIAN_POINT('Ctrl Pts',(-6.72332256944408,-0.79267614496839,
3.73427718897591));
#48729=CARTESIAN_POINT('Ctrl Pts',(-6.69729681504176,-0.988647016979515,
3.74357716236443));
#48730=CARTESIAN_POINT('Ctrl Pts',(-6.66281218223202,-1.18288749435462,
3.75287713575294));
#48731=CARTESIAN_POINT('Ctrl Pts',(-6.62816067813818,-1.37806790222179,
3.76222211175204));
#48732=CARTESIAN_POINT('Ctrl Pts',(-6.58496831618429,-1.57150096816226,
3.77156708775114));
#48733=CARTESIAN_POINT('Ctrl Pts',(-6.53344434709676,-1.76249651443324,
3.78091206375024));
#48734=CARTESIAN_POINT('Ctrl Pts',(-6.50274784322497,-1.87628618610319,
3.78647953258112));
#48735=CARTESIAN_POINT('Ctrl Pts',(-6.46909501792016,-1.98921105644742,
3.79204700141197));
#48736=CARTESIAN_POINT('Ctrl Pts',(-6.43253814042731,-2.10112876139182,
3.79761447024285));
#48737=CARTESIAN_POINT('Ctrl Pts',(-6.37387008642234,-2.28073912223503,
3.80654938439423));
#48738=CARTESIAN_POINT('Ctrl Pts',(-6.30763797513442,-2.45800506845748,
3.8154842985456));
#48739=CARTESIAN_POINT('Ctrl Pts',(-6.23404071453184,-2.63230419396379,
3.82441921269698));
#48740=CARTESIAN_POINT('Ctrl Pts',(-6.16055367844835,-2.80634227663877,
3.83334074528216));
#48741=CARTESIAN_POINT('Ctrl Pts',(-6.07972360312658,-2.97742216707847,
3.84226227786734));
#48742=CARTESIAN_POINT('Ctrl Pts',(-5.9917982268079,-3.14493926956019,3.85118381045251));
#48743=CARTESIAN_POINT('Ctrl Pts',(-5.90408727843435,-3.31204783983466,
3.86008358565682));
#48744=CARTESIAN_POINT('Ctrl Pts',(-5.80931568407483,-3.47561073504441,
3.86898336086114));
#48745=CARTESIAN_POINT('Ctrl Pts',(-5.70777771719143,-3.63504642764477,
3.87788313606545));
#48746=CARTESIAN_POINT('Ctrl Pts',(-5.60639602489657,-3.79423673669034,
3.88676921384454));
#48747=CARTESIAN_POINT('Ctrl Pts',(-5.49826887131707,-3.94931229701519,
3.89565529162364));
#48748=CARTESIAN_POINT('Ctrl Pts',(-5.38373602133471,-4.09971650880682,
3.90454136940274));
#48749=CARTESIAN_POINT('Ctrl Pts',(-5.26949589102941,-4.24973632195375,
3.91340473640655));
#48750=CARTESIAN_POINT('Ctrl Pts',(-5.14888288868192,-4.39510840494872,
3.9222681034104));
#48751=CARTESIAN_POINT('Ctrl Pts',(-5.02227914829755,-4.53530607088162,
3.93113147041421));
#48752=CARTESIAN_POINT('Ctrl Pts',(-4.90207127817228,-4.66842111761849,
3.93954707066767));
#48753=CARTESIAN_POINT('Ctrl Pts',(-4.77646309170414,-4.79687137201919,
3.9479626709211));
#48754=CARTESIAN_POINT('Ctrl Pts',(-4.64581777032901,-4.92023030405033,
3.95637827117456));
#48755=CARTESIAN_POINT('Ctrl Pts',(-4.51835837990954,-5.04058099180545,
3.96458864768887));
#48756=CARTESIAN_POINT('Ctrl Pts',(-4.38622634044855,-5.15596923144747,
3.97279902420316));
#48757=CARTESIAN_POINT('Ctrl Pts',(-4.24985108100136,-5.26602836958856,
3.98100940071744));
#48758=CARTESIAN_POINT('Ctrl Pts',(-4.11344336853475,-5.37611369834049,
3.98922173104292));
#48759=CARTESIAN_POINT('Ctrl Pts',(-3.97279070135292,-5.4808671755143,3.99743406136838));
#48760=CARTESIAN_POINT('Ctrl Pts',(-3.8283542946149,-5.57996347612631,4.00564639169386));
#48761=CARTESIAN_POINT('Ctrl Pts',(-3.6838577994082,-5.67910100280515,4.01386213851497));
#48762=CARTESIAN_POINT('Ctrl Pts',(-3.53557472192143,-5.77257646303051,
4.02207788533611));
#48763=CARTESIAN_POINT('Ctrl Pts',(-3.38399391700499,-5.86010871654044,
4.03029363215722));
#48764=CARTESIAN_POINT('Ctrl Pts',(-3.23224285304114,-5.94773928829131,
4.03851860709418));
#48765=CARTESIAN_POINT('Ctrl Pts',(-3.07718697174119,-6.02941314203681,
4.04674358203113));
#48766=CARTESIAN_POINT('Ctrl Pts',(-2.91933917756931,-6.1048953935599,4.05496855696809));
#48767=CARTESIAN_POINT('Ctrl Pts',(-2.76139025085872,-6.18042600630188,
4.0631988016182));
#48768=CARTESIAN_POINT('Ctrl Pts',(-2.60064617143321,-6.24975696832185,
4.07142904626831));
#48769=CARTESIAN_POINT('Ctrl Pts',(-2.43763827545052,-6.31270216611386,
4.07965929091841));
#48770=CARTESIAN_POINT('Ctrl Pts',(-2.27440686957213,-6.37573367183904,
4.08790082055022));
#48771=CARTESIAN_POINT('Ctrl Pts',(-2.10890578288484,-6.43236180945014,
4.09614235018204));
#48772=CARTESIAN_POINT('Ctrl Pts',(-1.94168086722592,-6.48245049420733,
4.10438387981385));
#48773=CARTESIAN_POINT('Ctrl Pts',(-1.86891776461991,-6.50424514181726,
4.10796994391122));
#48774=CARTESIAN_POINT('Ctrl Pts',(-1.79582841503726,-6.52480232806352,
4.11155600800859));
#48775=CARTESIAN_POINT('Ctrl Pts',(-1.72245825573738,-6.54411388632886,
4.11514207210595));
#48776=CARTESIAN_POINT('Ctrl Pts',(-1.54960436937608,-6.58961028336151,
4.12359053564869));
#48777=CARTESIAN_POINT('Ctrl Pts',(-1.37479715599412,-6.62829333036955,
4.13203899919145));
#48778=CARTESIAN_POINT('Ctrl Pts',(-1.19860077262665,-6.66000339248103,
4.1404874627342));
#48779=CARTESIAN_POINT('Ctrl Pts',(-1.02256534778356,-6.6916844868878,4.14892820845551));
#48780=CARTESIAN_POINT('Ctrl Pts',(-0.845143609124331,-6.71640523485003,
4.15736895417682));
#48781=CARTESIAN_POINT('Ctrl Pts',(-0.666912211242663,-6.73405651167968,
4.16580969989813));
#48782=CARTESIAN_POINT('Ctrl Pts',(-0.488816221044837,-6.75169437831033,
4.17424403293435));
#48783=CARTESIAN_POINT('Ctrl Pts',(-0.309912128539771,-6.76227344797985,
4.18267836597059));
#48784=CARTESIAN_POINT('Ctrl Pts',(-0.130784456218596,-6.76573605944036,
4.19111269900681));
#48785=CARTESIAN_POINT('Ctrl Pts',(0.0482346374308115,-6.76919657203057,
4.19954191955166));
#48786=CARTESIAN_POINT('Ctrl Pts',(0.227476708134517,-6.76554922029455,
4.2079711400965));
#48787=CARTESIAN_POINT('Ctrl Pts',(0.406354063323646,-6.75478832941643,
4.21640036064136));
#48788=CARTESIAN_POINT('Ctrl Pts',(0.585150432551974,-6.74403231048582,
4.22482576489251));
#48789=CARTESIAN_POINT('Ctrl Pts',(0.763582083236608,-6.72616919437579,
4.23325116914365));
#48790=CARTESIAN_POINT('Ctrl Pts',(0.941062878659978,-6.70124538115179,
4.2416765733948));
#48791=CARTESIAN_POINT('Ctrl Pts',(1.11850467810437,-6.6763270441738,4.25010012642094));
#48792=CARTESIAN_POINT('Ctrl Pts',(1.29499570857545,-6.64435114693832,4.2585236794471));
#48793=CARTESIAN_POINT('Ctrl Pts',(1.46995596456517,-6.60541584324858,4.26694723247324));
#48794=CARTESIAN_POINT('Ctrl Pts',(1.64489663942007,-6.56648489710521,4.27536984275541));
#48795=CARTESIAN_POINT('Ctrl Pts',(1.81830655595167,-6.52059616966518,4.28379245303755));
#48796=CARTESIAN_POINT('Ctrl Pts',(1.9896165852714,-6.46789879664277,4.29221506331972));
#48797=CARTESIAN_POINT('Ctrl Pts',(2.16093133193039,-6.4151999725005,4.30063790553407));
#48798=CARTESIAN_POINT('Ctrl Pts',(2.33014575753758,-6.35569222737254,4.30906074774842));
#48799=CARTESIAN_POINT('Ctrl Pts',(2.49670620794372,-6.28957447775407,4.31748358996278));
#48800=CARTESIAN_POINT('Ctrl Pts',(2.66329447389768,-6.22344568649022,4.32590783878938));
#48801=CARTESIAN_POINT('Ctrl Pts',(2.82722757139699,-6.15070481350569,4.33433208761599));
#48802=CARTESIAN_POINT('Ctrl Pts',(2.98797178732154,-6.07159893258527,4.34275633644259));
#48803=CARTESIAN_POINT('Ctrl Pts',(3.14882456704112,-5.99243962495463,4.35118627485758));
#48804=CARTESIAN_POINT('Ctrl Pts',(3.30648386213934,-5.90690686675807,4.35961621327255));
#48805=CARTESIAN_POINT('Ctrl Pts',(3.46043963705768,-5.81529419017475,4.36804615168754));
#48806=CARTESIAN_POINT('Ctrl Pts',(3.61445045025472,-5.72364876260154,4.37647910375563));
#48807=CARTESIAN_POINT('Ctrl Pts',(3.76475481996355,-5.62591925847709,4.38491205582374));
#48808=CARTESIAN_POINT('Ctrl Pts',(3.91087120384815,-5.52244288579895,4.39334500789184));
#48809=CARTESIAN_POINT('Ctrl Pts',(4.05712202136199,-5.41887131021507,4.40178571865421));
#48810=CARTESIAN_POINT('Ctrl Pts',(4.1991768860085,-5.30954249988483,4.41022642941658));
#48811=CARTESIAN_POINT('Ctrl Pts',(4.33658601516312,-5.19483500537713,4.41866714017895));
#48812=CARTESIAN_POINT('Ctrl Pts',(4.41256997860826,-5.13140450317413,4.42333465144232));
#48813=CARTESIAN_POINT('Ctrl Pts',(4.48713396538458,-5.06632998999995,4.4280021627057));
#48814=CARTESIAN_POINT('Ctrl Pts',(4.56020668196633,-4.99968039156001,4.43266967396907));
#48815=CARTESIAN_POINT('Ctrl Pts',(4.68766484965754,-4.88342584277769,4.44081104958964));
#48816=CARTESIAN_POINT('Ctrl Pts',(4.81083698689081,-4.76214595966299,4.44895242521021));
#48817=CARTESIAN_POINT('Ctrl Pts',(4.92930031154187,-4.63619320549017,4.45709380083078));
#48818=CARTESIAN_POINT('Ctrl Pts',(5.04766022586806,-4.51035039939848,4.46522806959105));
#48819=CARTESIAN_POINT('Ctrl Pts',(5.16131926047743,-4.37984310656541,4.47336233835132));
#48820=CARTESIAN_POINT('Ctrl Pts',(5.26988909277935,-4.24506277336452,4.48149660711159));
#48821=CARTESIAN_POINT('Ctrl Pts',(5.37838486178295,-4.11037438353145,4.48962532690158));
#48822=CARTESIAN_POINT('Ctrl Pts',(5.48179811185529,-3.97141904080256,4.49775404669156));
#48823=CARTESIAN_POINT('Ctrl Pts',(5.57977870456578,-3.8286235918505,4.50588276648155));
#48824=CARTESIAN_POINT('Ctrl Pts',(5.67771257065771,-3.68589624157279,4.51400760971212));
#48825=CARTESIAN_POINT('Ctrl Pts',(5.77021873195068,-3.5393327330905,4.52213245294268));
#48826=CARTESIAN_POINT('Ctrl Pts',(5.85698856180224,-3.38939138886581,4.53025729617325));
#48827=CARTESIAN_POINT('Ctrl Pts',(5.94373409947056,-3.23949202239556,4.53837986476319));
#48828=CARTESIAN_POINT('Ctrl Pts',(6.02474632197434,-3.08621702072262,4.54650243335314));
#48829=CARTESIAN_POINT('Ctrl Pts',(6.09976103573944,-2.93005192904066,4.55462500194308));
#48830=CARTESIAN_POINT('Ctrl Pts',(6.17477973512309,-2.77387854012668,4.56274800209449));
#48831=CARTESIAN_POINT('Ctrl Pts',(6.24380012715659,-2.61481508271665,4.57087100224589));
#48832=CARTESIAN_POINT('Ctrl Pts',(6.30660484032441,-2.45337000633754,4.57899400239729));
#48833=CARTESIAN_POINT('Ctrl Pts',(6.33866432113846,-2.37095827212793,4.58314049323168));
#48834=CARTESIAN_POINT('Ctrl Pts',(6.36910493527291,-2.28792628966559,4.58728698406607));
#48835=CARTESIAN_POINT('Ctrl Pts',(6.39790266492223,-2.20434355085161,4.59143347490046));
#48836=CARTESIAN_POINT('Ctrl Pts',(6.46029499361516,-2.02325560480029,4.60041714209268));
#48837=CARTESIAN_POINT('Ctrl Pts',(6.51494192559734,-1.83967109875961,4.60940080928488));
#48838=CARTESIAN_POINT('Ctrl Pts',(6.56168958327112,-1.65424267046623,4.6183844764771));
#48839=CARTESIAN_POINT('Ctrl Pts',(6.60851755533095,-1.46849566855624,4.62738357797665));
#48840=CARTESIAN_POINT('Ctrl Pts',(6.64741906944594,-1.28089864450445,4.63638267947621));
#48841=CARTESIAN_POINT('Ctrl Pts',(6.67829134828466,-1.09211431060412,4.64538178097575));
#48842=CARTESIAN_POINT('Ctrl Pts',(6.70923601581433,-0.902887319040711,
4.6544019833853));
#48843=CARTESIAN_POINT('Ctrl Pts',(6.73211374025193,-0.712467684336141,
4.66342218579482));
#48844=CARTESIAN_POINT('Ctrl Pts',(6.74687333082256,-0.521525893734312,
4.67244238820436));
#48845=CARTESIAN_POINT('Ctrl Pts',(6.7616478695633,-0.33039072172708,4.68147172606515));
#48846=CARTESIAN_POINT('Ctrl Pts',(6.76828783679952,-0.13873257604197,4.69050106392597));
#48847=CARTESIAN_POINT('Ctrl Pts',(6.7667941920583,0.0527765319631494,4.69953040178676));
#48848=CARTESIAN_POINT('Ctrl Pts',(6.76529844154432,0.244555633664026,4.70857246940398));
#48849=CARTESIAN_POINT('Ctrl Pts',(6.75564615263741,0.436185038294863,4.7176145370212));
#48850=CARTESIAN_POINT('Ctrl Pts',(6.73789043526874,0.626994005006506,4.72665660463842));
#48851=CARTESIAN_POINT('Ctrl Pts',(6.72248166218426,0.792581911678803,4.73450349503633));
#48852=CARTESIAN_POINT('Ctrl Pts',(6.70097092684326,0.957551909317143,4.74235038543425));
#48853=CARTESIAN_POINT('Ctrl Pts',(6.67342442468385,1.12147021718506,4.75019727583216));
#48854=CARTESIAN_POINT('Ctrl Pts',(6.64304648950995,1.30223725981751,4.75885072760054));
#48855=CARTESIAN_POINT('Ctrl Pts',(6.60530011697497,1.48188441432217,4.76750417936893));
#48856=CARTESIAN_POINT('Ctrl Pts',(6.56028481952129,1.65980483393636,4.77615763113732));
#48857=CARTESIAN_POINT('Ctrl Pts',(6.51531099087796,1.83756135042082,4.78480311120786));
#48858=CARTESIAN_POINT('Ctrl Pts',(6.46308166746408,2.01359401099816,4.7934485912784));
#48859=CARTESIAN_POINT('Ctrl Pts',(6.40374738637307,2.18730619976264,4.80209407134893));
#48860=CARTESIAN_POINT('Ctrl Pts',(6.34262800292173,2.36624460906066,4.81099965513348));
#48861=CARTESIAN_POINT('Ctrl Pts',(6.27396951615173,2.54272041893106,4.819905238918));
#48862=CARTESIAN_POINT('Ctrl Pts',(6.19799251255383,2.7160960613216,4.82881082270255));
#48863=CARTESIAN_POINT('Ctrl Pts',(6.12437450848591,2.88408858724872,4.83743989824162));
#48864=CARTESIAN_POINT('Ctrl Pts',(6.04388575616793,3.04917026101768,4.8460689737807));
#48865=CARTESIAN_POINT('Ctrl Pts',(5.95677668112415,3.21077881069618,4.85469804931977));
#48866=CARTESIAN_POINT('Ctrl Pts',(5.86548064930897,3.3801551849217,4.86374188722706));
#48867=CARTESIAN_POINT('Ctrl Pts',(5.76691229103232,3.54571600631978,4.87278572513433));
#48868=CARTESIAN_POINT('Ctrl Pts',(5.66141575166245,3.70683971690553,4.88182956304162));
#48869=CARTESIAN_POINT('Ctrl Pts',(5.55591921229258,3.86796342749129,4.89087340094891));
#48870=CARTESIAN_POINT('Ctrl Pts',(5.44349467392716,4.02464968591883,4.89991723885619));
#48871=CARTESIAN_POINT('Ctrl Pts',(5.32454098894455,4.17630844850442,4.90896107676348));
#48872=CARTESIAN_POINT('Ctrl Pts',(5.21372353180683,4.31759401208191,4.91738633168347));
#48873=CARTESIAN_POINT('Ctrl Pts',(5.09728824589692,4.45445456856581,4.92581158660348));
#48874=CARTESIAN_POINT('Ctrl Pts',(4.97562218340768,4.58644447126327,4.93423684152347));
#48875=CARTESIAN_POINT('Ctrl Pts',(4.85392901435793,4.71846378061868,4.94266397354607));
#48876=CARTESIAN_POINT('Ctrl Pts',(4.72700297008946,4.8456100292338,4.95109110556866));
#48877=CARTESIAN_POINT('Ctrl Pts',(4.59526875740729,4.96747360810266,4.95951823759125));
#48878=CARTESIAN_POINT('Ctrl Pts',(4.46343886480488,5.08942569774841,4.96795149032694));
#48879=CARTESIAN_POINT('Ctrl Pts',(4.32679406965878,5.20608722611458,4.97638474306262));
#48880=CARTESIAN_POINT('Ctrl Pts',(4.18579381123436,5.31708747058314,4.98481799579831));
#48881=CARTESIAN_POINT('Ctrl Pts',(4.04473729166143,5.42813200575943,4.99325461352417));
#48882=CARTESIAN_POINT('Ctrl Pts',(3.89932210751482,5.53351055251236,5.00169123125004));
#48883=CARTESIAN_POINT('Ctrl Pts',(3.75003810094601,5.63289474794739,5.0101278489759));
#48884=CARTESIAN_POINT('Ctrl Pts',(3.60061690377252,5.73237027652774,5.01857221987448));
#48885=CARTESIAN_POINT('Ctrl Pts',(3.44732006085961,5.82584027050847,5.02701659077309));
#48886=CARTESIAN_POINT('Ctrl Pts',(3.29066442005884,5.91302094318622,5.03546096167167));
#48887=CARTESIAN_POINT('Ctrl Pts',(3.2273415935653,5.94826082718493,5.03887431742781));
#48888=CARTESIAN_POINT('Ctrl Pts',(3.16347023679114,5.98247362281432,5.04228767318394));
#48889=CARTESIAN_POINT('Ctrl Pts',(3.09908550384713,6.01564277861016,5.04570102894007));
#48890=CARTESIAN_POINT('Ctrl Pts',(3.0990855038473,6.01564277861008,3.04562247039135));
#48891=CARTESIAN_POINT('Ctrl Pts',(2.94198259178318,6.09657766376005,3.05392813220987));
#48892=CARTESIAN_POINT('Ctrl Pts',(2.78177728831488,6.17131830222165,3.06223379402837));
#48893=CARTESIAN_POINT('Ctrl Pts',(2.61899753780536,6.23964268984767,3.07053945584688));
#48894=CARTESIAN_POINT('Ctrl Pts',(2.45602509856137,6.30804795571404,3.07885494940098));
#48895=CARTESIAN_POINT('Ctrl Pts',(2.29047244483192,6.37002166148446,3.08717044295508));
#48896=CARTESIAN_POINT('Ctrl Pts',(2.12288585117006,6.42539062337085,3.09548593650918));
#48897=CARTESIAN_POINT('Ctrl Pts',(1.95519200029967,6.48079502198377,3.1038067520679));
#48898=CARTESIAN_POINT('Ctrl Pts',(1.78546194739057,6.52958615091888,3.1121275676266));
#48899=CARTESIAN_POINT('Ctrl Pts',(1.61425441948635,6.5716414744848,3.12044838318532));
#48900=CARTESIAN_POINT('Ctrl Pts',(1.44279498787196,6.6137586755404,3.12878144145518));
#48901=CARTESIAN_POINT('Ctrl Pts',(1.26985407772748,6.64912019672616,3.13711449972508));
#48902=CARTESIAN_POINT('Ctrl Pts',(1.09599913746674,6.67765489454735,3.14544755799494));
#48903=CARTESIAN_POINT('Ctrl Pts',(0.97699700697648,6.6971866365187,3.15115146083559));
#48904=CARTESIAN_POINT('Ctrl Pts',(0.857566756986758,6.71352090508499,3.15685536367623));
#48905=CARTESIAN_POINT('Ctrl Pts',(0.737890778038132,6.72664895766728,3.16255926651688));
#48906=CARTESIAN_POINT('Ctrl Pts',(0.568537405535535,6.74522645332459,3.17063085440759));
#48907=CARTESIAN_POINT('Ctrl Pts',(0.398170534689765,6.75743827932392,3.17870244229829));
#48908=CARTESIAN_POINT('Ctrl Pts',(0.227320024121162,6.76318080540758,3.186774030189));
#48909=CARTESIAN_POINT('Ctrl Pts',(0.0566839668140396,6.76891612341534,
3.19483548654225));
#48910=CARTESIAN_POINT('Ctrl Pts',(-0.114434154292643,6.76819828652658,
3.20289694289552));
#48911=CARTESIAN_POINT('Ctrl Pts',(-0.285495674491022,6.76097487200233,
3.21095839924877));
#48912=CARTESIAN_POINT('Ctrl Pts',(-0.456379988047669,6.75375894038264,
3.21901150455026));
#48913=CARTESIAN_POINT('Ctrl Pts',(-0.627207447921226,6.74005085810645,
3.22706460985174));
#48914=CARTESIAN_POINT('Ctrl Pts',(-0.797435769424155,6.71985008714056,
3.23511771515324));
#48915=CARTESIAN_POINT('Ctrl Pts',(-0.967525020543475,6.69966581947413,
3.24316424135888));
#48916=CARTESIAN_POINT('Ctrl Pts',(-1.13701573904788,6.67299946420441,3.25121076756455));
#48917=CARTESIAN_POINT('Ctrl Pts',(-1.30536725142705,6.63990250974378,3.25925729377019));
#48918=CARTESIAN_POINT('Ctrl Pts',(-1.47361805046999,6.60682535495502,3.26729900628282));
#48919=CARTESIAN_POINT('Ctrl Pts',(-1.64073063505616,6.56732533099749,3.27534071879545));
#48920=CARTESIAN_POINT('Ctrl Pts',(-1.80617116299231,6.52150555699948,3.28338243130808));
#48921=CARTESIAN_POINT('Ctrl Pts',(-1.97478619091406,6.47480658566263,3.29157844951941));
#48922=CARTESIAN_POINT('Ctrl Pts',(-2.14166395004368,6.4215429198229,3.29977446773074));
#48923=CARTESIAN_POINT('Ctrl Pts',(-2.30625148463374,6.3618781102458,3.30797048594206));
#48924=CARTESIAN_POINT('Ctrl Pts',(-2.46768464545086,6.30335679620113,3.31600942479162));
#48925=CARTESIAN_POINT('Ctrl Pts',(-2.62691421728593,6.23867763171685,3.32404836364116));
#48926=CARTESIAN_POINT('Ctrl Pts',(-2.78343544430358,6.16804475724638,3.33208730249072));
#48927=CARTESIAN_POINT('Ctrl Pts',(-2.93997183450435,6.09740504013079,3.3401270201222));
#48928=CARTESIAN_POINT('Ctrl Pts',(-3.0937990169911,6.02081061809264,3.3481667377537));
#48929=CARTESIAN_POINT('Ctrl Pts',(-3.24443416750943,5.93851293950745,3.35620645538518));
#48930=CARTESIAN_POINT('Ctrl Pts',(-3.39511373456322,5.85619099448944,3.36424854362141));
#48931=CARTESIAN_POINT('Ctrl Pts',(-3.54259906864289,5.76816262455319,3.37229063185763));
#48932=CARTESIAN_POINT('Ctrl Pts',(-3.68643393892883,5.67472411786808,3.38033272009386));
#48933=CARTESIAN_POINT('Ctrl Pts',(-3.83511137773307,5.57813976504727,3.38864556578436));
#48934=CARTESIAN_POINT('Ctrl Pts',(-3.97988789073937,5.47577486069885,3.39695841147487));
#48935=CARTESIAN_POINT('Ctrl Pts',(-4.12029512519974,5.36800308133809,3.40527125716537));
#48936=CARTESIAN_POINT('Ctrl Pts',(-4.25636500106121,5.26356050973309,3.41332730844726));
#48937=CARTESIAN_POINT('Ctrl Pts',(-4.38833129304228,5.15404043836785,3.42138335972915));
#48938=CARTESIAN_POINT('Ctrl Pts',(-4.51580438545681,5.03982140083248,3.42943941101105));
#48939=CARTESIAN_POINT('Ctrl Pts',(-4.64937246961748,4.92014110023488,3.43788065390585));
#48940=CARTESIAN_POINT('Ctrl Pts',(-4.77800678073316,4.79530178657098,3.44632189680064));
#48941=CARTESIAN_POINT('Ctrl Pts',(-4.90130605290549,4.66577838905279,3.45476313969544));
#48942=CARTESIAN_POINT('Ctrl Pts',(-5.02460532507778,4.53625499153463,3.46320438259025));
#48943=CARTESIAN_POINT('Ctrl Pts',(-5.1425693182831,4.40204791278835,3.47164562548506));
#48944=CARTESIAN_POINT('Ctrl Pts',(-5.25484872399403,4.26366671867518,3.48008686837986));
#48945=CARTESIAN_POINT('Ctrl Pts',(-5.36544908633879,4.12735489805491,3.48840187964033));
#48946=CARTESIAN_POINT('Ctrl Pts',(-5.47089587792703,3.98654743576582,3.49671689090081));
#48947=CARTESIAN_POINT('Ctrl Pts',(-5.57080753044914,3.84166532361828,3.50503190216128));
#48948=CARTESIAN_POINT('Ctrl Pts',(-5.67054849216198,3.69703073059735,3.51333270791153));
#48949=CARTESIAN_POINT('Ctrl Pts',(-5.76477296970168,3.54833565032679,3.52163351366177));
#48950=CARTESIAN_POINT('Ctrl Pts',(-5.85313928068442,3.39603438747447,3.52993431941202));
#48951=CARTESIAN_POINT('Ctrl Pts',(-5.94141619507938,3.24388720158953,3.53822672757611));
#48952=CARTESIAN_POINT('Ctrl Pts',(-6.02384657241075,3.08814139897192,3.5465191357402));
#48953=CARTESIAN_POINT('Ctrl Pts',(-6.10013110229294,2.92928140246689,3.55481154390429));
#48954=CARTESIAN_POINT('Ctrl Pts',(-6.1763513325648,2.77055530776197,3.56309696246493));
#48955=CARTESIAN_POINT('Ctrl Pts',(-6.24643588385274,2.60872056119268,3.57138238102557));
#48956=CARTESIAN_POINT('Ctrl Pts',(-6.31013052885371,2.44428756672132,3.5796677995862));
#48957=CARTESIAN_POINT('Ctrl Pts',(-6.3737822314333,2.27996543166265,3.58794763218376));
#48958=CARTESIAN_POINT('Ctrl Pts',(-6.43105248490995,2.11304886338099,3.59622746478131));
#48959=CARTESIAN_POINT('Ctrl Pts',(-6.4817344408519,1.94406986455588,3.60450729737887));
#48960=CARTESIAN_POINT('Ctrl Pts',(-6.53239046240314,1.77517733373101,3.61278289311521));
#48961=CARTESIAN_POINT('Ctrl Pts',(-6.57646480485888,1.60422480958536,3.62105848885156));
#48962=CARTESIAN_POINT('Ctrl Pts',(-6.61379985985277,1.4317612977768,3.6293340845879));
#48963=CARTESIAN_POINT('Ctrl Pts',(-6.65112325433395,1.25935164990315,3.6376070956839));
#48964=CARTESIAN_POINT('Ctrl Pts',(-6.68171148249384,1.08543229603188,3.64588010677991));
#48965=CARTESIAN_POINT('Ctrl Pts',(-6.70545756805903,0.910564551780863,
3.65415311787591));
#48966=CARTESIAN_POINT('Ctrl Pts',(-6.729203618725,0.735697064530014,3.6624261168132));
#48967=CARTESIAN_POINT('Ctrl Pts',(-6.74610749360351,0.559881535000381,
3.67069911575047));
#48968=CARTESIAN_POINT('Ctrl Pts',(-6.7561137723544,0.383686975284884,3.67897211468777));
#48969=CARTESIAN_POINT('Ctrl Pts',(-6.76345456110672,0.254427429915391,
3.6850413377285));
#48970=CARTESIAN_POINT('Ctrl Pts',(-6.76708416463921,0.124964074613623,
3.69111056076924));
#48971=CARTESIAN_POINT('Ctrl Pts',(-6.7669985187373,-0.00447743310165752,
3.69717978380997));
#48972=CARTESIAN_POINT('',(-6.76706252418698,0.0012438250213078,3.30292897675432));
#48973=CARTESIAN_POINT('Ctrl Pts',(3.09908550384727,6.01564277861009,2.65150531920281));
#48974=CARTESIAN_POINT('Ctrl Pts',(2.94012272934183,6.09753581120053,2.65991673722147));
#48975=CARTESIAN_POINT('Ctrl Pts',(2.77785065443283,6.17315569312117,2.6683281552401));
#48976=CARTESIAN_POINT('Ctrl Pts',(2.61279470237935,6.24224261329359,2.67673957325876));
#48977=CARTESIAN_POINT('Ctrl Pts',(2.44778162890434,6.31131158592222,2.68514880614175));
#48978=CARTESIAN_POINT('Ctrl Pts',(2.27998642812488,6.37385084902689,2.69355803902475));
#48979=CARTESIAN_POINT('Ctrl Pts',(2.10995579167536,6.42964816744864,2.70196727190773));
#48980=CARTESIAN_POINT('Ctrl Pts',(1.9399483019024,6.48543789004819,2.71037536002177));
#48981=CARTESIAN_POINT('Ctrl Pts',(1.7677063014232,6.53448739297538,2.7187834481358));
#48982=CARTESIAN_POINT('Ctrl Pts',(1.5937932815841,6.57663378755252,2.72719153624983));
#48983=CARTESIAN_POINT('Ctrl Pts',(1.41987906201742,6.61878047287381,2.73559968236651));
#48984=CARTESIAN_POINT('Ctrl Pts',(1.24429412590556,6.65402387628327,2.74400782848317));
#48985=CARTESIAN_POINT('Ctrl Pts',(1.06761418108446,6.68225178815849,2.75241597459986));
#48986=CARTESIAN_POINT('Ctrl Pts',(0.890907746284581,6.71048393230121,2.76082538136676));
#48987=CARTESIAN_POINT('Ctrl Pts',(0.713106306489074,6.73169843567122,2.76923478813368));
#48988=CARTESIAN_POINT('Ctrl Pts',(0.534793098444444,6.74583466606292,2.77764419490059));
#48989=CARTESIAN_POINT('Ctrl Pts',(0.356359160763974,6.75998046760173,2.78605929538266));
#48990=CARTESIAN_POINT('Ctrl Pts',(0.177413096882429,6.76703839267651,2.79447439586472));
#48991=CARTESIAN_POINT('Ctrl Pts',(-0.0014584028518669,6.76699984284477,
2.80288949634679));
#48992=CARTESIAN_POINT('Ctrl Pts',(-0.180392226196036,6.76696127958124,
2.81130752887472));
#48993=CARTESIAN_POINT('Ctrl Pts',(-0.35925109842801,6.75982131768624,2.81972556140265));
#48994=CARTESIAN_POINT('Ctrl Pts',(-0.537450480721161,6.74562346864785,
2.82814359393058));
#48995=CARTESIAN_POINT('Ctrl Pts',(-0.715820944584164,6.73141198886467,
2.83656970824981));
#48996=CARTESIAN_POINT('Ctrl Pts',(-0.893530319532771,6.71012911523428,
2.84499582256906));
#48997=CARTESIAN_POINT('Ctrl Pts',(-1.07000016315762,6.68187014621226,2.8534219368883));
#48998=CARTESIAN_POINT('Ctrl Pts',(-1.18898013307135,6.6628173085434,2.85910301421913));
#48999=CARTESIAN_POINT('Ctrl Pts',(-1.30739680774279,6.6405943749332,2.86478409154997));
#49000=CARTESIAN_POINT('Ctrl Pts',(-1.42507603784582,6.61524355457588,2.8704651688808));
#49001=CARTESIAN_POINT('Ctrl Pts',(-1.59401445790201,6.57885032244354,2.87862083260878));
#49002=CARTESIAN_POINT('Ctrl Pts',(-1.76176990886751,6.53593573372507,2.88677649633676));
#49003=CARTESIAN_POINT('Ctrl Pts',(-1.92779815956372,6.486592576691,2.89493216006474));
#49004=CARTESIAN_POINT('Ctrl Pts',(-2.09368110021672,6.43729260541748,2.90308068585178));
#49005=CARTESIAN_POINT('Ctrl Pts',(-2.25783950261943,6.38157536912555,2.9112292116388));
#49006=CARTESIAN_POINT('Ctrl Pts',(-2.41973936295995,6.31958467111109,2.91937773742583));
#49007=CARTESIAN_POINT('Ctrl Pts',(-2.58152815278813,6.25763650147543,2.92752067296139));
#49008=CARTESIAN_POINT('Ctrl Pts',(-2.74106114652839,6.18942356940207,2.93566360849696));
#49009=CARTESIAN_POINT('Ctrl Pts',(-2.89781956935012,6.11513947048565,2.94380654403251));
#49010=CARTESIAN_POINT('Ctrl Pts',(-3.0545015159481,6.04089161183796,2.95194550695244));
#49011=CARTESIAN_POINT('Ctrl Pts',(-3.20841125861373,5.96057864095412,2.96008446987237));
#49012=CARTESIAN_POINT('Ctrl Pts',(-3.35905009070085,5.87444222783428,2.9682234327923));
#49013=CARTESIAN_POINT('Ctrl Pts',(-3.50964587413398,5.78833043025743,2.97636006980865));
#49014=CARTESIAN_POINT('Ctrl Pts',(-3.65697229301819,5.69639868682647,2.98449670682498));
#49015=CARTESIAN_POINT('Ctrl Pts',(-3.80055534488504,5.59893454779263,2.99263334384133));
#49016=CARTESIAN_POINT('Ctrl Pts',(-3.94414386966314,5.50146669374801,3.00077029099939));
#49017=CARTESIAN_POINT('Ctrl Pts',(-4.08398843838153,5.39846622421434,3.00890723815746));
#49018=CARTESIAN_POINT('Ctrl Pts',(-4.21964398358273,5.29026404367628,3.01704418531551));
#49019=CARTESIAN_POINT('Ctrl Pts',(-4.28735707679175,5.23625442449465,3.02110578014773));
#49020=CARTESIAN_POINT('Ctrl Pts',(-4.35402693308373,5.18094942794208,3.02516737497994));
#49021=CARTESIAN_POINT('Ctrl Pts',(-4.41960125263066,5.12439399029246,3.02922896981215));
#49022=CARTESIAN_POINT('Ctrl Pts',(-4.56448897329967,4.99943366269614,3.03820314173778));
#49023=CARTESIAN_POINT('Ctrl Pts',(-4.70395281213403,4.86842988574425,3.04717731366341));
#49024=CARTESIAN_POINT('Ctrl Pts',(-4.83753202993561,4.73186779816883,3.05615148558904));
#49025=CARTESIAN_POINT('Ctrl Pts',(-4.97133572982691,4.59507621574158,3.06514073875934));
#49026=CARTESIAN_POINT('Ctrl Pts',(-5.09923487511697,4.45270782605835,3.07412999192963));
#49027=CARTESIAN_POINT('Ctrl Pts',(-5.22080781295147,4.30528219519056,3.08311924509994));
#49028=CARTESIAN_POINT('Ctrl Pts',(-5.34266155771033,4.15751604332598,3.09212926148104));
#49029=CARTESIAN_POINT('Ctrl Pts',(-5.45815970544682,4.00466946574594,3.10113927786215));
#49030=CARTESIAN_POINT('Ctrl Pts',(-5.56692128171149,3.84729469149787,3.11014929424324));
#49031=CARTESIAN_POINT('Ctrl Pts',(-5.67579166418284,3.68976247789667,3.11916832433799));
#49032=CARTESIAN_POINT('Ctrl Pts',(-5.77791188001264,3.52769321951944,3.12818735443274));
#49033=CARTESIAN_POINT('Ctrl Pts',(-5.87294525261792,3.3616667086064,3.13720638452749));
#49034=CARTESIAN_POINT('Ctrl Pts',(-5.96811274491677,3.19540588605992,3.1462381430935));
#49035=CARTESIAN_POINT('Ctrl Pts',(-6.0561732759664,3.02517685346559,3.15526990165949));
#49036=CARTESIAN_POINT('Ctrl Pts',(-6.13683587545888,2.85158454857661,3.1643016602255));
#49037=CARTESIAN_POINT('Ctrl Pts',(-6.20736427976691,2.69980183464221,3.17219869706493));
#49038=CARTESIAN_POINT('Ctrl Pts',(-6.27223756172802,2.54544829755473,3.18009573390438));
#49039=CARTESIAN_POINT('Ctrl Pts',(-6.33129152425901,2.38894048373877,3.1879927707438));
#49040=CARTESIAN_POINT('Ctrl Pts',(-6.39738835287652,2.21376730815948,3.1968316203009));
#49041=CARTESIAN_POINT('Ctrl Pts',(-6.45624613323741,2.0357566951229,3.20567046985799));
#49042=CARTESIAN_POINT('Ctrl Pts',(-6.50763970763448,1.85550921194668,3.21450931941509));
#49043=CARTESIAN_POINT('Ctrl Pts',(-6.55895606112458,1.67553255784385,3.22333488824619));
#49044=CARTESIAN_POINT('Ctrl Pts',(-6.60283052208568,1.49332600640725,3.23216045707728));
#49045=CARTESIAN_POINT('Ctrl Pts',(-6.63908756720368,1.30950573691053,3.24098602590838));
#49046=CARTESIAN_POINT('Ctrl Pts',(-6.6753082553054,1.12586979452889,3.24980274483602));
#49047=CARTESIAN_POINT('Ctrl Pts',(-6.70392671212931,0.94062363059039,3.25861946376365));
#49048=CARTESIAN_POINT('Ctrl Pts',(-6.72481789286447,0.754395988728612,
3.26743618269128));
#49049=CARTESIAN_POINT('Ctrl Pts',(-6.74567962581321,0.568430849589584,
3.27624047374999));
#49050=CARTESIAN_POINT('Ctrl Pts',(-6.75883579085114,0.38148726583158,3.28504476480866));
#49051=CARTESIAN_POINT('Ctrl Pts',(-6.76421279127097,0.194201736362655,
3.29384905586735));
#49052=CARTESIAN_POINT('Ctrl Pts',(-6.76603909515312,0.130590008106184,
3.29683944264152));
#49053=CARTESIAN_POINT('Ctrl Pts',(-6.76696840997942,0.0669389024656748,
3.2998298294157));
#49054=CARTESIAN_POINT('Ctrl Pts',(-6.76699920820775,0.00327354788297447,
3.30282021618987));
#49055=CARTESIAN_POINT('Ctrl Pts',(-6.767,2.04925086815431E-12,3.30282021618987));
#49056=CARTESIAN_POINT('Ctrl Pts',(-6.76700000000006,-0.186007249558088,
3.31156972800262));
#49057=CARTESIAN_POINT('Ctrl Pts',(-6.75932637294257,-0.372014355814404,
3.32031923981535));
#49058=CARTESIAN_POINT('Ctrl Pts',(-6.74400518263375,-0.55738953758491,
3.3290687516281));
#49059=CARTESIAN_POINT('Ctrl Pts',(-6.72868405703744,-0.742763936381449,
3.3378182264853));
#49060=CARTESIAN_POINT('Ctrl Pts',(-6.70571545643581,-0.927506130403824,
3.34656770134251));
#49061=CARTESIAN_POINT('Ctrl Pts',(-6.67517739401592,-1.11098864009441,
3.35531717619972));
#49062=CARTESIAN_POINT('Ctrl Pts',(-6.6446394580441,-1.29447039004436,3.36406661482823));
#49063=CARTESIAN_POINT('Ctrl Pts',(-6.60653217002748,-1.47669218339172,
3.37281605345675));
#49064=CARTESIAN_POINT('Ctrl Pts',(-6.56098496085507,-1.65703510627676,
3.38156549208526));
#49065=CARTESIAN_POINT('Ctrl Pts',(-6.51543793649584,-1.83737729739912,
3.39031489521189));
#49066=CARTESIAN_POINT('Ctrl Pts',(-6.46245112156923,-2.01584035544866,
3.39906429833851));
#49067=CARTESIAN_POINT('Ctrl Pts',(-6.40220448361743,-2.19181813797332,
3.40781370146514));
#49068=CARTESIAN_POINT('Ctrl Pts',(-6.34195808511996,-2.36779522106242,
3.41656306981668));
#49069=CARTESIAN_POINT('Ctrl Pts',(-6.27445201416373,-2.54128677725699,
3.42531243816824));
#49070=CARTESIAN_POINT('Ctrl Pts',(-6.19991555052738,-2.71170355428628,
3.43406180651978));
#49071=CARTESIAN_POINT('Ctrl Pts',(-6.12537937695124,-2.88211966813509,
3.44281114082297));
#49072=CARTESIAN_POINT('Ctrl Pts',(-6.04381298028344,-3.04946076419884,
3.45156047512614));
#49073=CARTESIAN_POINT('Ctrl Pts',(-5.9554933930886,-3.21315848424538,3.46030980942933));
#49074=CARTESIAN_POINT('Ctrl Pts',(-5.86717414225678,-3.37685558085311,
3.46905911041089));
#49075=CARTESIAN_POINT('Ctrl Pts',(-5.77210188843925,-3.53690907700231,
3.47780841139246));
#49076=CARTESIAN_POINT('Ctrl Pts',(-5.6705995331122,-3.69277537024224,3.48655771237402));
#49077=CARTESIAN_POINT('Ctrl Pts',(-5.56909755592538,-3.84864108281273,
3.49530698076065));
#49078=CARTESIAN_POINT('Ctrl Pts',(-5.46116568154777,-4.00031938355088,
3.50405624914725));
#49079=CARTESIAN_POINT('Ctrl Pts',(-5.34717048488167,-4.14729511918435,
3.51280551753388));
#49080=CARTESIAN_POINT('Ctrl Pts',(-5.23317570343074,-4.29427031947461,
3.52155475405224));
#49081=CARTESIAN_POINT('Ctrl Pts',(-5.11311781951294,-4.43654276249848,
3.53030399057061));
#49082=CARTESIAN_POINT('Ctrl Pts',(-4.98740458928968,-4.57362924412684,
3.53905322708897));
#49083=CARTESIAN_POINT('Ctrl Pts',(-4.86169180652458,-4.71071523781559,
3.54780243246568));
#49084=CARTESIAN_POINT('Ctrl Pts',(-4.73032391141284,-4.84261509584771,
3.55655163784241));
#49085=CARTESIAN_POINT('Ctrl Pts',(-4.59374706947033,-4.9688808459987,3.56530084321912));
#49086=CARTESIAN_POINT('Ctrl Pts',(-4.45717070231229,-5.09514615720986,
3.57405001818082));
#49087=CARTESIAN_POINT('Ctrl Pts',(-4.315385634971,-5.21577720520799,3.58279919314252));
#49088=CARTESIAN_POINT('Ctrl Pts',(-4.16887340951796,-5.33036429293666,
3.59154836810421));
#49089=CARTESIAN_POINT('Ctrl Pts',(-4.02236168122269,-5.44495099183866,
3.60029751337747));
#49090=CARTESIAN_POINT('Ctrl Pts',(-3.87112305262959,-5.55349359498083,
3.60904665865072));
#49091=CARTESIAN_POINT('Ctrl Pts',(-3.71567116928768,-5.65562346357361,
3.61779580392397));
#49092=CARTESIAN_POINT('Ctrl Pts',(-3.56021980053059,-5.75775299409084,
3.62654492023535));
#49093=CARTESIAN_POINT('Ctrl Pts',(-3.40055544441806,-5.85346967520042,
3.63529403654672));
#49094=CARTESIAN_POINT('Ctrl Pts',(-3.23722035886538,-5.94244843041549,
3.6440431528581));
#49095=CARTESIAN_POINT('Ctrl Pts',(-3.07388580043206,-6.03142689847594,
3.6527922409341));
#49096=CARTESIAN_POINT('Ctrl Pts',(-2.90688078788962,-6.11366734708025,
3.66154132901011));
#49097=CARTESIAN_POINT('Ctrl Pts',(-2.73677250610157,-6.18889047001533,
3.67029041708611));
#49098=CARTESIAN_POINT('Ctrl Pts',(-2.56666475916696,-6.26411335643431,
3.67903947765328));
#49099=CARTESIAN_POINT('Ctrl Pts',(-2.39345402456853,-6.33231884545347,
3.68778853822045));
#49100=CARTESIAN_POINT('Ctrl Pts',(-2.21772855943823,-6.39327529804967,
3.69653759878761));
#49101=CARTESIAN_POINT('Ctrl Pts',(-2.04200363223381,-6.45423156404768,
3.7052866325724));
#49102=CARTESIAN_POINT('Ctrl Pts',(-1.86376426060856,-6.50793874412503,
3.7140356663572));
#49103=CARTESIAN_POINT('Ctrl Pts',(-1.68361577621544,-6.55421443943349,
3.72278470014199));
#49104=CARTESIAN_POINT('Ctrl Pts',(-1.50346782833056,-6.60048999692624,
3.73153370787089));
#49105=CARTESIAN_POINT('Ctrl Pts',(-1.32141105657213,-6.63933404265197,
3.74028271559977));
#49106=CARTESIAN_POINT('Ctrl Pts',(-1.13806375346346,-6.67061465631561,
3.74903172332867));
#49107=CARTESIAN_POINT('Ctrl Pts',(-0.954716981167858,-6.70189517941802,
3.75778070572811));
#49108=CARTESIAN_POINT('Ctrl Pts',(-0.770079967439874,-6.72561226609032,
3.76652968812759));
#49109=CARTESIAN_POINT('Ctrl Pts',(-0.584779764070404,-6.74168536996008,
3.77527867052703));
#49110=CARTESIAN_POINT('Ctrl Pts',(-0.39148958759023,-6.75845153117888,
3.78440490094265));
#49111=CARTESIAN_POINT('Ctrl Pts',(-0.197478091802452,-6.76689985146402,
3.79353113135825));
#49112=CARTESIAN_POINT('Ctrl Pts',(-0.00346214752819375,-6.76699911434415,
3.80265736177387));
#49113=CARTESIAN_POINT('Ctrl Pts',(0.18449079848745,-6.76709527525927,3.81149839748899));
#49114=CARTESIAN_POINT('Ctrl Pts',(0.372447602157554,-6.75935633790748,
3.82033943320412));
#49115=CARTESIAN_POINT('Ctrl Pts',(0.559756448196956,-6.7438091401449,3.82918046891925));
#49116=CARTESIAN_POINT('Ctrl Pts',(0.745136131046012,-6.72842206873125,
3.83793044753255));
#49117=CARTESIAN_POINT('Ctrl Pts',(0.929880851947613,-6.70538686355687,
3.84668042614584));
#49118=CARTESIAN_POINT('Ctrl Pts',(1.11336305057711,-6.67478177303271,3.85543040475915));
#49119=CARTESIAN_POINT('Ctrl Pts',(1.29684337090384,-6.6441769958121,3.86418029379913));
#49120=CARTESIAN_POINT('Ctrl Pts',(1.47906091205463,-6.60600253547999,3.87293018283914));
#49121=CARTESIAN_POINT('Ctrl Pts',(1.65939671095507,-6.5603880644114,3.88168007187913));
#49122=CARTESIAN_POINT('Ctrl Pts',(1.83973072369444,-6.51477404513769,3.89042987425462));
#49123=CARTESIAN_POINT('Ctrl Pts',(2.01818275357318,-6.46172023288573,3.89917967663011));
#49124=CARTESIAN_POINT('Ctrl Pts',(2.19414664033606,-6.40140683918012,3.9079294790056));
#49125=CARTESIAN_POINT('Ctrl Pts',(2.37010884271534,-6.34109402281395,3.91667919762514));
#49126=CARTESIAN_POINT('Ctrl Pts',(2.54358267848075,-6.27352185699683,3.92542891624467));
#49127=CARTESIAN_POINT('Ctrl Pts',(2.71397890842005,-6.19891986435146,3.93417863486421));
#49128=CARTESIAN_POINT('Ctrl Pts',(2.884373563892,-6.12431856103122,3.94292827263603));
#49129=CARTESIAN_POINT('Ctrl Pts',(3.05169040787425,-6.04268767582429,3.95167791040785));
#49130=CARTESIAN_POINT('Ctrl Pts',(3.21536112512301,-5.95430447953812,3.96042754817967));
#49131=CARTESIAN_POINT('Ctrl Pts',(3.37903038443089,-5.86592207054901,3.96917710801174));
#49132=CARTESIAN_POINT('Ctrl Pts',(3.53905332980219,-5.77078760703226,3.9779266678438));
#49133=CARTESIAN_POINT('Ctrl Pts',(3.69488643042137,-5.66922422085139,3.98667622767587));
#49134=CARTESIAN_POINT('Ctrl Pts',(3.85071819468991,-5.56766170562986,3.99542571247587));
#49135=CARTESIAN_POINT('Ctrl Pts',(4.00235994599477,-5.45967053456066,4.00417519727587));
#49136=CARTESIAN_POINT('Ctrl Pts',(4.14929662974557,-5.34561750206486,4.01292468207588));
#49137=CARTESIAN_POINT('Ctrl Pts',(4.29623210225293,-5.23156540974262,4.02167409475123));
#49138=CARTESIAN_POINT('Ctrl Pts',(4.43846235842358,-5.11145173171977,4.03042350742659));
#49139=CARTESIAN_POINT('Ctrl Pts',(4.57550431797661,-4.98568443006348,4.03917292010195));
#49140=CARTESIAN_POINT('Ctrl Pts',(4.71254519337732,-4.85991812336459,4.04792226355985));
#49141=CARTESIAN_POINT('Ctrl Pts',(4.84439764315226,-4.72849847630854,4.05667160701774));
#49142=CARTESIAN_POINT('Ctrl Pts',(4.97061384196931,-4.59187184425079,4.06542095047564));
#49143=CARTESIAN_POINT('Ctrl Pts',(5.09682908420441,-4.45524624767479,4.074170227623));
#49144=CARTESIAN_POINT('Ctrl Pts',(5.21740796650395,-4.31341395556621,4.08291950477036));
#49145=CARTESIAN_POINT('Ctrl Pts',(5.33194095942466,-4.16685668162582,4.09166878191772));
#49146=CARTESIAN_POINT('Ctrl Pts',(5.44647312235341,-4.02030046974933,4.10041799566126));
#49147=CARTESIAN_POINT('Ctrl Pts',(5.55495930712489,-3.86901957035258,4.10916720940481));
#49148=CARTESIAN_POINT('Ctrl Pts',(5.65703106079989,-3.71352778058079,4.11791642314834));
#49149=CARTESIAN_POINT('Ctrl Pts',(5.75910210868923,-3.558037065973,4.12666557639454));
#49150=CARTESIAN_POINT('Ctrl Pts',(5.85475865698729,-3.3983357588059,4.13541472964074));
#49151=CARTESIAN_POINT('Ctrl Pts',(5.94367583069235,-3.23496624706404,4.14416388288694));
#49152=CARTESIAN_POINT('Ctrl Pts',(6.03259241910246,-3.07159781069769,4.15291297854207));
#49153=CARTESIAN_POINT('Ctrl Pts',(6.11476958471132,-2.90456146975489,4.16166207419719));
#49154=CARTESIAN_POINT('Ctrl Pts',(6.18992823574544,-2.73442451647898,4.17041116985231));
#49155=CARTESIAN_POINT('Ctrl Pts',(6.26508641701081,-2.56428862662059,4.17916021082243));
#49156=CARTESIAN_POINT('Ctrl Pts',(6.33322605570431,-2.39105242530922,4.18790925179253));
#49157=CARTESIAN_POINT('Ctrl Pts',(6.39411573747889,-2.21530425353376,4.19665829276265));
#49158=CARTESIAN_POINT('Ctrl Pts',(6.45500505889232,-2.03955712188223,4.20540728195364));
#49159=CARTESIAN_POINT('Ctrl Pts',(6.50864441545021,-1.8612983202525,4.21415627114463));
#49160=CARTESIAN_POINT('Ctrl Pts',(6.55485164049985,-1.68113324012004,4.22290526033562));
#49161=CARTESIAN_POINT('Ctrl Pts',(6.60199852639179,-1.49730435912592,4.23183216721251));
#49162=CARTESIAN_POINT('Ctrl Pts',(6.64140767441071,-1.31149113173343,4.24075907408939));
#49163=CARTESIAN_POINT('Ctrl Pts',(6.67293975269654,-1.12435050446122,4.24968598096628));
#49164=CARTESIAN_POINT('Ctrl Pts',(6.7038466483155,-0.940920291560661,4.25843589515027));
#49165=CARTESIAN_POINT('Ctrl Pts',(6.727185858897,-0.756215114274866,4.26718580933427));
#49166=CARTESIAN_POINT('Ctrl Pts',(6.7428781045189,-0.570862389372079,4.27593572351826));
#49167=CARTESIAN_POINT('Ctrl Pts',(6.75857004154141,-0.385513309565091,
4.28468546562884));
#49168=CARTESIAN_POINT('Ctrl Pts',(6.76661529035565,-0.199516993256255,
4.29343520773942));
#49169=CARTESIAN_POINT('Ctrl Pts',(6.76698652348897,-0.0135052182021578,
4.30218494985));
#49170=CARTESIAN_POINT('Ctrl Pts',(6.76735774981516,0.172503146040806,4.31093453152064));
#49171=CARTESIAN_POINT('Ctrl Pts',(6.76005524147469,0.358526681835397,4.31968411319129));
#49172=CARTESIAN_POINT('Ctrl Pts',(6.74510380214866,0.543933542116802,4.32843369486193));
#49173=CARTESIAN_POINT('Ctrl Pts',(6.73015261710958,0.729337249086645,4.33718312772386));
#49174=CARTESIAN_POINT('Ctrl Pts',(6.70755278444579,0.91412401585657,4.34593256058577));
#49175=CARTESIAN_POINT('Ctrl Pts',(6.67738106408258,1.09766621749575,4.3546819934477));
#49176=CARTESIAN_POINT('Ctrl Pts',(6.64720981677218,1.28120554143509,4.36343128913005));
#49177=CARTESIAN_POINT('Ctrl Pts',(6.60946696581482,1.46350005650805,4.37218058481241));
#49178=CARTESIAN_POINT('Ctrl Pts',(6.56428070010948,1.64393062206717,4.38092988049476));
#49179=CARTESIAN_POINT('Ctrl Pts',(6.51909508282691,1.8243585984483,4.38967905062475));
#49180=CARTESIAN_POINT('Ctrl Pts',(6.46646633415608,2.00292240086736,4.39842822075474));
#49181=CARTESIAN_POINT('Ctrl Pts',(6.40657319597136,2.17901557696621,4.40717739088473));
#49182=CARTESIAN_POINT('Ctrl Pts',(6.34668083768231,2.35510646007606,4.41592644708781));
#49183=CARTESIAN_POINT('Ctrl Pts',(6.27952437143814,2.52872650996707,4.42467550329088));
#49184=CARTESIAN_POINT('Ctrl Pts',(6.20533187335057,2.69928607998106,4.43342455949396));
#49185=CARTESIAN_POINT('Ctrl Pts',(6.12831449784172,2.87633970115568,4.4425067357828));
#49186=CARTESIAN_POINT('Ctrl Pts',(6.04371489463072,3.0500949056251,4.45158891207163));
#49187=CARTESIAN_POINT('Ctrl Pts',(5.95184265120409,3.21991584599782,4.46067108836047));
#49188=CARTESIAN_POINT('Ctrl Pts',(5.86333281335406,3.38352155905451,4.46942086871489));
#49189=CARTESIAN_POINT('Ctrl Pts',(5.76807337235593,3.54347560903973,4.47817064906932));
#49190=CARTESIAN_POINT('Ctrl Pts',(5.66638790086259,3.69923467178795,4.48692042942373));
#49191=CARTESIAN_POINT('Ctrl Pts',(5.56470608502642,3.85498813489909,4.495669895218));
#49192=CARTESIAN_POINT('Ctrl Pts',(5.45659885766848,4.00654667256403,4.50441936101225));
#49193=CARTESIAN_POINT('Ctrl Pts',(5.34243340580399,4.1533955150635,4.51316882680652));
#49194=CARTESIAN_POINT('Ctrl Pts',(5.22827145140479,4.3002398588401,4.52191802456039));
#49195=CARTESIAN_POINT('Ctrl Pts',(5.10805181977968,4.44237456993183,4.53066722231426));
#49196=CARTESIAN_POINT('Ctrl Pts',(4.98218281282423,4.57931691626588,4.53941642006814));
#49197=CARTESIAN_POINT('Ctrl Pts',(4.85631699296099,4.71625579512295,4.54816539628614));
#49198=CARTESIAN_POINT('Ctrl Pts',(4.72480227791707,4.84800236135897,4.55691437250414));
#49199=CARTESIAN_POINT('Ctrl Pts',(4.58808530847982,4.9741091867903,4.56566334872214));
#49200=CARTESIAN_POINT('Ctrl Pts',(4.45135945056829,5.10022421089132,4.57441289374334));
#49201=CARTESIAN_POINT('Ctrl Pts',(4.30943087207889,5.22069856612111,4.58316243876453));
#49202=CARTESIAN_POINT('Ctrl Pts',(4.16278164322307,5.33512305301809,4.59191198378574));
#49203=CARTESIAN_POINT('Ctrl Pts',(4.01614103534237,5.4495408133154,4.60066101445299));
#49204=CARTESIAN_POINT('Ctrl Pts',(3.86478055833267,5.55790924068439,4.60941004512025));
#49205=CARTESIAN_POINT('Ctrl Pts',(3.70921425811814,5.65986029751381,4.6181590757875));
#49206=CARTESIAN_POINT('Ctrl Pts',(3.55364584529982,5.76181273884739,4.62690822526735));
#49207=CARTESIAN_POINT('Ctrl Pts',(3.39387173464207,5.85734747818143,4.63565737474719));
#49208=CARTESIAN_POINT('Ctrl Pts',(3.23043456092267,5.94614005448882,4.64440652422704));
#49209=CARTESIAN_POINT('Ctrl Pts',(3.18690768806298,5.96978744811331,4.64673661296005));
#49210=CARTESIAN_POINT('Ctrl Pts',(3.14312114982832,5.99295688499326,4.64906670169307));
#49211=CARTESIAN_POINT('Ctrl Pts',(3.09908550384716,6.01564277861015,4.65139679042609));
#49212=CARTESIAN_POINT('Origin',(0.,0.,-63.6971797838103));
#49213=CARTESIAN_POINT('',(3.09908550384722,6.01564277861012,7.04591868117257));
#49214=CARTESIAN_POINT('',(3.09908550384729,6.01564277861008,6.6512241499329));
#49215=CARTESIAN_POINT('',(3.09908550384721,6.01564277861012,-63.6971797838103));
#49216=CARTESIAN_POINT('',(-6.76699915828328,-0.00337517308289641,5.69717978377259));
#49217=CARTESIAN_POINT('Ctrl Pts',(-6.76699915828289,-0.00337517387210557,
5.69717978380996));
#49218=CARTESIAN_POINT('Ctrl Pts',(-6.76697949862955,-0.0427914714202488,
5.69904654968036));
#49219=CARTESIAN_POINT('Ctrl Pts',(-6.76661545789972,-0.0822029254710357,
5.70091331555085));
#49220=CARTESIAN_POINT('Ctrl Pts',(-6.76590726115161,-0.121605647467519,
5.70278008142134));
#49221=CARTESIAN_POINT('Ctrl Pts',(-6.76278486510318,-0.295329833278017,
5.71101053770748));
#49222=CARTESIAN_POINT('Ctrl Pts',(-6.75296268258051,-0.469187948267381,
5.71924099399363));
#49223=CARTESIAN_POINT('Ctrl Pts',(-6.73641782758042,-0.642622635966649,
5.72747145027979));
#49224=CARTESIAN_POINT('Ctrl Pts',(-6.71989261229359,-0.815851446519408,
5.73569213653161));
#49225=CARTESIAN_POINT('Ctrl Pts',(-6.69666064861334,-0.98865747724068,
5.74391282278344));
#49226=CARTESIAN_POINT('Ctrl Pts',(-6.66675102227233,-1.16048257506558,
5.75213350903526));
#49227=CARTESIAN_POINT('Ctrl Pts',(-6.63687089961681,-1.3321381798454,5.76034608617401));
#49228=CARTESIAN_POINT('Ctrl Pts',(-6.60032629336207,-1.50281442795062,
5.76855866331277));
#49229=CARTESIAN_POINT('Ctrl Pts',(-6.55719813960777,-1.67195740314293,
5.77677124045152));
#49230=CARTESIAN_POINT('Ctrl Pts',(-6.51410387892953,-1.84096745412623,
5.78497736358106));
#49231=CARTESIAN_POINT('Ctrl Pts',(-6.46443646400532,-2.00844628634816,
5.79318348671062));
#49232=CARTESIAN_POINT('Ctrl Pts',(-6.408328064148,-2.17384921792042,5.80138960984016));
#49233=CARTESIAN_POINT('Ctrl Pts',(-6.35225250799491,-2.33915532896351,
5.80959092942011));
#49234=CARTESIAN_POINT('Ctrl Pts',(-6.28974359265882,-2.50238762147196,
5.81779224900005));
#49235=CARTESIAN_POINT('Ctrl Pts',(-6.22098361389318,-2.66301556053895,
5.82599356858));
#49236=CARTESIAN_POINT('Ctrl Pts',(-6.15224336072521,-2.82359741928192,
5.834192535397));
#49237=CARTESIAN_POINT('Ctrl Pts',(-6.07725575340116,-2.98157608203589,
5.842391502214));
#49238=CARTESIAN_POINT('Ctrl Pts',(-5.99625169893546,-3.13643979107102,
5.850590469031));
#49239=CARTESIAN_POINT('Ctrl Pts',(-5.91525834141358,-3.29128304966812,
5.85878835313816));
#49240=CARTESIAN_POINT('Ctrl Pts',(-5.82825028453694,-3.44301185574427,
5.86698623724531));
#49241=CARTESIAN_POINT('Ctrl Pts',(-5.73550499072217,-3.59113791177687,
5.87518412135246));
#49242=CARTESIAN_POINT('Ctrl Pts',(-5.64275509688695,-3.73927131462846,
5.88338241206175));
#49243=CARTESIAN_POINT('Ctrl Pts',(-5.54426758949399,-3.88380130744567,
5.89158070277106));
#49244=CARTESIAN_POINT('Ctrl Pts',(-5.44036399118967,-4.02426746667849,
5.89977899348035));
#49245=CARTESIAN_POINT('Ctrl Pts',(-5.33643636509712,-4.16476610882027,
5.90797918005077));
#49246=CARTESIAN_POINT('Ctrl Pts',(-5.22709036675116,-4.30119875739443,
5.91617936662118));
#49247=CARTESIAN_POINT('Ctrl Pts',(-5.11268865573878,-4.43313700549396,
5.9243795531916));
#49248=CARTESIAN_POINT('Ctrl Pts',(-4.99817878689707,-4.56519999084082,
5.93258749239414));
#49249=CARTESIAN_POINT('Ctrl Pts',(-4.87860389115694,-4.69275981518642,
5.94079543159667));
#49250=CARTESIAN_POINT('Ctrl Pts',(-4.75436509247631,-4.81542330096148,
5.9490033707992));
#49251=CARTESIAN_POINT('Ctrl Pts',(-4.63006602179254,-4.93814629450769,
5.95721529192158));
#49252=CARTESIAN_POINT('Ctrl Pts',(-4.50109880166452,-5.05596797183455,
5.96542721304397));
#49253=CARTESIAN_POINT('Ctrl Pts',(-4.36789861035503,-5.16853467915797,
5.97363913416635));
#49254=CARTESIAN_POINT('Ctrl Pts',(-4.23451575612425,-5.28125575385428,
5.98186231663518));
#49255=CARTESIAN_POINT('Ctrl Pts',(-4.09688861259461,-5.38870723610298,
5.99008549910399));
#49256=CARTESIAN_POINT('Ctrl Pts',(-3.95548335788428,-5.49057742004432,
5.99830868157282));
#49257=CARTESIAN_POINT('Ctrl Pts',(-3.82938560711906,-5.5814198791266,6.00564168214324));
#49258=CARTESIAN_POINT('Ctrl Pts',(-3.70028400509378,-5.66782453499294,
6.01297468271367));
#49259=CARTESIAN_POINT('Ctrl Pts',(-3.56852566469042,-5.74960116707636,
6.02030768328409));
#49260=CARTESIAN_POINT('Ctrl Pts',(-3.4079794778143,-5.8492451548222,6.02924286929461));
#49261=CARTESIAN_POINT('Ctrl Pts',(-3.24315549910538,-5.94222435605987,
6.03817805530512));
#49262=CARTESIAN_POINT('Ctrl Pts',(-3.07460673310888,-6.02819064369414,
6.04711324131564));
#49263=CARTESIAN_POINT('Ctrl Pts',(-2.90631040097667,-6.11402818044698,
6.05603504518409));
#49264=CARTESIAN_POINT('Ctrl Pts',(-2.73430064234891,-6.19287364395915,
6.06495684905255));
#49265=CARTESIAN_POINT('Ctrl Pts',(-2.55915635159388,-6.26442397735791,
6.073878652921));
#49266=CARTESIAN_POINT('Ctrl Pts',(-2.38443927900038,-6.33579978264753,
6.08277869440924));
#49267=CARTESIAN_POINT('Ctrl Pts',(-2.20660317282507,-6.39991587517573,
6.09167873589749));
#49268=CARTESIAN_POINT('Ctrl Pts',(-2.02624767534499,-6.45651681312448,
6.10057877738573));
#49269=CARTESIAN_POINT('Ctrl Pts',(-1.84616983754887,-6.51303061317744,
6.10946511714189));
#49270=CARTESIAN_POINT('Ctrl Pts',(-1.66358059057379,-6.56205226019557,
6.11835145689805));
#49271=CARTESIAN_POINT('Ctrl Pts',(-1.47909832937744,-6.60337467754427,
6.1272377966542));
#49272=CARTESIAN_POINT('Ctrl Pts',(-1.2950877565163,-6.64459144082021,6.13610141561986));
#49273=CARTESIAN_POINT('Ctrl Pts',(-1.10919407888226,-6.67814819944702,
6.14496503458552));
#49274=CARTESIAN_POINT('Ctrl Pts',(-0.922048844575116,-6.70388804562082,
6.15382865355119));
#49275=CARTESIAN_POINT('Ctrl Pts',(-0.744390957219133,-6.7283230076386,
6.16224293043939));
#49276=CARTESIAN_POINT('Ctrl Pts',(-0.565605501815782,-6.74571381361739,
6.1706572073276));
#49277=CARTESIAN_POINT('Ctrl Pts',(-0.386244720236502,-6.75596802953429,
6.17907148421581));
#49278=CARTESIAN_POINT('Ctrl Pts',(-0.211233057546137,-6.76597360244382,
6.18728173271928));
#49279=CARTESIAN_POINT('Ctrl Pts',(-0.0358417702284699,-6.76917385162462,
6.19549198122275));
#49280=CARTESIAN_POINT('Ctrl Pts',(0.139364509554821,-6.76556476086635,
6.20370222972622));
#49281=CARTESIAN_POINT('Ctrl Pts',(0.31461243945397,-6.7619548121534,6.21191442997366));
#49282=CARTESIAN_POINT('Ctrl Pts',(0.489674918318395,-6.75153230587871,
6.22012663022108));
#49283=CARTESIAN_POINT('Ctrl Pts',(0.663989605743369,-6.73434531364889,
6.22833883046853));
#49284=CARTESIAN_POINT('Ctrl Pts',(0.838376771885889,-6.71715117519879,
6.23655444528621));
#49285=CARTESIAN_POINT('Ctrl Pts',(1.01201517321715,-6.693186982332,6.24477006010389));
#49286=CARTESIAN_POINT('Ctrl Pts',(1.18434977292205,-6.66255240995367,6.25298567492156));
#49287=CARTESIAN_POINT('Ctrl Pts',(1.35687789691903,-6.63188343627728,6.26121051551887));
#49288=CARTESIAN_POINT('Ctrl Pts',(1.52809894439632,-6.59452918436298,6.26943535611618));
#49289=CARTESIAN_POINT('Ctrl Pts',(1.6974692629602,-6.55064020545362,6.2776601967135));
#49290=CARTESIAN_POINT('Ctrl Pts',(1.86694806915528,-6.50672311411347,6.28589030560977));
#49291=CARTESIAN_POINT('Ctrl Pts',(2.03457344333143,-6.45626305408508,6.29412041450605));
#49292=CARTESIAN_POINT('Ctrl Pts',(2.19981903502714,-6.39945975947441,6.30235052340232));
#49293=CARTESIAN_POINT('Ctrl Pts',(2.36529118100769,-6.34257858666042,6.31059191590633));
#49294=CARTESIAN_POINT('Ctrl Pts',(2.52837669668185,-6.27933693688937,6.31883330841034));
#49295=CARTESIAN_POINT('Ctrl Pts',(2.68857033994664,-6.20998216802264,6.32707470091434));
#49296=CARTESIAN_POINT('Ctrl Pts',(2.75829064474062,-6.17979722731116,6.33066156232529));
#49297=CARTESIAN_POINT('Ctrl Pts',(2.82746349428713,-6.14845491737255,6.33424842373623));
#49298=CARTESIAN_POINT('Ctrl Pts',(2.89604883868045,-6.11597826385752,6.33783528514718));
#49299=CARTESIAN_POINT('Ctrl Pts',(3.05759478607773,-6.03948274128214,6.34628377993772));
#49300=CARTESIAN_POINT('Ctrl Pts',(3.21624791209868,-5.95651654239338,6.35473227472826));
#49301=CARTESIAN_POINT('Ctrl Pts',(3.37147378993975,-5.86732080968386,6.36318076951881));
#49302=CARTESIAN_POINT('Ctrl Pts',(3.52655787794422,-5.77820655210299,6.37162154709935));
#49303=CARTESIAN_POINT('Ctrl Pts',(3.67822067026002,-5.68287426856504,6.38006232467991));
#49304=CARTESIAN_POINT('Ctrl Pts',(3.82595070324274,-5.58161179377036,6.38850310226046));
#49305=CARTESIAN_POINT('Ctrl Pts',(3.97356851111394,-5.48042624438007,6.3969374676905));
#49306=CARTESIAN_POINT('Ctrl Pts',(4.11725924134089,-5.37331967226206,6.40537183312054));
#49307=CARTESIAN_POINT('Ctrl Pts',(4.25653854931731,-5.26062435250567,6.41380619855059));
#49308=CARTESIAN_POINT('Ctrl Pts',(4.39573344069351,-5.14799733690654,6.42223545194737));
#49309=CARTESIAN_POINT('Ctrl Pts',(4.53052198199207,-5.02978853632031,6.43066470534415));
#49310=CARTESIAN_POINT('Ctrl Pts',(4.660450878617,-4.90637204133543,6.43909395874094));
#49311=CARTESIAN_POINT('Ctrl Pts',(4.79032095660291,-4.783011416834,6.4475193962259));
#49312=CARTESIAN_POINT('Ctrl Pts',(4.91533553530226,-4.65444802811535,6.45594483371087));
#49313=CARTESIAN_POINT('Ctrl Pts',(5.03507604279997,-4.52109480582102,6.46437027119583));
#49314=CARTESIAN_POINT('Ctrl Pts',(5.15479024652157,-4.38777087765092,6.47279385783829));
#49315=CARTESIAN_POINT('Ctrl Pts',(5.26923246448506,-4.24965945989318,6.48121744448073));
#49316=CARTESIAN_POINT('Ctrl Pts',(5.37802214117491,-4.10720913139719,6.48964103112318));
#49317=CARTESIAN_POINT('Ctrl Pts',(5.48679964486749,-3.96477474234979,6.49806367521024));
#49318=CARTESIAN_POINT('Ctrl Pts',(5.58992566587883,-3.81800267535937,6.5064863192973));
#49319=CARTESIAN_POINT('Ctrl Pts',(5.68706079874458,-3.6673735112997,6.51490896338436));
#49320=CARTESIAN_POINT('Ctrl Pts',(5.78419860779792,-3.51674019722873,6.5233318395252));
#49321=CARTESIAN_POINT('Ctrl Pts',(5.87534501926892,-3.36224985462393,6.53175471566604));
#49322=CARTESIAN_POINT('Ctrl Pts',(5.96020452225528,-3.20441118661255,6.54017759180688));
#49323=CARTESIAN_POINT('Ctrl Pts',(6.04507819724907,-3.04654615866864,6.54860187461473));
#49324=CARTESIAN_POINT('Ctrl Pts',(6.12366271314895,-2.88533198435989,6.55702615742259));
#49325=CARTESIAN_POINT('Ctrl Pts',(6.19570882530371,-2.72130137104544,6.56545044023044));
#49326=CARTESIAN_POINT('Ctrl Pts',(6.26780359474061,-2.55715997751545,6.57388041248763));
#49327=CARTESIAN_POINT('Ctrl Pts',(6.33335100247243,-2.39019864968037,6.58231038474483));
#49328=CARTESIAN_POINT('Ctrl Pts',(6.392149834919,-2.22097039330673,6.59074035700202));
#49329=CARTESIAN_POINT('Ctrl Pts',(6.45096968699995,-2.05168164056049,6.59917334283835));
#49330=CARTESIAN_POINT('Ctrl Pts',(6.50303604976619,-1.88012466031485,6.60760632867468));
#49331=CARTESIAN_POINT('Ctrl Pts',(6.54819763334468,-1.70686752698011,6.61603931451101));
#49332=CARTESIAN_POINT('Ctrl Pts',(6.59340076530773,-1.53345099812744,6.62448005864346));
#49333=CARTESIAN_POINT('Ctrl Pts',(6.63168634815482,-1.35833151540637,6.63292080277589));
#49334=CARTESIAN_POINT('Ctrl Pts',(6.66295401245846,-1.18208833335911,6.64136154690834));
#49335=CARTESIAN_POINT('Ctrl Pts',(6.68024274100485,-1.08463876044005,6.64602866027563));
#49336=CARTESIAN_POINT('Ctrl Pts',(6.69538680924868,-0.986845782646499,
6.65069577364292));
#49337=CARTESIAN_POINT('Ctrl Pts',(6.70837605612388,-0.888808016178895,
6.65536288701021));
#49338=CARTESIAN_POINT('Ctrl Pts',(6.73103465036691,-0.717789789161911,
6.66350425418043));
#49339=CARTESIAN_POINT('Ctrl Pts',(6.74717813261609,-0.545686580013392,
6.67164562135067));
#49340=CARTESIAN_POINT('Ctrl Pts',(6.75670999377169,-0.373040292818122,
6.67978698852089));
#49341=CARTESIAN_POINT('Ctrl Pts',(6.76623353433732,-0.200544712703207,
6.68792124889665));
#49342=CARTESIAN_POINT('Ctrl Pts',(6.76915692190001,-0.0275073611784341,
6.69605550927243));
#49343=CARTESIAN_POINT('Ctrl Pts',(6.76543511410328,0.145522221184218,6.7041897696482));
#49344=CARTESIAN_POINT('Ctrl Pts',(6.76171584518942,0.318433769014059,6.71231848112526));
#49345=CARTESIAN_POINT('Ctrl Pts',(6.75136041403936,0.491337193762728,6.7204471926023));
#49346=CARTESIAN_POINT('Ctrl Pts',(6.73437578768639,0.663680457918825,6.72857590407938));
#49347=CARTESIAN_POINT('Ctrl Pts',(6.71739926098773,0.835941534758323,6.73670073912422));
#49348=CARTESIAN_POINT('Ctrl Pts',(6.69379987025165,1.00764261944256,6.74482557416907));
#49349=CARTESIAN_POINT('Ctrl Pts',(6.66363661077261,1.17823432286236,6.75295040921391));
#49350=CARTESIAN_POINT('Ctrl Pts',(6.6334817955826,1.34877826865671,6.76107296968841));
#49351=CARTESIAN_POINT('Ctrl Pts',(6.59676683623637,1.51821309179151,6.76919553016291));
#49352=CARTESIAN_POINT('Ctrl Pts',(6.55360225270403,1.68599718663843,6.77731809063741));
#49353=CARTESIAN_POINT('Ctrl Pts',(6.51043537508505,1.8537901987786,6.78544108280512));
#49354=CARTESIAN_POINT('Ctrl Pts',(6.46081827591302,2.01993195187524,6.79356407497283));
#49355=CARTESIAN_POINT('Ctrl Pts',(6.40491204692447,2.18389346607424,6.80168706714053));
#49356=CARTESIAN_POINT('Ctrl Pts',(6.37637361860923,2.26759082867735,6.80583360740764));
#49357=CARTESIAN_POINT('Ctrl Pts',(6.34619717801268,2.35072030385674,6.80998014767477));
#49358=CARTESIAN_POINT('Ctrl Pts',(6.31440909758854,2.43321325581854,6.81412668794188));
#49359=CARTESIAN_POINT('Ctrl Pts',(6.24553884434618,2.61193780969269,6.82311034705137));
#49360=CARTESIAN_POINT('Ctrl Pts',(6.16913507327727,2.78758505283654,6.83209400616087));
#49361=CARTESIAN_POINT('Ctrl Pts',(6.0855002992279,2.95955657288337,6.84107766527036));
#49362=CARTESIAN_POINT('Ctrl Pts',(6.00172184149015,3.13182353824678,6.85007675821453));
#49363=CARTESIAN_POINT('Ctrl Pts',(5.91068765571257,3.30040194380193,6.85907585115871));
#49364=CARTESIAN_POINT('Ctrl Pts',(5.81274584040255,3.4647185736915,6.86807494410289));
#49365=CARTESIAN_POINT('Ctrl Pts',(5.7145743788657,3.6294204802266,6.87709513740887));
#49366=CARTESIAN_POINT('Ctrl Pts',(5.60946300447908,3.78984041127712,6.88611533071484));
#49367=CARTESIAN_POINT('Ctrl Pts',(5.49780429068075,3.94543242007418,6.89513552402083));
#49368=CARTESIAN_POINT('Ctrl Pts',(5.38603249445696,4.10118200476601,6.90416485253268));
#49369=CARTESIAN_POINT('Ctrl Pts',(5.26770025628819,4.25209370862804,6.91319418104454));
#49370=CARTESIAN_POINT('Ctrl Pts',(5.14324103084691,4.39765399941979,6.92222350955639));
#49371=CARTESIAN_POINT('Ctrl Pts',(5.01860634297532,4.54341950089229,6.9312655676021));
#49372=CARTESIAN_POINT('Ctrl Pts',(4.88782755191063,4.68381832229776,6.9403076256478));
#49373=CARTESIAN_POINT('Ctrl Pts',(4.75137719411006,4.81837148415218,6.94934968369351));
#49374=CARTESIAN_POINT('Ctrl Pts',(4.63296199580585,4.93514024606876,6.95719661875341));
#49375=CARTESIAN_POINT('Ctrl Pts',(4.51027606519611,5.04750702371292,6.96504355381332));
#49376=CARTESIAN_POINT('Ctrl Pts',(4.3836493741138,5.15518255397728,6.97289048887322));
#49377=CARTESIAN_POINT('Ctrl Pts',(4.24400118439036,5.27393076377734,6.98154435376242));
#49378=CARTESIAN_POINT('Ctrl Pts',(4.09943611034982,5.38707693006477,6.99019821865163));
#49379=CARTESIAN_POINT('Ctrl Pts',(3.95042111681411,5.49422078186062,6.99885208354083));
#49380=CARTESIAN_POINT('Ctrl Pts',(3.8015765489339,5.60124209524111,7.00749605116693));
#49381=CARTESIAN_POINT('Ctrl Pts',(3.64829246275145,5.7022746152954,7.01614001879301));
#49382=CARTESIAN_POINT('Ctrl Pts',(3.4910679425598,5.79695899764966,7.02478398641911));
#49383=CARTESIAN_POINT('Ctrl Pts',(3.36292878294622,5.87412747727749,7.03182888467026));
#49384=CARTESIAN_POINT('Ctrl Pts',(3.23217292507896,5.94707998107329,7.03887378292142));
#49385=CARTESIAN_POINT('Ctrl Pts',(3.09908550384722,6.01564277861012,7.04591868117257));
#49386=CARTESIAN_POINT('Ctrl Pts',(3.09908550384713,6.01564277861016,5.04570102894007));
#49387=CARTESIAN_POINT('Ctrl Pts',(2.96060988807933,6.08698141842904,5.05304231185843));
#49388=CARTESIAN_POINT('Ctrl Pts',(2.81975889686845,6.15349062528649,5.06038359477678));
#49389=CARTESIAN_POINT('Ctrl Pts',(2.67689005748957,6.21502603535283,5.06772487769516));
#49390=CARTESIAN_POINT('Ctrl Pts',(2.51502762950118,6.28474222345865,5.07604214185773));
#49391=CARTESIAN_POINT('Ctrl Pts',(2.35028361639528,6.34819853892449,5.08435940602031));
#49392=CARTESIAN_POINT('Ctrl Pts',(2.18317710810674,6.40515625997045,5.0926766701829));
#49393=CARTESIAN_POINT('Ctrl Pts',(2.01621154182683,6.46206594138173,5.10098691934691));
#49394=CARTESIAN_POINT('Ctrl Pts',(1.84688777793817,6.51248783712324,5.10929716851094));
#49395=CARTESIAN_POINT('Ctrl Pts',(1.67574511035961,6.55623118301253,5.11760741767495));
#49396=CARTESIAN_POINT('Ctrl Pts',(1.50471544614211,6.5999456457181,5.12591217968546));
#49397=CARTESIAN_POINT('Ctrl Pts',(1.33186960724448,6.63699025972096,5.13421694169597));
#49398=CARTESIAN_POINT('Ctrl Pts',(1.15776250433495,6.66722393380904,5.14252170370648));
#49399=CARTESIAN_POINT('Ctrl Pts',(0.983738490705086,6.69744317945532,5.15082250242841));
#49400=CARTESIAN_POINT('Ctrl Pts',(0.808454754614934,6.72085790351684,5.15912330115034));
#49401=CARTESIAN_POINT('Ctrl Pts',(0.632477093025629,6.73737795635645,5.16742409987226));
#49402=CARTESIAN_POINT('Ctrl Pts',(0.456551210467332,6.75389314839544,5.17572245619718));
#49403=CARTESIAN_POINT('Ctrl Pts',(0.279932155294058,6.76351768047052,5.1840208125221));
#49404=CARTESIAN_POINT('Ctrl Pts',(0.10319178066811,6.76621315481581,5.19231916884702));
#49405=CARTESIAN_POINT('Ctrl Pts',(-0.0735665763870974,6.76890890341184,
5.20061836948726));
#49406=CARTESIAN_POINT('Ctrl Pts',(-0.250445929904685,6.76467417280375,
5.2089175701275));
#49407=CARTESIAN_POINT('Ctrl Pts',(-0.42687288964805,6.75352267606199,5.21721677076773));
#49408=CARTESIAN_POINT('Ctrl Pts',(-0.603317735450877,6.74237004878818,
5.22551681277596));
#49409=CARTESIAN_POINT('Ctrl Pts',(-0.779309748703458,6.72429927912349,
5.23381685478417));
#49410=CARTESIAN_POINT('Ctrl Pts',(-0.954279217350867,6.6993761034392,5.2421168967924));
#49411=CARTESIAN_POINT('Ctrl Pts',(-1.12929546965289,6.67444626375089,5.25041915808094));
#49412=CARTESIAN_POINT('Ctrl Pts',(-1.30328828795574,6.64266041533566,5.25872141936948));
#49413=CARTESIAN_POINT('Ctrl Pts',(-1.47569653483271,6.60413572975925,5.26702368065803));
#49414=CARTESIAN_POINT('Ctrl Pts',(-1.64817950415611,6.56559434742496,5.27532954018091));
#49415=CARTESIAN_POINT('Ctrl Pts',(-1.81907619401594,6.52030838287258,5.2836353997038));
#49416=CARTESIAN_POINT('Ctrl Pts',(-1.98783885772199,6.46844538322235,5.29194125922669));
#49417=CARTESIAN_POINT('Ctrl Pts',(-2.15680101067289,6.41652107788751,5.30025693685512));
#49418=CARTESIAN_POINT('Ctrl Pts',(-2.32362376455614,6.35800430652203,5.30857261448358));
#49419=CARTESIAN_POINT('Ctrl Pts',(-2.48777653396244,6.29311186274849,5.31688829211201));
#49420=CARTESIAN_POINT('Ctrl Pts',(-2.6520331285876,6.2281783750608,5.32520922933523));
#49421=CARTESIAN_POINT('Ctrl Pts',(-2.8136160531346,6.15686131328763,5.33353016655844));
#49422=CARTESIAN_POINT('Ctrl Pts',(-2.97201757871664,6.07942435694362,5.34185110378165));
#49423=CARTESIAN_POINT('Ctrl Pts',(-3.13065453812543,6.00187230525001,5.35018440849997));
#49424=CARTESIAN_POINT('Ctrl Pts',(-3.28610034261774,5.91818234570724,5.35851771321829));
#49425=CARTESIAN_POINT('Ctrl Pts',(-3.43787343049739,5.82866324948355,5.36685101793661));
#49426=CARTESIAN_POINT('Ctrl Pts',(-3.54958768017435,5.76277173468273,5.37298483847715));
#49427=CARTESIAN_POINT('Ctrl Pts',(-3.65931267820274,5.69372300525311,5.37911865901768));
#49428=CARTESIAN_POINT('Ctrl Pts',(-3.76686754625777,5.62165437295375,5.38525247955822));
#49429=CARTESIAN_POINT('Ctrl Pts',(-3.90796295367395,5.52711143668235,5.39329910658529));
#49430=CARTESIAN_POINT('Ctrl Pts',(-4.04576267621236,5.42707475399575,5.40134573361236));
#49431=CARTESIAN_POINT('Ctrl Pts',(-4.17979619976959,5.32180352215222,5.40939236063943));
#49432=CARTESIAN_POINT('Ctrl Pts',(-4.31366165359394,5.21666429391006,5.41742889769484));
#49433=CARTESIAN_POINT('Ctrl Pts',(-4.4437700129408,5.1063038040983,5.42546543475023));
#49434=CARTESIAN_POINT('Ctrl Pts',(-4.56967686955862,4.99102617783367,5.43350197180564));
#49435=CARTESIAN_POINT('Ctrl Pts',(-4.69545376133827,4.87586754459646,5.44153021330618));
#49436=CARTESIAN_POINT('Ctrl Pts',(-4.81703750576381,4.75580212563093,5.44955845480673));
#49437=CARTESIAN_POINT('Ctrl Pts',(-4.93401423702517,4.63117614746329,5.45758669630726));
#49438=CARTESIAN_POINT('Ctrl Pts',(-5.05089610727587,4.50665123338008,5.46560842739248));
#49439=CARTESIAN_POINT('Ctrl Pts',(-5.1631781441165,4.37757339245244,5.4736301584777));
#49440=CARTESIAN_POINT('Ctrl Pts',(-5.27048114814646,4.24432768139229,5.48165188956293));
#49441=CARTESIAN_POINT('Ctrl Pts',(-5.37772084964118,4.11116057755657,5.48966888829308));
#49442=CARTESIAN_POINT('Ctrl Pts',(-5.47998713047492,3.97383078937911,5.49768588702323));
#49443=CARTESIAN_POINT('Ctrl Pts',(-5.57693922378061,3.83275852282105,5.50570288575338));
#49444=CARTESIAN_POINT('Ctrl Pts',(-5.67386901811393,3.69171870287106,5.51371804057458));
#49445=CARTESIAN_POINT('Ctrl Pts',(-5.76548683904399,3.54693842249234,5.52173319539578));
#49446=CARTESIAN_POINT('Ctrl Pts',(-5.85149359751363,3.39886917639632,5.52974835021698));
#49447=CARTESIAN_POINT('Ctrl Pts',(-5.9374922841178,3.2508138268249,5.53776275280367));
#49448=CARTESIAN_POINT('Ctrl Pts',(-6.01788076646333,3.09947044990491,5.54577715539037));
#49449=CARTESIAN_POINT('Ctrl Pts',(-6.0924046714446,2.94531735460885,5.55379155797706));
#49450=CARTESIAN_POINT('Ctrl Pts',(-6.16693648268986,2.7911479051635,5.56180681081419));
#49451=CARTESIAN_POINT('Ctrl Pts',(-6.23560231446444,2.63416848215493,5.56982206365131));
#49452=CARTESIAN_POINT('Ctrl Pts',(-6.29819500581745,2.47487952609741,5.57783731648844));
#49453=CARTESIAN_POINT('Ctrl Pts',(-6.36080685614849,2.31554181333134,5.5858550227119));
#49454=CARTESIAN_POINT('Ctrl Pts',(-6.41734172925842,2.15389351004909,5.59387272893535));
#49455=CARTESIAN_POINT('Ctrl Pts',(-6.46764166901062,1.99045227053492,5.60189043515881));
#49456=CARTESIAN_POINT('Ctrl Pts',(-6.51799867509558,1.82682560351907,5.60991723763752));
#49457=CARTESIAN_POINT('Ctrl Pts',(-6.56210650942972,1.66140229693687,5.61794404011624));
#49458=CARTESIAN_POINT('Ctrl Pts',(-6.59985770159272,1.49471312255139,5.62597084259495));
#49459=CARTESIAN_POINT('Ctrl Pts',(-6.6376307381098,1.32792749512324,5.63400228970356));
#49460=CARTESIAN_POINT('Ctrl Pts',(-6.66903973921222,1.15987490950143,5.64203373681217));
#49461=CARTESIAN_POINT('Ctrl Pts',(-6.69402897970091,0.991092840718971,
5.65006518392077));
#49462=CARTESIAN_POINT('Ctrl Pts',(-6.71905865329892,0.822037679049174,
5.65810962607735));
#49463=CARTESIAN_POINT('Ctrl Pts',(-6.73764777526922,0.652251048843681,
5.66615406823393));
#49464=CARTESIAN_POINT('Ctrl Pts',(-6.74979270623879,0.482273182756081,
5.67419851039051));
#49465=CARTESIAN_POINT('Ctrl Pts',(-6.76135787439611,0.320409553456583,
5.6818589348512));
#49466=CARTESIAN_POINT('Ctrl Pts',(-6.76707983323911,0.158372786142489,
5.68951935931186));
#49467=CARTESIAN_POINT('Ctrl Pts',(-6.76699915828328,-0.00337517308298123,
5.69717978377255));
#49468=CARTESIAN_POINT('',(-6.76699945935947,-0.00162771900841451,5.30282021618985));
#49469=CARTESIAN_POINT('Ctrl Pts',(3.09908550384716,6.01564277861015,4.65139679042609));
#49470=CARTESIAN_POINT('Ctrl Pts',(2.93373232018321,6.10082796552484,4.66014623832538));
#49471=CARTESIAN_POINT('Ctrl Pts',(2.76486502144414,6.17919158180196,4.66889568622467));
#49472=CARTESIAN_POINT('Ctrl Pts',(2.59305716434336,6.25046746591386,4.67764513412396));
#49473=CARTESIAN_POINT('Ctrl Pts',(2.42125069459268,6.3217427744723,4.68639451137138));
#49474=CARTESIAN_POINT('Ctrl Pts',(2.24650397871045,6.3859303555783,4.6951438886188));
#49475=CARTESIAN_POINT('Ctrl Pts',(2.06941053323759,6.44281220003543,4.70389326586621));
#49476=CARTESIAN_POINT('Ctrl Pts',(1.89231845896674,6.49969360406688,4.71264257536881));
#49477=CARTESIAN_POINT('Ctrl Pts',(1.71287996431498,6.54926929700883,4.7213918848714));
#49478=CARTESIAN_POINT('Ctrl Pts',(1.531704491735,6.5913709006548,4.730141194374));
#49479=CARTESIAN_POINT('Ctrl Pts',(1.35053036178162,6.63347219230085,4.73889043903859));
#49480=CARTESIAN_POINT('Ctrl Pts',(1.16761955878833,6.66809944062456,4.74763968370318));
#49481=CARTESIAN_POINT('Ctrl Pts',(0.983593309310341,6.69513503985393,4.75638892836777));
#49482=CARTESIAN_POINT('Ctrl Pts',(0.799568362459814,6.72217044771216,4.76513811110095));
#49483=CARTESIAN_POINT('Ctrl Pts',(0.614428268438406,6.74161427235979,4.77388729383413));
#49484=CARTESIAN_POINT('Ctrl Pts',(0.428801816330058,6.75340047696803,4.7826364765673));
#49485=CARTESIAN_POINT('Ctrl Pts',(0.243176616522525,6.76518660206243,4.79138560027544));
#49486=CARTESIAN_POINT('Ctrl Pts',(0.0570653511651543,6.76931519233997,
4.80013472398358));
#49487=CARTESIAN_POINT('Ctrl Pts',(-0.128899900800383,6.76577222610794,
4.80888384769172));
#49488=CARTESIAN_POINT('Ctrl Pts',(-0.314863959942484,6.76222928260131,
4.81763291528098));
#49489=CARTESIAN_POINT('Ctrl Pts',(-0.500681721081251,6.75101488651273,
4.82638198287024));
#49490=CARTESIAN_POINT('Ctrl Pts',(-0.685722110173975,6.73216712415984,
4.83513105045951));
#49491=CARTESIAN_POINT('Ctrl Pts',(-0.870761373828219,6.71331947644137,
4.84388006483587));
#49492=CARTESIAN_POINT('Ctrl Pts',(-1.05502298984397,6.68683858439988,4.85262907921223));
#49493=CARTESIAN_POINT('Ctrl Pts',(-1.23788117676106,6.65281438131417,4.86137809358858));
#49494=CARTESIAN_POINT('Ctrl Pts',(-1.4300964145184,6.61704912302367,4.87057480447611));
#49495=CARTESIAN_POINT('Ctrl Pts',(-1.62076048992743,6.57294837083153,4.87977151536364));
#49496=CARTESIAN_POINT('Ctrl Pts',(-1.80915798961179,6.52067760042036,4.88896822625117));
#49497=CARTESIAN_POINT('Ctrl Pts',(-1.98840443003052,6.47094578577396,4.89771822395767));
#49498=CARTESIAN_POINT('Ctrl Pts',(-2.16559895952225,6.41381888474464,4.90646822166418));
#49499=CARTESIAN_POINT('Ctrl Pts',(-2.34013966242349,6.34949095285225,4.91521821937069));
#49500=CARTESIAN_POINT('Ctrl Pts',(-2.51467682554032,6.28516432556678,4.92396803962228));
#49501=CARTESIAN_POINT('Ctrl Pts',(-2.68656000078851,6.21363705879657,4.93271785987386));
#49502=CARTESIAN_POINT('Ctrl Pts',(-2.85520533840889,6.13515211510859,4.94146768012546));
#49503=CARTESIAN_POINT('Ctrl Pts',(-3.02384747998326,6.05666865881122,4.9502173345567));
#49504=CARTESIAN_POINT('Ctrl Pts',(-3.18925164684535,5.97122791039845,4.95896698898793));
#49505=CARTESIAN_POINT('Ctrl Pts',(-3.35085601829155,5.8791200825191,4.96771664341918));
#49506=CARTESIAN_POINT('Ctrl Pts',(-3.51245754191412,5.78701387778178,4.97646614366232));
#49507=CARTESIAN_POINT('Ctrl Pts',(-3.67025915510926,5.68824097060989,4.98521564390547));
#49508=CARTESIAN_POINT('Ctrl Pts',(-3.82372487928822,5.58313684656863,4.9939651441486));
#49509=CARTESIAN_POINT('Ctrl Pts',(-3.97718810300776,5.47803443501788,5.00271450183372));
#49510=CARTESIAN_POINT('Ctrl Pts',(-4.12631534262996,5.36660117496398,5.01146385951883));
#49511=CARTESIAN_POINT('Ctrl Pts',(-4.27060009886188,5.24921554097381,5.02021321720395));
#49512=CARTESIAN_POINT('Ctrl Pts',(-4.41488269594184,5.13183166360317,5.02896244395913));
#49513=CARTESIAN_POINT('Ctrl Pts',(-4.55432273235067,5.00849577139491,5.03771167071432));
#49514=CARTESIAN_POINT('Ctrl Pts',(-4.68844662480192,4.87962675277356,5.0464608974695));
#49515=CARTESIAN_POINT('Ctrl Pts',(-4.82256868835141,4.75075949139898,5.05521000492099));
#49516=CARTESIAN_POINT('Ctrl Pts',(-4.95137454637844,4.61635945312545,5.06395911237248));
#49517=CARTESIAN_POINT('Ctrl Pts',(-5.07442674461058,4.47688309134613,5.07270821982397));
#49518=CARTESIAN_POINT('Ctrl Pts',(-5.19747742838508,4.33740844616388,5.08145721959633));
#49519=CARTESIAN_POINT('Ctrl Pts',(-5.31477440450886,4.19285781736081,5.09020621936869));
#49520=CARTESIAN_POINT('Ctrl Pts',(-5.42591931531102,4.04372211999474,5.09895521914106));
#49521=CARTESIAN_POINT('Ctrl Pts',(-5.53707636462934,3.89457013500869,5.10770517442164));
#49522=CARTESIAN_POINT('Ctrl Pts',(-5.64207983273426,3.74083230916487,5.11645512970222));
#49523=CARTESIAN_POINT('Ctrl Pts',(-5.74057303468706,3.58303087251894,5.1252050849828));
#49524=CARTESIAN_POINT('Ctrl Pts',(-5.83906243363735,3.42523552887483,5.13395470241161));
#49525=CARTESIAN_POINT('Ctrl Pts',(-5.93104191768405,3.26337713157031,5.14270431984042));
#49526=CARTESIAN_POINT('Ctrl Pts',(-6.01619906699645,3.09800545291178,5.15145393726924));
#49527=CARTESIAN_POINT('Ctrl Pts',(-6.10135338095373,2.93263928039616,5.16020326337463));
#49528=CARTESIAN_POINT('Ctrl Pts',(-6.1796856835283,2.76376031540244,5.16895258948003));
#49529=CARTESIAN_POINT('Ctrl Pts',(-6.25092992694879,2.5919421383156,5.17770191558542));
#49530=CARTESIAN_POINT('Ctrl Pts',(-6.32217217691096,2.42012876880839,5.18645099687921));
#49531=CARTESIAN_POINT('Ctrl Pts',(-6.38632665483843,2.24537661647691,5.19520007817299));
#49532=CARTESIAN_POINT('Ctrl Pts',(-6.44317547869343,2.06827917621478,5.20394915946679));
#49533=CARTESIAN_POINT('Ctrl Pts',(-6.50002944235931,1.89116572423442,5.21269903178175));
#49534=CARTESIAN_POINT('Ctrl Pts',(-6.54957634250395,1.71170683289213,5.22144890409672));
#49535=CARTESIAN_POINT('Ctrl Pts',(-6.59164787708393,1.53051209225375,5.23019877641168));
#49536=CARTESIAN_POINT('Ctrl Pts',(-6.63371649075007,1.34932993148038,5.23894804124648));
#49537=CARTESIAN_POINT('Ctrl Pts',(-6.66831071257123,1.16641244174009,5.24769730608128));
#49538=CARTESIAN_POINT('Ctrl Pts',(-6.69531304840333,0.98238087516003,5.25644657091607));
#49539=CARTESIAN_POINT('Ctrl Pts',(-6.72231677033044,0.79833986179583,5.26519628487173));
#49540=CARTESIAN_POINT('Ctrl Pts',(-6.7417277847789,0.613184940730109,5.27394599882738));
#49541=CARTESIAN_POINT('Ctrl Pts',(-6.75348015835518,0.427545027690477,
5.28269571278304));
#49542=CARTESIAN_POINT('Ctrl Pts',(-6.76249038365217,0.285219953547529,
5.28940388058531));
#49543=CARTESIAN_POINT('Ctrl Pts',(-6.76699999999996,0.1426099957588,5.29611204838757));
#49544=CARTESIAN_POINT('Ctrl Pts',(-6.767,2.19816073760199E-12,5.30282021618984));
#49545=CARTESIAN_POINT('Ctrl Pts',(-6.76699850691525,-0.00449526492710441,
5.30282021618984));
#49546=CARTESIAN_POINT('Ctrl Pts',(-6.76686712558602,-0.202271652565106,
5.3121201420737));
#49547=CARTESIAN_POINT('Ctrl Pts',(-6.75806106437177,-0.39986068289801,
5.32142006795755));
#49548=CARTESIAN_POINT('Ctrl Pts',(-6.74065422882093,-0.596548042892271,
5.33071999384141));
#49549=CARTESIAN_POINT('Ctrl Pts',(-6.72321584937777,-0.793591830962378,
5.34003677263686));
#49550=CARTESIAN_POINT('Ctrl Pts',(-6.69714555455995,-0.989730505222333,
5.34935355143229));
#49551=CARTESIAN_POINT('Ctrl Pts',(-6.6625689230473,-1.18425687485627,5.35867033022774));
#49552=CARTESIAN_POINT('Ctrl Pts',(-6.6279234183554,-1.37917072149241,5.36800566711135));
#49553=CARTESIAN_POINT('Ctrl Pts',(-6.58473771102242,-1.57246566374954,
5.37734100399497));
#49554=CARTESIAN_POINT('Ctrl Pts',(-6.53318870196399,-1.76344389888935,
5.38667634087858));
#49555=CARTESIAN_POINT('Ctrl Pts',(-6.48899557088559,-1.92717015343461,
5.39467955518074));
#49556=CARTESIAN_POINT('Ctrl Pts',(-6.43865651999273,-2.08919386410022,
5.40268276948291));
#49557=CARTESIAN_POINT('Ctrl Pts',(-6.38231203820803,-2.24908471315442,
5.41068598378507));
#49558=CARTESIAN_POINT('Ctrl Pts',(-6.32138973410239,-2.42196622029136,
5.41933943555346));
#49559=CARTESIAN_POINT('Ctrl Pts',(-6.25340012608952,-2.59248103478967,
5.42799288732183));
#49560=CARTESIAN_POINT('Ctrl Pts',(-6.17854530260445,-2.76004835893586,
5.43664633909022));
#49561=CARTESIAN_POINT('Ctrl Pts',(-6.10375943657722,-2.9274613173892,5.44529181916075));
#49562=CARTESIAN_POINT('Ctrl Pts',(-6.02212109271198,-3.09193192456616,
5.45393729923131));
#49563=CARTESIAN_POINT('Ctrl Pts',(-5.93388087430132,-3.25289821076544,
5.46258277930184));
#49564=CARTESIAN_POINT('Ctrl Pts',(-5.84298590354066,-3.41870725046482,
5.47148836308639));
#49565=CARTESIAN_POINT('Ctrl Pts',(-5.74508571091698,-3.58079750791184,
5.48039394687094));
#49566=CARTESIAN_POINT('Ctrl Pts',(-5.64050693340576,-3.73857867834844,
5.48929953065549));
#49567=CARTESIAN_POINT('Ctrl Pts',(-5.53917520796711,-3.89146092293535,
5.49792860619455));
#49568=CARTESIAN_POINT('Ctrl Pts',(-5.43157357537333,-4.04029736648063,
5.5065576817336));
#49569=CARTESIAN_POINT('Ctrl Pts',(-5.31804515951534,-4.18457700148479,
5.51518675727266));
#49570=CARTESIAN_POINT('Ctrl Pts',(-5.19905992335141,-4.33579153499937,
5.52423059517995));
#49571=CARTESIAN_POINT('Ctrl Pts',(-5.07356426827074,-4.48200010995743,
5.53327443308723));
#49572=CARTESIAN_POINT('Ctrl Pts',(-4.94200381528476,-4.6226493799239,5.54231827099453));
#49573=CARTESIAN_POINT('Ctrl Pts',(-4.81044336229875,-4.76329864989043,
5.55136210890182));
#49574=CARTESIAN_POINT('Ctrl Pts',(-4.67281834933547,-4.89838830979678,
5.56040594680911));
#49575=CARTESIAN_POINT('Ctrl Pts',(-4.52962289084241,-5.02740544085679,
5.56944978471641));
#49576=CARTESIAN_POINT('Ctrl Pts',(-4.39621318227486,-5.14760574634184,
5.57787558112254));
#49577=CARTESIAN_POINT('Ctrl Pts',(-4.25802693377784,-5.26248265905892,
5.58630137752867));
#49578=CARTESIAN_POINT('Ctrl Pts',(-4.11552196541618,-5.37166342506462,
5.5947271739348));
#49579=CARTESIAN_POINT('Ctrl Pts',(-3.97298392881197,-5.48086952643998,
5.60315492554489));
#49580=CARTESIAN_POINT('Ctrl Pts',(-3.82612543733519,-5.584376644035,5.61158267715496));
#49581=CARTESIAN_POINT('Ctrl Pts',(-3.6754352504014,-5.68185398616568,5.62001042876506));
#49582=CARTESIAN_POINT('Ctrl Pts',(-3.52468969024317,-5.77936714771402,
5.62844127727078));
#49583=CARTESIAN_POINT('Ctrl Pts',(-3.37010990539355,-5.87084593587486,
5.63687212577652));
#49584=CARTESIAN_POINT('Ctrl Pts',(-3.2122116538631,-5.95600413790875,5.64530297428225));
#49585=CARTESIAN_POINT('Ctrl Pts',(-3.0541683115073,-6.04124059080164,5.65374156979439));
#49586=CARTESIAN_POINT('Ctrl Pts',(-2.89280070223597,-6.12014469643793,
5.66218016530653));
#49587=CARTESIAN_POINT('Ctrl Pts',(-2.72864809358529,-6.19247677277625,
5.67061876081867));
#49588=CARTESIAN_POINT('Ctrl Pts',(-2.56440940912534,-6.26484677749145,
5.67906178123118));
#49589=CARTESIAN_POINT('Ctrl Pts',(-2.3973831189156,-6.33063775359861,5.68750480164366));
#49590=CARTESIAN_POINT('Ctrl Pts',(-2.22812680736587,-6.38965882737862,
5.69594782205617));
#49591=CARTESIAN_POINT('Ctrl Pts',(-2.0586926790306,-6.4487419073404,5.70439971251161));
#49592=CARTESIAN_POINT('Ctrl Pts',(-1.88702416464294,-6.50104077596697,
5.71285160296706));
#49593=CARTESIAN_POINT('Ctrl Pts',(-1.71369331326014,-6.54641460863025,
5.7213034934225));
#49594=CARTESIAN_POINT('Ctrl Pts',(-1.66645606399572,-6.55878018017448,
5.7236068574977));
#49595=CARTESIAN_POINT('Ctrl Pts',(-1.61909540894081,-6.57063171786553,
5.72591022157289));
#49596=CARTESIAN_POINT('Ctrl Pts',(-1.57162304102097,-6.58196703250115,
5.72821358564809));
#49597=CARTESIAN_POINT('Ctrl Pts',(-1.40020410266727,-6.62289795054643,
5.73653084981068));
#49598=CARTESIAN_POINT('Ctrl Pts',(-1.22701956688522,-6.65716762216335,
5.74484811397329));
#49599=CARTESIAN_POINT('Ctrl Pts',(-1.05262176761499,-6.68462986367556,
5.75316537813588));
#49600=CARTESIAN_POINT('Ctrl Pts',(-0.878371060019486,-6.71206894281351,
5.76147562729988));
#49601=CARTESIAN_POINT('Ctrl Pts',(-0.702909469604499,-6.73271197739186,
5.76978587646388));
#49602=CARTESIAN_POINT('Ctrl Pts',(-0.526801012309971,-6.74646349530102,
5.77809612562788));
#49603=CARTESIAN_POINT('Ctrl Pts',(-0.35080883722523,-6.76020593325504,
5.78640088763839));
#49604=CARTESIAN_POINT('Ctrl Pts',(-0.174170991962337,-6.7670658947502,
5.7947056496489));
#49605=CARTESIAN_POINT('Ctrl Pts',(0.00254163895903234,-6.76699952268887,
5.80301041165941));
#49606=CARTESIAN_POINT('Ctrl Pts',(0.179169937162344,-6.76693318230234,
5.81131121038134));
#49607=CARTESIAN_POINT('Ctrl Pts',(0.355872602784891,-6.75994709595507,
5.81961200910326));
#49608=CARTESIAN_POINT('Ctrl Pts',(0.532076760645481,-6.74604946029756,
5.82791280782519));
#49609=CARTESIAN_POINT('Ctrl Pts',(0.708229072831554,-6.73215591383014,
5.8362111641501));
#49610=CARTESIAN_POINT('Ctrl Pts',(0.883882823289214,-6.7113548989976,5.84450952047502));
#49611=CARTESIAN_POINT('Ctrl Pts',(1.0584680436725,-6.68370663633018,5.85280787679993));
#49612=CARTESIAN_POINT('Ctrl Pts',(1.23307102720931,-6.6560555605934,5.86110707744017));
#49613=CARTESIAN_POINT('Ctrl Pts',(1.40660491873926,-6.62155589197754,5.8694062780804));
#49614=CARTESIAN_POINT('Ctrl Pts',(1.57850717050345,-6.58031945369442,5.87770547872064));
#49615=CARTESIAN_POINT('Ctrl Pts',(1.75042684961498,-6.53907883488588,5.88600552072887));
#49616=CARTESIAN_POINT('Ctrl Pts',(1.92071422071009,-6.49110016576597,5.8943055627371));
#49617=CARTESIAN_POINT('Ctrl Pts',(2.08881927963228,-6.43654589178361,5.90260560474533));
#49618=CARTESIAN_POINT('Ctrl Pts',(2.25696928679073,-6.3819770309803,5.91090786603388));
#49619=CARTESIAN_POINT('Ctrl Pts',(2.42293548783468,-6.32082916845419,5.91921012732243));
#49620=CARTESIAN_POINT('Ctrl Pts',(2.58618514530947,-6.25331395295172,5.92751238861098));
#49621=CARTESIAN_POINT('Ctrl Pts',(2.74950555586026,-6.18576947607591,5.93581824813387));
#49622=CARTESIAN_POINT('Ctrl Pts',(2.91010675505354,-6.11185227910375,5.94412410765676));
#49623=CARTESIAN_POINT('Ctrl Pts',(3.06747783523843,-6.03182134436366,5.95242996717965));
#49624=CARTESIAN_POINT('Ctrl Pts',(3.22503493902153,-5.9516958074741,5.96074564480809));
#49625=CARTESIAN_POINT('Ctrl Pts',(3.37935398466859,-5.86544225163518,5.96906132243655));
#49626=CARTESIAN_POINT('Ctrl Pts',(3.52994941545288,-5.77336523392933,5.97737700006499));
#49627=CARTESIAN_POINT('Ctrl Pts',(3.68064009655534,-5.68122997829961,5.9856979372882));
#49628=CARTESIAN_POINT('Ctrl Pts',(3.82760217695544,-5.58326410807159,5.9940188745114));
#49629=CARTESIAN_POINT('Ctrl Pts',(3.97038065700308,-5.47981445292592,6.0023398117346));
#49630=CARTESIAN_POINT('Ctrl Pts',(4.11337135018338,-5.37621103948709,6.01067311645292));
#49631=CARTESIAN_POINT('Ctrl Pts',(4.2521657429859,-5.26710776735871,6.01900642117124));
#49632=CARTESIAN_POINT('Ctrl Pts',(4.38634234683893,-5.15289140350615,6.02733972588956));
#49633=CARTESIAN_POINT('Ctrl Pts',(4.48510451102092,-5.06882119338642,6.03347354643007));
#49634=CARTESIAN_POINT('Ctrl Pts',(4.58136554754155,-4.98198159944445,6.03960736697059));
#49635=CARTESIAN_POINT('Ctrl Pts',(4.6749708000818,-4.89253891332328,6.0457411875111));
#49636=CARTESIAN_POINT('Ctrl Pts',(4.79814471550554,-4.77484246406876,6.0538126009412));
#49637=CARTESIAN_POINT('Ctrl Pts',(4.91709761676779,-4.65227487782898,6.06188401437129));
#49638=CARTESIAN_POINT('Ctrl Pts',(5.03140928200621,-4.52517509461698,6.06995542780139));
#49639=CARTESIAN_POINT('Ctrl Pts',(5.14557743843213,-4.39823487463869,6.07801670824152));
#49640=CARTESIAN_POINT('Ctrl Pts',(5.25511570620615,-4.26677405271283,6.08607798868166));
#49641=CARTESIAN_POINT('Ctrl Pts',(5.35963739888591,-4.1311712567338,6.0941392691218));
#49642=CARTESIAN_POINT('Ctrl Pts',(5.46405079534005,-3.99570896049804,6.10219219716902));
#49643=CARTESIAN_POINT('Ctrl Pts',(5.56345773458674,-3.85611352341332,6.11024512521624));
#49644=CARTESIAN_POINT('Ctrl Pts',(5.6575089208742,-3.71279972665222,6.11829805326346));
#49645=CARTESIAN_POINT('Ctrl Pts',(5.75148325460727,-3.56960303666878,6.12634440097804));
#49646=CARTESIAN_POINT('Ctrl Pts',(5.84011034227156,-3.42269434469623,6.13439074869264));
#49647=CARTESIAN_POINT('Ctrl Pts',(5.92308175312647,-3.27252067155889,6.14243709640722));
#49648=CARTESIAN_POINT('Ctrl Pts',(6.00600351495872,-3.12243686041164,6.15047862929106));
#49649=CARTESIAN_POINT('Ctrl Pts',(6.08327615720387,-2.96909228302733,6.15852016217489));
#49650=CARTESIAN_POINT('Ctrl Pts',(6.15463516987641,-2.81296194885754,6.16656169505873));
#49651=CARTESIAN_POINT('Ctrl Pts',(6.22736603805992,-2.65383005607113,6.17475782398854));
#49652=CARTESIAN_POINT('Ctrl Pts',(6.2939533711383,-2.49180453750885,6.18295395291833));
#49653=CARTESIAN_POINT('Ctrl Pts',(6.3541666018031,-2.32741397188599,6.19115008184814));
#49654=CARTESIAN_POINT('Ctrl Pts',(6.41322369269179,-2.16617983001973,6.19918883887544));
#49655=CARTESIAN_POINT('Ctrl Pts',(6.46614912570988,-2.0026710103283,6.20722759590274));
#49656=CARTESIAN_POINT('Ctrl Pts',(6.51277444295866,-1.83740525065771,6.21526635293004));
#49657=CARTESIAN_POINT('Ctrl Pts',(6.55940427304571,-1.67212349500706,6.22330588802412));
#49658=CARTESIAN_POINT('Ctrl Pts',(6.5997326716581,-1.50508482020148,6.23134542311823));
#49659=CARTESIAN_POINT('Ctrl Pts',(6.63364150784911,-1.33682061075577,6.23938495821231));
#49660=CARTESIAN_POINT('Ctrl Pts',(6.66756034001819,-1.1685067987422,6.24742686327911));
#49661=CARTESIAN_POINT('Ctrl Pts',(6.69505576921223,-0.998967098891834,
6.25546876834588));
#49662=CARTESIAN_POINT('Ctrl Pts',(6.71606110128753,-0.828741385338382,
6.26351067341267));
#49663=CARTESIAN_POINT('Ctrl Pts',(6.73777498972122,-0.652773581573344,
6.27182384974279));
#49664=CARTESIAN_POINT('Ctrl Pts',(6.75255321792446,-0.476073106315516,
6.28013702607293));
#49665=CARTESIAN_POINT('Ctrl Pts',(6.76038053759128,-0.299239013093287,
6.28845020240306));
#49666=CARTESIAN_POINT('Ctrl Pts',(6.76796558691103,-0.127878269493019,
6.2965060702035));
#49667=CARTESIAN_POINT('Ctrl Pts',(6.7690236753614,0.0436075749619817,6.30456193800392));
#49668=CARTESIAN_POINT('Ctrl Pts',(6.76359393379158,0.214676730871604,6.31261780580436));
#49669=CARTESIAN_POINT('Ctrl Pts',(6.75790404914573,0.393941941024649,6.32105963639933));
#49670=CARTESIAN_POINT('Ctrl Pts',(6.74508940122597,0.572749067923802,6.32950146699429));
#49671=CARTESIAN_POINT('Ctrl Pts',(6.72525545491745,0.750485220442785,6.33794329758925));
#49672=CARTESIAN_POINT('Ctrl Pts',(6.70542150860894,0.928221372961769,6.34638512818421));
#49673=CARTESIAN_POINT('Ctrl Pts',(6.67856841781384,1.1048861080945,6.35482695877917));
#49674=CARTESIAN_POINT('Ctrl Pts',(6.64486161298533,1.27988403547902,6.36326878937413));
#49675=CARTESIAN_POINT('Ctrl Pts',(6.61199655583655,1.45051180377893,6.3714998052285));
#49676=CARTESIAN_POINT('Ctrl Pts',(6.57250706355629,1.62012263742595,6.37973082108288));
#49677=CARTESIAN_POINT('Ctrl Pts',(6.52646616979,1.78816339706041,6.38796183693725));
#49678=CARTESIAN_POINT('Ctrl Pts',(6.48048053554156,1.9560024696598,6.39618297370522));
#49679=CARTESIAN_POINT('Ctrl Pts',(6.42795925162016,2.12227487825813,6.40440411047317));
#49680=CARTESIAN_POINT('Ctrl Pts',(6.36902669903641,2.28643563367993,6.41262524724114));
#49681=CARTESIAN_POINT('Ctrl Pts',(6.31015305450766,2.45043229658609,6.42083816628977));
#49682=CARTESIAN_POINT('Ctrl Pts',(6.24488102496868,2.61232117491342,6.42905108533843));
#49683=CARTESIAN_POINT('Ctrl Pts',(6.17338535119798,2.77157036815129,6.43726400438706));
#49684=CARTESIAN_POINT('Ctrl Pts',(6.10194680368452,2.93069231857991,6.44547036117393));
#49685=CARTESIAN_POINT('Ctrl Pts',(6.0242946634999,3.08717845949579,6.45367671796081));
#49686=CARTESIAN_POINT('Ctrl Pts',(5.94065256135273,3.2405147963392,6.46188307474767));
#49687=CARTESIAN_POINT('Ctrl Pts',(5.85706221792892,3.39375624684144,6.47008435334378));
#49688=CARTESIAN_POINT('Ctrl Pts',(5.76748946947354,3.54385146309567,6.47828563193988));
#49689=CARTESIAN_POINT('Ctrl Pts',(5.67220488218159,3.69030903510199,6.48648691053599));
#49690=CARTESIAN_POINT('Ctrl Pts',(5.57695197524829,3.83671791268103,6.49468546235901));
#49691=CARTESIAN_POINT('Ctrl Pts',(5.47599120643469,3.97949125429586,6.502884014182));
#49692=CARTESIAN_POINT('Ctrl Pts',(5.36963776826787,4.11816454717283,6.51108256600503));
#49693=CARTESIAN_POINT('Ctrl Pts',(5.26330037137964,4.25681692397073,6.51927988124129));
#49694=CARTESIAN_POINT('Ctrl Pts',(5.15157214349014,4.39137019951896,6.52747719647758));
#49695=CARTESIAN_POINT('Ctrl Pts',(5.0348100912214,4.52139097461557,6.53567451171385));
#49696=CARTESIAN_POINT('Ctrl Pts',(4.91804444064793,4.6514157566165,6.54387207957019));
#49697=CARTESIAN_POINT('Ctrl Pts',(4.79624489699761,4.77690749391079,6.55206964742652));
#49698=CARTESIAN_POINT('Ctrl Pts',(4.66980706179267,4.89746781568101,6.56026721528286));
#49699=CARTESIAN_POINT('Ctrl Pts',(4.54329344311045,5.01810039810321,6.56846969654346));
#49700=CARTESIAN_POINT('Ctrl Pts',(4.41213623779877,5.13379541143023,6.57667217780403));
#49701=CARTESIAN_POINT('Ctrl Pts',(4.27676655490759,5.24419267712619,6.58487465906462));
#49702=CARTESIAN_POINT('Ctrl Pts',(4.14135426349279,5.35462469110847,6.59307972211169));
#49703=CARTESIAN_POINT('Ctrl Pts',(4.00172713568375,5.45975541490273,6.6012847851588));
#49704=CARTESIAN_POINT('Ctrl Pts',(3.8583472856512,5.55926660840331,6.60948984820587));
#49705=CARTESIAN_POINT('Ctrl Pts',(3.71482347932203,5.65887771317375,6.61770314930375));
#49706=CARTESIAN_POINT('Ctrl Pts',(3.56753972349512,5.75285781936648,6.62591645040162));
#49707=CARTESIAN_POINT('Ctrl Pts',(3.41698563581462,5.84093298751463,6.6341297514995));
#49708=CARTESIAN_POINT('Ctrl Pts',(3.31253589305714,5.90203679942786,6.63982788431064));
#49709=CARTESIAN_POINT('Ctrl Pts',(3.20651263816237,5.96029942014812,6.64552601712176));
#49710=CARTESIAN_POINT('Ctrl Pts',(3.09908550384729,6.01564277861008,6.6512241499329));
#49711=CARTESIAN_POINT('Origin',(0.,0.,-63.6971797838103));
#49712=CARTESIAN_POINT('',(3.09908550384729,6.01564277861008,9.04575635804621));
#49713=CARTESIAN_POINT('',(3.09908550384719,6.01564277861013,8.6513967904261));
#49714=CARTESIAN_POINT('',(3.09908550384721,6.01564277861012,-63.6971797838103));
#49715=CARTESIAN_POINT('',(-6.76699807574441,0.00297333156401857,7.69717978380994));
#49716=CARTESIAN_POINT('Ctrl Pts',(-6.767,2.65028120476538E-12,7.69717978380994));
#49717=CARTESIAN_POINT('Ctrl Pts',(-6.76700000000007,-0.186007249557489,
7.70592929562269));
#49718=CARTESIAN_POINT('Ctrl Pts',(-6.7593263729426,-0.372014355813802,
7.71467880743544));
#49719=CARTESIAN_POINT('Ctrl Pts',(-6.7440051826338,-0.557389537584311,
7.72342831924819));
#49720=CARTESIAN_POINT('Ctrl Pts',(-6.72868405703751,-0.742763936380853,
7.73217779410539));
#49721=CARTESIAN_POINT('Ctrl Pts',(-6.70571545643589,-0.927506130403236,
7.7409272689626));
#49722=CARTESIAN_POINT('Ctrl Pts',(-6.67517739401602,-1.11098864009382,
7.7496767438198));
#49723=CARTESIAN_POINT('Ctrl Pts',(-6.6446394580442,-1.29447039004384,7.75842618244832));
#49724=CARTESIAN_POINT('Ctrl Pts',(-6.60653217002758,-1.47669218339127,
7.76717562107683));
#49725=CARTESIAN_POINT('Ctrl Pts',(-6.56098496085516,-1.65703510627638,
7.77592505970534));
#49726=CARTESIAN_POINT('Ctrl Pts',(-6.51543793649591,-1.83737729739887,
7.78467446283198));
#49727=CARTESIAN_POINT('Ctrl Pts',(-6.46245112156928,-2.01584035544853,
7.79342386595862));
#49728=CARTESIAN_POINT('Ctrl Pts',(-6.40220448361744,-2.19181813797332,
7.80217326908526));
#49729=CARTESIAN_POINT('Ctrl Pts',(-6.34195808511996,-2.36779522106242,
7.8109226374368));
#49730=CARTESIAN_POINT('Ctrl Pts',(-6.27445201416373,-2.54128677725698,
7.81967200578835));
#49731=CARTESIAN_POINT('Ctrl Pts',(-6.19991555052738,-2.71170355428628,
7.82842137413989));
#49732=CARTESIAN_POINT('Ctrl Pts',(-6.12537937695135,-2.88211966813485,
7.83717070844307));
#49733=CARTESIAN_POINT('Ctrl Pts',(-6.04381298028366,-3.04946076419838,
7.84592004274624));
#49734=CARTESIAN_POINT('Ctrl Pts',(-5.95549339308896,-3.21315848424471,
7.85466937704942));
#49735=CARTESIAN_POINT('Ctrl Pts',(-5.86717414225719,-3.37685558085239,
7.86341867803098));
#49736=CARTESIAN_POINT('Ctrl Pts',(-5.77210188843971,-3.53690907700155,
7.87216797901254));
#49737=CARTESIAN_POINT('Ctrl Pts',(-5.67059953311272,-3.69277537024145,
7.88091727999409));
#49738=CARTESIAN_POINT('Ctrl Pts',(-5.56909755592581,-3.84864108281211,
7.88966654838073));
#49739=CARTESIAN_POINT('Ctrl Pts',(-5.4611656815481,-4.00031938355043,7.89841581676734));
#49740=CARTESIAN_POINT('Ctrl Pts',(-5.3471704848819,-4.14729511918406,7.90716508515398));
#49741=CARTESIAN_POINT('Ctrl Pts',(-5.23317570343097,-4.29427031947433,
7.91591432167234));
#49742=CARTESIAN_POINT('Ctrl Pts',(-5.11311781951318,-4.4365427624982,7.92466355819071));
#49743=CARTESIAN_POINT('Ctrl Pts',(-4.98740458928993,-4.57362924412657,
7.93341279470907));
#49744=CARTESIAN_POINT('Ctrl Pts',(-4.86169180652478,-4.71071523781538,
7.94216200008579));
#49745=CARTESIAN_POINT('Ctrl Pts',(-4.730323911413,-4.84261509584755,7.9509112054625));
#49746=CARTESIAN_POINT('Ctrl Pts',(-4.59374706947045,-4.96888084599859,
7.95966041083922));
#49747=CARTESIAN_POINT('Ctrl Pts',(-4.45717070231241,-5.09514615720975,
7.96840958580092));
#49748=CARTESIAN_POINT('Ctrl Pts',(-4.31538563497112,-5.21577720520789,
7.97715876076261));
#49749=CARTESIAN_POINT('Ctrl Pts',(-4.16887340951809,-5.33036429293656,
7.98590793572431));
#49750=CARTESIAN_POINT('Ctrl Pts',(-4.02236168122281,-5.44495099183856,
7.99465708099757));
#49751=CARTESIAN_POINT('Ctrl Pts',(-3.87112305262972,-5.55349359498074,
8.00340622627082));
#49752=CARTESIAN_POINT('Ctrl Pts',(-3.71567116928781,-5.65562346357352,
8.01215537154407));
#49753=CARTESIAN_POINT('Ctrl Pts',(-3.56021980053088,-5.75775299409066,
8.02090448785544));
#49754=CARTESIAN_POINT('Ctrl Pts',(-3.40055544441852,-5.85346967520014,
8.02965360416682));
#49755=CARTESIAN_POINT('Ctrl Pts',(-3.23722035886602,-5.94244843041514,
8.03840272047819));
#49756=CARTESIAN_POINT('Ctrl Pts',(-3.0738858004326,-6.03142689847568,8.04715180855419));
#49757=CARTESIAN_POINT('Ctrl Pts',(-2.90688078789005,-6.11366734708005,
8.0559008966302));
#49758=CARTESIAN_POINT('Ctrl Pts',(-2.73677250610187,-6.18889047001519,
8.06464998470621));
#49759=CARTESIAN_POINT('Ctrl Pts',(-2.56666475916727,-6.26411335643419,
8.07339904527338));
#49760=CARTESIAN_POINT('Ctrl Pts',(-2.39345402456884,-6.33231884545335,
8.08214810584053));
#49761=CARTESIAN_POINT('Ctrl Pts',(-2.21772855943854,-6.39327529804956,
8.0908971664077));
#49762=CARTESIAN_POINT('Ctrl Pts',(-2.04200363223406,-6.4542315640476,8.09964620019249));
#49763=CARTESIAN_POINT('Ctrl Pts',(-1.86376426060876,-6.50793874412497,
8.10839523397729));
#49764=CARTESIAN_POINT('Ctrl Pts',(-1.68361577621558,-6.55421443943346,
8.11714426776209));
#49765=CARTESIAN_POINT('Ctrl Pts',(-1.50346782833082,-6.60048999692618,
8.12589327549098));
#49766=CARTESIAN_POINT('Ctrl Pts',(-1.32141105657251,-6.63933404265189,
8.13464228321988));
#49767=CARTESIAN_POINT('Ctrl Pts',(-1.13806375346396,-6.67061465631553,
8.14339129094877));
#49768=CARTESIAN_POINT('Ctrl Pts',(-0.954716981167985,-6.70189517941801,
8.15214027334823));
#49769=CARTESIAN_POINT('Ctrl Pts',(-0.77007996743962,-6.72561226609036,
8.1608892557477));
#49770=CARTESIAN_POINT('Ctrl Pts',(-0.584779764069763,-6.74168536996014,
8.16963823814716));
#49771=CARTESIAN_POINT('Ctrl Pts',(-0.39148958758965,-6.75845153117892,
8.17876446856277));
#49772=CARTESIAN_POINT('Ctrl Pts',(-0.197478091801936,-6.76689985146404,
8.1878906989784));
#49773=CARTESIAN_POINT('Ctrl Pts',(-0.00346214752773997,-6.76699911434415,
8.19701692939401));
#49774=CARTESIAN_POINT('Ctrl Pts',(0.184490798487905,-6.76709527525926,
8.20585796510914));
#49775=CARTESIAN_POINT('Ctrl Pts',(0.372447602158016,-6.75935633790745,
8.21469900082425));
#49776=CARTESIAN_POINT('Ctrl Pts',(0.559756448197419,-6.74380914014487,
8.22354003653938));
#49777=CARTESIAN_POINT('Ctrl Pts',(0.745136131046603,-6.72842206873119,
8.23229001515269));
#49778=CARTESIAN_POINT('Ctrl Pts',(0.929880851948329,-6.70538686355678,
8.24103999376599));
#49779=CARTESIAN_POINT('Ctrl Pts',(1.11336305057795,-6.67478177303257,8.2497899723793));
#49780=CARTESIAN_POINT('Ctrl Pts',(1.29684337090462,-6.64417699581195,8.25853986141929));
#49781=CARTESIAN_POINT('Ctrl Pts',(1.47906091205535,-6.60600253547983,8.26728975045928));
#49782=CARTESIAN_POINT('Ctrl Pts',(1.65939671095571,-6.56038806441123,8.27603963949926));
#49783=CARTESIAN_POINT('Ctrl Pts',(1.83973072369515,-6.51477404513749,8.28478944187476));
#49784=CARTESIAN_POINT('Ctrl Pts',(2.01818275357394,-6.46172023288549,8.29353924425025));
#49785=CARTESIAN_POINT('Ctrl Pts',(2.19414664033687,-6.40140683917984,8.30228904662575));
#49786=CARTESIAN_POINT('Ctrl Pts',(2.37010884271615,-6.34109402281364,8.31103876524528));
#49787=CARTESIAN_POINT('Ctrl Pts',(2.54358267848155,-6.2735218569965,8.31978848386482));
#49788=CARTESIAN_POINT('Ctrl Pts',(2.71397890842085,-6.19891986435111,8.32853820248435));
#49789=CARTESIAN_POINT('Ctrl Pts',(2.88437356389273,-6.12431856103087,8.33728784025617));
#49790=CARTESIAN_POINT('Ctrl Pts',(3.05169040787491,-6.04268767582396,8.34603747802799));
#49791=CARTESIAN_POINT('Ctrl Pts',(3.2153611251236,-5.9543044795378,8.35478711579981));
#49792=CARTESIAN_POINT('Ctrl Pts',(3.37903038443137,-5.86592207054873,8.36353667563187));
#49793=CARTESIAN_POINT('Ctrl Pts',(3.53905332980255,-5.77078760703204,8.37228623546392));
#49794=CARTESIAN_POINT('Ctrl Pts',(3.69488643042162,-5.66922422085123,8.38103579529599));
#49795=CARTESIAN_POINT('Ctrl Pts',(3.85071819469011,-5.56766170562973,8.38978528009599));
#49796=CARTESIAN_POINT('Ctrl Pts',(4.00235994599491,-5.45967053456056,8.39853476489598));
#49797=CARTESIAN_POINT('Ctrl Pts',(4.14929662974566,-5.34561750206479,8.40728424969598));
#49798=CARTESIAN_POINT('Ctrl Pts',(4.29623210225307,-5.23156540974251,8.41603366237134));
#49799=CARTESIAN_POINT('Ctrl Pts',(4.43846235842376,-5.11145173171961,8.42478307504672));
#49800=CARTESIAN_POINT('Ctrl Pts',(4.57550431797684,-4.98568443006327,8.43353248772208));
#49801=CARTESIAN_POINT('Ctrl Pts',(4.71254519337745,-4.85991812336446,8.44228183117997));
#49802=CARTESIAN_POINT('Ctrl Pts',(4.84439764315229,-4.72849847630849,8.45103117463786));
#49803=CARTESIAN_POINT('Ctrl Pts',(4.97061384196926,-4.59187184425084,8.45978051809576));
#49804=CARTESIAN_POINT('Ctrl Pts',(5.0968290842045,-4.4552462476747,8.46852979524312));
#49805=CARTESIAN_POINT('Ctrl Pts',(5.21740796650416,-4.31341395556596,8.47727907239049));
#49806=CARTESIAN_POINT('Ctrl Pts',(5.33194095942497,-4.16685668162541,8.48602834953786));
#49807=CARTESIAN_POINT('Ctrl Pts',(5.44647312235371,-4.02030046974891,8.4947775632814));
#49808=CARTESIAN_POINT('Ctrl Pts',(5.55495930712519,-3.86901957035216,8.50352677702493));
#49809=CARTESIAN_POINT('Ctrl Pts',(5.65703106080017,-3.71352778058036,8.51227599076847));
#49810=CARTESIAN_POINT('Ctrl Pts',(5.7591021086894,-3.55803706597272,8.52102514401466));
#49811=CARTESIAN_POINT('Ctrl Pts',(5.85475865698736,-3.39833575880577,8.52977429726085));
#49812=CARTESIAN_POINT('Ctrl Pts',(5.94367583069233,-3.23496624706408,8.53852345050704));
#49813=CARTESIAN_POINT('Ctrl Pts',(6.03259241910241,-3.07159781069779,8.54727254616217));
#49814=CARTESIAN_POINT('Ctrl Pts',(6.11476958471124,-2.90456146975505,8.55602164181729));
#49815=CARTESIAN_POINT('Ctrl Pts',(6.18992823574535,-2.7344245164792,8.56477073747241));
#49816=CARTESIAN_POINT('Ctrl Pts',(6.26508641701077,-2.56428862662069,8.57351977844253));
#49817=CARTESIAN_POINT('Ctrl Pts',(6.33322605570432,-2.3910524253092,8.58226881941264));
#49818=CARTESIAN_POINT('Ctrl Pts',(6.39411573747894,-2.21530425353361,8.59101786038276));
#49819=CARTESIAN_POINT('Ctrl Pts',(6.45500505889243,-2.03955712188191,8.59976684957376));
#49820=CARTESIAN_POINT('Ctrl Pts',(6.50864441545036,-1.86129832025199,8.60851583876477));
#49821=CARTESIAN_POINT('Ctrl Pts',(6.55485164050003,-1.68113324011933,8.61726482795576));
#49822=CARTESIAN_POINT('Ctrl Pts',(6.60199852639196,-1.4973043591252,8.62619173483265));
#49823=CARTESIAN_POINT('Ctrl Pts',(6.64140767441085,-1.31149113173271,8.63511864170954));
#49824=CARTESIAN_POINT('Ctrl Pts',(6.67293975269667,-1.1243505044605,8.64404554858642));
#49825=CARTESIAN_POINT('Ctrl Pts',(6.7038466483156,-0.94092029155993,8.65279546277041));
#49826=CARTESIAN_POINT('Ctrl Pts',(6.72718585889709,-0.756215114274129,
8.6615453769544));
#49827=CARTESIAN_POINT('Ctrl Pts',(6.74287810451896,-0.570862389371339,
8.67029529113839));
#49828=CARTESIAN_POINT('Ctrl Pts',(6.75857004154145,-0.385513309564348,
8.67904503324897));
#49829=CARTESIAN_POINT('Ctrl Pts',(6.76661529035567,-0.199516993255511,
8.68779477535956));
#49830=CARTESIAN_POINT('Ctrl Pts',(6.76698652348897,-0.0135052182014118,
8.69654451747014));
#49831=CARTESIAN_POINT('Ctrl Pts',(6.76735774981515,0.17250314604149,8.70529409914078));
#49832=CARTESIAN_POINT('Ctrl Pts',(6.76005524147466,0.358526681836017,8.71404368081143));
#49833=CARTESIAN_POINT('Ctrl Pts',(6.74510380214861,0.543933542117359,8.72279326248207));
#49834=CARTESIAN_POINT('Ctrl Pts',(6.73015261710952,0.729337249087202,8.731542695344));
#49835=CARTESIAN_POINT('Ctrl Pts',(6.70755278444572,0.914124015857128,8.74029212820592));
#49836=CARTESIAN_POINT('Ctrl Pts',(6.67738106408249,1.0976662174963,8.74904156106784));
#49837=CARTESIAN_POINT('Ctrl Pts',(6.64720981677208,1.28120554143558,8.75779085675019));
#49838=CARTESIAN_POINT('Ctrl Pts',(6.60946696581472,1.46350005650848,8.76654015243254));
#49839=CARTESIAN_POINT('Ctrl Pts',(6.56428070010939,1.64393062206754,8.77528944811489));
#49840=CARTESIAN_POINT('Ctrl Pts',(6.51909508282681,1.82435859844867,8.78403861824488));
#49841=CARTESIAN_POINT('Ctrl Pts',(6.46646633415597,2.00292240086772,8.79278778837485));
#49842=CARTESIAN_POINT('Ctrl Pts',(6.40657319597123,2.17901557696657,8.80153695850484));
#49843=CARTESIAN_POINT('Ctrl Pts',(6.34668083768224,2.35510646007624,8.81028601470791));
#49844=CARTESIAN_POINT('Ctrl Pts',(6.27952437143814,2.52872650996707,8.81903507091099));
#49845=CARTESIAN_POINT('Ctrl Pts',(6.20533187335065,2.69928607998089,8.82778412711406));
#49846=CARTESIAN_POINT('Ctrl Pts',(6.1283144978418,2.87633970115551,8.8368663034029));
#49847=CARTESIAN_POINT('Ctrl Pts',(6.0437148946308,3.05009490562493,8.84594847969175));
#49848=CARTESIAN_POINT('Ctrl Pts',(5.95184265120418,3.21991584599766,8.85503065598058));
#49849=CARTESIAN_POINT('Ctrl Pts',(5.86333281335415,3.38352155905435,8.863780436335));
#49850=CARTESIAN_POINT('Ctrl Pts',(5.76807337235603,3.54347560903958,8.87253021668942));
#49851=CARTESIAN_POINT('Ctrl Pts',(5.66638790086269,3.6992346717878,8.88127999704383));
#49852=CARTESIAN_POINT('Ctrl Pts',(5.56470608502652,3.85498813489894,8.8900294628381));
#49853=CARTESIAN_POINT('Ctrl Pts',(5.45659885766858,4.00654667256389,8.89877892863237));
#49854=CARTESIAN_POINT('Ctrl Pts',(5.3424334058041,4.15339551506336,8.90752839442663));
#49855=CARTESIAN_POINT('Ctrl Pts',(5.22827145140486,4.30023985884002,8.91627759218051));
#49856=CARTESIAN_POINT('Ctrl Pts',(5.10805181977971,4.4423745699318,8.92502678993438));
#49857=CARTESIAN_POINT('Ctrl Pts',(4.98218281282421,4.5793169162659,8.93377598768825));
#49858=CARTESIAN_POINT('Ctrl Pts',(4.85631699296106,4.71625579512287,8.94252496390624));
#49859=CARTESIAN_POINT('Ctrl Pts',(4.72480227791723,4.84800236135881,8.95127394012425));
#49860=CARTESIAN_POINT('Ctrl Pts',(4.58808530848008,4.97410918679006,8.96002291634224));
#49861=CARTESIAN_POINT('Ctrl Pts',(4.4513594505686,5.10022421089105,8.96877246136344));
#49862=CARTESIAN_POINT('Ctrl Pts',(4.30943087207926,5.22069856612081,8.97752200638464));
#49863=CARTESIAN_POINT('Ctrl Pts',(4.16278164322349,5.33512305301776,8.98627155140584));
#49864=CARTESIAN_POINT('Ctrl Pts',(4.01614103534265,5.4495408133152,8.9950205820731));
#49865=CARTESIAN_POINT('Ctrl Pts',(3.8647805583328,5.5579092406843,9.00376961274037));
#49866=CARTESIAN_POINT('Ctrl Pts',(3.70921425811811,5.65986029751383,9.01251864340763));
#49867=CARTESIAN_POINT('Ctrl Pts',(3.55364584529979,5.76181273884741,9.02126779288748));
#49868=CARTESIAN_POINT('Ctrl Pts',(3.39387173464203,5.85734747818145,9.03001694236732));
#49869=CARTESIAN_POINT('Ctrl Pts',(3.23043456092263,5.94614005448885,9.03876609184717));
#49870=CARTESIAN_POINT('Ctrl Pts',(3.186907688063,5.9697874481133,9.04109618058018));
#49871=CARTESIAN_POINT('Ctrl Pts',(3.1431211498284,5.99295688499322,9.04342626931319));
#49872=CARTESIAN_POINT('Ctrl Pts',(3.09908550384729,6.01564277861008,9.04575635804621));
#49873=CARTESIAN_POINT('Ctrl Pts',(3.09908550384722,6.01564277861012,7.04591868117257));
#49874=CARTESIAN_POINT('Ctrl Pts',(2.93604628566889,6.09963587730468,7.05454905880241));
#49875=CARTESIAN_POINT('Ctrl Pts',(2.76950740353687,6.17703973348651,7.06317943643227));
#49876=CARTESIAN_POINT('Ctrl Pts',(2.60001743979206,6.24757539472531,7.07180981406212));
#49877=CARTESIAN_POINT('Ctrl Pts',(2.43064033119356,6.3180640896884,7.08043444514209));
#49878=CARTESIAN_POINT('Ctrl Pts',(2.25831633964846,6.38169359341765,7.08905907622205));
#49879=CARTESIAN_POINT('Ctrl Pts',(2.08361602112917,6.43823215459756,7.09768370730202));
#49880=CARTESIAN_POINT('Ctrl Pts',(1.90904874164956,6.4947276601268,7.10630177049108));
#49881=CARTESIAN_POINT('Ctrl Pts',(1.73210903495208,6.54414290516573,7.11491983368014));
#49882=CARTESIAN_POINT('Ctrl Pts',(1.55338505763979,6.58629515453881,7.12353789686919));
#49883=CARTESIAN_POINT('Ctrl Pts',(1.49727832789166,6.59952798932359,7.1262433611811));
#49884=CARTESIAN_POINT('Ctrl Pts',(1.44099587813452,6.61204540909544,7.12894882549301));
#49885=CARTESIAN_POINT('Ctrl Pts',(1.38455622043201,6.62384277232356,7.13165428980491));
#49886=CARTESIAN_POINT('Ctrl Pts',(1.20878280736886,6.66058400861317,7.14008007967293));
#49887=CARTESIAN_POINT('Ctrl Pts',(1.0315604014241,6.69032138189369,7.14850586954092));
#49888=CARTESIAN_POINT('Ctrl Pts',(0.85347220600288,6.71296314555507,7.15693165940894));
#49889=CARTESIAN_POINT('Ctrl Pts',(0.675342688121898,6.73561016286825,7.16535940434401));
#49890=CARTESIAN_POINT('Ctrl Pts',(0.496347309072643,6.75115824602896,7.17378714927912));
#49891=CARTESIAN_POINT('Ctrl Pts',(0.317074893630531,6.75956747964167,7.18221489421418));
#49892=CARTESIAN_POINT('Ctrl Pts',(0.137736604564098,6.76797980322611,7.19064573592297));
#49893=CARTESIAN_POINT('Ctrl Pts',(-0.0418785928876334,6.76924803137516,
7.19907657763173));
#49894=CARTESIAN_POINT('Ctrl Pts',(-0.22118097478846,6.76338435817392,7.20750741934052));
#49895=CARTESIAN_POINT('Ctrl Pts',(-0.400648112698848,6.75751529700522,
7.21594600791703));
#49896=CARTESIAN_POINT('Ctrl Pts',(-0.579801529226361,6.74450125243955,
7.22438459649354));
#49897=CARTESIAN_POINT('Ctrl Pts',(-0.758054598562708,6.72440645898193,
7.23282318507006));
#49898=CARTESIAN_POINT('Ctrl Pts',(-0.936401135934701,6.70430112870226,
7.24126619846967));
#49899=CARTESIAN_POINT('Ctrl Pts',(-1.1138460564091,6.67710768954954,7.2497092118693));
#49900=CARTESIAN_POINT('Ctrl Pts',(-1.28981146573857,6.64294177174912,7.25815222526892));
#49901=CARTESIAN_POINT('Ctrl Pts',(-1.46596173899787,6.6087399602702,7.2666041086427));
#49902=CARTESIAN_POINT('Ctrl Pts',(-1.64062907266469,6.56755110853779,7.27505599201648));
#49903=CARTESIAN_POINT('Ctrl Pts',(-1.81324825739576,6.51954137628187,7.28350787539027));
#49904=CARTESIAN_POINT('Ctrl Pts',(-1.8602924362528,6.50645720817712,7.28581128050561));
#49905=CARTESIAN_POINT('Ctrl Pts',(-1.90718459024933,6.49286671192376,7.28811468562096));
#49906=CARTESIAN_POINT('Ctrl Pts',(-1.95391351250368,6.47877387980593,7.2904180907363));
#49907=CARTESIAN_POINT('Ctrl Pts',(-2.12264494513047,6.42788668535989,7.29873535606751));
#49908=CARTESIAN_POINT('Ctrl Pts',(-2.28955019583296,6.37035459592245,7.30705262139872));
#49909=CARTESIAN_POINT('Ctrl Pts',(-2.45407839486155,6.30632922006723,7.31536988672994));
#49910=CARTESIAN_POINT('Ctrl Pts',(-2.61846782701356,6.24235784469024,7.3236801370878));
#49911=CARTESIAN_POINT('Ctrl Pts',(-2.78048387941258,6.17190421984677,7.33199038744566));
#49912=CARTESIAN_POINT('Ctrl Pts',(-2.9395911052866,6.09516965586028,7.34030063780352));
#49913=CARTESIAN_POINT('Ctrl Pts',(-3.09859327511113,6.01848575852396,7.34860540103113));
#49914=CARTESIAN_POINT('Ctrl Pts',(-3.25469013329891,5.93552933645976,7.35691016425877));
#49915=CARTESIAN_POINT('Ctrl Pts',(-3.40736627027555,5.84654976034486,7.36521492748638));
#49916=CARTESIAN_POINT('Ctrl Pts',(-3.55996954589234,5.75761264779396,7.37351572744668));
#49917=CARTESIAN_POINT('Ctrl Pts',(-3.70915505374586,5.66265828441473,7.38181652740696));
#49918=CARTESIAN_POINT('Ctrl Pts',(-3.85443185757403,5.56198202579965,7.39011732736726));
#49919=CARTESIAN_POINT('Ctrl Pts',(-3.9996659160247,5.46133538956451,7.39841568494986));
#49920=CARTESIAN_POINT('Ctrl Pts',(-4.14099327733758,5.35497041184807,7.40671404253244));
#49921=CARTESIAN_POINT('Ctrl Pts',(-4.27795169579387,5.24322594291476,7.41501240011503));
#49922=CARTESIAN_POINT('Ctrl Pts',(-4.41492404945482,5.13147010423828,7.42331160203646));
#49923=CARTESIAN_POINT('Ctrl Pts',(-4.54752629780061,5.01433389473508,7.4316108039579));
#49924=CARTESIAN_POINT('Ctrl Pts',(-4.67532857434755,4.89219702402605,7.43991000587933));
#49925=CARTESIAN_POINT('Ctrl Pts',(-4.80314380762242,4.77004777095384,7.44821004918249));
#49926=CARTESIAN_POINT('Ctrl Pts',(-4.92615784717814,4.64289708623193,7.45651009248565));
#49927=CARTESIAN_POINT('Ctrl Pts',(-5.04397713955261,4.51116211365438,7.46481013578881));
#49928=CARTESIAN_POINT('Ctrl Pts',(-5.16182793482981,4.37939191735462,7.47311239838434));
#49929=CARTESIAN_POINT('Ctrl Pts',(-5.27448098258482,4.24303524948044,7.48141466097987));
#49930=CARTESIAN_POINT('Ctrl Pts',(-5.38158240991591,4.10254308512216,7.4897169235754));
#49931=CARTESIAN_POINT('Ctrl Pts',(-5.48873025557395,3.96199003071432,7.4980227844156));
#49932=CARTESIAN_POINT('Ctrl Pts',(-5.59032147462727,3.81729818415243,7.50632864525581));
#49933=CARTESIAN_POINT('Ctrl Pts',(-5.68604487717728,3.66894843991109,7.514634506096));
#49934=CARTESIAN_POINT('Ctrl Pts',(-5.78188143154271,3.52042333580549,7.52295018504972));
#49935=CARTESIAN_POINT('Ctrl Pts',(-5.87183612232255,3.36823198765155,7.53126586400344));
#49936=CARTESIAN_POINT('Ctrl Pts',(-5.95564260041542,3.21288191754958,7.53958154295715));
#49937=CARTESIAN_POINT('Ctrl Pts',(-6.03950208543819,3.05743358976558,7.54790248151157));
#49938=CARTESIAN_POINT('Ctrl Pts',(-6.11720544988682,2.89882286774888,7.55622342006601));
#49939=CARTESIAN_POINT('Ctrl Pts',(-6.18853402279732,2.7375784278592,7.56454435862044));
#49940=CARTESIAN_POINT('Ctrl Pts',(-6.2599686120612,2.57609432878636,7.57287766466697));
#49941=CARTESIAN_POINT('Ctrl Pts',(-6.32500934646575,2.41196901207523,7.58121097071347));
#49942=CARTESIAN_POINT('Ctrl Pts',(-6.38348661080446,2.24574880378019,7.58954427675999));
#49943=CARTESIAN_POINT('Ctrl Pts',(-6.42652933007401,2.12340091621269,7.59567808203977));
#49944=CARTESIAN_POINT('Ctrl Pts',(-6.46601711060719,1.99991839314941,7.60181188731956));
#49945=CARTESIAN_POINT('Ctrl Pts',(-6.50189998196639,1.87552276032725,7.60794569259934));
#49946=CARTESIAN_POINT('Ctrl Pts',(-6.55964575326826,1.67533471818333,7.61781673422672));
#49947=CARTESIAN_POINT('Ctrl Pts',(-6.60820101134001,1.47227423754519,7.62768777585408));
#49948=CARTESIAN_POINT('Ctrl Pts',(-6.64730986736617,1.26710714906689,7.63755881748146));
#49949=CARTESIAN_POINT('Ctrl Pts',(-6.68667936649135,1.06057271336363,7.64749564520288));
#49950=CARTESIAN_POINT('Ctrl Pts',(-6.71647593457217,0.851903446939668,
7.65743247292432));
#49951=CARTESIAN_POINT('Ctrl Pts',(-6.7364861811604,0.641905702603612,7.66736930064573));
#49952=CARTESIAN_POINT('Ctrl Pts',(-6.75649642774862,0.431907958267619,
7.67730612836714));
#49953=CARTESIAN_POINT('Ctrl Pts',(-6.7667201599113,0.22058172300754,7.68724295608853));
#49954=CARTESIAN_POINT('Ctrl Pts',(-6.76699433154345,0.00875881606655957,
7.69717978380994));
#49955=CARTESIAN_POINT('',(-6.767,2.34075020651148E-12,7.30282021618984));
#49956=CARTESIAN_POINT('Ctrl Pts',(3.09908550384729,6.01564277861008,6.6512241499329));
#49957=CARTESIAN_POINT('Ctrl Pts',(2.94401248051215,6.09553192368441,6.65944950834));
#49958=CARTESIAN_POINT('Ctrl Pts',(2.78601358709771,6.1693358723004,6.66767486674707));
#49959=CARTESIAN_POINT('Ctrl Pts',(2.62561376615818,6.23686149845904,6.67590022515418));
#49960=CARTESIAN_POINT('Ctrl Pts',(2.59378762865569,6.25025976692641,6.67753228051521));
#49961=CARTESIAN_POINT('Ctrl Pts',(2.561867014533,6.26341101841259,6.67916433587622));
#49962=CARTESIAN_POINT('Ctrl Pts',(2.52985608944668,6.27631397929466,6.68079639123724));
#49963=CARTESIAN_POINT('Ctrl Pts',(2.3546024939825,6.34695518321549,6.68973157724778));
#49964=CARTESIAN_POINT('Ctrl Pts',(2.17627719690743,6.41029683020603,6.69866676325832));
#49965=CARTESIAN_POINT('Ctrl Pts',(1.99548470311922,6.46609076642272,6.70760194926886));
#49966=CARTESIAN_POINT('Ctrl Pts',(1.81496298050897,6.52180114059812,6.71652375313731));
#49967=CARTESIAN_POINT('Ctrl Pts',(1.6319816804589,6.56998628365692,6.72544555700577));
#49968=CARTESIAN_POINT('Ctrl Pts',(1.44716308657288,6.61044688359727,6.73436736087422));
#49969=CARTESIAN_POINT('Ctrl Pts',(1.26279530875128,6.65080879060827,6.74326740236247));
#49970=CARTESIAN_POINT('Ctrl Pts',(1.07659943348155,6.68348370473627,6.7521674438507));
#49971=CARTESIAN_POINT('Ctrl Pts',(0.889210020969436,6.70832278133719,6.76106748533896));
#49972=CARTESIAN_POINT('Ctrl Pts',(0.702109096946915,6.73312361784976,6.76995382509512));
#49973=CARTESIAN_POINT('Ctrl Pts',(0.513818555767998,6.75011264636526,6.77884016485127));
#49974=CARTESIAN_POINT('Ctrl Pts',(0.324983139942513,6.7591918865167,6.78772650460743));
#49975=CARTESIAN_POINT('Ctrl Pts',(0.136630542694427,6.76824791266564,6.79659012357311));
#49976=CARTESIAN_POINT('Ctrl Pts',(-0.0522638920024719,6.76943449366325,
6.8054537425388));
#49977=CARTESIAN_POINT('Ctrl Pts',(-0.241051065202706,6.76270533026278,
6.81431736150448));
#49978=CARTESIAN_POINT('Ctrl Pts',(-0.420267653187079,6.75631730249491,
6.82273163839255));
#49979=CARTESIAN_POINT('Ctrl Pts',(-0.599387323621606,6.7427961021518,6.8311459152806));
#49980=CARTESIAN_POINT('Ctrl Pts',(-0.777850164000041,6.72214535117808,
6.83956019216866));
#49981=CARTESIAN_POINT('Ctrl Pts',(-0.951985658663627,6.70199533715636,
6.84777044067212));
#49982=CARTESIAN_POINT('Ctrl Pts',(-1.12532831860155,6.67507568806264,6.85598068917558));
#49983=CARTESIAN_POINT('Ctrl Pts',(-1.29732118457894,6.64147925872262,6.86419093767904));
#49984=CARTESIAN_POINT('Ctrl Pts',(-1.46935493677815,6.60787484282423,6.87240313792648));
#49985=CARTESIAN_POINT('Ctrl Pts',(-1.64003790639215,6.56759055274846,6.88061533817391));
#49986=CARTESIAN_POINT('Ctrl Pts',(-1.80882432295702,6.52077016683452,6.88882753842135));
#49987=CARTESIAN_POINT('Ctrl Pts',(-1.97768091962694,6.47393031336111,6.89704315323904));
#49988=CARTESIAN_POINT('Ctrl Pts',(-2.14463904952465,6.42054904494424,6.90525876805674));
#49989=CARTESIAN_POINT('Ctrl Pts',(-2.30916898549506,6.36081972676696,6.91347438287443));
#49990=CARTESIAN_POINT('Ctrl Pts',(-2.47388368145781,6.30102333515224,6.92169922347173));
#49991=CARTESIAN_POINT('Ctrl Pts',(-2.63616440256881,6.23486477719519,6.92992406406903));
#49992=CARTESIAN_POINT('Ctrl Pts',(-2.7955013607369,6.16258558902983,6.93814890466633));
#49993=CARTESIAN_POINT('Ctrl Pts',(-2.95494037981667,6.09026010350871,6.94637901356259));
#49994=CARTESIAN_POINT('Ctrl Pts',(-3.11143155976109,6.01180633160917,6.95460912245886));
#49995=CARTESIAN_POINT('Ctrl Pts',(-3.26449059105997,5.92751129740644,6.96283923135512));
#49996=CARTESIAN_POINT('Ctrl Pts',(-3.41775946867916,5.84310069339644,6.9710806238591));
#49997=CARTESIAN_POINT('Ctrl Pts',(-3.56758649486585,5.75283301417291,6.97932201636308));
#49998=CARTESIAN_POINT('Ctrl Pts',(-3.71351632142453,5.65703858308511,6.98756340886706));
#49999=CARTESIAN_POINT('Ctrl Pts',(-3.77702865424248,5.61534643602491,6.99115027027805));
#50000=CARTESIAN_POINT('Ctrl Pts',(-3.83980319701256,5.57260792544221,6.99473713168906));
#50001=CARTESIAN_POINT('Ctrl Pts',(-3.90180444088853,5.52885260294237,6.99832399310006));
#50002=CARTESIAN_POINT('Ctrl Pts',(-4.04691716796378,5.42644410635298,7.00671897372387));
#50003=CARTESIAN_POINT('Ctrl Pts',(-4.18813387617185,5.31822146221833,7.01511395434766));
#50004=CARTESIAN_POINT('Ctrl Pts',(-4.32497312565706,5.20450732176872,7.02350893497146));
#50005=CARTESIAN_POINT('Ctrl Pts',(-4.46168406247309,5.09089980982621,7.03189604371365));
#50006=CARTESIAN_POINT('Ctrl Pts',(-4.59402546078445,4.97181127976229,7.04028315245586));
#50007=CARTESIAN_POINT('Ctrl Pts',(-4.72154622672205,4.84760664956706,7.04867026119805));
#50008=CARTESIAN_POINT('Ctrl Pts',(-4.84896882731571,4.72349763195816,7.05705091355325));
#50009=CARTESIAN_POINT('Ctrl Pts',(-4.97157794932228,4.59428060019929,7.06543156590843));
#50010=CARTESIAN_POINT('Ctrl Pts',(-5.08895663059961,4.4603597850259,7.07381221826363));
#50011=CARTESIAN_POINT('Ctrl Pts',(-5.20626464185742,4.32651959937159,7.08218782489111));
#50012=CARTESIAN_POINT('Ctrl Pts',(-5.31834826629925,4.18798153057609,7.09056343151859));
#50013=CARTESIAN_POINT('Ctrl Pts',(-5.42482816582768,4.04518582654032,7.09893903814607));
#50014=CARTESIAN_POINT('Ctrl Pts',(-5.53282654890704,3.90035374823408,7.10743408723123));
#50015=CARTESIAN_POINT('Ctrl Pts',(-5.63505990996985,3.75114192589885,7.11592913631642));
#50016=CARTESIAN_POINT('Ctrl Pts',(-5.73117487541204,3.59804440598581,7.12442418540158));
#50017=CARTESIAN_POINT('Ctrl Pts',(-5.82588046173029,3.44719182730019,7.13279466757062));
#50018=CARTESIAN_POINT('Ctrl Pts',(-5.91464568360222,3.29256703035907,7.14116514973963));
#50019=CARTESIAN_POINT('Ctrl Pts',(-5.99717618495803,3.13467172229762,7.14953563190868));
#50020=CARTESIAN_POINT('Ctrl Pts',(-6.07970145403767,2.97678642449714,7.15790558340514));
#50021=CARTESIAN_POINT('Ctrl Pts',(-6.15599263309959,2.81563133004938,7.1662755349016));
#50022=CARTESIAN_POINT('Ctrl Pts',(-6.22580144058283,2.65173253222055,7.17464548639806));
#50023=CARTESIAN_POINT('Ctrl Pts',(-6.29561644392233,2.48781918761132,7.18301618076664));
#50024=CARTESIAN_POINT('Ctrl Pts',(-6.35894779614614,2.32116196708482,7.19138687513521));
#50025=CARTESIAN_POINT('Ctrl Pts',(-6.41559534740355,2.15230698051507,7.19975756950379));
#50026=CARTESIAN_POINT('Ctrl Pts',(-6.47371723375101,1.9790572967995,7.2083461233943));
#50027=CARTESIAN_POINT('Ctrl Pts',(-6.5248025468967,1.80349424587402,7.2169346772848));
#50028=CARTESIAN_POINT('Ctrl Pts',(-6.56868967529199,1.62622413882972,7.2255232311753));
#50029=CARTESIAN_POINT('Ctrl Pts',(-6.61150605251964,1.45327903961906,7.23390224289609));
#50030=CARTESIAN_POINT('Ctrl Pts',(-6.64747135569544,1.27870955593672,7.24228125461689));
#50031=CARTESIAN_POINT('Ctrl Pts',(-6.67648739447263,1.10308887740201,7.25066026633768));
#50032=CARTESIAN_POINT('Ctrl Pts',(-6.70659188208925,0.920880320859626,
7.25935359131304));
#50033=CARTESIAN_POINT('Ctrl Pts',(-6.72921558440873,0.737540577943572,
7.2680469162884));
#50034=CARTESIAN_POINT('Ctrl Pts',(-6.74430784407182,0.553715364055754,
7.27674024126377));
#50035=CARTESIAN_POINT('Ctrl Pts',(-6.7594001037349,0.369890150168001,7.28543356623913));
#50036=CARTESIAN_POINT('Ctrl Pts',(-6.76696093792726,0.185579872223753,
7.2941268912145));
#50037=CARTESIAN_POINT('Ctrl Pts',(-6.76699984893368,0.00142987115423253,
7.30282021618986));
#50038=CARTESIAN_POINT('Ctrl Pts',(-6.767,2.53308028912622E-12,7.30282021618984));
#50039=CARTESIAN_POINT('Ctrl Pts',(-6.76700000000007,-0.186007249557542,
7.31156972800259));
#50040=CARTESIAN_POINT('Ctrl Pts',(-6.7593263729426,-0.372014355813791,
7.32031923981533));
#50041=CARTESIAN_POINT('Ctrl Pts',(-6.74400518263381,-0.557389537584237,
7.32906875162807));
#50042=CARTESIAN_POINT('Ctrl Pts',(-6.72868405703753,-0.742763936380651,
7.33781822648527));
#50043=CARTESIAN_POINT('Ctrl Pts',(-6.70571545643593,-0.927506130402907,
7.34656770134246));
#50044=CARTESIAN_POINT('Ctrl Pts',(-6.6751773940161,-1.11098864009337,7.35531717619966));
#50045=CARTESIAN_POINT('Ctrl Pts',(-6.64463945804429,-1.29447039004339,
7.36406661482818));
#50046=CARTESIAN_POINT('Ctrl Pts',(-6.60653217002768,-1.47669218339082,
7.37281605345669));
#50047=CARTESIAN_POINT('Ctrl Pts',(-6.56098496085528,-1.65703510627594,
7.3815654920852));
#50048=CARTESIAN_POINT('Ctrl Pts',(-6.51543793649603,-1.83737729739843,
7.39031489521184));
#50049=CARTESIAN_POINT('Ctrl Pts',(-6.46245112156941,-2.01584035544809,
7.39906429833849));
#50050=CARTESIAN_POINT('Ctrl Pts',(-6.40220448361758,-2.19181813797288,
7.40781370146513));
#50051=CARTESIAN_POINT('Ctrl Pts',(-6.34195808512014,-2.36779522106193,
7.41656306981667));
#50052=CARTESIAN_POINT('Ctrl Pts',(-6.27445201416395,-2.54128677725644,
7.4253124381682));
#50053=CARTESIAN_POINT('Ctrl Pts',(-6.19991555052764,-2.71170355428568,
7.43406180651974));
#50054=CARTESIAN_POINT('Ctrl Pts',(-6.12537937695157,-2.88211966813438,
7.44281114082292));
#50055=CARTESIAN_POINT('Ctrl Pts',(-6.04381298028384,-3.04946076419803,
7.45156047512609));
#50056=CARTESIAN_POINT('Ctrl Pts',(-5.95549339308909,-3.21315848424447,
7.46030980942928));
#50057=CARTESIAN_POINT('Ctrl Pts',(-5.86717414225738,-3.37685558085204,
7.46905911041083));
#50058=CARTESIAN_POINT('Ctrl Pts',(-5.77210188843998,-3.5369090770011,7.47780841139239));
#50059=CARTESIAN_POINT('Ctrl Pts',(-5.67059953311307,-3.6927753702409,7.48655771237394));
#50060=CARTESIAN_POINT('Ctrl Pts',(-5.56909755592636,-3.84864108281131,
7.49530698076056));
#50061=CARTESIAN_POINT('Ctrl Pts',(-5.46116568154886,-4.00031938354938,
7.50405624914717));
#50062=CARTESIAN_POINT('Ctrl Pts',(-5.34717048488289,-4.14729511918278,
7.51280551753379));
#50063=CARTESIAN_POINT('Ctrl Pts',(-5.23317570343208,-4.29427031947298,
7.52155475405215));
#50064=CARTESIAN_POINT('Ctrl Pts',(-5.11311781951441,-4.43654276249679,
7.5303039905705));
#50065=CARTESIAN_POINT('Ctrl Pts',(-4.98740458929128,-4.5736292441251,7.53905322708886));
#50066=CARTESIAN_POINT('Ctrl Pts',(-4.861691806526,-4.71071523781413,7.54780243246559));
#50067=CARTESIAN_POINT('Ctrl Pts',(-4.73032391141408,-4.84261509584652,
7.55655163784232));
#50068=CARTESIAN_POINT('Ctrl Pts',(-4.59374706947136,-4.96888084599775,
7.56530084321905));
#50069=CARTESIAN_POINT('Ctrl Pts',(-4.45717070231348,-5.09514615720881,
7.57405001818074));
#50070=CARTESIAN_POINT('Ctrl Pts',(-4.31538563497237,-5.21577720520685,
7.58279919314242));
#50071=CARTESIAN_POINT('Ctrl Pts',(-4.16887340951951,-5.33036429293545,
7.59154836810411));
#50072=CARTESIAN_POINT('Ctrl Pts',(-4.02236168122442,-5.44495099183737,
7.60029751337736));
#50073=CARTESIAN_POINT('Ctrl Pts',(-3.87112305263152,-5.55349359497948,
7.6090466586506));
#50074=CARTESIAN_POINT('Ctrl Pts',(-3.71567116928981,-5.65562346357221,
7.61779580392384));
#50075=CARTESIAN_POINT('Ctrl Pts',(-3.56021980053318,-5.75775299408923,
7.6265449202352));
#50076=CARTESIAN_POINT('Ctrl Pts',(-3.40055544442113,-5.85346967519861,
7.63529403654655));
#50077=CARTESIAN_POINT('Ctrl Pts',(-3.23722035886896,-5.94244843041354,
7.6440431528579));
#50078=CARTESIAN_POINT('Ctrl Pts',(-3.07388580043524,-6.03142689847434,
7.65279224093393));
#50079=CARTESIAN_POINT('Ctrl Pts',(-2.90688078789238,-6.11366734707895,
7.66154132900996));
#50080=CARTESIAN_POINT('Ctrl Pts',(-2.73677250610388,-6.18889047001431,
7.67029041708598));
#50081=CARTESIAN_POINT('Ctrl Pts',(-2.5666647591693,-6.26411335643336,7.67903947765315));
#50082=CARTESIAN_POINT('Ctrl Pts',(-2.39345402457089,-6.33231884545257,
7.68778853822033));
#50083=CARTESIAN_POINT('Ctrl Pts',(-2.21772855944062,-6.39327529804884,
7.6965375987875));
#50084=CARTESIAN_POINT('Ctrl Pts',(-2.04200363223591,-6.45423156404703,
7.7052866325723));
#50085=CARTESIAN_POINT('Ctrl Pts',(-1.86376426061038,-6.50793874412452,
7.7140356663571));
#50086=CARTESIAN_POINT('Ctrl Pts',(-1.68361577621695,-6.5542144394331,7.7227847001419));
#50087=CARTESIAN_POINT('Ctrl Pts',(-1.50346782833202,-6.60048999692591,
7.73153370787081));
#50088=CARTESIAN_POINT('Ctrl Pts',(-1.32141105657353,-6.63933404265169,
7.74028271559971));
#50089=CARTESIAN_POINT('Ctrl Pts',(-1.1380637534648,-6.67061465631539,7.74903172332861));
#50090=CARTESIAN_POINT('Ctrl Pts',(-0.954716981169521,-6.70189517941778,
7.75778070572804));
#50091=CARTESIAN_POINT('Ctrl Pts',(-0.770079967441858,-6.72561226609009,
7.76652968812747));
#50092=CARTESIAN_POINT('Ctrl Pts',(-0.58477976407271,-6.74168536995988,
7.7752786705269));
#50093=CARTESIAN_POINT('Ctrl Pts',(-0.391489587592541,-6.75845153117875,
7.78440490094252));
#50094=CARTESIAN_POINT('Ctrl Pts',(-0.197478091804768,-6.76689985146396,
7.79353113135814));
#50095=CARTESIAN_POINT('Ctrl Pts',(-0.00346214753050771,-6.76699911434415,
7.80265736177375));
#50096=CARTESIAN_POINT('Ctrl Pts',(0.184490798485202,-6.76709527525933,
7.81149839748888));
#50097=CARTESIAN_POINT('Ctrl Pts',(0.372447602155378,-6.7593563379076,7.82033943320402));
#50098=CARTESIAN_POINT('Ctrl Pts',(0.559756448194851,-6.74380914014508,
7.82918046891915));
#50099=CARTESIAN_POINT('Ctrl Pts',(0.745136131043977,-6.72842206873148,
7.83793044753245));
#50100=CARTESIAN_POINT('Ctrl Pts',(0.92988085194565,-6.70538686355715,7.84668042614576));
#50101=CARTESIAN_POINT('Ctrl Pts',(1.11336305057522,-6.67478177303302,7.85543040475906));
#50102=CARTESIAN_POINT('Ctrl Pts',(1.2968433709019,-6.64417699581248,7.86418029379905));
#50103=CARTESIAN_POINT('Ctrl Pts',(1.47906091205264,-6.60600253548043,7.87293018283903));
#50104=CARTESIAN_POINT('Ctrl Pts',(1.65939671095303,-6.56038806441191,7.88168007187902));
#50105=CARTESIAN_POINT('Ctrl Pts',(1.83973072369242,-6.51477404513826,7.89042987425451));
#50106=CARTESIAN_POINT('Ctrl Pts',(2.01818275357117,-6.46172023288635,7.89917967663001));
#50107=CARTESIAN_POINT('Ctrl Pts',(2.19414664033407,-6.4014068391808,7.9079294790055));
#50108=CARTESIAN_POINT('Ctrl Pts',(2.37010884271337,-6.34109402281468,7.91667919762504));
#50109=CARTESIAN_POINT('Ctrl Pts',(2.54358267847881,-6.27352185699761,7.92542891624456));
#50110=CARTESIAN_POINT('Ctrl Pts',(2.71397890841814,-6.1989198643523,7.9341786348641));
#50111=CARTESIAN_POINT('Ctrl Pts',(2.88437356389017,-6.12431856103208,7.94292827263592));
#50112=CARTESIAN_POINT('Ctrl Pts',(3.0516904078725,-6.04268767582518,7.95167791040775));
#50113=CARTESIAN_POINT('Ctrl Pts',(3.21536112512134,-5.95430447953902,7.96042754817957));
#50114=CARTESIAN_POINT('Ctrl Pts',(3.37903038442914,-5.86592207055001,7.96917710801163));
#50115=CARTESIAN_POINT('Ctrl Pts',(3.53905332980035,-5.77078760703338,7.9779266678437));
#50116=CARTESIAN_POINT('Ctrl Pts',(3.69488643041946,-5.66922422085263,7.98667622767576));
#50117=CARTESIAN_POINT('Ctrl Pts',(3.85071819468793,-5.56766170563123,7.99542571247575));
#50118=CARTESIAN_POINT('Ctrl Pts',(4.00235994599273,-5.45967053456216,8.00417519727574));
#50119=CARTESIAN_POINT('Ctrl Pts',(4.14929662974347,-5.34561750206648,8.01292468207573));
#50120=CARTESIAN_POINT('Ctrl Pts',(4.29623210225092,-5.23156540974426,8.02167409475109));
#50121=CARTESIAN_POINT('Ctrl Pts',(4.43846235842167,-5.11145173172143,8.03042350742646));
#50122=CARTESIAN_POINT('Ctrl Pts',(4.5755043179748,-4.98568443006514,8.03917292010182));
#50123=CARTESIAN_POINT('Ctrl Pts',(4.71254519337551,-4.85991812336635,8.04792226355972));
#50124=CARTESIAN_POINT('Ctrl Pts',(4.84439764315045,-4.72849847631039,8.05667160701763));
#50125=CARTESIAN_POINT('Ctrl Pts',(4.97061384196751,-4.59187184425273,8.06542095047553));
#50126=CARTESIAN_POINT('Ctrl Pts',(5.09682908420275,-4.45524624767669,8.0741702276229));
#50127=CARTESIAN_POINT('Ctrl Pts',(5.21740796650244,-4.31341395556805,8.08291950477024));
#50128=CARTESIAN_POINT('Ctrl Pts',(5.33194095942327,-4.1668566816276,8.0916687819176));
#50129=CARTESIAN_POINT('Ctrl Pts',(5.44647312235203,-4.0203004697512,8.10041799566114));
#50130=CARTESIAN_POINT('Ctrl Pts',(5.55495930712353,-3.86901957035454,8.10916720940468));
#50131=CARTESIAN_POINT('Ctrl Pts',(5.65703106079855,-3.71352778058284,8.11791642314822));
#50132=CARTESIAN_POINT('Ctrl Pts',(5.75910210868784,-3.55803706597524,8.12666557639441));
#50133=CARTESIAN_POINT('Ctrl Pts',(5.85475865698587,-3.39833575880834,8.1354147296406));
#50134=CARTESIAN_POINT('Ctrl Pts',(5.94367583069091,-3.23496624706669,8.14416388288679));
#50135=CARTESIAN_POINT('Ctrl Pts',(6.03259241910106,-3.07159781070043,8.15291297854191));
#50136=CARTESIAN_POINT('Ctrl Pts',(6.11476958470997,-2.90456146975773,8.16166207419705));
#50137=CARTESIAN_POINT('Ctrl Pts',(6.18992823574415,-2.73442451648191,8.17041116985217));
#50138=CARTESIAN_POINT('Ctrl Pts',(6.2650864170096,-2.56428862662355,8.17916021082229));
#50139=CARTESIAN_POINT('Ctrl Pts',(6.33322605570318,-2.39105242531221,8.18790925179239));
#50140=CARTESIAN_POINT('Ctrl Pts',(6.39411573747785,-2.21530425353678,8.19665829276251));
#50141=CARTESIAN_POINT('Ctrl Pts',(6.4550050588915,-2.03955712188486,8.20540728195352));
#50142=CARTESIAN_POINT('Ctrl Pts',(6.50864441544959,-1.86129832025472,8.21415627114451));
#50143=CARTESIAN_POINT('Ctrl Pts',(6.55485164049939,-1.68113324012183,8.22290526033552));
#50144=CARTESIAN_POINT('Ctrl Pts',(6.6019985263914,-1.49730435912765,8.23183216721241));
#50145=CARTESIAN_POINT('Ctrl Pts',(6.64140767441038,-1.31149113173512,8.2407590740893));
#50146=CARTESIAN_POINT('Ctrl Pts',(6.67293975269627,-1.12435050446285,8.24968598096619));
#50147=CARTESIAN_POINT('Ctrl Pts',(6.70384664831528,-0.94092029156223,8.25843589515019));
#50148=CARTESIAN_POINT('Ctrl Pts',(6.72718585889684,-0.756215114276376,
8.26718580933418));
#50149=CARTESIAN_POINT('Ctrl Pts',(6.74287810451878,-0.570862389373527,
8.27593572351817));
#50150=CARTESIAN_POINT('Ctrl Pts',(6.75857004154132,-0.385513309566605,
8.28468546562875));
#50151=CARTESIAN_POINT('Ctrl Pts',(6.7666152903556,-0.199516993257833,8.29343520773934));
#50152=CARTESIAN_POINT('Ctrl Pts',(6.76698652348897,-0.0135052182037979,
8.30218494984992));
#50153=CARTESIAN_POINT('Ctrl Pts',(6.76735774981521,0.172503146039168,8.31093453152056));
#50154=CARTESIAN_POINT('Ctrl Pts',(6.76005524147478,0.358526681833763,8.3196841131912));
#50155=CARTESIAN_POINT('Ctrl Pts',(6.74510380214879,0.543933542115173,8.32843369486184));
#50156=CARTESIAN_POINT('Ctrl Pts',(6.73015261710976,0.729337249085021,8.33718312772377));
#50157=CARTESIAN_POINT('Ctrl Pts',(6.70755278444601,0.914124015854953,8.3459325605857));
#50158=CARTESIAN_POINT('Ctrl Pts',(6.67738106408284,1.09766621749414,8.35468199344763));
#50159=CARTESIAN_POINT('Ctrl Pts',(6.64720981677249,1.28120554143349,8.36343128912998));
#50160=CARTESIAN_POINT('Ctrl Pts',(6.60946696581517,1.46350005650646,8.37218058481233));
#50161=CARTESIAN_POINT('Ctrl Pts',(6.56428070010988,1.6439306220656,8.38092988049468));
#50162=CARTESIAN_POINT('Ctrl Pts',(6.51909508282735,1.82435859844674,8.38967905062466));
#50163=CARTESIAN_POINT('Ctrl Pts',(6.46646633415656,2.00292240086581,8.39842822075465));
#50164=CARTESIAN_POINT('Ctrl Pts',(6.40657319597188,2.17901557696468,8.40717739088464));
#50165=CARTESIAN_POINT('Ctrl Pts',(6.34668083768289,2.35510646007448,8.41592644708772));
#50166=CARTESIAN_POINT('Ctrl Pts',(6.27952437143879,2.52872650996545,8.42467550329079));
#50167=CARTESIAN_POINT('Ctrl Pts',(6.20533187335129,2.6992860799794,8.43342455949387));
#50168=CARTESIAN_POINT('Ctrl Pts',(6.12831449784246,2.8763397011541,8.44250673578271));
#50169=CARTESIAN_POINT('Ctrl Pts',(6.04371489463147,3.0500949056236,8.45158891207156));
#50170=CARTESIAN_POINT('Ctrl Pts',(5.95184265120486,3.21991584599641,8.4606710883604));
#50171=CARTESIAN_POINT('Ctrl Pts',(5.86333281335483,3.38352155905317,8.46942086871482));
#50172=CARTESIAN_POINT('Ctrl Pts',(5.76807337235671,3.54347560903848,8.47817064906924));
#50173=CARTESIAN_POINT('Ctrl Pts',(5.66638790086336,3.69923467178677,8.48692042942366));
#50174=CARTESIAN_POINT('Ctrl Pts',(5.56470608502723,3.85498813489793,8.49566989521793));
#50175=CARTESIAN_POINT('Ctrl Pts',(5.45659885766931,4.0065466725629,8.5044193610122));
#50176=CARTESIAN_POINT('Ctrl Pts',(5.34243340580486,4.15339551506239,8.51316882680646));
#50177=CARTESIAN_POINT('Ctrl Pts',(5.22827145140568,4.30023985883902,8.52191802456033));
#50178=CARTESIAN_POINT('Ctrl Pts',(5.1080518197806,4.44237456993077,8.53066722231419));
#50179=CARTESIAN_POINT('Ctrl Pts',(4.98218281282518,4.57931691626485,8.53941642006806));
#50180=CARTESIAN_POINT('Ctrl Pts',(4.85631699296184,4.71625579512209,8.54816539628607));
#50181=CARTESIAN_POINT('Ctrl Pts',(4.7248022779178,4.84800236135827,8.55691437250409));
#50182=CARTESIAN_POINT('Ctrl Pts',(4.58808530848042,4.97410918678974,8.5656633487221));
#50183=CARTESIAN_POINT('Ctrl Pts',(4.45135945056895,5.10022421089074,8.5744128937433));
#50184=CARTESIAN_POINT('Ctrl Pts',(4.30943087207962,5.22069856612051,8.58316243876449));
#50185=CARTESIAN_POINT('Ctrl Pts',(4.16278164322386,5.33512305301747,8.59191198378569));
#50186=CARTESIAN_POINT('Ctrl Pts',(4.01614103534297,5.44954081331496,8.60066101445296));
#50187=CARTESIAN_POINT('Ctrl Pts',(3.86478055833308,5.55790924068411,8.60941004512022));
#50188=CARTESIAN_POINT('Ctrl Pts',(3.70921425811833,5.65986029751368,8.61815907578749));
#50189=CARTESIAN_POINT('Ctrl Pts',(3.55364584530002,5.76181273884727,8.62690822526733));
#50190=CARTESIAN_POINT('Ctrl Pts',(3.39387173464226,5.85734747818132,8.63565737474718));
#50191=CARTESIAN_POINT('Ctrl Pts',(3.23043456092287,5.94614005448872,8.64440652422702));
#50192=CARTESIAN_POINT('Ctrl Pts',(3.18690768806312,5.96978744811324,8.64673661296004));
#50193=CARTESIAN_POINT('Ctrl Pts',(3.14312114982841,5.99295688499321,8.64906670169307));
#50194=CARTESIAN_POINT('Ctrl Pts',(3.09908550384719,6.01564277861013,8.65139679042609));
#50195=CARTESIAN_POINT('Origin',(0.,0.,-63.6971797838103));
#50196=CARTESIAN_POINT('',(3.09908550384726,6.0156427786101,11.0457658645337));
#50197=CARTESIAN_POINT('',(3.09908550384714,6.01564277861016,10.6513967904261));
#50198=CARTESIAN_POINT('',(3.09908550384721,6.01564277861012,-63.6971797838103));
#50199=CARTESIAN_POINT('',(-6.76842911963828,-0.00288457139099718,9.69470657721669));
#50200=CARTESIAN_POINT('Ctrl Pts',(-6.76699802906409,-0.00516475002166228,
9.69717978380996));
#50201=CARTESIAN_POINT('Ctrl Pts',(-6.76684617121268,-0.204133098312014,
9.70651087210626));
#50202=CARTESIAN_POINT('Ctrl Pts',(-6.75791508724367,-0.402765009104481,
9.71584196040255));
#50203=CARTESIAN_POINT('Ctrl Pts',(-6.74031724594989,-0.60034358824799,
9.72517304869886));
#50204=CARTESIAN_POINT('Ctrl Pts',(-6.72258670926816,-0.799411995932042,
9.73457449746501));
#50205=CARTESIAN_POINT('Ctrl Pts',(-6.69605829151014,-0.997410976137869,
9.74397594623116));
#50206=CARTESIAN_POINT('Ctrl Pts',(-6.66089694743609,-1.19362509006664,
9.7533773949973));
#50207=CARTESIAN_POINT('Ctrl Pts',(-6.62561182536618,-1.39052993384153,
9.76281193955421));
#50208=CARTESIAN_POINT('Ctrl Pts',(-6.58163298569832,-1.58563718982377,
9.7722464841111));
#50209=CARTESIAN_POINT('Ctrl Pts',(-6.52917590122111,-1.77824381087451,
9.781681028668));
#50210=CARTESIAN_POINT('Ctrl Pts',(-6.47649039451653,-1.97168912957352,
9.79115665556304));
#50211=CARTESIAN_POINT('Ctrl Pts',(-6.41525272681293,-2.16261185559198,
9.80063228245812));
#50212=CARTESIAN_POINT('Ctrl Pts',(-6.34572897970457,-2.35032183245989,
9.81010790935316));
#50213=CARTESIAN_POINT('Ctrl Pts',(-6.29551623179225,-2.48589326152001,
9.81695157478234));
#50214=CARTESIAN_POINT('Ctrl Pts',(-6.24098222467483,-2.61978928377327,
9.82379524021147));
#50215=CARTESIAN_POINT('Ctrl Pts',(-6.18224224289037,-2.75175759292526,
9.83063890564064));
#50216=CARTESIAN_POINT('Ctrl Pts',(-6.11296435785666,-2.90740090556831,
9.83871031888266));
#50217=CARTESIAN_POINT('Ctrl Pts',(-6.03767742973509,-3.06071262367723,
9.8467817321247));
#50218=CARTESIAN_POINT('Ctrl Pts',(-5.95655887786007,-3.21118285598724,
9.85485314536672));
#50219=CARTESIAN_POINT('Ctrl Pts',(-5.8755421636081,-3.36146418538362,9.86291442561795));
#50220=CARTESIAN_POINT('Ctrl Pts',(-5.78870856749346,-3.50891080276374,
9.87097570586917));
#50221=CARTESIAN_POINT('Ctrl Pts',(-5.69628417944841,-3.65303100821301,
9.8790369861204));
#50222=CARTESIAN_POINT('Ctrl Pts',(-5.60395555347136,-3.7970018889093,9.88708991397802));
#50223=CARTESIAN_POINT('Ctrl Pts',(-5.50604786281596,-3.93765290509485,
9.89514284183564));
#50224=CARTESIAN_POINT('Ctrl Pts',(-5.40283384014468,-4.07451536943813,
9.90319576969327));
#50225=CARTESIAN_POINT('Ctrl Pts',(-5.29970415731547,-4.21126599860311,
9.91124211721766));
#50226=CARTESIAN_POINT('Ctrl Pts',(-5.19127699599953,-4.34423394128255,
9.91928846474205));
#50227=CARTESIAN_POINT('Ctrl Pts',(-5.07786921845359,-4.47297811310111,
9.92733481226644));
#50228=CARTESIAN_POINT('Ctrl Pts',(-4.96452930266831,-4.60164524605723,
9.93537634495959));
#50229=CARTESIAN_POINT('Ctrl Pts',(-4.84621494955229,-4.7260933604144,9.94341787765274));
#50230=CARTESIAN_POINT('Ctrl Pts',(-4.72328417905465,-4.84591328480938,
9.95145941034589));
#50231=CARTESIAN_POINT('Ctrl Pts',(-4.5979900967641,-4.96803671579757,9.95965553939413));
#50232=CARTESIAN_POINT('Ctrl Pts',(-4.46790053134225,-5.08535187909609,
9.96785166844238));
#50233=CARTESIAN_POINT('Ctrl Pts',(-4.33343537934581,-5.19746349799919,
9.97604779749062));
#50234=CARTESIAN_POINT('Ctrl Pts',(-4.20155206547098,-5.3074224844376,9.98408655432672));
#50235=CARTESIAN_POINT('Ctrl Pts',(-4.06545998304518,-5.41237570910219,
9.9921253111628));
#50236=CARTESIAN_POINT('Ctrl Pts',(-3.92558976240521,-5.5119900233309,10.0001640679989));
#50237=CARTESIAN_POINT('Ctrl Pts',(-3.78570600380607,-5.61161397917248,
10.0082036029017));
#50238=CARTESIAN_POINT('Ctrl Pts',(-3.64204368301207,-5.70589777888392,
10.0162431378045));
#50239=CARTESIAN_POINT('Ctrl Pts',(-3.49506324561321,-5.79455105328822,
10.0242826727073));
#50240=CARTESIAN_POINT('Ctrl Pts',(-3.34803947988359,-5.88323046177176,
10.0323245775828));
#50241=CARTESIAN_POINT('Ctrl Pts',(-3.19769597020124,-5.96627584832997,
10.0403664824583));
#50242=CARTESIAN_POINT('Ctrl Pts',(-3.04451849647632,-6.04344240682523,
10.0484083873339));
#50243=CARTESIAN_POINT('Ctrl Pts',(-2.88617399696951,-6.12321196945387,
10.0567215640147));
#50244=CARTESIAN_POINT('Ctrl Pts',(-2.72480138680157,-6.19669895739926,
10.0650347406955));
#50245=CARTESIAN_POINT('Ctrl Pts',(-2.56095950535423,-6.26368704613631,
10.0733479173763));
#50246=CARTESIAN_POINT('Ctrl Pts',(-2.40218885044364,-6.32860172256725,
10.0814037849868));
#50247=CARTESIAN_POINT('Ctrl Pts',(-2.24109987559649,-6.38741375553719,
10.0894596525974));
#50248=CARTESIAN_POINT('Ctrl Pts',(-2.07821584240643,-6.43997732234912,
10.0975155202079));
#50249=CARTESIAN_POINT('Ctrl Pts',(-1.90752789388964,-6.4950592552442,10.1059573514238));
#50250=CARTESIAN_POINT('Ctrl Pts',(-1.73486911782119,-6.54327912242878,
10.1143991826398));
#50251=CARTESIAN_POINT('Ctrl Pts',(-1.56085207914365,-6.58452957978267,
10.1228410138558));
#50252=CARTESIAN_POINT('Ctrl Pts',(-1.38683504046617,-6.62578003713655,
10.1312828450717));
#50253=CARTESIAN_POINT('Ctrl Pts',(-1.21146020813647,-6.66006108019321,
10.1397246762877));
#50254=CARTESIAN_POINT('Ctrl Pts',(-1.0353438881606,-6.68732771989294,10.1481665075036));
#50255=CARTESIAN_POINT('Ctrl Pts',(-0.863637347590903,-6.71391162975685,
10.1563969635702));
#50256=CARTESIAN_POINT('Ctrl Pts',(-0.690654969195276,-6.73391699050144,
10.1646274196367));
#50257=CARTESIAN_POINT('Ctrl Pts',(-0.516942018526933,-6.74722609295711,
10.1728578757033));
#50258=CARTESIAN_POINT('Ctrl Pts',(-0.343435275367393,-6.76051939672391,
10.1810785617335));
#50259=CARTESIAN_POINT('Ctrl Pts',(-0.169200040751129,-6.76713224302291,
10.1892992477637));
#50260=CARTESIAN_POINT('Ctrl Pts',(0.00520876157270132,-6.7669979953302,
10.1975199337939));
#50261=CARTESIAN_POINT('Ctrl Pts',(0.179445522171758,-6.76686388006316,
10.2057325107093));
#50262=CARTESIAN_POINT('Ctrl Pts',(0.3538551534552,-6.75999592547768,10.2139450876247));
#50263=CARTESIAN_POINT('Ctrl Pts',(0.527878053718226,-6.74637930748062,
10.2221576645401));
#50264=CARTESIAN_POINT('Ctrl Pts',(0.701764194754424,-6.73277339036342,
10.2303637874447));
#50265=CARTESIAN_POINT('Ctrl Pts',(0.875263854289261,-6.71242940120123,
10.2385699103494));
#50266=CARTESIAN_POINT('Ctrl Pts',(1.04781778217753,-6.68538457348211,10.246776033254));
#50267=CARTESIAN_POINT('Ctrl Pts',(1.22027070358692,-6.65835557677219,10.2549773526078));
#50268=CARTESIAN_POINT('Ctrl Pts',(1.39177864292623,-6.62463361077684,10.2631786719614));
#50269=CARTESIAN_POINT('Ctrl Pts',(1.56178773107372,-6.58430771479186,10.2713799913152));
#50270=CARTESIAN_POINT('Ctrl Pts',(1.73174804764207,-6.54399338735095,10.2795789579047));
#50271=CARTESIAN_POINT('Ctrl Pts',(1.9002100201813,-6.49707898234912,10.2877779244942));
#50272=CARTESIAN_POINT('Ctrl Pts',(2.06662998149656,-6.44370464248475,10.2959768910837));
#50273=CARTESIAN_POINT('Ctrl Pts',(2.23302796630399,-6.39033735094312,10.3041747749627));
#50274=CARTESIAN_POINT('Ctrl Pts',(2.3973841353217,-6.33051193223582,10.3123726588416));
#50275=CARTESIAN_POINT('Ctrl Pts',(2.55916998855588,-6.26441840633868,10.3205705427205));
#50276=CARTESIAN_POINT('Ctrl Pts',(2.72096386610309,-6.19832160231104,10.3287688332011));
#50277=CARTESIAN_POINT('Ctrl Pts',(2.88018684186813,-6.12595620732234,10.3369671236816));
#50278=CARTESIAN_POINT('Ctrl Pts',(3.03633035802638,-6.04756041366495,10.3451654141622));
#50279=CARTESIAN_POINT('Ctrl Pts',(3.19250998248926,-5.96914649092178,10.3533656005035));
#50280=CARTESIAN_POINT('Ctrl Pts',(3.34560840857727,-5.88469955288408,10.3615657868448));
#50281=CARTESIAN_POINT('Ctrl Pts',(3.49514160158241,-5.7945037910841,10.3697659731861));
#50282=CARTESIAN_POINT('Ctrl Pts',(3.64481616648852,-5.70422275626848,10.3779739121602));
#50283=CARTESIAN_POINT('Ctrl Pts',(3.79091845666016,-5.60818222450421,10.3861818511343));
#50284=CARTESIAN_POINT('Ctrl Pts',(3.93299258232579,-5.50671030174735,10.3943897901084));
#50285=CARTESIAN_POINT('Ctrl Pts',(4.07513563245421,-5.40518915188645,10.4026017110024));
#50286=CARTESIAN_POINT('Ctrl Pts',(4.21324633853173,-5.29823157703008,10.4108136318963));
#50287=CARTESIAN_POINT('Ctrl Pts',(4.34690194006119,-5.18620598544758,10.4190255527903));
#50288=CARTESIAN_POINT('Ctrl Pts',(4.48074082907466,-5.07402676851312,10.4272487350328));
#50289=CARTESIAN_POINT('Ctrl Pts',(4.61011213816752,-4.95676588637834,10.4354719172754));
#50290=CARTESIAN_POINT('Ctrl Pts',(4.7346291461588,-4.83482945390461,10.443695099518));
#50291=CARTESIAN_POINT('Ctrl Pts',(4.84566689303691,-4.72609292913055,10.4510281028009));
#50292=CARTESIAN_POINT('Ctrl Pts',(4.95284484943451,-4.61363897515007,10.4583611060838));
#50293=CARTESIAN_POINT('Ctrl Pts',(5.05591632381215,-4.49777713171849,10.4656941093667));
#50294=CARTESIAN_POINT('Ctrl Pts',(5.1815078229504,-4.35660070344525,10.474629296149));
#50295=CARTESIAN_POINT('Ctrl Pts',(5.30126275186575,-4.21007139260991,10.4835644829313));
#50296=CARTESIAN_POINT('Ctrl Pts',(5.4147436786938,-4.05867464747367,10.4924996697136));
#50297=CARTESIAN_POINT('Ctrl Pts',(5.52805464619939,-3.90750464782625,10.5014214743502));
#50298=CARTESIAN_POINT('Ctrl Pts',(5.63511020633228,-3.75148196600656,10.5103432789868));
#50299=CARTESIAN_POINT('Ctrl Pts',(5.73551291545298,-3.59112525494058,10.5192650836234));
#50300=CARTESIAN_POINT('Ctrl Pts',(5.83567071855538,-3.43115969192189,10.5281651258627));
#50301=CARTESIAN_POINT('Ctrl Pts',(5.92920792189058,-3.26688141757251,10.537065168102));
#50302=CARTESIAN_POINT('Ctrl Pts',(6.01577045540629,-3.09883765755175,10.5459652103413));
#50303=CARTESIAN_POINT('Ctrl Pts',(6.10219972462893,-2.93105260337027,10.5548515508347));
#50304=CARTESIAN_POINT('Ctrl Pts',(6.18167562506326,-2.75951385558025,10.5637378913281));
#50305=CARTESIAN_POINT('Ctrl Pts',(6.25388854000848,-2.5847953747155,10.5726242318215));
#50306=CARTESIAN_POINT('Ctrl Pts',(6.32591681913538,-2.41052361850816,10.5814878514934));
#50307=CARTESIAN_POINT('Ctrl Pts',(6.39071907004853,-2.2330885902073,10.5903514711654));
#50308=CARTESIAN_POINT('Ctrl Pts',(6.4480328625905,-2.05308577583914,10.5992150908373));
#50309=CARTESIAN_POINT('Ctrl Pts',(6.50244109802557,-1.88220831216498,10.6076293639909));
#50310=CARTESIAN_POINT('Ctrl Pts',(6.55010112360273,-1.70901716807654,10.6160436371445));
#50311=CARTESIAN_POINT('Ctrl Pts',(6.59082757677796,-1.53404069476112,10.6244579102981));
#50312=CARTESIAN_POINT('Ctrl Pts',(6.63056651595371,-1.36330696058711,10.6326681585026));
#50313=CARTESIAN_POINT('Ctrl Pts',(6.66366486677742,-1.19103728197648,10.6408784067072));
#50314=CARTESIAN_POINT('Ctrl Pts',(6.69002227061687,-1.01778731503707,10.6490886549117));
#50315=CARTESIAN_POINT('Ctrl Pts',(6.71638594013664,-0.84449616312675,10.6573008548559));
#50316=CARTESIAN_POINT('Ctrl Pts',(6.73600541657981,-0.670224610522699,
10.6655130548002));
#50317=CARTESIAN_POINT('Ctrl Pts',(6.74883205562075,-0.495534948339518,
10.6737252547444));
#50318=CARTESIAN_POINT('Ctrl Pts',(6.76166402787439,-0.320772651608627,
10.6819408692549));
#50319=CARTESIAN_POINT('Ctrl Pts',(6.76769750984418,-0.145592253658605,
10.6901564837653));
#50320=CARTESIAN_POINT('Ctrl Pts',(6.76693594979251,0.02944234035846,10.6983720982758));
#50321=CARTESIAN_POINT('Ctrl Pts',(6.76617353454229,0.204673490551597,10.7065969385613));
#50322=CARTESIAN_POINT('Ctrl Pts',(6.7586008381732,0.379758153708125,10.7148217788467));
#50323=CARTESIAN_POINT('Ctrl Pts',(6.74427338198156,0.554134955669637,10.7230466191321));
#50324=CARTESIAN_POINT('Ctrl Pts',(6.72993674855619,0.728623452034429,10.7312767277137));
#50325=CARTESIAN_POINT('Ctrl Pts',(6.70883677312071,0.90240283091759,10.7395068362952));
#50326=CARTESIAN_POINT('Ctrl Pts',(6.68108039171039,1.07492036891251,10.7477369448767));
#50327=CARTESIAN_POINT('Ctrl Pts',(6.65328595587521,1.24767443109938,10.7559783370635));
#50328=CARTESIAN_POINT('Ctrl Pts',(6.61881695570913,1.41916284896096,10.7642197292501));
#50329=CARTESIAN_POINT('Ctrl Pts',(6.57783085565331,1.58884556657195,10.7724611214368));
#50330=CARTESIAN_POINT('Ctrl Pts',(6.559992663597,1.66269579631466,10.7760479847012));
#50331=CARTESIAN_POINT('Ctrl Pts',(6.54092062560285,1.7362042097666,10.7796348479655));
#50332=CARTESIAN_POINT('Ctrl Pts',(6.52063059142613,1.8093274137529,10.7832217112298));
#50333=CARTESIAN_POINT('Ctrl Pts',(6.47283500247094,1.98157781857599,10.7916709942978));
#50334=CARTESIAN_POINT('Ctrl Pts',(6.41816856105709,2.15208230878793,10.8001202773659));
#50335=CARTESIAN_POINT('Ctrl Pts',(6.3567776680875,2.32027297499756,10.808569560434));
#50336=CARTESIAN_POINT('Ctrl Pts',(6.2954439444839,2.48830701612346,10.8170109752314));
#50337=CARTESIAN_POINT('Ctrl Pts',(6.22739836603516,2.65403121662498,10.8254523900289));
#50338=CARTESIAN_POINT('Ctrl Pts',(6.1528372684843,2.81689235640105,10.8338938048264));
#50339=CARTESIAN_POINT('Ctrl Pts',(6.07486152976478,2.98721197480637,10.8427218073142));
#50340=CARTESIAN_POINT('Ctrl Pts',(5.98975953431458,3.15439976562703,10.851549809802));
#50341=CARTESIAN_POINT('Ctrl Pts',(5.8978131589271,3.31784402020143,10.8603778122898));
#50342=CARTESIAN_POINT('Ctrl Pts',(5.8100258909488,3.473895028361,10.8688064884268));
#50343=CARTESIAN_POINT('Ctrl Pts',(5.71599996201079,3.62653336835884,10.8772351645638));
#50344=CARTESIAN_POINT('Ctrl Pts',(5.61602866345865,3.77524979984251,10.8856638407007));
#50345=CARTESIAN_POINT('Ctrl Pts',(5.51609820318497,3.92390548065944,10.8940890737233));
#50346=CARTESIAN_POINT('Ctrl Pts',(5.41022740046718,4.06864217043807,10.9025143067458));
#50347=CARTESIAN_POINT('Ctrl Pts',(5.2987536581543,4.20897834042852,10.9109395397683));
#50348=CARTESIAN_POINT('Ctrl Pts',(5.18730989897394,4.34927676414892,10.9193625066529));
#50349=CARTESIAN_POINT('Ctrl Pts',(5.07026641222063,4.4851767672602,10.9277854735375));
#50350=CARTESIAN_POINT('Ctrl Pts',(4.9480020163163,4.61622844392799,10.936208440422));
#50351=CARTESIAN_POINT('Ctrl Pts',(4.82575345400299,4.74726314902662,10.9446303165081));
#50352=CARTESIAN_POINT('Ctrl Pts',(4.69828555868826,4.8734505366306,10.9530521925942));
#50353=CARTESIAN_POINT('Ctrl Pts',(4.56601551626838,4.99437596754554,10.9614740686804));
#50354=CARTESIAN_POINT('Ctrl Pts',(4.43371847846059,5.11532607849275,10.9698976636123));
#50355=CARTESIAN_POINT('Ctrl Pts',(4.29661757959628,5.23101186001651,10.9783212585443));
#50356=CARTESIAN_POINT('Ctrl Pts',(4.1551652661537,5.34105706868499,10.9867448534763));
#50357=CARTESIAN_POINT('Ctrl Pts',(4.01369811032806,5.45111382423525,10.9951693322836));
#50358=CARTESIAN_POINT('Ctrl Pts',(3.86787889546673,5.55552862572213,11.003593811091));
#50359=CARTESIAN_POINT('Ctrl Pts',(3.71819135113202,5.65396693272671,11.0120182898984));
#50360=CARTESIAN_POINT('Ctrl Pts',(3.56843267028355,5.7524520208981,11.0204467722991));
#50361=CARTESIAN_POINT('Ctrl Pts',(3.41480226851862,5.84495476121324,11.0288752546998));
#50362=CARTESIAN_POINT('Ctrl Pts',(3.25781157025836,5.93118476973115,11.0373037371005));
#50363=CARTESIAN_POINT('Ctrl Pts',(3.20527244433795,5.96004284429127,11.0401244462449));
#50364=CARTESIAN_POINT('Ctrl Pts',(3.15235716997192,5.98819875403474,11.0429451553893));
#50365=CARTESIAN_POINT('Ctrl Pts',(3.09908550384726,6.0156427786101,11.0457658645337));
#50366=CARTESIAN_POINT('Ctrl Pts',(3.09908550384729,6.01564277861008,9.04575635804621));
#50367=CARTESIAN_POINT('Ctrl Pts',(2.93373232018328,6.10082796552481,9.0545058059455));
#50368=CARTESIAN_POINT('Ctrl Pts',(2.76486502144416,6.17919158180196,9.06325525384478));
#50369=CARTESIAN_POINT('Ctrl Pts',(2.59305716434331,6.25046746591388,9.07200470174408));
#50370=CARTESIAN_POINT('Ctrl Pts',(2.42125069459257,6.32174277447235,9.0807540789915));
#50371=CARTESIAN_POINT('Ctrl Pts',(2.24650397871028,6.38593035557837,9.08950345623892));
#50372=CARTESIAN_POINT('Ctrl Pts',(2.06941053323735,6.4428122000355,9.09825283348634));
#50373=CARTESIAN_POINT('Ctrl Pts',(1.89231845896656,6.49969360406693,9.10700214298893));
#50374=CARTESIAN_POINT('Ctrl Pts',(1.71287996431486,6.54926929700886,9.11575145249154));
#50375=CARTESIAN_POINT('Ctrl Pts',(1.53170449173494,6.59137090065481,9.12450076199413));
#50376=CARTESIAN_POINT('Ctrl Pts',(1.35053036178163,6.63347219230085,9.13325000665872));
#50377=CARTESIAN_POINT('Ctrl Pts',(1.1676195587884,6.66809944062455,9.14199925132329));
#50378=CARTESIAN_POINT('Ctrl Pts',(0.983593309310468,6.69513503985392,9.15074849598788));
#50379=CARTESIAN_POINT('Ctrl Pts',(0.799568362460066,6.72217044771213,9.15949767872105));
#50380=CARTESIAN_POINT('Ctrl Pts',(0.614428268438786,6.74161427235975,9.16824686145422));
#50381=CARTESIAN_POINT('Ctrl Pts',(0.428801816330565,6.753400476968,9.17699604418739));
#50382=CARTESIAN_POINT('Ctrl Pts',(0.243176616523095,6.76518660206241,9.18574516789552));
#50383=CARTESIAN_POINT('Ctrl Pts',(0.0570653511657863,6.76931519233996,
9.19449429160367));
#50384=CARTESIAN_POINT('Ctrl Pts',(-0.128899900799689,6.76577222610796,
9.2032434153118));
#50385=CARTESIAN_POINT('Ctrl Pts',(-0.3148639599416,6.76222928260135,9.21199248290106));
#50386=CARTESIAN_POINT('Ctrl Pts',(-0.500681721080178,6.7510148865128,9.22074155049031));
#50387=CARTESIAN_POINT('Ctrl Pts',(-0.685722110172717,6.73216712415997,
9.22949061807957));
#50388=CARTESIAN_POINT('Ctrl Pts',(-0.870761373826965,6.71331947644153,
9.23823963245592));
#50389=CARTESIAN_POINT('Ctrl Pts',(-1.05502298984272,6.68683858440007,9.24698864683228));
#50390=CARTESIAN_POINT('Ctrl Pts',(-1.23788117675982,6.6528143813144,9.25573766120864));
#50391=CARTESIAN_POINT('Ctrl Pts',(-1.43009641451717,6.61704912302394,9.26493437209617));
#50392=CARTESIAN_POINT('Ctrl Pts',(-1.62076048992621,6.57294837083183,9.2741310829837));
#50393=CARTESIAN_POINT('Ctrl Pts',(-1.80915798961058,6.5206776004207,9.28332779387122));
#50394=CARTESIAN_POINT('Ctrl Pts',(-1.98840443002939,6.47094578577431,9.29207779157773));
#50395=CARTESIAN_POINT('Ctrl Pts',(-2.16559895952119,6.413818884745,9.30082778928424));
#50396=CARTESIAN_POINT('Ctrl Pts',(-2.3401396624225,6.34949095285261,9.30957778699074));
#50397=CARTESIAN_POINT('Ctrl Pts',(-2.51467682553946,6.28516432556712,9.31832760724234));
#50398=CARTESIAN_POINT('Ctrl Pts',(-2.68656000078778,6.21363705879689,9.32707742749393));
#50399=CARTESIAN_POINT('Ctrl Pts',(-2.85520533840828,6.13515211510887,9.33582724774553));
#50400=CARTESIAN_POINT('Ctrl Pts',(-3.02384747998267,6.05666865881151,9.34457690217677));
#50401=CARTESIAN_POINT('Ctrl Pts',(-3.18925164684476,5.97122791039876,9.35332655660802));
#50402=CARTESIAN_POINT('Ctrl Pts',(-3.35085601829097,5.87912008251942,9.36207621103927));
#50403=CARTESIAN_POINT('Ctrl Pts',(-3.51245754191361,5.78701387778209,9.37082571128241));
#50404=CARTESIAN_POINT('Ctrl Pts',(-3.67025915510882,5.68824097061018,9.37957521152556));
#50405=CARTESIAN_POINT('Ctrl Pts',(-3.82372487928783,5.5831368465689,9.3883247117687));
#50406=CARTESIAN_POINT('Ctrl Pts',(-3.97718810300744,5.47803443501812,9.39707406945382));
#50407=CARTESIAN_POINT('Ctrl Pts',(-4.12631534262969,5.36660117496419,9.40582342713893));
#50408=CARTESIAN_POINT('Ctrl Pts',(-4.27060009886167,5.24921554097398,9.41457278482405));
#50409=CARTESIAN_POINT('Ctrl Pts',(-4.41488269594169,5.1318316636033,9.42332201157923));
#50410=CARTESIAN_POINT('Ctrl Pts',(-4.55432273235057,5.008495771395,9.43207123833443));
#50411=CARTESIAN_POINT('Ctrl Pts',(-4.68844662480187,4.87962675277361,9.44082046508962));
#50412=CARTESIAN_POINT('Ctrl Pts',(-4.82256868835141,4.75075949139899,9.44956957254111));
#50413=CARTESIAN_POINT('Ctrl Pts',(-4.95137454637848,4.6163594531254,9.4583186799926));
#50414=CARTESIAN_POINT('Ctrl Pts',(-5.07442674461067,4.47688309134603,9.46706778744409));
#50415=CARTESIAN_POINT('Ctrl Pts',(-5.19747742838507,4.33740844616388,9.47581678721645));
#50416=CARTESIAN_POINT('Ctrl Pts',(-5.31477440450878,4.1928578173609,9.48456578698882));
#50417=CARTESIAN_POINT('Ctrl Pts',(-5.42591931531087,4.04372211999494,9.49331478676118));
#50418=CARTESIAN_POINT('Ctrl Pts',(-5.53707636462923,3.89457013500884,9.50206474204176));
#50419=CARTESIAN_POINT('Ctrl Pts',(-5.64207983273419,3.74083230916498,9.51081469732233));
#50420=CARTESIAN_POINT('Ctrl Pts',(-5.74057303468702,3.583030872519,9.51956465260291));
#50421=CARTESIAN_POINT('Ctrl Pts',(-5.83906243363725,3.42523552887499,9.52831427003172));
#50422=CARTESIAN_POINT('Ctrl Pts',(-5.9310419176839,3.26337713157057,9.53706388746053));
#50423=CARTESIAN_POINT('Ctrl Pts',(-6.01619906699625,3.09800545291216,9.54581350488934));
#50424=CARTESIAN_POINT('Ctrl Pts',(-6.10135338095357,2.93263928039649,9.55456283099473));
#50425=CARTESIAN_POINT('Ctrl Pts',(-6.17968568352818,2.76376031540271,9.56331215710014));
#50426=CARTESIAN_POINT('Ctrl Pts',(-6.2509299269487,2.59194213831582,9.57206148320553));
#50427=CARTESIAN_POINT('Ctrl Pts',(-6.32217217691088,2.42012876880861,9.58081056449933));
#50428=CARTESIAN_POINT('Ctrl Pts',(-6.38632665483835,2.24537661647713,9.58955964579312));
#50429=CARTESIAN_POINT('Ctrl Pts',(-6.44317547869336,2.068279176215,9.59830872708692));
#50430=CARTESIAN_POINT('Ctrl Pts',(-6.50002944235922,1.8911657242347,9.60705859940188));
#50431=CARTESIAN_POINT('Ctrl Pts',(-6.54957634250385,1.71170683289247,9.61580847171683));
#50432=CARTESIAN_POINT('Ctrl Pts',(-6.59164787708383,1.53051209225416,9.6245583440318));
#50433=CARTESIAN_POINT('Ctrl Pts',(-6.63371649074996,1.34932993148091,9.63330760886658));
#50434=CARTESIAN_POINT('Ctrl Pts',(-6.66831071257111,1.16641244174075,9.64205687370137));
#50435=CARTESIAN_POINT('Ctrl Pts',(-6.69531304840321,0.982380875160824,
9.65080613853615));
#50436=CARTESIAN_POINT('Ctrl Pts',(-6.72231677033034,0.798339861796689,
9.65955585249181));
#50437=CARTESIAN_POINT('Ctrl Pts',(-6.74172778477882,0.613184940731031,
9.66830556644746));
#50438=CARTESIAN_POINT('Ctrl Pts',(-6.75348015835512,0.427545027691463,
9.67705528040311));
#50439=CARTESIAN_POINT('Ctrl Pts',(-6.76249038365214,0.285219953548324,
9.68376344820539));
#50440=CARTESIAN_POINT('Ctrl Pts',(-6.76699999999995,0.142609995759399,
9.69047161600768));
#50441=CARTESIAN_POINT('Ctrl Pts',(-6.767,2.60385621481446E-12,9.69717978380996));
#50442=CARTESIAN_POINT('',(-6.767,5.79285625171286E-10,9.30282021616271));
#50443=CARTESIAN_POINT('Ctrl Pts',(3.09908550384719,6.01564277861013,8.65139679042609));
#50444=CARTESIAN_POINT('Ctrl Pts',(2.93373232018324,6.10082796552483,8.66014623832538));
#50445=CARTESIAN_POINT('Ctrl Pts',(2.76486502144417,6.17919158180195,8.66889568622467));
#50446=CARTESIAN_POINT('Ctrl Pts',(2.59305716434338,6.25046746591385,8.67764513412396));
#50447=CARTESIAN_POINT('Ctrl Pts',(2.4212506945927,6.32174277447229,8.68639451137138));
#50448=CARTESIAN_POINT('Ctrl Pts',(2.24650397871047,6.38593035557829,8.6951438886188));
#50449=CARTESIAN_POINT('Ctrl Pts',(2.06941053323761,6.44281220003542,8.70389326586621));
#50450=CARTESIAN_POINT('Ctrl Pts',(1.89231845896676,6.49969360406687,8.71264257536881));
#50451=CARTESIAN_POINT('Ctrl Pts',(1.712879964315,6.54926929700882,8.7213918848714));
#50452=CARTESIAN_POINT('Ctrl Pts',(1.53170449173501,6.59137090065479,8.730141194374));
#50453=CARTESIAN_POINT('Ctrl Pts',(1.3505303617817,6.63347219230083,8.73889043903859));
#50454=CARTESIAN_POINT('Ctrl Pts',(1.16761955878848,6.66809944062453,8.74763968370318));
#50455=CARTESIAN_POINT('Ctrl Pts',(0.983593309310546,6.69513503985391,8.75638892836777));
#50456=CARTESIAN_POINT('Ctrl Pts',(0.799568362460019,6.72217044771214,8.76513811110095));
#50457=CARTESIAN_POINT('Ctrl Pts',(0.614428268438608,6.74161427235977,8.77388729383413));
#50458=CARTESIAN_POINT('Ctrl Pts',(0.428801816330259,6.75340047696802,8.7826364765673));
#50459=CARTESIAN_POINT('Ctrl Pts',(0.243176616522789,6.76518660206242,8.79138560027544));
#50460=CARTESIAN_POINT('Ctrl Pts',(0.0570653511654812,6.76931519233997,
8.80013472398356));
#50461=CARTESIAN_POINT('Ctrl Pts',(-0.128899900799994,6.76577222610795,
8.80888384769169));
#50462=CARTESIAN_POINT('Ctrl Pts',(-0.314863959941904,6.76222928260133,
8.81763291528095));
#50463=CARTESIAN_POINT('Ctrl Pts',(-0.500681721080484,6.75101488651278,
8.82638198287021));
#50464=CARTESIAN_POINT('Ctrl Pts',(-0.685722110173022,6.73216712415994,
8.83513105045947));
#50465=CARTESIAN_POINT('Ctrl Pts',(-0.870761373827397,6.71331947644148,
8.84388006483583));
#50466=CARTESIAN_POINT('Ctrl Pts',(-1.05502298984328,6.68683858439999,8.85262907921219));
#50467=CARTESIAN_POINT('Ctrl Pts',(-1.2378811767605,6.65281438131428,8.86137809358856));
#50468=CARTESIAN_POINT('Ctrl Pts',(-1.430096414506,6.617049123026,8.87057480447552));
#50469=CARTESIAN_POINT('Ctrl Pts',(-1.62076048990337,6.57294837083711,8.87977151536247));
#50470=CARTESIAN_POINT('Ctrl Pts',(-1.8091579895764,6.52067760043018,8.88896822624943));
#50471=CARTESIAN_POINT('Ctrl Pts',(-1.98840442999547,6.47094578578474,8.89771822395594));
#50472=CARTESIAN_POINT('Ctrl Pts',(-2.16559895948757,6.41381888475635,8.90646822166245));
#50473=CARTESIAN_POINT('Ctrl Pts',(-2.34013966238922,6.34949095286488,8.91521821936895));
#50474=CARTESIAN_POINT('Ctrl Pts',(-2.5146768255064,6.28516432558035,8.92396803962054));
#50475=CARTESIAN_POINT('Ctrl Pts',(-2.68656000075498,6.21363705881107,8.93271785987215));
#50476=CARTESIAN_POINT('Ctrl Pts',(-2.85520533837578,6.135152115124,8.94146768012374));
#50477=CARTESIAN_POINT('Ctrl Pts',(-3.02384747995052,6.05666865882756,8.95021733455498));
#50478=CARTESIAN_POINT('Ctrl Pts',(-3.18925164681301,5.97122791041572,8.95896698898622));
#50479=CARTESIAN_POINT('Ctrl Pts',(-3.35085601825965,5.87912008253727,8.96771664341746));
#50480=CARTESIAN_POINT('Ctrl Pts',(-3.51245754188273,5.78701387780083,8.9764661436606));
#50481=CARTESIAN_POINT('Ctrl Pts',(-3.67025915507841,5.68824097062979,8.98521564390373));
#50482=CARTESIAN_POINT('Ctrl Pts',(-3.82372487925794,5.58313684658937,8.99396514414687));
#50483=CARTESIAN_POINT('Ctrl Pts',(-3.97718810297827,5.47803443503931,9.002714501832));
#50484=CARTESIAN_POINT('Ctrl Pts',(-4.12631534260126,5.36660117498606,9.01146385951711));
#50485=CARTESIAN_POINT('Ctrl Pts',(-4.27060009883401,5.24921554099648,9.02021321720224));
#50486=CARTESIAN_POINT('Ctrl Pts',(-4.41488269591464,5.13183166362657,9.02896244395743));
#50487=CARTESIAN_POINT('Ctrl Pts',(-4.55432273232418,5.008495771419,9.03771167071264));
#50488=CARTESIAN_POINT('Ctrl Pts',(-4.68844662477616,4.87962675279832,9.04646089746782));
#50489=CARTESIAN_POINT('Ctrl Pts',(-4.82256868832633,4.75075949142444,9.05521000491931));
#50490=CARTESIAN_POINT('Ctrl Pts',(-4.95137454635407,4.61635945315159,9.0639591123708));
#50491=CARTESIAN_POINT('Ctrl Pts',(-5.07442674458695,4.47688309137292,9.07270821982229));
#50492=CARTESIAN_POINT('Ctrl Pts',(-5.19747742836243,4.33740844619103,9.08145721959467));
#50493=CARTESIAN_POINT('Ctrl Pts',(-5.31477440448721,4.19285781738826,9.09020621936706));
#50494=CARTESIAN_POINT('Ctrl Pts',(-5.42591931529037,4.04372212002246,9.09895521913944));
#50495=CARTESIAN_POINT('Ctrl Pts',(-5.53707636460948,3.89457013503692,9.10770517442002));
#50496=CARTESIAN_POINT('Ctrl Pts',(-5.64207983271522,3.74083230919359,9.11645512970061));
#50497=CARTESIAN_POINT('Ctrl Pts',(-5.74057303466886,3.5830308725481,9.12520508498119));
#50498=CARTESIAN_POINT('Ctrl Pts',(-5.83906243361988,3.4252355289046,9.13395470241));
#50499=CARTESIAN_POINT('Ctrl Pts',(-5.93104191766735,3.26337713160065,9.14270431983881));
#50500=CARTESIAN_POINT('Ctrl Pts',(-6.01619906698054,3.09800545294267,9.15145393726762));
#50501=CARTESIAN_POINT('Ctrl Pts',(-6.10135338093861,2.93263928042761,9.160203263373));
#50502=CARTESIAN_POINT('Ctrl Pts',(-6.179685683514,2.7637603154344,9.16895258947838));
#50503=CARTESIAN_POINT('Ctrl Pts',(-6.25092992693533,2.59194213834805,9.17770191558377));
#50504=CARTESIAN_POINT('Ctrl Pts',(-6.32217217689837,2.42012876884127,9.18645099687756));
#50505=CARTESIAN_POINT('Ctrl Pts',(-6.38632665482673,2.24537661651018,9.19520007817135));
#50506=CARTESIAN_POINT('Ctrl Pts',(-6.44317547868264,2.06827917624841,9.20394915946514));
#50507=CARTESIAN_POINT('Ctrl Pts',(-6.5000294423494,1.89116572426846,9.2126990317801));
#50508=CARTESIAN_POINT('Ctrl Pts',(-6.54957634249494,1.71170683292655,9.22144890409506));
#50509=CARTESIAN_POINT('Ctrl Pts',(-6.59164787707586,1.53051209228852,9.23019877641002));
#50510=CARTESIAN_POINT('Ctrl Pts',(-6.63371649074297,1.34932993151531,9.23894804124482));
#50511=CARTESIAN_POINT('Ctrl Pts',(-6.6683107125651,1.16641244177513,9.24769730607961));
#50512=CARTESIAN_POINT('Ctrl Pts',(-6.69531304839817,0.982380875195151,
9.25644657091441));
#50513=CARTESIAN_POINT('Ctrl Pts',(-6.72231677032625,0.79833986183109,9.26519628487006));
#50514=CARTESIAN_POINT('Ctrl Pts',(-6.74172778477569,0.613184940765469,
9.27394599882572));
#50515=CARTESIAN_POINT('Ctrl Pts',(-6.75348015835294,0.427545027725897,
9.28269571278138));
#50516=CARTESIAN_POINT('Ctrl Pts',(-6.76249038363927,0.285219953763168,
9.28940388057515));
#50517=CARTESIAN_POINT('Ctrl Pts',(-6.76699999998779,0.142609996155356,
9.29611204836894));
#50518=CARTESIAN_POINT('Ctrl Pts',(-6.767,5.79286453889775E-10,9.30282021616271));
#50519=CARTESIAN_POINT('Ctrl Pts',(-6.767,2.48800301388039E-12,9.30282021618984));
#50520=CARTESIAN_POINT('Ctrl Pts',(-6.76700000000007,-0.18600724955762,
9.31156972800259));
#50521=CARTESIAN_POINT('Ctrl Pts',(-6.75932637294259,-0.372014355813903,
9.32031923981534));
#50522=CARTESIAN_POINT('Ctrl Pts',(-6.74400518263379,-0.55738953758438,
9.32906875162809));
#50523=CARTESIAN_POINT('Ctrl Pts',(-6.7286840570375,-0.742763936380955,
9.33781822648529));
#50524=CARTESIAN_POINT('Ctrl Pts',(-6.70571545643587,-0.927506130403373,
9.3465677013425));
#50525=CARTESIAN_POINT('Ctrl Pts',(-6.67517739401599,-1.11098864009399,
9.3553171761997));
#50526=CARTESIAN_POINT('Ctrl Pts',(-6.64463945804417,-1.29447039004398,
9.36406661482822));
#50527=CARTESIAN_POINT('Ctrl Pts',(-6.60653217002755,-1.47669218339137,
9.37281605345672));
#50528=CARTESIAN_POINT('Ctrl Pts',(-6.56098496085515,-1.65703510627646,
9.38156549208523));
#50529=CARTESIAN_POINT('Ctrl Pts',(-6.5154379364959,-1.83737729739891,9.39031489521187));
#50530=CARTESIAN_POINT('Ctrl Pts',(-6.46245112156927,-2.01584035544854,
9.39906429833851));
#50531=CARTESIAN_POINT('Ctrl Pts',(-6.40220448361744,-2.1918181379733,9.40781370146514));
#50532=CARTESIAN_POINT('Ctrl Pts',(-6.34195808511996,-2.36779522106244,
9.41656306981669));
#50533=CARTESIAN_POINT('Ctrl Pts',(-6.27445201416371,-2.54128677725703,
9.42531243816822));
#50534=CARTESIAN_POINT('Ctrl Pts',(-6.19991555052734,-2.71170355428635,
9.43406180651976));
#50535=CARTESIAN_POINT('Ctrl Pts',(-6.12537937695127,-2.88211966813502,
9.44281114082295));
#50536=CARTESIAN_POINT('Ctrl Pts',(-6.04381298028354,-3.04946076419863,
9.45156047512612));
#50537=CARTESIAN_POINT('Ctrl Pts',(-5.95549339308879,-3.21315848424503,
9.4603098094293));
#50538=CARTESIAN_POINT('Ctrl Pts',(-5.86717414225702,-3.37685558085269,
9.46905911041086));
#50539=CARTESIAN_POINT('Ctrl Pts',(-5.77210188843955,-3.53690907700182,
9.47780841139242));
#50540=CARTESIAN_POINT('Ctrl Pts',(-5.67059953311257,-3.69277537024168,
9.48655771237398));
#50541=CARTESIAN_POINT('Ctrl Pts',(-5.56909755592581,-3.8486410828121,9.4953069807606));
#50542=CARTESIAN_POINT('Ctrl Pts',(-5.46116568154827,-4.00031938355018,
9.50405624914723));
#50543=CARTESIAN_POINT('Ctrl Pts',(-5.34717048488226,-4.1472951191836,9.51280551753385));
#50544=CARTESIAN_POINT('Ctrl Pts',(-5.2331757034314,-4.2942703194738,9.52155475405221));
#50545=CARTESIAN_POINT('Ctrl Pts',(-5.11311781951369,-4.43654276249762,
9.53030399057056));
#50546=CARTESIAN_POINT('Ctrl Pts',(-4.98740458929052,-4.57362924412593,
9.53905322708891));
#50547=CARTESIAN_POINT('Ctrl Pts',(-4.86169180652541,-4.71071523781473,
9.54780243246563));
#50548=CARTESIAN_POINT('Ctrl Pts',(-4.73032391141367,-4.8426150958469,9.55655163784235));
#50549=CARTESIAN_POINT('Ctrl Pts',(-4.59374706947116,-4.96888084599793,
9.56530084321906));
#50550=CARTESIAN_POINT('Ctrl Pts',(-4.4571707023134,-5.09514615720887,9.57405001818075));
#50551=CARTESIAN_POINT('Ctrl Pts',(-4.3153856349724,-5.21577720520682,9.58279919314242));
#50552=CARTESIAN_POINT('Ctrl Pts',(-4.16887340951967,-5.33036429293532,
9.5915483681041));
#50553=CARTESIAN_POINT('Ctrl Pts',(-4.02236168122451,-5.4449509918373,9.60029751337735));
#50554=CARTESIAN_POINT('Ctrl Pts',(-3.87112305263153,-5.55349359497947,
9.60904665865059));
#50555=CARTESIAN_POINT('Ctrl Pts',(-3.71567116928974,-5.65562346357226,
9.61779580392384));
#50556=CARTESIAN_POINT('Ctrl Pts',(-3.56021980053292,-5.75775299408939,
9.62654492023521));
#50557=CARTESIAN_POINT('Ctrl Pts',(-3.40055544442068,-5.85346967519888,
9.63529403654658));
#50558=CARTESIAN_POINT('Ctrl Pts',(-3.23722035886829,-5.9424484304139,9.64404315285795));
#50559=CARTESIAN_POINT('Ctrl Pts',(-3.07388580043488,-6.03142689847452,
9.65279224093395));
#50560=CARTESIAN_POINT('Ctrl Pts',(-2.90688078789233,-6.11366734707897,
9.66154132900997));
#50561=CARTESIAN_POINT('Ctrl Pts',(-2.73677250610415,-6.18889047001419,
9.67029041708598));
#50562=CARTESIAN_POINT('Ctrl Pts',(-2.56666475916967,-6.26411335643321,
9.67903947765314));
#50563=CARTESIAN_POINT('Ctrl Pts',(-2.39345402457135,-6.3323188454524,9.68778853822029));
#50564=CARTESIAN_POINT('Ctrl Pts',(-2.21772855944117,-6.39327529804865,
9.69653759878746));
#50565=CARTESIAN_POINT('Ctrl Pts',(-2.04200363223662,-6.4542315640468,9.70528663257226));
#50566=CARTESIAN_POINT('Ctrl Pts',(-1.86376426061124,-6.50793874412426,
9.71403566635705));
#50567=CARTESIAN_POINT('Ctrl Pts',(-1.68361577621798,-6.55421443943284,
9.72278470014184));
#50568=CARTESIAN_POINT('Ctrl Pts',(-1.50346782833284,-6.60048999692573,
9.73153370787076));
#50569=CARTESIAN_POINT('Ctrl Pts',(-1.32141105657414,-6.63933404265158,
9.74028271559967));
#50570=CARTESIAN_POINT('Ctrl Pts',(-1.13806375346518,-6.67061465631532,
9.74903172332859));
#50571=CARTESIAN_POINT('Ctrl Pts',(-0.954716981169746,-6.70189517941775,
9.75778070572802));
#50572=CARTESIAN_POINT('Ctrl Pts',(-0.770079967441923,-6.72561226609008,
9.76652968812746));
#50573=CARTESIAN_POINT('Ctrl Pts',(-0.584779764072615,-6.74168536995989,
9.7752786705269));
#50574=CARTESIAN_POINT('Ctrl Pts',(-0.391489587592477,-6.75845153117875,
9.78440490094252));
#50575=CARTESIAN_POINT('Ctrl Pts',(-0.197478091804735,-6.76689985146396,
9.79353113135812));
#50576=CARTESIAN_POINT('Ctrl Pts',(-0.00346214753050771,-6.76699911434415,
9.80265736177374));
#50577=CARTESIAN_POINT('Ctrl Pts',(0.18449079848517,-6.76709527525933,9.81149839748887));
#50578=CARTESIAN_POINT('Ctrl Pts',(0.372447602155317,-6.7593563379076,9.820339433204));
#50579=CARTESIAN_POINT('Ctrl Pts',(0.559756448194758,-6.74380914014509,
9.82918046891913));
#50580=CARTESIAN_POINT('Ctrl Pts',(0.745136131043981,-6.72842206873148,
9.83793044753244));
#50581=CARTESIAN_POINT('Ctrl Pts',(0.929880851945746,-6.70538686355714,
9.84668042614576));
#50582=CARTESIAN_POINT('Ctrl Pts',(1.11336305057541,-6.67478177303299,9.85543040475908));
#50583=CARTESIAN_POINT('Ctrl Pts',(1.29684337090212,-6.64417699581243,9.86418029379906));
#50584=CARTESIAN_POINT('Ctrl Pts',(1.4790609120529,-6.60600253548038,9.87293018283905));
#50585=CARTESIAN_POINT('Ctrl Pts',(1.65939671095331,-6.56038806441184,9.88168007187903));
#50586=CARTESIAN_POINT('Ctrl Pts',(1.83973072369273,-6.51477404513818,9.89042987425453));
#50587=CARTESIAN_POINT('Ctrl Pts',(2.01818275357152,-6.46172023288625,9.89917967663001));
#50588=CARTESIAN_POINT('Ctrl Pts',(2.19414664033445,-6.40140683918067,9.9079294790055));
#50589=CARTESIAN_POINT('Ctrl Pts',(2.37010884271371,-6.34109402281455,9.91667919762504));
#50590=CARTESIAN_POINT('Ctrl Pts',(2.54358267847912,-6.27352185699749,9.92542891624459));
#50591=CARTESIAN_POINT('Ctrl Pts',(2.71397890841841,-6.19891986435218,9.93417863486413));
#50592=CARTESIAN_POINT('Ctrl Pts',(2.88437356389041,-6.12431856103197,9.94292827263594));
#50593=CARTESIAN_POINT('Ctrl Pts',(3.05169040787271,-6.04268767582507,9.95167791040775));
#50594=CARTESIAN_POINT('Ctrl Pts',(3.21536112512152,-5.95430447953892,9.96042754817957));
#50595=CARTESIAN_POINT('Ctrl Pts',(3.3790303844294,-5.86592207054986,9.96917710801164));
#50596=CARTESIAN_POINT('Ctrl Pts',(3.5390533298007,-5.77078760703318,9.9779266678437));
#50597=CARTESIAN_POINT('Ctrl Pts',(3.69488643041988,-5.66922422085236,9.98667622767577));
#50598=CARTESIAN_POINT('Ctrl Pts',(3.85071819468837,-5.56766170563093,9.99542571247577));
#50599=CARTESIAN_POINT('Ctrl Pts',(4.00235994599318,-5.45967053456182,10.0041751972758));
#50600=CARTESIAN_POINT('Ctrl Pts',(4.14929662974394,-5.34561750206612,10.0129246820758));
#50601=CARTESIAN_POINT('Ctrl Pts',(4.29623210225136,-5.2315654097439,10.0216740947511));
#50602=CARTESIAN_POINT('Ctrl Pts',(4.43846235842208,-5.11145173172108,10.0304235074265));
#50603=CARTESIAN_POINT('Ctrl Pts',(4.57550431797517,-4.9856844300648,10.0391729201018));
#50604=CARTESIAN_POINT('Ctrl Pts',(4.71254519337589,-4.85991812336597,10.0479222635597));
#50605=CARTESIAN_POINT('Ctrl Pts',(4.84439764315085,-4.72849847630998,10.0566716070176));
#50606=CARTESIAN_POINT('Ctrl Pts',(4.97061384196792,-4.59187184425229,10.0654209504755));
#50607=CARTESIAN_POINT('Ctrl Pts',(5.09682908420313,-4.45524624767625,10.0741702276229));
#50608=CARTESIAN_POINT('Ctrl Pts',(5.21740796650278,-4.31341395556763,10.0829195047703));
#50609=CARTESIAN_POINT('Ctrl Pts',(5.33194095942358,-4.16685668162719,10.0916687819176));
#50610=CARTESIAN_POINT('Ctrl Pts',(5.44647312235243,-4.02030046975066,10.1004179956612));
#50611=CARTESIAN_POINT('Ctrl Pts',(5.55495930712401,-3.86901957035386,10.1091672094047));
#50612=CARTESIAN_POINT('Ctrl Pts',(5.65703106079909,-3.713527780582,10.1179164231483));
#50613=CARTESIAN_POINT('Ctrl Pts',(5.75910210868842,-3.55803706597431,10.1266655763945));
#50614=CARTESIAN_POINT('Ctrl Pts',(5.85475865698647,-3.39833575880731,10.1354147296406));
#50615=CARTESIAN_POINT('Ctrl Pts',(5.94367583069153,-3.23496624706556,10.1441638828868));
#50616=CARTESIAN_POINT('Ctrl Pts',(6.03259241910163,-3.07159781069931,10.152912978542));
#50617=CARTESIAN_POINT('Ctrl Pts',(6.11476958471049,-2.90456146975662,10.1616620741971));
#50618=CARTESIAN_POINT('Ctrl Pts',(6.18992823574463,-2.73442451648082,10.1704111698522));
#50619=CARTESIAN_POINT('Ctrl Pts',(6.26508641701014,-2.56428862662224,10.1791602108223));
#50620=CARTESIAN_POINT('Ctrl Pts',(6.33322605570376,-2.39105242531068,10.1879092517925));
#50621=CARTESIAN_POINT('Ctrl Pts',(6.39411573747846,-2.21530425353501,10.1966582927626));
#50622=CARTESIAN_POINT('Ctrl Pts',(6.45500505889195,-2.03955712188341,10.2054072819536));
#50623=CARTESIAN_POINT('Ctrl Pts',(6.5086444154499,-1.86129832025359,10.2141562711446));
#50624=CARTESIAN_POINT('Ctrl Pts',(6.55485164049959,-1.68113324012104,10.2229052603356));
#50625=CARTESIAN_POINT('Ctrl Pts',(6.60199852639157,-1.49730435912689,10.2318321672125));
#50626=CARTESIAN_POINT('Ctrl Pts',(6.64140767441052,-1.31149113173438,10.2407590740893));
#50627=CARTESIAN_POINT('Ctrl Pts',(6.67293975269639,-1.12435050446214,10.2496859809662));
#50628=CARTESIAN_POINT('Ctrl Pts',(6.70384664831538,-0.940920291561549,
10.2584358951502));
#50629=CARTESIAN_POINT('Ctrl Pts',(6.72718585889691,-0.756215114275723,
10.2671858093342));
#50630=CARTESIAN_POINT('Ctrl Pts',(6.74287810451883,-0.570862389372904,
10.2759357235182));
#50631=CARTESIAN_POINT('Ctrl Pts',(6.75857004154136,-0.385513309565947,
10.2846854656288));
#50632=CARTESIAN_POINT('Ctrl Pts',(6.76661529035562,-0.199516993257141,
10.2934352077394));
#50633=CARTESIAN_POINT('Ctrl Pts',(6.76698652348897,-0.0135052182030729,
10.3021849498499));
#50634=CARTESIAN_POINT('Ctrl Pts',(6.76735774981519,0.172503146039862,10.3109345315206));
#50635=CARTESIAN_POINT('Ctrl Pts',(6.76005524147474,0.358526681834424,10.3196841131912));
#50636=CARTESIAN_POINT('Ctrl Pts',(6.74510380214874,0.543933542115802,10.3284336948619));
#50637=CARTESIAN_POINT('Ctrl Pts',(6.73015261710969,0.729337249085682,10.3371831277238));
#50638=CARTESIAN_POINT('Ctrl Pts',(6.70755278444592,0.914124015855645,10.3459325605857));
#50639=CARTESIAN_POINT('Ctrl Pts',(6.67738106408273,1.09766621749486,10.3546819934477));
#50640=CARTESIAN_POINT('Ctrl Pts',(6.64720981677235,1.28120554143418,10.36343128913));
#50641=CARTESIAN_POINT('Ctrl Pts',(6.60946696581502,1.46350005650712,10.3721805848124));
#50642=CARTESIAN_POINT('Ctrl Pts',(6.56428070010972,1.64393062206621,10.3809298804947));
#50643=CARTESIAN_POINT('Ctrl Pts',(6.5190950828272,1.82435859844726,10.3896790506247));
#50644=CARTESIAN_POINT('Ctrl Pts',(6.46646633415642,2.00292240086623,10.3984282207547));
#50645=CARTESIAN_POINT('Ctrl Pts',(6.40657319597176,2.17901557696501,10.4071773908847));
#50646=CARTESIAN_POINT('Ctrl Pts',(6.34668083768276,2.35510646007485,10.4159264470877));
#50647=CARTESIAN_POINT('Ctrl Pts',(6.27952437143864,2.52872650996584,10.4246755032908));
#50648=CARTESIAN_POINT('Ctrl Pts',(6.20533187335111,2.69928607997982,10.4334245594939));
#50649=CARTESIAN_POINT('Ctrl Pts',(6.12831449784228,2.87633970115448,10.4425067357827));
#50650=CARTESIAN_POINT('Ctrl Pts',(6.0437148946313,3.05009490562395,10.4515889120716));
#50651=CARTESIAN_POINT('Ctrl Pts',(5.95184265120469,3.21991584599672,10.4606710883604));
#50652=CARTESIAN_POINT('Ctrl Pts',(5.86333281335467,3.38352155905345,10.4694208687148));
#50653=CARTESIAN_POINT('Ctrl Pts',(5.76807337235655,3.54347560903872,10.4781706490692));
#50654=CARTESIAN_POINT('Ctrl Pts',(5.66638790086322,3.69923467178698,10.4869204294237));
#50655=CARTESIAN_POINT('Ctrl Pts',(5.56470608502706,3.85498813489817,10.4956698952179));
#50656=CARTESIAN_POINT('Ctrl Pts',(5.45659885766912,4.00654667256316,10.5044193610122));
#50657=CARTESIAN_POINT('Ctrl Pts',(5.34243340580464,4.15339551506267,10.5131688268065));
#50658=CARTESIAN_POINT('Ctrl Pts',(5.22827145140547,4.30023985883927,10.5219180245603));
#50659=CARTESIAN_POINT('Ctrl Pts',(5.1080518197804,4.44237456993099,10.5306672223142));
#50660=CARTESIAN_POINT('Ctrl Pts',(4.982182812825,4.57931691626505,10.5394164200681));
#50661=CARTESIAN_POINT('Ctrl Pts',(4.8563169929618,4.71625579512211,10.5481653962861));
#50662=CARTESIAN_POINT('Ctrl Pts',(4.72480227791793,4.84800236135813,10.5569143725041));
#50663=CARTESIAN_POINT('Ctrl Pts',(4.58808530848072,4.97410918678947,10.5656633487221));
#50664=CARTESIAN_POINT('Ctrl Pts',(4.45135945056924,5.1002242108905,10.5744128937433));
#50665=CARTESIAN_POINT('Ctrl Pts',(4.30943087207988,5.2206985661203,10.5831624387645));
#50666=CARTESIAN_POINT('Ctrl Pts',(4.1627816432241,5.33512305301729,10.5919119837857));
#50667=CARTESIAN_POINT('Ctrl Pts',(4.01614103534319,5.4495408133148,10.6006610144529));
#50668=CARTESIAN_POINT('Ctrl Pts',(3.86478055833327,5.55790924068398,10.6094100451202));
#50669=CARTESIAN_POINT('Ctrl Pts',(3.70921425811851,5.65986029751357,10.6181590757875));
#50670=CARTESIAN_POINT('Ctrl Pts',(3.55364584530017,5.76181273884718,10.6269082252673));
#50671=CARTESIAN_POINT('Ctrl Pts',(3.39387173464239,5.85734747818125,10.6356573747472));
#50672=CARTESIAN_POINT('Ctrl Pts',(3.23043456092297,5.94614005448866,10.644406524227));
#50673=CARTESIAN_POINT('Ctrl Pts',(3.18690768806317,5.96978744811321,10.64673661296));
#50674=CARTESIAN_POINT('Ctrl Pts',(3.14312114982841,5.99295688499321,10.6490667016931));
#50675=CARTESIAN_POINT('Ctrl Pts',(3.09908550384714,6.01564277861016,10.6513967904261));
#50676=CARTESIAN_POINT('Origin',(0.,0.,-63.6971797838103));
#50677=CARTESIAN_POINT('',(3.09908550384717,6.01564277861014,13.0457845165097));
#50678=CARTESIAN_POINT('',(3.09908550384725,6.0156427786101,12.6512833602796));
#50679=CARTESIAN_POINT('',(3.09908550384721,6.01564277861012,-63.6971797838103));
#50680=CARTESIAN_POINT('',(-6.76699966570739,-0.00212704398872074,11.6971797837775));
#50681=CARTESIAN_POINT('Ctrl Pts',(-6.76699966570717,-0.00212704467573977,
11.6971797838099));
#50682=CARTESIAN_POINT('Ctrl Pts',(-6.76692897361369,-0.22702752675126,
11.7077762688185));
#50683=CARTESIAN_POINT('Ctrl Pts',(-6.75564229943246,-0.451681332267032,
11.7183727538272));
#50684=CARTESIAN_POINT('Ctrl Pts',(-6.73323789820075,-0.675126955641032,
11.7289692388358));
#50685=CARTESIAN_POINT('Ctrl Pts',(-6.72842056772625,-0.723171596501596,
11.7312476648302));
#50686=CARTESIAN_POINT('Ctrl Pts',(-6.72308942464251,-0.771160425130636,
11.7335260908246));
#50687=CARTESIAN_POINT('Ctrl Pts',(-6.71724575091993,-0.819083952808324,
11.7358045168189));
#50688=CARTESIAN_POINT('Ctrl Pts',(-6.69591375023501,-0.994026082327715,
11.7441217821523));
#50689=CARTESIAN_POINT('Ctrl Pts',(-6.6677226297911,-1.16830334640407,11.7524390474857));
#50690=CARTESIAN_POINT('Ctrl Pts',(-6.6327277204654,-1.34134707893591,11.7607563128191));
#50691=CARTESIAN_POINT('Ctrl Pts',(-6.59776232665293,-1.51424486239472,
11.7690665631792));
#50692=CARTESIAN_POINT('Ctrl Pts',(-6.55600464577617,-1.68591084794382,
11.7773768135394));
#50693=CARTESIAN_POINT('Ctrl Pts',(-6.50756161391943,-1.85578308027698,
11.7856870638994));
#50694=CARTESIAN_POINT('Ctrl Pts',(-6.45915056824995,-2.02554314859347,
11.7939918271293));
#50695=CARTESIAN_POINT('Ctrl Pts',(-6.40406306257704,-2.19351149035547,
11.8022965903592));
#50696=CARTESIAN_POINT('Ctrl Pts',(-6.34245680869598,-2.35913768776348,
11.810601353589));
#50697=CARTESIAN_POINT('Ctrl Pts',(-6.28087995505695,-2.52468484367839,
11.8189021535516));
#50698=CARTESIAN_POINT('Ctrl Pts',(-6.21279067400815,-2.68789175744743,
11.8272029535143));
#50699=CARTESIAN_POINT('Ctrl Pts',(-6.13839616548183,-2.84822427410448,
11.8355037534769));
#50700=CARTESIAN_POINT('Ctrl Pts',(-6.06402354635039,-3.00850961548154,
11.8438021110618));
#50701=CARTESIAN_POINT('Ctrl Pts',(-5.98334954395937,-3.16592193042428,
11.8521004686467));
#50702=CARTESIAN_POINT('Ctrl Pts',(-5.89662911271887,-3.31994790727751,
11.8603988262316));
#50703=CARTESIAN_POINT('Ctrl Pts',(-5.80989985787322,-3.47398955592091,
11.8686980281554));
#50704=CARTESIAN_POINT('Ctrl Pts',(-5.71712310901313,-3.62464387126268,
11.8769972300792));
#50705=CARTESIAN_POINT('Ctrl Pts',(-5.61859960818609,-3.77142246942597,
11.885296432003));
#50706=CARTESIAN_POINT('Ctrl Pts',(-5.52006611894369,-3.91821594815677,
11.8935964753085));
#50707=CARTESIAN_POINT('Ctrl Pts',(-5.41578490998046,-4.06113263727009,
11.901896518614));
#50708=CARTESIAN_POINT('Ctrl Pts',(-5.30609980771636,-4.19971354148737,
11.9101965619195));
#50709=CARTESIAN_POINT('Ctrl Pts',(-5.19638537749535,-4.33833149991442,
11.9184988245175));
#50710=CARTESIAN_POINT('Ctrl Pts',(-5.08126439006012,-4.47261108999051,
11.9268010871154));
#50711=CARTESIAN_POINT('Ctrl Pts',(-4.96112078117622,-4.60212663825991,
11.9351033497133));
#50712=CARTESIAN_POINT('Ctrl Pts',(-4.84092510141443,-4.73169831925547,
11.9434092105559));
#50713=CARTESIAN_POINT('Ctrl Pts',(-4.71570269820271,-4.85650158844747,
11.9517150713985));
#50714=CARTESIAN_POINT('Ctrl Pts',(-4.58587427479379,-4.9761477204545,11.9600209322411));
#50715=CARTESIAN_POINT('Ctrl Pts',(-4.45589238502848,-5.09593528263109,
11.9683366111973));
#50716=CARTESIAN_POINT('Ctrl Pts',(-4.32129385294283,-5.21055329179029,
11.9766522901534));
#50717=CARTESIAN_POINT('Ctrl Pts',(-4.1825332742568,-5.31965265874895,11.9849679691095));
#50718=CARTESIAN_POINT('Ctrl Pts',(-4.04368493060976,-5.4288210301884,11.9932889076664));
#50719=CARTESIAN_POINT('Ctrl Pts',(-3.90066957185888,-5.53246359462947,
12.0016098462233));
#50720=CARTESIAN_POINT('Ctrl Pts',(-3.75397077761656,-5.63027462925219,
12.0099307847801));
#50721=CARTESIAN_POINT('Ctrl Pts',(-3.60705394352661,-5.72823104136896,
12.018264090829));
#50722=CARTESIAN_POINT('Ctrl Pts',(-3.45644302955745,-5.8203384207047,12.026597396878));
#50723=CARTESIAN_POINT('Ctrl Pts',(-3.3026473813108,-5.90633636654068,12.0349307029269));
#50724=CARTESIAN_POINT('Ctrl Pts',(-3.18944470408375,-5.96963593200723,
12.0410645081785));
#50725=CARTESIAN_POINT('Ctrl Pts',(-3.07451710530569,-6.0296264745796,12.0471983134301));
#50726=CARTESIAN_POINT('Ctrl Pts',(-2.95807432651365,-6.08622093575486,
12.0533321186817));
#50727=CARTESIAN_POINT('Ctrl Pts',(-2.8048484335932,-6.16069302357251,12.0614035319237));
#50728=CARTESIAN_POINT('Ctrl Pts',(-2.64852642815876,-6.22951188052598,
12.0694749451657));
#50729=CARTESIAN_POINT('Ctrl Pts',(-2.48957238179492,-6.29240163656167,
12.0775463584078));
#50730=CARTESIAN_POINT('Ctrl Pts',(-2.33081788907027,-6.35521243971776,
12.085607638659));
#50731=CARTESIAN_POINT('Ctrl Pts',(-2.16943827254946,-6.41210881713044,
12.0936689189102));
#50732=CARTESIAN_POINT('Ctrl Pts',(-2.00592312754502,-6.4628601568021,12.1017301991615));
#50733=CARTESIAN_POINT('Ctrl Pts',(-1.84257740263408,-6.5135589123739,12.1097831270191));
#50734=CARTESIAN_POINT('Ctrl Pts',(-1.67710090565475,-6.55812519100345,
12.1178360548767));
#50735=CARTESIAN_POINT('Ctrl Pts',(-1.51000409965097,-6.5963760216529,12.1258889827343));
#50736=CARTESIAN_POINT('Ctrl Pts',(-1.34304383437945,-6.63459559619068,
12.1339353302587));
#50737=CARTESIAN_POINT('Ctrl Pts',(-1.17446625702939,-6.66650991125675,
12.1419816777831));
#50738=CARTESIAN_POINT('Ctrl Pts',(-1.00479781975984,-6.69198553057356,
12.1500280253074));
#50739=CARTESIAN_POINT('Ctrl Pts',(-0.835230909908369,-6.71744590560631,
12.1580695580006));
#50740=CARTESIAN_POINT('Ctrl Pts',(-0.664574807488492,-6.73647519952897,
12.1661110906938));
#50741=CARTESIAN_POINT('Ctrl Pts',(-0.493366904661608,-6.7489908947475,
12.174152623387));
#50742=CARTESIAN_POINT('Ctrl Pts',(-0.318867574845682,-6.76174720092118,
12.1823487524352));
#50743=CARTESIAN_POINT('Ctrl Pts',(-0.143795398482077,-6.76773682818488,
12.1905448814834));
#50744=CARTESIAN_POINT('Ctrl Pts',(0.031273837992906,-6.76692773325216,
12.1987410105317));
#50745=CARTESIAN_POINT('Ctrl Pts',(0.20298160555235,-6.76613417358721,12.2067797673678));
#50746=CARTESIAN_POINT('Ctrl Pts',(0.374686158268147,-6.75880063125281,
12.2148185242039));
#50747=CARTESIAN_POINT('Ctrl Pts',(0.545843502883641,-6.74494950836251,
12.22285728104));
#50748=CARTESIAN_POINT('Ctrl Pts',(0.717017413721061,-6.73109704482992,
12.2308968159428));
#50749=CARTESIAN_POINT('Ctrl Pts',(0.887643638714671,-6.71072577466029,
12.2389363508456));
#50750=CARTESIAN_POINT('Ctrl Pts',(1.05718291976407,-6.68391002887974,12.2469758857484));
#50751=CARTESIAN_POINT('Ctrl Pts',(1.22677217926078,-6.6570863780914,12.2550177906239));
#50752=CARTESIAN_POINT('Ctrl Pts',(1.39527348834118,-6.62381452857332,12.2630596954994));
#50753=CARTESIAN_POINT('Ctrl Pts',(1.56215754477672,-6.58421998457655,12.2711016003749));
#50754=CARTESIAN_POINT('Ctrl Pts',(1.73467098131165,-6.54328982624501,12.2794147770557));
#50755=CARTESIAN_POINT('Ctrl Pts',(1.90545572464091,-6.49560305495819,12.2877279537366));
#50756=CARTESIAN_POINT('Ctrl Pts',(2.07394491517358,-6.44135401051873,12.2960411304174));
#50757=CARTESIAN_POINT('Ctrl Pts',(2.23721903586767,-6.38878408006001,12.3040969980279));
#50758=CARTESIAN_POINT('Ctrl Pts',(2.39833726918149,-6.33005224939568,12.3121528656384));
#50759=CARTESIAN_POINT('Ctrl Pts',(2.55680537338761,-6.26538388948485,12.320208733249));
#50760=CARTESIAN_POINT('Ctrl Pts',(2.72286582193264,-6.1976172123528,12.328650564465));
#50761=CARTESIAN_POINT('Ctrl Pts',(2.88601551180843,-6.12333136418268,12.337092395681));
#50762=CARTESIAN_POINT('Ctrl Pts',(3.0457166531056,-6.04283865985145,12.3455342268969));
#50763=CARTESIAN_POINT('Ctrl Pts',(3.2054177944027,-5.96234595552025,12.3539760581129));
#50764=CARTESIAN_POINT('Ctrl Pts',(3.36167002544971,-5.87564669358153,12.3624178893289));
#50765=CARTESIAN_POINT('Ctrl Pts',(3.5139728457726,-5.78310330524822,12.3708597205448));
#50766=CARTESIAN_POINT('Ctrl Pts',(3.66246215329503,-5.69287711232376,12.3790901766114));
#50767=CARTESIAN_POINT('Ctrl Pts',(3.80769153283813,-5.59679618283451,12.387320632678));
#50768=CARTESIAN_POINT('Ctrl Pts',(3.94916801048369,-5.49512156598671,12.3955510887446));
#50769=CARTESIAN_POINT('Ctrl Pts',(4.09047654721358,-5.39356764290044,12.4037717747748));
#50770=CARTESIAN_POINT('Ctrl Pts',(4.22804076450014,-5.28643346142516,12.411992460805));
#50771=CARTESIAN_POINT('Ctrl Pts',(4.36139318572993,-5.17402536517444,12.4202131468352));
#50772=CARTESIAN_POINT('Ctrl Pts',(4.49461406439839,-5.06172815141659,12.4284257237506));
#50773=CARTESIAN_POINT('Ctrl Pts',(4.62363114867729,-4.94416761276181,12.436638300666));
#50774=CARTESIAN_POINT('Ctrl Pts',(4.74800674596515,-4.82169274635677,12.4448508775814));
#50775=CARTESIAN_POINT('Ctrl Pts',(4.87228460030948,-4.69931412916951,12.453057000486));
#50776=CARTESIAN_POINT('Ctrl Pts',(4.99192797856486,-4.57202912693668,12.4612631233907));
#50777=CARTESIAN_POINT('Ctrl Pts',(5.1065329780435,-4.44022633929332,12.4694692462953));
#50778=CARTESIAN_POINT('Ctrl Pts',(5.22107089213271,-4.30850070396773,12.4776705656491));
#50779=CARTESIAN_POINT('Ctrl Pts',(5.3305760681249,-4.17226282128462,12.4858718850028));
#50780=CARTESIAN_POINT('Ctrl Pts',(5.43468207912903,-4.03193746216305,12.4940732043565));
#50781=CARTESIAN_POINT('Ctrl Pts',(5.53875822458536,-3.89165235906205,12.502272170946));
#50782=CARTESIAN_POINT('Ctrl Pts',(5.63743807373739,-3.74728240041451,12.5104711375355));
#50783=CARTESIAN_POINT('Ctrl Pts',(5.73039591163477,-3.59928488674063,12.5186701041251));
#50784=CARTESIAN_POINT('Ctrl Pts',(5.82334147402965,-3.45130691680714,12.526867988004));
#50785=CARTESIAN_POINT('Ctrl Pts',(5.91056633870804,-3.29970264905851,12.535065871883));
#50786=CARTESIAN_POINT('Ctrl Pts',(5.99178851202737,-3.14495777827571,12.5432637557619));
#50787=CARTESIAN_POINT('Ctrl Pts',(6.07301471383325,-2.99020523240117,12.5514620462424));
#50788=CARTESIAN_POINT('Ctrl Pts',(6.14823746442675,-2.83231209069919,12.559660336723));
#50789=CARTESIAN_POINT('Ctrl Pts',(6.21722104690627,-2.67178806305923,12.5678586272035));
#50790=CARTESIAN_POINT('Ctrl Pts',(6.28622058189078,-2.51122691411791,12.5760588135448));
#50791=CARTESIAN_POINT('Ctrl Pts',(6.34897793354415,-2.34803399690603,12.5842589998862));
#50792=CARTESIAN_POINT('Ctrl Pts',(6.40530576726585,-2.1827384240515,12.5924591862275));
#50793=CARTESIAN_POINT('Ctrl Pts',(6.46168685453462,-2.01728657720262,12.6006671252016));
#50794=CARTESIAN_POINT('Ctrl Pts',(6.51162616367455,-1.84972844299934,12.6088750641757));
#50795=CARTESIAN_POINT('Ctrl Pts',(6.55498617095785,-1.68060860956719,12.6170830031498));
#50796=CARTESIAN_POINT('Ctrl Pts',(6.59836721349436,-1.51140673098,12.6252949240438));
#50797=CARTESIAN_POINT('Ctrl Pts',(6.63516251493869,-1.3406419929803,12.6335068449378));
#50798=CARTESIAN_POINT('Ctrl Pts',(6.66528585000365,-1.16886848607579,12.6417187658317));
#50799=CARTESIAN_POINT('Ctrl Pts',(6.69545049445055,-0.996859419018739,
12.6499419480743));
#50800=CARTESIAN_POINT('Ctrl Pts',(6.71892483917329,-0.823839173858465,
12.6581651303169));
#50801=CARTESIAN_POINT('Ctrl Pts',(6.73567451233863,-0.650367483682722,
12.6663883125594));
#50802=CARTESIAN_POINT('Ctrl Pts',(6.75061099370125,-0.495674514949851,
12.6737213158422));
#50803=CARTESIAN_POINT('Ctrl Pts',(6.76020064985613,-0.340622766822271,
12.681054319125));
#50804=CARTESIAN_POINT('Ctrl Pts',(6.76445405791795,-0.18560791555702,12.6883873224078));
#50805=CARTESIAN_POINT('Ctrl Pts',(6.76963679056211,0.00327603780625371,
12.6973225091901));
#50806=CARTESIAN_POINT('Ctrl Pts',(6.76690717688361,0.192497154869291,12.7062576959724));
#50807=CARTESIAN_POINT('Ctrl Pts',(6.75624313107965,0.381402351512242,12.7151928827547));
#50808=CARTESIAN_POINT('Ctrl Pts',(6.74559505671733,0.570024626609443,12.7241146873913));
#50809=CARTESIAN_POINT('Ctrl Pts',(6.72703627610263,0.758331668059542,12.7330364920279));
#50810=CARTESIAN_POINT('Ctrl Pts',(6.70059667928441,0.945670736336247,12.7419582966646));
#50811=CARTESIAN_POINT('Ctrl Pts',(6.67422157491306,1.13255284019742,12.7508583389038));
#50812=CARTESIAN_POINT('Ctrl Pts',(6.64000405656431,1.31847142794225,12.7597583811431));
#50813=CARTESIAN_POINT('Ctrl Pts',(6.59802559765879,1.50277982839781,12.7686584233824));
#50814=CARTESIAN_POINT('Ctrl Pts',(6.55611176520797,1.686804483361,12.7775447638758));
#50815=CARTESIAN_POINT('Ctrl Pts',(6.50646088260922,1.86922364518446,12.7864311043692));
#50816=CARTESIAN_POINT('Ctrl Pts',(6.44920564933973,2.04939881246294,12.7953174448626));
#50817=CARTESIAN_POINT('Ctrl Pts',(6.39209680770747,2.22911330328934,12.8041810645345));
#50818=CARTESIAN_POINT('Ctrl Pts',(6.32742249070003,2.40659500294075,12.8130446842065));
#50819=CARTESIAN_POINT('Ctrl Pts',(6.25536536056838,2.58121932539667,12.8219083038784));
#50820=CARTESIAN_POINT('Ctrl Pts',(6.18696120988939,2.74699096303567,12.8303225770321));
#50821=CARTESIAN_POINT('Ctrl Pts',(6.11190422848109,2.91018747026337,12.8387368501858));
#50822=CARTESIAN_POINT('Ctrl Pts',(6.03039281295544,3.07028525082857,12.8471511233395));
#50823=CARTESIAN_POINT('Ctrl Pts',(5.9508578441299,3.22650106310683,12.855361371544));
#50824=CARTESIAN_POINT('Ctrl Pts',(5.8652531850374,3.37961600469497,12.8635716197486));
#50825=CARTESIAN_POINT('Ctrl Pts',(5.77385985034016,3.5291403243042,12.8717818679531));
#50826=CARTESIAN_POINT('Ctrl Pts',(5.68244478962528,3.67870018882505,12.8799940678974));
#50827=CARTESIAN_POINT('Ctrl Pts',(5.58523849739068,3.82466742711152,12.8882062678416));
#50828=CARTESIAN_POINT('Ctrl Pts',(5.48256582694271,3.96658051137752,12.8964184677858));
#50829=CARTESIAN_POINT('Ctrl Pts',(5.37985046602956,4.1085526019551,12.9046340822963));
#50830=CARTESIAN_POINT('Ctrl Pts',(5.27166440730891,4.24646689211029,12.9128496968067));
#50831=CARTESIAN_POINT('Ctrl Pts',(5.15837339904699,4.37989416264874,12.9210653113172));
#50832=CARTESIAN_POINT('Ctrl Pts',(5.04495516994897,4.51347126616313,12.9292901516026));
#50833=CARTESIAN_POINT('Ctrl Pts',(4.92642077185495,4.64255101465771,12.9375149918881));
#50834=CARTESIAN_POINT('Ctrl Pts',(4.80317416396026,4.7667396562708,12.9457398321735));
#50835=CARTESIAN_POINT('Ctrl Pts',(4.67984861232892,4.89100784502589,12.9539699407551));
#50836=CARTESIAN_POINT('Ctrl Pts',(4.55180509367817,5.01037843947844,12.9622000493366));
#50837=CARTESIAN_POINT('Ctrl Pts',(4.41948133383884,5.12449741339091,12.9704301579182));
#50838=CARTESIAN_POINT('Ctrl Pts',(4.28697615609421,5.23877284616782,12.9786715501049));
#50839=CARTESIAN_POINT('Ctrl Pts',(4.1501792934497,5.34778205588775,12.9869129422916));
#50840=CARTESIAN_POINT('Ctrl Pts',(4.00955897379088,5.451213244379,12.9951543344783));
#50841=CARTESIAN_POINT('Ctrl Pts',(3.94835743801168,5.49622912543012,12.9987411977425));
#50842=CARTESIAN_POINT('Ctrl Pts',(3.88643199844304,5.54018898684203,13.0023280610067));
#50843=CARTESIAN_POINT('Ctrl Pts',(3.82382272336396,5.58306983480284,13.0059149242709));
#50844=CARTESIAN_POINT('Ctrl Pts',(3.67635322098209,5.68407112099415,13.0143633999962));
#50845=CARTESIAN_POINT('Ctrl Pts',(3.52475190117989,5.77931344038154,13.0228118757215));
#50846=CARTESIAN_POINT('Ctrl Pts',(3.36949632418923,5.86845665582317,13.0312603514468));
#50847=CARTESIAN_POINT('Ctrl Pts',(3.28052731169263,5.91954006295315,13.0361017398011));
#50848=CARTESIAN_POINT('Ctrl Pts',(3.19035890213008,5.96862135863634,13.0409431281554));
#50849=CARTESIAN_POINT('Ctrl Pts',(3.09908550384717,6.01564277861014,13.0457845165097));
#50850=CARTESIAN_POINT('Ctrl Pts',(3.09908550384726,6.0156427786101,11.0457658645337));
#50851=CARTESIAN_POINT('Ctrl Pts',(2.9397938181652,6.09770525674393,11.0542002828111));
#50852=CARTESIAN_POINT('Ctrl Pts',(2.77731417815122,6.17339906158248,11.0626347010885));
#50853=CARTESIAN_POINT('Ctrl Pts',(2.61218824820048,6.24249642018026,11.0710691193659));
#50854=CARTESIAN_POINT('Ctrl Pts',(2.44692139132781,6.31165275000117,11.0795107360077));
#50855=CARTESIAN_POINT('Ctrl Pts',(2.27900404382807,6.37420126766874,11.0879523526494));
#50856=CARTESIAN_POINT('Ctrl Pts',(2.10899567926727,6.42996315890161,11.0963939692912));
#50857=CARTESIAN_POINT('Ctrl Pts',(2.07975780109613,6.43955303635659,11.0978457505584));
#50858=CARTESIAN_POINT('Ctrl Pts',(2.05045810985601,6.44894230753634,11.0992975318256));
#50859=CARTESIAN_POINT('Ctrl Pts',(2.02109948945974,6.45813021343683,11.1007493130928));
#50860=CARTESIAN_POINT('Ctrl Pts',(1.85646083827064,6.50965458393826,11.1088906803107));
#50861=CARTESIAN_POINT('Ctrl Pts',(1.68964079039257,6.55494474398137,11.1170320475285));
#50862=CARTESIAN_POINT('Ctrl Pts',(1.52115681601926,6.59381308053831,11.1251734147464));
#50863=CARTESIAN_POINT('Ctrl Pts',(1.35281991534155,6.63264748799358,11.1333076751698));
#50864=CARTESIAN_POINT('Ctrl Pts',(1.18282233360269,6.66507114858489,11.1414419355933));
#50865=CARTESIAN_POINT('Ctrl Pts',(1.01169785243365,6.69094585655729,11.1495761960168));
#50866=CARTESIAN_POINT('Ctrl Pts',(0.84069010620479,6.71680291373848,11.1577049075416));
#50867=CARTESIAN_POINT('Ctrl Pts',(0.668557351521036,6.73611985836785,11.1658336190664));
#50868=CARTESIAN_POINT('Ctrl Pts',(0.49584471001288,6.74880930413301,11.1739623305912));
#50869=CARTESIAN_POINT('Ctrl Pts',(0.323214431971352,6.76149269853601,11.1820871656837));
#50870=CARTESIAN_POINT('Ctrl Pts',(0.150005182080456,6.76755486103975,11.1902120007762));
#50871=CARTESIAN_POINT('Ctrl Pts',(-0.0232316446019987,6.76696012184859,
11.1983368358687));
#50872=CARTESIAN_POINT('Ctrl Pts',(-0.196419973149235,6.76636554915634,
11.2064593963909));
#50873=CARTESIAN_POINT('Ctrl Pts',(-0.369635497385828,6.75911778882147,
11.214581956913));
#50874=CARTESIAN_POINT('Ctrl Pts',(-0.542325694487193,6.74523326810119,
11.2227045174352));
#50875=CARTESIAN_POINT('Ctrl Pts',(-0.715025069624446,6.73134800945465,
11.2308275096504));
#50876=CARTESIAN_POINT('Ctrl Pts',(-0.887198696654032,6.71082531120946,
11.2389505018656));
#50877=CARTESIAN_POINT('Ctrl Pts',(-1.05829785887319,6.68373358549729,11.2470734940807));
#50878=CARTESIAN_POINT('Ctrl Pts',(-1.1456387670123,6.66990408512997,11.2512200340619));
#50879=CARTESIAN_POINT('Ctrl Pts',(-1.23269978871727,6.65436366597106,11.255366574043));
#50880=CARTESIAN_POINT('Ctrl Pts',(-1.31940879331736,6.63712659485389,11.2595131140241));
#50881=CARTESIAN_POINT('Ctrl Pts',(-1.50726761912444,6.59978173136066,11.2684967730525));
#50882=CARTESIAN_POINT('Ctrl Pts',(-1.69338053795594,6.55448856373644,11.2774804320809));
#50883=CARTESIAN_POINT('Ctrl Pts',(-1.87710627446768,6.50144299631659,11.2864640911093));
#50884=CARTESIAN_POINT('Ctrl Pts',(-2.0611476498483,6.4483062971739,11.2954631839687));
#50885=CARTESIAN_POINT('Ctrl Pts',(-2.2427934160623,6.38739064456191,11.3044622768281));
#50886=CARTESIAN_POINT('Ctrl Pts',(-2.42141934168466,6.31894115906419,11.3134613696876));
#50887=CARTESIAN_POINT('Ctrl Pts',(-2.60046409518568,6.25033117865115,11.322481562905));
#50888=CARTESIAN_POINT('Ctrl Pts',(-2.7764746166958,6.17415210727052,11.3315017561224));
#50889=CARTESIAN_POINT('Ctrl Pts',(-2.94884595015438,6.09069754316024,11.3405219493398));
#50890=CARTESIAN_POINT('Ctrl Pts',(-3.12139185275069,6.00715846040637,11.3495512777615));
#50891=CARTESIAN_POINT('Ctrl Pts',(-3.2902909919746,5.91632927451426,11.3585806061832));
#50892=CARTESIAN_POINT('Ctrl Pts',(-3.45496337058348,5.81854939894184,11.3676099346049));
#50893=CARTESIAN_POINT('Ctrl Pts',(-3.61986790405356,5.72063167345413,11.3766519925597));
#50894=CARTESIAN_POINT('Ctrl Pts',(-3.78053355632665,5.61574378709345,11.3856940505145));
#50895=CARTESIAN_POINT('Ctrl Pts',(-3.93640770303687,5.50426956057495,11.3947361084692));
#50896=CARTESIAN_POINT('Ctrl Pts',(-4.07167938353012,5.40752929754162,11.4025830439648));
#50897=CARTESIAN_POINT('Ctrl Pts',(-4.20334286747106,5.30582944319444,11.4104299794603));
#50898=CARTESIAN_POINT('Ctrl Pts',(-4.33105680174991,5.19944573777012,11.4182769149559));
#50899=CARTESIAN_POINT('Ctrl Pts',(-4.47189751232059,5.08212763344809,11.4269303792567));
#50900=CARTESIAN_POINT('Ctrl Pts',(-4.60805834060706,4.95900892120961,11.4355838435575));
#50901=CARTESIAN_POINT('Ctrl Pts',(-4.73906523145384,4.83048131473721,11.4442373078582));
#50902=CARTESIAN_POINT('Ctrl Pts',(-4.86995143815756,4.70207210847984,11.4528828005484));
#50903=CARTESIAN_POINT('Ctrl Pts',(-4.99569296083439,4.56826415827005,11.4615282932386));
#50904=CARTESIAN_POINT('Ctrl Pts',(-5.11585029001451,4.42948809798135,11.4701737859288));
#50905=CARTESIAN_POINT('Ctrl Pts',(-5.23962234617609,4.28653719814747,11.4790793634253));
#50906=CARTESIAN_POINT('Ctrl Pts',(-5.35746872426019,4.13831480601132,11.4879849409218));
#50907=CARTESIAN_POINT('Ctrl Pts',(-5.46894983688847,3.98533269396642,11.4968905184184));
#50908=CARTESIAN_POINT('Ctrl Pts',(-5.57696982220859,3.83710018078338,11.5055196065909));
#50909=CARTESIAN_POINT('Ctrl Pts',(-5.67901364914984,3.68439932452288,11.5141486947635));
#50910=CARTESIAN_POINT('Ctrl Pts',(-5.77472180219839,3.52772973840324,11.522777782936));
#50911=CARTESIAN_POINT('Ctrl Pts',(-5.87502991100254,3.3635302487023,11.5318216050946));
#50912=CARTESIAN_POINT('Ctrl Pts',(-5.96837809447859,3.19497138617176,11.5408654272531));
#50913=CARTESIAN_POINT('Ctrl Pts',(-6.05440284903171,3.02266358393333,11.5499092494116));
#50914=CARTESIAN_POINT('Ctrl Pts',(-6.14042760358484,2.8503557816949,11.5589530715702));
#50915=CARTESIAN_POINT('Ctrl Pts',(-6.2191287261133,2.67429936902006,11.5679968937287));
#50916=CARTESIAN_POINT('Ctrl Pts',(-6.29019749782052,2.49513615628736,11.5770407158872));
#50917=CARTESIAN_POINT('Ctrl Pts',(-6.35419382912098,2.33380245030844,11.5851845380637));
#50918=CARTESIAN_POINT('Ctrl Pts',(-6.41198934629365,2.16997942501787,11.5933283602401));
#50919=CARTESIAN_POINT('Ctrl Pts',(-6.46339792467016,2.00418967849092,11.6014721824165));
#50920=CARTESIAN_POINT('Ctrl Pts',(-6.51482563647354,1.8383382277486,11.6096190355895));
#50921=CARTESIAN_POINT('Ctrl Pts',(-6.55986154742279,1.67051894024127,11.6177658887625));
#50922=CARTESIAN_POINT('Ctrl Pts',(-6.59836929786719,1.50126999868901,11.6259127419355));
#50923=CARTESIAN_POINT('Ctrl Pts',(-6.63688350849126,1.33199266340928,11.6340609618499));
#50924=CARTESIAN_POINT('Ctrl Pts',(-6.66886730313274,1.16128555336923,11.6422091817643));
#50925=CARTESIAN_POINT('Ctrl Pts',(-6.694235521968,0.989696810352488,11.6503574016787));
#50926=CARTESIAN_POINT('Ctrl Pts',(-6.71962615788893,0.817956439837697,
11.658512821915));
#50927=CARTESIAN_POINT('Ctrl Pts',(-6.73838949092252,0.64533324160695,11.6666682421514));
#50928=CARTESIAN_POINT('Ctrl Pts',(-6.75049221241431,0.472381085707059,
11.6748236623878));
#50929=CARTESIAN_POINT('Ctrl Pts',(-6.76155111160754,0.314345518364135,
11.682275702851));
#50930=CARTESIAN_POINT('Ctrl Pts',(-6.76704938032223,0.156035544008866,
11.6897277433143));
#50931=CARTESIAN_POINT('Ctrl Pts',(-6.76699966570739,-0.00212704398872441,
11.6971797837775));
#50932=CARTESIAN_POINT('',(-6.767,2.82623737238828E-12,11.3028202161898));
#50933=CARTESIAN_POINT('Ctrl Pts',(3.09908550384714,6.01564277861016,10.6513967904261));
#50934=CARTESIAN_POINT('Ctrl Pts',(2.93373232018321,6.10082796552484,10.6601462383254));
#50935=CARTESIAN_POINT('Ctrl Pts',(2.76486502144417,6.17919158180194,10.6688956862247));
#50936=CARTESIAN_POINT('Ctrl Pts',(2.59305716434341,6.25046746591383,10.6776451341239));
#50937=CARTESIAN_POINT('Ctrl Pts',(2.4212506945927,6.32174277447229,10.6863945113714));
#50938=CARTESIAN_POINT('Ctrl Pts',(2.24650397871044,6.38593035557831,10.6951438886188));
#50939=CARTESIAN_POINT('Ctrl Pts',(2.06941053323755,6.44281220003544,10.7038932658662));
#50940=CARTESIAN_POINT('Ctrl Pts',(1.89231845896654,6.49969360406694,10.7126425753688));
#50941=CARTESIAN_POINT('Ctrl Pts',(1.71287996431462,6.54926929700892,10.7213918848714));
#50942=CARTESIAN_POINT('Ctrl Pts',(1.53170449173448,6.59137090065492,10.730141194374));
#50943=CARTESIAN_POINT('Ctrl Pts',(1.35053036178113,6.63347219230095,10.7388904390386));
#50944=CARTESIAN_POINT('Ctrl Pts',(1.16761955878787,6.66809944062464,10.7476396837032));
#50945=CARTESIAN_POINT('Ctrl Pts',(0.983593309309904,6.695135039854,10.7563889283678));
#50946=CARTESIAN_POINT('Ctrl Pts',(0.799568362459278,6.72217044771223,10.765138111101));
#50947=CARTESIAN_POINT('Ctrl Pts',(0.614428268437771,6.74161427235985,10.7738872938342));
#50948=CARTESIAN_POINT('Ctrl Pts',(0.428801816329323,6.75340047696808,10.7826364765673));
#50949=CARTESIAN_POINT('Ctrl Pts',(0.243176616522011,6.76518660206244,10.7913856002755));
#50950=CARTESIAN_POINT('Ctrl Pts',(0.0570653511648604,6.76931519233997,
10.8001347239836));
#50951=CARTESIAN_POINT('Ctrl Pts',(-0.128899900800456,6.76577222610794,
10.8088838476917));
#50952=CARTESIAN_POINT('Ctrl Pts',(-0.314863959942527,6.76222928260131,
10.817632915281));
#50953=CARTESIAN_POINT('Ctrl Pts',(-0.500681721081265,6.75101488651272,
10.8263819828702));
#50954=CARTESIAN_POINT('Ctrl Pts',(-0.68572211017396,6.73216712415984,10.8351310504595));
#50955=CARTESIAN_POINT('Ctrl Pts',(-0.870761373828175,6.71331947644137,
10.8438800648359));
#50956=CARTESIAN_POINT('Ctrl Pts',(-1.05502298984389,6.68683858439989,10.8526290792122));
#50957=CARTESIAN_POINT('Ctrl Pts',(-1.23788117676096,6.65281438131419,10.8613780935886));
#50958=CARTESIAN_POINT('Ctrl Pts',(-1.43009641451827,6.6170491230237,10.8705748044761));
#50959=CARTESIAN_POINT('Ctrl Pts',(-1.62076048992727,6.57294837083157,10.8797715153636));
#50960=CARTESIAN_POINT('Ctrl Pts',(-1.8091579896116,6.52067760042041,10.8889682262511));
#50961=CARTESIAN_POINT('Ctrl Pts',(-1.98840443003043,6.47094578577399,10.8977182239576));
#50962=CARTESIAN_POINT('Ctrl Pts',(-2.16559895952225,6.41381888474464,10.9064682216642));
#50963=CARTESIAN_POINT('Ctrl Pts',(-2.34013966242358,6.34949095285221,10.9152182193707));
#50964=CARTESIAN_POINT('Ctrl Pts',(-2.51467682554045,6.28516432556673,10.9239680396223));
#50965=CARTESIAN_POINT('Ctrl Pts',(-2.68656000078867,6.2136370587965,10.9327178598739));
#50966=CARTESIAN_POINT('Ctrl Pts',(-2.85520533840907,6.1351521151085,10.9414676801255));
#50967=CARTESIAN_POINT('Ctrl Pts',(-3.02384747998342,6.05666865881114,10.9502173345567));
#50968=CARTESIAN_POINT('Ctrl Pts',(-3.18925164684548,5.97122791039838,10.9589669889879));
#50969=CARTESIAN_POINT('Ctrl Pts',(-3.35085601829165,5.87912008251904,10.9677166434192));
#50970=CARTESIAN_POINT('Ctrl Pts',(-3.51245754191425,5.7870138777817,10.9764661436623));
#50971=CARTESIAN_POINT('Ctrl Pts',(-3.67025915510942,5.68824097060979,10.9852156439055));
#50972=CARTESIAN_POINT('Ctrl Pts',(-3.8237248792884,5.58313684656851,10.9939651441486));
#50973=CARTESIAN_POINT('Ctrl Pts',(-3.97718810300802,5.4780344350177,11.0027145018337));
#50974=CARTESIAN_POINT('Ctrl Pts',(-4.12631534263029,5.36660117496373,11.0114638595188));
#50975=CARTESIAN_POINT('Ctrl Pts',(-4.27060009886228,5.24921554097348,11.020213217204));
#50976=CARTESIAN_POINT('Ctrl Pts',(-4.41488269594226,5.13183166360281,11.0289624439591));
#50977=CARTESIAN_POINT('Ctrl Pts',(-4.5543227323511,5.00849577139452,11.0377116707143));
#50978=CARTESIAN_POINT('Ctrl Pts',(-4.68844662480237,4.87962675277313,11.0464608974695));
#50979=CARTESIAN_POINT('Ctrl Pts',(-4.82256868835201,4.75075949139838,11.055210004921));
#50980=CARTESIAN_POINT('Ctrl Pts',(-4.95137454637918,4.61635945312466,11.0639591123725));
#50981=CARTESIAN_POINT('Ctrl Pts',(-5.07442674461144,4.47688309134515,11.072708219824));
#50982=CARTESIAN_POINT('Ctrl Pts',(-5.19747742838585,4.33740844616295,11.0814572195964));
#50983=CARTESIAN_POINT('Ctrl Pts',(-5.31477440450955,4.19285781735993,11.0902062193687));
#50984=CARTESIAN_POINT('Ctrl Pts',(-5.42591931531163,4.04372211999392,11.0989552191411));
#50985=CARTESIAN_POINT('Ctrl Pts',(-5.53707636462999,3.89457013500777,11.1077051744217));
#50986=CARTESIAN_POINT('Ctrl Pts',(-5.64207983273493,3.74083230916387,11.1164551297023));
#50987=CARTESIAN_POINT('Ctrl Pts',(-5.74057303468775,3.58303087251783,11.1252050849829));
#50988=CARTESIAN_POINT('Ctrl Pts',(-5.83906243363789,3.42523552887389,11.1339547024117));
#50989=CARTESIAN_POINT('Ctrl Pts',(-5.93104191768447,3.26337713156954,11.1427043198405));
#50990=CARTESIAN_POINT('Ctrl Pts',(-6.01619906699674,3.0980054529112,11.1514539372693));
#50991=CARTESIAN_POINT('Ctrl Pts',(-6.10135338095403,2.93263928039554,11.1602032633747));
#50992=CARTESIAN_POINT('Ctrl Pts',(-6.1796856835286,2.76376031540178,11.16895258948));
#50993=CARTESIAN_POINT('Ctrl Pts',(-6.25092992694908,2.59194213831491,11.1777019155854));
#50994=CARTESIAN_POINT('Ctrl Pts',(-6.32217217691122,2.42012876880772,11.1864509968792));
#50995=CARTESIAN_POINT('Ctrl Pts',(-6.38632665483866,2.24537661647625,11.195200078173));
#50996=CARTESIAN_POINT('Ctrl Pts',(-6.44317547869363,2.06827917621415,11.2039491594668));
#50997=CARTESIAN_POINT('Ctrl Pts',(-6.50002944235945,1.89116572423393,11.2126990317818));
#50998=CARTESIAN_POINT('Ctrl Pts',(-6.54957634250403,1.71170683289178,11.2214489040967));
#50999=CARTESIAN_POINT('Ctrl Pts',(-6.59164787708397,1.53051209225356,11.2301987764117));
#51000=CARTESIAN_POINT('Ctrl Pts',(-6.63371649075016,1.34932993147997,11.2389480412465));
#51001=CARTESIAN_POINT('Ctrl Pts',(-6.66831071257135,1.16641244173945,11.2476973060813));
#51002=CARTESIAN_POINT('Ctrl Pts',(-6.69531304840345,0.982380875159165,
11.2564465709161));
#51003=CARTESIAN_POINT('Ctrl Pts',(-6.72231677033054,0.79833986179499,11.2651962848718));
#51004=CARTESIAN_POINT('Ctrl Pts',(-6.74172778477898,0.613184940729295,
11.2739459988274));
#51005=CARTESIAN_POINT('Ctrl Pts',(-6.75348015835523,0.427545027689691,
11.2826957127831));
#51006=CARTESIAN_POINT('Ctrl Pts',(-6.76249038365217,0.285219953547213,
11.2894038805853));
#51007=CARTESIAN_POINT('Ctrl Pts',(-6.76699999999994,0.142609995758956,
11.2961120483876));
#51008=CARTESIAN_POINT('Ctrl Pts',(-6.767,2.82623743936056E-12,11.3028202161898));
#51009=CARTESIAN_POINT('Ctrl Pts',(-6.76699999572935,-0.000240414293744514,
11.3028202161898));
#51010=CARTESIAN_POINT('Ctrl Pts',(-6.76699367167169,-0.178245213700239,
11.3111542497933));
#51011=CARTESIAN_POINT('Ctrl Pts',(-6.75995944046259,-0.35617527161172,
11.3194882833967));
#51012=CARTESIAN_POINT('Ctrl Pts',(-6.74594087271596,-0.533451723982817,
11.3278223170002));
#51013=CARTESIAN_POINT('Ctrl Pts',(-6.73191375254288,-0.710836328901932,
11.3361614350182));
#51014=CARTESIAN_POINT('Ctrl Pts',(-6.7108938272577,-0.887566193870075,
11.3445005530362));
#51015=CARTESIAN_POINT('Ctrl Pts',(-6.68297634044918,-1.06306925127034,
11.3528396710542));
#51016=CARTESIAN_POINT('Ctrl Pts',(-6.65501988782158,-1.23881726698042,
11.3611904283922));
#51017=CARTESIAN_POINT('Ctrl Pts',(-6.62014669057205,-1.41333471678057,
11.3695411857303));
#51018=CARTESIAN_POINT('Ctrl Pts',(-6.57850306471982,-1.58606003274529,
11.3778919430683));
#51019=CARTESIAN_POINT('Ctrl Pts',(-6.53682765482578,-1.75891717941763,
11.3862490740305));
#51020=CARTESIAN_POINT('Ctrl Pts',(-6.48837160213316,-1.92997913682426,
11.3946062049927));
#51021=CARTESIAN_POINT('Ctrl Pts',(-6.43333069050316,-2.09870084257621,
11.4029633359549));
#51022=CARTESIAN_POINT('Ctrl Pts',(-6.378201535987,-2.26769304694154,11.4113338652664));
#51023=CARTESIAN_POINT('Ctrl Pts',(-6.31646654296931,-2.43433718232206,
11.4197043945778));
#51024=CARTESIAN_POINT('Ctrl Pts',(-6.24836964538579,-2.59810811449821,
11.4280749238893));
#51025=CARTESIAN_POINT('Ctrl Pts',(-6.20596974919273,-2.7000785532424,11.4332867556537));
#51026=CARTESIAN_POINT('Ctrl Pts',(-6.16110438861522,-2.80093556954357,
11.4384985874182));
#51027=CARTESIAN_POINT('Ctrl Pts',(-6.11384123733026,-2.9005575885888,11.4437104191826));
#51028=CARTESIAN_POINT('Ctrl Pts',(-6.03722662134645,-3.06204708992703,
11.4521589140111));
#51029=CARTESIAN_POINT('Ctrl Pts',(-5.95414346373569,-3.22063899955504,
11.4606074088395));
#51030=CARTESIAN_POINT('Ctrl Pts',(-5.86483330098463,-3.37579906861497,
11.4690559036679));
#51031=CARTESIAN_POINT('Ctrl Pts',(-5.77560471787926,-3.530817407965,11.477496681287));
#51032=CARTESIAN_POINT('Ctrl Pts',(-5.68016063310411,-3.68240986772118,
11.4859374589062));
#51033=CARTESIAN_POINT('Ctrl Pts',(-5.57878925840906,-3.83006519660693,
11.4943782365254));
#51034=CARTESIAN_POINT('Ctrl Pts',(-5.47749489183758,-3.97760835714293,
11.5028126019947));
#51035=CARTESIAN_POINT('Ctrl Pts',(-5.37028239968252,-4.12122007525554,
11.511246967464));
#51036=CARTESIAN_POINT('Ctrl Pts',(-5.25748441407456,-4.26041625146687,
11.5196813329333));
#51037=CARTESIAN_POINT('Ctrl Pts',(-5.1447547948415,-4.39952806147331,11.5281105863699));
#51038=CARTESIAN_POINT('Ctrl Pts',(-5.02644664106432,-4.53422940688327,
11.5365398398065));
#51039=CARTESIAN_POINT('Ctrl Pts',(-4.90293437746686,-4.66406726905323,
11.5449690932431));
#51040=CARTESIAN_POINT('Ctrl Pts',(-4.77947802770037,-4.79384635380248,
11.5533945307683));
#51041=CARTESIAN_POINT('Ctrl Pts',(-4.6508224952366,-4.9187661043324,11.5618199682935));
#51042=CARTESIAN_POINT('Ctrl Pts',(-4.51738101923936,-5.03840825330937,
11.5702454058187));
#51043=CARTESIAN_POINT('Ctrl Pts',(-4.38396885674569,-5.1580241201238,11.5786689925019));
#51044=CARTESIAN_POINT('Ctrl Pts',(-4.24577309316775,-5.272364472556,11.5870925791851));
#51045=CARTESIAN_POINT('Ctrl Pts',(-4.10324258783639,-5.38104908594651,
11.5955161658683));
#51046=CARTESIAN_POINT('Ctrl Pts',(-3.9607280309213,-5.48972153809861,11.6039388099963));
#51047=CARTESIAN_POINT('Ctrl Pts',(-3.81387996426694,-5.59273931070984,
11.6123614541243));
#51048=CARTESIAN_POINT('Ctrl Pts',(-3.66317921887819,-5.68976335275721,
11.6207840982523));
#51049=CARTESIAN_POINT('Ctrl Pts',(-3.51247432150342,-5.78679006793314,
11.6292069744342));
#51050=CARTESIAN_POINT('Ctrl Pts',(-3.35791681430515,-5.87782254315894,
11.6376298506161));
#51051=CARTESIAN_POINT('Ctrl Pts',(-3.20001561816885,-5.9625656426974,11.6460527267981));
#51052=CARTESIAN_POINT('Ctrl Pts',(-3.04208805165652,-6.04732289480376,
11.6544770096471));
#51053=CARTESIAN_POINT('Ctrl Pts',(-2.88081597690753,-6.12578852000872,
11.6629012924961));
#51054=CARTESIAN_POINT('Ctrl Pts',(-2.71673228491875,-6.19771366651285,
11.6713255753451));
#51055=CARTESIAN_POINT('Ctrl Pts',(-2.55253777687123,-6.26968738860157,
11.6797555476432));
#51056=CARTESIAN_POINT('Ctrl Pts',(-2.38552816289065,-6.33511167145496,
11.6881855199414));
#51057=CARTESIAN_POINT('Ctrl Pts',(-2.21625659696054,-6.39378570929844,
11.6966154922395));
#51058=CARTESIAN_POINT('Ctrl Pts',(-2.04692451917771,-6.45248072216342,
11.7050484781167));
#51059=CARTESIAN_POINT('Ctrl Pts',(-1.87532919410823,-6.50442057503272,
11.7134814639939));
#51060=CARTESIAN_POINT('Ctrl Pts',(-1.70203880756469,-6.54945439693596,
11.7219144498711));
#51061=CARTESIAN_POINT('Ctrl Pts',(-1.52858899492133,-6.59452964968097,
11.7303551940439));
#51062=CARTESIAN_POINT('Ctrl Pts',(-1.35344132944133,-6.63268609947081,
11.7387959382167));
#51063=CARTESIAN_POINT('Ctrl Pts',(-1.17717513952058,-6.66382380401033,
11.7472366823896));
#51064=CARTESIAN_POINT('Ctrl Pts',(-1.07971285546168,-6.68104067246444,
11.751903795275));
#51065=CARTESIAN_POINT('Ctrl Pts',(-0.981908748035641,-6.69611262843616,
11.7565709081603));
#51066=CARTESIAN_POINT('Ctrl Pts',(-0.883861440877113,-6.70902958357844,
11.7612380210457));
#51067=CARTESIAN_POINT('Ctrl Pts',(-0.712826552306661,-6.73156207373501,
11.7693793882636));
#51068=CARTESIAN_POINT('Ctrl Pts',(-0.540711485736337,-6.74757865359124,
11.7775207554814));
#51069=CARTESIAN_POINT('Ctrl Pts',(-0.368058216269429,-6.75698321364176,
11.7856621226993));
#51070=CARTESIAN_POINT('Ctrl Pts',(-0.195555659975322,-6.76637956422664,
11.7937963831228));
#51071=CARTESIAN_POINT('Ctrl Pts',(-0.0225161989652834,-6.76917536405671,
11.8019306435463));
#51072=CARTESIAN_POINT('Ctrl Pts',(0.150510593120949,-6.76532597598655,
11.8100649039698));
#51073=CARTESIAN_POINT('Ctrl Pts',(0.323419352579259,-6.76147921382989,
11.8181936154946));
#51074=CARTESIAN_POINT('Ctrl Pts',(0.496315095855285,-6.75099629715473,
11.8263223270194));
#51075=CARTESIAN_POINT('Ctrl Pts',(0.668645790719264,-6.73388460003239,
11.8344510385443));
#51076=CARTESIAN_POINT('Ctrl Pts',(0.840894304259591,-6.71678106316218,
11.8425758736368));
#51077=CARTESIAN_POINT('Ctrl Pts',(1.01257794249337,-6.69305507688452,11.8507007087293));
#51078=CARTESIAN_POINT('Ctrl Pts',(1.18314735995491,-6.662766041565,11.8588255438218));
#51079=CARTESIAN_POINT('Ctrl Pts',(1.35366902602979,-6.63248548574584,11.866948104344));
#51080=CARTESIAN_POINT('Ctrl Pts',(1.52307673268356,-6.59564560527994,11.8750706648661));
#51081=CARTESIAN_POINT('Ctrl Pts',(1.69082895592043,-6.55235731945542,11.8831932253883));
#51082=CARTESIAN_POINT('Ctrl Pts',(1.85859009475282,-6.50906673297081,11.8913162176035));
#51083=CARTESIAN_POINT('Ctrl Pts',(2.02469521897243,-6.45932714415243,11.8994392098187));
#51084=CARTESIAN_POINT('Ctrl Pts',(2.18861546764281,-6.40330003473167,11.9075622020339));
#51085=CARTESIAN_POINT('Ctrl Pts',(2.27229175918843,-6.37469990277496,11.9117087420149));
#51086=CARTESIAN_POINT('Ctrl Pts',(2.3553989557734,-6.34446217793446,11.915855281996));
#51087=CARTESIAN_POINT('Ctrl Pts',(2.43786844108258,-6.31261328325865,11.9200018219771));
#51088=CARTESIAN_POINT('Ctrl Pts',(2.61654216414868,-6.24361126916906,11.9289854810055));
#51089=CARTESIAN_POINT('Ctrl Pts',(2.7921330226587,-6.167078008446,11.9379691400338));
#51090=CARTESIAN_POINT('Ctrl Pts',(2.96404282747277,-6.08331645707399,11.9469527990622));
#51091=CARTESIAN_POINT('Ctrl Pts',(3.13624797151036,-5.99941100424407,11.9559518919216));
#51092=CARTESIAN_POINT('Ctrl Pts',(3.30475920691669,-5.90825254518361,11.964950984781));
#51093=CARTESIAN_POINT('Ctrl Pts',(3.46900357466484,-5.81018960094785,11.9739500776404));
#51094=CARTESIAN_POINT('Ctrl Pts',(3.63363304955753,-5.71189672651141,11.9829702708578));
#51095=CARTESIAN_POINT('Ctrl Pts',(3.79397543317875,-5.60666709849133,11.9919904640751));
#51096=CARTESIAN_POINT('Ctrl Pts',(3.94948506837573,-5.49489369275486,12.0010106572925));
#51097=CARTESIAN_POINT('Ctrl Pts',(4.10515219601855,-5.3830070884566,12.0100399857142));
#51098=CARTESIAN_POINT('Ctrl Pts',(4.25597660700428,-5.26456361125743,12.0190693141359));
#51099=CARTESIAN_POINT('Ctrl Pts',(4.40144508884287,-5.13999709434753,12.0280986425576));
#51100=CARTESIAN_POINT('Ctrl Pts',(4.54711865191911,-5.01525496375737,12.0371407005124));
#51101=CARTESIAN_POINT('Ctrl Pts',(4.68742100623655,-4.8843726887987,12.0461827584671));
#51102=CARTESIAN_POINT('Ctrl Pts',(4.8218735208686,-4.74782315895888,12.0552248164218));
#51103=CARTESIAN_POINT('Ctrl Pts',(4.93855494613993,-4.62932188878596,12.0630717519175));
#51104=CARTESIAN_POINT('Ctrl Pts',(5.05083123888825,-4.50655313272352,12.0709186874131));
#51105=CARTESIAN_POINT('Ctrl Pts',(5.15841337933475,-4.37984707585782,12.0787656229088));
#51106=CARTESIAN_POINT('Ctrl Pts',(5.27705309700226,-4.24011783501058,12.0874190872096));
#51107=CARTESIAN_POINT('Ctrl Pts',(5.39008766652695,-4.09547629687063,12.0960725515104));
#51108=CARTESIAN_POINT('Ctrl Pts',(5.49711721599856,-3.94638965556777,12.1047260158113));
#51109=CARTESIAN_POINT('Ctrl Pts',(5.60404816936307,-3.79744035355602,12.1133715085014));
#51110=CARTESIAN_POINT('Ctrl Pts',(5.70498495941745,-3.64405436176327,12.1220170011916));
#51111=CARTESIAN_POINT('Ctrl Pts',(5.79956842159314,-3.4867312949609,12.1306624938818));
#51112=CARTESIAN_POINT('Ctrl Pts',(5.89699726486195,-3.32467543376197,12.1395680713784));
#51113=CARTESIAN_POINT('Ctrl Pts',(5.98768433488902,-3.15844215885032,12.1484736488749));
#51114=CARTESIAN_POINT('Ctrl Pts',(6.07128430232286,-2.98861103530855,12.1573792263714));
#51115=CARTESIAN_POINT('Ctrl Pts',(6.15228876166216,-2.82405261783819,12.166008314544));
#51116=CARTESIAN_POINT('Ctrl Pts',(6.22663942259502,-2.65611669750417,12.1746374027165));
#51117=CARTESIAN_POINT('Ctrl Pts',(6.2940677570571,-2.48535713119347,12.1832664908891));
#51118=CARTESIAN_POINT('Ctrl Pts',(6.36473685362026,-2.30639046418374,12.1923103130476));
#51119=CARTESIAN_POINT('Ctrl Pts',(6.42780163725656,-2.12432232704686,12.2013541352061));
#51120=CARTESIAN_POINT('Ctrl Pts',(6.48300865200716,-1.93981643925407,12.2103979573646));
#51121=CARTESIAN_POINT('Ctrl Pts',(6.53821566675777,-1.75531055146122,12.2194417795231));
#51122=CARTESIAN_POINT('Ctrl Pts',(6.58556476898538,-1.56836727223152,12.2284856016816));
#51123=CARTESIAN_POINT('Ctrl Pts',(6.62486185615985,-1.37967184025708,12.2375294238401));
#51124=CARTESIAN_POINT('Ctrl Pts',(6.66147347815302,-1.20387138470126,12.2459552136899));
#51125=CARTESIAN_POINT('Ctrl Pts',(6.69108017067793,-1.0266271008646,12.2543810035397));
#51126=CARTESIAN_POINT('Ctrl Pts',(6.71359061716581,-0.848522259639202,
12.2628067933895));
#51127=CARTESIAN_POINT('Ctrl Pts',(6.73610628683456,-0.670376092098958,
12.271234538306));
#51128=CARTESIAN_POINT('Ctrl Pts',(6.75152238588159,-0.491369297929553,
12.2796622832225));
#51129=CARTESIAN_POINT('Ctrl Pts',(6.75979943308341,-0.312090731174892,
12.288090028139));
#51130=CARTESIAN_POINT('Ctrl Pts',(6.76807952168481,-0.132746288541368,
12.2965208698289));
#51131=CARTESIAN_POINT('Ctrl Pts',(6.7692153126499,0.0468697948018875,12.3049517115188));
#51132=CARTESIAN_POINT('Ctrl Pts',(6.76321943488462,0.226167804072546,12.3133825532087));
#51133=CARTESIAN_POINT('Ctrl Pts',(6.75721804767299,0.405630565328126,12.321821141766));
#51134=CARTESIAN_POINT('Ctrl Pts',(6.74407191035636,0.584774337033546,12.3302597303234));
#51135=CARTESIAN_POINT('Ctrl Pts',(6.72384568996211,0.763012540904812,12.3386983188807));
#51136=CARTESIAN_POINT('Ctrl Pts',(6.70360886383172,0.941344205013449,12.347141332261));
#51137=CARTESIAN_POINT('Ctrl Pts',(6.67628459558111,1.11876902615511,12.3555843456412));
#51138=CARTESIAN_POINT('Ctrl Pts',(6.64198894150593,1.29470919550026,12.3640273590214));
#51139=CARTESIAN_POINT('Ctrl Pts',(6.60765725745575,1.47083420225629,12.3724792423757));
#51140=CARTESIAN_POINT('Ctrl Pts',(6.56633962850735,1.64547111803245,12.38093112573));
#51141=CARTESIAN_POINT('Ctrl Pts',(6.51820263109422,1.8180548561571,12.3893830090843));
#51142=CARTESIAN_POINT('Ctrl Pts',(6.50508377853655,1.86508937712808,12.3916864143135));
#51143=CARTESIAN_POINT('Ctrl Pts',(6.49145871001122,1.91197149993074,12.3939898195427));
#51144=CARTESIAN_POINT('Ctrl Pts',(6.4773314260651,1.95869002062843,12.3962932247719));
#51145=CARTESIAN_POINT('Ctrl Pts',(6.42631507109697,2.12739963562528,12.4046112666019));
#51146=CARTESIAN_POINT('Ctrl Pts',(6.36865392812675,2.29427782756339,12.4129293084319));
#51147=CARTESIAN_POINT('Ctrl Pts',(6.30450005681102,2.45877368492302,12.4212473502619));
#51148=CARTESIAN_POINT('Ctrl Pts',(6.24040189617653,2.62312669546625,12.4295581687745));
#51149=CARTESIAN_POINT('Ctrl Pts',(6.16982236764962,2.78510117112147,12.4378689872871));
#51150=CARTESIAN_POINT('Ctrl Pts',(6.09296322397741,2.9441617060309,12.4461798057997));
#51151=CARTESIAN_POINT('Ctrl Pts',(6.01392927394398,3.10772301790209,12.4547257872363));
#51152=CARTESIAN_POINT('Ctrl Pts',(5.92825518985636,3.26820269193904,12.463271768673));
#51153=CARTESIAN_POINT('Ctrl Pts',(5.83621387980417,3.42503964198682,12.4718177501097));
#51154=CARTESIAN_POINT('Ctrl Pts',(5.74681276250543,3.57737774495436,12.4801185912039));
#51155=CARTESIAN_POINT('Ctrl Pts',(5.65140485702718,3.72627890193112,12.4884194322982));
#51156=CARTESIAN_POINT('Ctrl Pts',(5.55028720305213,3.87125315158229,12.4967202733924));
#51157=CARTESIAN_POINT('Ctrl Pts',(5.44919593882082,4.01618956577005,12.5050189481284));
#51158=CARTESIAN_POINT('Ctrl Pts',(5.34239809400194,4.15720082965892,12.5133176228644));
#51159=CARTESIAN_POINT('Ctrl Pts',(5.23023413478742,4.29382578772177,12.5216162976004));
#51160=CARTESIAN_POINT('Ctrl Pts',(5.1180808301031,4.43043776768764,12.5299141840396));
#51161=CARTESIAN_POINT('Ctrl Pts',(5.00056264787511,4.56266400379488,12.5382120704789));
#51162=CARTESIAN_POINT('Ctrl Pts',(4.87806057260666,4.69007612411359,12.5465099569181));
#51163=CARTESIAN_POINT('Ctrl Pts',(4.74916269563243,4.82414039832184,12.5552410738649));
#51164=CARTESIAN_POINT('Ctrl Pts',(4.61474685148551,4.95287409026204,12.5639721908117));
#51165=CARTESIAN_POINT('Ctrl Pts',(4.47530120284403,5.0758219180565,12.5727033077585));
#51166=CARTESIAN_POINT('Ctrl Pts',(4.34269155605801,5.19274251167682,12.5810064018001));
#51167=CARTESIAN_POINT('Ctrl Pts',(4.2055337520006,5.30443073289881,12.5893094958417));
#51168=CARTESIAN_POINT('Ctrl Pts',(4.06428169622938,5.41053632218607,12.5976125898833));
#51169=CARTESIAN_POINT('Ctrl Pts',(3.92298254815063,5.51667728622959,12.6059184521101));
#51170=CARTESIAN_POINT('Ctrl Pts',(3.77758671001731,5.61723170586951,12.614224314337));
#51171=CARTESIAN_POINT('Ctrl Pts',(3.62857748778439,5.71189236725836,12.6225301765638));
#51172=CARTESIAN_POINT('Ctrl Pts',(3.47945071810508,5.80662770267647,12.6308425909549));
#51173=CARTESIAN_POINT('Ctrl Pts',(3.32670517036247,5.89545981713876,12.6391550053459));
#51174=CARTESIAN_POINT('Ctrl Pts',(3.17084976882889,5.97812685910209,12.647467419737));
#51175=CARTESIAN_POINT('Ctrl Pts',(3.14700050283917,5.99077671437157,12.6487393999178));
#51176=CARTESIAN_POINT('Ctrl Pts',(3.12307845892274,6.00328230076835,12.6500113800987));
#51177=CARTESIAN_POINT('Ctrl Pts',(3.09908550384725,6.0156427786101,12.6512833602796));
#51178=CARTESIAN_POINT('Origin',(0.,0.,-63.6971797838103));
#51179=CARTESIAN_POINT('',(3.09908550384723,6.01564277861011,15.0459090623666));
#51180=CARTESIAN_POINT('',(3.09908550384726,6.0156427786101,14.6514674425353));
#51181=CARTESIAN_POINT('',(3.09908550384721,6.01564277861012,-63.6971797838103));
#51182=CARTESIAN_POINT('',(-6.7669990707839,0.00354626703724618,13.697179783782));
#51183=CARTESIAN_POINT('Ctrl Pts',(-6.76699907078421,0.00354626644463786,
13.6971797838099));
#51184=CARTESIAN_POINT('Ctrl Pts',(-6.76709416588778,-0.177914570622926,
13.7057259625698));
#51185=CARTESIAN_POINT('Ctrl Pts',(-6.75988576497314,-0.359512959521169,
13.7142721413297));
#51186=CARTESIAN_POINT('Ctrl Pts',(-6.74536894644925,-0.540635529981356,
13.7228183200896));
#51187=CARTESIAN_POINT('Ctrl Pts',(-6.73108277756305,-0.718880344879146,
13.7312287133789));
#51188=CARTESIAN_POINT('Ctrl Pts',(-6.70971871563235,-0.896663999759646,
13.7396391066682));
#51189=CARTESIAN_POINT('Ctrl Pts',(-6.68132449676958,-1.07340205369036,
13.7480494999575));
#51190=CARTESIAN_POINT('Ctrl Pts',(-6.65224264257796,-1.25442025106941,
13.7566635714526));
#51191=CARTESIAN_POINT('Ctrl Pts',(-6.6157858083811,-1.43434120511028,13.7652776429478));
#51192=CARTESIAN_POINT('Ctrl Pts',(-6.57206171372395,-1.61254266021207,
13.773891714443));
#51193=CARTESIAN_POINT('Ctrl Pts',(-6.52833761906682,-1.79074411531379,
13.7825057859381));
#51194=CARTESIAN_POINT('Ctrl Pts',(-6.47734633166832,-1.96722569930743,
13.7911198574333));
#51195=CARTESIAN_POINT('Ctrl Pts',(-6.41925196146298,-2.14137648610742,
13.7997339289284));
#51196=CARTESIAN_POINT('Ctrl Pts',(-6.36242738610591,-2.31172078062388,
13.8081597187782));
#51197=CARTESIAN_POINT('Ctrl Pts',(-6.29882283260392,-2.47978788974719,
13.8165855086281));
#51198=CARTESIAN_POINT('Ctrl Pts',(-6.22865289128799,-2.64502781835083,
13.8250112984779));
#51199=CARTESIAN_POINT('Ctrl Pts',(-6.15846666818502,-2.81030608817692,
13.8334390433944));
#51200=CARTESIAN_POINT('Ctrl Pts',(-6.08171214942431,-2.97275556438013,
13.8418667883109));
#51201=CARTESIAN_POINT('Ctrl Pts',(-5.99865152927202,-3.13184751071353,
13.8502945332274));
#51202=CARTESIAN_POINT('Ctrl Pts',(-5.915560388509,-3.2909979153555,13.8587253749174));
#51203=CARTESIAN_POINT('Ctrl Pts',(-5.82615867946626,-3.44678803647088,
13.8671562166073));
#51204=CARTESIAN_POINT('Ctrl Pts',(-5.73075406147579,-3.59871461592591,
13.8755870582973));
#51205=CARTESIAN_POINT('Ctrl Pts',(-5.63526177881876,-3.75078079651566,
13.8840256468546));
#51206=CARTESIAN_POINT('Ctrl Pts',(-5.53375574337052,-3.89897606174041,
13.892464235412));
#51207=CARTESIAN_POINT('Ctrl Pts',(-5.42658700588314,-4.04282604963165,
13.9009028239694));
#51208=CARTESIAN_POINT('Ctrl Pts',(-5.31936207384588,-4.18675146609945,
13.9093458373496));
#51209=CARTESIAN_POINT('Ctrl Pts',(-5.20646872196533,-4.32632680021686,
13.9177888507299));
#51210=CARTESIAN_POINT('Ctrl Pts',(-5.08829799717866,-4.46111112750037,
13.9262318641102));
#51211=CARTESIAN_POINT('Ctrl Pts',(-4.97000312580897,-4.59603705511432,
13.9346837474645));
#51212=CARTESIAN_POINT('Ctrl Pts',(-4.84642003064305,-4.72616167770075,
13.9431356308188));
#51213=CARTESIAN_POINT('Ctrl Pts',(-4.71797701471852,-4.85108048671507,
13.9515875141731));
#51214=CARTESIAN_POINT('Ctrl Pts',(-4.68297223506109,-4.88512480865146,
13.9538909194021));
#51215=CARTESIAN_POINT('Ctrl Pts',(-4.64760668654054,-4.91878270383548,
13.9561943246311));
#51216=CARTESIAN_POINT('Ctrl Pts',(-4.61188946415064,-4.95204650326068,
13.9584977298601));
#51217=CARTESIAN_POINT('Ctrl Pts',(-4.48291970587711,-5.07215730371138,
13.9668149951935));
#51218=CARTESIAN_POINT('Ctrl Pts',(-4.34913020695709,-5.18734269351666,
13.9751322605269));
#51219=CARTESIAN_POINT('Ctrl Pts',(-4.21092947632851,-5.29720321918914,
13.9834495258603));
#51220=CARTESIAN_POINT('Ctrl Pts',(-4.072845307382,-5.40697108596171,13.9917597762204));
#51221=CARTESIAN_POINT('Ctrl Pts',(-3.93035759035839,-5.5114228212473,14.0000700265805));
#51222=CARTESIAN_POINT('Ctrl Pts',(-3.7839099957345,-5.61019733558282,14.0083802769406));
#51223=CARTESIAN_POINT('Ctrl Pts',(-3.63755909819999,-5.70890663062903,
14.0166850401705));
#51224=CARTESIAN_POINT('Ctrl Pts',(-3.48725382047601,-5.80194598038974,
14.0249898034004));
#51225=CARTESIAN_POINT('Ctrl Pts',(-3.33346925191896,-5.8889958181774,14.0332945666303));
#51226=CARTESIAN_POINT('Ctrl Pts',(-3.17975807369543,-5.97600411332727,
14.0415953665929));
#51227=CARTESIAN_POINT('Ctrl Pts',(-3.02257121576365,-6.0570284219602,14.0498961665555));
#51228=CARTESIAN_POINT('Ctrl Pts',(-2.86241115851228,-6.131793486381,14.0581969665182));
#51229=CARTESIAN_POINT('Ctrl Pts',(-2.7022982257973,-6.20653655237684,14.0664953241031));
#51230=CARTESIAN_POINT('Ctrl Pts',(-2.53921415233772,-6.27502389822606,
14.074793681688));
#51231=CARTESIAN_POINT('Ctrl Pts',(-2.37368453368196,-6.33702696337637,
14.083092039273));
#51232=CARTESIAN_POINT('Ctrl Pts',(-2.20813807276732,-6.39903633719628,
14.0913912411968));
#51233=CARTESIAN_POINT('Ctrl Pts',(-2.04014589254418,-6.45455998300652,
14.0996904431206));
#51234=CARTESIAN_POINT('Ctrl Pts',(-1.87025256883398,-6.50341789590442,
14.1079896450443));
#51235=CARTESIAN_POINT('Ctrl Pts',(-1.70034202116121,-6.55228076206855,
14.1162896883499));
#51236=CARTESIAN_POINT('Ctrl Pts',(-1.52853028014549,-6.59447645164882,
14.1245897316554));
#51237=CARTESIAN_POINT('Ctrl Pts',(-1.35537596122062,-6.62987518764458,
14.132889774961));
#51238=CARTESIAN_POINT('Ctrl Pts',(-1.18217534373489,-6.66528338866867,
14.1411920375589));
#51239=CARTESIAN_POINT('Ctrl Pts',(-1.0076317737392,-6.69389094417816,14.1494943001568));
#51240=CARTESIAN_POINT('Ctrl Pts',(-0.832313097425561,-6.71561939867455,
14.1577965627548));
#51241=CARTESIAN_POINT('Ctrl Pts',(-0.656918437066145,-6.73735727039856,
14.1661024235974));
#51242=CARTESIAN_POINT('Ctrl Pts',(-0.480748345908473,-6.75221005629532,
14.17440828444));
#51243=CARTESIAN_POINT('Ctrl Pts',(-0.304375009054581,-6.76015124489556,
14.1827141452827));
#51244=CARTESIAN_POINT('Ctrl Pts',(-0.12779318647331,-6.76810182054099,
14.1910298242388));
#51245=CARTESIAN_POINT('Ctrl Pts',(0.048992013903208,-6.76912445982801,
14.1993455031949));
#51246=CARTESIAN_POINT('Ctrl Pts',(0.225407998656858,-6.763244800696,14.2076611821511));
#51247=CARTESIAN_POINT('Ctrl Pts',(0.401935565115987,-6.75736142272642,
14.2159821207079));
#51248=CARTESIAN_POINT('Ctrl Pts',(0.578093103757538,-6.74456706528404,
14.2243030592648));
#51249=CARTESIAN_POINT('Ctrl Pts',(0.753313770290341,-6.72493920890672,
14.2326239978217));
#51250=CARTESIAN_POINT('Ctrl Pts',(0.928794869007725,-6.70528217945515,
14.2409573038706));
#51251=CARTESIAN_POINT('Ctrl Pts',(1.10333596904297,-6.67877140554487,14.2492906099196));
#51252=CARTESIAN_POINT('Ctrl Pts',(1.27637969656503,-6.64553563455923,14.2576239159685));
#51253=CARTESIAN_POINT('Ctrl Pts',(1.40375009654633,-6.62107214486939,14.26375772122));
#51254=CARTESIAN_POINT('Ctrl Pts',(1.53030947374522,-6.59296623442997,14.2698915264716));
#51255=CARTESIAN_POINT('Ctrl Pts',(1.65584129774007,-6.5612863522863,14.2760253317231));
#51256=CARTESIAN_POINT('Ctrl Pts',(1.82102737472401,-6.51959911088335,14.2840967449651));
#51257=CARTESIAN_POINT('Ctrl Pts',(1.98494203352834,-6.47159297497934,14.2921681582071));
#51258=CARTESIAN_POINT('Ctrl Pts',(2.14705257811262,-6.41735570362279,14.3002395714491));
#51259=CARTESIAN_POINT('Ctrl Pts',(2.30895960633557,-6.36318652266802,14.3083008517004));
#51260=CARTESIAN_POINT('Ctrl Pts',(2.46906667773576,-6.30280188820965,14.3163621319516));
#51261=CARTESIAN_POINT('Ctrl Pts',(2.62685071084514,-6.23634062114413,14.3244234122028));
#51262=CARTESIAN_POINT('Ctrl Pts',(2.7844712619378,-6.16994821543144,14.3324763400604));
#51263=CARTESIAN_POINT('Ctrl Pts',(2.93977322379651,-6.09749185003728,14.340529267918));
#51264=CARTESIAN_POINT('Ctrl Pts',(3.092248226194,-6.01916023275673,14.3485821957756));
#51265=CARTESIAN_POINT('Ctrl Pts',(3.2445986358545,-5.94089262302127,14.3566285433));
#51266=CARTESIAN_POINT('Ctrl Pts',(3.39412635370123,-5.85675948634532,14.3646748908244));
#51267=CARTESIAN_POINT('Ctrl Pts',(3.54034267279721,-5.76699772491468,14.3727212383487));
#51268=CARTESIAN_POINT('Ctrl Pts',(3.68647149792179,-5.67728967577167,14.3807627710419));
#51269=CARTESIAN_POINT('Ctrl Pts',(3.82929255183924,-5.58195990141865,14.388804303735));
#51270=CARTESIAN_POINT('Ctrl Pts',(3.96834154507748,-5.48129130603475,14.3968458364282));
#51271=CARTESIAN_POINT('Ctrl Pts',(4.11006371870998,-5.37868738333038,14.4050419654764));
#51272=CARTESIAN_POINT('Ctrl Pts',(4.24786697040222,-5.27053745778933,14.4132380945247));
#51273=CARTESIAN_POINT('Ctrl Pts',(4.38129013694641,-5.15718777396132,14.421434223573));
#51274=CARTESIAN_POINT('Ctrl Pts',(4.51215147232026,-5.04601449443175,14.4294729804091));
#51275=CARTESIAN_POINT('Ctrl Pts',(4.63879911983766,-4.92983959333512,14.4375117372451));
#51276=CARTESIAN_POINT('Ctrl Pts',(4.76083129951727,-4.80903049871144,14.4455504940812));
#51277=CARTESIAN_POINT('Ctrl Pts',(4.8828752906221,-4.68820971104423,14.453590028984));
#51278=CARTESIAN_POINT('Ctrl Pts',(5.00030265887253,-4.5627540994133,14.4616295638868));
#51279=CARTESIAN_POINT('Ctrl Pts',(5.1127486852055,-4.43306777321635,14.4696690987896));
#51280=CARTESIAN_POINT('Ctrl Pts',(5.22522785947751,-4.30334321681622,14.4777110036651));
#51281=CARTESIAN_POINT('Ctrl Pts',(5.33272252439571,-4.16938574540773,14.4857529085406));
#51282=CARTESIAN_POINT('Ctrl Pts',(5.43490852954296,-4.03163220985015,14.4937948134161));
#51283=CARTESIAN_POINT('Ctrl Pts',(5.54054150186107,-3.88923193314583,14.502107990097));
#51284=CARTESIAN_POINT('Ctrl Pts',(5.64050114311577,-3.74277536337125,14.5104211667778));
#51285=CARTESIAN_POINT('Ctrl Pts',(5.73447889264906,-3.59277620090126,14.5187343434586));
#51286=CARTESIAN_POINT('Ctrl Pts',(5.82554784711029,-3.44741980575408,14.5267902110692));
#51287=CARTESIAN_POINT('Ctrl Pts',(5.91099957511724,-3.29873720683962,14.5348460786797));
#51288=CARTESIAN_POINT('Ctrl Pts',(5.99060105698889,-3.14721908611454,14.5429019462902));
#51289=CARTESIAN_POINT('Ctrl Pts',(6.07401631490912,-2.98844160078769,14.5513437775062));
#51290=CARTESIAN_POINT('Ctrl Pts',(6.15100674604125,-2.82655064347649,14.5597856087222));
#51291=CARTESIAN_POINT('Ctrl Pts',(6.22136199727863,-2.66213145783924,14.5682274399382));
#51292=CARTESIAN_POINT('Ctrl Pts',(6.29171724851601,-2.49771227220198,14.5766692711542));
#51293=CARTESIAN_POINT('Ctrl Pts',(6.35543723539127,-2.3307653195474,14.5851111023702));
#51294=CARTESIAN_POINT('Ctrl Pts',(6.41237240559569,-2.16189017573857,14.5935529335862));
#51295=CARTESIAN_POINT('Ctrl Pts',(6.46788197514518,-1.99724349940867,14.6017833896528));
#51296=CARTESIAN_POINT('Ctrl Pts',(6.51712741399373,-1.83021654216366,14.6100138457193));
#51297=CARTESIAN_POINT('Ctrl Pts',(6.55989964640253,-1.66132646675118,14.6182443017859));
#51298=CARTESIAN_POINT('Ctrl Pts',(6.60262110565111,-1.49263687381008,14.6264649878161));
#51299=CARTESIAN_POINT('Ctrl Pts',(6.63888457201858,-1.32208891068805,14.6346856738463));
#51300=CARTESIAN_POINT('Ctrl Pts',(6.66852964355521,-1.15021797630948,14.6429063598765));
#51301=CARTESIAN_POINT('Ctrl Pts',(6.69814547236329,-0.978516580232526,
14.6511189367919));
#51302=CARTESIAN_POINT('Ctrl Pts',(6.72115584739485,-0.805495162698951,
14.6593315137073));
#51303=CARTESIAN_POINT('Ctrl Pts',(6.73745061970401,-0.63170257799859,14.6675440906227));
#51304=CARTESIAN_POINT('Ctrl Pts',(6.75373258645454,-0.458046571526462,
14.6757502135273));
#51305=CARTESIAN_POINT('Ctrl Pts',(6.76330942894072,-0.283620960328507,
14.6839563364319));
#51306=CARTESIAN_POINT('Ctrl Pts',(6.76612235147591,-0.108983140246803,
14.6921624593366));
#51307=CARTESIAN_POINT('Ctrl Pts',(6.76893362743368,0.065552453524236,14.7003637786903));
#51308=CARTESIAN_POINT('Ctrl Pts',(6.76498886514755,0.240299651204914,14.708565098044));
#51309=CARTESIAN_POINT('Ctrl Pts',(6.75428123280918,0.414697514004833,14.7167664173976));
#51310=CARTESIAN_POINT('Ctrl Pts',(6.74357667223676,0.589045346190983,14.7249653839872));
#51311=CARTESIAN_POINT('Ctrl Pts',(6.72611312406623,0.763043685475608,14.7331643505767));
#51312=CARTESIAN_POINT('Ctrl Pts',(6.70193585136313,0.936132920163386,14.7413633171662));
#51313=CARTESIAN_POINT('Ctrl Pts',(6.67776177137814,1.10919929763553,14.7495612010452));
#51314=CARTESIAN_POINT('Ctrl Pts',(6.64687578138272,1.28135645444196,14.7577590849241));
#51315=CARTESIAN_POINT('Ctrl Pts',(6.60937487893045,1.45205120769313,14.765956968803));
#51316=CARTESIAN_POINT('Ctrl Pts',(6.571872116495,1.62275442712379,14.7741552592835));
#51317=CARTESIAN_POINT('Ctrl Pts',(6.5277538648852,1.79199474820034,14.782353549764));
#51318=CARTESIAN_POINT('Ctrl Pts',(6.47716799146005,1.95923041279106,14.7905518402446));
#51319=CARTESIAN_POINT('Ctrl Pts',(6.42657042001371,2.1265047507547,14.7987520265859));
#51320=CARTESIAN_POINT('Ctrl Pts',(6.36950235167999,2.29177316573873,14.8069522129272));
#51321=CARTESIAN_POINT('Ctrl Pts',(6.30616116457238,2.4545102090721,14.8151523992686));
#51322=CARTESIAN_POINT('Ctrl Pts',(6.24276009334236,2.61740110751092,14.8233603382427));
#51323=CARTESIAN_POINT('Ctrl Pts',(6.17307418462033,2.77775551830354,14.8315682772168));
#51324=CARTESIAN_POINT('Ctrl Pts',(6.09734889143322,2.93506822682849,14.8397762161909));
#51325=CARTESIAN_POINT('Ctrl Pts',(6.02158686161215,3.09245725251441,14.8479881370849));
#51326=CARTESIAN_POINT('Ctrl Pts',(5.93977977364929,3.24680131722539,14.8562000579788));
#51327=CARTESIAN_POINT('Ctrl Pts',(5.85221844740126,3.39762096825064,14.8644119788728));
#51328=CARTESIAN_POINT('Ctrl Pts',(5.76453704466559,3.5486474445347,14.8726351611154));
#51329=CARTESIAN_POINT('Ctrl Pts',(5.67108582560821,3.69613954517809,14.8808583433579));
#51330=CARTESIAN_POINT('Ctrl Pts',(5.57219891614664,3.83964688987077,14.8890815256005));
#51331=CARTESIAN_POINT('Ctrl Pts',(5.48401674891213,3.96761922451014,14.8964145288833));
#51332=CARTESIAN_POINT('Ctrl Pts',(5.39151274046028,4.09242312878907,14.9037475321662));
#51333=CARTESIAN_POINT('Ctrl Pts',(5.29494976727265,4.21376268459192,14.9110805354491));
#51334=CARTESIAN_POINT('Ctrl Pts',(5.17726978944369,4.36163754557937,14.9200171664916));
#51335=CARTESIAN_POINT('Ctrl Pts',(5.05331699973582,4.50467388222966,14.9289537975341));
#51336=CARTESIAN_POINT('Ctrl Pts',(4.92349523383776,4.6423575564983,14.9378904285766));
#51337=CARTESIAN_POINT('Ctrl Pts',(4.79273035422974,4.78104145873289,14.9468919813925));
#51338=CARTESIAN_POINT('Ctrl Pts',(4.65601100815203,4.9142943786491,14.9558935342083));
#51339=CARTESIAN_POINT('Ctrl Pts',(4.51379255778441,5.04162332441547,14.9648950870241));
#51340=CARTESIAN_POINT('Ctrl Pts',(4.37312634939398,5.1675625395666,14.973798392474));
#51341=CARTESIAN_POINT('Ctrl Pts',(4.22708064891526,5.28770623900974,14.9827016979239));
#51342=CARTESIAN_POINT('Ctrl Pts',(4.07613507253603,5.40161196962922,14.9916050033737));
#51343=CARTESIAN_POINT('Ctrl Pts',(3.92269098500821,5.51740311315492,15.0006556798726));
#51344=CARTESIAN_POINT('Ctrl Pts',(3.76418354441934,5.62674775083,15.0097063563714));
#51345=CARTESIAN_POINT('Ctrl Pts',(3.60115508114248,5.72922080928652,15.0187570328702));
#51346=CARTESIAN_POINT('Ctrl Pts',(3.43812661786561,5.83169386774304,15.027807709369));
#51347=CARTESIAN_POINT('Ctrl Pts',(3.27057733268523,5.92729513890819,15.0368583858678));
#51348=CARTESIAN_POINT('Ctrl Pts',(3.09908550384722,6.01564277861011,15.0459090623666));
#51349=CARTESIAN_POINT('Ctrl Pts',(3.09908550384717,6.01564277861014,13.0457845165097));
#51350=CARTESIAN_POINT('Ctrl Pts',(2.94002611072669,6.09758558632192,13.0542214576994));
#51351=CARTESIAN_POINT('Ctrl Pts',(2.77760959688775,6.17327019142043,13.062658398889));
#51352=CARTESIAN_POINT('Ctrl Pts',(2.61235697521166,6.24242581326066,13.0710953400787));
#51353=CARTESIAN_POINT('Ctrl Pts',(2.44721533292437,6.31153499197299,13.0795266152368));
#51354=CARTESIAN_POINT('Ctrl Pts',(2.27924168670711,6.37412380057255,13.0879578903949));
#51355=CARTESIAN_POINT('Ctrl Pts',(2.10897936049659,6.42996851135365,13.0963891655529));
#51356=CARTESIAN_POINT('Ctrl Pts',(1.93880524877013,6.48578428847421,13.1048160723894));
#51357=CARTESIAN_POINT('Ctrl Pts',(1.76634513758492,6.53486283106964,13.113242979226));
#51358=CARTESIAN_POINT('Ctrl Pts',(1.59216031042803,6.57702931009872,13.1216698860625));
#51359=CARTESIAN_POINT('Ctrl Pts',(1.41802841216451,6.61918297615719,13.1300942322463));
#51360=CARTESIAN_POINT('Ctrl Pts',(1.24217316610256,6.65442868615755,13.1385185784301));
#51361=CARTESIAN_POINT('Ctrl Pts',(1.06516941800624,6.68264192598588,13.1469429246139));
#51362=CARTESIAN_POINT('Ctrl Pts',(0.888196003982625,6.71085033076141,13.1553658270727));
#51363=CARTESIAN_POINT('Ctrl Pts',(0.710074809391342,6.73202861530033,13.1637887295315));
#51364=CARTESIAN_POINT('Ctrl Pts',(0.531389593725857,6.7461036235504,13.1722116319904));
#51365=CARTESIAN_POINT('Ctrl Pts',(0.352710082313214,6.76017818247731,13.1806342655609));
#51366=CARTESIAN_POINT('Ctrl Pts',(0.173466918097244,6.76714989123629,13.1890568991314));
#51367=CARTESIAN_POINT('Ctrl Pts',(-0.00575193952454701,6.76699755542971,
13.1974795327019));
#51368=CARTESIAN_POINT('Ctrl Pts',(-0.184990067383262,6.76684520324346,
13.2059030719034));
#51369=CARTESIAN_POINT('Ctrl Pts',(-0.364203550049273,6.75956728013755,
13.2143266111049));
#51370=CARTESIAN_POINT('Ctrl Pts',(-0.54280497774089,6.74519471595444,13.2227501503064));
#51371=CARTESIAN_POINT('Ctrl Pts',(-0.721522516916806,6.73081280795039,
13.2311791657778));
#51372=CARTESIAN_POINT('Ctrl Pts',(-0.899626873024427,6.70932706658896,
13.2396081812493));
#51373=CARTESIAN_POINT('Ctrl Pts',(-1.07653522714635,6.68082037662389,13.2480371967207));
#51374=CARTESIAN_POINT('Ctrl Pts',(-1.25349717761354,6.65230505024136,13.2564687658558));
#51375=CARTESIAN_POINT('Ctrl Pts',(-1.42926207521128,6.61676459281632,13.2649003349909));
#51376=CARTESIAN_POINT('Ctrl Pts',(-1.60325725162761,6.57433306009845,13.273331904126));
#51377=CARTESIAN_POINT('Ctrl Pts',(-1.77742662637449,6.53185904630546,13.2817719146747));
#51378=CARTESIAN_POINT('Ctrl Pts',(-1.94982241538522,6.48248025198872,13.2902119252235));
#51379=CARTESIAN_POINT('Ctrl Pts',(-2.11988577858572,6.42638104112649,13.2986519357723));
#51380=CARTESIAN_POINT('Ctrl Pts',(-2.28639312073834,6.3714548634846,13.3069154658928));
#51381=CARTESIAN_POINT('Ctrl Pts',(-2.45066434411047,6.31008666730127,13.3151789960134));
#51382=CARTESIAN_POINT('Ctrl Pts',(-2.61219368322618,6.24249414587737,13.323442526134));
#51383=CARTESIAN_POINT('Ctrl Pts',(-2.77133507280265,6.17590087035688,13.3315838933519));
#51384=CARTESIAN_POINT('Ctrl Pts',(-2.92813109737699,6.10313320137953,13.3397252605697));
#51385=CARTESIAN_POINT('Ctrl Pts',(-3.08206503653218,6.02438080723537,13.3478666277876));
#51386=CARTESIAN_POINT('Ctrl Pts',(-3.23586460306598,5.94569715794177,13.356000888211));
#51387=CARTESIAN_POINT('Ctrl Pts',(-3.38680673358627,5.86103934792309,13.3641351486345));
#51388=CARTESIAN_POINT('Ctrl Pts',(-3.53439404226829,5.77064534987019,13.372269409058));
#51389=CARTESIAN_POINT('Ctrl Pts',(-3.68188067221889,5.68031301533791,13.3803981205828));
#51390=CARTESIAN_POINT('Ctrl Pts',(-3.8260167258597,5.58425247387798,13.3885268321075));
#51391=CARTESIAN_POINT('Ctrl Pts',(-3.96632886489278,5.4827478818124,13.3966555436323));
#51392=CARTESIAN_POINT('Ctrl Pts',(-4.10657409166014,5.38129169541067,13.4047803787248));
#51393=CARTESIAN_POINT('Ctrl Pts',(-4.24299873920578,5.27439684238225,13.4129052138174));
#51394=CARTESIAN_POINT('Ctrl Pts',(-4.37515797079932,5.16239108655584,13.4210300489099));
#51395=CARTESIAN_POINT('Ctrl Pts',(-4.50728020404572,5.05041668705457,13.429152609432));
#51396=CARTESIAN_POINT('Ctrl Pts',(-4.6351391213156,4.93333447174832,13.4372751699542));
#51397=CARTESIAN_POINT('Ctrl Pts',(-4.75832256938735,4.81151278972206,13.4453977304764));
#51398=CARTESIAN_POINT('Ctrl Pts',(-4.88151256433965,4.68968463318959,13.4535207226915));
#51399=CARTESIAN_POINT('Ctrl Pts',(-5.00002633065173,4.56311676134893,13.4616437149067));
#51400=CARTESIAN_POINT('Ctrl Pts',(-5.11348810125801,4.43221484568299,13.4697667071219));
#51401=CARTESIAN_POINT('Ctrl Pts',(-5.17140687745421,4.36539340691471,13.4739132471031));
#51402=CARTESIAN_POINT('Ctrl Pts',(-5.22800981914079,4.29744318159846,13.4780597870842));
#51403=CARTESIAN_POINT('Ctrl Pts',(-5.28325092638768,4.22842153159117,13.4822063270654));
#51404=CARTESIAN_POINT('Ctrl Pts',(-5.40293318535753,4.0788831279929,13.4911899860938));
#51405=CARTESIAN_POINT('Ctrl Pts',(-5.51616158888885,3.92438776164471,13.5001736451222));
#51406=CARTESIAN_POINT('Ctrl Pts',(-5.62257164882376,3.76549824775464,13.5091573041505));
#51407=CARTESIAN_POINT('Ctrl Pts',(-5.72916452011397,3.60633576336352,13.5181563970099));
#51408=CARTESIAN_POINT('Ctrl Pts',(-5.82891550203853,3.44276424163258,13.5271554898693));
#51409=CARTESIAN_POINT('Ctrl Pts',(-5.92150483796006,3.27537317782503,13.5361545827287));
#51410=CARTESIAN_POINT('Ctrl Pts',(-6.01431127000053,3.10758962874974,13.5451747759461));
#51411=CARTESIAN_POINT('Ctrl Pts',(-6.09992234188846,2.93596882881938,13.5541949691634));
#51412=CARTESIAN_POINT('Ctrl Pts',(-6.1780642601733,2.76112495138655,13.5632151623808));
#51413=CARTESIAN_POINT('Ctrl Pts',(-6.25628531671751,2.58610400074608,13.5722444908025));
#51414=CARTESIAN_POINT('Ctrl Pts',(-6.32702201589748,2.40785367219275,13.5812738192242));
#51415=CARTESIAN_POINT('Ctrl Pts',(-6.39004916142147,2.22700712046836,13.5903031476459));
#51416=CARTESIAN_POINT('Ctrl Pts',(-6.45316516251637,2.04590561155897,13.5993452056006));
#51417=CARTESIAN_POINT('Ctrl Pts',(-6.508549798691,1.86220078690502,13.6083872635554));
#51418=CARTESIAN_POINT('Ctrl Pts',(-6.55602741117472,1.67654215095407,13.6174293215101));
#51419=CARTESIAN_POINT('Ctrl Pts',(-6.59722973088013,1.51542270803466,13.6252762570057));
#51420=CARTESIAN_POINT('Ctrl Pts',(-6.63247786449317,1.35283211035126,13.6331231925014));
#51421=CARTESIAN_POINT('Ctrl Pts',(-6.66168820007206,1.18920112891837,13.640970127997));
#51422=CARTESIAN_POINT('Ctrl Pts',(-6.69711427398505,0.99075071307011,13.6504868319769));
#51423=CARTESIAN_POINT('Ctrl Pts',(-6.72368001736206,0.790651468887019,
13.6600035359568));
#51424=CARTESIAN_POINT('Ctrl Pts',(-6.7412618041006,0.589642509131079,13.6695202399368));
#51425=CARTESIAN_POINT('Ctrl Pts',(-6.75829515942328,0.394903653206785,
13.6787400878852));
#51426=CARTESIAN_POINT('Ctrl Pts',(-6.7668964796064,0.199311108068396,13.6879599358336));
#51427=CARTESIAN_POINT('Ctrl Pts',(-6.7669990707839,0.00354626703724167,
13.697179783782));
#51428=CARTESIAN_POINT('',(-6.76699798626915,-0.00522052001777089,13.302820216157));
#51429=CARTESIAN_POINT('Ctrl Pts',(3.09908550384725,6.0156427786101,12.6512833602796));
#51430=CARTESIAN_POINT('Ctrl Pts',(2.94210374532802,6.09651524895113,12.6596057067752));
#51431=CARTESIAN_POINT('Ctrl Pts',(2.78208499805338,6.17117181071805,12.6679280532708));
#51432=CARTESIAN_POINT('Ctrl Pts',(2.6195623649851,6.23940558194077,12.6762503997664));
#51433=CARTESIAN_POINT('Ctrl Pts',(2.45680893777207,6.30773625015917,12.6845845646088));
#51434=CARTESIAN_POINT('Ctrl Pts',(2.29154484584409,6.36962578316633,12.6929187294512));
#51435=CARTESIAN_POINT('Ctrl Pts',(2.12431953451885,6.42491677107662,12.7012528942936));
#51436=CARTESIAN_POINT('Ctrl Pts',(2.04026086604636,6.45270973366963,12.705442205074));
#51437=CARTESIAN_POINT('Ctrl Pts',(1.95570683751969,6.4788362144871,12.7096315158543));
#51438=CARTESIAN_POINT('Ctrl Pts',(1.87072815952385,6.50328110673101,12.7138208266347));
#51439=CARTESIAN_POINT('Ctrl Pts',(1.70700241492626,6.55037831133143,12.7218922398767));
#51440=CARTESIAN_POINT('Ctrl Pts',(1.54119570789558,6.59137514485665,12.7299636531187));
#51441=CARTESIAN_POINT('Ctrl Pts',(1.37381253820462,6.62607939205921,12.7380350663608));
#51442=CARTESIAN_POINT('Ctrl Pts',(1.2066395042192,6.6607400709539,12.746096346612));
#51443=CARTESIAN_POINT('Ctrl Pts',(1.03789430607367,6.68912380738644,12.7541576268632));
#51444=CARTESIAN_POINT('Ctrl Pts',(0.868098829367446,6.71108735023252,12.7622189071144));
#51445=CARTESIAN_POINT('Ctrl Pts',(0.698479279885125,6.73302813637626,12.770271834972));
#51446=CARTESIAN_POINT('Ctrl Pts',(0.527811984151826,6.74856191925419,12.7783247628297));
#51447=CARTESIAN_POINT('Ctrl Pts',(0.356631217975381,6.75759596116588,12.7863776906873));
#51448=CARTESIAN_POINT('Ctrl Pts',(0.185590329679652,6.76662262104123,12.7944240382117));
#51449=CARTESIAN_POINT('Ctrl Pts',(0.014037176588647,6.76916009143369,12.802470385736));
#51450=CARTESIAN_POINT('Ctrl Pts',(-0.157486706361212,6.76516717733712,
12.8105167332604));
#51451=CARTESIAN_POINT('Ctrl Pts',(-0.32890795161737,6.76117665254918,12.8185582659536));
#51452=CARTESIAN_POINT('Ctrl Pts',(-0.500299589675203,6.7506635310307,12.8265997986467));
#51453=CARTESIAN_POINT('Ctrl Pts',(-0.67111803809773,6.73363865818028,12.8346413313399));
#51454=CARTESIAN_POINT('Ctrl Pts',(-0.845220426351066,6.71628648661836,
12.8428374603881));
#51455=CARTESIAN_POINT('Ctrl Pts',(-1.01872696642979,6.69216962278029,12.8510335894364));
#51456=CARTESIAN_POINT('Ctrl Pts',(-1.19106490449715,6.66135522197062,12.8592297184846));
#51457=CARTESIAN_POINT('Ctrl Pts',(-1.36009381675582,6.63113248222351,12.8672684753207));
#51458=CARTESIAN_POINT('Ctrl Pts',(-1.52799821947554,6.59446716054457,12.8753072321568));
#51459=CARTESIAN_POINT('Ctrl Pts',(-1.69424601636151,6.55147460012196,12.8833459889929));
#51460=CARTESIAN_POINT('Ctrl Pts',(-1.86050990427714,6.50847787847389,12.8913855238957));
#51461=CARTESIAN_POINT('Ctrl Pts',(-2.02511650546706,6.45915279207153,12.8994250587985));
#51462=CARTESIAN_POINT('Ctrl Pts',(-2.18754729237714,6.40366503212133,12.9074645937013));
#51463=CARTESIAN_POINT('Ctrl Pts',(-2.35002596222311,6.3481609149466,12.9155064985768));
#51464=CARTESIAN_POINT('Ctrl Pts',(-2.51032718785764,6.28649062880948,12.9235484034523));
#51465=CARTESIAN_POINT('Ctrl Pts',(-2.6679510243003,6.21886857329651,12.9315903083278));
#51466=CARTESIAN_POINT('Ctrl Pts',(-2.83089187248764,6.14896547151873,12.9399034850087));
#51467=CARTESIAN_POINT('Ctrl Pts',(-2.99097114177248,6.07270221526078,12.9482166616895));
#51468=CARTESIAN_POINT('Ctrl Pts',(-3.14766368850354,5.99036745985389,12.9565298383704));
#51469=CARTESIAN_POINT('Ctrl Pts',(-3.29950629458373,5.91058112608898,12.9645857059809));
#51470=CARTESIAN_POINT('Ctrl Pts',(-3.44816842299859,5.82509379009984,12.9726415735914));
#51471=CARTESIAN_POINT('Ctrl Pts',(-3.59320179316167,5.73421222781471,12.9806974412019));
#51472=CARTESIAN_POINT('Ctrl Pts',(-3.74518383790148,5.63897645104341,12.9891392724179));
#51473=CARTESIAN_POINT('Ctrl Pts',(-3.8931804549649,5.53781712185059,12.9975811036339));
#51474=CARTESIAN_POINT('Ctrl Pts',(-4.03671536784392,5.43113413929473,13.0060229348499));
#51475=CARTESIAN_POINT('Ctrl Pts',(-4.18025028072295,5.32445115673887,13.0144647660659));
#51476=CARTESIAN_POINT('Ctrl Pts',(-4.31932318429191,5.21224487696434,13.0229065972819));
#51477=CARTESIAN_POINT('Ctrl Pts',(-4.45350313218815,5.09495817957227,13.0313484284979));
#51478=CARTESIAN_POINT('Ctrl Pts',(-4.58315933088935,4.98162569151799,13.0395056514116));
#51479=CARTESIAN_POINT('Ctrl Pts',(-4.70869264445891,4.86316062911941,13.0476628743253));
#51480=CARTESIAN_POINT('Ctrl Pts',(-4.82966607146199,4.73989605773892,13.055820097239));
#51481=CARTESIAN_POINT('Ctrl Pts',(-4.95049448812238,4.61677924308634,13.0639675421236));
#51482=CARTESIAN_POINT('Ctrl Pts',(-5.06677364563792,4.48887463075528,13.0721149870082));
#51483=CARTESIAN_POINT('Ctrl Pts',(-5.17809910981238,4.35655581956208,13.0802624318929));
#51484=CARTESIAN_POINT('Ctrl Pts',(-5.28931456857467,4.22436775819753,13.0884018259417));
#51485=CARTESIAN_POINT('Ctrl Pts',(-5.39558584606881,4.08777446054306,13.0965412199905));
#51486=CARTESIAN_POINT('Ctrl Pts',(-5.49654494194717,3.94718668182226,13.1046806140393));
#51487=CARTESIAN_POINT('Ctrl Pts',(-5.59894811720977,3.80458799055156,13.1129364307942));
#51488=CARTESIAN_POINT('Ctrl Pts',(-5.69588569719101,3.6578799265307,13.1211922475492));
#51489=CARTESIAN_POINT('Ctrl Pts',(-5.78701486954364,3.50752731987662,13.1294480643041));
#51490=CARTESIAN_POINT('Ctrl Pts',(-5.87673678152078,3.35949653026787,13.137576390778));
#51491=CARTESIAN_POINT('Ctrl Pts',(-5.9608281827451,3.2079332702881,13.1457047172519));
#51492=CARTESIAN_POINT('Ctrl Pts',(-6.03900474827512,3.05331142373499,13.1538330437259));
#51493=CARTESIAN_POINT('Ctrl Pts',(-6.117158453127,2.89873479226958,13.1619589932848));
#51494=CARTESIAN_POINT('Ctrl Pts',(-6.18940060090174,2.7411016810502,13.1700849428437));
#51495=CARTESIAN_POINT('Ctrl Pts',(-6.25549260177143,2.5809109456126,13.1782108924026));
#51496=CARTESIAN_POINT('Ctrl Pts',(-6.32157786448275,2.42073654181168,13.1863360135112));
#51497=CARTESIAN_POINT('Ctrl Pts',(-6.38151409000943,2.25800537143498,13.1944611346199));
#51498=CARTESIAN_POINT('Ctrl Pts',(-6.43511068145649,2.0932366128569,13.2025862557285));
#51499=CARTESIAN_POINT('Ctrl Pts',(-6.49020933326299,1.92385016098802,13.2109390857642));
#51500=CARTESIAN_POINT('Ctrl Pts',(-6.53860766597136,1.75231062191697,13.2192919157999));
#51501=CARTESIAN_POINT('Ctrl Pts',(-6.58015348247487,1.57919889408327,13.2276447458356));
#51502=CARTESIAN_POINT('Ctrl Pts',(-6.62059538367987,1.41068692383746,13.2357756325413));
#51503=CARTESIAN_POINT('Ctrl Pts',(-6.65454425660174,1.24068562579775,13.243906519247));
#51504=CARTESIAN_POINT('Ctrl Pts',(-6.68191166322437,1.06974086809197,13.2520374059527));
#51505=CARTESIAN_POINT('Ctrl Pts',(-6.71039961430526,0.891796864766862,
13.2605012076534));
#51506=CARTESIAN_POINT('Ctrl Pts',(-6.73175569899097,0.71283094874556,13.2689650093542));
#51507=CARTESIAN_POINT('Ctrl Pts',(-6.74593991475798,0.533463838020057,
13.2774288110549));
#51508=CARTESIAN_POINT('Ctrl Pts',(-6.76012413052499,0.354096727294553,
13.2858926127556));
#51509=CARTESIAN_POINT('Ctrl Pts',(-6.7671365028122,0.17432886676091,13.2943564144563));
#51510=CARTESIAN_POINT('Ctrl Pts',(-6.76699798626915,-0.00522052001777006,
13.302820216157));
#51511=CARTESIAN_POINT('Ctrl Pts',(-6.76699798626862,-0.00522052071405314,
13.3028202161898));
#51512=CARTESIAN_POINT('Ctrl Pts',(-6.76680254782566,-0.258553784264194,
13.3147621255739));
#51513=CARTESIAN_POINT('Ctrl Pts',(-6.75237781066175,-0.511376352775485,
13.3267040349581));
#51514=CARTESIAN_POINT('Ctrl Pts',(-6.72391519900023,-0.762399761708883,
13.3386459443422));
#51515=CARTESIAN_POINT('Ctrl Pts',(-6.7157876610372,-0.834079841877793,
13.3420559730151));
#51516=CARTESIAN_POINT('Ctrl Pts',(-6.70651576063321,-0.905613394825189,
13.345466001688));
#51517=CARTESIAN_POINT('Ctrl Pts',(-6.69610462071302,-0.976970781787121,
13.3488760303609));
#51518=CARTESIAN_POINT('Ctrl Pts',(-6.66882465074012,-1.16394621277629,
13.3578112171431));
#51519=CARTESIAN_POINT('Ctrl Pts',(-6.63369169714627,-1.34989716734416,
13.3667464039253));
#51520=CARTESIAN_POINT('Ctrl Pts',(-6.59079597868481,-1.53417644596446,
13.3756815907075));
#51521=CARTESIAN_POINT('Ctrl Pts',(-6.54796450473953,-1.7181797312334,13.3846033953441));
#51522=CARTESIAN_POINT('Ctrl Pts',(-6.4973935226934,-1.9005160851843,13.3935251999807));
#51523=CARTESIAN_POINT('Ctrl Pts',(-6.43922439836573,-2.08054755953608,
13.4024470046173));
#51524=CARTESIAN_POINT('Ctrl Pts',(-6.38119716232729,-2.26013989442687,
13.4113470468565));
#51525=CARTESIAN_POINT('Ctrl Pts',(-6.31560885333637,-2.43743832519912,
13.4202470890957));
#51526=CARTESIAN_POINT('Ctrl Pts',(-6.24265061621746,-2.61181972652015,
13.429147131335));
#51527=CARTESIAN_POINT('Ctrl Pts',(-6.16980469937722,-2.78593266511011,
13.4380334718283));
#51528=CARTESIAN_POINT('Ctrl Pts',(-6.08961158617208,-2.95713729512159,
13.4469198123217));
#51529=CARTESIAN_POINT('Ctrl Pts',(-6.00231148810044,-3.12482732320003,
13.4558061528151));
#51530=CARTESIAN_POINT('Ctrl Pts',(-5.91523460114094,-3.29208859714774,
13.464669772487));
#51531=CARTESIAN_POINT('Ctrl Pts',(-5.82108710798822,-3.45585297216316,
13.4735333921588));
#51532=CARTESIAN_POINT('Ctrl Pts',(-5.7201560570988,-3.61553643079916,13.4823970118307));
#51533=CARTESIAN_POINT('Ctrl Pts',(-5.62434176639866,-3.76712464068034,
13.4908112849846));
#51534=CARTESIAN_POINT('Ctrl Pts',(-5.52241469626898,-3.91503516365269,
13.4992255581386));
#51535=CARTESIAN_POINT('Ctrl Pts',(-5.41466008086214,-4.05878617430359,
13.5076398312925));
#51536=CARTESIAN_POINT('Ctrl Pts',(-5.30951824371354,-4.19905158469682,
13.515850079497));
#51537=CARTESIAN_POINT('Ctrl Pts',(-5.19892827514438,-4.33522133848849,
13.5240603277016));
#51538=CARTESIAN_POINT('Ctrl Pts',(-5.08325100083917,-4.46686111967538,
13.5322705759061));
#51539=CARTESIAN_POINT('Ctrl Pts',(-4.96754622773981,-4.59853219426252,
13.5404827758503));
#51540=CARTESIAN_POINT('Ctrl Pts',(-4.84675197448823,-4.72567088343414,
13.5486949757945));
#51541=CARTESIAN_POINT('Ctrl Pts',(-4.72126741702553,-4.8478781932855,13.5569071757387));
#51542=CARTESIAN_POINT('Ctrl Pts',(-4.59573068409985,-4.97013631594683,
13.5651227902492));
#51543=CARTESIAN_POINT('Ctrl Pts',(-4.46550001654741,-5.08745872624941,
13.5733384047596));
#51544=CARTESIAN_POINT('Ctrl Pts',(-4.33100934004682,-5.19948527225794,
13.5815540192701));
#51545=CARTESIAN_POINT('Ctrl Pts',(-4.19636763641176,-5.31163761916708,
13.5897788595555));
#51546=CARTESIAN_POINT('Ctrl Pts',(-4.05745664262412,-5.41848199575201,
13.5980036998409));
#51547=CARTESIAN_POINT('Ctrl Pts',(-3.91474184822035,-5.51969974380784,
13.6062285401263));
#51548=CARTESIAN_POINT('Ctrl Pts',(-3.7719356400296,-5.62098232534992,13.6144586487079));
#51549=CARTESIAN_POINT('Ctrl Pts',(-3.62532107159179,-5.71663089988303,
13.6226887572894));
#51550=CARTESIAN_POINT('Ctrl Pts',(-3.47539008769781,-5.80637173614744,
13.630918865871));
#51551=CARTESIAN_POINT('Ctrl Pts',(-3.32525354612426,-5.89623560847542,
13.6391602580577));
#51552=CARTESIAN_POINT('Ctrl Pts',(-3.17179181859186,-5.98017539413079,
13.6474016502444));
#51553=CARTESIAN_POINT('Ctrl Pts',(-3.01551965984233,-6.05796419443895,
13.6556430424311));
#51554=CARTESIAN_POINT('Ctrl Pts',(-2.94750604603211,-6.09181985667115,
13.6592299056953));
#51555=CARTESIAN_POINT('Ctrl Pts',(-2.87896031322669,-6.12451101748651,
13.6628167689596));
#51556=CARTESIAN_POINT('Ctrl Pts',(-2.80992587884854,-6.15602189367267,
13.6664036322238));
#51557=CARTESIAN_POINT('Ctrl Pts',(-2.64732222801011,-6.23024258592781,
13.6748521270522));
#51558=CARTESIAN_POINT('Ctrl Pts',(-2.4816353628965,-6.29808112664666,13.6833006218806));
#51559=CARTESIAN_POINT('Ctrl Pts',(-2.31339409499536,-6.35928429630573,
13.6917491167091));
#51560=CARTESIAN_POINT('Ctrl Pts',(-2.14530650571936,-6.42043156042458,
13.7001898943282));
#51561=CARTESIAN_POINT('Ctrl Pts',(-1.97466947648193,-6.47495542149956,
13.7086306719474));
#51562=CARTESIAN_POINT('Ctrl Pts',(-1.80203272105282,-6.52265031043785,
13.7170714495666));
#51563=CARTESIAN_POINT('Ctrl Pts',(-1.62952711144905,-6.57030896731444,
13.7255058150359));
#51564=CARTESIAN_POINT('Ctrl Pts',(-1.4550251243115,-6.61114890534553,13.7339401805052));
#51565=CARTESIAN_POINT('Ctrl Pts',(-1.27909297551313,-6.64501393226478,
13.7423745459745));
#51566=CARTESIAN_POINT('Ctrl Pts',(-1.1032674584349,-6.67885843373659,13.7508037994111));
#51567=CARTESIAN_POINT('Ctrl Pts',(-0.926013834524638,-6.70573638968763,
13.7592330528477));
#51568=CARTESIAN_POINT('Ctrl Pts',(-0.747910281271728,-6.72554229866767,
13.7676623062843));
#51569=CARTESIAN_POINT('Ctrl Pts',(-0.569887355251328,-6.74533924154009,
13.7760877438095));
#51570=CARTESIAN_POINT('Ctrl Pts',(-0.391015597954095,-6.75807048450108,
13.7845131813347));
#51571=CARTESIAN_POINT('Ctrl Pts',(-0.211880506429093,-6.76368210747632,
13.7929386188599));
#51572=CARTESIAN_POINT('Ctrl Pts',(-0.0327847660661349,-6.76929249772891,
13.8013622055431));
#51573=CARTESIAN_POINT('Ctrl Pts',(0.146573860306079,-6.76778637322521,
13.8097857922263));
#51574=CARTESIAN_POINT('Ctrl Pts',(0.325607119369595,-6.75916185660736,
13.8182093789094));
#51575=CARTESIAN_POINT('Ctrl Pts',(0.504620345550144,-6.7505383050277,13.8266320230374));
#51576=CARTESIAN_POINT('Ctrl Pts',(0.683307944051406,-6.73479796526905,
13.8350546671654));
#51577=CARTESIAN_POINT('Ctrl Pts',(0.861083712811642,-6.71199104882676,
13.8434773112934));
#51578=CARTESIAN_POINT('Ctrl Pts',(1.03886437950728,-6.6891835040266,13.8519001874753));
#51579=CARTESIAN_POINT('Ctrl Pts',(1.21573283573447,-6.65930903718829,13.8603230636573));
#51580=CARTESIAN_POINT('Ctrl Pts',(1.39110966602265,-6.62246954670978,13.8687459398392));
#51581=CARTESIAN_POINT('Ctrl Pts',(1.56651578521461,-6.58562390383193,13.8771702226882));
#51582=CARTESIAN_POINT('Ctrl Pts',(1.74042945570415,-6.54181098736379,13.8855945055372));
#51583=CARTESIAN_POINT('Ctrl Pts',(1.91228272583966,-6.49118354204033,13.8940187883862));
#51584=CARTESIAN_POINT('Ctrl Pts',(2.08425205931978,-6.44052190481218,13.9024487606843));
#51585=CARTESIAN_POINT('Ctrl Pts',(2.25415789174803,-6.38303663665025,13.9108787329825));
#51586=CARTESIAN_POINT('Ctrl Pts',(2.42144770622888,-6.31893028969294,13.9193087052806));
#51587=CARTESIAN_POINT('Ctrl Pts',(2.5887973241183,-6.25480102575129,13.9277416911578));
#51588=CARTESIAN_POINT('Ctrl Pts',(2.75352875025348,-6.18404608850153,13.936174677035));
#51589=CARTESIAN_POINT('Ctrl Pts',(2.91511012103796,-6.10691591412736,13.9446076629122));
#51590=CARTESIAN_POINT('Ctrl Pts',(3.07684014569905,-6.02971478046272,13.953048407085));
#51591=CARTESIAN_POINT('Ctrl Pts',(3.23541402651578,-5.94612684050535,13.9614891512578));
#51592=CARTESIAN_POINT('Ctrl Pts',(3.39032416879734,-5.85644867052283,13.9699298954306));
#51593=CARTESIAN_POINT('Ctrl Pts',(3.47597812374837,-5.80686321524766,13.9745970083161));
#51594=CARTESIAN_POINT('Ctrl Pts',(3.56051245230653,-5.75541659648905,13.9792641212015));
#51595=CARTESIAN_POINT('Ctrl Pts',(3.64384520217654,-5.70216460149784,13.983931234087));
#51596=CARTESIAN_POINT('Ctrl Pts',(3.78921184202792,-5.60927118817199,13.9920726013048));
#51597=CARTESIAN_POINT('Ctrl Pts',(3.93120919044798,-5.51069695212364,14.0002139685227));
#51598=CARTESIAN_POINT('Ctrl Pts',(4.06936069948131,-5.40671734951227,14.0083553357406));
#51599=CARTESIAN_POINT('Ctrl Pts',(4.20739161275435,-5.30282851318583,14.0164895961641));
#51600=CARTESIAN_POINT('Ctrl Pts',(4.34158307856815,-5.19354392110617,14.0246238565875));
#51601=CARTESIAN_POINT('Ctrl Pts',(4.47148587948624,-5.07918330340175,14.032758117011));
#51602=CARTESIAN_POINT('Ctrl Pts',(4.60130006540548,-4.96490069838018,14.0408868285358));
#51603=CARTESIAN_POINT('Ctrl Pts',(4.72683113752287,-4.84554920271323,14.0490155400606));
#51604=CARTESIAN_POINT('Ctrl Pts',(4.84766148843627,-4.72148992305732,14.0571442515854));
#51605=CARTESIAN_POINT('Ctrl Pts',(4.96843421758857,-4.59748980497895,14.065269086678));
#51606=CARTESIAN_POINT('Ctrl Pts',(5.08451043466415,-4.46878663527642,14.0733939217705));
#51607=CARTESIAN_POINT('Ctrl Pts',(5.19550808867569,-4.33577959547133,14.081518756863));
#51608=CARTESIAN_POINT('Ctrl Pts',(5.30647466858273,-4.20280979136,14.0896413173852));
#51609=CARTESIAN_POINT('Ctrl Pts',(5.41236528359747,-4.06553879836356,14.0977638779073));
#51610=CARTESIAN_POINT('Ctrl Pts',(5.51283704096533,-3.92440017834071,14.1058864384295));
#51611=CARTESIAN_POINT('Ctrl Pts',(5.61331413814655,-3.78325405716622,14.1140094306447));
#51612=CARTESIAN_POINT('Ctrl Pts',(5.7083715868624,-3.63824019427199,14.1221324228599));
#51613=CARTESIAN_POINT('Ctrl Pts',(5.79770874095827,-3.48982268246054,14.1302554150751));
#51614=CARTESIAN_POINT('Ctrl Pts',(5.84331263561209,-3.41406006564192,14.1344019550561));
#51615=CARTESIAN_POINT('Ctrl Pts',(5.88742664052992,-3.33741099064498,14.1385484950372));
#51616=CARTESIAN_POINT('Ctrl Pts',(5.93001527222362,-3.25993985699041,14.1426950350183));
#51617=CARTESIAN_POINT('Ctrl Pts',(6.02228539318372,-3.0920952799532,14.1516786940467));
#51618=CARTESIAN_POINT('Ctrl Pts',(6.10734731431897,-2.92047372197738,14.160662353075));
#51619=CARTESIAN_POINT('Ctrl Pts',(6.18493844514299,-2.74569215859904,14.1696460121034));
#51620=CARTESIAN_POINT('Ctrl Pts',(6.26266287670776,-2.57061032234645,14.1786451049628));
#51621=CARTESIAN_POINT('Ctrl Pts',(6.33289076787979,-2.39235784854027,14.1876441978222));
#51622=CARTESIAN_POINT('Ctrl Pts',(6.39540817182099,-2.21157032802606,14.1966432906816));
#51623=CARTESIAN_POINT('Ctrl Pts',(6.45807216160402,-2.03035891129711,14.205663483899));
#51624=CARTESIAN_POINT('Ctrl Pts',(6.51298941293532,-1.84660078194002,14.2146836771164));
#51625=CARTESIAN_POINT('Ctrl Pts',(6.55999549279584,-1.66094796260998,14.2237038703338));
#51626=CARTESIAN_POINT('Ctrl Pts',(6.60704917808271,-1.47510712331225,14.2327331987555));
#51627=CARTESIAN_POINT('Ctrl Pts',(6.6461756330223,-1.28736799376254,14.2417625271772));
#51628=CARTESIAN_POINT('Ctrl Pts',(6.67726155662699,-1.09839296446732,14.2507918555988));
#51629=CARTESIAN_POINT('Ctrl Pts',(6.70839130511806,-0.90915151847199,14.2598339135536));
#51630=CARTESIAN_POINT('Ctrl Pts',(6.73145781792007,-0.718670924939345,
14.2688759715084));
#51631=CARTESIAN_POINT('Ctrl Pts',(6.74639940128629,-0.527621188281867,
14.2779180294631));
#51632=CARTESIAN_POINT('Ctrl Pts',(6.75936609995866,-0.361823206504845,
14.2857649649587));
#51633=CARTESIAN_POINT('Ctrl Pts',(6.76621454360319,-0.19559675795372,14.2936119004544));
#51634=CARTESIAN_POINT('Ctrl Pts',(6.76693621826582,-0.0293805704898146,
14.30145883595));
#51635=CARTESIAN_POINT('Ctrl Pts',(6.76773206856092,0.153919756782495,14.3101123002508));
#51636=CARTESIAN_POINT('Ctrl Pts',(6.7610763336698,0.337369176667206,14.3187657645516));
#51637=CARTESIAN_POINT('Ctrl Pts',(6.74696391042136,0.520352756763833,14.3274192288524));
#51638=CARTESIAN_POINT('Ctrl Pts',(6.73286448760132,0.703167771555361,14.3360647215426));
#51639=CARTESIAN_POINT('Ctrl Pts',(6.71132210038471,0.885517500421605,14.3447102142328));
#51640=CARTESIAN_POINT('Ctrl Pts',(6.68238366679435,1.06678841845987,14.353355706923));
#51641=CARTESIAN_POINT('Ctrl Pts',(6.65257467010642,1.25351256088969,14.3622612844195));
#51642=CARTESIAN_POINT('Ctrl Pts',(6.61491767142006,1.43909164593957,14.371166861916));
#51643=CARTESIAN_POINT('Ctrl Pts',(6.56952165561464,1.62285988810197,14.3800724394126));
#51644=CARTESIAN_POINT('Ctrl Pts',(6.52553503900052,1.80092272182056,14.3887015275851));
#51645=CARTESIAN_POINT('Ctrl Pts',(6.47428280818188,1.97728514116082,14.3973306157577));
#51646=CARTESIAN_POINT('Ctrl Pts',(6.4159161540952,2.15135048367771,14.4059597039302));
#51647=CARTESIAN_POINT('Ctrl Pts',(6.35474426327739,2.33378181016412,14.4150035260888));
#51648=CARTESIAN_POINT('Ctrl Pts',(6.28575726983507,2.51368947601402,14.4240473482473));
#51649=CARTESIAN_POINT('Ctrl Pts',(6.20918863901788,2.69040246897956,14.4330911704058));
#51650=CARTESIAN_POINT('Ctrl Pts',(6.13262000820066,2.86711546194517,14.4421349925643));
#51651=CARTESIAN_POINT('Ctrl Pts',(6.04846986142122,3.04063341469961,14.4511788147229));
#51652=CARTESIAN_POINT('Ctrl Pts',(5.9570309314573,3.21030706968367,14.4602226368814));
#51653=CARTESIAN_POINT('Ctrl Pts',(5.87184071050187,3.3683856491696,14.4686484267312));
#51654=CARTESIAN_POINT('Ctrl Pts',(5.78036136009623,3.5230582739114,14.477074216581));
#51655=CARTESIAN_POINT('Ctrl Pts',(5.68289859464026,3.67381988712509,14.4855000064308));
#51656=CARTESIAN_POINT('Ctrl Pts',(5.58541321454388,3.82461648210493,14.4939277513473));
#51657=CARTESIAN_POINT('Ctrl Pts',(5.48194183119702,3.97149997776411,14.5023554962638));
#51658=CARTESIAN_POINT('Ctrl Pts',(5.37283341293857,4.11399442352696,14.5107832411803));
#51659=CARTESIAN_POINT('Ctrl Pts',(5.26368490281046,4.25654122884956,14.5192140828703));
#51660=CARTESIAN_POINT('Ctrl Pts',(5.14889542917268,4.39469550550699,14.5276449245602));
#51661=CARTESIAN_POINT('Ctrl Pts',(5.02885438368019,4.52801419915403,14.5360757662501));
#51662=CARTESIAN_POINT('Ctrl Pts',(4.90870303578885,4.66145539566383,14.5445143548075));
#51663=CARTESIAN_POINT('Ctrl Pts',(4.78329069707587,4.79005188537434,14.5529529433648));
#51664=CARTESIAN_POINT('Ctrl Pts',(4.65304455351723,4.91339652205922,14.5613915319221));
#51665=CARTESIAN_POINT('Ctrl Pts',(4.52273011463673,5.03680583522075,14.5698345453024));
#51666=CARTESIAN_POINT('Ctrl Pts',(4.38757706164631,5.1549575811245,14.5782775586827));
#51667=CARTESIAN_POINT('Ctrl Pts',(4.24804625123498,5.26748441358572,14.5867205720629));
#51668=CARTESIAN_POINT('Ctrl Pts',(4.1083688539821,5.38012946332748,14.5951724554172));
#51669=CARTESIAN_POINT('Ctrl Pts',(3.9643047748306,5.48713759344893,14.6036243387715));
#51670=CARTESIAN_POINT('Ctrl Pts',(3.81634533099098,5.58818372233979,14.6120762221258));
#51671=CARTESIAN_POINT('Ctrl Pts',(3.77602170815514,5.61572198474927,14.6143796273549));
#51672=CARTESIAN_POINT('Ctrl Pts',(3.73540891556891,5.64281768567938,14.6166830325839));
#51673=CARTESIAN_POINT('Ctrl Pts',(3.69451722846398,5.66946482911596,14.618986437813));
#51674=CARTESIAN_POINT('Ctrl Pts',(3.54685060464839,5.76569205729348,14.6273044138501));
#51675=CARTESIAN_POINT('Ctrl Pts',(3.39527945585105,5.85623945284287,14.6356223898873));
#51676=CARTESIAN_POINT('Ctrl Pts',(3.24027485363508,5.94078343932012,14.6439403659244));
#51677=CARTESIAN_POINT('Ctrl Pts',(3.19351942856848,5.96628519841667,14.6464493914614));
#51678=CARTESIAN_POINT('Ctrl Pts',(3.14645182243516,5.99124101861392,14.6489584169983));
#51679=CARTESIAN_POINT('Ctrl Pts',(3.09908550384726,6.0156427786101,14.6514674425353));
#51680=CARTESIAN_POINT('Origin',(0.,0.,-63.6971797838103));
#51681=CARTESIAN_POINT('',(3.09908550384729,6.01564277861008,17.0455658338557));
#51682=CARTESIAN_POINT('',(3.09908550384718,6.01564277861013,16.6515258479908));
#51683=CARTESIAN_POINT('',(3.09908550384721,6.01564277861012,-63.6971797838103));
#51684=CARTESIAN_POINT('',(-6.76699962369028,-0.00225676218481283,15.6971797837776));
#51685=CARTESIAN_POINT('Ctrl Pts',(-6.76699962369006,-0.00225676287355765,
15.6971797838099));
#51686=CARTESIAN_POINT('Ctrl Pts',(-6.76698132045164,-0.0571398030595781,
15.6997530359089));
#51687=CARTESIAN_POINT('Ctrl Pts',(-6.76629528591052,-0.112013453905497,
15.7023262880079));
#51688=CARTESIAN_POINT('Ctrl Pts',(-6.7649424930389,-0.166859419502339,
15.7048995401069));
#51689=CARTESIAN_POINT('Ctrl Pts',(-6.76021966393885,-0.358335977203184,
15.7138831991354));
#51690=CARTESIAN_POINT('Ctrl Pts',(-6.74736714906962,-0.549449300788106,
15.7228668581638));
#51691=CARTESIAN_POINT('Ctrl Pts',(-6.72646848946574,-0.739534083206774,
15.7318505171923));
#51692=CARTESIAN_POINT('Ctrl Pts',(-6.70553392618607,-0.929945429267811,
15.7408496100518));
#51693=CARTESIAN_POINT('Ctrl Pts',(-6.67652561563581,-1.11932446463432,
15.7498487029113));
#51694=CARTESIAN_POINT('Ctrl Pts',(-6.63957850243178,-1.30701427308417,
15.7588477957708));
#51695=CARTESIAN_POINT('Ctrl Pts',(-6.60254475857209,-1.49514416168525,
15.7678679889883));
#51696=CARTESIAN_POINT('Ctrl Pts',(-6.55753501457225,-1.68157666299484,
15.7768881822058));
#51697=CARTESIAN_POINT('Ctrl Pts',(-6.50473527186347,-1.86566557640304,
15.7859083754233));
#51698=CARTESIAN_POINT('Ctrl Pts',(-6.45188205619393,-2.04994092593268,
15.7949377038451));
#51699=CARTESIAN_POINT('Ctrl Pts',(-6.39122315256914,-2.23186771794581,
15.8039670322669));
#51700=CARTESIAN_POINT('Ctrl Pts',(-6.32299396624546,-2.41081652201563,
15.8129963606887));
#51701=CARTESIAN_POINT('Ctrl Pts',(-6.25466859052188,-2.59001760782884,
15.8220384186436));
#51702=CARTESIAN_POINT('Ctrl Pts',(-6.17875167741203,-2.76623208745566,
15.8310804765984));
#51703=CARTESIAN_POINT('Ctrl Pts',(-6.09552706086693,-2.93884991965207,
15.8401225345533));
#51704=CARTESIAN_POINT('Ctrl Pts',(-6.02330255170285,-3.08865221037933,
15.8479694700483));
#51705=CARTESIAN_POINT('Ctrl Pts',(-5.9455752328829,-3.23574604873654,15.8558164055433));
#51706=CARTESIAN_POINT('Ctrl Pts',(-5.86255851577818,-3.37974801561844,
15.8636633410382));
#51707=CARTESIAN_POINT('Ctrl Pts',(-5.77100912069394,-3.53855088591681,
15.8723168053389));
#51708=CARTESIAN_POINT('Ctrl Pts',(-5.67294527554543,-3.69373294266671,
15.8809702696397));
#51709=CARTESIAN_POINT('Ctrl Pts',(-5.56867200572264,-3.84476021263759,
15.8896237339404));
#51710=CARTESIAN_POINT('Ctrl Pts',(-5.46449479290955,-3.9956483556015,15.8982692266305));
#51711=CARTESIAN_POINT('Ctrl Pts',(-5.35411973653381,-4.14238909634571,
15.9069147193207));
#51712=CARTESIAN_POINT('Ctrl Pts',(-5.23789610881431,-4.28447585513887,
15.9155602120108));
#51713=CARTESIAN_POINT('Ctrl Pts',(-5.11817609276777,-4.43083705016001,
15.9244657895074));
#51714=CARTESIAN_POINT('Ctrl Pts',(-4.99225027491115,-4.57225958993237,
15.933371367004));
#51715=CARTESIAN_POINT('Ctrl Pts',(-4.86054786135095,-4.70822296493239,
15.9422769445006));
#51716=CARTESIAN_POINT('Ctrl Pts',(-4.7329343809704,-4.83996511770704,15.9509060326731));
#51717=CARTESIAN_POINT('Ctrl Pts',(-4.59989783696624,-4.96658175199479,
15.9595351208455));
#51718=CARTESIAN_POINT('Ctrl Pts',(-4.4618691257133,-5.08763333044024,15.968164209018));
#51719=CARTESIAN_POINT('Ctrl Pts',(-4.31720643454498,-5.21450292843281,
15.9772080311766));
#51720=CARTESIAN_POINT('Ctrl Pts',(-4.16706008848616,-5.33525908049973,
15.9862518533353));
#51721=CARTESIAN_POINT('Ctrl Pts',(-4.0119694957848,-5.44943939913935,15.995295675494));
#51722=CARTESIAN_POINT('Ctrl Pts',(-3.85687890308344,-5.56361971777898,
16.0043394976526));
#51723=CARTESIAN_POINT('Ctrl Pts',(-3.69684435350022,-5.67122394665413,
16.0133833198112));
#51724=CARTESIAN_POINT('Ctrl Pts',(-3.53244552541382,-5.7718383215388,16.0224271419699));
#51725=CARTESIAN_POINT('Ctrl Pts',(-3.37928130427869,-5.86557696033318,
16.0308529318197));
#51726=CARTESIAN_POINT('Ctrl Pts',(-3.22239609884637,-5.95320757548475,
16.0392787216696));
#51727=CARTESIAN_POINT('Ctrl Pts',(-3.06230824364645,-6.03444754893893,
16.0477045115194));
#51728=CARTESIAN_POINT('Ctrl Pts',(-2.90218324267878,-6.11570637279985,
16.0561322564359));
#51729=CARTESIAN_POINT('Ctrl Pts',(-2.73885440588408,-6.1905714483703,16.0645600013524));
#51730=CARTESIAN_POINT('Ctrl Pts',(-2.57286280017949,-6.25880707574954,
16.072987746269));
#51731=CARTESIAN_POINT('Ctrl Pts',(-2.40681020088744,-6.32706777629853,
16.0814185879589));
#51732=CARTESIAN_POINT('Ctrl Pts',(-2.23809318823863,-6.38869404553378,
16.0898494296489));
#51733=CARTESIAN_POINT('Ctrl Pts',(-2.06727120825433,-6.44349895255076,
16.0982802713388));
#51734=CARTESIAN_POINT('Ctrl Pts',(-1.89629226467413,-6.49835421828199,
16.1067188598962));
#51735=CARTESIAN_POINT('Ctrl Pts',(-1.72320480529395,-6.54637549765692,
16.1151574484536));
#51736=CARTESIAN_POINT('Ctrl Pts',(-1.54858286775491,-6.58742590863047,
16.1235960370109));
#51737=CARTESIAN_POINT('Ctrl Pts',(-1.37386936618862,-6.62849784462546,
16.1320390503912));
#51738=CARTESIAN_POINT('Ctrl Pts',(-1.19762010586276,-6.66259155412601,
16.1404820637715));
#51739=CARTESIAN_POINT('Ctrl Pts',(-1.02041819412114,-6.68962149221513,
16.1489250771518));
#51740=CARTESIAN_POINT('Ctrl Pts',(-0.843030119420576,-6.71667982713815,
16.1573769605061));
#51741=CARTESIAN_POINT('Ctrl Pts',(-0.664687722586519,-6.73665952446968,
16.1658288438604));
#51742=CARTESIAN_POINT('Ctrl Pts',(-0.485979166360038,-6.74952689081716,
16.1742807272147));
#51743=CARTESIAN_POINT('Ctrl Pts',(-0.43727543896636,-6.7530336546571,16.1765841324436));
#51744=CARTESIAN_POINT('Ctrl Pts',(-0.388544518088214,-6.75601245986053,
16.1788875376724));
#51745=CARTESIAN_POINT('Ctrl Pts',(-0.339798300466749,-6.75846329538009,
16.1811909429013));
#51746=CARTESIAN_POINT('Ctrl Pts',(-0.16378271237999,-6.76731291031081,
16.1895082082347));
#51747=CARTESIAN_POINT('Ctrl Pts',(0.0127488507593406,-6.76929060122636,
16.1978254735681));
#51748=CARTESIAN_POINT('Ctrl Pts',(0.18922662558176,-6.76435379649608,16.2061427389015));
#51749=CARTESIAN_POINT('Ctrl Pts',(0.365555554980591,-6.75942115558072,
16.2144529892616));
#51750=CARTESIAN_POINT('Ctrl Pts',(0.541830440502447,-6.74758564794832,
16.2227632396216));
#51751=CARTESIAN_POINT('Ctrl Pts',(0.717479320325822,-6.72885669522727,
16.2310734899817));
#51752=CARTESIAN_POINT('Ctrl Pts',(0.893012221901616,-6.71014010894497,
16.2393782532116));
#51753=CARTESIAN_POINT('Ctrl Pts',(1.06791959669993,-6.68453918402528,16.2476830164414));
#51754=CARTESIAN_POINT('Ctrl Pts',(1.24163218191214,-6.65211534211788,16.2559877796713));
#51755=CARTESIAN_POINT('Ctrl Pts',(1.41526186657815,-6.61970697378254,16.2642885796339));
#51756=CARTESIAN_POINT('Ctrl Pts',(1.58769755676741,-6.58048224122146,16.2725893795965));
#51757=CARTESIAN_POINT('Ctrl Pts',(1.75837756446174,-6.53455410420616,16.2808901795591));
#51758=CARTESIAN_POINT('Ctrl Pts',(1.929007352293,-6.48863948081079,16.289188537144));
#51759=CARTESIAN_POINT('Ctrl Pts',(2.09788215184669,-6.43602547475562,16.2974868947289));
#51760=CARTESIAN_POINT('Ctrl Pts',(2.26445265911187,-6.37687565776856,16.3057852523139));
#51761=CARTESIAN_POINT('Ctrl Pts',(2.4310401145442,-6.31771982242326,16.3140844542376));
#51762=CARTESIAN_POINT('Ctrl Pts',(2.59532247894716,-6.25202695670496,16.3223836561614));
#51763=CARTESIAN_POINT('Ctrl Pts',(2.75676719261827,-6.18001000368961,16.3306828580852));
#51764=CARTESIAN_POINT('Ctrl Pts',(2.91822827372315,-6.1079857495203,16.3389829013907));
#51765=CARTESIAN_POINT('Ctrl Pts',(3.07685081263101,-6.02963627140844,16.3472829446963));
#51766=CARTESIAN_POINT('Ctrl Pts',(3.23212385080766,-5.94522198181365,16.3555829880018));
#51767=CARTESIAN_POINT('Ctrl Pts',(3.38743840639054,-5.86078512125359,16.3638852505997));
#51768=CARTESIAN_POINT('Ctrl Pts',(3.5394013705374,-5.77028038332949,16.3721875131976));
#51769=CARTESIAN_POINT('Ctrl Pts',(3.687527769292,-5.67401339007059,16.3804897757955));
#51770=CARTESIAN_POINT('Ctrl Pts',(3.83571836681454,-5.57770467418553,16.3887956366381));
#51771=CARTESIAN_POINT('Ctrl Pts',(3.9800687934584,-5.47562891508982,16.3971014974808));
#51772=CARTESIAN_POINT('Ctrl Pts',(4.12012420341948,-5.3681342707124,16.4054073583234));
#51773=CARTESIAN_POINT('Ctrl Pts',(4.26034516875616,-5.2605125600815,16.4137230372795));
#51774=CARTESIAN_POINT('Ctrl Pts',(4.39626069742289,-5.14745937821396,16.4220387162356));
#51775=CARTESIAN_POINT('Ctrl Pts',(4.52744921128366,-5.02936304508305,16.4303543951918));
#51776=CARTESIAN_POINT('Ctrl Pts',(4.65872070083473,-4.91119201696189,16.4386753337486));
#51777=CARTESIAN_POINT('Ctrl Pts',(4.78525896426821,-4.78797171875699,16.4469962723055));
#51778=CARTESIAN_POINT('Ctrl Pts',(4.90668020456831,-4.66012643284466,16.4553172108623));
#51779=CARTESIAN_POINT('Ctrl Pts',(5.02828191444139,-4.53209112923774,16.4636505169112));
#51780=CARTESIAN_POINT('Ctrl Pts',(5.14475117255765,-4.3994173614894,16.4719838229601));
#51781=CARTESIAN_POINT('Ctrl Pts',(5.2557444394465,-4.26256253763241,16.4803171290091));
#51782=CARTESIAN_POINT('Ctrl Pts',(5.33744203693728,-4.16182930734253,16.4864509342608));
#51783=CARTESIAN_POINT('Ctrl Pts',(5.41617369798555,-4.05883152237425,16.4925847395126));
#51784=CARTESIAN_POINT('Ctrl Pts',(5.49181783252645,-3.95376098093253,16.4987185447643));
#51785=CARTESIAN_POINT('Ctrl Pts',(5.59135719580181,-3.81549970188449,16.5067899580063));
#51786=CARTESIAN_POINT('Ctrl Pts',(5.6858549415438,-3.6732225761573,16.5148613712484));
#51787=CARTESIAN_POINT('Ctrl Pts',(5.77496001784963,-3.52733976138368,16.5229327844904));
#51788=CARTESIAN_POINT('Ctrl Pts',(5.86395323011254,-3.38164009040082,16.5309940647416));
#51789=CARTESIAN_POINT('Ctrl Pts',(5.94756705165948,-3.2323440514801,16.5390553449929));
#51790=CARTESIAN_POINT('Ctrl Pts',(6.02549066639004,-3.07989467827174,16.5471166252441));
#51791=CARTESIAN_POINT('Ctrl Pts',(6.10333354348565,-2.92760325977174,16.5551695531017));
#51792=CARTESIAN_POINT('Ctrl Pts',(6.17549777806015,-2.77216533810599,16.5632224809594));
#51793=CARTESIAN_POINT('Ctrl Pts',(6.24171593266433,-2.61405264214863,16.571275408817));
#51794=CARTESIAN_POINT('Ctrl Pts',(6.30787997806362,-2.4560691456882,16.5793217563414));
#51795=CARTESIAN_POINT('Ctrl Pts',(6.36810747072865,-2.29541556739407,16.5873681038658));
#51796=CARTESIAN_POINT('Ctrl Pts',(6.42217705079707,-2.13258784771353,16.5954144513901));
#51797=CARTESIAN_POINT('Ctrl Pts',(6.47621427632177,-1.96985756205353,16.6034559840833));
#51798=CARTESIAN_POINT('Ctrl Pts',(6.52410080741377,-1.80495607794764,16.6114975167765));
#51799=CARTESIAN_POINT('Ctrl Pts',(6.5656635874515,-1.63839880871953,16.6195390494696));
#51800=CARTESIAN_POINT('Ctrl Pts',(6.608025401025,-1.46863951971262,16.6277351785179));
#51801=CARTESIAN_POINT('Ctrl Pts',(6.64381769250576,-1.29716049929915,16.6359313075661));
#51802=CARTESIAN_POINT('Ctrl Pts',(6.67291058330975,-1.12452360897969,16.6441274366143));
#51803=CARTESIAN_POINT('Ctrl Pts',(6.70144486741583,-0.955201484590184,
16.6521661934504));
#51804=CARTESIAN_POINT('Ctrl Pts',(6.72353464443878,-0.784765936603242,
16.6602049502865));
#51805=CARTESIAN_POINT('Ctrl Pts',(6.73910910993699,-0.613756795778476,
16.6682437071226));
#51806=CARTESIAN_POINT('Ctrl Pts',(6.75468508287886,-0.442731103076344,
16.6762832420254));
#51807=CARTESIAN_POINT('Ctrl Pts',(6.76374445465041,-0.27113207893276,16.6843227769282));
#51808=CARTESIAN_POINT('Ctrl Pts',(6.76626839571479,-0.0995037544578944,
16.692362311831));
#51809=CARTESIAN_POINT('Ctrl Pts',(6.7687930808112,0.0721751642929305,16.7004042167066));
#51810=CARTESIAN_POINT('Ctrl Pts',(6.76477849490892,0.243883027340105,16.7084461215821));
#51811=CARTESIAN_POINT('Ctrl Pts',(6.75425793013242,0.415076876305283,16.7164880264576));
#51812=CARTESIAN_POINT('Ctrl Pts',(6.74338248269518,0.592045484507614,16.7248012031384));
#51813=CARTESIAN_POINT('Ctrl Pts',(6.72555448240518,0.76846435854144,16.7331143798192));
#51814=CARTESIAN_POINT('Ctrl Pts',(6.70086863396485,0.943741781604503,16.7414275565001));
#51815=CARTESIAN_POINT('Ctrl Pts',(6.67694686079383,1.11359402576181,16.7494834241106));
#51816=CARTESIAN_POINT('Ctrl Pts',(6.64658557937559,1.28237407680473,16.7575392917211));
#51817=CARTESIAN_POINT('Ctrl Pts',(6.60992246821841,1.44955647152551,16.7655951593317));
#51818=CARTESIAN_POINT('Ctrl Pts',(6.57150279560167,1.62474871980245,16.7740369905476));
#51819=CARTESIAN_POINT('Ctrl Pts',(6.52616270811494,1.79818598515055,16.7824788217636));
#51820=CARTESIAN_POINT('Ctrl Pts',(6.47411811650042,1.96928505138314,16.7909206529795));
#51821=CARTESIAN_POINT('Ctrl Pts',(6.42207352488591,2.14038411761566,16.7993624841955));
#51822=CARTESIAN_POINT('Ctrl Pts',(6.36332466156437,2.30914457739854,16.8078043154114));
#51823=CARTESIAN_POINT('Ctrl Pts',(6.29814318431123,2.47501139995638,16.8162461466274));
#51824=CARTESIAN_POINT('Ctrl Pts',(6.23458005286255,2.63676002992794,16.8244783814564));
#51825=CARTESIAN_POINT('Ctrl Pts',(6.16468883442206,2.79629523656879,16.8327106162853));
#51826=CARTESIAN_POINT('Ctrl Pts',(6.08864269601374,2.95308637196385,16.8409428511143));
#51827=CARTESIAN_POINT('Ctrl Pts',(6.00988326236478,3.11547175120014,16.8494688087285));
#51828=CARTESIAN_POINT('Ctrl Pts',(5.92452164224108,3.27491325502656,16.8579947663427));
#51829=CARTESIAN_POINT('Ctrl Pts',(5.83280655248278,3.43083906957379,16.866520723957));
#51830=CARTESIAN_POINT('Ctrl Pts',(5.74447415848501,3.58101392652816,16.8747322216415));
#51831=CARTESIAN_POINT('Ctrl Pts',(5.65024876378823,3.72792742854062,16.8829437193261));
#51832=CARTESIAN_POINT('Ctrl Pts',(5.55040114885524,3.87108978025393,16.8911552170106));
#51833=CARTESIAN_POINT('Ctrl Pts',(5.4506260637312,4.01414813811596,16.899360749822));
#51834=CARTESIAN_POINT('Ctrl Pts',(5.34523709463131,4.15346047881291,16.9075662826334));
#51835=CARTESIAN_POINT('Ctrl Pts',(5.23454974979036,4.28856361932171,16.9157718154448));
#51836=CARTESIAN_POINT('Ctrl Pts',(5.12392269914392,4.42359316573496,16.923972878495));
#51837=CARTESIAN_POINT('Ctrl Pts',(5.008003247532,4.55441780195135,16.9321739415453));
#51838=CARTESIAN_POINT('Ctrl Pts',(4.88714885980716,4.68060519827143,16.9403750045955));
#51839=CARTESIAN_POINT('Ctrl Pts',(4.7663383495365,4.80674678093259,16.9485730901638));
#51840=CARTESIAN_POINT('Ctrl Pts',(4.64059672034411,4.92825421936213,16.956771175732));
#51841=CARTESIAN_POINT('Ctrl Pts',(4.51032021251044,5.04472998094247,16.9649692613002));
#51842=CARTESIAN_POINT('Ctrl Pts',(4.38004966843678,5.16120041052934,16.9731669715789));
#51843=CARTESIAN_POINT('Ctrl Pts',(4.24524492243483,5.27263937874268,16.9813646818575));
#51844=CARTESIAN_POINT('Ctrl Pts',(4.10633760909274,5.37868761317764,16.9895623921362));
#51845=CARTESIAN_POINT('Ctrl Pts',(3.96743304694315,5.48473374722565,16.9977599400513));
#51846=CARTESIAN_POINT('Ctrl Pts',(3.82442636712194,5.58538914637848,17.0059574879665));
#51847=CARTESIAN_POINT('Ctrl Pts',(3.67778050834567,5.6803362164957,17.0141550358816));
#51848=CARTESIAN_POINT('Ctrl Pts',(3.53108214213304,5.77531728298543,17.0223555189783));
#51849=CARTESIAN_POINT('Ctrl Pts',(3.38074229823093,5.86458574775904,17.0305560020751));
#51850=CARTESIAN_POINT('Ctrl Pts',(3.22725130109749,5.94786836098149,17.0387564851718));
#51851=CARTESIAN_POINT('Ctrl Pts',(3.18476706746597,5.97091986278722,17.0410262680665));
#51852=CARTESIAN_POINT('Ctrl Pts',(3.14204156470054,5.99351305608632,17.0432960509611));
#51853=CARTESIAN_POINT('Ctrl Pts',(3.09908550384729,6.01564277861008,17.0455658338557));
#51854=CARTESIAN_POINT('Ctrl Pts',(3.09908550384722,6.01564277861011,15.0459090623666));
#51855=CARTESIAN_POINT('Ctrl Pts',(2.94791065649508,6.09352369594803,15.053887487038));
#51856=CARTESIAN_POINT('Ctrl Pts',(2.79367270731465,6.16576841633157,15.0618659117094));
#51857=CARTESIAN_POINT('Ctrl Pts',(2.63678901268786,6.23214511244472,15.0698443363808));
#51858=CARTESIAN_POINT('Ctrl Pts',(2.47534685772831,6.30045047002248,15.0780545845853));
#51859=CARTESIAN_POINT('Ctrl Pts',(2.31125754215692,6.36247497736568,15.0862648327899));
#51860=CARTESIAN_POINT('Ctrl Pts',(2.14505142902513,6.41802488050937,15.0944750809944));
#51861=CARTESIAN_POINT('Ctrl Pts',(1.97880580538659,6.47358798897253,15.1026872809386));
#51862=CARTESIAN_POINT('Ctrl Pts',(1.81044271925723,6.52267331398955,15.1108994808828));
#51863=CARTESIAN_POINT('Ctrl Pts',(1.64050790061722,6.56513692378251,15.119111680827));
#51864=CARTESIAN_POINT('Ctrl Pts',(1.47050242445597,6.6076181896005,15.1273272953375));
#51865=CARTESIAN_POINT('Ctrl Pts',(1.29892425888759,6.643472168885,15.135542909848));
#51866=CARTESIAN_POINT('Ctrl Pts',(1.12632961815818,6.67260598201779,15.1437585243584));
#51867=CARTESIAN_POINT('Ctrl Pts',(0.953541161212214,6.70177251114578,15.1519833646439));
#51868=CARTESIAN_POINT('Ctrl Pts',(0.779734300361377,6.72420374214697,15.1602082049293));
#51869=CARTESIAN_POINT('Ctrl Pts',(0.605471646608188,6.73985853598973,15.1684330452147));
#51870=CARTESIAN_POINT('Ctrl Pts',(0.431097371567741,6.75552335727211,15.1766631537963));
#51871=CARTESIAN_POINT('Ctrl Pts',(0.256267076202778,6.76440307072837,15.1848932623778));
#51872=CARTESIAN_POINT('Ctrl Pts',(0.0815436259758152,6.76650867412898,
15.1931233709594));
#51873=CARTESIAN_POINT('Ctrl Pts',(-0.0934193727826761,6.76861716434417,
15.2013647631461));
#51874=CARTESIAN_POINT('Ctrl Pts',(-0.268274879042422,6.76393300338852,
15.2096061553328));
#51875=CARTESIAN_POINT('Ctrl Pts',(-0.442463881960391,6.75251913830391,
15.2178475475195));
#51876=CARTESIAN_POINT('Ctrl Pts',(-0.518275361554963,6.74755153423326,
15.2214344107837));
#51877=CARTESIAN_POINT('Ctrl Pts',(-0.593960701927358,6.74130984104823,
15.2250212740479));
#51878=CARTESIAN_POINT('Ctrl Pts',(-0.66947444095361,6.73380226713778,15.2286081373121));
#51879=CARTESIAN_POINT('Ctrl Pts',(-0.847339440716848,6.71611893362755,
15.2370566321405));
#51880=CARTESIAN_POINT('Ctrl Pts',(-1.02465734435062,6.69136886435576,15.245505126969));
#51881=CARTESIAN_POINT('Ctrl Pts',(-1.20084374890138,6.65959933409845,15.2539536217974));
#51882=CARTESIAN_POINT('Ctrl Pts',(-1.37686921740663,6.62785882346147,15.2623943994166));
#51883=CARTESIAN_POINT('Ctrl Pts',(-1.55176492044309,6.58911169152856,15.2708351770357));
#51884=CARTESIAN_POINT('Ctrl Pts',(-1.72495236976604,6.54345690916037,15.2792759546549));
#51885=CARTESIAN_POINT('Ctrl Pts',(-1.89800825492073,6.49783680905982,15.2877103201242));
#51886=CARTESIAN_POINT('Ctrl Pts',(-2.0693581520363,6.44531960414918,15.2961446855935));
#51887=CARTESIAN_POINT('Ctrl Pts',(-2.23843415879977,6.38605523909075,15.3045790510627));
#51888=CARTESIAN_POINT('Ctrl Pts',(-2.40740768932165,6.32682679390946,15.3130083044993));
#51889=CARTESIAN_POINT('Ctrl Pts',(-2.57410976335735,6.26085945185644,15.3214375579359));
#51890=CARTESIAN_POINT('Ctrl Pts',(-2.73798764947457,6.18835298212091,15.3298668113725));
#51891=CARTESIAN_POINT('Ctrl Pts',(-2.90179134829885,6.11587933596419,15.3382922488977));
#51892=CARTESIAN_POINT('Ctrl Pts',(-3.06277310414549,6.03687259960411,15.3467176864229));
#51893=CARTESIAN_POINT('Ctrl Pts',(-3.22039981611449,5.95158080045712,15.3551431239481));
#51894=CARTESIAN_POINT('Ctrl Pts',(-3.37799190173474,5.8663077376242,15.3635667106312));
#51895=CARTESIAN_POINT('Ctrl Pts',(-3.5322301186995,5.77475252099084,15.3719902973144));
#51896=CARTESIAN_POINT('Ctrl Pts',(-3.68260517224159,5.67720953861838,15.3804138839976));
#51897=CARTESIAN_POINT('Ctrl Pts',(-3.83296339960315,5.57967747079452,15.3888365281256));
#51898=CARTESIAN_POINT('Ctrl Pts',(-3.9794590456418,5.47615915432116,15.3972591722536));
#51899=CARTESIAN_POINT('Ctrl Pts',(-4.12161079945174,5.36699295861684,15.4056818163816));
#51900=CARTESIAN_POINT('Ctrl Pts',(-4.26376646971315,5.25782375525278,15.4141046925635));
#51901=CARTESIAN_POINT('Ctrl Pts',(-4.40157774494995,5.14300656579612,15.4225275687454));
#51902=CARTESIAN_POINT('Ctrl Pts',(-4.53459518798329,5.0229210108381,15.4309504449274));
#51903=CARTESIAN_POINT('Ctrl Pts',(-4.66763484566817,4.90281540092564,15.4393747277764));
#51904=CARTESIAN_POINT('Ctrl Pts',(-4.79587882796318,4.77743989519189,15.4477990106255));
#51905=CARTESIAN_POINT('Ctrl Pts',(-4.91891319035554,4.64721228541868,15.4562232934745));
#51906=CARTESIAN_POINT('Ctrl Pts',(-5.04203064560674,4.51689672473334,15.4646532657726));
#51907=CARTESIAN_POINT('Ctrl Pts',(-5.15993122124276,4.38172275455596,15.4730832380708));
#51908=CARTESIAN_POINT('Ctrl Pts',(-5.27223937418251,4.24214344186046,15.4815132103689));
#51909=CARTESIAN_POINT('Ctrl Pts',(-5.38458767547467,4.10251423181297,15.4899461962462));
#51910=CARTESIAN_POINT('Ctrl Pts',(-5.49133936356548,3.95847680267804,15.4983791821234));
#51911=CARTESIAN_POINT('Ctrl Pts',(-5.59216083866854,3.81051520853309,15.5068121680006));
#51912=CARTESIAN_POINT('Ctrl Pts',(-5.69307506891403,3.66241749062359,15.5152529121734));
#51913=CARTESIAN_POINT('Ctrl Pts',(-5.78804800305449,3.51038867373545,15.5236936563462));
#51914=CARTESIAN_POINT('Ctrl Pts',(-5.87679023152679,3.35494047259133,15.532134400519));
#51915=CARTESIAN_POINT('Ctrl Pts',(-5.92585817974336,3.26898901052635,15.5368015134044));
#51916=CARTESIAN_POINT('Ctrl Pts',(-5.97302204020799,3.18199258788588,15.5414686262898));
#51917=CARTESIAN_POINT('Ctrl Pts',(-6.01823906458843,3.09404065284569,15.5461357391752));
#51918=CARTESIAN_POINT('Ctrl Pts',(-6.09744684373968,2.93997307449344,15.5543112361648));
#51919=CARTESIAN_POINT('Ctrl Pts',(-6.17083323312904,2.78267001192737,15.5624867331544));
#51920=CARTESIAN_POINT('Ctrl Pts',(-6.23812381222279,2.62261325844644,15.5706622301439));
#51921=CARTESIAN_POINT('Ctrl Pts',(-6.30535387216047,2.46270045527436,15.5788303743334));
#51922=CARTESIAN_POINT('Ctrl Pts',(-6.36649889697672,2.30003922375514,15.5869985185228));
#51923=CARTESIAN_POINT('Ctrl Pts',(-6.42133040351226,2.13513579168377,15.5951666627123));
#51924=CARTESIAN_POINT('Ctrl Pts',(-6.47839694748146,1.96351057925462,15.6036677561344));
#51925=CARTESIAN_POINT('Ctrl Pts',(-6.52862424305058,1.78945686915077,15.6121688495565));
#51926=CARTESIAN_POINT('Ctrl Pts',(-6.57180970945634,1.61356937957296,15.6206699429786));
#51927=CARTESIAN_POINT('Ctrl Pts',(-6.61325069369425,1.44478688652871,15.628827633698));
#51928=CARTESIAN_POINT('Ctrl Pts',(-6.64820750101947,1.27431625047136,15.6369853244174));
#51929=CARTESIAN_POINT('Ctrl Pts',(-6.67655179969668,1.10269899155074,15.6451430151368));
#51930=CARTESIAN_POINT('Ctrl Pts',(-6.70488750477797,0.931133764588747,
15.6532982325582));
#51931=CARTESIAN_POINT('Ctrl Pts',(-6.7266146365196,0.758422964707003,15.6614534499795));
#51932=CARTESIAN_POINT('Ctrl Pts',(-6.74165602440339,0.585117978381655,
15.6696086674009));
#51933=CARTESIAN_POINT('Ctrl Pts',(-6.75669650310326,0.411823467559594,
15.6777633918762));
#51934=CARTESIAN_POINT('Ctrl Pts',(-6.76505201088149,0.237935202829579,
15.6859181163516));
#51935=CARTESIAN_POINT('Ctrl Pts',(-6.76669725855707,0.0640094605216243,
15.6940728408269));
#51936=CARTESIAN_POINT('Ctrl Pts',(-6.76690620453611,0.0419209415431688,
15.6951084884771));
#51937=CARTESIAN_POINT('Ctrl Pts',(-6.76700699012752,0.0198318204418481,
15.6961441361274));
#51938=CARTESIAN_POINT('Ctrl Pts',(-6.76699962369028,-0.0022567621848848,
15.6971797837776));
#51939=CARTESIAN_POINT('',(-6.76699885577408,0.00393521947970883,15.302820216215));
#51940=CARTESIAN_POINT('Ctrl Pts',(3.09908550384726,6.0156427786101,14.6514674425353));
#51941=CARTESIAN_POINT('Ctrl Pts',(2.94223581389065,6.09644721104014,14.6597758753902));
#51942=CARTESIAN_POINT('Ctrl Pts',(2.7821086280402,6.17117268014464,14.668084308245));
#51943=CARTESIAN_POINT('Ctrl Pts',(2.61921061121263,6.239553251164,14.6763927410999));
#51944=CARTESIAN_POINT('Ctrl Pts',(2.45641114893688,6.30789245141248,14.684696147289));
#51945=CARTESIAN_POINT('Ctrl Pts',(2.29084451598339,6.36989426874963,14.6929995534781));
#51946=CARTESIAN_POINT('Ctrl Pts',(2.12303989010122,6.42533972837538,14.7013029596673));
#51947=CARTESIAN_POINT('Ctrl Pts',(1.95530607309647,6.48076179156177,14.7096028620503));
#51948=CARTESIAN_POINT('Ctrl Pts',(1.78533647498609,6.52963290194865,14.7179027644333));
#51949=CARTESIAN_POINT('Ctrl Pts',(1.6136782828608,6.5717829695923,14.7262026668164));
#51950=CARTESIAN_POINT('Ctrl Pts',(1.44206111582549,6.61392296366885,14.7345005855816));
#51951=CARTESIAN_POINT('Ctrl Pts',(1.26875649672477,6.64934503422806,14.7427985043469));
#51952=CARTESIAN_POINT('Ctrl Pts',(1.09432495510236,6.67792946149031,14.7510964231121));
#51953=CARTESIAN_POINT('Ctrl Pts',(0.919864152507174,6.70651868380361,14.7593957338571));
#51954=CARTESIAN_POINT('Ctrl Pts',(0.744276391991946,6.72826790884433,14.7676950446021));
#51955=CARTESIAN_POINT('Ctrl Pts',(0.568131141044132,6.7431087790852,14.7759943553472));
#51956=CARTESIAN_POINT('Ctrl Pts',(0.391959205880474,6.75795189756713,14.7842949233534));
#51957=CARTESIAN_POINT('Ctrl Pts',(0.215229958711135,6.76588454577244,14.7925954913597));
#51958=CARTESIAN_POINT('Ctrl Pts',(0.0385166028543294,6.76689038416499,
14.800896059366));
#51959=CARTESIAN_POINT('Ctrl Pts',(-0.138252858901103,6.76789654190786,
14.8091992627748));
#51960=CARTESIAN_POINT('Ctrl Pts',(-0.315006071414334,6.76197150467151,
14.8175024661836));
#51961=CARTESIAN_POINT('Ctrl Pts',(-0.491171025936373,6.74915105945041,
14.8258056695924));
#51962=CARTESIAN_POINT('Ctrl Pts',(-0.667421161029729,6.73632441519358,
14.834112887827));
#51963=CARTESIAN_POINT('Ctrl Pts',(-0.843082124584112,6.71659574321202,
14.8424201060617));
#51964=CARTESIAN_POINT('Ctrl Pts',(-1.01758801963393,6.69005258740897,14.8507273242963));
#51965=CARTESIAN_POINT('Ctrl Pts',(-1.19230221256526,6.66347774853229,14.8590444583906));
#51966=CARTESIAN_POINT('Ctrl Pts',(-1.36585823866266,6.63007222923399,14.8673615924849));
#51967=CARTESIAN_POINT('Ctrl Pts',(-1.53770026841016,6.58997472563676,14.8756787265792));
#51968=CARTESIAN_POINT('Ctrl Pts',(-1.70965875565764,6.54985004792485,14.8840014972028));
#51969=CARTESIAN_POINT('Ctrl Pts',(-1.8799005955692,6.50302443424873,14.8923242678264));
#51970=CARTESIAN_POINT('Ctrl Pts',(-2.04788593809083,6.44968620822516,14.90064703845));
#51971=CARTESIAN_POINT('Ctrl Pts',(-2.21610664706218,6.39627324931892,14.9089814702159));
#51972=CARTESIAN_POINT('Ctrl Pts',(-2.38206421600202,6.33632956638265,14.9173159019817));
#51973=CARTESIAN_POINT('Ctrl Pts',(-2.54523850425461,6.27009170239636,14.9256503337476));
#51974=CARTESIAN_POINT('Ctrl Pts',(-2.61613625839305,6.24131194888345,14.9292715690571));
#51975=CARTESIAN_POINT('Ctrl Pts',(-2.68650888650556,6.2113445558385,14.9328928043665));
#51976=CARTESIAN_POINT('Ctrl Pts',(-2.7563152404219,6.18021158985823,14.936514039676));
#51977=CARTESIAN_POINT('Ctrl Pts',(-2.91190742961283,6.11081896209426,14.944585452918));
#51978=CARTESIAN_POINT('Ctrl Pts',(-3.06516359421407,6.03541901204667,14.9526568661601));
#51979=CARTESIAN_POINT('Ctrl Pts',(-3.21557397391724,5.95418953496327,14.9607282794021));
#51980=CARTESIAN_POINT('Ctrl Pts',(-3.365795525847,5.87306203476021,14.9687895596533));
#51981=CARTESIAN_POINT('Ctrl Pts',(-3.51317807752925,5.78611974441354,14.9768508399045));
#51982=CARTESIAN_POINT('Ctrl Pts',(-3.65723009588752,5.69358911634257,14.9849121201558));
#51983=CARTESIAN_POINT('Ctrl Pts',(-3.80113286014219,5.6011543604163,14.9929650480134));
#51984=CARTESIAN_POINT('Ctrl Pts',(-3.94171164713815,5.50314298918696,15.001017975871));
#51985=CARTESIAN_POINT('Ctrl Pts',(-4.07849797076714,5.39982808082335,15.0090709037287));
#51986=CARTESIAN_POINT('Ctrl Pts',(-4.21517252143495,5.2965975947392,15.0171172512531));
#51987=CARTESIAN_POINT('Ctrl Pts',(-4.34806048061897,5.18807242072281,15.0251635987774));
#51988=CARTESIAN_POINT('Ctrl Pts',(-4.476720997698,5.07456974617256,15.0332099463018));
#51989=CARTESIAN_POINT('Ctrl Pts',(-4.60530452597265,4.961134990168,15.041251478995));
#51990=CARTESIAN_POINT('Ctrl Pts',(-4.72966536895888,4.84272890902312,15.0492930116881));
#51991=CARTESIAN_POINT('Ctrl Pts',(-4.84939461938599,4.7197098242869,15.0573345443813));
#51992=CARTESIAN_POINT('Ctrl Pts',(-4.97142563322307,4.5943257299397,15.0655306734295));
#51993=CARTESIAN_POINT('Ctrl Pts',(-5.08864484479072,4.46414969907813,15.0737268024778));
#51994=CARTESIAN_POINT('Ctrl Pts',(-5.20065728709588,4.32960191959683,15.081922931526));
#51995=CARTESIAN_POINT('Ctrl Pts',(-5.31051900120609,4.19763756475071,15.0899616883621));
#51996=CARTESIAN_POINT('Ctrl Pts',(-5.41537185162273,4.06146813343074,15.0980004451982));
#51997=CARTESIAN_POINT('Ctrl Pts',(-5.51488300729395,3.92152450149944,15.1060392020343));
#51998=CARTESIAN_POINT('Ctrl Pts',(-5.61440379459327,3.7815673245037,15.1140787369371));
#51999=CARTESIAN_POINT('Ctrl Pts',(-5.70858164114063,3.63783552383456,15.1221182718399));
#52000=CARTESIAN_POINT('Ctrl Pts',(-5.79712651734152,3.49078975905679,15.1301578067427));
#52001=CARTESIAN_POINT('Ctrl Pts',(-5.885697495667,3.34370064669036,15.1381997116182));
#52002=CARTESIAN_POINT('Ctrl Pts',(-5.96863200582886,3.19329594544603,15.1462416164937));
#52003=CARTESIAN_POINT('Ctrl Pts',(-6.04568559993949,3.04006161560655,15.1542835213693));
#52004=CARTESIAN_POINT('Ctrl Pts',(-6.1253383876371,2.88165834209843,15.1625966980501));
#52005=CARTESIAN_POINT('Ctrl Pts',(-6.19870636962145,2.72023159112665,15.1709098747309));
#52006=CARTESIAN_POINT('Ctrl Pts',(-6.26557363347915,2.55634036142509,15.1792230514117));
#52007=CARTESIAN_POINT('Ctrl Pts',(-6.33037122479694,2.39752188568526,15.1872789190223));
#52008=CARTESIAN_POINT('Ctrl Pts',(-6.38906446492972,2.23638959034347,15.1953347866328));
#52009=CARTESIAN_POINT('Ctrl Pts',(-6.44150791704022,2.07346684437157,15.2033906542433));
#52010=CARTESIAN_POINT('Ctrl Pts',(-6.49646398043434,1.90273832830993,15.2118324854593));
#52011=CARTESIAN_POINT('Ctrl Pts',(-6.54455652681935,1.73004404488682,15.2202743166753));
#52012=CARTESIAN_POINT('Ctrl Pts',(-6.58567866377099,1.55599663802708,15.2287161478912));
#52013=CARTESIAN_POINT('Ctrl Pts',(-6.62680080072263,1.38194923116734,15.2371579791072));
#52014=CARTESIAN_POINT('Ctrl Pts',(-6.66095252412015,1.20654916983101,15.2455998103232));
#52015=CARTESIAN_POINT('Ctrl Pts',(-6.68808929934124,1.03041279302872,15.2540416415391));
#52016=CARTESIAN_POINT('Ctrl Pts',(-6.74035652201825,0.691162489599462,
15.2703011664227));
#52017=CARTESIAN_POINT('Ctrl Pts',(-6.766798755653,0.34802710901653,15.2865606913062));
#52018=CARTESIAN_POINT('Ctrl Pts',(-6.76699885577377,0.00393522001405927,
15.3028202161898));
#52019=CARTESIAN_POINT('Ctrl Pts',(-6.76699885577408,0.00393521947970433,
15.3028202162151));
#52020=CARTESIAN_POINT('Ctrl Pts',(-6.76709797409406,-0.166508528672056,
15.3108742693703));
#52021=CARTESIAN_POINT('Ctrl Pts',(-6.76075336727106,-0.33721982332612,
15.3189283225256));
#52022=CARTESIAN_POINT('Ctrl Pts',(-6.74793081125063,-0.507660089601789,
15.3269823756808));
#52023=CARTESIAN_POINT('Ctrl Pts',(-6.73512136567371,-0.677926088946617,
15.3350281939562));
#52024=CARTESIAN_POINT('Ctrl Pts',(-6.71584717939243,-0.847921241071309,
15.3430740122315));
#52025=CARTESIAN_POINT('Ctrl Pts',(-6.69012601859959,-1.01710513480999,
15.3511198305069));
#52026=CARTESIAN_POINT('Ctrl Pts',(-6.66442548622603,-1.18615334274805,
15.3591591960208));
#52027=CARTESIAN_POINT('Ctrl Pts',(-6.63228832647834,-1.35439121892961,
15.3671985615348));
#52028=CARTESIAN_POINT('Ctrl Pts',(-6.59378425325154,-1.52128176928934,
15.3752379270487));
#52029=CARTESIAN_POINT('Ctrl Pts',(-6.5546043610467,-1.69110156301832,15.3834183985635));
#52030=CARTESIAN_POINT('Ctrl Pts',(-6.50883198403785,-1.85952590036126,
15.3915988700782));
#52031=CARTESIAN_POINT('Ctrl Pts',(-6.45659539920556,-2.02599724850693,
15.3997793415929));
#52032=CARTESIAN_POINT('Ctrl Pts',(-6.40530323508075,-2.18945884804641,
15.4078119128052));
#52033=CARTESIAN_POINT('Ctrl Pts',(-6.34777874086579,-2.35103710651839,
15.4158444840175));
#52034=CARTESIAN_POINT('Ctrl Pts',(-6.28419419467783,-2.51021758490723,
15.4238770552298));
#52035=CARTESIAN_POINT('Ctrl Pts',(-6.22061531511023,-2.66938387721793,
15.4319089105836));
#52036=CARTESIAN_POINT('Ctrl Pts',(-6.15097759710344,-2.82615246665587,
15.4399407659375));
#52037=CARTESIAN_POINT('Ctrl Pts',(-6.07550194224933,-2.98002770955652,
15.4479726212914));
#52038=CARTESIAN_POINT('Ctrl Pts',(-6.00001797688494,-3.13391989542759,
15.4560053610207));
#52039=CARTESIAN_POINT('Ctrl Pts',(-5.9186949608861,-3.28491776452564,15.46403810075));
#52040=CARTESIAN_POINT('Ctrl Pts',(-5.83180026134308,-3.43254930216578,
15.4720708404793));
#52041=CARTESIAN_POINT('Ctrl Pts',(-5.74210604203649,-3.58493714150813,
15.4803623740562));
#52042=CARTESIAN_POINT('Ctrl Pts',(-5.64647532842407,-3.73373773384368,
15.4886539076331));
#52043=CARTESIAN_POINT('Ctrl Pts',(-5.54525076988173,-3.8784639870864,15.49694544121));
#52044=CARTESIAN_POINT('Ctrl Pts',(-5.44705977048966,-4.01885299592785,
15.5049884890645));
#52045=CARTESIAN_POINT('Ctrl Pts',(-5.3436056502797,-4.15540808818343,15.513031536919));
#52046=CARTESIAN_POINT('Ctrl Pts',(-5.23524201657913,-4.28771851079854,
15.5210745847735));
#52047=CARTESIAN_POINT('Ctrl Pts',(-5.12185662689373,-4.42616042452312,
15.5294903612116));
#52048=CARTESIAN_POINT('Ctrl Pts',(-5.00309616237061,-4.55995452387688,
15.5379061376497));
#52049=CARTESIAN_POINT('Ctrl Pts',(-4.87940813424595,-4.68867414728881,
15.5463219140878));
#52050=CARTESIAN_POINT('Ctrl Pts',(-4.75572010612129,-4.81739377070075,
15.5547376905258));
#52051=CARTESIAN_POINT('Ctrl Pts',(-4.62710489635256,-4.94103864852683,
15.5631534669639));
#52052=CARTESIAN_POINT('Ctrl Pts',(-4.49404799525706,-5.0592313266272,15.571569243402));
#52053=CARTESIAN_POINT('Ctrl Pts',(-4.3527790021099,-5.18471869703139,15.5805044301843));
#52054=CARTESIAN_POINT('Ctrl Pts',(-4.20616143137451,-5.30436555192128,
15.5894396169665));
#52055=CARTESIAN_POINT('Ctrl Pts',(-4.05468105371477,-5.41773481749029,
15.5983748037488));
#52056=CARTESIAN_POINT('Ctrl Pts',(-3.9034275467992,-5.53093429097109,15.6072966083855));
#52057=CARTESIAN_POINT('Ctrl Pts',(-3.74732597137332,-5.63787478071781,
15.6162184130221));
#52058=CARTESIAN_POINT('Ctrl Pts',(-3.586895273272,-5.73815922562097,15.6251402176587));
#52059=CARTESIAN_POINT('Ctrl Pts',(-3.4268559036905,-5.83819905297992,15.634040259898));
#52060=CARTESIAN_POINT('Ctrl Pts',(-3.26250870556334,-5.93161510245008,
15.6429403021373));
#52061=CARTESIAN_POINT('Ctrl Pts',(-3.09440116547005,-6.01805370756507,
15.6518403443766));
#52062=CARTESIAN_POINT('Ctrl Pts',(-2.92655242940633,-6.10435923917661,
15.6607266848699));
#52063=CARTESIAN_POINT('Ctrl Pts',(-2.75495512773007,-6.18370863615309,
15.6696130253633));
#52064=CARTESIAN_POINT('Ctrl Pts',(-2.58018344911085,-6.25579270508018,
15.6784993658567));
#52065=CARTESIAN_POINT('Ctrl Pts',(-2.40585863116678,-6.32769246762559,
15.6873629855286));
#52066=CARTESIAN_POINT('Ctrl Pts',(-2.22837587000653,-6.39236387152424,
15.6962266052005));
#52067=CARTESIAN_POINT('Ctrl Pts',(-2.04833084499392,-6.44954492576387,
15.7050902248724));
#52068=CARTESIAN_POINT('Ctrl Pts',(-1.87741331056537,-6.50382715214573,
15.7135044980262));
#52069=CARTESIAN_POINT('Ctrl Pts',(-1.70418707205572,-6.55135946454181,
15.72191877118));
#52070=CARTESIAN_POINT('Ctrl Pts',(-1.52918061718334,-6.59195689003128,
15.7303330443337));
#52071=CARTESIAN_POINT('Ctrl Pts',(-1.3584176284331,-6.63156993011715,15.7385432925382));
#52072=CARTESIAN_POINT('Ctrl Pts',(-1.18612359201481,-6.66454125114756,
15.7467535407428));
#52073=CARTESIAN_POINT('Ctrl Pts',(-1.01285423788337,-6.69077090422335,
15.7549637889473));
#52074=CARTESIAN_POINT('Ctrl Pts',(-0.839543694171909,-6.71700679261062,
15.7631759888915));
#52075=CARTESIAN_POINT('Ctrl Pts',(-0.665257722775855,-6.73649776686892,
15.7713881888357));
#52076=CARTESIAN_POINT('Ctrl Pts',(-0.490558650524202,-6.74919559728386,
15.77960038878));
#52077=CARTESIAN_POINT('Ctrl Pts',(-0.315786939811825,-6.76189870735395,
15.7878160032905));
#52078=CARTESIAN_POINT('Ctrl Pts',(-0.140602140771924,-6.76780302070672,
15.796031617801));
#52079=CARTESIAN_POINT('Ctrl Pts',(0.0344318441392134,-6.76691240139173,
15.8042472323115));
#52080=CARTESIAN_POINT('Ctrl Pts',(0.209662384541716,-6.76602078195029,
15.8124720725969));
#52081=CARTESIAN_POINT('Ctrl Pts',(0.384741416475649,-6.75831899125156,
15.8206969128824));
#52082=CARTESIAN_POINT('Ctrl Pts',(0.559107606873107,-6.74386296449866,
15.8289217531678));
#52083=CARTESIAN_POINT('Ctrl Pts',(0.73358548487677,-6.72939767815811,15.8371518617493));
#52084=CARTESIAN_POINT('Ctrl Pts',(0.907349258729725,-6.70816957450446,
15.8453819703309));
#52085=CARTESIAN_POINT('Ctrl Pts',(1.0798462840235,-6.6802859970873,15.8536120789124));
#52086=CARTESIAN_POINT('Ctrl Pts',(1.25257980538611,-6.65236419085759,15.8618534710991));
#52087=CARTESIAN_POINT('Ctrl Pts',(1.42404276136469,-6.61776875531765,15.8700948632858));
#52088=CARTESIAN_POINT('Ctrl Pts',(1.59369521228511,-6.576657553069,15.8783362554725));
#52089=CARTESIAN_POINT('Ctrl Pts',(1.66753226919263,-6.55876491336058,15.8819231187367));
#52090=CARTESIAN_POINT('Ctrl Pts',(1.74102660014215,-6.53963868008357,15.8855099820009));
#52091=CARTESIAN_POINT('Ctrl Pts',(1.81413482365718,-6.51929473498433,15.8890968452651));
#52092=CARTESIAN_POINT('Ctrl Pts',(1.98633387413338,-6.47137662316876,15.8975453400935));
#52093=CARTESIAN_POINT('Ctrl Pts',(2.15678227119935,-6.41659023055404,15.9059938349219));
#52094=CARTESIAN_POINT('Ctrl Pts',(2.32491237193879,-6.35508233328302,15.9144423297504));
#52095=CARTESIAN_POINT('Ctrl Pts',(2.49288889559806,-6.2936306199031,15.9228831073695));
#52096=CARTESIAN_POINT('Ctrl Pts',(2.65855103235927,-6.22546975417097,15.9313238849887));
#52097=CARTESIAN_POINT('Ctrl Pts',(2.8213458302109,-6.1507964286222,15.9397646626079));
#52098=CARTESIAN_POINT('Ctrl Pts',(2.98401695881191,-6.07617982966625,15.9481990280772));
#52099=CARTESIAN_POINT('Ctrl Pts',(3.1438247887736,-5.99506077187894,15.9566333935465));
#52100=CARTESIAN_POINT('Ctrl Pts',(3.30023553719457,-5.90768435167605,15.9650677590158));
#52101=CARTESIAN_POINT('Ctrl Pts',(3.45655148573321,-5.82036088994588,15.9734970124524));
#52102=CARTESIAN_POINT('Ctrl Pts',(3.60947416737169,-5.72678778939718,15.9819262658891));
#52103=CARTESIAN_POINT('Ctrl Pts',(3.75849328831579,-5.62725663193755,15.9903555193258));
#52104=CARTESIAN_POINT('Ctrl Pts',(3.90744494850998,-5.52777053209522,15.998780956851));
#52105=CARTESIAN_POINT('Ctrl Pts',(4.05249629488894,-5.42233193849658,16.0072063943763));
#52106=CARTESIAN_POINT('Ctrl Pts',(4.19316464781808,-5.31127661078659,16.0156318319016));
#52107=CARTESIAN_POINT('Ctrl Pts',(4.3338020996922,-5.20024567894619,16.0240554185847));
#52108=CARTESIAN_POINT('Ctrl Pts',(4.47005821470849,-5.08360067739934,16.0324790052679));
#52109=CARTESIAN_POINT('Ctrl Pts',(4.60148171579809,-4.9617189581007,16.0409025919511));
#52110=CARTESIAN_POINT('Ctrl Pts',(4.7328905112872,-4.83985087672721,16.0493252360791));
#52111=CARTESIAN_POINT('Ctrl Pts',(4.85946752644858,-4.71274747241858,16.0577478802072));
#52112=CARTESIAN_POINT('Ctrl Pts',(4.98079659468887,-4.58082462907452,16.0661705243352));
#52113=CARTESIAN_POINT('Ctrl Pts',(5.10212900569004,-4.44889815109842,16.0745934005171));
#52114=CARTESIAN_POINT('Ctrl Pts',(5.21821295609764,-4.31215221501692,16.083016276699));
#52115=CARTESIAN_POINT('Ctrl Pts',(5.32867075393888,-4.17103787996663,16.091439152881));
#52116=CARTESIAN_POINT('Ctrl Pts',(5.43914699884538,-4.0298999780392,16.0998634357299));
#52117=CARTESIAN_POINT('Ctrl Pts',(5.54399501290666,-3.88439248551719,16.1082877185789));
#52118=CARTESIAN_POINT('Ctrl Pts',(5.64287861602505,-3.73499798190135,16.1167120014279));
#52119=CARTESIAN_POINT('Ctrl Pts',(5.7418290014728,-3.5855025827616,16.1251419737261));
#52120=CARTESIAN_POINT('Ctrl Pts',(5.8348067426431,-3.43211520519866,16.1335719460242));
#52121=CARTESIAN_POINT('Ctrl Pts',(5.9215195404571,-3.27534659722978,16.1420019183224));
#52122=CARTESIAN_POINT('Ctrl Pts',(6.00826333669684,-3.11852194701369,16.1504349041996));
#52123=CARTESIAN_POINT('Ctrl Pts',(6.08873756791653,-2.95831395092299,16.1588678900768));
#52124=CARTESIAN_POINT('Ctrl Pts',(6.16269657023468,-2.79525669361826,16.1673008759539));
#52125=CARTESIAN_POINT('Ctrl Pts',(6.23672361438426,-2.6320494246305,16.1757416201267));
#52126=CARTESIAN_POINT('Ctrl Pts',(6.30422332174809,-2.46598796345006,16.1841823642996));
#52127=CARTESIAN_POINT('Ctrl Pts',(6.36499830694323,-2.29762606892631,16.1926231084724));
#52128=CARTESIAN_POINT('Ctrl Pts',(6.39860241941228,-2.20453428090018,16.1972902213576));
#52129=CARTESIAN_POINT('Ctrl Pts',(6.43015147300926,-2.11073948092309,16.2019573342429));
#52130=CARTESIAN_POINT('Ctrl Pts',(6.45961868919637,-2.01633712215615,16.2066244471281));
#52131=CARTESIAN_POINT('Ctrl Pts',(6.5110216515342,-1.85166052490023,16.214765814346));
#52132=CARTESIAN_POINT('Ctrl Pts',(6.55618879668403,-1.68480712826192,16.2229071815638));
#52133=CARTESIAN_POINT('Ctrl Pts',(6.59493289321892,-1.51629454062829,16.2310485487817));
#52134=CARTESIAN_POINT('Ctrl Pts',(6.63364316910437,-1.34792905166677,16.2391828092052));
#52135=CARTESIAN_POINT('Ctrl Pts',(6.66594147538702,-1.17790760897593,16.2473170696287));
#52136=CARTESIAN_POINT('Ctrl Pts',(6.69168999992635,-1.00676409594586,16.2554513300522));
#52137=CARTESIAN_POINT('Ctrl Pts',(6.71742095975214,-0.835737330839642,
16.263580041577));
#52138=CARTESIAN_POINT('Ctrl Pts',(6.73661097929366,-0.663590379850863,
16.2717087531018));
#52139=CARTESIAN_POINT('Ctrl Pts',(6.74917307420059,-0.49086842889498,16.2798374646266));
#52140=CARTESIAN_POINT('Ctrl Pts',(6.76172917847663,-0.318228845845166,
16.2879622997191));
#52141=CARTESIAN_POINT('Ctrl Pts',(6.76766362575598,-0.145015173182179,
16.2960871348116));
#52142=CARTESIAN_POINT('Ctrl Pts',(6.76694115281663,0.0282211678854143,
16.3042119699041));
#52143=CARTESIAN_POINT('Ctrl Pts',(6.7662188821356,0.201409010953095,16.3123345304262));
#52144=CARTESIAN_POINT('Ctrl Pts',(6.75884340556819,0.374619144061783,16.3204570909483));
#52145=CARTESIAN_POINT('Ctrl Pts',(6.74483155776262,0.547299056649524,16.3285796514704));
#52146=CARTESIAN_POINT('Ctrl Pts',(6.73081896526366,0.719988146726942,16.3367026436856));
#52147=CARTESIAN_POINT('Ctrl Pts',(6.71016932262387,0.892146594810273,16.3448256359007));
#52148=CARTESIAN_POINT('Ctrl Pts',(6.68295144654538,1.06322573478871,16.3529486281159));
#52149=CARTESIAN_POINT('Ctrl Pts',(6.66905755025985,1.15055642218789,16.3570951680972));
#52150=CARTESIAN_POINT('Ctrl Pts',(6.65345294201825,1.23760596170539,16.3612417080785));
#52151=CARTESIAN_POINT('Ctrl Pts',(6.63615194183469,1.32430223320951,16.3653882480598));
#52152=CARTESIAN_POINT('Ctrl Pts',(6.59866857324288,1.5121334722041,16.3743719070882));
#52153=CARTESIAN_POINT('Ctrl Pts',(6.55323819000232,1.69821294411952,16.3833555661166));
#52154=CARTESIAN_POINT('Ctrl Pts',(6.50005716923112,1.88189951823341,16.3923392251451));
#52155=CARTESIAN_POINT('Ctrl Pts',(6.44678478402949,2.06590166393613,16.4013383180045));
#52156=CARTESIAN_POINT('Ctrl Pts',(6.38573521384414,2.24750246541374,16.410337410864));
#52157=CARTESIAN_POINT('Ctrl Pts',(6.3171540394609,2.42607787214733,16.4193365037235));
#52158=CARTESIAN_POINT('Ctrl Pts',(6.24841206138861,2.60507198830713,16.428356696941));
#52159=CARTESIAN_POINT('Ctrl Pts',(6.17210323165745,2.78102629233047,16.4373768901584));
#52160=CARTESIAN_POINT('Ctrl Pts',(6.08852159448198,2.95333604480198,16.4463970833759));
#52161=CARTESIAN_POINT('Ctrl Pts',(6.00485530996999,3.12582030404431,16.4554264117977));
#52162=CARTESIAN_POINT('Ctrl Pts',(5.91390161319471,3.29465242564326,16.4644557402194));
#52163=CARTESIAN_POINT('Ctrl Pts',(5.81600034517519,3.45925266277589,16.4734850686412));
#52164=CARTESIAN_POINT('Ctrl Pts',(5.71796105610107,3.62408495306551,16.482527126596));
#52165=CARTESIAN_POINT('Ctrl Pts',(5.61295473353225,3.7846732239533,16.4915691845509));
#52166=CARTESIAN_POINT('Ctrl Pts',(5.50136560554989,3.94046513422879,16.5006112425057));
#52167=CARTESIAN_POINT('Ctrl Pts',(5.4045256280128,4.07566544777477,16.5084581780009));
#52168=CARTESIAN_POINT('Ctrl Pts',(5.30272872096714,4.20725390885981,16.516305113496));
#52169=CARTESIAN_POINT('Ctrl Pts',(5.19625087626687,4.33488936778043,16.5241520489911));
#52170=CARTESIAN_POINT('Ctrl Pts',(5.0788151465547,4.4756600914712,16.532806531043));
#52171=CARTESIAN_POINT('Ctrl Pts',(4.95558089663504,4.61174555463093,16.5414610130948));
#52172=CARTESIAN_POINT('Ctrl Pts',(4.82694033039609,4.74267182575346,16.5501154951466));
#52173=CARTESIAN_POINT('Ctrl Pts',(4.69846128022556,4.87343371096583,16.5587591109689));
#52174=CARTESIAN_POINT('Ctrl Pts',(4.56458967290304,4.9990491156275,16.5674027267913));
#52175=CARTESIAN_POINT('Ctrl Pts',(4.42575618602506,5.1190791341667,16.5760463426136));
#52176=CARTESIAN_POINT('Ctrl Pts',(4.28703063180706,5.23901583833723,16.5846832386706));
#52177=CARTESIAN_POINT('Ctrl Pts',(4.14335111950464,5.35337561723113,16.5933201347277));
#52178=CARTESIAN_POINT('Ctrl Pts',(3.99518423232107,5.46175722179347,16.6019570307847));
#52179=CARTESIAN_POINT('Ctrl Pts',(3.84716005678295,5.57003443516951,16.6105856079409));
#52180=CARTESIAN_POINT('Ctrl Pts',(3.69465737613545,5.67234478586437,16.619214185097));
#52181=CARTESIAN_POINT('Ctrl Pts',(3.53817498594311,5.76832790060053,16.6278427622532));
#52182=CARTESIAN_POINT('Ctrl Pts',(3.39500785667449,5.85614370516579,16.6357371241658));
#52183=CARTESIAN_POINT('Ctrl Pts',(3.24850999897858,5.93866359220831,16.6436314860783));
#52184=CARTESIAN_POINT('Ctrl Pts',(3.09908550384718,6.01564277861014,16.6515258479909));
#52185=CARTESIAN_POINT('Origin',(0.,0.,-63.6971797838103));
#52186=CARTESIAN_POINT('',(3.0990855038472,6.01564277861012,19.0457563580462));
#52187=CARTESIAN_POINT('',(3.09908550384716,6.01564277861015,18.6513967904261));
#52188=CARTESIAN_POINT('',(3.09908550384721,6.01564277861012,-63.6971797838103));
#52189=CARTESIAN_POINT('',(-6.767,-4.88839462225982E-8,17.6971797861095));
#52190=CARTESIAN_POINT('Ctrl Pts',(-6.767,-4.88839462226118E-8,17.6971797861095));
#52191=CARTESIAN_POINT('Ctrl Pts',(-6.76699999865631,-0.186007298443953,
17.7059292979222));
#52192=CARTESIAN_POINT('Ctrl Pts',(-6.75932637025508,-0.3720144046447,17.7146788097349));
#52193=CARTESIAN_POINT('Ctrl Pts',(-6.7440051786071,-0.557389586304395,
17.7234283215477));
#52194=CARTESIAN_POINT('Ctrl Pts',(-6.72868405167163,-0.742763984990187,
17.7321777964049));
#52195=CARTESIAN_POINT('Ctrl Pts',(-6.70571544973541,-0.927506178846571,
17.7409272712621));
#52196=CARTESIAN_POINT('Ctrl Pts',(-6.67517738599004,-1.11098868831648,
17.7496767461193));
#52197=CARTESIAN_POINT('Ctrl Pts',(-6.64463944869275,-1.2944704380457,17.7584261847478));
#52198=CARTESIAN_POINT('Ctrl Pts',(-6.60653215935977,-1.47669223111764,
17.7671756233763));
#52199=CARTESIAN_POINT('Ctrl Pts',(-6.56098494888459,-1.65703515367352,
17.7759250620048));
#52200=CARTESIAN_POINT('Ctrl Pts',(-6.51543792322256,-1.83737734446685,
17.7846744651314));
#52201=CARTESIAN_POINT('Ctrl Pts',(-6.46245110700674,-2.0158404021336,17.7934238682581));
#52202=CARTESIAN_POINT('Ctrl Pts',(-6.40220446778367,-2.19181818422304,
17.8021732713847));
#52203=CARTESIAN_POINT('Ctrl Pts',(-6.34195806801502,-2.36779526687668,
17.8109226397362));
#52204=CARTESIAN_POINT('Ctrl Pts',(-6.27445199580558,-2.54128682258334,
17.8196720080878));
#52205=CARTESIAN_POINT('Ctrl Pts',(-6.19991553093826,-2.71170359907395,
17.8284213764393));
#52206=CARTESIAN_POINT('Ctrl Pts',(-6.12537935613118,-2.88211971238402,
17.8371707107425));
#52207=CARTESIAN_POINT('Ctrl Pts',(-6.04381295825467,-3.04946080785825,
17.8459200450456));
#52208=CARTESIAN_POINT('Ctrl Pts',(-5.95549336987747,-3.21315852726651,
17.8546693793488));
#52209=CARTESIAN_POINT('Ctrl Pts',(-5.86717411786317,-3.37685562323618,
17.8634186803304));
#52210=CARTESIAN_POINT('Ctrl Pts',(-5.77210186288949,-3.53690911869855,
17.8721679813119));
#52211=CARTESIAN_POINT('Ctrl Pts',(-5.67059950643654,-3.6927754112052,17.8809172822935));
#52212=CARTESIAN_POINT('Ctrl Pts',(-5.56909752812385,-3.84864112304235,
17.8896665506801));
#52213=CARTESIAN_POINT('Ctrl Pts',(-5.46116565265063,-4.00031942300073,
17.8984158190667));
#52214=CARTESIAN_POINT('Ctrl Pts',(-5.34717045492291,-4.14729515781063,
17.9071650874533));
#52215=CARTESIAN_POINT('Ctrl Pts',(-5.23317567241028,-4.29427035727743,
17.9159143239717));
#52216=CARTESIAN_POINT('Ctrl Pts',(-5.11311778746475,-4.43654279943404,
17.9246635604901));
#52217=CARTESIAN_POINT('Ctrl Pts',(-4.98740455625122,-4.57362928015428,
17.9334127970084));
#52218=CARTESIAN_POINT('Ctrl Pts',(-4.86169177249585,-4.71071527293492,
17.9421620023852));
#52219=CARTESIAN_POINT('Ctrl Pts',(-4.73032387643131,-4.84261513001808,
17.9509112077619));
#52220=CARTESIAN_POINT('Ctrl Pts',(-4.5937470335767,-4.96888087918248,17.9596604131386));
#52221=CARTESIAN_POINT('Ctrl Pts',(-4.45717066550651,-5.09514618940709,
17.9684095881003));
#52222=CARTESIAN_POINT('Ctrl Pts',(-4.31538559729377,-5.21577723638106,
17.977158763062));
#52223=CARTESIAN_POINT('Ctrl Pts',(-4.16887337101294,-5.3303643230514,17.9859079380237));
#52224=CARTESIAN_POINT('Ctrl Pts',(-4.02236164188988,-5.44495102089508,
17.9946570832969));
#52225=CARTESIAN_POINT('Ctrl Pts',(-3.87112301251265,-5.55349362294478,
18.0034062285702));
#52226=CARTESIAN_POINT('Ctrl Pts',(-3.71567112843293,-5.65562349041465,
18.0121553738434));
#52227=CARTESIAN_POINT('Ctrl Pts',(-3.56021975893851,-5.75775301980866,
18.0209044901548));
#52228=CARTESIAN_POINT('Ctrl Pts',(-3.40055540213499,-5.85346969976462,
18.0296536064661));
#52229=CARTESIAN_POINT('Ctrl Pts',(-3.23722031594003,-5.94244845379959,
18.0384027227775));
#52230=CARTESIAN_POINT('Ctrl Pts',(-3.07388575686353,-6.03142692068044,
18.0471518108535));
#52231=CARTESIAN_POINT('Ctrl Pts',(-2.90688074372655,-6.11366736807859,
18.0559008989296));
#52232=CARTESIAN_POINT('Ctrl Pts',(-2.73677246139464,-6.18889048978506,
18.0646499870056));
#52233=CARTESIAN_POINT('Ctrl Pts',(-2.56666471391664,-6.26411337497523,
18.0733990475727));
#52234=CARTESIAN_POINT('Ctrl Pts',(-2.39345397882551,-6.33231886274315,
18.0821481081399));
#52235=CARTESIAN_POINT('Ctrl Pts',(-2.21772851325488,-6.39327531406996,
18.0908971687071));
#52236=CARTESIAN_POINT('Ctrl Pts',(-2.04200358560971,-6.45423157879873,
18.0996462024919));
#52237=CARTESIAN_POINT('Ctrl Pts',(-1.86376421359607,-6.50793875758863,
18.1083952362767));
#52238=CARTESIAN_POINT('Ctrl Pts',(-1.68361572886822,-6.55421445159582,
18.1171442700615));
#52239=CARTESIAN_POINT('Ctrl Pts',(-1.50346778064905,-6.6004900077872,18.1258932777904));
#52240=CARTESIAN_POINT('Ctrl Pts',(-1.32141100861001,-6.63933405219776,
18.1346422855193));
#52241=CARTESIAN_POINT('Ctrl Pts',(-1.13806370527537,-6.67061466453691,
18.1433912932482));
#52242=CARTESIAN_POINT('Ctrl Pts',(-0.954716932754182,-6.70189518631477,
18.1521402756477));
#52243=CARTESIAN_POINT('Ctrl Pts',(-0.770079918855252,-6.72561227165323,
18.1608892580471));
#52244=CARTESIAN_POINT('Ctrl Pts',(-0.584779715370058,-6.74168537418439,
18.1696382404465));
#52245=CARTESIAN_POINT('Ctrl Pts',(-0.391489539276155,-6.7584515339629,
18.1787644708382));
#52246=CARTESIAN_POINT('Ctrl Pts',(-0.197478043938523,-6.76689985284623,
18.1878907012298));
#52247=CARTESIAN_POINT('Ctrl Pts',(-0.00346210017286045,-6.76699911436838,
18.1970169316215));
#52248=CARTESIAN_POINT('Ctrl Pts',(0.184490845350193,-6.76709527396796,
18.2058579673134));
#52249=CARTESIAN_POINT('Ctrl Pts',(0.372447648472862,-6.75935633534174,
18.2146990030053));
#52250=CARTESIAN_POINT('Ctrl Pts',(0.559756493915292,-6.74380913635014,
18.2235400386973));
#52251=CARTESIAN_POINT('Ctrl Pts',(0.745136176659968,-6.72842206367975,
18.2322900173106));
#52252=CARTESIAN_POINT('Ctrl Pts',(0.929880897405338,-6.70538685725295,
18.2410399959238));
#52253=CARTESIAN_POINT('Ctrl Pts',(1.11336309582729,-6.67478176548491,18.2497899745372));
#52254=CARTESIAN_POINT('Ctrl Pts',(1.29684341594623,-6.6441769870205,18.2585398635771));
#52255=CARTESIAN_POINT('Ctrl Pts',(1.47906095683791,-6.60600252545316,18.2672897526171));
#52256=CARTESIAN_POINT('Ctrl Pts',(1.6593967554288,-6.56038805316213,18.2760396416571));
#52257=CARTESIAN_POINT('Ctrl Pts',(1.83973076785883,-6.51477403266595,18.2847894440326));
#52258=CARTESIAN_POINT('Ctrl Pts',(2.01818279737779,-6.46172021920427,18.293539246408));
#52259=CARTESIAN_POINT('Ctrl Pts',(2.19414668373167,-6.40140682430584,18.3022890487835));
#52260=CARTESIAN_POINT('Ctrl Pts',(2.3701088857019,-6.34109400674686,18.3110387674031));
#52261=CARTESIAN_POINT('Ctrl Pts',(2.54358272100906,-6.27352183975383,18.3197884860226));
#52262=CARTESIAN_POINT('Ctrl Pts',(2.71397895044246,-6.19891984595343,18.3285382046421));
#52263=CARTESIAN_POINT('Ctrl Pts',(2.88437360540857,-6.12431854147813,18.3372878424139));
#52264=CARTESIAN_POINT('Ctrl Pts',(3.05169044883733,-6.04268765513703,18.3460374801857));
#52265=CARTESIAN_POINT('Ctrl Pts',(3.21536116548682,-5.95430445774141,18.3547871179576));
#52266=CARTESIAN_POINT('Ctrl Pts',(3.37903042419546,-5.86592204764285,18.3635366777896));
#52267=CARTESIAN_POINT('Ctrl Pts',(3.53905336892174,-5.7707875830414,18.3722862376217));
#52268=CARTESIAN_POINT('Ctrl Pts',(3.69488646885232,-5.66922419580422,18.3810357974537));
#52269=CARTESIAN_POINT('Ctrl Pts',(3.85071823243222,-5.56766167952644,18.3897852822537));
#52270=CARTESIAN_POINT('Ctrl Pts',(4.00235998300487,-5.4596705074294,18.3985347670537));
#52271=CARTESIAN_POINT('Ctrl Pts',(4.14929666598237,-5.34561747393766,18.4072842518537));
#52272=CARTESIAN_POINT('Ctrl Pts',(4.29623213771649,-5.23156538061946,18.4160336645291));
#52273=CARTESIAN_POINT('Ctrl Pts',(4.43846239307282,-5.11145170163255,18.4247830772044));
#52274=CARTESIAN_POINT('Ctrl Pts',(4.57550435177322,-4.98568439904737,18.4335324898798));
#52275=CARTESIAN_POINT('Ctrl Pts',(4.71254522632129,-4.85991809141961,18.4422818333377));
#52276=CARTESIAN_POINT('Ctrl Pts',(4.84439767520529,-4.72849844346986,18.4510311767956));
#52277=CARTESIAN_POINT('Ctrl Pts',(4.9706138730961,-4.59187181055662,18.4597805202535));
#52278=CARTESIAN_POINT('Ctrl Pts',(5.09682911440502,-4.4552462131251,18.4685297974008));
#52279=CARTESIAN_POINT('Ctrl Pts',(5.21740799574309,-4.31341392019921,18.4772790745482));
#52280=CARTESIAN_POINT('Ctrl Pts',(5.33194098767029,-4.16685664548249,18.4860283516956));
#52281=CARTESIAN_POINT('Ctrl Pts',(5.44647314960563,-4.02030043282958,18.4947775654391));
#52282=CARTESIAN_POINT('Ctrl Pts',(5.55495933335167,-3.8690195326974,18.5035267791826));
#52283=CARTESIAN_POINT('Ctrl Pts',(5.65703108597267,-3.71352774223364,18.5122759929262));
#52284=CARTESIAN_POINT('Ctrl Pts',(5.75910213280788,-3.55803702693411,18.5210251461724));
#52285=CARTESIAN_POINT('Ctrl Pts',(5.85475868002329,-3.39833571911875,18.5297742994185));
#52286=CARTESIAN_POINT('Ctrl Pts',(5.94367585262084,-3.23496620677433,18.5385234526647));
#52287=CARTESIAN_POINT('Ctrl Pts',(6.03259243992342,-3.07159776980548,18.5472725483198));
#52288=CARTESIAN_POINT('Ctrl Pts',(6.1147696043999,-2.90456142830587,18.5560216439749));
#52289=CARTESIAN_POINT('Ctrl Pts',(6.18992825428066,-2.73442447452074,18.5647707396301));
#52290=CARTESIAN_POINT('Ctrl Pts',(6.26508643439276,-2.56428858415288,18.5735197806002));
#52291=CARTESIAN_POINT('Ctrl Pts',(6.33322607191198,-2.39105238237964,18.5822688215703));
#52292=CARTESIAN_POINT('Ctrl Pts',(6.39411575249527,-2.21530421019144,18.5910178625404));
#52293=CARTESIAN_POINT('Ctrl Pts',(6.45500507271743,-2.03955707812706,18.5997668517314));
#52294=CARTESIAN_POINT('Ctrl Pts',(6.50864442806703,-1.86129827613362,18.6085158409224));
#52295=CARTESIAN_POINT('Ctrl Pts',(6.55485165189545,-1.68113319568781,18.6172648301134));
#52296=CARTESIAN_POINT('Ctrl Pts',(6.6019985363039,-1.49730431529977,18.6261917369453));
#52297=CARTESIAN_POINT('Ctrl Pts',(6.64140768290384,-1.3114910885858,18.6351186437773));
#52298=CARTESIAN_POINT('Ctrl Pts',(6.67293975984165,-1.12435046205555,18.6440455506092));
#52299=CARTESIAN_POINT('Ctrl Pts',(6.70384665429488,-0.940920248958837,
18.6527954647932));
#52300=CARTESIAN_POINT('Ctrl Pts',(6.72718586370259,-0.75621507152498,18.6615453789772));
#52301=CARTESIAN_POINT('Ctrl Pts',(6.74287810814659,-0.57086234652273,18.6702952931611));
#52302=CARTESIAN_POINT('Ctrl Pts',(6.75857004399123,-0.385513266616217,
18.6790450352717));
#52303=CARTESIAN_POINT('Ctrl Pts',(6.76661529162351,-0.199516950256453,
18.6877947773823));
#52304=CARTESIAN_POINT('Ctrl Pts',(6.76698652357479,-0.0135051752001907,
18.6965445194929));
#52305=CARTESIAN_POINT('Ctrl Pts',(6.76735774871896,0.172503189044874,18.7052941011635));
#52306=CARTESIAN_POINT('Ctrl Pts',(6.76005523919639,0.358526724792804,18.7140436828341));
#52307=CARTESIAN_POINT('Ctrl Pts',(6.7451037986922,0.543933584978941,18.7227932645048));
#52308=CARTESIAN_POINT('Ctrl Pts',(6.73015261247498,0.729337291853583,18.7315426973667));
#52309=CARTESIAN_POINT('Ctrl Pts',(6.70755277863699,0.914124058479703,18.7402921302286));
#52310=CARTESIAN_POINT('Ctrl Pts',(6.67738105710749,1.09766625992696,18.7490415630905));
#52311=CARTESIAN_POINT('Ctrl Pts',(6.64720980863084,1.28120558367433,18.7577908587729));
#52312=CARTESIAN_POINT('Ctrl Pts',(6.60946695651515,1.4635000985072,18.7665401544552));
#52313=CARTESIAN_POINT('Ctrl Pts',(6.56428068966336,1.64393066377894,18.7752894501375));
#52314=CARTESIAN_POINT('Ctrl Pts',(6.51909507123432,1.82435863987282,18.7840386202675));
#52315=CARTESIAN_POINT('Ctrl Pts',(6.46646632142887,2.00292244195733,18.7927877903975));
#52316=CARTESIAN_POINT('Ctrl Pts',(6.40657318212524,2.17901561767548,18.8015369605275));
#52317=CARTESIAN_POINT('Ctrl Pts',(6.34668082271735,2.35510650040452,18.8102860167305));
#52318=CARTESIAN_POINT('Ctrl Pts',(6.27952435537005,2.52872654986856,18.8190350729336));
#52319=CARTESIAN_POINT('Ctrl Pts',(6.20533185619881,2.69928611941088,18.8277841291367));
#52320=CARTESIAN_POINT('Ctrl Pts',(6.12831448027958,2.8763397384532,18.8368663053412));
#52321=CARTESIAN_POINT('Ctrl Pts',(6.04371487681997,3.0500949408034,18.8459484815458));
#52322=CARTESIAN_POINT('Ctrl Pts',(5.95184263330165,3.21991587908953,18.8550306577504));
#52323=CARTESIAN_POINT('Ctrl Pts',(5.86333279454217,3.38352159165377,18.8637804381048));
#52324=CARTESIAN_POINT('Ctrl Pts',(5.76807335265492,3.54347564110903,18.8725302184592));
#52325=CARTESIAN_POINT('Ctrl Pts',(5.66638788029581,3.69923470329158,18.8812799988136));
#52326=CARTESIAN_POINT('Ctrl Pts',(5.56470606359391,3.85498816583708,18.8900294646078));
#52327=CARTESIAN_POINT('Ctrl Pts',(5.45659883539358,4.00654670290066,18.898778930402));
#52328=CARTESIAN_POINT('Ctrl Pts',(5.34243338271291,4.15339554476511,18.9075283961963));
#52329=CARTESIAN_POINT('Ctrl Pts',(5.22827142749751,4.30023988790677,18.9162775939502));
#52330=CARTESIAN_POINT('Ctrl Pts',(5.10805179508241,4.44237459832989,18.925026791704));
#52331=CARTESIAN_POINT('Ctrl Pts',(4.98218278736586,4.57931694396395,18.9337759894579));
#52332=CARTESIAN_POINT('Ctrl Pts',(4.85631696674133,4.71625582212127,18.9425249656759));
#52333=CARTESIAN_POINT('Ctrl Pts',(4.72480225096497,4.84800238762615,18.9512739418939));
#52334=CARTESIAN_POINT('Ctrl Pts',(4.58808528082664,4.97410921229741,18.9600229181119));
#52335=CARTESIAN_POINT('Ctrl Pts',(4.45135942221465,5.10022423563771,18.968772463133));
#52336=CARTESIAN_POINT('Ctrl Pts',(4.30943084305619,5.2206985900779,18.9775220081542));
#52337=CARTESIAN_POINT('Ctrl Pts',(4.16278161356498,5.3351230761591,18.9862715531754));
#52338=CARTESIAN_POINT('Ctrl Pts',(4.01614100504849,5.44954083564103,18.9950205838426));
#52339=CARTESIAN_POINT('Ctrl Pts',(3.86478052743664,5.55790926216842,19.0037696145098));
#52340=CARTESIAN_POINT('Ctrl Pts',(3.70921422665565,5.65986031813289,19.0125186451771));
#52341=CARTESIAN_POINT('Ctrl Pts',(3.55364581327177,5.76181275860091,19.0212677946569));
#52342=CARTESIAN_POINT('Ctrl Pts',(3.39387170208419,5.85734749704611,19.0300169441366));
#52343=CARTESIAN_POINT('Ctrl Pts',(3.23043452787251,5.94614007244441,19.0387660936164));
#52344=CARTESIAN_POINT('Ctrl Pts',(3.18690766589811,5.96978745984176,19.0410961817597));
#52345=CARTESIAN_POINT('Ctrl Pts',(3.14312113868286,5.99295689073508,19.0434262699029));
#52346=CARTESIAN_POINT('Ctrl Pts',(3.0990855038472,6.01564277861012,19.0457563580462));
#52347=CARTESIAN_POINT('Ctrl Pts',(3.09908550384729,6.01564277861008,17.0455658338557));
#52348=CARTESIAN_POINT('Ctrl Pts',(2.94372784046354,6.09567856202065,17.0537748772338));
#52349=CARTESIAN_POINT('Ctrl Pts',(2.7853529842944,6.16964826932369,17.0619839206119));
#52350=CARTESIAN_POINT('Ctrl Pts',(2.62448024722065,6.23733856961033,17.0701929639901));
#52351=CARTESIAN_POINT('Ctrl Pts',(2.46352124048431,6.30506516951786,17.0784064095523));
#52352=CARTESIAN_POINT('Ctrl Pts',(2.30006201767863,6.36650552350461,17.0866198551145));
#52353=CARTESIAN_POINT('Ctrl Pts',(2.13463849340305,6.42149573716918,17.0948333006768));
#52354=CARTESIAN_POINT('Ctrl Pts',(1.96900103712844,6.47655706627146,17.1030573681794));
#52355=CARTESIAN_POINT('Ctrl Pts',(1.80139454849196,6.52515149144324,17.1112814356821));
#52356=CARTESIAN_POINT('Ctrl Pts',(1.63236758722803,6.56716567936026,17.1195055031848));
#52357=CARTESIAN_POINT('Ctrl Pts',(1.53461716767009,6.59146301314397,17.1242615849534));
#52358=CARTESIAN_POINT('Ctrl Pts',(1.43639184567715,6.61356057311733,17.1290176667219));
#52359=CARTESIAN_POINT('Ctrl Pts',(1.33779861920245,6.63344434320965,17.1337737484904));
#52360=CARTESIAN_POINT('Ctrl Pts',(1.15257285209219,6.67079971436528,17.1427089352727));
#52361=CARTESIAN_POINT('Ctrl Pts',(0.965663972667169,6.70041647862909,17.151644122055));
#52362=CARTESIAN_POINT('Ctrl Pts',(0.777711705246082,6.72216137142833,17.1605793088373));
#52363=CARTESIAN_POINT('Ctrl Pts',(0.590040932177247,6.7438736971051,17.1695011134739));
#52364=CARTESIAN_POINT('Ctrl Pts',(0.401330145213883,6.75773764608581,17.1784229181105));
#52365=CARTESIAN_POINT('Ctrl Pts',(0.212227603136763,6.76367122533812,17.1873447227472));
#52366=CARTESIAN_POINT('Ctrl Pts',(0.0235863270061176,6.76959033118346,
17.1962447649865));
#52367=CARTESIAN_POINT('Ctrl Pts',(-0.165444539324304,6.76761766664595,
17.2051448072258));
#52368=CARTESIAN_POINT('Ctrl Pts',(-0.354213909340622,6.75772310075144,
17.214044849465));
#52369=CARTESIAN_POINT('Ctrl Pts',(-0.542692666135895,6.74784376768662,
17.2229311899584));
#52370=CARTESIAN_POINT('Ctrl Pts',(-0.730910472961369,6.730066874345,17.2318175304518));
#52371=CARTESIAN_POINT('Ctrl Pts',(-0.918215547135476,6.70441415852263,
17.2407038709452));
#52372=CARTESIAN_POINT('Ctrl Pts',(-1.10504171493065,6.67882703221672,17.2495674906171));
#52373=CARTESIAN_POINT('Ctrl Pts',(-1.29095955165088,6.64540430071771,17.258431110289));
#52374=CARTESIAN_POINT('Ctrl Pts',(-1.4753224553871,6.60421930682428,17.267294729961));
#52375=CARTESIAN_POINT('Ctrl Pts',(-1.6503389710822,6.5651222109114,17.2757090031146));
#52376=CARTESIAN_POINT('Ctrl Pts',(-1.82395402431221,6.51903030575848,17.2841232762682));
#52377=CARTESIAN_POINT('Ctrl Pts',(-1.99561783376145,6.46604967979471,17.2925375494218));
#52378=CARTESIAN_POINT('Ctrl Pts',(-2.16311922783132,6.41435370068241,17.3007477976263));
#52379=CARTESIAN_POINT('Ctrl Pts',(-2.3286015770788,6.35614772948267,17.3089580458309));
#52380=CARTESIAN_POINT('Ctrl Pts',(-2.49153434258356,6.29162503807456,17.3171682940354));
#52381=CARTESIAN_POINT('Ctrl Pts',(-2.65450584045484,6.22708700833641,17.3253804939796));
#52382=CARTESIAN_POINT('Ctrl Pts',(-2.81492621613493,6.15622939780991,17.3335926939238));
#52383=CARTESIAN_POINT('Ctrl Pts',(-2.97228525510381,6.07929349203446,17.341804893868));
#52384=CARTESIAN_POINT('Ctrl Pts',(-3.12970972268787,6.00232559693188,17.3500205083785));
#52385=CARTESIAN_POINT('Ctrl Pts',(-3.28406999819524,5.91927452784803,17.358236122889));
#52386=CARTESIAN_POINT('Ctrl Pts',(-3.43488071919935,5.83042738097925,17.3664517373995));
#52387=CARTESIAN_POINT('Ctrl Pts',(-3.58586079403171,5.74148046265954,17.3746765776849));
#52388=CARTESIAN_POINT('Ctrl Pts',(-3.733283046241,5.6467246472369,17.3829014179704));
#52389=CARTESIAN_POINT('Ctrl Pts',(-3.87669053610912,5.54649073624413,17.3911262582558));
#52390=CARTESIAN_POINT('Ctrl Pts',(-4.02018988345974,5.44619262194697,17.3993563668373));
#52391=CARTESIAN_POINT('Ctrl Pts',(-4.15966905924843,5.34040963177509,17.4075864754188));
#52392=CARTESIAN_POINT('Ctrl Pts',(-4.29470450102172,5.2295126205894,17.4158165840004));
#52393=CARTESIAN_POINT('Ctrl Pts',(-4.42992507845766,5.11846356789977,17.4240579761871));
#52394=CARTESIAN_POINT('Ctrl Pts',(-4.5606894875852,5.00228672537704,17.4322993683738));
#52395=CARTESIAN_POINT('Ctrl Pts',(-4.68661056628652,4.88139021181175,17.4405407605605));
#52396=CARTESIAN_POINT('Ctrl Pts',(-4.74141461894764,4.8287729775543,17.4441276238248));
#52397=CARTESIAN_POINT('Ctrl Pts',(-4.79530175147435,4.77526217089232,17.4477144870891));
#52398=CARTESIAN_POINT('Ctrl Pts',(-4.84824246668574,4.72089334599131,17.4513013503535));
#52399=CARTESIAN_POINT('Ctrl Pts',(-4.97142674868588,4.59438608911196,17.4596473875025));
#52400=CARTESIAN_POINT('Ctrl Pts',(-5.08978376569604,4.46292358682828,17.4679934246516));
#52401=CARTESIAN_POINT('Ctrl Pts',(-5.20290147465994,4.32690481117639,17.4763394618006));
#52402=CARTESIAN_POINT('Ctrl Pts',(-5.31590899936957,4.19101852695755,17.4846773693483));
#52403=CARTESIAN_POINT('Ctrl Pts',(-5.42368716556202,4.05058507736566,17.493015276896));
#52404=CARTESIAN_POINT('Ctrl Pts',(-5.52586131619716,3.90603964574808,17.5013531844437));
#52405=CARTESIAN_POINT('Ctrl Pts',(-5.62793962359984,3.7616298032332,17.5096832707176));
#52406=CARTESIAN_POINT('Ctrl Pts',(-5.72442419844025,3.6131159509024,17.5180133569914));
#52407=CARTESIAN_POINT('Ctrl Pts',(-5.81498115372413,3.46096564297208,17.5263434432652));
#52408=CARTESIAN_POINT('Ctrl Pts',(-5.90548912695851,3.30889763279453,17.5346690238145));
#52409=CARTESIAN_POINT('Ctrl Pts',(-5.99007569229831,3.15319738202128,17.5429946043638));
#52410=CARTESIAN_POINT('Ctrl Pts',(-6.06845038561592,2.99436118685071,17.5513201849131));
#52411=CARTESIAN_POINT('Ctrl Pts',(-6.14679541776859,2.8355851037697,17.5596426146185));
#52412=CARTESIAN_POINT('Ctrl Pts',(-6.21893310991805,2.6736757507284,17.567965044324));
#52413=CARTESIAN_POINT('Ctrl Pts',(-6.28461895029311,2.50915397088675,17.5762874740295));
#52414=CARTESIAN_POINT('Ctrl Pts',(-6.35029059907227,2.34466773640165,17.5846081056524));
#52415=CARTESIAN_POINT('Ctrl Pts',(-6.40951304675221,2.17757052097107,17.5929287372754));
#52416=CARTESIAN_POINT('Ctrl Pts',(-6.46208984800146,2.00840329524636,17.6012493688984));
#52417=CARTESIAN_POINT('Ctrl Pts',(-6.51467647471934,1.83920445582076,17.6095715554677));
#52418=CARTESIAN_POINT('Ctrl Pts',(-6.56061486540809,1.66793516159074,17.617893742037));
#52419=CARTESIAN_POINT('Ctrl Pts',(-6.59975822020709,1.49515231157531,17.6262159286064));
#52420=CARTESIAN_POINT('Ctrl Pts',(-6.63890425509947,1.32235763134818,17.6345386849847));
#52421=CARTESIAN_POINT('Ctrl Pts',(-6.6712542550039,1.14804952700332,17.642861441363));
#52422=CARTESIAN_POINT('Ctrl Pts',(-6.69671245309473,0.97279562116923,17.6511841977414));
#52423=CARTESIAN_POINT('Ctrl Pts',(-6.72218643939624,0.797433029497346,
17.6595121155782));
#52424=CARTESIAN_POINT('Ctrl Pts',(-6.74076003656308,0.621123807099775,
17.667840033415));
#52425=CARTESIAN_POINT('Ctrl Pts',(-6.75238922133331,0.444442126290663,
17.6761679512518));
#52426=CARTESIAN_POINT('Ctrl Pts',(-6.76213058743735,0.296441989510258,
17.6831439601583));
#52427=CARTESIAN_POINT('Ctrl Pts',(-6.76700008639309,0.148180702939684,
17.6901199690648));
#52428=CARTESIAN_POINT('Ctrl Pts',(-6.76699999999885,-3.9452790698771E-6,
17.6970959779713));
#52429=CARTESIAN_POINT('',(-6.767,3.26333198744783E-12,17.3028202161898));
#52430=CARTESIAN_POINT('Ctrl Pts',(3.09908550384718,6.01564277861014,16.6515258479909));
#52431=CARTESIAN_POINT('Ctrl Pts',(2.93597037955409,6.09967498194382,16.6601435101984));
#52432=CARTESIAN_POINT('Ctrl Pts',(2.76936763087946,6.17710392388078,16.668761172406));
#52433=CARTESIAN_POINT('Ctrl Pts',(2.59982817764029,6.24765415550089,16.6773788346136));
#52434=CARTESIAN_POINT('Ctrl Pts',(2.56351738067913,6.26276412009602,16.6792245063833));
#52435=CARTESIAN_POINT('Ctrl Pts',(2.52707196505644,6.27755872568492,16.6810701781531));
#52436=CARTESIAN_POINT('Ctrl Pts',(2.49049748311316,6.292035543972,16.6829158499228));
#52437=CARTESIAN_POINT('Ctrl Pts',(2.32352906339011,6.3581245585959,16.6913416397726));
#52438=CARTESIAN_POINT('Ctrl Pts',(2.15394204162623,6.41755800409971,16.6997674296224));
#52439=CARTESIAN_POINT('Ctrl Pts',(1.98229553397733,6.47014632106366,16.7081932194722));
#52440=CARTESIAN_POINT('Ctrl Pts',(1.81060919856209,6.52274684028694,16.7166209643889));
#52441=CARTESIAN_POINT('Ctrl Pts',(1.63686274142149,6.56849896702093,16.7250487093055));
#52442=CARTESIAN_POINT('Ctrl Pts',(1.46162962989451,6.60726326288082,16.7334764542221));
#52443=CARTESIAN_POINT('Ctrl Pts',(1.28633212899157,6.64604180267438,16.7419072959121));
#52444=CARTESIAN_POINT('Ctrl Pts',(1.10954720801154,6.67782732030957,16.7503381376021));
#52445=CARTESIAN_POINT('Ctrl Pts',(0.931858079315654,6.7025315754582,16.7587689792921));
#52446=CARTESIAN_POINT('Ctrl Pts',(0.754005676991051,6.72725853066401,16.7672075678495));
#52447=CARTESIAN_POINT('Ctrl Pts',(0.575247735563395,6.74489117777599,16.7756461564068));
#52448=CARTESIAN_POINT('Ctrl Pts',(0.396173261575324,6.75539308603228,16.7840847449642));
#52449=CARTESIAN_POINT('Ctrl Pts',(0.217004888846535,6.76590050102518,16.7925277583445));
#52450=CARTESIAN_POINT('Ctrl Pts',(0.0375199835359462,6.76926970846292,
16.8009707717248));
#52451=CARTESIAN_POINT('Ctrl Pts',(-0.141692314662265,6.76551640955557,
16.8094137851052));
#52452=CARTESIAN_POINT('Ctrl Pts',(-0.321092887870196,6.76175916754612,
16.8178656684595));
#52453=CARTESIAN_POINT('Ctrl Pts',(-0.500219950993989,6.7508644867019,16.8263175518138));
#52454=CARTESIAN_POINT('Ctrl Pts',(-0.678488274244354,6.73290001869276,
16.8347694351681));
#52455=CARTESIAN_POINT('Ctrl Pts',(-0.727072024240753,6.72800413362097,
16.8370728403968));
#52456=CARTESIAN_POINT('Ctrl Pts',(-0.775592041482276,6.72258344578304,
16.8393762456255));
#52457=CARTESIAN_POINT('Ctrl Pts',(-0.824036603510481,6.71663998410477,
16.8416796508542));
#52458=CARTESIAN_POINT('Ctrl Pts',(-0.998962956602453,6.69517899792604,
16.8499969161876));
#52459=CARTESIAN_POINT('Ctrl Pts',(-1.17321938694986,6.66685938408274,16.858314181521));
#52460=CARTESIAN_POINT('Ctrl Pts',(-1.34623726940326,6.63173689273554,16.8666314468543));
#52461=CARTESIAN_POINT('Ctrl Pts',(-1.51910922458655,6.59664402450712,16.8749416972144));
#52462=CARTESIAN_POINT('Ctrl Pts',(-1.69074437399089,6.55475977931087,16.8832519475745));
#52463=CARTESIAN_POINT('Ctrl Pts',(-1.86058084131076,6.50619150755243,16.8915621979346));
#52464=CARTESIAN_POINT('Ctrl Pts',(-2.03030516822879,6.4576553046753,16.8998669611645));
#52465=CARTESIAN_POINT('Ctrl Pts',(-2.19823284627887,6.40244396471579,16.9081717243943));
#52466=CARTESIAN_POINT('Ctrl Pts',(-2.36381357409787,6.3407156052697,16.9164764876242));
#52467=CARTESIAN_POINT('Ctrl Pts',(-2.52931528212255,6.27901670433808,16.9247772875867));
#52468=CARTESIAN_POINT('Ctrl Pts',(-2.69247194678431,6.210807103314,16.9330780875493));
#52469=CARTESIAN_POINT('Ctrl Pts',(-2.85274956603841,6.13629439592558,16.9413788875119));
#52470=CARTESIAN_POINT('Ctrl Pts',(-3.01298002616589,6.06180361270985,16.9496772450968));
#52471=CARTESIAN_POINT('Ctrl Pts',(-3.17033281439747,5.98101356633595,16.9579756026817));
#52472=CARTESIAN_POINT('Ctrl Pts',(-3.32429480720481,5.89417958962833,16.9662739602666));
#52473=CARTESIAN_POINT('Ctrl Pts',(-3.47827246529225,5.80733677776248,16.9745731621904));
#52474=CARTESIAN_POINT('Ctrl Pts',(-3.62885833195818,5.71444897113201,16.9828723641142));
#52475=CARTESIAN_POINT('Ctrl Pts',(-3.77556424520675,5.61581727180616,16.9911715660379));
#52476=CARTESIAN_POINT('Ctrl Pts',(-3.92228503165374,5.51717557309581,16.9994716093435));
#52477=CARTESIAN_POINT('Ctrl Pts',(-4.0651247915311,5.41278901472721,17.007771652649));
#52478=CARTESIAN_POINT('Ctrl Pts',(-4.20362478320096,5.30300176146102,17.0160716959545));
#52479=CARTESIAN_POINT('Ctrl Pts',(-4.34216180744667,5.19318515292387,17.0243739585525));
#52480=CARTESIAN_POINT('Ctrl Pts',(-4.47635647806641,5.07796518748133,17.0326762211504));
#52481=CARTESIAN_POINT('Ctrl Pts',(-4.60578340481018,4.95772611465934,17.0409784837484));
#52482=CARTESIAN_POINT('Ctrl Pts',(-4.7352664258707,4.83743492958523,17.049284344591));
#52483=CARTESIAN_POINT('Ctrl Pts',(-4.85997733003502,4.71212053835371,17.0575902054336));
#52484=CARTESIAN_POINT('Ctrl Pts',(-4.97952770222746,4.58220393072474,17.0658960662762));
#52485=CARTESIAN_POINT('Ctrl Pts',(-5.09921939139417,4.45213375249988,17.0742117452323));
#52486=CARTESIAN_POINT('Ctrl Pts',(-5.2137381249279,4.317450744912,17.0825274241885));
#52487=CARTESIAN_POINT('Ctrl Pts',(-5.32273514893061,4.17860976095384,17.0908431031446));
#52488=CARTESIAN_POINT('Ctrl Pts',(-5.43180111268308,4.03968096117887,17.0991640417014));
#52489=CARTESIAN_POINT('Ctrl Pts',(-5.53533819844516,3.89658922181437,17.1074849802583));
#52490=CARTESIAN_POINT('Ctrl Pts',(-5.63304104004112,3.74981834776199,17.1158059188151));
#52491=CARTESIAN_POINT('Ctrl Pts',(-5.73088909832283,3.60282932672896,17.124139224864));
#52492=CARTESIAN_POINT('Ctrl Pts',(-5.82288540163198,3.45215053952877,17.1324725309129));
#52493=CARTESIAN_POINT('Ctrl Pts',(-5.90876992487993,3.29829152362772,17.1408058369619));
#52494=CARTESIAN_POINT('Ctrl Pts',(-5.97198600462747,3.18504220406173,17.1469396422137));
#52495=CARTESIAN_POINT('Ctrl Pts',(-6.03189179053176,3.07007040327827,17.1530734474655));
#52496=CARTESIAN_POINT('Ctrl Pts',(-6.08840037876368,2.95358592694884,17.1592072527174));
#52497=CARTESIAN_POINT('Ctrl Pts',(-6.16789901937184,2.7897107035556,17.1678365459723));
#52498=CARTESIAN_POINT('Ctrl Pts',(-6.2408922449539,2.62238745399539,17.1764658392272));
#52499=CARTESIAN_POINT('Ctrl Pts',(-6.30708074887625,2.45214628991718,17.1850951324822));
#52500=CARTESIAN_POINT('Ctrl Pts',(-6.37313275158236,2.28225621590106,17.193706629459));
#52501=CARTESIAN_POINT('Ctrl Pts',(-6.4324078944947,2.10946050270718,17.2023181264358));
#52502=CARTESIAN_POINT('Ctrl Pts',(-6.48465262896137,1.93431364615575,17.2109296234126));
#52503=CARTESIAN_POINT('Ctrl Pts',(-6.53674933660995,1.75966303926738,17.2195167211363));
#52504=CARTESIAN_POINT('Ctrl Pts',(-6.58185527279857,1.58267486333834,17.2281038188601));
#52505=CARTESIAN_POINT('Ctrl Pts',(-6.61976514174731,1.40392252923987,17.2366909165839));
#52506=CARTESIAN_POINT('Ctrl Pts',(-6.6576116461526,1.2254689711687,17.2452636613821));
#52507=CARTESIAN_POINT('Ctrl Pts',(-6.68828598970659,1.04525742598236,17.2538364061803));
#52508=CARTESIAN_POINT('Ctrl Pts',(-6.71163198982137,0.863877904108215,
17.2624091509785));
#52509=CARTESIAN_POINT('Ctrl Pts',(-6.73492455131497,0.682913557061215,
17.2709622729009));
#52510=CARTESIAN_POINT('Ctrl Pts',(-6.75092218215173,0.50078686477468,17.2795153948233));
#52511=CARTESIAN_POINT('Ctrl Pts',(-6.75951936688239,0.318098929174461,
17.2880685167456));
#52512=CARTESIAN_POINT('Ctrl Pts',(-6.76446193196228,0.213070708971655,
17.2929857498937));
#52513=CARTESIAN_POINT('Ctrl Pts',(-6.76695945626195,0.107857245431671,
17.2979029830418));
#52514=CARTESIAN_POINT('Ctrl Pts',(-6.76699951028476,0.00257445253156413,
17.3028202161898));
#52515=CARTESIAN_POINT('Ctrl Pts',(-6.767,3.26333214810868E-12,17.3028202161898));
#52516=CARTESIAN_POINT('Ctrl Pts',(-6.76700000000009,-0.186007249556681,
17.3115697280026));
#52517=CARTESIAN_POINT('Ctrl Pts',(-6.75932637294265,-0.372014355812802,
17.3203192398153));
#52518=CARTESIAN_POINT('Ctrl Pts',(-6.7440051826339,-0.557389537583119,
17.329068751628));
#52519=CARTESIAN_POINT('Ctrl Pts',(-6.72868405703764,-0.742763936379661,
17.3378182264852));
#52520=CARTESIAN_POINT('Ctrl Pts',(-6.70571545643605,-0.927506130402047,
17.3465677013424));
#52521=CARTESIAN_POINT('Ctrl Pts',(-6.67517739401622,-1.11098864009264,
17.3553171761996));
#52522=CARTESIAN_POINT('Ctrl Pts',(-6.64463945804443,-1.29447039004266,
17.3640666148282));
#52523=CARTESIAN_POINT('Ctrl Pts',(-6.60653217002784,-1.47669218339009,
17.3728160534567));
#52524=CARTESIAN_POINT('Ctrl Pts',(-6.56098496085546,-1.65703510627521,
17.3815654920852));
#52525=CARTESIAN_POINT('Ctrl Pts',(-6.51543793649627,-1.83737729739757,
17.3903148952118));
#52526=CARTESIAN_POINT('Ctrl Pts',(-6.46245112156971,-2.01584035544712,
17.3990642983385));
#52527=CARTESIAN_POINT('Ctrl Pts',(-6.40220448361796,-2.1918181379718,17.4078137014651));
#52528=CARTESIAN_POINT('Ctrl Pts',(-6.34195808512052,-2.36779522106091,
17.4165630698166));
#52529=CARTESIAN_POINT('Ctrl Pts',(-6.27445201416433,-2.5412867772555,17.4253124381682));
#52530=CARTESIAN_POINT('Ctrl Pts',(-6.19991555052802,-2.7117035542848,17.4340618065197));
#52531=CARTESIAN_POINT('Ctrl Pts',(-6.12537937695198,-2.88211966813351,
17.4428111408229));
#52532=CARTESIAN_POINT('Ctrl Pts',(-6.04381298028428,-3.04946076419717,
17.4515604751261));
#52533=CARTESIAN_POINT('Ctrl Pts',(-5.95549339308955,-3.21315848424362,
17.4603098094292));
#52534=CARTESIAN_POINT('Ctrl Pts',(-5.86717414225774,-3.37685558085143,
17.4690591104108));
#52535=CARTESIAN_POINT('Ctrl Pts',(-5.77210188844023,-3.53690907700072,
17.4778084113924));
#52536=CARTESIAN_POINT('Ctrl Pts',(-5.67059953311319,-3.69277537024073,
17.4865577123739));
#52537=CARTESIAN_POINT('Ctrl Pts',(-5.56909755592633,-3.84864108281135,
17.4953069807606));
#52538=CARTESIAN_POINT('Ctrl Pts',(-5.46116568154869,-4.00031938354963,
17.5040562491472));
#52539=CARTESIAN_POINT('Ctrl Pts',(-5.34717048488254,-4.14729511918322,
17.5128055175338));
#52540=CARTESIAN_POINT('Ctrl Pts',(-5.23317570343161,-4.29427031947356,
17.5215547540522));
#52541=CARTESIAN_POINT('Ctrl Pts',(-5.1131178195138,-4.4365427624975,17.5303039905705));
#52542=CARTESIAN_POINT('Ctrl Pts',(-4.98740458929052,-4.57362924412592,
17.5390532270889));
#52543=CARTESIAN_POINT('Ctrl Pts',(-4.86169180652526,-4.71071523781489,
17.5478024324656));
#52544=CARTESIAN_POINT('Ctrl Pts',(-4.73032391141336,-4.84261509584721,
17.5565516378424));
#52545=CARTESIAN_POINT('Ctrl Pts',(-4.59374706947068,-4.96888084599838,
17.5653008432191));
#52546=CARTESIAN_POINT('Ctrl Pts',(-4.45717070231264,-5.09514615720954,
17.5740500181808));
#52547=CARTESIAN_POINT('Ctrl Pts',(-4.31538563497136,-5.21577720520769,
17.5827991931425));
#52548=CARTESIAN_POINT('Ctrl Pts',(-4.16887340951833,-5.33036429293637,
17.5915483681042));
#52549=CARTESIAN_POINT('Ctrl Pts',(-4.02236168122307,-5.44495099183837,
17.6002975133775));
#52550=CARTESIAN_POINT('Ctrl Pts',(-3.87112305262998,-5.55349359498056,
17.6090466586507));
#52551=CARTESIAN_POINT('Ctrl Pts',(-3.71567116928808,-5.65562346357335,
17.6177958039239));
#52552=CARTESIAN_POINT('Ctrl Pts',(-3.56021980053164,-5.75775299409017,
17.6265449202353));
#52553=CARTESIAN_POINT('Ctrl Pts',(-3.40055544441979,-5.85346967519938,
17.6352940365466));
#52554=CARTESIAN_POINT('Ctrl Pts',(-3.23722035886783,-5.94244843041416,
17.644043152858));
#52555=CARTESIAN_POINT('Ctrl Pts',(-3.07388580043432,-6.0314268984748,17.652792240934));
#52556=CARTESIAN_POINT('Ctrl Pts',(-2.90688078789168,-6.11366734707928,
17.66154132901));
#52557=CARTESIAN_POINT('Ctrl Pts',(-2.73677250610341,-6.18889047001451,
17.670290417086));
#52558=CARTESIAN_POINT('Ctrl Pts',(-2.56666475916883,-6.26411335643355,
17.6790394776532));
#52559=CARTESIAN_POINT('Ctrl Pts',(-2.39345402457042,-6.33231884545275,
17.6877885382203));
#52560=CARTESIAN_POINT('Ctrl Pts',(-2.21772855944014,-6.393275298049,17.6965375987875));
#52561=CARTESIAN_POINT('Ctrl Pts',(-2.04200363223574,-6.45423156404707,
17.7052866325723));
#52562=CARTESIAN_POINT('Ctrl Pts',(-1.86376426061051,-6.50793874412447,
17.7140356663571));
#52563=CARTESIAN_POINT('Ctrl Pts',(-1.68361577621741,-6.55421443943299,
17.7227847001419));
#52564=CARTESIAN_POINT('Ctrl Pts',(-1.50346782833254,-6.60048999692579,
17.7315337078708));
#52565=CARTESIAN_POINT('Ctrl Pts',(-1.32141105657412,-6.63933404265157,
17.7402827155997));
#52566=CARTESIAN_POINT('Ctrl Pts',(-1.13806375346546,-6.67061465631527,
17.7490317233286));
#52567=CARTESIAN_POINT('Ctrl Pts',(-0.954716981169866,-6.70189517941774,
17.757780705728));
#52568=CARTESIAN_POINT('Ctrl Pts',(-0.770079967441888,-6.72561226609009,
17.7665296881275));
#52569=CARTESIAN_POINT('Ctrl Pts',(-0.584779764072423,-6.7416853699599,
17.7752786705269));
#52570=CARTESIAN_POINT('Ctrl Pts',(-0.391489587592256,-6.75845153117877,
17.7844049009425));
#52571=CARTESIAN_POINT('Ctrl Pts',(-0.197478091804486,-6.76689985146396,
17.7935311313582));
#52572=CARTESIAN_POINT('Ctrl Pts',(-0.00346214753022823,-6.76699911434415,
17.8026573617738));
#52573=CARTESIAN_POINT('Ctrl Pts',(0.184490798485415,-6.76709527525933,
17.8114983974889));
#52574=CARTESIAN_POINT('Ctrl Pts',(0.372447602155526,-6.75935633790759,
17.820339433204));
#52575=CARTESIAN_POINT('Ctrl Pts',(0.559756448194932,-6.74380914014507,
17.8291804689192));
#52576=CARTESIAN_POINT('Ctrl Pts',(0.745136131044055,-6.72842206873147,
17.8379304475325));
#52577=CARTESIAN_POINT('Ctrl Pts',(0.929880851945723,-6.70538686355714,
17.8466804261458));
#52578=CARTESIAN_POINT('Ctrl Pts',(1.11336305057529,-6.67478177303301,17.8554304047591));
#52579=CARTESIAN_POINT('Ctrl Pts',(1.29684337090197,-6.64417699581246,17.8641802937991));
#52580=CARTESIAN_POINT('Ctrl Pts',(1.47906091205271,-6.60600253548042,17.872930182839));
#52581=CARTESIAN_POINT('Ctrl Pts',(1.65939671095309,-6.5603880644119,17.881680071879));
#52582=CARTESIAN_POINT('Ctrl Pts',(1.8397307236926,-6.51477404513822,17.8904298742545));
#52583=CARTESIAN_POINT('Ctrl Pts',(2.01818275357148,-6.46172023288626,17.89917967663));
#52584=CARTESIAN_POINT('Ctrl Pts',(2.19414664033449,-6.40140683918066,17.9079294790055));
#52585=CARTESIAN_POINT('Ctrl Pts',(2.37010884271373,-6.34109402281455,17.9166791976251));
#52586=CARTESIAN_POINT('Ctrl Pts',(2.54358267847909,-6.27352185699749,17.9254289162446));
#52587=CARTESIAN_POINT('Ctrl Pts',(2.71397890841836,-6.1989198643522,17.9341786348641));
#52588=CARTESIAN_POINT('Ctrl Pts',(2.88437356389044,-6.12431856103195,17.9429282726359));
#52589=CARTESIAN_POINT('Ctrl Pts',(3.05169040787282,-6.04268767582502,17.9516779104078));
#52590=CARTESIAN_POINT('Ctrl Pts',(3.21536112512171,-5.95430447953882,17.9604275481796));
#52591=CARTESIAN_POINT('Ctrl Pts',(3.3790303844295,-5.8659220705498,17.9691771080117));
#52592=CARTESIAN_POINT('Ctrl Pts',(3.53905332980071,-5.77078760703316,17.9779266678437));
#52593=CARTESIAN_POINT('Ctrl Pts',(3.69488643041981,-5.6692242208524,17.9866762276758));
#52594=CARTESIAN_POINT('Ctrl Pts',(3.85071819468833,-5.56766170563095,17.9954257124758));
#52595=CARTESIAN_POINT('Ctrl Pts',(4.00235994599317,-5.45967053456184,18.0041751972758));
#52596=CARTESIAN_POINT('Ctrl Pts',(4.14929662974394,-5.34561750206611,18.0129246820758));
#52597=CARTESIAN_POINT('Ctrl Pts',(4.29623210225124,-5.231565409744,18.0216740947511));
#52598=CARTESIAN_POINT('Ctrl Pts',(4.43846235842183,-5.11145173172129,18.0304235074265));
#52599=CARTESIAN_POINT('Ctrl Pts',(4.57550431797482,-4.98568443006513,18.0391729201018));
#52600=CARTESIAN_POINT('Ctrl Pts',(4.71254519337547,-4.85991812336638,18.0479222635597));
#52601=CARTESIAN_POINT('Ctrl Pts',(4.84439764315037,-4.72849847631046,18.0566716070176));
#52602=CARTESIAN_POINT('Ctrl Pts',(4.97061384196739,-4.59187184425286,18.0654209504755));
#52603=CARTESIAN_POINT('Ctrl Pts',(5.09682908420268,-4.45524624767677,18.0741702276229));
#52604=CARTESIAN_POINT('Ctrl Pts',(5.2174079665024,-4.31341395556809,18.0829195047702));
#52605=CARTESIAN_POINT('Ctrl Pts',(5.33194095942327,-4.16685668162759,18.0916687819176));
#52606=CARTESIAN_POINT('Ctrl Pts',(5.44647312235211,-4.02030046975109,18.1004179956612));
#52607=CARTESIAN_POINT('Ctrl Pts',(5.55495930712368,-3.86901957035433,18.1091672094047));
#52608=CARTESIAN_POINT('Ctrl Pts',(5.65703106079876,-3.71352778058251,18.1179164231482));
#52609=CARTESIAN_POINT('Ctrl Pts',(5.75910210868811,-3.55803706597481,18.1266655763944));
#52610=CARTESIAN_POINT('Ctrl Pts',(5.85475865698619,-3.39833575880779,18.1354147296406));
#52611=CARTESIAN_POINT('Ctrl Pts',(5.94367583069127,-3.23496624706602,18.1441638828868));
#52612=CARTESIAN_POINT('Ctrl Pts',(6.03259241910144,-3.0715978106997,18.152912978542));
#52613=CARTESIAN_POINT('Ctrl Pts',(6.11476958471035,-2.90456146975693,18.1616620741971));
#52614=CARTESIAN_POINT('Ctrl Pts',(6.18992823574453,-2.73442451648105,18.1704111698522));
#52615=CARTESIAN_POINT('Ctrl Pts',(6.26508641701006,-2.56428862662244,18.1791602108223));
#52616=CARTESIAN_POINT('Ctrl Pts',(6.3332260557037,-2.39105242531085,18.1879092517925));
#52617=CARTESIAN_POINT('Ctrl Pts',(6.3941157374784,-2.21530425353517,18.1966582927626));
#52618=CARTESIAN_POINT('Ctrl Pts',(6.45500505889191,-2.03955712188354,18.2054072819536));
#52619=CARTESIAN_POINT('Ctrl Pts',(6.50864441544987,-1.8612983202537,18.2141562711446));
#52620=CARTESIAN_POINT('Ctrl Pts',(6.55485164049957,-1.68113324012112,18.2229052603356));
#52621=CARTESIAN_POINT('Ctrl Pts',(6.60199852639155,-1.497304359127,18.2318321672124));
#52622=CARTESIAN_POINT('Ctrl Pts',(6.64140767441049,-1.31149113173452,18.2407590740894));
#52623=CARTESIAN_POINT('Ctrl Pts',(6.67293975269636,-1.12435050446232,18.2496859809662));
#52624=CARTESIAN_POINT('Ctrl Pts',(6.70384664831534,-0.940920291561764,
18.2584358951502));
#52625=CARTESIAN_POINT('Ctrl Pts',(6.72718585889688,-0.756215114275973,
18.2671858093342));
#52626=CARTESIAN_POINT('Ctrl Pts',(6.74287810451881,-0.57086238937319,18.2759357235182));
#52627=CARTESIAN_POINT('Ctrl Pts',(6.75857004154135,-0.385513309566141,
18.2846854656288));
#52628=CARTESIAN_POINT('Ctrl Pts',(6.76661529035562,-0.199516993257244,
18.2934352077394));
#52629=CARTESIAN_POINT('Ctrl Pts',(6.76698652348897,-0.0135052182030834,
18.30218494985));
#52630=CARTESIAN_POINT('Ctrl Pts',(6.76735774981519,0.17250314603988,18.3109345315206));
#52631=CARTESIAN_POINT('Ctrl Pts',(6.76005524147474,0.358526681834471,18.3196841131912));
#52632=CARTESIAN_POINT('Ctrl Pts',(6.74510380214873,0.543933542115877,18.3284336948619));
#52633=CARTESIAN_POINT('Ctrl Pts',(6.73015261710969,0.729337249085657,18.3371831277238));
#52634=CARTESIAN_POINT('Ctrl Pts',(6.70755278444593,0.914124015855522,18.3459325605857));
#52635=CARTESIAN_POINT('Ctrl Pts',(6.67738106408276,1.09766621749464,18.3546819934477));
#52636=CARTESIAN_POINT('Ctrl Pts',(6.64720981677239,1.28120554143399,18.36343128913));
#52637=CARTESIAN_POINT('Ctrl Pts',(6.60946696581506,1.46350005650695,18.3721805848124));
#52638=CARTESIAN_POINT('Ctrl Pts',(6.56428070010976,1.64393062206608,18.3809298804947));
#52639=CARTESIAN_POINT('Ctrl Pts',(6.51909508282721,1.82435859844722,18.3896790506247));
#52640=CARTESIAN_POINT('Ctrl Pts',(6.46646633415641,2.00292240086628,18.3984282207547));
#52641=CARTESIAN_POINT('Ctrl Pts',(6.40657319597172,2.17901557696514,18.4071773908847));
#52642=CARTESIAN_POINT('Ctrl Pts',(6.3466808376827,2.355106460075,18.4159264470877));
#52643=CARTESIAN_POINT('Ctrl Pts',(6.27952437143856,2.52872650996602,18.4246755032908));
#52644=CARTESIAN_POINT('Ctrl Pts',(6.20533187335102,2.69928607998002,18.4334245594939));
#52645=CARTESIAN_POINT('Ctrl Pts',(6.1283144978422,2.87633970115466,18.4425067357828));
#52646=CARTESIAN_POINT('Ctrl Pts',(6.04371489463123,3.05009490562409,18.4515889120716));
#52647=CARTESIAN_POINT('Ctrl Pts',(5.95184265120463,3.21991584599683,18.4606710883604));
#52648=CARTESIAN_POINT('Ctrl Pts',(5.86333281335462,3.38352155905352,18.4694208687148));
#52649=CARTESIAN_POINT('Ctrl Pts',(5.76807337235653,3.54347560903877,18.4781706490693));
#52650=CARTESIAN_POINT('Ctrl Pts',(5.66638790086321,3.699234671787,18.4869204294237));
#52651=CARTESIAN_POINT('Ctrl Pts',(5.564706085027,3.85498813489826,18.4956698952179));
#52652=CARTESIAN_POINT('Ctrl Pts',(5.456598857669,4.00654667256333,18.5044193610122));
#52653=CARTESIAN_POINT('Ctrl Pts',(5.34243340580445,4.1533955150629,18.5131688268065));
#52654=CARTESIAN_POINT('Ctrl Pts',(5.22827145140523,4.30023985883957,18.5219180245604));
#52655=CARTESIAN_POINT('Ctrl Pts',(5.10805181978009,4.44237456993136,18.5306672223142));
#52656=CARTESIAN_POINT('Ctrl Pts',(4.98218281282461,4.57931691626547,18.5394164200681));
#52657=CARTESIAN_POINT('Ctrl Pts',(4.85631699296121,4.71625579512274,18.5481653962861));
#52658=CARTESIAN_POINT('Ctrl Pts',(4.72480227791711,4.84800236135894,18.5569143725041));
#52659=CARTESIAN_POINT('Ctrl Pts',(4.58808530847967,4.97410918679044,18.5656633487221));
#52660=CARTESIAN_POINT('Ctrl Pts',(4.45135945056814,5.10022421089146,18.5744128937433));
#52661=CARTESIAN_POINT('Ctrl Pts',(4.30943087207873,5.22069856612124,18.5831624387646));
#52662=CARTESIAN_POINT('Ctrl Pts',(4.16278164322291,5.33512305301822,18.5919119837858));
#52663=CARTESIAN_POINT('Ctrl Pts',(4.01614103534205,5.44954081331564,18.600661014453));
#52664=CARTESIAN_POINT('Ctrl Pts',(3.86478055833219,5.55790924068473,18.6094100451203));
#52665=CARTESIAN_POINT('Ctrl Pts',(3.70921425811749,5.65986029751424,18.6181590757875));
#52666=CARTESIAN_POINT('Ctrl Pts',(3.55364584529916,5.76181273884779,18.6269082252674));
#52667=CARTESIAN_POINT('Ctrl Pts',(3.39387173464139,5.85734747818182,18.6356573747472));
#52668=CARTESIAN_POINT('Ctrl Pts',(3.23043456092199,5.94614005448919,18.6444065242271));
#52669=CARTESIAN_POINT('Ctrl Pts',(3.18690768806252,5.96978744811355,18.6467366129601));
#52670=CARTESIAN_POINT('Ctrl Pts',(3.14312114982809,5.99295688499337,18.6490667016931));
#52671=CARTESIAN_POINT('Ctrl Pts',(3.09908550384716,6.01564277861015,18.6513967904261));
#52672=CARTESIAN_POINT('Origin',(0.,0.,-63.6971797838103));
#52673=CARTESIAN_POINT('',(3.0990855038473,6.01564277861008,21.0460278352566));
#52674=CARTESIAN_POINT('',(3.09908550384707,6.01564277861019,20.6515076495525));
#52675=CARTESIAN_POINT('',(3.09908550384721,6.01564277861012,-63.6971797838103));
#52676=CARTESIAN_POINT('',(-6.767,7.50599334255745E-8,19.6971817862495));
#52677=CARTESIAN_POINT('Ctrl Pts',(-6.767,7.50599334255761E-8,19.6971817862495));
#52678=CARTESIAN_POINT('Ctrl Pts',(-6.7670000019611,-0.176801917699121,
19.7055396886733));
#52679=CARTESIAN_POINT('Ctrl Pts',(-6.76006670113114,-0.35378666355907,
19.7138975910971));
#52680=CARTESIAN_POINT('Ctrl Pts',(-6.74618310727778,-0.53037956510401,
19.722255493521));
#52681=CARTESIAN_POINT('Ctrl Pts',(-6.73231304500031,-0.70680035125333,
19.7306052499567));
#52682=CARTESIAN_POINT('Ctrl Pts',(-6.71150621456675,-0.882829712877172,
19.7389550063924));
#52683=CARTESIAN_POINT('Ctrl Pts',(-6.68379765480675,-1.05789314658895,
19.7473047628281));
#52684=CARTESIAN_POINT('Ctrl Pts',(-6.65611120922512,-1.2328168623206,19.7556478553301));
#52685=CARTESIAN_POINT('Ctrl Pts',(-6.62153406509078,-1.40677584781493,
19.7639909478322));
#52686=CARTESIAN_POINT('Ctrl Pts',(-6.58015308656352,-1.57920054375262,
19.7723340403343));
#52687=CARTESIAN_POINT('Ctrl Pts',(-6.53879783380593,-1.75151804652644,
19.7806719460939));
#52688=CARTESIAN_POINT('Ctrl Pts',(-6.49064725738989,-1.92230282704946,
19.7890098518536));
#52689=CARTESIAN_POINT('Ctrl Pts',(-6.43583938430197,-2.09099507877653,
19.7973477576132));
#52690=CARTESIAN_POINT('Ctrl Pts',(-6.38105405776363,-2.25961793484924,
19.8056822333729));
#52691=CARTESIAN_POINT('Ctrl Pts',(-6.31961699868245,-2.42614965081121,
19.8140167091326));
#52692=CARTESIAN_POINT('Ctrl Pts',(-6.25171630185697,-2.59004484152221,
19.8223511848922));
#52693=CARTESIAN_POINT('Ctrl Pts',(-6.18383044630271,-2.7539042091402,19.830683838959));
#52694=CARTESIAN_POINT('Ctrl Pts',(-6.10948389970995,-2.91512788198916,
19.8390164930258));
#52695=CARTESIAN_POINT('Ctrl Pts',(-6.02891329099595,-3.0731894718114,19.8473491470925));
#52696=CARTESIAN_POINT('Ctrl Pts',(-5.94834740506893,-3.23124179657743,
19.8556813127262));
#52697=CARTESIAN_POINT('Ctrl Pts',(-5.86155834060649,-3.38613210120756,
19.86401347836));
#52698=CARTESIAN_POINT('Ctrl Pts',(-5.76882927709368,-3.53735745603224,
19.8723456439937));
#52699=CARTESIAN_POINT('Ctrl Pts',(-5.6760908173443,-3.68859813452304,19.8806786539258));
#52700=CARTESIAN_POINT('Ctrl Pts',(-5.57741133947012,-3.83617283005422,
19.8890116638578));
#52701=CARTESIAN_POINT('Ctrl Pts',(-5.47311817133102,-3.97960632257089,
19.8973446737899));
#52702=CARTESIAN_POINT('Ctrl Pts',(-5.36875617982275,-4.1231344672722,19.9056831826999));
#52703=CARTESIAN_POINT('Ctrl Pts',(-5.25877329786672,-4.2625156692081,19.9140216916098));
#52704=CARTESIAN_POINT('Ctrl Pts',(-5.14353865202304,-4.39730589510726,
19.9223602005197));
#52705=CARTESIAN_POINT('Ctrl Pts',(-5.02826519893037,-4.53214151393333,
19.9307015175659));
#52706=CARTESIAN_POINT('Ctrl Pts',(-4.90773668534676,-4.66238281766333,
19.9390428346121));
#52707=CARTESIAN_POINT('Ctrl Pts',(-4.78236037383168,-4.78762135666602,
19.9473841516583));
#52708=CARTESIAN_POINT('Ctrl Pts',(-4.65685677636424,-4.9129870417501,19.9557339370705));
#52709=CARTESIAN_POINT('Ctrl Pts',(-4.52649579541607,-5.03333957507811,
19.9640837224826));
#52710=CARTESIAN_POINT('Ctrl Pts',(-4.39171998876124,-5.14830890101934,
19.9724335078948));
#52711=CARTESIAN_POINT('Ctrl Pts',(-4.28901518590022,-5.23592033699538,
19.9787963936824));
#52712=CARTESIAN_POINT('Ctrl Pts',(-4.18374738657325,-5.32040648979079,
19.9851592794701));
#52713=CARTESIAN_POINT('Ctrl Pts',(-4.07612420460264,-5.40162017071291,
19.9915221652578));
#52714=CARTESIAN_POINT('Ctrl Pts',(-3.93841941548391,-5.50553377557166,
19.9996635324756));
#52715=CARTESIAN_POINT('Ctrl Pts',(-3.7965628885728,-5.60431055798295,20.0078048996935));
#52716=CARTESIAN_POINT('Ctrl Pts',(-3.65097880291341,-5.69759973854578,
20.0159462669114));
#52717=CARTESIAN_POINT('Ctrl Pts',(-3.50552180108836,-5.79080748474912,
20.0240805273348));
#52718=CARTESIAN_POINT('Ctrl Pts',(-3.35634402349876,-5.87853696802974,
20.0322147877583));
#52719=CARTESIAN_POINT('Ctrl Pts',(-3.20390163287579,-5.96047844781406,
20.0403490481818));
#52720=CARTESIAN_POINT('Ctrl Pts',(-3.05156323294489,-6.04236403008091,
20.0484777597066));
#52721=CARTESIAN_POINT('Ctrl Pts',(-2.89596497497535,-6.11846929732322,
20.0566064712315));
#52722=CARTESIAN_POINT('Ctrl Pts',(-2.73759079890839,-6.1885285502882,20.0647351827564));
#52723=CARTESIAN_POINT('Ctrl Pts',(-2.57929214855954,-6.25855439329,20.0728600178489));
#52724=CARTESIAN_POINT('Ctrl Pts',(-2.41822055028159,-6.32253981577258,
20.0809848529414));
#52725=CARTESIAN_POINT('Ctrl Pts',(-2.25488325185526,-6.38026570923991,
20.0891096880339));
#52726=CARTESIAN_POINT('Ctrl Pts',(-2.0915916801637,-6.43797544218147,20.0972322485561));
#52727=CARTESIAN_POINT('Ctrl Pts',(-1.92603601680998,-6.4894290154097,20.1053548090783));
#52728=CARTESIAN_POINT('Ctrl Pts',(-1.75874209977583,-6.5344560008065,20.1134773696004));
#52729=CARTESIAN_POINT('Ctrl Pts',(-1.59143929150364,-6.57948537927086,
20.1216003618156));
#52730=CARTESIAN_POINT('Ctrl Pts',(-1.42239839745797,-6.61808738865115,
20.1297233540308));
#52731=CARTESIAN_POINT('Ctrl Pts',(-1.25215916183377,-6.65014183558785,
20.137846346246));
#52732=CARTESIAN_POINT('Ctrl Pts',(-1.1652572200179,-6.66650465390303,20.1419928862271));
#52733=CARTESIAN_POINT('Ctrl Pts',(-1.0780432045147,-6.68116213074483,20.1461394262081));
#52734=CARTESIAN_POINT('Ctrl Pts',(-0.99058984092042,-6.69410343265364,
20.1502859661891));
#52735=CARTESIAN_POINT('Ctrl Pts',(-0.801118329007074,-6.72214132551464,
20.1592696252175));
#52736=CARTESIAN_POINT('Ctrl Pts',(-0.61061671185007,-6.74210688210214,
20.1682532842459));
#52737=CARTESIAN_POINT('Ctrl Pts',(-0.419754791226097,-6.75396882693744,
20.1772369432742));
#52738=CARTESIAN_POINT('Ctrl Pts',(-0.228564971845571,-6.76585115046825,
20.1862360361336));
#52739=CARTESIAN_POINT('Ctrl Pts',(-0.0370138505142297,-6.76960202140709,
20.1952351289929));
#52740=CARTESIAN_POINT('Ctrl Pts',(0.154228262328821,-6.76524224570703,
20.2042342218523));
#52741=CARTESIAN_POINT('Ctrl Pts',(0.34591878448494,-6.76087224755126,20.2132544150697));
#52742=CARTESIAN_POINT('Ctrl Pts',(0.537298608434677,-6.74835355818315,
20.222274608287));
#52743=CARTESIAN_POINT('Ctrl Pts',(0.727699264931206,-6.72775912022856,
20.2312948015044));
#52744=CARTESIAN_POINT('Ctrl Pts',(0.918292749769805,-6.70714382524859,
20.2403241299261));
#52745=CARTESIAN_POINT('Ctrl Pts',(1.10790484918032,-6.67843647431839,20.2493534583478));
#52746=CARTESIAN_POINT('Ctrl Pts',(1.29587518300171,-6.64176155173312,20.2583827867695));
#52747=CARTESIAN_POINT('Ctrl Pts',(1.4841105171046,-6.60503492489956,20.2674248447242));
#52748=CARTESIAN_POINT('Ctrl Pts',(1.67069922279195,-6.56031831238033,20.276466902679));
#52749=CARTESIAN_POINT('Ctrl Pts',(1.85499175602118,-6.50778722647671,20.2855089606337));
#52750=CARTESIAN_POINT('Ctrl Pts',(2.01492565910245,-6.46219936974455,20.2933558961294));
#52751=CARTESIAN_POINT('Ctrl Pts',(2.17313038866878,-6.41072707698854,20.3012028316251));
#52752=CARTESIAN_POINT('Ctrl Pts',(2.32919171885851,-6.35351516381294,20.3090497671208));
#52753=CARTESIAN_POINT('Ctrl Pts',(2.5012934457399,-6.29042285873173,20.3177032314216));
#52754=CARTESIAN_POINT('Ctrl Pts',(2.67093975429473,-6.22029356059689,20.3263566957224));
#52755=CARTESIAN_POINT('Ctrl Pts',(2.83755243353247,-6.14333664932616,20.3350101600233));
#52756=CARTESIAN_POINT('Ctrl Pts',(3.00401162841341,-6.0664506311116,20.3436556527135));
#52757=CARTESIAN_POINT('Ctrl Pts',(3.16744249283284,-5.98274967161941,20.3523011454037));
#52758=CARTESIAN_POINT('Ctrl Pts',(3.32728625269314,-5.89249142491011,20.3609466380939));
#52759=CARTESIAN_POINT('Ctrl Pts',(3.49193863767322,-5.79951791379029,20.3698522155904));
#52760=CARTESIAN_POINT('Ctrl Pts',(3.65278441561305,-5.69958652694498,20.3787577930869));
#52761=CARTESIAN_POINT('Ctrl Pts',(3.8092374397924,-5.59303130040266,20.3876633705835));
#52762=CARTESIAN_POINT('Ctrl Pts',(3.96083310453578,-5.48978426836671,20.396292458756));
#52763=CARTESIAN_POINT('Ctrl Pts',(4.10830440336963,-5.38031870236594,20.4049215469286));
#52764=CARTESIAN_POINT('Ctrl Pts',(4.25114468426882,-5.26498412850532,20.4135506351012));
#52765=CARTESIAN_POINT('Ctrl Pts',(4.40085020027326,-5.1441063075975,20.4225944572597));
#52766=CARTESIAN_POINT('Ctrl Pts',(4.54546827328342,-5.01678157922803,20.4316382794181));
#52767=CARTESIAN_POINT('Ctrl Pts',(4.68445121006545,-4.88346248685462,20.4406821015766));
#52768=CARTESIAN_POINT('Ctrl Pts',(4.82343414684748,-4.75014339448122,20.4497259237351));
#52769=CARTESIAN_POINT('Ctrl Pts',(4.95678164535619,-4.61083017984488,20.4587697458936));
#52770=CARTESIAN_POINT('Ctrl Pts',(5.08398704627084,-4.46602336686121,20.4678135680522));
#52771=CARTESIAN_POINT('Ctrl Pts',(5.20249954652553,-4.33111229125269,20.4762393579019));
#52772=CARTESIAN_POINT('Ctrl Pts',(5.31562900031493,-4.19149202381202,20.4846651477517));
#52773=CARTESIAN_POINT('Ctrl Pts',(5.42300844233551,-4.04762503628459,20.4930909376015));
#52774=CARTESIAN_POINT('Ctrl Pts',(5.53041279999891,-3.90372466677633,20.5015186825179));
#52775=CARTESIAN_POINT('Ctrl Pts',(5.63206428741306,-3.75557587813829,20.5099464274344));
#52776=CARTESIAN_POINT('Ctrl Pts',(5.72763828737402,-3.60367155121097,20.5183741723508));
#52777=CARTESIAN_POINT('Ctrl Pts',(5.82324740598551,-3.45171140706374,20.5268050140408));
#52778=CARTESIAN_POINT('Ctrl Pts',(5.91277440794826,-3.29599325354146,20.5352358557307));
#52779=CARTESIAN_POINT('Ctrl Pts',(5.99593959107438,-3.13703640721411,20.5436666974207));
#52780=CARTESIAN_POINT('Ctrl Pts',(6.07918119238835,-2.9779334998347,20.552105285978));
#52781=CARTESIAN_POINT('Ctrl Pts',(6.15604914192404,-2.81558624792901,20.5605438745353));
#52782=CARTESIAN_POINT('Ctrl Pts',(6.2263105602298,-2.65053689043766,20.5689824630926));
#52783=CARTESIAN_POINT('Ctrl Pts',(6.29660882051841,-2.48540098835689,20.5774254764729));
#52784=CARTESIAN_POINT('Ctrl Pts',(6.36029351816141,-2.31756046262265,20.5858684898532));
#52785=CARTESIAN_POINT('Ctrl Pts',(6.41718080857057,-2.14757525365552,20.5943115032334));
#52786=CARTESIAN_POINT('Ctrl Pts',(6.47412786304321,-1.97741146337882,20.6027633865877));
#52787=CARTESIAN_POINT('Ctrl Pts',(6.52426314762407,-1.80509880553376,20.6112152699419));
#52788=CARTESIAN_POINT('Ctrl Pts',(6.56745304480664,-1.63121105448068,20.6196671532962));
#52789=CARTESIAN_POINT('Ctrl Pts',(6.57922365626102,-1.58382114878889,20.6219705585254));
#52790=CARTESIAN_POINT('Ctrl Pts',(6.59047870375266,-1.53631430889342,20.6242739637547));
#52791=CARTESIAN_POINT('Ctrl Pts',(6.60121614522942,-1.48870225497327,20.6265773689839));
#52792=CARTESIAN_POINT('Ctrl Pts',(6.63998750366456,-1.31678196908697,20.6348946343173));
#52793=CARTESIAN_POINT('Ctrl Pts',(6.67207593033756,-1.14318001944469,20.6432118996508));
#52794=CARTESIAN_POINT('Ctrl Pts',(6.69734220124111,-0.968450535378533,
20.6515291649842));
#52795=CARTESIAN_POINT('Ctrl Pts',(6.72258716198922,-0.793868422187867,
20.6598394153443));
#52796=CARTESIAN_POINT('Ctrl Pts',(6.74102138152034,-0.618161011823664,
20.6681496657043));
#52797=CARTESIAN_POINT('Ctrl Pts',(6.75255649033741,-0.441893476759026,
20.6764599160644));
#52798=CARTESIAN_POINT('Ctrl Pts',(6.76408398269993,-0.265742328430808,
20.6847646792943));
#52799=CARTESIAN_POINT('Ctrl Pts',(6.76872141886024,-0.0890321382852432,
20.6930694425242));
#52800=CARTESIAN_POINT('Ctrl Pts',(6.76643212665369,0.0876657024660587,
20.701374205754));
#52801=CARTESIAN_POINT('Ctrl Pts',(6.76414392696195,0.264279218024154,20.7096750057166));
#52802=CARTESIAN_POINT('Ctrl Pts',(6.7549355912046,0.440880048849934,20.7179758056792));
#52803=CARTESIAN_POINT('Ctrl Pts',(6.73882252188824,0.616895468042915,20.7262766056419));
#52804=CARTESIAN_POINT('Ctrl Pts',(6.72271419358492,0.792859097512794,20.7345749632268));
#52805=CARTESIAN_POINT('Ctrl Pts',(6.69970521299222,0.968237312720989,20.7428733208117));
#52806=CARTESIAN_POINT('Ctrl Pts',(6.66986296581343,1.14246094780981,20.7511716783966));
#52807=CARTESIAN_POINT('Ctrl Pts',(6.64001768225444,1.31670230975392,20.7594708803204));
#52808=CARTESIAN_POINT('Ctrl Pts',(6.60333779420146,1.48978851276434,20.7677700822442));
#52809=CARTESIAN_POINT('Ctrl Pts',(6.55994219260918,1.66115846011929,20.776069284168));
#52810=CARTESIAN_POINT('Ctrl Pts',(6.51654219152551,1.8325457811384,20.7843693274735));
#52811=CARTESIAN_POINT('Ctrl Pts',(6.46642520474349,2.00221616218893,20.792669370779));
#52812=CARTESIAN_POINT('Ctrl Pts',(6.40976058365726,2.16962168596135,20.8009694140846));
#52813=CARTESIAN_POINT('Ctrl Pts',(6.35308081140155,2.33707197116365,20.8092716766825));
#52814=CARTESIAN_POINT('Ctrl Pts',(6.28985002702341,2.50225586252743,20.8175739392805));
#52815=CARTESIAN_POINT('Ctrl Pts',(6.22028656411547,2.66464332702982,20.8258762018784));
#52816=CARTESIAN_POINT('Ctrl Pts',(6.1506929520334,2.82710117112143,20.834182062721));
#52817=CARTESIAN_POINT('Ctrl Pts',(6.07476132826883,2.98675985325214,20.8424879235636));
#52818=CARTESIAN_POINT('Ctrl Pts',(5.99275708164464,3.143111763905,20.8507937844063));
#52819=CARTESIAN_POINT('Ctrl Pts',(5.91065590021539,3.29964849354718,20.8591094633624));
#52820=CARTESIAN_POINT('Ctrl Pts',(5.82246791573087,3.45287033355623,20.8674251423185));
#52821=CARTESIAN_POINT('Ctrl Pts',(5.72850376926257,3.6022955966362,20.8757408212746));
#52822=CARTESIAN_POINT('Ctrl Pts',(5.63448019122017,3.75181537000471,20.8840617598315));
#52823=CARTESIAN_POINT('Ctrl Pts',(5.53467336173813,3.89753349101612,20.8923826983883));
#52824=CARTESIAN_POINT('Ctrl Pts',(5.42943580675272,4.03899935879562,20.9007036369451));
#52825=CARTESIAN_POINT('Ctrl Pts',(5.32404183616345,4.18067548867345,20.909036942994));
#52826=CARTESIAN_POINT('Ctrl Pts',(5.21320122733091,4.31808646410224,20.917370249043));
#52827=CARTESIAN_POINT('Ctrl Pts',(5.09730601876832,4.4508156950191,20.9257035550919));
#52828=CARTESIAN_POINT('Ctrl Pts',(5.01200030279605,4.54851224532726,20.9318373603435));
#52829=CARTESIAN_POINT('Ctrl Pts',(4.92395689847716,4.64367304143043,20.9379711655951));
#52830=CARTESIAN_POINT('Ctrl Pts',(4.83334402846156,4.73614553223769,20.9441049708467));
#52831=CARTESIAN_POINT('Ctrl Pts',(4.70787102970677,4.8641935757652,20.9525985428809));
#52832=CARTESIAN_POINT('Ctrl Pts',(4.57706282676204,4.98749972683568,20.961092114915));
#52833=CARTESIAN_POINT('Ctrl Pts',(4.44132178010929,5.10558026531038,20.9695856869492));
#52834=CARTESIAN_POINT('Ctrl Pts',(4.31250030380911,5.21764150001963,20.9776462884804));
#52835=CARTESIAN_POINT('Ctrl Pts',(4.17923668925624,5.32499628093545,20.9857068900117));
#52836=CARTESIAN_POINT('Ctrl Pts',(4.04191632955374,5.42726463191974,20.9937674915429));
#52837=CARTESIAN_POINT('Ctrl Pts',(3.90472119891727,5.52943971945709,21.0018207422224));
#52838=CARTESIAN_POINT('Ctrl Pts',(3.76347697774605,5.62653738171646,21.009873992902));
#52839=CARTESIAN_POINT('Ctrl Pts',(3.61860468201547,5.71821555691072,21.0179272435815));
#52840=CARTESIAN_POINT('Ctrl Pts',(3.47385946705332,5.80981331277502,21.0259734300168));
#52841=CARTESIAN_POINT('Ctrl Pts',(3.32549282799942,5.89600084867242,21.034019616452));
#52842=CARTESIAN_POINT('Ctrl Pts',(3.17395719995998,5.97647761585553,21.0420658028873));
#52843=CARTESIAN_POINT('Ctrl Pts',(3.14908458615611,5.98968683652678,21.0433864803437));
#52844=CARTESIAN_POINT('Ctrl Pts',(3.12412666215165,6.00274229672367,21.0447071578001));
#52845=CARTESIAN_POINT('Ctrl Pts',(3.0990855038473,6.01564277861008,21.0460278352566));
#52846=CARTESIAN_POINT('Ctrl Pts',(3.0990855038472,6.01564277861012,19.0457563580462));
#52847=CARTESIAN_POINT('Ctrl Pts',(2.93373232018331,6.10082796552479,19.0545058059455));
#52848=CARTESIAN_POINT('Ctrl Pts',(2.76486502144431,6.17919158180188,19.0632552538448));
#52849=CARTESIAN_POINT('Ctrl Pts',(2.59305716434359,6.25046746591376,19.0720047017441));
#52850=CARTESIAN_POINT('Ctrl Pts',(2.42125069459297,6.32174277447219,19.0807540789915));
#52851=CARTESIAN_POINT('Ctrl Pts',(2.2465039787108,6.38593035557818,19.0895034562389));
#52852=CARTESIAN_POINT('Ctrl Pts',(2.06941053323801,6.44281220003529,19.0982528334863));
#52853=CARTESIAN_POINT('Ctrl Pts',(1.8923184589671,6.49969360406677,19.1070021429889));
#52854=CARTESIAN_POINT('Ctrl Pts',(1.71287996431529,6.54926929700875,19.1157514524915));
#52855=CARTESIAN_POINT('Ctrl Pts',(1.53170449173525,6.59137090065474,19.1245007619941));
#52856=CARTESIAN_POINT('Ctrl Pts',(1.35053036178188,6.6334721923008,19.1332500066587));
#52857=CARTESIAN_POINT('Ctrl Pts',(1.16761955878859,6.66809944062452,19.1419992513233));
#52858=CARTESIAN_POINT('Ctrl Pts',(0.983593309310603,6.6951350398539,19.1507484959879));
#52859=CARTESIAN_POINT('Ctrl Pts',(0.799568362460142,6.72217044771212,19.1594976787211));
#52860=CARTESIAN_POINT('Ctrl Pts',(0.614428268438801,6.74161427235975,19.1682468614542));
#52861=CARTESIAN_POINT('Ctrl Pts',(0.42880181633052,6.753400476968,19.1769960441874));
#52862=CARTESIAN_POINT('Ctrl Pts',(0.243176616523182,6.7651866020624,19.1857451678955));
#52863=CARTESIAN_POINT('Ctrl Pts',(0.0570653511660035,6.76931519233996,
19.1944942916037));
#52864=CARTESIAN_POINT('Ctrl Pts',(-0.128899900799341,6.76577222610797,
19.2032434153118));
#52865=CARTESIAN_POINT('Ctrl Pts',(-0.314863959941376,6.76222928260136,
19.2119924829011));
#52866=CARTESIAN_POINT('Ctrl Pts',(-0.500681721080079,6.75101488651281,
19.2207415504903));
#52867=CARTESIAN_POINT('Ctrl Pts',(-0.685722110172742,6.73216712415997,
19.2294906180796));
#52868=CARTESIAN_POINT('Ctrl Pts',(-0.870761373826987,6.71331947644153,
19.2382396324559));
#52869=CARTESIAN_POINT('Ctrl Pts',(-1.05502298984274,6.68683858440007,19.2469886468323));
#52870=CARTESIAN_POINT('Ctrl Pts',(-1.23788117675984,6.6528143813144,19.2557376612087));
#52871=CARTESIAN_POINT('Ctrl Pts',(-1.43009641451712,6.61704912302395,19.2649343720962));
#52872=CARTESIAN_POINT('Ctrl Pts',(-1.62076048992609,6.57294837083186,19.2741310829837));
#52873=CARTESIAN_POINT('Ctrl Pts',(-1.8091579896104,6.52067760042075,19.2833277938712));
#52874=CARTESIAN_POINT('Ctrl Pts',(-1.98840443002914,6.47094578577439,19.2920777915777));
#52875=CARTESIAN_POINT('Ctrl Pts',(-2.16559895952088,6.4138188847451,19.3008277892842));
#52876=CARTESIAN_POINT('Ctrl Pts',(-2.34013966242213,6.34949095285274,19.3095777869907));
#52877=CARTESIAN_POINT('Ctrl Pts',(-2.5146768255391,6.28516432556727,19.3183276072423));
#52878=CARTESIAN_POINT('Ctrl Pts',(-2.68656000078742,6.21363705879704,19.3270774274939));
#52879=CARTESIAN_POINT('Ctrl Pts',(-2.85520533840792,6.13515211510904,19.3358272477455));
#52880=CARTESIAN_POINT('Ctrl Pts',(-3.02384747998231,6.05666865881169,19.3445769021768));
#52881=CARTESIAN_POINT('Ctrl Pts',(-3.1892516468444,5.97122791039895,19.353326556608));
#52882=CARTESIAN_POINT('Ctrl Pts',(-3.35085601829061,5.87912008251963,19.3620762110393));
#52883=CARTESIAN_POINT('Ctrl Pts',(-3.5124575419132,5.78701387778234,19.3708257112824));
#52884=CARTESIAN_POINT('Ctrl Pts',(-3.67025915510836,5.68824097061047,19.3795752115255));
#52885=CARTESIAN_POINT('Ctrl Pts',(-3.82372487928733,5.58313684656924,19.3883247117687));
#52886=CARTESIAN_POINT('Ctrl Pts',(-3.9771881030071,5.47803443501837,19.3970740694538));
#52887=CARTESIAN_POINT('Ctrl Pts',(-4.12631534262951,5.36660117496434,19.4058234271389));
#52888=CARTESIAN_POINT('Ctrl Pts',(-4.27060009886163,5.24921554097401,19.414572784824));
#52889=CARTESIAN_POINT('Ctrl Pts',(-4.41488269594165,5.13183166360333,19.4233220115792));
#52890=CARTESIAN_POINT('Ctrl Pts',(-4.55432273235053,5.00849577139504,19.4320712383344));
#52891=CARTESIAN_POINT('Ctrl Pts',(-4.68844662480183,4.87962675277365,19.4408204650896));
#52892=CARTESIAN_POINT('Ctrl Pts',(-4.82256868835128,4.75075949139912,19.4495695725411));
#52893=CARTESIAN_POINT('Ctrl Pts',(-4.95137454637826,4.61635945312563,19.4583186799926));
#52894=CARTESIAN_POINT('Ctrl Pts',(-5.07442674461037,4.47688309134637,19.4670677874441));
#52895=CARTESIAN_POINT('Ctrl Pts',(-5.19747742838517,4.33740844616379,19.4758167872165));
#52896=CARTESIAN_POINT('Ctrl Pts',(-5.31477440450922,4.19285781736036,19.4845657869888));
#52897=CARTESIAN_POINT('Ctrl Pts',(-5.42591931531163,4.04372211999392,19.4933147867612));
#52898=CARTESIAN_POINT('Ctrl Pts',(-5.53707636462996,3.8945701350078,19.5020647420418));
#52899=CARTESIAN_POINT('Ctrl Pts',(-5.64207983273489,3.74083230916393,19.5108146973224));
#52900=CARTESIAN_POINT('Ctrl Pts',(-5.74057303468769,3.58303087251792,19.519564652603));
#52901=CARTESIAN_POINT('Ctrl Pts',(-5.83906243363792,3.42523552887385,19.5283142700318));
#52902=CARTESIAN_POINT('Ctrl Pts',(-5.93104191768457,3.26337713156936,19.5370638874606));
#52903=CARTESIAN_POINT('Ctrl Pts',(-6.01619906699691,3.09800545291088,19.5458135048894));
#52904=CARTESIAN_POINT('Ctrl Pts',(-6.10135338095419,2.9326392803952,19.5545628309948));
#52905=CARTESIAN_POINT('Ctrl Pts',(-6.17968568352877,2.7637603154014,19.5633121571002));
#52906=CARTESIAN_POINT('Ctrl Pts',(-6.25092992694924,2.5919421383145,19.5720614832056));
#52907=CARTESIAN_POINT('Ctrl Pts',(-6.32217217691139,2.42012876880728,19.5808105644994));
#52908=CARTESIAN_POINT('Ctrl Pts',(-6.38632665483883,2.24537661647578,19.5895596457932));
#52909=CARTESIAN_POINT('Ctrl Pts',(-6.44317547869379,2.06827917621365,19.598308727087));
#52910=CARTESIAN_POINT('Ctrl Pts',(-6.50002944235964,1.89116572423327,19.6070585994019));
#52911=CARTESIAN_POINT('Ctrl Pts',(-6.54957634250424,1.71170683289098,19.6158084717169));
#52912=CARTESIAN_POINT('Ctrl Pts',(-6.5916478770842,1.5305120922526,19.6245583440319));
#52913=CARTESIAN_POINT('Ctrl Pts',(-6.63371649075029,1.34932993147928,19.6333076088667));
#52914=CARTESIAN_POINT('Ctrl Pts',(-6.66831071257141,1.16641244173905,19.6420568737015));
#52915=CARTESIAN_POINT('Ctrl Pts',(-6.69531304840347,0.982380875159052,
19.6508061385363));
#52916=CARTESIAN_POINT('Ctrl Pts',(-6.72231677033056,0.798339861794849,
19.6595558524919));
#52917=CARTESIAN_POINT('Ctrl Pts',(-6.74172778477899,0.613184940729128,
19.6683055664476));
#52918=CARTESIAN_POINT('Ctrl Pts',(-6.75348015835525,0.427545027689496,
19.6770552804032));
#52919=CARTESIAN_POINT('Ctrl Pts',(-6.76249038365216,0.28521995354738,19.6837634482055));
#52920=CARTESIAN_POINT('Ctrl Pts',(-6.76699999999992,0.142609995759486,
19.6904716160077));
#52921=CARTESIAN_POINT('Ctrl Pts',(-6.767,3.718767489228E-12,19.6971797838099));
#52922=CARTESIAN_POINT('',(-6.76699844390314,-0.0035429858251562,19.3028202161898));
#52923=CARTESIAN_POINT('Ctrl Pts',(3.09908550384716,6.01564277861015,18.6513967904261));
#52924=CARTESIAN_POINT('Ctrl Pts',(2.93373232018326,6.10082796552481,18.6601462383254));
#52925=CARTESIAN_POINT('Ctrl Pts',(2.76486502144426,6.17919158180191,18.6688956862247));
#52926=CARTESIAN_POINT('Ctrl Pts',(2.59305716434353,6.25046746591379,18.677645134124));
#52927=CARTESIAN_POINT('Ctrl Pts',(2.4212506945928,6.32174277447226,18.6863945113714));
#52928=CARTESIAN_POINT('Ctrl Pts',(2.24650397871051,6.38593035557828,18.6951438886188));
#52929=CARTESIAN_POINT('Ctrl Pts',(2.06941053323759,6.44281220003543,18.7038932658662));
#52930=CARTESIAN_POINT('Ctrl Pts',(1.8923184589668,6.49969360406686,18.7126425753688));
#52931=CARTESIAN_POINT('Ctrl Pts',(1.7128799643151,6.54926929700879,18.7213918848714));
#52932=CARTESIAN_POINT('Ctrl Pts',(1.53170449173519,6.59137090065475,18.730141194374));
#52933=CARTESIAN_POINT('Ctrl Pts',(1.35053036178182,6.63347219230081,18.7388904390386));
#52934=CARTESIAN_POINT('Ctrl Pts',(1.16761955878853,6.66809944062453,18.7476396837032));
#52935=CARTESIAN_POINT('Ctrl Pts',(0.983593309310539,6.69513503985391,18.7563889283678));
#52936=CARTESIAN_POINT('Ctrl Pts',(0.79956836245995,6.72217044771215,18.765138111101));
#52937=CARTESIAN_POINT('Ctrl Pts',(0.614428268438478,6.74161427235978,18.7738872938341));
#52938=CARTESIAN_POINT('Ctrl Pts',(0.428801816330067,6.75340047696803,18.7826364765673));
#52939=CARTESIAN_POINT('Ctrl Pts',(0.243176616522471,6.76518660206243,18.7913856002754));
#52940=CARTESIAN_POINT('Ctrl Pts',(0.0570653511650372,6.76931519233997,
18.8001347239836));
#52941=CARTESIAN_POINT('Ctrl Pts',(-0.128899900800564,6.76577222610794,
18.8088838476917));
#52942=CARTESIAN_POINT('Ctrl Pts',(-0.314863959942471,6.76222928260131,
18.817632915281));
#52943=CARTESIAN_POINT('Ctrl Pts',(-0.500681721081045,6.75101488651274,
18.8263819828703));
#52944=CARTESIAN_POINT('Ctrl Pts',(-0.685722110173579,6.73216712415988,
18.8351310504595));
#52945=CARTESIAN_POINT('Ctrl Pts',(-0.870761373827823,6.71331947644142,
18.8438800648359));
#52946=CARTESIAN_POINT('Ctrl Pts',(-1.05502298984357,6.68683858439994,18.8526290792122));
#52947=CARTESIAN_POINT('Ctrl Pts',(-1.23788117676067,6.65281438131425,18.8613780935886));
#52948=CARTESIAN_POINT('Ctrl Pts',(-1.43009641451794,6.61704912302377,18.8705748044761));
#52949=CARTESIAN_POINT('Ctrl Pts',(-1.62076048992691,6.57294837083166,18.8797715153636));
#52950=CARTESIAN_POINT('Ctrl Pts',(-1.80915798961122,6.52067760042052,18.8889682262512));
#52951=CARTESIAN_POINT('Ctrl Pts',(-1.98840443002995,6.47094578577414,18.8977182239577));
#52952=CARTESIAN_POINT('Ctrl Pts',(-2.16559895952168,6.41381888474483,18.9064682216642));
#52953=CARTESIAN_POINT('Ctrl Pts',(-2.34013966242293,6.34949095285245,18.9152182193707));
#52954=CARTESIAN_POINT('Ctrl Pts',(-2.51467682553989,6.28516432556695,18.9239680396223));
#52955=CARTESIAN_POINT('Ctrl Pts',(-2.6865600007882,6.21363705879671,18.9327178598739));
#52956=CARTESIAN_POINT('Ctrl Pts',(-2.85520533840869,6.13515211510868,18.9414676801255));
#52957=CARTESIAN_POINT('Ctrl Pts',(-3.02384747998307,6.05666865881131,18.9502173345567));
#52958=CARTESIAN_POINT('Ctrl Pts',(-3.18925164684516,5.97122791039855,18.9589669889879));
#52959=CARTESIAN_POINT('Ctrl Pts',(-3.35085601829136,5.87912008251921,18.9677166434192));
#52960=CARTESIAN_POINT('Ctrl Pts',(-3.51245754191393,5.78701387778189,18.9764661436623));
#52961=CARTESIAN_POINT('Ctrl Pts',(-3.67025915510908,5.68824097061001,18.9852156439055));
#52962=CARTESIAN_POINT('Ctrl Pts',(-3.82372487928803,5.58313684656876,18.9939651441486));
#52963=CARTESIAN_POINT('Ctrl Pts',(-3.97718810300769,5.47803443501794,19.0027145018337));
#52964=CARTESIAN_POINT('Ctrl Pts',(-4.12631534262998,5.36660117496397,19.0114638595188));
#52965=CARTESIAN_POINT('Ctrl Pts',(-4.270600098862,5.24921554097371,19.020213217204));
#52966=CARTESIAN_POINT('Ctrl Pts',(-4.41488269594181,5.13183166360319,19.0289624439591));
#52967=CARTESIAN_POINT('Ctrl Pts',(-4.5543227323505,5.00849577139506,19.0377116707143));
#52968=CARTESIAN_POINT('Ctrl Pts',(-4.68844662480162,4.87962675277385,19.0464608974695));
#52969=CARTESIAN_POINT('Ctrl Pts',(-4.82256868835107,4.75075949139933,19.055210004921));
#52970=CARTESIAN_POINT('Ctrl Pts',(-4.95137454637806,4.61635945312585,19.0639591123725));
#52971=CARTESIAN_POINT('Ctrl Pts',(-5.07442674461018,4.47688309134659,19.072708219824));
#52972=CARTESIAN_POINT('Ctrl Pts',(-5.19747742838489,4.33740844616411,19.0814572195963));
#52973=CARTESIAN_POINT('Ctrl Pts',(-5.31477440450888,4.19285781736079,19.0902062193687));
#52974=CARTESIAN_POINT('Ctrl Pts',(-5.42591931531123,4.04372211999446,19.0989552191411));
#52975=CARTESIAN_POINT('Ctrl Pts',(-5.5370763646295,3.89457013500846,19.1077051744216));
#52976=CARTESIAN_POINT('Ctrl Pts',(-5.64207983273437,3.7408323091647,19.1164551297022));
#52977=CARTESIAN_POINT('Ctrl Pts',(-5.74057303468713,3.58303087251882,19.1252050849828));
#52978=CARTESIAN_POINT('Ctrl Pts',(-5.83906243363732,3.42523552887487,19.1339547024116));
#52979=CARTESIAN_POINT('Ctrl Pts',(-5.93104191768394,3.26337713157051,19.1427043198404));
#52980=CARTESIAN_POINT('Ctrl Pts',(-6.01619906699625,3.09800545291216,19.1514539372692));
#52981=CARTESIAN_POINT('Ctrl Pts',(-6.10135338095357,2.93263928039649,19.1602032633746));
#52982=CARTESIAN_POINT('Ctrl Pts',(-6.17968568352818,2.76376031540271,19.16895258948));
#52983=CARTESIAN_POINT('Ctrl Pts',(-6.2509299269487,2.59194213831582,19.1777019155854));
#52984=CARTESIAN_POINT('Ctrl Pts',(-6.32217217691088,2.42012876880862,19.1864509968792));
#52985=CARTESIAN_POINT('Ctrl Pts',(-6.38632665483835,2.24537661647713,19.195200078173));
#52986=CARTESIAN_POINT('Ctrl Pts',(-6.44317547869336,2.06827917621501,19.2039491594668));
#52987=CARTESIAN_POINT('Ctrl Pts',(-6.50002944235924,1.89116572423465,19.2126990317818));
#52988=CARTESIAN_POINT('Ctrl Pts',(-6.54957634250388,1.71170683289236,19.2214489040967));
#52989=CARTESIAN_POINT('Ctrl Pts',(-6.59164787708387,1.53051209225399,19.2301987764117));
#52990=CARTESIAN_POINT('Ctrl Pts',(-6.63371649075001,1.34932993148068,19.2389480412465));
#52991=CARTESIAN_POINT('Ctrl Pts',(-6.66831071257117,1.16641244174045,19.2476973060813));
#52992=CARTESIAN_POINT('Ctrl Pts',(-6.69531304840326,0.982380875160461,
19.2564465709161));
#52993=CARTESIAN_POINT('Ctrl Pts',(-6.72231677033039,0.798339861796263,
19.2651962848717));
#52994=CARTESIAN_POINT('Ctrl Pts',(-6.74172778477886,0.613184940730545,
19.2739459988274));
#52995=CARTESIAN_POINT('Ctrl Pts',(-6.75348015835516,0.427545027690915,
19.2826957127831));
#52996=CARTESIAN_POINT('Ctrl Pts',(-6.76249038365213,0.285219953548288,
19.2894038805853));
#52997=CARTESIAN_POINT('Ctrl Pts',(-6.76699999999993,0.142609995759882,
19.2961120483875));
#52998=CARTESIAN_POINT('Ctrl Pts',(-6.767,3.60156657358884E-12,19.3028202161898));
#52999=CARTESIAN_POINT('Ctrl Pts',(-6.7669973892787,-0.00594419845536852,
19.3028202161898));
#53000=CARTESIAN_POINT('Ctrl Pts',(-6.76678148696253,-0.251731821604794,
19.3144057968282));
#53001=CARTESIAN_POINT('Ctrl Pts',(-6.75317158476609,-0.496930574792495,
19.3259913774667));
#53002=CARTESIAN_POINT('Ctrl Pts',(-6.72637726539961,-0.740363345604933,
19.3375769581052));
#53003=CARTESIAN_POINT('Ctrl Pts',(-6.6982552193013,-0.995858829889866,
19.3497366337563));
#53004=CARTESIAN_POINT('Ctrl Pts',(-6.655609497569,-1.24940987343356,19.3618963094075));
#53005=CARTESIAN_POINT('Ctrl Pts',(-6.59872934408692,-1.49968664843233,
19.3740559850587));
#53006=CARTESIAN_POINT('Ctrl Pts',(-6.58649778794481,-1.55350637705577,
19.3766708119586));
#53007=CARTESIAN_POINT('Ctrl Pts',(-6.57360816990642,-1.60717477434293,
19.3792856388585));
#53008=CARTESIAN_POINT('Ctrl Pts',(-6.56006365577417,-1.66067872636184,
19.3819004657585));
#53009=CARTESIAN_POINT('Ctrl Pts',(-6.51825462790827,-1.8258340209005,19.3899718790005));
#53010=CARTESIAN_POINT('Ctrl Pts',(-6.47012764472255,-1.9897132384509,19.3980432922425));
#53011=CARTESIAN_POINT('Ctrl Pts',(-6.41577085801813,-2.15178374782535,
19.4061147054845));
#53012=CARTESIAN_POINT('Ctrl Pts',(-6.36148231175712,-2.31365079109937,
19.4141759857358));
#53013=CARTESIAN_POINT('Ctrl Pts',(-6.30097964085668,-2.47371329515649,
19.422237265987));
#53014=CARTESIAN_POINT('Ctrl Pts',(-6.23440205186282,-2.63144828102865,
19.4302985462383));
#53015=CARTESIAN_POINT('Ctrl Pts',(-6.16789344474438,-2.7890198357026,19.4383514740959));
#53016=CARTESIAN_POINT('Ctrl Pts',(-6.09532258917428,-2.94426833059145,
19.4464044019535));
#53017=CARTESIAN_POINT('Ctrl Pts',(-6.01687856773649,-3.09668553474732,
19.4544573298111));
#53018=CARTESIAN_POINT('Ctrl Pts',(-5.93849864569332,-3.24897819339498,
19.4625036773355));
#53019=CARTESIAN_POINT('Ctrl Pts',(-5.85425527957901,-3.39844383612653,
19.4705500248599));
#53020=CARTESIAN_POINT('Ctrl Pts',(-5.76438573185665,-3.54459393081457,
19.4785963723843));
#53021=CARTESIAN_POINT('Ctrl Pts',(-5.67456996091978,-3.69065657115916,
19.4866379050775));
#53022=CARTESIAN_POINT('Ctrl Pts',(-5.57913490524292,-3.83340729609017,
19.4946794377706));
#53023=CARTESIAN_POINT('Ctrl Pts',(-5.47836381126608,-3.9723820248574,19.5027209704638));
#53024=CARTESIAN_POINT('Ctrl Pts',(-5.37565541946049,-4.11402850630357,
19.510917099512));
#53025=CARTESIAN_POINT('Ctrl Pts',(-5.26740391589171,-4.25175197760208,
19.5191132285603));
#53026=CARTESIAN_POINT('Ctrl Pts',(-5.15395588504798,-4.38509153096937,
19.5273093576085));
#53027=CARTESIAN_POINT('Ctrl Pts',(-5.04268614684367,-4.51587085860614,
19.5353481144446));
#53028=CARTESIAN_POINT('Ctrl Pts',(-4.92641789533958,-4.64243281165157,
19.5433868712807));
#53029=CARTESIAN_POINT('Ctrl Pts',(-4.80551885472306,-4.76437588115182,
19.5514256281168));
#53030=CARTESIAN_POINT('Ctrl Pts',(-4.6846081123571,-4.88633075345248,19.5594651630196));
#53031=CARTESIAN_POINT('Ctrl Pts',(-4.55906595129381,-5.0036655867268,19.5675046979224));
#53032=CARTESIAN_POINT('Ctrl Pts',(-4.42929674974193,-5.11601595997565,
19.5755442328252));
#53033=CARTESIAN_POINT('Ctrl Pts',(-4.29948929355575,-5.22839945296625,
19.5835861377007));
#53034=CARTESIAN_POINT('Ctrl Pts',(-4.16545259877468,-5.33579531687339,
19.5916280425763));
#53035=CARTESIAN_POINT('Ctrl Pts',(-4.02762375514728,-5.43787972347434,
19.5996699474518));
#53036=CARTESIAN_POINT('Ctrl Pts',(-3.88514563006092,-5.54340767009469,
19.6079831241326));
#53037=CARTESIAN_POINT('Ctrl Pts',(-3.73861539616346,-5.64325929633916,
19.6162963008134));
#53038=CARTESIAN_POINT('Ctrl Pts',(-3.58854698120328,-5.73712642040393,
19.6246094774942));
#53039=CARTESIAN_POINT('Ctrl Pts',(-3.44312347706519,-5.82808817347159,
19.6326653451048));
#53040=CARTESIAN_POINT('Ctrl Pts',(-3.29437791185248,-5.91343024907903,
19.6407212127153));
#53041=CARTESIAN_POINT('Ctrl Pts',(-3.14280113920245,-5.99291998940648,
19.6487770803258));
#53042=CARTESIAN_POINT('Ctrl Pts',(-2.98396219188709,-6.07621815214766,
19.6572189115418));
#53043=CARTESIAN_POINT('Ctrl Pts',(-2.82201451069582,-6.1530891941694,19.6656607427577));
#53044=CARTESIAN_POINT('Ctrl Pts',(-2.65754349422894,-6.22332319394401,
19.6741025739737));
#53045=CARTESIAN_POINT('Ctrl Pts',(-2.49307247776206,-6.29355719371862,
19.6825444051897));
#53046=CARTESIAN_POINT('Ctrl Pts',(-2.32607858739046,-6.35715406711887,
19.6909862364056));
#53047=CARTESIAN_POINT('Ctrl Pts',(-2.15716150908466,-6.41396470396615,
19.6994280676216));
#53048=CARTESIAN_POINT('Ctrl Pts',(-1.99247394825558,-6.46935285835151,
19.7076585236881));
#53049=CARTESIAN_POINT('Ctrl Pts',(-1.82541072593333,-6.51847512866971,
19.7158889797547));
#53050=CARTESIAN_POINT('Ctrl Pts',(-1.65648915888423,-6.56112282056197,
19.7241194358212));
#53051=CARTESIAN_POINT('Ctrl Pts',(-1.48776811168905,-6.6037198871309,19.7323401218515));
#53052=CARTESIAN_POINT('Ctrl Pts',(-1.31719345653477,-6.63985759232926,
19.7405608078817));
#53053=CARTESIAN_POINT('Ctrl Pts',(-1.1453007104705,-6.66937592902033,19.7487814939119));
#53054=CARTESIAN_POINT('Ctrl Pts',(-0.973577524222988,-6.69886514799774,
19.7569940708273));
#53055=CARTESIAN_POINT('Ctrl Pts',(-0.800539187322688,-6.72174794169361,
19.7652066477426));
#53056=CARTESIAN_POINT('Ctrl Pts',(-0.62673463512712,-6.73791456588254,
19.773419224658));
#53057=CARTESIAN_POINT('Ctrl Pts',(-0.453066670565052,-6.75406848522046,
19.7816253475626));
#53058=CARTESIAN_POINT('Ctrl Pts',(-0.278634045422089,-6.76351671465871,
19.7898314704673));
#53059=CARTESIAN_POINT('Ctrl Pts',(-0.103994198741046,-6.7662008695152,
19.7980375933719));
#53060=CARTESIAN_POINT('Ctrl Pts',(0.0705434204438084,-6.76888345316995,
19.8062389127257));
#53061=CARTESIAN_POINT('Ctrl Pts',(0.245287662004282,-6.76480984439387,
19.8144402320794));
#53062=CARTESIAN_POINT('Ctrl Pts',(0.419677582265115,-6.75397362498138,
19.8226415514331));
#53063=CARTESIAN_POINT('Ctrl Pts',(0.594017474189871,-6.74314051422348,
19.8308405180226));
#53064=CARTESIAN_POINT('Ctrl Pts',(0.768002889656946,-6.72554867539881,
19.8390394846121));
#53065=CARTESIAN_POINT('Ctrl Pts',(0.941074250497254,-6.70124378418298,
19.8472384512016));
#53066=CARTESIAN_POINT('Ctrl Pts',(1.11412275648244,-6.67694210253784,19.8554363350806));
#53067=CARTESIAN_POINT('Ctrl Pts',(1.28625709310994,-6.64592918310876,19.8636342189595));
#53068=CARTESIAN_POINT('Ctrl Pts',(1.45692414916047,-6.60830243130511,19.8718321028384));
#53069=CARTESIAN_POINT('Ctrl Pts',(1.62759967001688,-6.57067381327633,19.8800303933189));
#53070=CARTESIAN_POINT('Ctrl Pts',(1.79680741507235,-6.52643078652049,19.8882286837995));
#53071=CARTESIAN_POINT('Ctrl Pts',(1.96400573537052,-6.47572161781463,19.89642697428));
#53072=CARTESIAN_POINT('Ctrl Pts',(2.13124272040526,-6.4250007225756,19.9046271606213));
#53073=CARTESIAN_POINT('Ctrl Pts',(2.29646901206936,-6.3678108112492,19.9128273469627));
#53074=CARTESIAN_POINT('Ctrl Pts',(2.45915930736879,-6.30434964932795,19.921027533304));
#53075=CARTESIAN_POINT('Ctrl Pts',(2.62200341357712,-6.24082848985751,19.9292354722781));
#53076=CARTESIAN_POINT('Ctrl Pts',(2.78230639878598,-6.17102436484951,19.9374434112522));
#53077=CARTESIAN_POINT('Ctrl Pts',(2.9395632294928,-6.09518309977755,19.9456513502263));
#53078=CARTESIAN_POINT('Ctrl Pts',(3.09689635025264,-6.01930504181013,19.9538632711202));
#53079=CARTESIAN_POINT('Ctrl Pts',(3.25118005362063,-5.93738417250636,19.9620751920142));
#53080=CARTESIAN_POINT('Ctrl Pts',(3.40193510144856,-5.84971166516198,19.9702871129082));
#53081=CARTESIAN_POINT('Ctrl Pts',(3.55289688594214,-5.76191892886277,19.9785102951507));
#53082=CARTESIAN_POINT('Ctrl Pts',(3.70032004145717,-5.66835898383597,19.9867334773933));
#53083=CARTESIAN_POINT('Ctrl Pts',(3.8437544341694,-5.56936628799032,19.9949566596358));
#53084=CARTESIAN_POINT('Ctrl Pts',(3.97166171405434,-5.48108978599754,20.0022896629187));
#53085=CARTESIAN_POINT('Ctrl Pts',(4.09639737778694,-5.38849378016287,20.0096226662017));
#53086=CARTESIAN_POINT('Ctrl Pts',(4.21766570116052,-5.29184136508779,20.0169556694846));
#53087=CARTESIAN_POINT('Ctrl Pts',(4.36542986794342,-5.17407142167784,20.0258908562669));
#53088=CARTESIAN_POINT('Ctrl Pts',(4.50835245263275,-5.05003426305525,20.0348260430492));
#53089=CARTESIAN_POINT('Ctrl Pts',(4.64591986172555,-4.92013390452171,20.0437612298314));
#53090=CARTESIAN_POINT('Ctrl Pts',(4.78328123739679,-4.79042809653985,20.0526830344681));
#53091=CARTESIAN_POINT('Ctrl Pts',(4.91530325354397,-4.65487678725042,20.0616048391047));
#53092=CARTESIAN_POINT('Ctrl Pts',(5.04150607776926,-4.51392351151585,20.0705266437414));
#53093=CARTESIAN_POINT('Ctrl Pts',(5.16740106337686,-4.37331405424833,20.0794266859806));
#53094=CARTESIAN_POINT('Ctrl Pts',(5.28750501464005,-4.2273291210464,20.0883267282199));
#53095=CARTESIAN_POINT('Ctrl Pts',(5.40137598380592,-4.07644777736262,20.0972267704592));
#53096=CARTESIAN_POINT('Ctrl Pts',(5.51507164694044,-3.92579871772594,20.1061131109526));
#53097=CARTESIAN_POINT('Ctrl Pts',(5.62255331420112,-3.77026848932627,20.114999451446));
#53098=CARTESIAN_POINT('Ctrl Pts',(5.72341829897401,-3.61037006066823,20.1238857919394));
#53099=CARTESIAN_POINT('Ctrl Pts',(5.82402538958749,-3.45088046438092,20.1327494116114));
#53100=CARTESIAN_POINT('Ctrl Pts',(5.91804941852547,-3.28704517217004,20.1416130312833));
#53101=CARTESIAN_POINT('Ctrl Pts',(6.00513053934645,-3.11940638670382,20.1504766509552));
#53102=CARTESIAN_POINT('Ctrl Pts',(6.08779703048986,-2.96026615006718,20.1588909241088));
#53103=CARTESIAN_POINT('Ctrl Pts',(6.16420688657542,-2.79769867385645,20.1673051972624));
#53104=CARTESIAN_POINT('Ctrl Pts',(6.23408762025623,-2.63219310518208,20.175719470416));
#53105=CARTESIAN_POINT('Ctrl Pts',(6.30227392200353,-2.47070063004526,20.1839297186205));
#53106=CARTESIAN_POINT('Ctrl Pts',(6.36417742337436,-2.30656562611901,20.192139966825));
#53107=CARTESIAN_POINT('Ctrl Pts',(6.41960476151267,-2.14031859917254,20.2003502150296));
#53108=CARTESIAN_POINT('Ctrl Pts',(6.47504527583429,-1.97403205199336,20.2085624149738));
#53109=CARTESIAN_POINT('Ctrl Pts',(6.52400644718736,-1.8056328192079,20.216774614918));
#53110=CARTESIAN_POINT('Ctrl Pts',(6.56634474621996,-1.63566673677421,20.2249868148623));
#53111=CARTESIAN_POINT('Ctrl Pts',(6.60870064917459,-1.46562998381924,20.2332024293727));
#53112=CARTESIAN_POINT('Ctrl Pts',(6.6444281077952,-1.29402542842772,20.2414180438832));
#53113=CARTESIAN_POINT('Ctrl Pts',(6.67343465260615,-1.12140935317816,20.2496336583937));
#53114=CARTESIAN_POINT('Ctrl Pts',(6.70247377049535,-0.94859943764315,20.2578584986791));
#53115=CARTESIAN_POINT('Ctrl Pts',(6.72477684118185,-0.774776084664146,
20.2660833389645));
#53116=CARTESIAN_POINT('Ctrl Pts',(6.74030314047907,-0.600501935424053,
20.27430817925));
#53117=CARTESIAN_POINT('Ctrl Pts',(6.75583938491071,-0.426116157533253,
20.2825382878315));
#53118=CARTESIAN_POINT('Ctrl Pts',(6.76459018712003,-0.251279362352467,
20.2907683964131));
#53119=CARTESIAN_POINT('Ctrl Pts',(6.76656695989601,-0.0765544070821397,
20.2989985049946));
#53120=CARTESIAN_POINT('Ctrl Pts',(6.7685464428578,0.0984100987830904,20.3072398971813));
#53121=CARTESIAN_POINT('Ctrl Pts',(6.76373335575344,0.273262103706231,20.315481289368));
#53122=CARTESIAN_POINT('Ctrl Pts',(6.75219105778701,0.447442643409409,20.3237226815547));
#53123=CARTESIAN_POINT('Ctrl Pts',(6.747167556463,0.523250439600418,20.327309544819));
#53124=CARTESIAN_POINT('Ctrl Pts',(6.74087005937798,0.598931157170586,20.3308964080833));
#53125=CARTESIAN_POINT('Ctrl Pts',(6.73330680843956,0.674439340060628,20.3344832713476));
#53126=CARTESIAN_POINT('Ctrl Pts',(6.71549231908453,0.852291394853806,20.3429317729193));
#53127=CARTESIAN_POINT('Ctrl Pts',(6.69061148799602,1.02959114221899,20.351380274491));
#53128=CARTESIAN_POINT('Ctrl Pts',(6.65871202097412,1.20575421282065,20.3598287760627));
#53129=CARTESIAN_POINT('Ctrl Pts',(6.62684169745718,1.38175634000225,20.3682695590431));
#53130=CARTESIAN_POINT('Ctrl Pts',(6.58796557872047,1.55662353387428,20.3767103420235));
#53131=CARTESIAN_POINT('Ctrl Pts',(6.54218306238557,1.72977737822977,20.3851511250039));
#53132=CARTESIAN_POINT('Ctrl Pts',(6.49643533279525,1.9027996557986,20.3935854944582));
#53133=CARTESIAN_POINT('Ctrl Pts',(6.44379175181674,2.07411085786092,20.4020198639125));
#53134=CARTESIAN_POINT('Ctrl Pts',(6.38440268310488,2.24314319203283,20.4104542333669));
#53135=CARTESIAN_POINT('Ctrl Pts',(6.3250496194929,2.41207304899458,20.418883489417));
#53136=CARTESIAN_POINT('Ctrl Pts',(6.2589593318243,2.57872647876713,20.4273127454671));
#53137=CARTESIAN_POINT('Ctrl Pts',(6.18633199707147,2.74255089688591,20.4357420015173));
#53138=CARTESIAN_POINT('Ctrl Pts',(6.11373755238869,2.90630112535411,20.4441674402881));
#53139=CARTESIAN_POINT('Ctrl Pts',(6.03461209856751,3.06722459248032,20.4525928790589));
#53140=CARTESIAN_POINT('Ctrl Pts',(5.94920405625126,3.22478838020165,20.4610183178298));
#53141=CARTESIAN_POINT('Ctrl Pts',(5.86381485763857,3.38231740438986,20.4694418976835));
#53142=CARTESIAN_POINT('Ctrl Pts',(5.77214599069726,3.53648793298379,20.4778654775372));
#53143=CARTESIAN_POINT('Ctrl Pts',(5.67449221830271,3.68679088970639,20.4862890573909));
#53144=CARTESIAN_POINT('Ctrl Pts',(5.57684939438853,3.83707699517039,20.4947116928326));
#53145=CARTESIAN_POINT('Ctrl Pts',(5.47322318431893,3.98349611368803,20.5031343282742));
#53146=CARTESIAN_POINT('Ctrl Pts',(5.36395231130543,4.12556718549597,20.5115569637159));
#53147=CARTESIAN_POINT('Ctrl Pts',(5.25467845185882,4.26764214018452,20.5199798293529));
#53148=CARTESIAN_POINT('Ctrl Pts',(5.13975982546946,4.40536854721088,20.5284026949898));
#53149=CARTESIAN_POINT('Ctrl Pts',(5.01957638258124,4.53829725111001,20.5368255606267));
#53150=CARTESIAN_POINT('Ctrl Pts',(4.89937289493421,4.67124812548241,20.5452498310687));
#53151=CARTESIAN_POINT('Ctrl Pts',(4.77390306415786,4.79939945453999,20.5536741015108));
#53152=CARTESIAN_POINT('Ctrl Pts',(4.64358498523711,4.92233760370827,20.5620983719528));
#53153=CARTESIAN_POINT('Ctrl Pts',(4.51317933547137,5.04535836457321,20.5705283033168));
#53154=CARTESIAN_POINT('Ctrl Pts',(4.37791917034344,5.16315871655745,20.5789582346808));
#53155=CARTESIAN_POINT('Ctrl Pts',(4.23825782685266,5.27536345602103,20.5873881660448));
#53156=CARTESIAN_POINT('Ctrl Pts',(4.09854656058211,5.38760830373761,20.595821110738));
#53157=CARTESIAN_POINT('Ctrl Pts',(3.95443124273722,5.49425334666627,20.6042540554313));
#53158=CARTESIAN_POINT('Ctrl Pts',(3.80639616587544,5.59496534648864,20.6126870001245));
#53159=CARTESIAN_POINT('Ctrl Pts',(3.65822600690346,5.69576924608063,20.6211276398856));
#53160=CARTESIAN_POINT('Ctrl Pts',(3.50612922199424,5.79062910351373,20.6295682796468));
#53161=CARTESIAN_POINT('Ctrl Pts',(3.3506177196932,5.87925589649557,20.6380089194079));
#53162=CARTESIAN_POINT('Ctrl Pts',(3.26771690240264,5.92650149224458,20.6425084961228));
#53163=CARTESIAN_POINT('Ctrl Pts',(3.18384611222608,5.97197655998786,20.6470080728376));
#53164=CARTESIAN_POINT('Ctrl Pts',(3.09908550384707,6.0156427786102,20.6515076495525));
#53165=CARTESIAN_POINT('Origin',(0.,0.,-63.6971797838103));
#53166=CARTESIAN_POINT('',(3.09908550384706,6.0156427786102,23.0456261631097));
#53167=CARTESIAN_POINT('',(3.09908550384738,6.01564277861003,22.6514909292461));
#53168=CARTESIAN_POINT('',(3.09908550384721,6.01564277861012,-63.6971797838103));
#53169=CARTESIAN_POINT('',(-6.76699855717881,0.00441895236067136,21.6971797837833));
#53170=CARTESIAN_POINT('Ctrl Pts',(-6.76699855717918,0.00441895179320035,
21.6971797838099));
#53171=CARTESIAN_POINT('Ctrl Pts',(-6.76711125264251,-0.168158182668951,
21.7052796560254));
#53172=CARTESIAN_POINT('Ctrl Pts',(-6.76061791801425,-0.340884502066218,
21.7133795282409));
#53173=CARTESIAN_POINT('Ctrl Pts',(-6.7475109834384,-0.513210023653212,
21.7214794004565));
#53174=CARTESIAN_POINT('Ctrl Pts',(-6.73864096822721,-0.62982996929403,
21.7269609254725));
#53175=CARTESIAN_POINT('Ctrl Pts',(-6.72674313303695,-0.74626625523307,
21.7324424504885));
#53176=CARTESIAN_POINT('Ctrl Pts',(-6.71182868254392,-0.862348384459978,
21.7379239755045));
#53177=CARTESIAN_POINT('Ctrl Pts',(-6.68948976408141,-1.03621662190972,
21.746134223709));
#53178=CARTESIAN_POINT('Ctrl Pts',(-6.66039171995952,-1.20920693037894,
21.7543444719136));
#53179=CARTESIAN_POINT('Ctrl Pts',(-6.62463440377626,-1.38076356278109,
21.7625547201181));
#53180=CARTESIAN_POINT('Ctrl Pts',(-6.58886858736612,-1.55236097761478,
21.7707669200624));
#53181=CARTESIAN_POINT('Ctrl Pts',(-6.5464404176516,-1.72252368891705,21.7789791200066));
#53182=CARTESIAN_POINT('Ctrl Pts',(-6.49750052696888,-1.89070777806598,
21.7871913199508));
#53183=CARTESIAN_POINT('Ctrl Pts',(-6.44854028747589,-2.05896179679732,
21.7954069344613));
#53184=CARTESIAN_POINT('Ctrl Pts',(-6.39306303241003,-2.22523521289516,
21.8036225489718));
#53185=CARTESIAN_POINT('Ctrl Pts',(-6.33126877521517,-2.38900077354223,
21.8118381634822));
#53186=CARTESIAN_POINT('Ctrl Pts',(-6.26940512577825,-2.5529502357352,21.8200630037677));
#53187=CARTESIAN_POINT('Ctrl Pts',(-6.20121043147482,-2.71438588443705,
21.8282878440531));
#53188=CARTESIAN_POINT('Ctrl Pts',(-6.12693262206969,-2.87280101027173,
21.8365126843385));
#53189=CARTESIAN_POINT('Ctrl Pts',(-6.05260723514554,-3.03131760650144,
21.8447427929201));
#53190=CARTESIAN_POINT('Ctrl Pts',(-5.97219112883533,-3.18680950768719,
21.8529729015016));
#53191=CARTESIAN_POINT('Ctrl Pts',(-5.88597739674428,-3.3387960532227,21.8612030100832));
#53192=CARTESIAN_POINT('Ctrl Pts',(-5.79964546430348,-3.49099097464454,
21.8694444022699));
#53193=CARTESIAN_POINT('Ctrl Pts',(-5.70750021648081,-3.63967063948447,
21.8776857944566));
#53194=CARTESIAN_POINT('Ctrl Pts',(-5.60987767841737,-3.78438389083276,
21.8859271866433));
#53195=CARTESIAN_POINT('Ctrl Pts',(-5.56738986960998,-3.8473667744696,21.8895140499075));
#53196=CARTESIAN_POINT('Ctrl Pts',(-5.52386505985673,-3.90959876316506,
21.8931009131717));
#53197=CARTESIAN_POINT('Ctrl Pts',(-5.47933324514882,-3.97104472256444,
21.8966877764359));
#53198=CARTESIAN_POINT('Ctrl Pts',(-5.3744430448401,-4.11577448558528,21.9051362712643));
#53199=CARTESIAN_POINT('Ctrl Pts',(-5.2637242651968,-4.25647116895907,21.9135847660927));
#53200=CARTESIAN_POINT('Ctrl Pts',(-5.14751218724185,-4.39265378583342,
21.9220332609211));
#53201=CARTESIAN_POINT('Ctrl Pts',(-5.03140626226963,-4.52871200779777,
21.9304740385403));
#53202=CARTESIAN_POINT('Ctrl Pts',(-4.90981725641308,-4.6602641298948,21.9389148161594));
#53203=CARTESIAN_POINT('Ctrl Pts',(-4.78312212557501,-4.78686032090292,
21.9473555937786));
#53204=CARTESIAN_POINT('Ctrl Pts',(-4.65652324039093,-4.91336034141801,
21.9557899592479));
#53205=CARTESIAN_POINT('Ctrl Pts',(-4.52482619797284,-5.03491170122852,
21.9642243247172));
#53206=CARTESIAN_POINT('Ctrl Pts',(-4.38844665165136,-5.1510993958193,21.9726586901865));
#53207=CARTESIAN_POINT('Ctrl Pts',(-4.25214976438765,-5.267216669547,21.9810879436231));
#53208=CARTESIAN_POINT('Ctrl Pts',(-4.11117628473948,-5.37797654378555,
21.9895171970597));
#53209=CARTESIAN_POINT('Ctrl Pts',(-3.96597726064723,-5.48300222214337,
21.9979464504963));
#53210=CARTESIAN_POINT('Ctrl Pts',(-3.82084396795233,-5.58798035552188,
22.0063718880216));
#53211=CARTESIAN_POINT('Ctrl Pts',(-3.67148921488254,-5.68722927411314,
22.0147973255468));
#53212=CARTESIAN_POINT('Ctrl Pts',(-3.51839584407446,-5.78041345272114,
22.023222763072));
#53213=CARTESIAN_POINT('Ctrl Pts',(-3.36533610376296,-5.87357716127102,
22.0316463497552));
#53214=CARTESIAN_POINT('Ctrl Pts',(-3.20853966636499,-5.96067861065335,
22.0400699364384));
#53215=CARTESIAN_POINT('Ctrl Pts',(-3.048517426255,-6.04142619766389,22.0484935231216));
#53216=CARTESIAN_POINT('Ctrl Pts',(-2.88851309179476,-6.12216474944278,
22.0569161672495));
#53217=CARTESIAN_POINT('Ctrl Pts',(-2.72528397179574,-6.19655070603551,
22.0653388113776));
#53218=CARTESIAN_POINT('Ctrl Pts',(-2.55936485224373,-6.26433879616192,
22.0737614555055));
#53219=CARTESIAN_POINT('Ctrl Pts',(-2.39344116142092,-6.33212875393156,
22.0821843316875));
#53220=CARTESIAN_POINT('Ctrl Pts',(-2.22482763206665,-6.39332035708,22.0906072078694));
#53221=CARTESIAN_POINT('Ctrl Pts',(-2.05407862358452,-6.4477166507325,22.0990300840514));
#53222=CARTESIAN_POINT('Ctrl Pts',(-1.88330109907076,-6.50212202886781,
22.1074543669004));
#53223=CARTESIAN_POINT('Ctrl Pts',(-1.71038770221262,-6.54972973433226,
22.1158786497494));
#53224=CARTESIAN_POINT('Ctrl Pts',(-1.53590788198711,-6.59039270287059,
22.1243029325984));
#53225=CARTESIAN_POINT('Ctrl Pts',(-1.36131022454225,-6.63108313367439,
22.1327329048965));
#53226=CARTESIAN_POINT('Ctrl Pts',(-1.18514435482528,-6.66481937969628,
22.1411628771946));
#53227=CARTESIAN_POINT('Ctrl Pts',(-1.0079908442802,-6.69150532076657,22.1495928494928));
#53228=CARTESIAN_POINT('Ctrl Pts',(-0.83077400421468,-6.71820080163004,
22.1580258353699));
#53229=CARTESIAN_POINT('Ctrl Pts',(-0.652569149889286,-6.73784090846588,
22.1664588212471));
#53230=CARTESIAN_POINT('Ctrl Pts',(-0.473962486645386,-6.7503813641344,
22.1748918071243));
#53231=CARTESIAN_POINT('Ctrl Pts',(-0.295191506358986,-6.76293335694576,
22.1833325512971));
#53232=CARTESIAN_POINT('Ctrl Pts',(-0.116018311720531,-6.76837263141582,
22.1917732954699));
#53233=CARTESIAN_POINT('Ctrl Pts',(0.0629692635081873,-6.76670701832533,
22.2002140396427));
#53234=CARTESIAN_POINT('Ctrl Pts',(0.161936274185537,-6.76578605636302,
22.2048811525281));
#53235=CARTESIAN_POINT('Ctrl Pts',(0.260846564772378,-6.76269385613586,
22.2095482654135));
#53236=CARTESIAN_POINT('Ctrl Pts',(0.359601331876994,-6.75743855925545,
22.2142153782989));
#53237=CARTESIAN_POINT('Ctrl Pts',(0.531870321990595,-6.74827115688209,
22.2223567455168));
#53238=CARTESIAN_POINT('Ctrl Pts',(0.704008070814728,-6.73250022156963,
22.2304981127347));
#53239=CARTESIAN_POINT('Ctrl Pts',(0.875464168136037,-6.71013051216665,
22.2386394799526));
#53240=CARTESIAN_POINT('Ctrl Pts',(1.04677059732388,-6.68778032981873,22.246773740376));
#53241=CARTESIAN_POINT('Ctrl Pts',(1.21739619892367,-6.65884288622386,22.2549080007994));
#53242=CARTESIAN_POINT('Ctrl Pts',(1.38679251798085,-6.62337493367787,22.2630422612229));
#53243=CARTESIAN_POINT('Ctrl Pts',(1.55607328098818,-6.58793117608792,22.2711709727477));
#53244=CARTESIAN_POINT('Ctrl Pts',(1.72412607420585,-6.54596585377698,22.2792996842726));
#53245=CARTESIAN_POINT('Ctrl Pts',(1.89040954964891,-6.49758730103692,22.2874283957974));
#53246=CARTESIAN_POINT('Ctrl Pts',(2.05661372757562,-6.44923181913457,22.2955532308899));
#53247=CARTESIAN_POINT('Ctrl Pts',(2.22104991720915,-6.39446929909738,22.3036780659824));
#53248=CARTESIAN_POINT('Ctrl Pts',(2.38318893864969,-6.33345872984878,22.311802901075));
#53249=CARTESIAN_POINT('Ctrl Pts',(2.54528256881695,-6.27246524067997,22.3199254615971));
#53250=CARTESIAN_POINT('Ctrl Pts',(2.7050799697127,-6.20522731586441,22.3280480221193));
#53251=CARTESIAN_POINT('Ctrl Pts',(2.86206908450194,-6.13195315992696,22.3361705826415));
#53252=CARTESIAN_POINT('Ctrl Pts',(3.01906654285522,-6.05867510965829,22.3442935748566));
#53253=CARTESIAN_POINT('Ctrl Pts',(3.17325508357313,-5.97936033865593,22.3524165670719));
#53254=CARTESIAN_POINT('Ctrl Pts',(3.32414435746671,-5.89426444017591,22.360539559287));
#53255=CARTESIAN_POINT('Ctrl Pts',(3.40116873350251,-5.85082557726341,22.3646860992681));
#53256=CARTESIAN_POINT('Ctrl Pts',(3.47733377062505,-5.80588101977382,22.3688326392492));
#53257=CARTESIAN_POINT('Ctrl Pts',(3.55257685114073,-5.75946930860292,22.3729791792303));
#53258=CARTESIAN_POINT('Ctrl Pts',(3.71559425424743,-5.65891631985014,22.3819628382587));
#53259=CARTESIAN_POINT('Ctrl Pts',(3.8742018412101,-5.55152394140958,22.3909464972871));
#53260=CARTESIAN_POINT('Ctrl Pts',(4.02786701279647,-5.43769954366974,22.3999301563154));
#53261=CARTESIAN_POINT('Ctrl Pts',(4.18179617951964,-5.32367959682047,22.4089292491748));
#53262=CARTESIAN_POINT('Ctrl Pts',(4.33076576751449,-5.20320568691012,22.4179283420343));
#53263=CARTESIAN_POINT('Ctrl Pts',(4.47427632467089,-5.07672535897793,22.4269274348937));
#53264=CARTESIAN_POINT('Ctrl Pts',(4.61812337397992,-4.94994847002155,22.435947628111));
#53265=CARTESIAN_POINT('Ctrl Pts',(4.75648560198327,-4.81713714346964,22.4449678213284));
#53266=CARTESIAN_POINT('Ctrl Pts',(4.88889853712001,-4.67877762815736,22.4539880145458));
#53267=CARTESIAN_POINT('Ctrl Pts',(5.0214455735105,-4.54027798918985,22.4630173429675));
#53268=CARTESIAN_POINT('Ctrl Pts',(5.14803111943441,-4.39621911301956,22.4720466713892));
#53269=CARTESIAN_POINT('Ctrl Pts',(5.26823008096148,-4.24712147389883,22.4810759998109));
#53270=CARTESIAN_POINT('Ctrl Pts',(5.38859849879596,-4.09781363716036,22.4901180577656));
#53271=CARTESIAN_POINT('Ctrl Pts',(5.50256217887023,-3.9434530199379,22.4991601157204));
#53272=CARTESIAN_POINT('Ctrl Pts',(5.60973717586073,-3.78459216003073,22.5082021736752));
#53273=CARTESIAN_POINT('Ctrl Pts',(5.70274645453809,-3.64672853133999,22.5160491091708));
#53274=CARTESIAN_POINT('Ctrl Pts',(5.79064364718261,-3.50547621488624,22.5238960446664));
#53275=CARTESIAN_POINT('Ctrl Pts',(5.87320508241612,-3.36121273648091,22.5317429801621));
#53276=CARTESIAN_POINT('Ctrl Pts',(5.96425240054603,-3.20212147582456,22.5403964444629));
#53277=CARTESIAN_POINT('Ctrl Pts',(6.0488898332124,-3.03922735851312,22.5490499087637));
#53278=CARTESIAN_POINT('Ctrl Pts',(6.12680981952343,-2.87306290139831,22.5577033730645));
#53279=CARTESIAN_POINT('Ctrl Pts',(6.20465802558881,-2.70705151573687,22.5663488657547));
#53280=CARTESIAN_POINT('Ctrl Pts',(6.27580099908149,-2.5377760733746,22.5749943584448));
#53281=CARTESIAN_POINT('Ctrl Pts',(6.33997713483556,-2.36579350953593,22.5836398511349));
#53282=CARTESIAN_POINT('Ctrl Pts',(6.40608389946652,-2.18863714549616,22.5925454286315));
#53283=CARTESIAN_POINT('Ctrl Pts',(6.46479793954806,-2.0086085148415,22.601451006128));
#53284=CARTESIAN_POINT('Ctrl Pts',(6.51588589123277,-1.82634061785687,22.6103565836246));
#53285=CARTESIAN_POINT('Ctrl Pts',(6.56538772756097,-1.64973154846018,22.6189856717971));
#53286=CARTESIAN_POINT('Ctrl Pts',(6.60772980164938,-1.47102048869803,22.6276147599697));
#53287=CARTESIAN_POINT('Ctrl Pts',(6.64274954482154,-1.29080110194142,22.6362438481422));
#53288=CARTESIAN_POINT('Ctrl Pts',(6.67945241805147,-1.10191995357932,22.6452876703008));
#53289=CARTESIAN_POINT('Ctrl Pts',(6.70811163163842,-0.911382232976675,
22.6543314924593));
#53290=CARTESIAN_POINT('Ctrl Pts',(6.72859955155919,-0.719886848579347,
22.6633753146178));
#53291=CARTESIAN_POINT('Ctrl Pts',(6.74908747147996,-0.528391464182019,
22.6724191367763));
#53292=CARTESIAN_POINT('Ctrl Pts',(6.76140402230401,-0.335938795437292,
22.6814629589349));
#53293=CARTESIAN_POINT('Ctrl Pts',(6.76548386034245,-0.143238037705902,
22.6905067810934));
#53294=CARTESIAN_POINT('Ctrl Pts',(6.76928489239844,0.0362940296087281,
22.6989325709432));
#53295=CARTESIAN_POINT('Ctrl Pts',(6.76593505134287,0.215962810871053,22.7073583607931));
#53296=CARTESIAN_POINT('Ctrl Pts',(6.75545136976293,0.395178175976516,22.7157841506429));
#53297=CARTESIAN_POINT('Ctrl Pts',(6.7449652556162,0.574435125075533,22.7242118955594));
#53298=CARTESIAN_POINT('Ctrl Pts',(6.72734201989472,0.753238117308931,22.732639640476));
#53299=CARTESIAN_POINT('Ctrl Pts',(6.70265067643537,0.931001025606562,22.7410673853925));
#53300=CARTESIAN_POINT('Ctrl Pts',(6.67795026014629,1.10882925285302,22.7494982270824));
#53301=CARTESIAN_POINT('Ctrl Pts',(6.64617660317425,1.28561630593951,22.7579290687723));
#53302=CARTESIAN_POINT('Ctrl Pts',(6.60745010600319,1.46078475371237,22.7663599104622));
#53303=CARTESIAN_POINT('Ctrl Pts',(6.568688024124,1.63611415893148,22.7747984990195));
#53304=CARTESIAN_POINT('Ctrl Pts',(6.52296040949227,1.80982166345399,22.7832370875769));
#53305=CARTESIAN_POINT('Ctrl Pts',(6.47043824649797,1.98134244850713,22.7916756761342));
#53306=CARTESIAN_POINT('Ctrl Pts',(6.41788854320256,2.15295317147983,22.8001186895145));
#53307=CARTESIAN_POINT('Ctrl Pts',(6.35853729042603,2.322374573866,22.8085617028947));
#53308=CARTESIAN_POINT('Ctrl Pts',(6.29260438710844,2.48905986817183,22.8170047162749));
#53309=CARTESIAN_POINT('Ctrl Pts',(6.22660221668023,2.65592027699772,22.8254565996292));
#53310=CARTESIAN_POINT('Ctrl Pts',(6.15400471257011,2.82003853073858,22.8339084829835));
#53311=CARTESIAN_POINT('Ctrl Pts',(6.07507911003739,2.98088959989922,22.8423603663378));
#53312=CARTESIAN_POINT('Ctrl Pts',(6.05356938990043,3.0247265979119,22.8446637715669));
#53313=CARTESIAN_POINT('Ctrl Pts',(6.03158991932571,3.06832107925754,22.846967176796));
#53314=CARTESIAN_POINT('Ctrl Pts',(6.00914668281669,3.1116627619961,22.8492705820251));
#53315=CARTESIAN_POINT('Ctrl Pts',(5.92811450439602,3.26814959344361,22.8575871162033));
#53316=CARTESIAN_POINT('Ctrl Pts',(5.84088749743472,3.42162030783587,22.8659036503815));
#53317=CARTESIAN_POINT('Ctrl Pts',(5.74771588976992,3.57156143031118,22.8742201845597));
#53318=CARTESIAN_POINT('Ctrl Pts',(5.6546185525653,3.72138302929165,22.8825300893276));
#53319=CARTESIAN_POINT('Ctrl Pts',(5.55558623646763,3.86768034702241,22.8908399940955));
#53320=CARTESIAN_POINT('Ctrl Pts',(5.4509152148054,4.00996412964044,22.8991498988634));
#53321=CARTESIAN_POINT('Ctrl Pts',(5.34631024165017,4.15215812970679,22.9074545599946));
#53322=CARTESIAN_POINT('Ctrl Pts',(5.23607385703312,4.29034336107764,22.9157592211258));
#53323=CARTESIAN_POINT('Ctrl Pts',(5.12054591546747,4.4240590556173,22.924063882257));
#53324=CARTESIAN_POINT('Ctrl Pts',(5.00507168780598,4.55771257998494,22.9323646821945));
#53325=CARTESIAN_POINT('Ctrl Pts',(4.88431103272458,4.68690044587856,22.9406654821319));
#53326=CARTESIAN_POINT('Ctrl Pts',(4.75864451946989,4.81119437742015,22.9489662820693));
#53327=CARTESIAN_POINT('Ctrl Pts',(4.63300123370041,4.93546533517674,22.957265547734));
#53328=CARTESIAN_POINT('Ctrl Pts',(4.50245414028907,5.05484391326157,22.9655648133987));
#53329=CARTESIAN_POINT('Ctrl Pts',(4.36742142712399,5.16893790617553,22.9738640790634));
#53330=CARTESIAN_POINT('Ctrl Pts',(4.23240744198006,5.28301607511126,22.9821621936824));
#53331=CARTESIAN_POINT('Ctrl Pts',(4.0929093442588,5.39181089714173,22.9904603083013));
#53332=CARTESIAN_POINT('Ctrl Pts',(3.9493792173035,5.49496977224909,22.9987584229203));
#53333=CARTESIAN_POINT('Ctrl Pts',(3.80580495801465,5.59816036642465,23.0070590890257));
#53334=CARTESIAN_POINT('Ctrl Pts',(3.65819647368515,5.69571134619766,23.015359755131));
#53335=CARTESIAN_POINT('Ctrl Pts',(3.50703625399584,5.78731247758049,23.0236604212364));
#53336=CARTESIAN_POINT('Ctrl Pts',(3.37369971107801,5.86811269215449,23.0309823351942));
#53337=CARTESIAN_POINT('Ctrl Pts',(3.23760020729334,5.94428400194773,23.0383042491519));
#53338=CARTESIAN_POINT('Ctrl Pts',(3.09908550384706,6.0156427786102,23.0456261631097));
#53339=CARTESIAN_POINT('Ctrl Pts',(3.0990855038473,6.01564277861008,21.0460278352566));
#53340=CARTESIAN_POINT('Ctrl Pts',(2.94662663691218,6.09418518577089,21.0540685571013));
#53341=CARTESIAN_POINT('Ctrl Pts',(2.79108041138924,6.1669791943634,21.062109278946));
#53342=CARTESIAN_POINT('Ctrl Pts',(2.63293047526607,6.23377623214174,21.0701500007907));
#53343=CARTESIAN_POINT('Ctrl Pts',(2.47480882144445,6.30056132445862,21.0781892846954));
#53344=CARTESIAN_POINT('Ctrl Pts',(2.31408472406724,6.36135142788615,21.0862285686001));
#53345=CARTESIAN_POINT('Ctrl Pts',(2.15126389991249,6.41594518624757,21.0942678525048));
#53346=CARTESIAN_POINT('Ctrl Pts',(1.98845319473804,6.47053555171887,21.1023066367845));
#53347=CARTESIAN_POINT('Ctrl Pts',(1.82354637576793,6.51893021863884,21.1103454210642));
#53348=CARTESIAN_POINT('Ctrl Pts',(1.65706622753046,6.56097710082713,21.1183842053439));
#53349=CARTESIAN_POINT('Ctrl Pts',(1.49056346858335,6.60302969366534,21.1264240814212));
#53350=CARTESIAN_POINT('Ctrl Pts',(1.32248731704382,6.63873269387233,21.1344639574984));
#53351=CARTESIAN_POINT('Ctrl Pts',(1.15337255970195,6.66798475842039,21.1425038335757));
#53352=CARTESIAN_POINT('Ctrl Pts',(0.984201347065698,6.69724658813584,21.1505463935912));
#53353=CARTESIAN_POINT('Ctrl Pts',(0.813991206228209,6.72005313214289,21.1585889536067));
#53354=CARTESIAN_POINT('Ctrl Pts',(0.643283735453474,6.73635472905792,21.1666315136222));
#53355=CARTESIAN_POINT('Ctrl Pts',(0.472377325898346,6.7526753235001,21.1746834462626));
#53356=CARTESIAN_POINT('Ctrl Pts',(0.300972800845152,6.76247579447924,21.1827353789029));
#53357=CARTESIAN_POINT('Ctrl Pts',(0.129614342912238,6.76575857698983,21.1907873115433));
#53358=CARTESIAN_POINT('Ctrl Pts',(-0.0418468513062848,6.76904332766053,
21.198844071641));
#53359=CARTESIAN_POINT('Ctrl Pts',(-0.213261551119682,6.76580261469696,
21.2069008317387));
#53360=CARTESIAN_POINT('Ctrl Pts',(-0.384089513756238,6.75609089973059,
21.2149575918365));
#53361=CARTESIAN_POINT('Ctrl Pts',(-0.555196049055262,6.74636334767144,
21.2230274902582));
#53362=CARTESIAN_POINT('Ctrl Pts',(-0.725713564944908,6.73014374840286,
21.2310973886798));
#53363=CARTESIAN_POINT('Ctrl Pts',(-0.895109663699864,6.70753812437552,
21.2391672871015));
#53364=CARTESIAN_POINT('Ctrl Pts',(-1.05230006604951,6.68656132997271,21.2466557156376));
#53365=CARTESIAN_POINT('Ctrl Pts',(-1.20852472136614,6.66008623194602,21.2541441441737));
#53366=CARTESIAN_POINT('Ctrl Pts',(-1.36337035817365,6.62823583364785,21.2616325727098));
#53367=CARTESIAN_POINT('Ctrl Pts',(-1.53355963149028,6.59322938301115,21.2698630287764));
#53368=CARTESIAN_POINT('Ctrl Pts',(-1.70264886980046,6.55161271349318,21.278093484843));
#53369=CARTESIAN_POINT('Ctrl Pts',(-1.87008600869319,6.50346579295148,21.2863239409096));
#53370=CARTESIAN_POINT('Ctrl Pts',(-2.03732438983509,6.45537602564173,21.2945446269398));
#53371=CARTESIAN_POINT('Ctrl Pts',(-2.20291423545044,6.40077154096288,21.30276531297));
#53372=CARTESIAN_POINT('Ctrl Pts',(-2.36631225253593,6.33978353916743,21.3109859990002));
#53373=CARTESIAN_POINT('Ctrl Pts',(-2.52954908924421,6.27885569764388,21.3191985759156));
#53374=CARTESIAN_POINT('Ctrl Pts',(-2.69059806960531,6.21155700367775,21.3274111528311));
#53375=CARTESIAN_POINT('Ctrl Pts',(-2.8489295973464,6.13806884527729,21.3356237297465));
#53376=CARTESIAN_POINT('Ctrl Pts',(-3.00713669722695,6.06463843895221,21.3438298526512));
#53377=CARTESIAN_POINT('Ctrl Pts',(-3.16263027431438,5.98502840667668,21.3520359755559));
#53378=CARTESIAN_POINT('Ctrl Pts',(-3.31489922795727,5.89946879884014,21.3602420984607));
#53379=CARTESIAN_POINT('Ctrl Pts',(-3.46707904916856,5.81395927433123,21.3684434178144));
#53380=CARTESIAN_POINT('Ctrl Pts',(-3.61603769547434,5.72250728726912,21.3766447371681));
#53381=CARTESIAN_POINT('Ctrl Pts',(-3.76128718727957,5.62538955938223,21.3848460565218));
#53382=CARTESIAN_POINT('Ctrl Pts',(-3.90649501044739,5.52829969227019,21.3930450231113));
#53383=CARTESIAN_POINT('Ctrl Pts',(-4.04799549874984,5.4255475176042,21.4012439897007));
#53384=CARTESIAN_POINT('Ctrl Pts',(-4.18532806637969,5.3174540878859,21.4094429562902));
#53385=CARTESIAN_POINT('Ctrl Pts',(-4.32264249862362,5.20937493239328,21.4176408401692));
#53386=CARTESIAN_POINT('Ctrl Pts',(-4.45578982416256,5.09595614770787,21.4258387240481));
#53387=CARTESIAN_POINT('Ctrl Pts',(-4.58434107624492,4.97756023536165,21.4340366079271));
#53388=CARTESIAN_POINT('Ctrl Pts',(-4.71289870425812,4.85915845077277,21.4422348984076));
#53389=CARTESIAN_POINT('Ctrl Pts',(-4.83685954083583,4.73577928965515,21.4504331888881));
#53390=CARTESIAN_POINT('Ctrl Pts',(-4.95583011811126,4.60782343850341,21.4586314793686));
#53391=CARTESIAN_POINT('Ctrl Pts',(-5.07482820742181,4.47983799746522,21.4668316657099));
#53392=CARTESIAN_POINT('Ctrl Pts',(-5.18883349486172,4.34727402102261,21.4750318520512));
#53393=CARTESIAN_POINT('Ctrl Pts',(-5.29749154609927,4.21056674558269,21.4832320383925));
#53394=CARTESIAN_POINT('Ctrl Pts',(-5.40625232499886,4.07373022414002,21.4914399773667));
#53395=CARTESIAN_POINT('Ctrl Pts',(-5.50965554416134,3.93274285874172,21.4996479163407));
#53396=CARTESIAN_POINT('Ctrl Pts',(-5.60738846940656,3.78807121806947,21.5078558553149));
#53397=CARTESIAN_POINT('Ctrl Pts',(-5.70516880785485,3.6433293928012,21.5160677762088));
#53398=CARTESIAN_POINT('Ctrl Pts',(-5.79727317890153,3.49490003321679,21.5242796971028));
#53399=CARTESIAN_POINT('Ctrl Pts',(-5.88343395903084,3.34327591588291,21.5324916179968));
#53400=CARTESIAN_POINT('Ctrl Pts',(-5.96971289502047,3.19144387009246,21.5407148002393));
#53401=CARTESIAN_POINT('Ctrl Pts',(-6.05003178615456,3.03640862951005,21.5489379824819));
#53402=CARTESIAN_POINT('Ctrl Pts',(-6.12416994087796,2.87868573054559,21.5571611647245));
#53403=CARTESIAN_POINT('Ctrl Pts',(-6.19028246470763,2.73803670906435,21.5644941680073));
#53404=CARTESIAN_POINT('Ctrl Pts',(-6.25148059307092,2.59525087227621,21.57182717129));
#53405=CARTESIAN_POINT('Ctrl Pts',(-6.30764116018424,2.45070438738532,21.5791601745728));
#53406=CARTESIAN_POINT('Ctrl Pts',(-6.38296327955959,2.25683975691834,21.588995142007));
#53407=CARTESIAN_POINT('Ctrl Pts',(-6.44937136978426,2.05942808343972,21.5988301094412));
#53408=CARTESIAN_POINT('Ctrl Pts',(-6.50657387259168,1.85924324403971,21.6086650768754));
#53409=CARTESIAN_POINT('Ctrl Pts',(-6.56154238031078,1.66687645325694,21.6181159480225));
#53410=CARTESIAN_POINT('Ctrl Pts',(-6.60801052598671,1.47194913615589,21.6275668191696));
#53411=CARTESIAN_POINT('Ctrl Pts',(-6.64576820312261,1.27516822041818,21.6370176903167));
#53412=CARTESIAN_POINT('Ctrl Pts',(-6.68341192004839,1.07898122878296,21.6464400368472));
#53413=CARTESIAN_POINT('Ctrl Pts',(-6.71239759196143,0.880951940409592,
21.6558623833778));
#53414=CARTESIAN_POINT('Ctrl Pts',(-6.73256559614496,0.681798719275146,
21.6652847299084));
#53415=CARTESIAN_POINT('Ctrl Pts',(-6.75263041947556,0.483664379287074,
21.6746588710864));
#53416=CARTESIAN_POINT('Ctrl Pts',(-6.76396749901039,0.284417716246836,
21.6840330122644));
#53417=CARTESIAN_POINT('Ctrl Pts',(-6.76646887602599,0.0847817773557425,
21.6934071534424));
#53418=CARTESIAN_POINT('Ctrl Pts',(-6.76680443639516,0.0580005648731028,
21.6946646968893));
#53419=CARTESIAN_POINT('Ctrl Pts',(-6.7669810606732,0.0312123682027215,
21.6959222403363));
#53420=CARTESIAN_POINT('Ctrl Pts',(-6.76699855717881,0.00441895236067369,
21.6971797837833));
#53421=CARTESIAN_POINT('',(-6.76699990728121,0.0011202036125479,21.3028202162152));
#53422=CARTESIAN_POINT('Ctrl Pts',(3.09908550384707,6.0156427786102,20.6515076495525));
#53423=CARTESIAN_POINT('Ctrl Pts',(3.09592568488907,6.01727062612174,20.6516753907719));
#53424=CARTESIAN_POINT('Ctrl Pts',(3.09276462949704,6.01889596023524,20.6518431319913));
#53425=CARTESIAN_POINT('Ctrl Pts',(3.08960234186716,6.02051877906954,20.6520108732107));
#53426=CARTESIAN_POINT('Ctrl Pts',(2.93611982316823,6.09928274719409,20.6601522404286));
#53427=CARTESIAN_POINT('Ctrl Pts',(2.77942780619768,6.1722741082475,20.6682936076464));
#53428=CARTESIAN_POINT('Ctrl Pts',(2.62000433287076,6.23922000699915,20.6764349748643));
#53429=CARTESIAN_POINT('Ctrl Pts',(2.46072002411105,6.30610746707278,20.6845692352878));
#53430=CARTESIAN_POINT('Ctrl Pts',(2.29870934028287,6.36695982847892,20.6927034957112));
#53431=CARTESIAN_POINT('Ctrl Pts',(2.13447479684968,6.42155015098485,20.7008377561347));
#53432=CARTESIAN_POINT('Ctrl Pts',(1.97035228828983,6.47610323394458,20.7089664676595));
#53433=CARTESIAN_POINT('Ctrl Pts',(1.8040092864421,6.52440266790771,20.7170951791843));
#53434=CARTESIAN_POINT('Ctrl Pts',(1.63596812132802,6.56626966442885,20.7252238907091));
#53435=CARTESIAN_POINT('Ctrl Pts',(1.46800709193988,6.60811669535311,20.7333487258017));
#53436=CARTESIAN_POINT('Ctrl Pts',(1.29834986636587,6.64353730902006,20.7414735608941));
#53437=CARTESIAN_POINT('Ctrl Pts',(1.12753374887625,6.67240261413721,20.7495983959867));
#53438=CARTESIAN_POINT('Ctrl Pts',(0.95676545183752,6.70125983833129,20.7577209565088));
#53439=CARTESIAN_POINT('Ctrl Pts',(0.784839269850681,6.72356534917233,20.765843517031));
#53440=CARTESIAN_POINT('Ctrl Pts',(0.612302475373419,6.73924140231314,20.7739660775532));
#53441=CARTESIAN_POINT('Ctrl Pts',(0.439756511013284,6.7549182885955,20.7820890697683));
#53442=CARTESIAN_POINT('Ctrl Pts',(0.266600233536377,6.7639649762837,20.7902120619835));
#53443=CARTESIAN_POINT('Ctrl Pts',(0.093386002451098,6.76635559622359,20.7983350541987));
#53444=CARTESIAN_POINT('Ctrl Pts',(0.00496541611165684,6.76757593484978,
20.8024815941798));
#53445=CARTESIAN_POINT('Ctrl Pts',(-0.0834702254333327,6.76706267811711,
20.806628134161));
#53446=CARTESIAN_POINT('Ctrl Pts',(-0.17184741606916,6.76481762249289,20.8107746741421));
#53447=CARTESIAN_POINT('Ctrl Pts',(-0.363320439401836,6.75995361193963,
20.8197583331705));
#53448=CARTESIAN_POINT('Ctrl Pts',(-0.554424234399817,6.74696018565322,
20.8287419921989));
#53449=CARTESIAN_POINT('Ctrl Pts',(-0.744493555791528,6.72592137520094,
20.8377256512272));
#53450=CARTESIAN_POINT('Ctrl Pts',(-0.934889414263731,6.70484642029519,
20.8467247440866));
#53451=CARTESIAN_POINT('Ctrl Pts',(-1.12424700925004,6.67569848147455,20.855723836946));
#53452=CARTESIAN_POINT('Ctrl Pts',(-1.31190952420657,6.63861298768772,20.8647229298055));
#53453=CARTESIAN_POINT('Ctrl Pts',(-1.50001205531867,6.60144053878145,20.8737431230228));
#53454=CARTESIAN_POINT('Ctrl Pts',(-1.68641131860128,6.55629334344968,20.8827633162402));
#53455=CARTESIAN_POINT('Ctrl Pts',(-1.87046125076591,6.50335787954063,20.8917835094576));
#53456=CARTESIAN_POINT('Ctrl Pts',(-2.05469757957372,6.45036880521912,20.9008128378793));
#53457=CARTESIAN_POINT('Ctrl Pts',(-2.23657959608153,6.38957577674257,20.909842166301));
#53458=CARTESIAN_POINT('Ctrl Pts',(-2.41547804360663,6.32121466340563,20.9188714947227));
#53459=CARTESIAN_POINT('Ctrl Pts',(-2.59462870188254,6.2527571746783,20.9279135526774));
#53460=CARTESIAN_POINT('Ctrl Pts',(-2.77078715726314,6.17671035276352,20.9369556106322));
#53461=CARTESIAN_POINT('Ctrl Pts',(-2.94334357795152,6.0933584813411,20.9459976685869));
#53462=CARTESIAN_POINT('Ctrl Pts',(-3.09309257417237,6.0210235370438,20.9538446040826));
#53463=CARTESIAN_POINT('Ctrl Pts',(-3.24012906133422,5.94318778162752,20.9616915395782));
#53464=CARTESIAN_POINT('Ctrl Pts',(-3.38406977779202,5.86006490911446,20.9695384750738));
#53465=CARTESIAN_POINT('Ctrl Pts',(-3.54280510217386,5.76839844769471,20.9781919393746));
#53466=CARTESIAN_POINT('Ctrl Pts',(-3.69791481064681,5.67022020774096,20.9868454036754));
#53467=CARTESIAN_POINT('Ctrl Pts',(-3.84886515503193,5.56583560827852,20.9954988679762));
#53468=CARTESIAN_POINT('Ctrl Pts',(-3.99967644327402,5.46154716838332,21.0041443606664));
#53469=CARTESIAN_POINT('Ctrl Pts',(-4.14633576052478,5.35106394464301,21.0127898533565));
#53470=CARTESIAN_POINT('Ctrl Pts',(-4.2883367847219,5.23473558270148,21.0214353460467));
#53471=CARTESIAN_POINT('Ctrl Pts',(-4.43460966596699,5.11490768168516,21.0303409235432));
#53472=CARTESIAN_POINT('Ctrl Pts',(-4.57593931753899,4.98887762199869,21.0392465010398));
#53473=CARTESIAN_POINT('Ctrl Pts',(-4.71180554652535,4.85707499342279,21.0481520785363));
#53474=CARTESIAN_POINT('Ctrl Pts',(-4.8434535693575,4.72936440937589,21.0567811667089));
#53475=CARTESIAN_POINT('Ctrl Pts',(-4.96997207647084,4.59623454241351,21.0654102548814));
#53476=CARTESIAN_POINT('Ctrl Pts',(-5.09092184834525,4.45811661288049,21.074039343054));
#53477=CARTESIAN_POINT('Ctrl Pts',(-5.21768474670377,4.31336041539825,21.0830831652125));
#53478=CARTESIAN_POINT('Ctrl Pts',(-5.33833015749739,4.16312507218579,21.092126987371));
#53479=CARTESIAN_POINT('Ctrl Pts',(-5.45239609107579,4.00795033227977,21.1011708095296));
#53480=CARTESIAN_POINT('Ctrl Pts',(-5.56646202465419,3.85277559237374,21.1102146316881));
#53481=CARTESIAN_POINT('Ctrl Pts',(-5.67394822489392,3.69266174572377,21.1192584538466));
#53482=CARTESIAN_POINT('Ctrl Pts',(-5.77444135509975,3.52818877563457,21.1283022760051));
#53483=CARTESIAN_POINT('Ctrl Pts',(-5.86806703477566,3.37495547917563,21.1367280658549));
#53484=CARTESIAN_POINT('Ctrl Pts',(-5.9555819488501,3.21800570310243,21.1451538557046));
#53485=CARTESIAN_POINT('Ctrl Pts',(-6.03670386153248,3.05785799018837,21.1535796455544));
#53486=CARTESIAN_POINT('Ctrl Pts',(-6.11784459722786,2.89767311761693,21.1620073904709));
#53487=CARTESIAN_POINT('Ctrl Pts',(-6.19258922406439,2.73428912443612,21.1704351353874));
#53488=CARTESIAN_POINT('Ctrl Pts',(-6.260702441154,2.56824725120623,21.1788628803039));
#53489=CARTESIAN_POINT('Ctrl Pts',(-6.32884068643314,2.4021443659195,21.1872937219937));
#53490=CARTESIAN_POINT('Ctrl Pts',(-6.39034253763179,2.23338195981157,21.1957245636836));
#53491=CARTESIAN_POINT('Ctrl Pts',(-6.44502147639647,2.06251961658264,21.2041554053735));
#53492=CARTESIAN_POINT('Ctrl Pts',(-6.49975065812689,1.89150027266843,21.2125939939308));
#53493=CARTESIAN_POINT('Ctrl Pts',(-6.54764430067226,1.71837745247793,21.2210325824881));
#53494=CARTESIAN_POINT('Ctrl Pts',(-6.58856594528387,1.5437252944244,21.2294711710454));
#53495=CARTESIAN_POINT('Ctrl Pts',(-6.62950904739746,1.36898155649757,21.2379141844256));
#53496=CARTESIAN_POINT('Ctrl Pts',(-6.66347279254201,1.19270720553275,21.2463571978058));
#53497=CARTESIAN_POINT('Ctrl Pts',(-6.69037206577036,1.01548541179066,21.254800211186));
#53498=CARTESIAN_POINT('Ctrl Pts',(-6.71729959856012,0.838077434201822,
21.2632520945403));
#53499=CARTESIAN_POINT('Ctrl Pts',(-6.73714779202576,0.659720354079816,
21.2717039778945));
#53500=CARTESIAN_POINT('Ctrl Pts',(-6.74988338645799,0.481002358849198,
21.2801558612488));
#53501=CARTESIAN_POINT('Ctrl Pts',(-6.75335423828881,0.432296059017696,
21.2824592664781));
#53502=CARTESIAN_POINT('Ctrl Pts',(-6.75629711157566,0.383562954992505,
21.2847626717074));
#53503=CARTESIAN_POINT('Ctrl Pts',(-6.75871200404307,0.334814943519694,
21.2870660769368));
#53504=CARTESIAN_POINT('Ctrl Pts',(-6.76421755610254,0.223677607766188,
21.2923174566878));
#53505=CARTESIAN_POINT('Ctrl Pts',(-6.76698148391198,0.11241325470507,21.2975688364388));
#53506=CARTESIAN_POINT('Ctrl Pts',(-6.76699990728112,0.00112020415150532,
21.3028202161898));
#53507=CARTESIAN_POINT('Ctrl Pts',(-6.76699990728121,0.00112020361273272,
21.3028202162152));
#53508=CARTESIAN_POINT('Ctrl Pts',(-6.76702891842711,-0.174132241042112,
21.311089529839));
#53509=CARTESIAN_POINT('Ctrl Pts',(-6.76024557647699,-0.34956410759948,
21.3193588434628));
#53510=CARTESIAN_POINT('Ctrl Pts',(-6.74663422670371,-0.524609960894863,
21.3276281570867));
#53511=CARTESIAN_POINT('Ctrl Pts',(-6.73303425497763,-0.699509489246982,
21.3358905581968));
#53512=CARTESIAN_POINT('Ctrl Pts',(-6.71261767259278,-0.874023296891779,
21.344152959307));
#53513=CARTESIAN_POINT('Ctrl Pts',(-6.68542086837122,-1.04758618392313,
21.3524153604172));
#53514=CARTESIAN_POINT('Ctrl Pts',(-6.65824157348432,-1.22103733096294,
21.3606724421838));
#53515=CARTESIAN_POINT('Ctrl Pts',(-6.62429080789634,-1.39353842939799,
21.3689295239503));
#53516=CARTESIAN_POINT('Ctrl Pts',(-6.58365677468221,-1.56452947341401,
21.3771866057169));
#53517=CARTESIAN_POINT('Ctrl Pts',(-6.54304109715321,-1.73544327533718,
21.3854399574971));
#53518=CARTESIAN_POINT('Ctrl Pts',(-6.49574824933605,-1.90484803923695,
21.3936933092772));
#53519=CARTESIAN_POINT('Ctrl Pts',(-6.44191753897369,-2.07219386666963,
21.4019466610573));
#53520=CARTESIAN_POINT('Ctrl Pts',(-6.38684580767145,-2.24339770887946,
21.4103902867966));
#53521=CARTESIAN_POINT('Ctrl Pts',(-6.32493118864368,-2.4124461586262,21.4188339125359));
#53522=CARTESIAN_POINT('Ctrl Pts',(-6.2563770741499,-2.57876615962974,21.4272775382751));
#53523=CARTESIAN_POINT('Ctrl Pts',(-6.18937543192634,-2.74131968809628,
21.435529950184));
#53524=CARTESIAN_POINT('Ctrl Pts',(-6.11603193000432,-2.90126668262016,
21.4437823620929));
#53525=CARTESIAN_POINT('Ctrl Pts',(-6.03658533437643,-3.05809197062342,
21.4520347740018));
#53526=CARTESIAN_POINT('Ctrl Pts',(-5.95712648527414,-3.21494144663166,
21.4602884587244));
#53527=CARTESIAN_POINT('Ctrl Pts',(-5.87156282614231,-3.36866794145217,
21.4685421434471));
#53528=CARTESIAN_POINT('Ctrl Pts',(-5.78017931513017,-3.5187804826305,21.4767958281697));
#53529=CARTESIAN_POINT('Ctrl Pts',(-5.68876579974297,-3.66894231096071,
21.4850522228632));
#53530=CARTESIAN_POINT('Ctrl Pts',(-5.59152880859176,-3.815487519726,21.4933086175567));
#53531=CARTESIAN_POINT('Ctrl Pts',(-5.48879695101422,-3.95795364178726,
21.5015650122502));
#53532=CARTESIAN_POINT('Ctrl Pts',(-5.3819673693051,-4.10610239122495,21.5101507344626));
#53533=CARTESIAN_POINT('Ctrl Pts',(-5.26919579675221,-4.24983960532958,
21.5187364566751));
#53534=CARTESIAN_POINT('Ctrl Pts',(-5.15089773603461,-4.38868334616586,
21.5273221788875));
#53535=CARTESIAN_POINT('Ctrl Pts',(-5.03694290077282,-4.52242954215717,
21.5355926826844));
#53536=CARTESIAN_POINT('Ctrl Pts',(-4.91786044315648,-4.65163497682704,
21.5438631864812));
#53537=CARTESIAN_POINT('Ctrl Pts',(-4.79405905529826,-4.77590690595124,
21.5521336902781));
#53538=CARTESIAN_POINT('Ctrl Pts',(-4.6701689978321,-4.90026784169665,21.5604101176137));
#53539=CARTESIAN_POINT('Ctrl Pts',(-4.54155353013335,-5.01968798830965,
21.5686865449494));
#53540=CARTESIAN_POINT('Ctrl Pts',(-4.40865475228873,-5.13381459298269,
21.5769629722851));
#53541=CARTESIAN_POINT('Ctrl Pts',(-4.27558143402515,-5.24809108395053,
21.5852502693302));
#53542=CARTESIAN_POINT('Ctrl Pts',(-4.13821384871292,-5.35705993324231,
21.5935375663753));
#53543=CARTESIAN_POINT('Ctrl Pts',(-3.99702406363177,-5.46041094009861,
21.6018248634203));
#53544=CARTESIAN_POINT('Ctrl Pts',(-3.98130006073072,-5.47192091959678,
21.6027478018801));
#53545=CARTESIAN_POINT('Ctrl Pts',(-3.96552867784857,-5.48336126855425,
21.6036707403399));
#53546=CARTESIAN_POINT('Ctrl Pts',(-3.94971058607144,-5.49473159365179,
21.6045936787997));
#53547=CARTESIAN_POINT('Ctrl Pts',(-3.81137595055879,-5.59416898472216,
21.6126650920417));
#53548=CARTESIAN_POINT('Ctrl Pts',(-3.66902918682942,-5.68856179859757,
21.6207365052837));
#53549=CARTESIAN_POINT('Ctrl Pts',(-3.52308071124807,-5.77755928589502,
21.6288079185258));
#53550=CARTESIAN_POINT('Ctrl Pts',(-3.3773154618892,-5.86644504421865,21.636869198777));
#53551=CARTESIAN_POINT('Ctrl Pts',(-3.22795781199351,-5.9499487615537,21.6449304790282));
#53552=CARTESIAN_POINT('Ctrl Pts',(-3.07545102426697,-6.02775994854932,
21.6529917592795));
#53553=CARTESIAN_POINT('Ctrl Pts',(-2.92310225073681,-6.10549051439773,
21.6610446871371));
#53554=CARTESIAN_POINT('Ctrl Pts',(-2.76761116196906,-6.17754011923568,
21.6690976149947));
#53555=CARTESIAN_POINT('Ctrl Pts',(-2.60944968390115,-6.2436416735098,21.6771505428523));
#53556=CARTESIAN_POINT('Ctrl Pts',(-2.45141744519182,-6.30968921385726,
21.6851968903767));
#53557=CARTESIAN_POINT('Ctrl Pts',(-2.29071950261418,-6.36979823433429,
21.6932432379011));
#53558=CARTESIAN_POINT('Ctrl Pts',(-2.12785195969749,-6.42374774081389,
21.7012895854255));
#53559=CARTESIAN_POINT('Ctrl Pts',(-1.96508187463137,-6.47766496460017,
21.7093311181186));
#53560=CARTESIAN_POINT('Ctrl Pts',(-1.80014512684374,-6.52542989472095,
21.7173726508118));
#53561=CARTESIAN_POINT('Ctrl Pts',(-1.63355725711915,-6.56686985463496,
21.7254141835049));
#53562=CARTESIAN_POINT('Ctrl Pts',(-1.46376677932882,-6.60910648690023,
21.7336103125531));
#53563=CARTESIAN_POINT('Ctrl Pts',(-1.29226141455064,-6.64477233083709,
21.7418064416014));
#53564=CARTESIAN_POINT('Ctrl Pts',(-1.11960311989676,-6.67373792217805,
21.7500025706496));
#53565=CARTESIAN_POINT('Ctrl Pts',(-0.950260002153118,-6.70214735107228,
21.7580413274857));
#53566=CARTESIAN_POINT('Ctrl Pts',(-0.779808212887768,-6.72411145366687,
21.7660800843218));
#53567=CARTESIAN_POINT('Ctrl Pts',(-0.608787634920312,-6.73955982357662,
21.7741188411579));
#53568=CARTESIAN_POINT('Ctrl Pts',(-0.437750503968559,-6.7550096887253,
21.7821583760607));
#53569=CARTESIAN_POINT('Ctrl Pts',(-0.266144846661902,-6.76394253173664,
21.7901979109635));
#53570=CARTESIAN_POINT('Ctrl Pts',(-0.0945147078463442,-6.76633992421314,
21.7982374458663));
#53571=CARTESIAN_POINT('Ctrl Pts',(0.0771660257802154,-6.76873802341645,
21.8062793507418));
#53572=CARTESIAN_POINT('Ctrl Pts',(0.248870882049254,-6.76459683205694,
21.8143212556174));
#53573=CARTESIAN_POINT('Ctrl Pts',(0.420056927277532,-6.75395004259331,
21.8223631604929));
#53574=CARTESIAN_POINT('Ctrl Pts',(0.597017468505102,-6.74294411262216,
21.8306763371737));
#53575=CARTESIAN_POINT('Ctrl Pts',(0.773423149339626,-6.72498603702747,
21.8389895138545));
#53576=CARTESIAN_POINT('Ctrl Pts',(0.948682322968968,-6.7001709567806,21.8473026905353));
#53577=CARTESIAN_POINT('Ctrl Pts',(1.11851688254776,-6.67612395178014,21.8553585581459));
#53578=CARTESIAN_POINT('Ctrl Pts',(1.28727450121639,-6.64563823085054,21.8634144257564));
#53579=CARTESIAN_POINT('Ctrl Pts',(1.45442981742539,-6.60885185990607,21.8714702933669));
#53580=CARTESIAN_POINT('Ctrl Pts',(1.62959368983613,-6.5703030220186,21.8799121245829));
#53581=CARTESIAN_POINT('Ctrl Pts',(1.80299747711763,-6.52483506515602,21.8883539557989));
#53582=CARTESIAN_POINT('Ctrl Pts',(1.97405812244072,-6.4726643300287,21.8967957870148));
#53583=CARTESIAN_POINT('Ctrl Pts',(2.14511876776381,-6.42049359490137,21.9052376182308));
#53584=CARTESIAN_POINT('Ctrl Pts',(2.31383586396583,-6.36162031423033,21.9136794494468));
#53585=CARTESIAN_POINT('Ctrl Pts',(2.47965458072558,-6.29631655496185,21.9221212806627));
#53586=CARTESIAN_POINT('Ctrl Pts',(2.64132135993411,-6.23264793758592,21.9303517367293));
#53587=CARTESIAN_POINT('Ctrl Pts',(2.80077100940199,-6.16265560244377,21.9385821927959));
#53588=CARTESIAN_POINT('Ctrl Pts',(2.95747335139946,-6.08651298986226,21.9468126488625));
#53589=CARTESIAN_POINT('Ctrl Pts',(3.11398967848306,-6.01046076304871,21.9550333348927));
#53590=CARTESIAN_POINT('Ctrl Pts',(3.26776487260306,-5.92827295135204,21.9632540209229));
#53591=CARTESIAN_POINT('Ctrl Pts',(3.41828618182501,-5.84017196486064,21.9714747069532));
#53592=CARTESIAN_POINT('Ctrl Pts',(3.56865901261323,-5.75215788364899,21.9796872838685));
#53593=CARTESIAN_POINT('Ctrl Pts',(3.71578404334172,-5.65824242369913,21.9878998607839));
#53594=CARTESIAN_POINT('Ctrl Pts',(3.85917062114248,-5.55869509119819,21.9961124376993));
#53595=CARTESIAN_POINT('Ctrl Pts',(4.00244451585767,-5.45922598987312,22.004318560604));
#53596=CARTESIAN_POINT('Ctrl Pts',(4.14198551617762,-5.35413403497812,22.0125246835086));
#53597=CARTESIAN_POINT('Ctrl Pts',(4.27732953458581,-5.24373350319788,22.0207308064133));
#53598=CARTESIAN_POINT('Ctrl Pts',(4.41259432777456,-5.13339759567264,22.028932125767));
#53599=CARTESIAN_POINT('Ctrl Pts',(4.54366675611459,-5.01775952764966,22.0371334451207));
#53600=CARTESIAN_POINT('Ctrl Pts',(4.67011351299529,-4.89717559167923,22.0453347644745));
#53601=CARTESIAN_POINT('Ctrl Pts',(4.79652399529741,-4.77662624838297,22.053533731064));
#53602=CARTESIAN_POINT('Ctrl Pts',(4.91831118749573,-4.6511341075736,22.0617326976535));
#53603=CARTESIAN_POINT('Ctrl Pts',(5.03507637203057,-4.52109443916177,22.069931664243));
#53604=CARTESIAN_POINT('Ctrl Pts',(5.15182613719535,-4.39107194307556,22.078129548122));
#53605=CARTESIAN_POINT('Ctrl Pts',(5.26355497537947,-4.25650338160682,22.0863274320009));
#53606=CARTESIAN_POINT('Ctrl Pts',(5.36990242666848,-4.11781943849655,22.0945253158799));
#53607=CARTESIAN_POINT('Ctrl Pts',(5.47625515261699,-3.9791286168897,22.1027236063604));
#53608=CARTESIAN_POINT('Ctrl Pts',(5.57722574165307,-3.83632229156312,22.110921896841));
#53609=CARTESIAN_POINT('Ctrl Pts',(5.67249525422541,-3.68986267912373,22.1191201873215));
#53610=CARTESIAN_POINT('Ctrl Pts',(5.76778679794314,-3.54336919779044,22.1273203736629));
#53611=CARTESIAN_POINT('Ctrl Pts',(5.85737444387502,-3.39322104724946,22.1355205600042));
#53612=CARTESIAN_POINT('Ctrl Pts',(5.94098363187514,-3.23990778970508,22.1437207463455));
#53613=CARTESIAN_POINT('Ctrl Pts',(6.02467186580247,-3.08644958650479,22.1519286853196));
#53614=CARTESIAN_POINT('Ctrl Pts',(6.10237017748786,-2.92982061314315,22.1601366242937));
#53615=CARTESIAN_POINT('Ctrl Pts',(6.17385046162314,-2.77053415021648,22.1683445632678));
#53616=CARTESIAN_POINT('Ctrl Pts',(6.24536542300995,-2.61117041260061,22.1765564841618));
#53617=CARTESIAN_POINT('Ctrl Pts',(6.31065620858617,-2.44914694741303,22.1847684050558));
#53618=CARTESIAN_POINT('Ctrl Pts',(6.36954364926308,-2.28499512037385,22.1929803259498));
#53619=CARTESIAN_POINT('Ctrl Pts',(6.42851184473591,-2.12061818510889,22.2012035081923));
#53620=CARTESIAN_POINT('Ctrl Pts',(6.48105903842363,-1.95410739707698,22.2094266904349));
#53621=CARTESIAN_POINT('Ctrl Pts',(6.52705620058236,-1.78600849786316,22.2176498726774));
#53622=CARTESIAN_POINT('Ctrl Pts',(6.5680740609629,-1.63610670274193,22.2249828759602));
#53623=CARTESIAN_POINT('Ctrl Pts',(6.60388392501553,-1.48494235595671,22.232315879243));
#53624=CARTESIAN_POINT('Ctrl Pts',(6.63442894834745,-1.33290717206014,22.2396488825258));
#53625=CARTESIAN_POINT('Ctrl Pts',(6.6716477355503,-1.14765391180549,22.2485840693081));
#53626=CARTESIAN_POINT('Ctrl Pts',(6.70112667694405,-0.960723245654245,
22.2575192560904));
#53627=CARTESIAN_POINT('Ctrl Pts',(6.72273297968455,-0.772754996012099,
22.2664544428727));
#53628=CARTESIAN_POINT('Ctrl Pts',(6.74430692286757,-0.585068264659009,
22.2753762475093));
#53629=CARTESIAN_POINT('Ctrl Pts',(6.75803172464734,-0.396347306592092,
22.2842980521459));
#53630=CARTESIAN_POINT('Ctrl Pts',(6.76382586999895,-0.207240440872359,
22.2932198567825));
#53631=CARTESIAN_POINT('Ctrl Pts',(6.76960588205595,-0.0185948516454272,
22.3021198990218));
#53632=CARTESIAN_POINT('Ctrl Pts',(6.7674938386161,0.170434508781644,22.3110199412611));
#53633=CARTESIAN_POINT('Ctrl Pts',(6.75746008878359,0.359196531855262,22.3199199835003));
#53634=CARTESIAN_POINT('Ctrl Pts',(6.74744178605647,0.547667953019138,22.3288063239937));
#53635=CARTESIAN_POINT('Ctrl Pts',(6.72952611760736,0.735872601121292,22.3376926644872));
#53636=CARTESIAN_POINT('Ctrl Pts',(6.70373530180988,0.923158709685429,22.3465790049806));
#53637=CARTESIAN_POINT('Ctrl Pts',(6.67801042862648,1.10996596036162,22.3554426246525));
#53638=CARTESIAN_POINT('Ctrl Pts',(6.64445062212603,1.29585910272873,22.3643062443244));
#53639=CARTESIAN_POINT('Ctrl Pts',(6.60312970185075,1.48019158913179,22.3731698639963));
#53640=CARTESIAN_POINT('Ctrl Pts',(6.56390357042496,1.65517922952111,22.38158413715));
#53641=CARTESIAN_POINT('Ctrl Pts',(6.51768366501041,1.82876025029509,22.3899984103037));
#53642=CARTESIAN_POINT('Ctrl Pts',(6.46457647938154,2.00038494851042,22.3984126834574));
#53643=CARTESIAN_POINT('Ctrl Pts',(6.41275700935809,2.16784817969352,22.406622931662));
#53644=CARTESIAN_POINT('Ctrl Pts',(6.35442903773312,2.33328756654549,22.4148331798665));
#53645=CARTESIAN_POINT('Ctrl Pts',(6.28978622751912,2.4961727127967,22.423043428071));
#53646=CARTESIAN_POINT('Ctrl Pts',(6.22512805042046,2.65909658009432,22.4312556280152));
#53647=CARTESIAN_POINT('Ctrl Pts',(6.15415217528793,2.81946466623393,22.4394678279595));
#53648=CARTESIAN_POINT('Ctrl Pts',(6.07710026379533,2.97676693474293,22.4476800279037));
#53649=CARTESIAN_POINT('Ctrl Pts',(6.00001631474162,3.13413460826189,22.4558956424141));
#53650=CARTESIAN_POINT('Ctrl Pts',(5.91685145270224,3.2884336051883,22.4641112569246));
#53651=CARTESIAN_POINT('Ctrl Pts',(5.82789313167117,3.43917877491416,22.4723268714351));
#53652=CARTESIAN_POINT('Ctrl Pts',(5.73883491434496,3.59009322485788,22.4805517117205));
#53653=CARTESIAN_POINT('Ctrl Pts',(5.64397042480884,3.73744557003128,22.488776552006));
#53654=CARTESIAN_POINT('Ctrl Pts',(5.54363080142423,3.88077911475267,22.4970013922914));
#53655=CARTESIAN_POINT('Ctrl Pts',(5.44322690702313,4.0242044695916,22.5052315008729));
#53656=CARTESIAN_POINT('Ctrl Pts',(5.33734110245925,4.16360560975987,22.5134616094545));
#53657=CARTESIAN_POINT('Ctrl Pts',(5.22634455480093,4.29855924636415,22.521691718036));
#53658=CARTESIAN_POINT('Ctrl Pts',(5.11519582917256,4.43369790647503,22.5299331102227));
#53659=CARTESIAN_POINT('Ctrl Pts',(4.99892260080244,4.56437661858004,22.5381745024094));
#53660=CARTESIAN_POINT('Ctrl Pts',(4.87793327383911,4.69020852158764,22.5464158945961));
#53661=CARTESIAN_POINT('Ctrl Pts',(4.82527564483445,4.74497376271946,22.5500027578603));
#53662=CARTESIAN_POINT('Ctrl Pts',(4.7717251197473,4.79882142510225,22.5535896211245));
#53663=CARTESIAN_POINT('Ctrl Pts',(4.71731727448285,4.85172203777851,22.5571764843888));
#53664=CARTESIAN_POINT('Ctrl Pts',(4.58917628301486,4.97631320518556,22.5656242406398));
#53665=CARTESIAN_POINT('Ctrl Pts',(4.45598542019436,5.09593252264637,22.5740719968909));
#53666=CARTESIAN_POINT('Ctrl Pts',(4.31815736177582,5.21016372093443,22.5825197531419));
#53667=CARTESIAN_POINT('Ctrl Pts',(4.18044024365649,5.32430297246315,22.590960709641));
#53668=CARTESIAN_POINT('Ctrl Pts',(4.03809362238139,5.43306253443922,22.5994016661401));
#53669=CARTESIAN_POINT('Ctrl Pts',(3.8915660252331,5.53606384277236,22.6078426226393));
#53670=CARTESIAN_POINT('Ctrl Pts',(3.7451621432242,5.63897818577292,22.61627645233));
#53671=CARTESIAN_POINT('Ctrl Pts',(3.59458459652159,5.73614377901942,22.6247102820207));
#53672=CARTESIAN_POINT('Ctrl Pts',(3.44031394494327,5.82722309168174,22.6331441117114));
#53673=CARTESIAN_POINT('Ctrl Pts',(3.32844797976623,5.89326724923467,22.6392597175563));
#53674=CARTESIAN_POINT('Ctrl Pts',(3.21464084663881,5.95611200178093,22.6453753234012));
#53675=CARTESIAN_POINT('Ctrl Pts',(3.09908550384738,6.01564277861003,22.6514909292461));
#53676=CARTESIAN_POINT('Origin',(0.,0.,-63.6971797838103));
#53677=CARTESIAN_POINT('',(3.09908550384716,6.01564277861014,25.0456934344376));
#53678=CARTESIAN_POINT('',(3.09908550384736,6.01564277861004,24.6513967904261));
#53679=CARTESIAN_POINT('',(3.09908550384721,6.01564277861012,-63.6971797838103));
#53680=CARTESIAN_POINT('',(-6.76699871332204,-0.00417299626651514,23.6971797838511));
#53681=CARTESIAN_POINT('Ctrl Pts',(-6.76699871332204,-0.00417299626651379,
23.6971797838512));
#53682=CARTESIAN_POINT('Ctrl Pts',(-6.76687805051677,-0.19984176658391,
23.7063512865483));
#53683=CARTESIAN_POINT('Ctrl Pts',(-6.75826665739669,-0.395211573173384,
23.7155227892454));
#53684=CARTESIAN_POINT('Ctrl Pts',(-6.74126652660386,-0.589588515229351,
23.7246942919426));
#53685=CARTESIAN_POINT('Ctrl Pts',(-6.72421153836498,-0.78459268908379,
23.7338953900129));
#53686=CARTESIAN_POINT('Ctrl Pts',(-6.69871368186293,-0.978597396112563,
23.7430964880832));
#53687=CARTESIAN_POINT('Ctrl Pts',(-6.66492609097329,-1.17091810211624,
23.7522975861535));
#53688=CARTESIAN_POINT('Ctrl Pts',(-6.63098536740846,-1.36411044718708,
23.7615403855918));
#53689=CARTESIAN_POINT('Ctrl Pts',(-6.58867968481332,-1.55560330970433,
23.7707831850301));
#53690=CARTESIAN_POINT('Ctrl Pts',(-6.5382134288921,-1.74472179967326,23.7800259844684));
#53691=CARTESIAN_POINT('Ctrl Pts',(-6.49848710569334,-1.89359320133012,
23.787301785517));
#53692=CARTESIAN_POINT('Ctrl Pts',(-6.45370497690736,-2.04099364387838,
23.7945775865655));
#53693=CARTESIAN_POINT('Ctrl Pts',(-6.4039874546103,-2.18660322902761,23.8018533876141));
#53694=CARTESIAN_POINT('Ctrl Pts',(-6.34293089944737,-2.36542186795322,
23.8107885743963));
#53695=CARTESIAN_POINT('Ctrl Pts',(-6.27434173768598,-2.54179536035517,
23.8197237611786));
#53696=CARTESIAN_POINT('Ctrl Pts',(-6.19842717401112,-2.7151039701051,23.8286589479608));
#53697=CARTESIAN_POINT('Ctrl Pts',(-6.12262630686811,-2.8881530171715,23.8375807525974));
#53698=CARTESIAN_POINT('Ctrl Pts',(-6.03952203253638,-3.05814610463433,
23.846502557234));
#53699=CARTESIAN_POINT('Ctrl Pts',(-5.94937014392125,-3.22448195693796,
23.8554243618706));
#53700=CARTESIAN_POINT('Ctrl Pts',(-5.85943815714215,-3.39041207665096,
23.8643244041099));
#53701=CARTESIAN_POINT('Ctrl Pts',(-5.76249298886226,-3.55270253902627,
23.8732244463491));
#53702=CARTESIAN_POINT('Ctrl Pts',(-5.65883665502042,-3.71077575606467,
23.8821244885884));
#53703=CARTESIAN_POINT('Ctrl Pts',(-5.55533990162899,-3.86860561706067,
23.8910108290818));
#53704=CARTESIAN_POINT('Ctrl Pts',(-5.44515273316735,-4.02223096864418,
23.8998971695751));
#53705=CARTESIAN_POINT('Ctrl Pts',(-5.32862232043915,-4.1710997549948,23.9087835100684));
#53706=CARTESIAN_POINT('Ctrl Pts',(-5.21238985563483,-4.31958790984517,
23.9176471297403));
#53707=CARTESIAN_POINT('Ctrl Pts',(-5.08984666846457,-4.46334356458428,
23.9265107494122));
#53708=CARTESIAN_POINT('Ctrl Pts',(-4.96138189572148,-4.60184513915963,
23.9353743690841));
#53709=CARTESIAN_POINT('Ctrl Pts',(-4.83942972172004,-4.7333252933017,23.943788642238));
#53710=CARTESIAN_POINT('Ctrl Pts',(-4.71214156169059,-4.86007060779907,
23.9522029153919));
#53711=CARTESIAN_POINT('Ctrl Pts',(-4.57988605599304,-4.98165963451143,
23.9606171885457));
#53712=CARTESIAN_POINT('Ctrl Pts',(-4.4508374134857,-5.10030043330662,23.9688274367503));
#53713=CARTESIAN_POINT('Ctrl Pts',(-4.3171827310238,-5.21391719638234,23.9770376849548));
#53714=CARTESIAN_POINT('Ctrl Pts',(-4.17935626272777,-5.32214902358044,
23.9852479331593));
#53715=CARTESIAN_POINT('Ctrl Pts',(-4.04149703033263,-5.43040657964148,
23.9934601331035));
#53716=CARTESIAN_POINT('Ctrl Pts',(-3.89946431627269,-5.53327642964444,
24.0016723330477));
#53717=CARTESIAN_POINT('Ctrl Pts',(-3.75372360851034,-5.63043942076568,
24.0098845329919));
#53718=CARTESIAN_POINT('Ctrl Pts',(-3.6079223029414,-5.72764281147214,24.0181001475024));
#53719=CARTESIAN_POINT('Ctrl Pts',(-3.4584102280793,-5.81913441874243,24.0263157620129));
#53720=CARTESIAN_POINT('Ctrl Pts',(-3.30567992154997,-5.90463963813723,
24.0345313765233));
#53721=CARTESIAN_POINT('Ctrl Pts',(-3.1527781055815,-5.99024087614521,24.0427562168087));
#53722=CARTESIAN_POINT('Ctrl Pts',(-2.99665115045636,-6.06984212542071,
24.0509810570942));
#53723=CARTESIAN_POINT('Ctrl Pts',(-2.83781502587742,-6.1432153534533,24.0592058973796));
#53724=CARTESIAN_POINT('Ctrl Pts',(-2.67887716123888,-6.21663557958921,
24.0674360059612));
#53725=CARTESIAN_POINT('Ctrl Pts',(-2.51722699571533,-6.28381969582728,
24.0756661145427));
#53726=CARTESIAN_POINT('Ctrl Pts',(-2.353398280191,-6.34458868129322,24.0838962231243));
#53727=CARTESIAN_POINT('Ctrl Pts',(-2.18934495298402,-6.40544098197063,
24.092137615311));
#53728=CARTESIAN_POINT('Ctrl Pts',(-2.02310744719204,-6.45986047389336,
24.1003790074976));
#53729=CARTESIAN_POINT('Ctrl Pts',(-1.85523336226345,-6.50771835373541,
24.1086203996843));
#53730=CARTESIAN_POINT('Ctrl Pts',(-1.7821702954165,-6.52854731894192,24.1122072629486));
#53731=CARTESIAN_POINT('Ctrl Pts',(-1.70879734349152,-6.54813403400726,
24.1157941262129));
#53732=CARTESIAN_POINT('Ctrl Pts',(-1.63516007992373,-6.5664709329307,24.1193809894771));
#53733=CARTESIAN_POINT('Ctrl Pts',(-1.46171492893776,-6.60966164980822,
24.1278294843055));
#53734=CARTESIAN_POINT('Ctrl Pts',(-1.28640735786213,-6.64601354661873,
24.1362779791339));
#53735=CARTESIAN_POINT('Ctrl Pts',(-1.10980360493438,-6.67537451821804,
24.1447264739624));
#53736=CARTESIAN_POINT('Ctrl Pts',(-0.933361169276194,-6.70470867027534,
24.1531672515816));
#53737=CARTESIAN_POINT('Ctrl Pts',(-0.755625239165976,-6.72706457154169,
24.1616080292007));
#53738=CARTESIAN_POINT('Ctrl Pts',(-0.57717387623315,-6.74234078911724,
24.1700488068199));
#53739=CARTESIAN_POINT('Ctrl Pts',(-0.398858076269871,-6.75760540190936,
24.1784831722892));
#53740=CARTESIAN_POINT('Ctrl Pts',(-0.219828257999102,-6.7658010241223,
24.1869175377585));
#53741=CARTESIAN_POINT('Ctrl Pts',(-0.0406696645354656,-6.76687778657089,
24.1953519032279));
#53742=CARTESIAN_POINT('Ctrl Pts',(0.138380341673131,-6.76795389639839,
24.2037811566645));
#53743=CARTESIAN_POINT('Ctrl Pts',(0.317558634847511,-6.7619197468726,24.2122104101011));
#53744=CARTESIAN_POINT('Ctrl Pts',(0.496277494712585,-6.74877749286801,
24.2206396635377));
#53745=CARTESIAN_POINT('Ctrl Pts',(0.674915448797272,-6.73564118834361,
24.2290651010629));
#53746=CARTESIAN_POINT('Ctrl Pts',(0.853094052309623,-6.71540322015307,
24.2374905385881));
#53747=CARTESIAN_POINT('Ctrl Pts',(1.03022783445546,-6.6881177927062,24.2459159761133));
#53748=CARTESIAN_POINT('Ctrl Pts',(1.20732270507286,-6.66083835913398,24.2543395627965));
#53749=CARTESIAN_POINT('Ctrl Pts',(1.38337288229526,-6.62651460110577,24.2627631494797));
#53750=CARTESIAN_POINT('Ctrl Pts',(1.5577997154205,-6.58525239050378,24.2711867361629));
#53751=CARTESIAN_POINT('Ctrl Pts',(1.73220703109782,-6.54399479692678,24.2796093802909));
#53752=CARTESIAN_POINT('Ctrl Pts',(1.90499104041301,-6.49580037526879,24.2880320244189));
#53753=CARTESIAN_POINT('Ctrl Pts',(2.07558464744206,-6.4408258299152,24.2964546685469));
#53754=CARTESIAN_POINT('Ctrl Pts',(2.24618295452916,-6.38584976994709,24.3048775447289));
#53755=CARTESIAN_POINT('Ctrl Pts',(2.41459042180088,-6.32409331648483,24.3133004209108));
#53756=CARTESIAN_POINT('Ctrl Pts',(2.58025608977679,-6.25576274415597,24.3217232970927));
#53757=CARTESIAN_POINT('Ctrl Pts',(2.74594942483861,-6.18742076024232,24.3301475799417));
#53758=CARTESIAN_POINT('Ctrl Pts',(2.9088997397551,-6.11250259621451,24.3385718627908));
#53759=CARTESIAN_POINT('Ctrl Pts',(3.06857665571365,-6.0312624141227,24.3469961456398));
#53760=CARTESIAN_POINT('Ctrl Pts',(3.22836141155734,-5.9499673654157,24.3554261179379));
#53761=CARTESIAN_POINT('Ctrl Pts',(3.3848680534537,-5.86234191824887,24.3638560902361));
#53762=CARTESIAN_POINT('Ctrl Pts',(3.53759049680964,-5.76868637359339,24.3722860625342));
#53763=CARTESIAN_POINT('Ctrl Pts',(3.69036753597431,-5.6749973485922,24.3807190484114));
#53764=CARTESIAN_POINT('Ctrl Pts',(3.83935739822696,-5.57527410732994,24.3891520342887));
#53765=CARTESIAN_POINT('Ctrl Pts',(3.98408307130611,-5.46986024327241,24.3975850201659));
#53766=CARTESIAN_POINT('Ctrl Pts',(4.12894189112241,-5.36434939910242,24.4060257643387));
#53767=CARTESIAN_POINT('Ctrl Pts',(4.26952841773963,-5.25313767347353,24.4144665085115));
#53768=CARTESIAN_POINT('Ctrl Pts',(4.40539794635658,-5.1366095758036,24.4229072526843));
#53769=CARTESIAN_POINT('Ctrl Pts',(4.48052383747979,-5.07217807841447,24.4275743655696));
#53770=CARTESIAN_POINT('Ctrl Pts',(4.55420822789292,-5.00612190614283,24.4322414784549));
#53771=CARTESIAN_POINT('Ctrl Pts',(4.62638076641204,-4.93851090959337,24.4369085913401));
#53772=CARTESIAN_POINT('Ctrl Pts',(4.75227940087219,-4.82056948319042,24.445049958558));
#53773=CARTESIAN_POINT('Ctrl Pts',(4.87382547408825,-4.69766025222511,24.4531913257758));
#53774=CARTESIAN_POINT('Ctrl Pts',(4.99060093565539,-4.57014127801708,24.4613326929937));
#53775=CARTESIAN_POINT('Ctrl Pts',(5.10727446112596,-4.44273361817504,24.4694669534172));
#53776=CARTESIAN_POINT('Ctrl Pts',(5.21918541867333,-4.31072449294497,24.4776012138406));
#53777=CARTESIAN_POINT('Ctrl Pts',(5.32595073348743,-4.17451048441188,24.4857354742641));
#53778=CARTESIAN_POINT('Ctrl Pts',(5.43264321686007,-4.03838939615543,24.4938641857889));
#53779=CARTESIAN_POINT('Ctrl Pts',(5.53419682124909,-3.89806942245095,24.5019928973137));
#53780=CARTESIAN_POINT('Ctrl Pts',(5.63026712403262,-3.75398203405895,24.5101216088385));
#53781=CARTESIAN_POINT('Ctrl Pts',(5.72629161266432,-3.60996335827949,24.518246443931));
#53782=CARTESIAN_POINT('Ctrl Pts',(5.81683780421136,-3.4621811494102,24.5263712790235));
#53783=CARTESIAN_POINT('Ctrl Pts',(5.90160320331277,-3.31109779841195,24.534496114116));
#53784=CARTESIAN_POINT('Ctrl Pts',(5.98634487210311,-3.16005674362131,24.5426186746382));
#53785=CARTESIAN_POINT('Ctrl Pts',(6.06530879365759,-3.00571670682226,24.5507412351604));
#53786=CARTESIAN_POINT('Ctrl Pts',(6.138237264273,-2.84856670757249,24.5588637956825));
#53787=CARTESIAN_POINT('Ctrl Pts',(6.21116961084736,-2.69140835620808,24.5669867878977));
#53788=CARTESIAN_POINT('Ctrl Pts',(6.27806570803365,-2.53144007444894,24.5751097801129));
#53789=CARTESIAN_POINT('Ctrl Pts',(6.33871497505609,-2.36917316061948,24.583232772328));
#53790=CARTESIAN_POINT('Ctrl Pts',(6.36967457761155,-2.28634084612172,24.5873793123093));
#53791=CARTESIAN_POINT('Ctrl Pts',(6.39900715896981,-2.20290988185016,24.5915258522905));
#53792=CARTESIAN_POINT('Ctrl Pts',(6.42668962807205,-2.11895007596477,24.5956723922718));
#53793=CARTESIAN_POINT('Ctrl Pts',(6.48666490013114,-1.93704750862493,24.6046560513002));
#53794=CARTESIAN_POINT('Ctrl Pts',(6.53886223245715,-1.75275174609116,24.6136397103287));
#53795=CARTESIAN_POINT('Ctrl Pts',(6.58313645147381,-1.56671741589757,24.6226233693571));
#53796=CARTESIAN_POINT('Ctrl Pts',(6.62748673312969,-1.38036348069562,24.6316224622166));
#53797=CARTESIAN_POINT('Ctrl Pts',(6.66388663988868,-1.19226524065869,24.640621555076));
#53798=CARTESIAN_POINT('Ctrl Pts',(6.69224222806581,-1.00308671653687,24.6496206479355));
#53799=CARTESIAN_POINT('Ctrl Pts',(6.7206643021733,-0.813464621641641,24.658640841153));
#53800=CARTESIAN_POINT('Ctrl Pts',(6.74100428323107,-0.622757412103681,
24.6676610343705));
#53801=CARTESIAN_POINT('Ctrl Pts',(6.75321991307334,-0.431636195967978,
24.6766812275879));
#53802=CARTESIAN_POINT('Ctrl Pts',(6.76544791429967,-0.240321421743524,
24.6857105560097));
#53803=CARTESIAN_POINT('Ctrl Pts',(6.76953511770094,-0.0485920421243081,
24.6947398844314));
#53804=CARTESIAN_POINT('Ctrl Pts',(6.76549143108519,0.142880005294184,24.7037692128532));
#53805=CARTESIAN_POINT('Ctrl Pts',(6.76144204368639,0.334621989705024,24.712811270808));
#53806=CARTESIAN_POINT('Ctrl Pts',(6.74923885109273,0.52610567730403,24.7218533287628));
#53807=CARTESIAN_POINT('Ctrl Pts',(6.7289438899742,0.716661095343454,24.7308953867177));
#53808=CARTESIAN_POINT('Ctrl Pts',(6.71133138941633,0.882030094422799,24.7387423222128));
#53809=CARTESIAN_POINT('Ctrl Pts',(6.68762562503935,1.0466999766423,24.746589257708));
#53810=CARTESIAN_POINT('Ctrl Pts',(6.65789856411851,1.21023787327482,24.7544361932031));
#53811=CARTESIAN_POINT('Ctrl Pts',(6.62511607717144,1.3905846279029,24.7630896575039));
#53812=CARTESIAN_POINT('Ctrl Pts',(6.58498069800237,1.56971346366483,24.7717431218046));
#53813=CARTESIAN_POINT('Ctrl Pts',(6.53760001254048,1.7470189111829,24.7803965861053));
#53814=CARTESIAN_POINT('Ctrl Pts',(6.49026297438123,1.92416102411745,24.7890420787955));
#53815=CARTESIAN_POINT('Ctrl Pts',(6.43569402042041,2.09948280635722,24.7976875714856));
#53816=CARTESIAN_POINT('Ctrl Pts',(6.37405162045641,2.27238969803972,24.8063330641757));
#53817=CARTESIAN_POINT('Ctrl Pts',(6.31055481470666,2.45049819674137,24.8152386416723));
#53818=CARTESIAN_POINT('Ctrl Pts',(6.23955237982781,2.62604391898996,24.8241442191689));
#53819=CARTESIAN_POINT('Ctrl Pts',(6.1612733726827,2.79839229327684,24.8330497966655));
#53820=CARTESIAN_POINT('Ctrl Pts',(6.08542467505829,2.96538980901066,24.8416788848379));
#53821=CARTESIAN_POINT('Ctrl Pts',(6.00274458260455,3.12938522489419,24.8503079730104));
#53822=CARTESIAN_POINT('Ctrl Pts',(5.91349098719739,3.28981965225075,24.8589370611829));
#53823=CARTESIAN_POINT('Ctrl Pts',(5.81994765703926,3.45796493019147,24.8679808833416));
#53824=CARTESIAN_POINT('Ctrl Pts',(5.71918348259384,3.62219816265412,24.8770247055002));
#53825=CARTESIAN_POINT('Ctrl Pts',(5.61155085342805,3.78190243388047,24.8860685276589));
#53826=CARTESIAN_POINT('Ctrl Pts',(5.50391822426225,3.94160670510681,24.8951123498175));
#53827=CARTESIAN_POINT('Ctrl Pts',(5.38941732699857,4.09678167621332,24.9041561719762));
#53828=CARTESIAN_POINT('Ctrl Pts',(5.26845483302557,4.24684267101685,24.9131999941348));
#53829=CARTESIAN_POINT('Ctrl Pts',(5.15576715296944,4.38663827886121,24.9216251456378));
#53830=CARTESIAN_POINT('Ctrl Pts',(5.03752120343059,4.52193457477448,24.9300502971407));
#53831=CARTESIAN_POINT('Ctrl Pts',(4.91410992194947,4.65229112104969,24.9384754486437));
#53832=CARTESIAN_POINT('Ctrl Pts',(4.79067136733749,4.78267647531638,24.9469024620531));
#53833=CARTESIAN_POINT('Ctrl Pts',(4.66206543304073,4.9081196631357,24.9553294754625));
#53834=CARTESIAN_POINT('Ctrl Pts',(4.52872222401741,5.02821678308432,24.9637564888719));
#53835=CARTESIAN_POINT('Ctrl Pts',(4.39528593922621,5.1483977328113,24.9721893844762));
#53836=CARTESIAN_POINT('Ctrl Pts',(4.2571060198141,5.26322493735222,24.9806222800805));
#53837=CARTESIAN_POINT('Ctrl Pts',(4.11464674081503,5.37233386884139,24.9890551756848));
#53838=CARTESIAN_POINT('Ctrl Pts',(3.97213064006988,5.48148631985448,24.9974914348597));
#53839=CARTESIAN_POINT('Ctrl Pts',(3.8253320428754,5.5849157532515,25.0059276940347));
#53840=CARTESIAN_POINT('Ctrl Pts',(3.67474505553761,5.68230039480508,25.0143639532097));
#53841=CARTESIAN_POINT('Ctrl Pts',(3.52402872618747,5.77976868186969,25.0228074584473));
#53842=CARTESIAN_POINT('Ctrl Pts',(3.36951778907315,5.87118163235017,25.0312509636848));
#53843=CARTESIAN_POINT('Ctrl Pts',(3.21173266199104,5.95626244451165,25.0396944689224));
#53844=CARTESIAN_POINT('Ctrl Pts',(3.17436478733321,5.97641192997604,25.0416941240941));
#53845=CARTESIAN_POINT('Ctrl Pts',(3.13681337133934,5.9962064703819,25.0436937792658));
#53846=CARTESIAN_POINT('Ctrl Pts',(3.09908550384716,6.01564277861015,25.0456934344376));
#53847=CARTESIAN_POINT('Ctrl Pts',(3.09908550384706,6.0156427786102,23.0456261631097));
#53848=CARTESIAN_POINT('Ctrl Pts',(2.94196606588778,6.0965861774243,23.0539315269246));
#53849=CARTESIAN_POINT('Ctrl Pts',(2.78173892819578,6.17133642383441,23.0622368907394));
#53850=CARTESIAN_POINT('Ctrl Pts',(2.61893168606547,6.23967032973075,23.0705422545543));
#53851=CARTESIAN_POINT('Ctrl Pts',(2.45593279780636,6.30808467387025,23.0788573949049));
#53852=CARTESIAN_POINT('Ctrl Pts',(2.29034805782135,6.3700674512532,23.0871725352556));
#53853=CARTESIAN_POINT('Ctrl Pts',(2.12272356423858,6.42544423910334,23.0954876756062));
#53854=CARTESIAN_POINT('Ctrl Pts',(1.95499601547681,6.48085507248383,23.1038079280873));
#53855=CARTESIAN_POINT('Ctrl Pts',(1.78522654617375,6.52965172074197,23.1121281805683));
#53856=CARTESIAN_POINT('Ctrl Pts',(1.61397385552916,6.5717103857115,23.1204484330494));
#53857=CARTESIAN_POINT('Ctrl Pts',(1.4424607602372,6.61383300454814,23.1287813371998));
#53858=CARTESIAN_POINT('Ctrl Pts',(1.2694602766696,6.64919709226822,23.1371142413502));
#53859=CARTESIAN_POINT('Ctrl Pts',(1.09554010378793,6.67773021924309,23.1454471455006));
#53860=CARTESIAN_POINT('Ctrl Pts',(0.946997402047146,6.70209994990593,23.1525641582964));
#53861=CARTESIAN_POINT('Ctrl Pts',(0.797784048357197,6.72148761566964,23.1596811710922));
#53862=CARTESIAN_POINT('Ctrl Pts',(0.648254563906394,6.73587819221626,23.166798183888));
#53863=CARTESIAN_POINT('Ctrl Pts',(0.478672985863151,6.75219856333698,23.1748695971301));
#53864=CARTESIAN_POINT('Ctrl Pts',(0.308162695173207,6.76214065689063,23.1829410103721));
#53865=CARTESIAN_POINT('Ctrl Pts',(0.137254858684796,6.76560788870944,23.1910124236141));
#53866=CARTESIAN_POINT('Ctrl Pts',(-0.0334384171712378,6.7690707677059,
23.1990737038653));
#53867=CARTESIAN_POINT('Ctrl Pts',(-0.204527877618031,6.76607495143243,
23.2071349841165));
#53868=CARTESIAN_POINT('Ctrl Pts',(-0.375474229969245,6.75657517553302,
23.2151962643678));
#53869=CARTESIAN_POINT('Ctrl Pts',(-0.54624346265954,6.74708524247063,23.2232491922254));
#53870=CARTESIAN_POINT('Ctrl Pts',(-0.716869513095837,6.73110478077824,
23.231302120083));
#53871=CARTESIAN_POINT('Ctrl Pts',(-0.88681015760305,6.70864045424794,23.2393550479406));
#53872=CARTESIAN_POINT('Ctrl Pts',(-1.05661193757673,6.68619448411634,23.247401395465));
#53873=CARTESIAN_POINT('Ctrl Pts',(-1.22572905848472,6.65727524299328,23.2554477429894));
#53874=CARTESIAN_POINT('Ctrl Pts',(-1.39362159845902,6.62194139511281,23.2634940905138));
#53875=CARTESIAN_POINT('Ctrl Pts',(-1.56141367369068,6.58662869055374,23.271535623207));
#53876=CARTESIAN_POINT('Ctrl Pts',(-1.72798226267916,6.54490909703747,23.2795771559002));
#53877=CARTESIAN_POINT('Ctrl Pts',(-1.89279496000941,6.49689281421227,23.2876186885934));
#53878=CARTESIAN_POINT('Ctrl Pts',(-2.06077613818036,6.44795343095465,23.2958148176416));
#53879=CARTESIAN_POINT('Ctrl Pts',(-2.22693283221004,6.39247284335409,23.3040109466899));
#53880=CARTESIAN_POINT('Ctrl Pts',(-2.39071426966323,6.33062195055341,23.3122070757381));
#53881=CARTESIAN_POINT('Ctrl Pts',(-2.55135097294168,6.26995864420546,23.3202458325742));
#53882=CARTESIAN_POINT('Ctrl Pts',(-2.70970245245694,6.20316760287597,23.3282845894103));
#53883=CARTESIAN_POINT('Ctrl Pts',(-2.86526672974682,6.13045965384375,23.3363233462464));
#53884=CARTESIAN_POINT('Ctrl Pts',(-3.02084606401434,6.05774466745062,23.3443628811492));
#53885=CARTESIAN_POINT('Ctrl Pts',(-3.17363732048882,5.97911179106404,23.352402416052));
#53886=CARTESIAN_POINT('Ctrl Pts',(-3.32316107945763,5.89481886405155,23.3604419509548));
#53887=CARTESIAN_POINT('Ctrl Pts',(-3.47272891650268,5.81050108834552,23.3684838558304));
#53888=CARTESIAN_POINT('Ctrl Pts',(-3.6190270136101,5.72052012416416,23.3765257607059));
#53889=CARTESIAN_POINT('Ctrl Pts',(-3.76160313863333,5.62517829294538,23.3845676655814));
#53890=CARTESIAN_POINT('Ctrl Pts',(-3.9089886817515,5.52662036416332,23.3928808422622));
#53891=CARTESIAN_POINT('Ctrl Pts',(-4.05239639633216,5.42233381609275,23.401194018943));
#53892=CARTESIAN_POINT('Ctrl Pts',(-4.19136287490199,5.31269858460777,23.4095071956238));
#53893=CARTESIAN_POINT('Ctrl Pts',(-4.32602806928495,5.20645677787069,23.4175630632344));
#53894=CARTESIAN_POINT('Ctrl Pts',(-4.45652262851063,5.09519275380206,23.4256189308449));
#53895=CARTESIAN_POINT('Ctrl Pts',(-4.58246202668122,4.97929018777021,23.4336747984555));
#53896=CARTESIAN_POINT('Ctrl Pts',(-4.7144352906662,4.85783462925833,23.4421166296714));
#53897=CARTESIAN_POINT('Ctrl Pts',(-4.84140582776385,4.73128546389627,23.4505584608874));
#53898=CARTESIAN_POINT('Ctrl Pts',(-4.96297864168079,4.60012304207402,23.4590002921033));
#53899=CARTESIAN_POINT('Ctrl Pts',(-5.08455145559772,4.46896062025177,23.4674421233193));
#53900=CARTESIAN_POINT('Ctrl Pts',(-5.20072631158247,4.33318534796473,23.4758839545352));
#53901=CARTESIAN_POINT('Ctrl Pts',(-5.31116064737433,4.19331152882568,23.4843257857512));
#53902=CARTESIAN_POINT('Ctrl Pts',(-5.42026318551523,4.05512453672664,23.4926658115739));
#53903=CARTESIAN_POINT('Ctrl Pts',(-5.52411789085058,3.91248865961095,23.5010058373966));
#53904=CARTESIAN_POINT('Ctrl Pts',(-5.62234753441595,3.76583286966468,23.5093458632193));
#53905=CARTESIAN_POINT('Ctrl Pts',(-5.72040644613119,3.61943198051454,23.5176713933359));
#53906=CARTESIAN_POINT('Ctrl Pts',(-5.81285959669981,3.4690253938297,23.5259969234526));
#53907=CARTESIAN_POINT('Ctrl Pts',(-5.89937016156137,3.31507476490039,23.5343224535693));
#53908=CARTESIAN_POINT('Ctrl Pts',(-5.98579102568036,3.16128376370853,23.5426393511422));
#53909=CARTESIAN_POINT('Ctrl Pts',(-6.06628140900166,3.00395633964463,23.5509562487151));
#53910=CARTESIAN_POINT('Ctrl Pts',(-6.14054729391427,2.84358364237842,23.559273146288));
#53911=CARTESIAN_POINT('Ctrl Pts',(-6.21474837457741,2.68335088597866,23.5675827865543));
#53912=CARTESIAN_POINT('Ctrl Pts',(-6.28273563240102,2.5200784629357,23.5758924268205));
#53913=CARTESIAN_POINT('Ctrl Pts',(-6.34426048947774,2.35428287205504,23.5842020670867));
#53914=CARTESIAN_POINT('Ctrl Pts',(-6.40574176168773,2.18860473254404,23.5925058207149));
#53915=CARTESIAN_POINT('Ctrl Pts',(-6.46076963478621,2.0204073104585,23.6008095743431));
#53916=CARTESIAN_POINT('Ctrl Pts',(-6.50914319088074,1.85022807259291,23.6091133279712));
#53917=CARTESIAN_POINT('Ctrl Pts',(-6.55748843617753,1.68014843273855,23.6174122217977));
#53918=CARTESIAN_POINT('Ctrl Pts',(-6.5991870333806,1.50808962186954,23.6257111156243));
#53919=CARTESIAN_POINT('Ctrl Pts',(-6.63408752911016,1.33460543086901,23.6340100094508));
#53920=CARTESIAN_POINT('Ctrl Pts',(-6.66897587017113,1.16118165857611,23.6423060130517));
#53921=CARTESIAN_POINT('Ctrl Pts',(-6.69707076005188,0.986333834813457,
23.6506020166527));
#53922=CARTESIAN_POINT('Ctrl Pts',(-6.71827151180999,0.810627469064775,
23.6588980202536));
#53923=CARTESIAN_POINT('Ctrl Pts',(-6.73947005152071,0.634939436194601,
23.6671931582649));
#53924=CARTESIAN_POINT('Ctrl Pts',(-6.75377584224094,0.458393383404347,
23.6754882962761));
#53925=CARTESIAN_POINT('Ctrl Pts',(-6.76113983933595,0.281561845682635,
23.6837834342873));
#53926=CARTESIAN_POINT('Ctrl Pts',(-6.76510403614756,0.186369654677821,
23.6882488841282));
#53927=CARTESIAN_POINT('Ctrl Pts',(-6.7670574619932,0.0910948258338363,
23.6927143339691));
#53928=CARTESIAN_POINT('Ctrl Pts',(-6.76699871332258,-0.00417299538677052,
23.6971797838099));
#53929=CARTESIAN_POINT('',(-6.76699967020645,0.00131471018405068,23.3028202161898));
#53930=CARTESIAN_POINT('Ctrl Pts',(3.09908550384738,6.01564277861003,22.6514909292461));
#53931=CARTESIAN_POINT('Ctrl Pts',(2.93986815724682,6.09766695939506,22.6599172859334));
#53932=CARTESIAN_POINT('Ctrl Pts',(2.77733107740478,6.17339780661688,22.6683436426207));
#53933=CARTESIAN_POINT('Ctrl Pts',(2.61200124368849,6.24257466939482,22.676769999308));
#53934=CARTESIAN_POINT('Ctrl Pts',(2.44671664424222,6.31173260537158,22.6851940505427));
#53935=CARTESIAN_POINT('Ctrl Pts',(2.27864112082035,6.37434000160425,22.6936181017774));
#53936=CARTESIAN_POINT('Ctrl Pts',(2.10832292993519,6.43018377833087,22.7020421530121));
#53937=CARTESIAN_POINT('Ctrl Pts',(1.93803032010428,6.48601916756421,22.7104649389908));
#53938=CARTESIAN_POINT('Ctrl Pts',(1.7654960309847,6.5350928585057,22.7188877249695));
#53939=CARTESIAN_POINT('Ctrl Pts',(1.59128515308273,6.57724110562921,22.7273105109482));
#53940=CARTESIAN_POINT('Ctrl Pts',(1.41707614735013,6.61938889980362,22.7357332064108));
#53941=CARTESIAN_POINT('Ctrl Pts',(1.24119091286643,6.65461132040979,22.7441559018735));
#53942=CARTESIAN_POINT('Ctrl Pts',(1.06420681222095,6.68279528796315,22.7525785973361));
#53943=CARTESIAN_POINT('Ctrl Pts',(0.887199933301354,6.71098288286008,22.7610023768197));
#53944=CARTESIAN_POINT('Ctrl Pts',(0.709094235577874,6.7321301668121,22.7694261563032));
#53945=CARTESIAN_POINT('Ctrl Pts',(0.530474687802311,6.74617562813192,22.7778499357868));
#53946=CARTESIAN_POINT('Ctrl Pts',(0.351737367345903,6.76023035031738,22.7862792694838));
#53947=CARTESIAN_POINT('Ctrl Pts',(0.172485852483893,6.76717386518292,22.7947086031807));
#53948=CARTESIAN_POINT('Ctrl Pts',(-0.0066913210940973,6.76699669175492,
22.8031379368777));
#53949=CARTESIAN_POINT('Ctrl Pts',(-0.185926256653699,6.76681946121089,
22.811569987969));
#53950=CARTESIAN_POINT('Ctrl Pts',(-0.365086469648003,6.75951697150564,
22.8200020390602));
#53951=CARTESIAN_POINT('Ctrl Pts',(-0.543585453003535,6.74513186344663,
22.8284340901514));
#53952=CARTESIAN_POINT('Ctrl Pts',(-0.72225783924089,6.73073278097081,22.8368743325608));
#53953=CARTESIAN_POINT('Ctrl Pts',(-0.900267379823388,6.70923736226023,
22.8453145749701));
#53954=CARTESIAN_POINT('Ctrl Pts',(-1.07703344825401,6.68074007512207,22.8537548173795));
#53955=CARTESIAN_POINT('Ctrl Pts',(-1.22328200824711,6.65716265868312,22.8607379070036));
#53956=CARTESIAN_POINT('Ctrl Pts',(-1.36867944026832,6.62879329037425,22.8677209966278));
#53957=CARTESIAN_POINT('Ctrl Pts',(-1.51290324157073,6.59571169637097,22.8747040862519));
#53958=CARTESIAN_POINT('Ctrl Pts',(-1.68104929026209,6.55714289381666,22.8828454534698));
#53959=CARTESIAN_POINT('Ctrl Pts',(-1.84793380259225,6.51209085151953,22.8909868206877));
#53960=CARTESIAN_POINT('Ctrl Pts',(-2.01301533523164,6.46065463092729,22.8991281879055));
#53961=CARTESIAN_POINT('Ctrl Pts',(-2.17795276424785,6.40926331024379,22.907262448329));
#53962=CARTESIAN_POINT('Ctrl Pts',(-2.34108999927349,6.35149901234894,22.9153967087524));
#53963=CARTESIAN_POINT('Ctrl Pts',(-2.50189643805424,6.28751168692763,22.9235309691759));
#53964=CARTESIAN_POINT('Ctrl Pts',(-2.6625931804919,6.22356801134805,22.9316596807008));
#53965=CARTESIAN_POINT('Ctrl Pts',(-2.82096195357071,6.15340989493447,22.9397883922256));
#53966=CARTESIAN_POINT('Ctrl Pts',(-2.97648800098441,6.07723688694096,22.9479171037505));
#53967=CARTESIAN_POINT('Ctrl Pts',(-3.13193988089993,6.00110020444743,22.956041938843));
#53968=CARTESIAN_POINT('Ctrl Pts',(-3.28455140667152,5.91895450301538,22.9641667739355));
#53969=CARTESIAN_POINT('Ctrl Pts',(-3.4338284951019,5.83104715006029,22.972291609028));
#53970=CARTESIAN_POINT('Ctrl Pts',(-3.58306379299294,5.74316440701507,22.9804141695502));
#53971=CARTESIAN_POINT('Ctrl Pts',(-3.72896619814001,5.6495234115118,22.9885367300724));
#53972=CARTESIAN_POINT('Ctrl Pts',(-3.8710669353214,5.55041708182921,22.9966592905946));
#53973=CARTESIAN_POINT('Ctrl Pts',(-4.01317522478872,5.45130548490201,23.0047822828098));
#53974=CARTESIAN_POINT('Ctrl Pts',(-4.15148114016511,5.34672817971588,23.012905275025));
#53975=CARTESIAN_POINT('Ctrl Pts',(-4.28554541765919,5.23702104952618,23.0210282672402));
#53976=CARTESIAN_POINT('Ctrl Pts',(-4.35398114576626,5.18101890284396,23.0251748072213));
#53977=CARTESIAN_POINT('Ctrl Pts',(-4.42131209509528,5.12368070100619,23.0293213472023));
#53978=CARTESIAN_POINT('Ctrl Pts',(-4.48748318345132,5.06505515056269,23.0334678871833));
#53979=CARTESIAN_POINT('Ctrl Pts',(-4.63084572138578,4.93804034835539,23.0424515462117));
#53980=CARTESIAN_POINT('Ctrl Pts',(-4.76869106892665,4.80504354482025,23.05143520524));
#53981=CARTESIAN_POINT('Ctrl Pts',(-4.90056436154782,4.66655739687486,23.0604188642684));
#53982=CARTESIAN_POINT('Ctrl Pts',(-5.03266421108922,4.52783333119382,23.0694179571278));
#53983=CARTESIAN_POINT('Ctrl Pts',(-5.15877133406117,4.38360124512236,23.0784170499873));
#53984=CARTESIAN_POINT('Ctrl Pts',(-5.2784704105158,4.2343876918994,23.0874161428467));
#53985=CARTESIAN_POINT('Ctrl Pts',(-5.39845014785484,4.08482427459184,23.0964363360642));
#53986=CARTESIAN_POINT('Ctrl Pts',(-5.5119916259134,3.9302562075175,23.1054565292816));
#53987=CARTESIAN_POINT('Ctrl Pts',(-5.61872062340603,3.77124217680485,23.114476722499));
#53988=CARTESIAN_POINT('Ctrl Pts',(-5.72555771073407,3.61206710456823,23.1235060509207));
#53989=CARTESIAN_POINT('Ctrl Pts',(-5.8255684061678,3.44843727526012,23.1325353793424));
#53990=CARTESIAN_POINT('Ctrl Pts',(-5.91842315118929,3.28093834191786,23.1415647077642));
#53991=CARTESIAN_POINT('Ctrl Pts',(-6.01140880268452,3.11320326884235,23.1506067657189));
#53992=CARTESIAN_POINT('Ctrl Pts',(-6.09721821579471,2.9415883943495,23.1596488236737));
#53993=CARTESIAN_POINT('Ctrl Pts',(-6.17556786884616,2.76670390487939,23.1686908816285));
#53994=CARTESIAN_POINT('Ctrl Pts',(-6.24356175659459,2.61493454939594,23.176537817124));
#53995=CARTESIAN_POINT('Ctrl Pts',(-6.3059382395626,2.46070320449476,23.1843847526195));
#53996=CARTESIAN_POINT('Ctrl Pts',(-6.36254168907972,2.30442015585758,23.192231688115));
#53997=CARTESIAN_POINT('Ctrl Pts',(-6.42901872513224,2.12087597352802,23.2014473987879));
#53998=CARTESIAN_POINT('Ctrl Pts',(-6.48758449919244,1.93435488806567,23.2106631094608));
#53999=CARTESIAN_POINT('Ctrl Pts',(-6.53799515801084,1.7455395480558,23.2198788201337));
#54000=CARTESIAN_POINT('Ctrl Pts',(-6.58641319465717,1.56418766204055,23.2287302540872));
#54001=CARTESIAN_POINT('Ctrl Pts',(-6.62730830956766,1.38071969702469,23.2375816880407));
#54002=CARTESIAN_POINT('Ctrl Pts',(-6.66051430440762,1.19575842074454,23.2464331219941));
#54003=CARTESIAN_POINT('Ctrl Pts',(-6.69368573792491,1.01098965507524,23.2552753432357));
#54004=CARTESIAN_POINT('Ctrl Pts',(-6.71918396897205,0.824730943739976,
23.2641175644772));
#54005=CARTESIAN_POINT('Ctrl Pts',(-6.73689348630898,0.637616776855506,
23.2729597857188));
#54006=CARTESIAN_POINT('Ctrl Pts',(-6.75457764120661,0.450770582926593,
23.281789343696));
#54007=CARTESIAN_POINT('Ctrl Pts',(-6.76449531809539,0.263071646712626,
23.2906189016732));
#54008=CARTESIAN_POINT('Ctrl Pts',(-6.7665825759315,0.0751614469011366,
23.2994484596503));
#54009=CARTESIAN_POINT('Ctrl Pts',(-6.76684826402433,0.0512422636802975,
23.3005723784968));
#54010=CARTESIAN_POINT('Ctrl Pts',(-6.76698714541347,0.0273196671605242,
23.3016962973433));
#54011=CARTESIAN_POINT('Ctrl Pts',(-6.76699914837107,0.00339498825326048,
23.3028202161898));
#54012=CARTESIAN_POINT('Ctrl Pts',(-6.767,3.50975458611922E-12,23.3028202161898));
#54013=CARTESIAN_POINT('Ctrl Pts',(-6.7670000000001,-0.186007249556406,
23.3115697280025));
#54014=CARTESIAN_POINT('Ctrl Pts',(-6.75932637294267,-0.3720143558125,23.3203192398153));
#54015=CARTESIAN_POINT('Ctrl Pts',(-6.74400518263393,-0.55738953758279,
23.329068751628));
#54016=CARTESIAN_POINT('Ctrl Pts',(-6.72868405703767,-0.742763936379368,
23.3378182264852));
#54017=CARTESIAN_POINT('Ctrl Pts',(-6.70571545643609,-0.927506130401786,
23.3465677013424));
#54018=CARTESIAN_POINT('Ctrl Pts',(-6.67517739401625,-1.11098864009241,
23.3553171761996));
#54019=CARTESIAN_POINT('Ctrl Pts',(-6.6446394580445,-1.29447039004228,23.3640666148281));
#54020=CARTESIAN_POINT('Ctrl Pts',(-6.60653217002795,-1.47669218338956,
23.3728160534566));
#54021=CARTESIAN_POINT('Ctrl Pts',(-6.56098496085563,-1.65703510627453,
23.3815654920851));
#54022=CARTESIAN_POINT('Ctrl Pts',(-6.51543793649644,-1.837377297397,23.3903148952118));
#54023=CARTESIAN_POINT('Ctrl Pts',(-6.46245112156986,-2.01584035544665,
23.3990642983384));
#54024=CARTESIAN_POINT('Ctrl Pts',(-6.40220448361808,-2.19181813797142,
23.4078137014651));
#54025=CARTESIAN_POINT('Ctrl Pts',(-6.34195808512073,-2.36779522106033,
23.4165630698166));
#54026=CARTESIAN_POINT('Ctrl Pts',(-6.27445201416464,-2.54128677725471,
23.4253124381681));
#54027=CARTESIAN_POINT('Ctrl Pts',(-6.19991555052845,-2.71170355428383,
23.4340618065196));
#54028=CARTESIAN_POINT('Ctrl Pts',(-6.12537937695242,-2.88211966813258,
23.4428111408228));
#54029=CARTESIAN_POINT('Ctrl Pts',(-6.04381298028472,-3.04946076419628,
23.451560475126));
#54030=CARTESIAN_POINT('Ctrl Pts',(-5.95549339309,-3.21315848424278,23.4603098094292));
#54031=CARTESIAN_POINT('Ctrl Pts',(-5.8671741422582,-3.37685558085064,23.4690591104108));
#54032=CARTESIAN_POINT('Ctrl Pts',(-5.77210188844069,-3.53690907699996,
23.4778084113923));
#54033=CARTESIAN_POINT('Ctrl Pts',(-5.67059953311365,-3.69277537024002,
23.4865577123739));
#54034=CARTESIAN_POINT('Ctrl Pts',(-5.5690975559269,-3.84864108281052,23.4953069807605));
#54035=CARTESIAN_POINT('Ctrl Pts',(-5.46116568154937,-4.00031938354869,
23.5040562491471));
#54036=CARTESIAN_POINT('Ctrl Pts',(-5.34717048488336,-4.14729511918218,
23.5128055175338));
#54037=CARTESIAN_POINT('Ctrl Pts',(-5.23317570343258,-4.29427031947236,
23.5215547540521));
#54038=CARTESIAN_POINT('Ctrl Pts',(-5.11311781951494,-4.43654276249617,
23.5303039905705));
#54039=CARTESIAN_POINT('Ctrl Pts',(-4.98740458929186,-4.57362924412447,
23.5390532270888));
#54040=CARTESIAN_POINT('Ctrl Pts',(-4.86169180652679,-4.71071523781331,
23.5478024324655));
#54041=CARTESIAN_POINT('Ctrl Pts',(-4.73032391141509,-4.84261509584551,
23.5565516378422));
#54042=CARTESIAN_POINT('Ctrl Pts',(-4.59374706947262,-4.96888084599659,
23.565300843219));
#54043=CARTESIAN_POINT('Ctrl Pts',(-4.4571707023148,-5.09514615720765,23.5740500181806));
#54044=CARTESIAN_POINT('Ctrl Pts',(-4.31538563497374,-5.21577720520572,
23.5827991931424));
#54045=CARTESIAN_POINT('Ctrl Pts',(-4.16887340952094,-5.33036429293433,
23.591548368104));
#54046=CARTESIAN_POINT('Ctrl Pts',(-4.0223616812255,-5.44495099183659,23.6002975133773));
#54047=CARTESIAN_POINT('Ctrl Pts',(-3.87112305263222,-5.55349359497901,
23.6090466586506));
#54048=CARTESIAN_POINT('Ctrl Pts',(-3.71567116929011,-5.65562346357201,
23.6177958039238));
#54049=CARTESIAN_POINT('Ctrl Pts',(-3.56021980053325,-5.75775299408919,
23.6265449202352));
#54050=CARTESIAN_POINT('Ctrl Pts',(-3.40055544442095,-5.85346967519873,
23.6352940365466));
#54051=CARTESIAN_POINT('Ctrl Pts',(-3.23722035886851,-5.94244843041378,
23.6440431528579));
#54052=CARTESIAN_POINT('Ctrl Pts',(-3.07388580043516,-6.03142689847437,
23.652792240934));
#54053=CARTESIAN_POINT('Ctrl Pts',(-2.90688078789267,-6.1136673470788,23.6615413290099));
#54054=CARTESIAN_POINT('Ctrl Pts',(-2.73677250610456,-6.18889047001401,
23.670290417086));
#54055=CARTESIAN_POINT('Ctrl Pts',(-2.56666475917031,-6.26411335643293,
23.6790394776531));
#54056=CARTESIAN_POINT('Ctrl Pts',(-2.39345402457224,-6.33231884545205,
23.6877885382203));
#54057=CARTESIAN_POINT('Ctrl Pts',(-2.21772855944231,-6.39327529804825,
23.6965375987874));
#54058=CARTESIAN_POINT('Ctrl Pts',(-2.04200363223765,-6.45423156404647,
23.7052866325722));
#54059=CARTESIAN_POINT('Ctrl Pts',(-1.86376426061217,-6.507938744124,23.714035666357));
#54060=CARTESIAN_POINT('Ctrl Pts',(-1.68361577621879,-6.55421443943263,
23.7227847001418));
#54061=CARTESIAN_POINT('Ctrl Pts',(-1.50346782833402,-6.60048999692545,
23.7315337078707));
#54062=CARTESIAN_POINT('Ctrl Pts',(-1.3214110565757,-6.63933404265125,23.7402827155996));
#54063=CARTESIAN_POINT('Ctrl Pts',(-1.13806375346714,-6.67061465631499,
23.7490317233285));
#54064=CARTESIAN_POINT('Ctrl Pts',(-0.954716981171266,-6.70189517941754,
23.757780705728));
#54065=CARTESIAN_POINT('Ctrl Pts',(-0.770079967443005,-6.72561226608997,
23.7665296881274));
#54066=CARTESIAN_POINT('Ctrl Pts',(-0.584779764073251,-6.74168536995983,
23.7752786705269));
#54067=CARTESIAN_POINT('Ctrl Pts',(-0.391489587593115,-6.75845153117872,
23.7844049009425));
#54068=CARTESIAN_POINT('Ctrl Pts',(-0.197478091805371,-6.76689985146394,
23.7935311313581));
#54069=CARTESIAN_POINT('Ctrl Pts',(-0.0034621475311433,-6.76699911434415,
23.8026573617737));
#54070=CARTESIAN_POINT('Ctrl Pts',(0.184490798484599,-6.76709527525935,
23.8114983974888));
#54071=CARTESIAN_POINT('Ctrl Pts',(0.372447602154806,-6.75935633790763,
23.820339433204));
#54072=CARTESIAN_POINT('Ctrl Pts',(0.559756448194312,-6.74380914014512,
23.8291804689191));
#54073=CARTESIAN_POINT('Ctrl Pts',(0.745136131043408,-6.72842206873154,
23.8379304475324));
#54074=CARTESIAN_POINT('Ctrl Pts',(0.92988085194505,-6.70538686355723,23.8466804261457));
#54075=CARTESIAN_POINT('Ctrl Pts',(1.11336305057459,-6.67478177303313,23.855430404759));
#54076=CARTESIAN_POINT('Ctrl Pts',(1.29684337090112,-6.64417699581263,23.864180293799));
#54077=CARTESIAN_POINT('Ctrl Pts',(1.47906091205171,-6.60600253548064,23.872930182839));
#54078=CARTESIAN_POINT('Ctrl Pts',(1.65939671095195,-6.56038806441219,23.881680071879));
#54079=CARTESIAN_POINT('Ctrl Pts',(1.83973072369144,-6.51477404513854,23.8904298742545));
#54080=CARTESIAN_POINT('Ctrl Pts',(2.0181827535703,-6.46172023288663,23.89917967663));
#54081=CARTESIAN_POINT('Ctrl Pts',(2.1941466403333,-6.40140683918107,23.9079294790055));
#54082=CARTESIAN_POINT('Ctrl Pts',(2.37010884271264,-6.34109402281496,23.916679197625));
#54083=CARTESIAN_POINT('Ctrl Pts',(2.54358267847811,-6.2735218569979,23.9254289162445));
#54084=CARTESIAN_POINT('Ctrl Pts',(2.71397890841748,-6.19891986435259,23.9341786348641));
#54085=CARTESIAN_POINT('Ctrl Pts',(2.88437356388955,-6.12431856103237,23.9429282726359));
#54086=CARTESIAN_POINT('Ctrl Pts',(3.05169040787191,-6.04268767582548,23.9516779104077));
#54087=CARTESIAN_POINT('Ctrl Pts',(3.21536112512079,-5.95430447953932,23.9604275481796));
#54088=CARTESIAN_POINT('Ctrl Pts',(3.37903038442868,-5.86592207055028,23.9691771080116));
#54089=CARTESIAN_POINT('Ctrl Pts',(3.53905332979999,-5.77078760703361,23.9779266678437));
#54090=CARTESIAN_POINT('Ctrl Pts',(3.69488643041918,-5.66922422085281,23.9866762276757));
#54091=CARTESIAN_POINT('Ctrl Pts',(3.85071819468769,-5.5676617056314,23.9954257124757));
#54092=CARTESIAN_POINT('Ctrl Pts',(4.00235994599251,-5.45967053456231,24.0041751972757));
#54093=CARTESIAN_POINT('Ctrl Pts',(4.14929662974328,-5.34561750206663,24.0129246820757));
#54094=CARTESIAN_POINT('Ctrl Pts',(4.29623210225067,-5.23156540974447,24.0216740947511));
#54095=CARTESIAN_POINT('Ctrl Pts',(4.43846235842135,-5.11145173172171,24.0304235074264));
#54096=CARTESIAN_POINT('Ctrl Pts',(4.57550431797442,-4.98568443006549,24.0391729201018));
#54097=CARTESIAN_POINT('Ctrl Pts',(4.71254519337506,-4.85991812336677,24.0479222635597));
#54098=CARTESIAN_POINT('Ctrl Pts',(4.84439764314995,-4.72849847631089,24.0566716070176));
#54099=CARTESIAN_POINT('Ctrl Pts',(4.97061384196697,-4.59187184425332,24.0654209504755));
#54100=CARTESIAN_POINT('Ctrl Pts',(5.09682908420216,-4.45524624767736,24.0741702276228));
#54101=CARTESIAN_POINT('Ctrl Pts',(5.2174079665018,-4.31341395556881,24.0829195047702));
#54102=CARTESIAN_POINT('Ctrl Pts',(5.3319409594226,-4.16685668162845,24.0916687819176));
#54103=CARTESIAN_POINT('Ctrl Pts',(5.44647312235144,-4.02030046975199,24.1004179956611));
#54104=CARTESIAN_POINT('Ctrl Pts',(5.55495930712302,-3.86901957035527,24.1091672094047));
#54105=CARTESIAN_POINT('Ctrl Pts',(5.65703106079811,-3.7135277805835,24.1179164231482));
#54106=CARTESIAN_POINT('Ctrl Pts',(5.75910210868747,-3.55803706597584,24.1266655763944));
#54107=CARTESIAN_POINT('Ctrl Pts',(5.85475865698557,-3.39833575880886,24.1354147296406));
#54108=CARTESIAN_POINT('Ctrl Pts',(5.94367583069067,-3.23496624706713,24.1441638828868));
#54109=CARTESIAN_POINT('Ctrl Pts',(6.03259241910079,-3.07159781070096,24.1529129785419));
#54110=CARTESIAN_POINT('Ctrl Pts',(6.11476958470967,-2.90456146975836,24.161662074197));
#54111=CARTESIAN_POINT('Ctrl Pts',(6.18992823574383,-2.73442451648264,24.1704111698521));
#54112=CARTESIAN_POINT('Ctrl Pts',(6.26508641700944,-2.56428862662396,24.1791602108223));
#54113=CARTESIAN_POINT('Ctrl Pts',(6.33322605570316,-2.39105242531229,24.1879092517924));
#54114=CARTESIAN_POINT('Ctrl Pts',(6.39411573747794,-2.21530425353652,24.1966582927625));
#54115=CARTESIAN_POINT('Ctrl Pts',(6.45500505889155,-2.03955712188469,24.2054072819535));
#54116=CARTESIAN_POINT('Ctrl Pts',(6.5086444154496,-1.86129832025464,24.2141562711445));
#54117=CARTESIAN_POINT('Ctrl Pts',(6.55485164049938,-1.68113324012185,24.2229052603356));
#54118=CARTESIAN_POINT('Ctrl Pts',(6.60199852639141,-1.49730435912764,24.2318321672124));
#54119=CARTESIAN_POINT('Ctrl Pts',(6.64140767441039,-1.31149113173507,24.2407590740893));
#54120=CARTESIAN_POINT('Ctrl Pts',(6.67293975269628,-1.12435050446277,24.2496859809662));
#54121=CARTESIAN_POINT('Ctrl Pts',(6.70384664831528,-0.940920291562243,
24.2584358951502));
#54122=CARTESIAN_POINT('Ctrl Pts',(6.72718585889682,-0.756215114276483,
24.2671858093342));
#54123=CARTESIAN_POINT('Ctrl Pts',(6.74287810451876,-0.570862389373729,
24.2759357235182));
#54124=CARTESIAN_POINT('Ctrl Pts',(6.75857004154131,-0.385513309566711,
24.2846854656288));
#54125=CARTESIAN_POINT('Ctrl Pts',(6.7666152903556,-0.199516993257844,24.2934352077393));
#54126=CARTESIAN_POINT('Ctrl Pts',(6.76698652348897,-0.0135052182037115,
24.3021849498499));
#54127=CARTESIAN_POINT('Ctrl Pts',(6.7673577498152,0.172503146039223,24.3109345315206));
#54128=CARTESIAN_POINT('Ctrl Pts',(6.76005524147477,0.358526681833787,24.3196841131912));
#54129=CARTESIAN_POINT('Ctrl Pts',(6.74510380214879,0.543933542115166,24.3284336948618));
#54130=CARTESIAN_POINT('Ctrl Pts',(6.73015261710976,0.729337249085047,24.3371831277238));
#54131=CARTESIAN_POINT('Ctrl Pts',(6.70755278444601,0.914124015855012,24.3459325605857));
#54132=CARTESIAN_POINT('Ctrl Pts',(6.67738106408283,1.09766621749423,24.3546819934476));
#54133=CARTESIAN_POINT('Ctrl Pts',(6.64720981677245,1.28120554143368,24.36343128913));
#54134=CARTESIAN_POINT('Ctrl Pts',(6.60946696581511,1.46350005650675,24.3721805848124));
#54135=CARTESIAN_POINT('Ctrl Pts',(6.56428070010979,1.64393062206597,24.3809298804947));
#54136=CARTESIAN_POINT('Ctrl Pts',(6.51909508282722,1.8243585984472,24.3896790506247));
#54137=CARTESIAN_POINT('Ctrl Pts',(6.46646633415639,2.00292240086636,24.3984282207547));
#54138=CARTESIAN_POINT('Ctrl Pts',(6.40657319597166,2.17901557696532,24.4071773908847));
#54139=CARTESIAN_POINT('Ctrl Pts',(6.34668083768269,2.35510646007503,24.4159264470877));
#54140=CARTESIAN_POINT('Ctrl Pts',(6.27952437143861,2.5287265099659,24.4246755032908));
#54141=CARTESIAN_POINT('Ctrl Pts',(6.20533187335114,2.69928607997976,24.4334245594939));
#54142=CARTESIAN_POINT('Ctrl Pts',(6.12831449784228,2.87633970115449,24.4425067357827));
#54143=CARTESIAN_POINT('Ctrl Pts',(6.04371489463127,3.05009490562401,24.4515889120716));
#54144=CARTESIAN_POINT('Ctrl Pts',(5.95184265120463,3.21991584599684,24.4606710883604));
#54145=CARTESIAN_POINT('Ctrl Pts',(5.86333281335457,3.38352155905362,24.4694208687148));
#54146=CARTESIAN_POINT('Ctrl Pts',(5.76807337235642,3.54347560903895,24.4781706490693));
#54147=CARTESIAN_POINT('Ctrl Pts',(5.66638790086304,3.69923467178725,24.4869204294237));
#54148=CARTESIAN_POINT('Ctrl Pts',(5.56470608502684,3.85498813489849,24.495669895218));
#54149=CARTESIAN_POINT('Ctrl Pts',(5.45659885766885,4.00654667256353,24.5044193610122));
#54150=CARTESIAN_POINT('Ctrl Pts',(5.34243340580432,4.15339551506308,24.5131688268065));
#54151=CARTESIAN_POINT('Ctrl Pts',(5.2282714514051,4.30023985883972,24.5219180245604));
#54152=CARTESIAN_POINT('Ctrl Pts',(5.10805181977998,4.44237456993148,24.5306672223142));
#54153=CARTESIAN_POINT('Ctrl Pts',(4.98218281282452,4.57931691626557,24.5394164200681));
#54154=CARTESIAN_POINT('Ctrl Pts',(4.85631699296131,4.71625579512262,24.5481653962861));
#54155=CARTESIAN_POINT('Ctrl Pts',(4.72480227791742,4.84800236135863,24.5569143725041));
#54156=CARTESIAN_POINT('Ctrl Pts',(4.5880853084802,4.97410918678995,24.5656633487221));
#54157=CARTESIAN_POINT('Ctrl Pts',(4.4513594505687,5.10022421089096,24.5744128937433));
#54158=CARTESIAN_POINT('Ctrl Pts',(4.30943087207933,5.22069856612075,24.5831624387645));
#54159=CARTESIAN_POINT('Ctrl Pts',(4.16278164322354,5.33512305301772,24.5919119837857));
#54160=CARTESIAN_POINT('Ctrl Pts',(4.01614103534282,5.44954081331506,24.600661014453));
#54161=CARTESIAN_POINT('Ctrl Pts',(3.86478055833311,5.55790924068408,24.6094100451202));
#54162=CARTESIAN_POINT('Ctrl Pts',(3.70921425811856,5.65986029751354,24.6181590757875));
#54163=CARTESIAN_POINT('Ctrl Pts',(3.55364584530038,5.76181273884704,24.6269082252673));
#54164=CARTESIAN_POINT('Ctrl Pts',(3.39387173464277,5.85734747818102,24.6356573747472));
#54165=CARTESIAN_POINT('Ctrl Pts',(3.23043456092353,5.94614005448836,24.644406524227));
#54166=CARTESIAN_POINT('Ctrl Pts',(3.18690768806362,5.96978744811297,24.64673661296));
#54167=CARTESIAN_POINT('Ctrl Pts',(3.14312114982874,5.99295688499304,24.6490667016931));
#54168=CARTESIAN_POINT('Ctrl Pts',(3.09908550384736,6.01564277861004,24.6513967904261));
#54169=CARTESIAN_POINT('Origin',(0.,0.,-63.6971797838103));
#54170=CARTESIAN_POINT('',(3.09908550384735,6.01564277861005,27.0459166703402));
#54171=CARTESIAN_POINT('',(3.09908550384733,6.01564277861006,26.6512146511404));
#54172=CARTESIAN_POINT('',(3.09908550384721,6.01564277861012,-63.6971797838103));
#54173=CARTESIAN_POINT('',(-6.76699883050778,-0.00397843013915454,25.6971797837804));
#54174=CARTESIAN_POINT('Ctrl Pts',(-6.76699883050741,-0.00397843076278133,
25.6971797838099));
#54175=CARTESIAN_POINT('Ctrl Pts',(-6.76695810834549,-0.0732436356925205,
25.7004595221374));
#54176=CARTESIAN_POINT('Ctrl Pts',(-6.765853956984,-0.142489156183605,25.7037392604649));
#54177=CARTESIAN_POINT('Ctrl Pts',(-6.76368796441601,-0.211693457655297,
25.7070189987924));
#54178=CARTESIAN_POINT('Ctrl Pts',(-6.75825243728204,-0.385360654853746,
25.7152494548589));
#54179=CARTESIAN_POINT('Ctrl Pts',(-6.74611593464877,-0.55907255138845,
25.7234799109255));
#54180=CARTESIAN_POINT('Ctrl Pts',(-6.72726299458639,-0.732271535476137,
25.731710366992));
#54181=CARTESIAN_POINT('Ctrl Pts',(-6.70843243407479,-0.905264922163828,
25.7399310530222));
#54182=CARTESIAN_POINT('Ctrl Pts',(-6.68290135018699,-1.07774625585958,
25.7481517390524));
#54183=CARTESIAN_POINT('Ctrl Pts',(-6.65070625872861,-1.24915782033659,
25.7563724250826));
#54184=CARTESIAN_POINT('Ctrl Pts',(-6.61854292540964,-1.42040029964833,
25.764585001998));
#54185=CARTESIAN_POINT('Ctrl Pts',(-6.57972874142569,-1.59057476132321,
25.7727975789134));
#54186=CARTESIAN_POINT('Ctrl Pts',(-6.53435201193211,-1.75912841605119,
25.7810101558288));
#54187=CARTESIAN_POINT('Ctrl Pts',(-6.48901094260993,-1.92754960966345,
25.7892162787335));
#54188=CARTESIAN_POINT('Ctrl Pts',(-6.43711769275813,-2.09435218870091,
25.7974224016381));
#54189=CARTESIAN_POINT('Ctrl Pts',(-6.3788116732331,-2.25899327963258,25.8056285245428));
#54190=CARTESIAN_POINT('Ctrl Pts',(-6.32053978382505,-2.42353799595766,
25.8138298438965));
#54191=CARTESIAN_POINT('Ctrl Pts',(-6.25586272209305,-2.58592340765658,
25.8220311632502));
#54192=CARTESIAN_POINT('Ctrl Pts',(-6.18496983250082,-2.7456214544352,25.8302324826039));
#54193=CARTESIAN_POINT('Ctrl Pts',(-6.1140972803988,-2.90527368762824,25.8384314491934));
#54194=CARTESIAN_POINT('Ctrl Pts',(-6.03701259396966,-3.06223976264625,
25.8466304157829));
#54195=CARTESIAN_POINT('Ctrl Pts',(-5.95395347458101,-3.21601104204024,
25.8548293823724));
#54196=CARTESIAN_POINT('Ctrl Pts',(-5.87090532352427,-3.36976201524217,
25.8630272662513));
#54197=CARTESIAN_POINT('Ctrl Pts',(-5.78188448046673,-3.52031871724852,
25.8712251501303));
#54198=CARTESIAN_POINT('Ctrl Pts',(-5.68717488564158,-3.66719658869383,
25.8794230340092));
#54199=CARTESIAN_POINT('Ctrl Pts',(-5.5924605933759,-3.81408174504061,25.8876213244897));
#54200=CARTESIAN_POINT('Ctrl Pts',(-5.49205718154599,-3.95728740587926,
25.8958196149703));
#54201=CARTESIAN_POINT('Ctrl Pts',(-5.38629227552321,-4.09635747007498,
25.9040179054508));
#54202=CARTESIAN_POINT('Ctrl Pts',(-5.28050291128713,-4.23545969432662,
25.9122180917921));
#54203=CARTESIAN_POINT('Ctrl Pts',(-5.16934980048246,-4.37042413176443,
25.9204182781334));
#54204=CARTESIAN_POINT('Ctrl Pts',(-5.05320127542262,-4.5008272428596,25.9286184644747));
#54205=CARTESIAN_POINT('Ctrl Pts',(-4.93694294104563,-4.63135363986459,
25.9368264034488));
#54206=CARTESIAN_POINT('Ctrl Pts',(-4.81567999566671,-4.75730982674317,
25.9450343424229));
#54207=CARTESIAN_POINT('Ctrl Pts',(-4.68981876342653,-4.87830800239309,
25.953242281397));
#54208=CARTESIAN_POINT('Ctrl Pts',(-4.56389647208926,-4.99936487792401,
25.961454202291));
#54209=CARTESIAN_POINT('Ctrl Pts',(-4.43337171404866,-5.11545870847014,
25.9696661231849));
#54210=CARTESIAN_POINT('Ctrl Pts',(-4.29868433841007,-5.22624166669587,
25.9778780440788));
#54211=CARTESIAN_POINT('Ctrl Pts',(-4.16381226037282,-5.33717654619869,
25.9861012263214));
#54212=CARTESIAN_POINT('Ctrl Pts',(-4.02476644234229,-5.44278578151289,
25.994324408564));
#54213=CARTESIAN_POINT('Ctrl Pts',(-3.88201717192874,-5.54276390231898,
26.0025475908065));
#54214=CARTESIAN_POINT('Ctrl Pts',(-3.75472084822987,-5.63191915468607,
26.0098805940895));
#54215=CARTESIAN_POINT('Ctrl Pts',(-3.62448003363244,-5.71659699308896,
26.0172135973724));
#54216=CARTESIAN_POINT('Ctrl Pts',(-3.49164434372748,-5.79661183597073,
26.0245466006554));
#54217=CARTESIAN_POINT('Ctrl Pts',(-3.32978546342189,-5.89410907399416,
26.0334817874377));
#54218=CARTESIAN_POINT('Ctrl Pts',(-3.16373792203329,-5.98488514976522,
26.04241697422));
#54219=CARTESIAN_POINT('Ctrl Pts',(-2.99405931104218,-6.06859933114402,
26.0513521610023));
#54220=CARTESIAN_POINT('Ctrl Pts',(-2.82463482611953,-6.15218813457645,
26.0602739656389));
#54221=CARTESIAN_POINT('Ctrl Pts',(-2.65159035386039,-6.22873603342583,
26.0691957702756));
#54222=CARTESIAN_POINT('Ctrl Pts',(-2.47550877308883,-6.29794770654379,
26.0781175749122));
#54223=CARTESIAN_POINT('Ctrl Pts',(-2.29985669705086,-6.36699055597734,
26.0870176171515));
#54224=CARTESIAN_POINT('Ctrl Pts',(-2.12118253804638,-6.42873280030971,
26.0959176593908));
#54225=CARTESIAN_POINT('Ctrl Pts',(-1.94008928689499,-6.48292700551806,
26.1048177016301));
#54226=CARTESIAN_POINT('Ctrl Pts',(-1.75927483146609,-6.53703777795075,
26.1137040421236));
#54227=CARTESIAN_POINT('Ctrl Pts',(-1.57604895901434,-6.58362361708434,
26.122590382617));
#54228=CARTESIAN_POINT('Ctrl Pts',(-1.39103276731701,-6.62248569951271,
26.1314767231104));
#54229=CARTESIAN_POINT('Ctrl Pts',(-1.20648962972656,-6.66124841837985,
26.1403403427824));
#54230=CARTESIAN_POINT('Ctrl Pts',(-1.02016555913015,-6.69232673410084,
26.1492039624543));
#54231=CARTESIAN_POINT('Ctrl Pts',(-0.832694137200324,-6.71557216280729,
26.1580675821263));
#54232=CARTESIAN_POINT('Ctrl Pts',(-0.654726691509346,-6.73763915055558,
26.1664818552797));
#54233=CARTESIAN_POINT('Ctrl Pts',(-0.475725582744447,-6.75264759780368,
26.1748961284332));
#54234=CARTESIAN_POINT('Ctrl Pts',(-0.296244233930681,-6.76051243278665,
26.1833104015867));
#54235=CARTESIAN_POINT('Ctrl Pts',(-0.121114856150621,-6.76818656531359,
26.1915206497912));
#54236=CARTESIAN_POINT('Ctrl Pts',(0.0543034891896902,-6.76905092275449,
26.1997308979957));
#54237=CARTESIAN_POINT('Ctrl Pts',(0.229446166549684,-6.76310900818963,
26.2079411462003));
#54238=CARTESIAN_POINT('Ctrl Pts',(0.404630478815592,-6.75716568111322,
26.2161533461445));
#54239=CARTESIAN_POINT('Ctrl Pts',(0.579538636792803,-6.74441287060682,
26.2243655460887));
#54240=CARTESIAN_POINT('Ctrl Pts',(0.753608990122599,-6.72490613243088,
26.2325777460329));
#54241=CARTESIAN_POINT('Ctrl Pts',(0.927751720496305,-6.70539128351109,
26.2407933605433));
#54242=CARTESIAN_POINT('Ctrl Pts',(1.10105559878524,-6.67911695192261,26.2490089750538));
#54243=CARTESIAN_POINT('Ctrl Pts',(1.27296696474913,-6.64619019489041,26.2572245895642));
#54244=CARTESIAN_POINT('Ctrl Pts',(1.4450713796411,-6.61322646255344,26.2654494298496));
#54245=CARTESIAN_POINT('Ctrl Pts',(1.61577980920721,-6.57359545098582,26.2736742701351));
#54246=CARTESIAN_POINT('Ctrl Pts',(1.78455065411568,-6.52745493763805,26.2818991104205));
#54247=CARTESIAN_POINT('Ctrl Pts',(1.95342960261712,-6.48128486968754,26.290129219002));
#54248=CARTESIAN_POINT('Ctrl Pts',(2.1203681538456,-6.42859709499531,26.2983593275835));
#54249=CARTESIAN_POINT('Ctrl Pts',(2.28484266381283,-6.36959833911218,26.3065894361651));
#54250=CARTESIAN_POINT('Ctrl Pts',(2.44954267085703,-6.31051869502943,26.3148308283518));
#54251=CARTESIAN_POINT('Ctrl Pts',(2.61177155981408,-6.24511092010381,26.3230722205384));
#54252=CARTESIAN_POINT('Ctrl Pts',(2.77102742736652,-6.17362907832844,26.3313136127251));
#54253=CARTESIAN_POINT('Ctrl Pts',(2.84033962705722,-6.14251836468543,26.3349004759896));
#54254=CARTESIAN_POINT('Ctrl Pts',(2.90908900729819,-6.11025767345907,26.338487339254));
#54255=CARTESIAN_POINT('Ctrl Pts',(2.97723582829392,-6.07687056162323,26.3420742025185));
#54256=CARTESIAN_POINT('Ctrl Pts',(3.13774879528164,-5.99823058544214,26.3505226973469));
#54257=CARTESIAN_POINT('Ctrl Pts',(3.29528303020821,-5.91315902906587,26.3589711921753));
#54258=CARTESIAN_POINT('Ctrl Pts',(3.44930736484255,-5.82190413033768,26.3674196870038));
#54259=CARTESIAN_POINT('Ctrl Pts',(3.60319100719453,-5.73073258765845,26.375860464623));
#54260=CARTESIAN_POINT('Ctrl Pts',(3.75357085446227,-5.63338913020284,26.3843012422422));
#54261=CARTESIAN_POINT('Ctrl Pts',(3.89993932131773,-5.5301683780912,26.3927420198613));
#54262=CARTESIAN_POINT('Ctrl Pts',(4.04619659740531,-5.42702603900754,26.4011763853307));
#54263=CARTESIAN_POINT('Ctrl Pts',(4.18844829635835,-5.31801549732248,26.4096107508));
#54264=CARTESIAN_POINT('Ctrl Pts',(4.32621454127569,-5.20347544847238,26.4180451162693));
#54265=CARTESIAN_POINT('Ctrl Pts',(4.46389728666329,-5.08900482185426,26.4264743697059));
#54266=CARTESIAN_POINT('Ctrl Pts',(4.59709974245636,-4.96901158256042,26.4349036231425));
#54267=CARTESIAN_POINT('Ctrl Pts',(4.72537363584976,-4.84387582433902,26.4433328765791));
#54268=CARTESIAN_POINT('Ctrl Pts',(4.85358945982906,-4.71879671490227,26.4517583141044));
#54269=CARTESIAN_POINT('Ctrl Pts',(4.97688093208074,-4.5885799610794,26.4601837516296));
#54270=CARTESIAN_POINT('Ctrl Pts',(5.09483501661782,-4.45364403084092,26.4686091891549));
#54271=CARTESIAN_POINT('Ctrl Pts',(5.21276318981455,-4.3187377423976,26.4770327758381));
#54272=CARTESIAN_POINT('Ctrl Pts',(5.32535609176861,-4.17911459354741,26.4854563625213));
#54273=CARTESIAN_POINT('Ctrl Pts',(5.43223917423329,-4.03522819105999,26.4938799492045));
#54274=CARTESIAN_POINT('Ctrl Pts',(5.53911029704153,-3.89135788870647,26.5023025933325));
#54275=CARTESIAN_POINT('Ctrl Pts',(5.64027267527523,-3.7432255513046,26.5107252374605));
#54276=CARTESIAN_POINT('Ctrl Pts',(5.73539333324714,-3.59131623683355,26.5191478815885));
#54277=CARTESIAN_POINT('Ctrl Pts',(5.83051661190702,-3.43940273707907,26.5275707577704));
#54278=CARTESIAN_POINT('Ctrl Pts',(5.91959766182598,-3.28371233556856,26.5359936339524));
#54279=CARTESIAN_POINT('Ctrl Pts',(6.00234777247844,-3.12475762551643,26.5444165101343));
#54280=CARTESIAN_POINT('Ctrl Pts',(6.08511170285861,-2.9657763691456,26.5528407929833));
#54281=CARTESIAN_POINT('Ctrl Pts',(6.16154243263012,-2.80353001331801,26.5612650758323));
#54282=CARTESIAN_POINT('Ctrl Pts',(6.23139783306991,-2.63855453724414,26.5696893586813));
#54283=CARTESIAN_POINT('Ctrl Pts',(6.30130041126432,-2.47346764283354,26.5781193309795));
#54284=CARTESIAN_POINT('Ctrl Pts',(6.36461865641622,-2.30564825247651,26.5865493032777));
#54285=CARTESIAN_POINT('Ctrl Pts',(6.42115873691968,-2.13565200238244,26.5949792755758));
#54286=CARTESIAN_POINT('Ctrl Pts',(6.47771902958934,-1.96559498137276,26.603412261453));
#54287=CARTESIAN_POINT('Ctrl Pts',(6.52749622671926,-1.79335986721838,26.6118452473302));
#54288=CARTESIAN_POINT('Ctrl Pts',(6.57034661664641,-1.61951669862434,26.6202782332074));
#54289=CARTESIAN_POINT('Ctrl Pts',(6.61323642867122,-1.44551359537438,26.6287189773803));
#54290=CARTESIAN_POINT('Ctrl Pts',(6.64918662740134,-1.2698998072055,26.6371597215531));
#54291=CARTESIAN_POINT('Ctrl Pts',(6.67810456598509,-1.09325587387819,26.6456004657259));
#54292=CARTESIAN_POINT('Ctrl Pts',(6.69409406655653,-0.995584725407506,
26.650267578611));
#54293=CARTESIAN_POINT('Ctrl Pts',(6.70793452446345,-0.897598762076486,
26.6549346914961));
#54294=CARTESIAN_POINT('Ctrl Pts',(6.7196170927716,-0.799396726620603,26.6596018043812));
#54295=CARTESIAN_POINT('Ctrl Pts',(6.73999630385679,-0.628091928158219,
26.6677431715991));
#54296=CARTESIAN_POINT('Ctrl Pts',(6.75384653233093,-0.455789002641146,
26.6758845388169));
#54297=CARTESIAN_POINT('Ctrl Pts',(6.7610784939512,-0.283031091278999,26.6840259060347));
#54298=CARTESIAN_POINT('Ctrl Pts',(6.76830414261901,-0.110423984434327,
26.6921601664582));
#54299=CARTESIAN_POINT('Ctrl Pts',(6.76892300890659,0.0626369544499142,
26.7002944268816));
#54300=CARTESIAN_POINT('Ctrl Pts',(6.76289737244261,0.235601633714247,26.708428687305));
#54301=CARTESIAN_POINT('Ctrl Pts',(6.75687584645019,0.408448322721779,26.7165573988298));
#54302=CARTESIAN_POINT('Ctrl Pts',(6.74421885474144,0.581198518511867,26.7246861103546));
#54303=CARTESIAN_POINT('Ctrl Pts',(6.72494071497385,0.753300325293346,26.7328148218794));
#54304=CARTESIAN_POINT('Ctrl Pts',(6.70567176859481,0.925320059903924,26.7409396569719));
#54305=CARTESIAN_POINT('Ctrl Pts',(6.67978800251816,1.09669165823763,26.7490644920644));
#54306=CARTESIAN_POINT('Ctrl Pts',(6.6473557227816,1.26686656550827,26.7571893271568));
#54307=CARTESIAN_POINT('Ctrl Pts',(6.61493252255269,1.43699383183649,26.765311887679));
#54308=CARTESIAN_POINT('Ctrl Pts',(6.5759645294767,1.6059247152823,26.7734344482011));
#54309=CARTESIAN_POINT('Ctrl Pts',(6.53056946604912,1.77311912998167,26.7815570087232));
#54310=CARTESIAN_POINT('Ctrl Pts',(6.48517198999165,1.94032243063054,26.7896800009384));
#54311=CARTESIAN_POINT('Ctrl Pts',(6.43334685333674,2.10578872386958,26.7978029931535));
#54312=CARTESIAN_POINT('Ctrl Pts',(6.37526217773027,2.26899122193144,26.8059259853687));
#54313=CARTESIAN_POINT('Ctrl Pts',(6.34561172093646,2.35230112367231,26.8100725253501));
#54314=CARTESIAN_POINT('Ctrl Pts',(6.31433095963519,2.43502137573639,26.8142190653315));
#54315=CARTESIAN_POINT('Ctrl Pts',(6.28144717792837,2.5170836996206,26.818365605313));
#54316=CARTESIAN_POINT('Ctrl Pts',(6.21020303612765,2.69487528975545,26.8273492643415));
#54317=CARTESIAN_POINT('Ctrl Pts',(6.1314670238083,2.86948952157552,26.8363329233699));
#54318=CARTESIAN_POINT('Ctrl Pts',(6.0455495977747,3.04033206424005,26.8453165823984));
#54319=CARTESIAN_POINT('Ctrl Pts',(5.95948456651342,3.21146811258291,26.8543156752579));
#54320=CARTESIAN_POINT('Ctrl Pts',(5.86621356961772,3.37881930694775,26.8633147681174));
#54321=CARTESIAN_POINT('Ctrl Pts',(5.76609230798076,3.54181711778644,26.8723138609769));
#54322=CARTESIAN_POINT('Ctrl Pts',(5.66573628996394,3.70519711294216,26.8813340541944));
#54323=CARTESIAN_POINT('Ctrl Pts',(5.55849799574921,3.86420309664514,26.8903542474118));
#54324=CARTESIAN_POINT('Ctrl Pts',(5.44477723408637,4.01829439827083,26.8993744406293));
#54325=CARTESIAN_POINT('Ctrl Pts',(5.3309413016762,4.17254175592452,26.9084037690511));
#54326=CARTESIAN_POINT('Ctrl Pts',(5.21060993306272,4.32186429932877,26.9174330974729));
#54327=CARTESIAN_POINT('Ctrl Pts',(5.08422338295535,4.46575431391048,26.9264624258947));
#54328=CARTESIAN_POINT('Ctrl Pts',(4.95765865328782,4.60984718440913,26.9355044838496));
#54329=CARTESIAN_POINT('Ctrl Pts',(4.82502183102855,4.74849203251823,26.9445465418045));
#54330=CARTESIAN_POINT('Ctrl Pts',(4.68679178908261,4.8812162137922,26.9535885997593));
#54331=CARTESIAN_POINT('Ctrl Pts',(4.56683212635577,4.99639774594819,26.9614355352543));
#54332=CARTESIAN_POINT('Ctrl Pts',(4.44266072880168,5.10712081221389,26.9692824707493));
#54333=CARTESIAN_POINT('Ctrl Pts',(4.31461139104306,5.21310056917009,26.9771294062443));
#54334=CARTESIAN_POINT('Ctrl Pts',(4.17338976130643,5.32998234504197,26.9857835472062));
#54335=CARTESIAN_POINT('Ctrl Pts',(4.02732597406175,5.44119673635603,26.9944376881681));
#54336=CARTESIAN_POINT('Ctrl Pts',(3.87689232870796,5.54634968890399,27.0030918291301));
#54337=CARTESIAN_POINT('Ctrl Pts',(3.72662796509449,5.65138431370176,27.0117362316585));
#54338=CARTESIAN_POINT('Ctrl Pts',(3.57200380360275,5.75037093627247,27.020380634187));
#54339=CARTESIAN_POINT('Ctrl Pts',(3.41352374733898,5.84295683933681,27.0290250367155));
#54340=CARTESIAN_POINT('Ctrl Pts',(3.31029752519016,5.90326280604888,27.0346555812571));
#54341=CARTESIAN_POINT('Ctrl Pts',(3.20543607517873,5.96085403431976,27.0402861257987));
#54342=CARTESIAN_POINT('Ctrl Pts',(3.09908550384735,6.01564277861005,27.0459166703402));
#54343=CARTESIAN_POINT('Ctrl Pts',(3.09908550384716,6.01564277861015,25.0456934344376));
#54344=CARTESIAN_POINT('Ctrl Pts',(2.93386957082307,6.10075725795725,25.0544502213138));
#54345=CARTESIAN_POINT('Ctrl Pts',(2.76526825588463,6.17899746639908,25.06320700819));
#54346=CARTESIAN_POINT('Ctrl Pts',(2.59388993472329,6.25012191933415,25.0719637950662));
#54347=CARTESIAN_POINT('Ctrl Pts',(2.43111345179144,6.31767648645075,25.0802810603996));
#54348=CARTESIAN_POINT('Ctrl Pts',(2.26553899905849,6.3789333607424,25.088598325733));
#54349=CARTESIAN_POINT('Ctrl Pts',(2.09768879961298,6.43366075418795,25.0969155910664));
#54350=CARTESIAN_POINT('Ctrl Pts',(1.92998016889498,6.48834198928829,25.1052258414265));
#54351=CARTESIAN_POINT('Ctrl Pts',(1.75999994470735,6.53650460852614,25.1135360917866));
#54352=CARTESIAN_POINT('Ctrl Pts',(1.5882899136827,6.57796504628094,25.1218463421467));
#54353=CARTESIAN_POINT('Ctrl Pts',(1.41669326014494,6.61939810834773,25.1301511053765));
#54354=CARTESIAN_POINT('Ctrl Pts',(1.24336941265814,6.65413772561488,25.1384558686064));
#54355=CARTESIAN_POINT('Ctrl Pts',(1.06887511172934,6.68205020899466,25.1467606318363));
#54356=CARTESIAN_POINT('Ctrl Pts',(0.894464084403035,6.70994937175002,25.1550614317989));
#54357=CARTESIAN_POINT('Ctrl Pts',(0.718884059572879,6.73102783887337,25.1633622317614));
#54358=CARTESIAN_POINT('Ctrl Pts',(0.542701984691165,6.7452030033063,25.171663031724));
#54359=CARTESIAN_POINT('Ctrl Pts',(0.366571748568069,6.75937399692373,25.179961389309));
#54360=CARTESIAN_POINT('Ctrl Pts',(0.189840161791331,6.76664570874752,25.1882597468939));
#54361=CARTESIAN_POINT('Ctrl Pts',(0.0130795383062143,6.7669873596511,25.1965581044788));
#54362=CARTESIAN_POINT('Ctrl Pts',(-0.163699070167067,6.76732904531687,
25.2048573064026));
#54363=CARTESIAN_POINT('Ctrl Pts',(-0.340506373458073,6.76073925297585,
25.2131565083264));
#54364=CARTESIAN_POINT('Ctrl Pts',(-0.516769214631858,6.747239330186,25.2214557102502));
#54365=CARTESIAN_POINT('Ctrl Pts',(-0.693049925516606,6.73373803875987,
25.2297557535557));
#54366=CARTESIAN_POINT('Ctrl Pts',(-0.868785717218181,6.7133252465697,25.2380557968612));
#54367=CARTESIAN_POINT('Ctrl Pts',(-1.04340780343969,6.68607427087982,25.2463558401668));
#54368=CARTESIAN_POINT('Ctrl Pts',(-1.21807658067824,6.65881600873611,25.2546581027647));
#54369=CARTESIAN_POINT('Ctrl Pts',(-1.39163071514237,6.62471597252829,25.2629603653626));
#54370=CARTESIAN_POINT('Ctrl Pts',(-1.5635106793521,6.58389879596823,25.2712626279605));
#54371=CARTESIAN_POINT('Ctrl Pts',(-1.73546513725157,6.54306392902698,25.2795684888031));
#54372=CARTESIAN_POINT('Ctrl Pts',(-1.90574364050117,6.4955061999138,25.2878743496458));
#54373=CARTESIAN_POINT('Ctrl Pts',(-2.07380072200634,6.44140043510773,25.2961802104884));
#54374=CARTESIAN_POINT('Ctrl Pts',(-2.24205645883823,6.3872307134705,25.3044958894446));
#54375=CARTESIAN_POINT('Ctrl Pts',(-2.40808519599487,6.32649759811053,25.3128115684007));
#54376=CARTESIAN_POINT('Ctrl Pts',(-2.57135928194027,6.25942492911127,25.3211272473568));
#54377=CARTESIAN_POINT('Ctrl Pts',(-2.73473663744468,6.19230983718304,25.3294481859136));
#54378=CARTESIAN_POINT('Ctrl Pts',(-2.8953555512352,6.11884733970848,25.3377691244705));
#54379=CARTESIAN_POINT('Ctrl Pts',(-3.05271185063397,6.03930785413353,25.3460900630273));
#54380=CARTESIAN_POINT('Ctrl Pts',(-3.21030203023437,5.95965014824586,25.3544233690762));
#54381=CARTESIAN_POINT('Ctrl Pts',(-3.36461960048107,5.8738975724953,25.3627566751251));
#54382=CARTESIAN_POINT('Ctrl Pts',(-3.51518715403526,5.78236528352417,25.3710899811741));
#54383=CARTESIAN_POINT('Ctrl Pts',(-3.62601376298369,5.71499211476036,25.3772237864258));
#54384=CARTESIAN_POINT('Ctrl Pts',(-3.73480926329466,5.64448851718007,25.3833575916775));
#54385=CARTESIAN_POINT('Ctrl Pts',(-3.84139462256851,5.5709941979598,25.3894913969293));
#54386=CARTESIAN_POINT('Ctrl Pts',(-3.9809256705174,5.47478267839503,25.3975211702539));
#54387=CARTESIAN_POINT('Ctrl Pts',(-4.11710711489268,5.37314122535884,25.4055509435785));
#54388=CARTESIAN_POINT('Ctrl Pts',(-4.24947299795826,5.26633347212495,25.413580716903));
#54389=CARTESIAN_POINT('Ctrl Pts',(-4.38167304827217,5.15965953149601,25.421600430238));
#54390=CARTESIAN_POINT('Ctrl Pts',(-4.51006675783186,5.04783240040823,25.4296201435731));
#54391=CARTESIAN_POINT('Ctrl Pts',(-4.63421478721721,4.93116034072482,25.437639856908));
#54392=CARTESIAN_POINT('Ctrl Pts',(-4.75823499883584,4.8146084018535,25.4456513134721));
#54393=CARTESIAN_POINT('Ctrl Pts',(-4.87801795547243,4.69322171487695,25.453662770036));
#54394=CARTESIAN_POINT('Ctrl Pts',(-4.99315535615592,4.5673502809935,25.4616742266001));
#54395=CARTESIAN_POINT('Ctrl Pts',(-5.10819986744137,4.4415803964038,25.4696792197614));
#54396=CARTESIAN_POINT('Ctrl Pts',(-5.21860602822786,4.31133324155964,25.4776842129228));
#54397=CARTESIAN_POINT('Ctrl Pts',(-5.32400067600738,4.17699722311051,25.4856892060842));
#54398=CARTESIAN_POINT('Ctrl Pts',(-5.42933373903935,4.04273970058085,25.4936895217264));
#54399=CARTESIAN_POINT('Ctrl Pts',(-5.5296608857929,3.9043983655855,25.5016898373686));
#54400=CARTESIAN_POINT('Ctrl Pts',(-5.62464782667414,3.7623962877254,25.5096901530109));
#54401=CARTESIAN_POINT('Ctrl Pts',(-5.71961342979113,3.62042610905937,25.5176886714708));
#54402=CARTESIAN_POINT('Ctrl Pts',(-5.80924099902817,3.47479713290247,25.5256871899307));
#54403=CARTESIAN_POINT('Ctrl Pts',(-5.89323832783158,3.32596317047812,25.5336857083907));
#54404=CARTESIAN_POINT('Ctrl Pts',(-5.97722837469604,3.17714211084298,25.541683533439));
#54405=CARTESIAN_POINT('Ctrl Pts',(-6.0555889660689,3.02511694561341,25.5496813584873));
#54406=CARTESIAN_POINT('Ctrl Pts',(-6.12807296701681,2.870367696118,25.5576791835357));
#54407=CARTESIAN_POINT('Ctrl Pts',(-6.20056526889467,2.71560072460584,25.5656779245018));
#54408=CARTESIAN_POINT('Ctrl Pts',(-6.26717948091634,2.55810938944274,25.5736766654679));
#54409=CARTESIAN_POINT('Ctrl Pts',(-6.32771598043466,2.39839518656785,25.581675406434));
#54410=CARTESIAN_POINT('Ctrl Pts',(-6.38827159765289,2.2386305452265,25.5896766734386));
#54411=CARTESIAN_POINT('Ctrl Pts',(-6.44274554949837,2.07664199166433,25.5976779404432));
#54412=CARTESIAN_POINT('Ctrl Pts',(-6.49098765538635,1.91294753133014,25.6056792074478));
#54413=CARTESIAN_POINT('Ctrl Pts',(-6.53928378200302,1.74906976859098,25.6136894341417));
#54414=CARTESIAN_POINT('Ctrl Pts',(-6.58133402071878,1.58348264631413,25.6216996608354));
#54415=CARTESIAN_POINT('Ctrl Pts',(-6.61703886627128,1.41671650031164,25.6297098875292));
#54416=CARTESIAN_POINT('Ctrl Pts',(-6.65276478283154,1.2498519382342,25.6377248414119));
#54417=CARTESIAN_POINT('Ctrl Pts',(-6.68213778570095,1.08180733729416,25.6457397952946));
#54418=CARTESIAN_POINT('Ctrl Pts',(-6.70511019851716,0.91311895486905,25.6537547491773));
#54419=CARTESIAN_POINT('Ctrl Pts',(-6.7281183001261,0.744168506601595,25.6617821546918));
#54420=CARTESIAN_POINT('Ctrl Pts',(-6.74470591615529,0.574572653351214,
25.6698095602064));
#54421=CARTESIAN_POINT('Ctrl Pts',(-6.75487747544724,0.404869474887251,
25.677836965721));
#54422=CARTESIAN_POINT('Ctrl Pts',(-6.76304726415453,0.268564010679525,
25.6842845717408));
#54423=CARTESIAN_POINT('Ctrl Pts',(-6.76707888580151,0.132189369752193,
25.6907321777606));
#54424=CARTESIAN_POINT('Ctrl Pts',(-6.76699883050778,-0.00397843013914469,
25.6971797837804));
#54425=CARTESIAN_POINT('',(-6.76699952998211,-0.00142798523079344,25.3028202161898));
#54426=CARTESIAN_POINT('Ctrl Pts',(3.09908550384736,6.01564277861004,24.6513967904261));
#54427=CARTESIAN_POINT('Ctrl Pts',(2.93373232018338,6.10082796552476,24.6601462383254));
#54428=CARTESIAN_POINT('Ctrl Pts',(2.76486502144429,6.1791915818019,24.6688956862247));
#54429=CARTESIAN_POINT('Ctrl Pts',(2.59305716434347,6.25046746591381,24.677645134124));
#54430=CARTESIAN_POINT('Ctrl Pts',(2.42125069459276,6.32174277447227,24.6863945113714));
#54431=CARTESIAN_POINT('Ctrl Pts',(2.2465039787105,6.38593035557829,24.6951438886188));
#54432=CARTESIAN_POINT('Ctrl Pts',(2.06941053323761,6.44281220003542,24.7038932658662));
#54433=CARTESIAN_POINT('Ctrl Pts',(1.89231845896684,6.49969360406685,24.7126425753688));
#54434=CARTESIAN_POINT('Ctrl Pts',(1.71287996431518,6.54926929700877,24.7213918848714));
#54435=CARTESIAN_POINT('Ctrl Pts',(1.53170449173529,6.59137090065473,24.730141194374));
#54436=CARTESIAN_POINT('Ctrl Pts',(1.35053036178195,6.63347219230078,24.7388904390386));
#54437=CARTESIAN_POINT('Ctrl Pts',(1.16761955878869,6.6680994406245,24.7476396837032));
#54438=CARTESIAN_POINT('Ctrl Pts',(0.983593309310725,6.69513503985388,24.7563889283678));
#54439=CARTESIAN_POINT('Ctrl Pts',(0.799568362460165,6.72217044771212,24.7651381111009));
#54440=CARTESIAN_POINT('Ctrl Pts',(0.614428268438725,6.74161427235976,24.7738872938341));
#54441=CARTESIAN_POINT('Ctrl Pts',(0.428801816330343,6.75340047696802,24.7826364765673));
#54442=CARTESIAN_POINT('Ctrl Pts',(0.243176616522904,6.76518660206241,24.7913856002754));
#54443=CARTESIAN_POINT('Ctrl Pts',(0.057065351165626,6.76931519233997,24.8001347239836));
#54444=CARTESIAN_POINT('Ctrl Pts',(-0.128899900799819,6.76577222610796,
24.8088838476917));
#54445=CARTESIAN_POINT('Ctrl Pts',(-0.314863959941826,6.76222928260134,
24.817632915281));
#54446=CARTESIAN_POINT('Ctrl Pts',(-0.500681721080501,6.75101488651278,
24.8263819828702));
#54447=CARTESIAN_POINT('Ctrl Pts',(-0.685722110173135,6.73216712415993,
24.8351310504595));
#54448=CARTESIAN_POINT('Ctrl Pts',(-0.870761373827479,6.71331947644147,
24.8438800648359));
#54449=CARTESIAN_POINT('Ctrl Pts',(-1.05502298984333,6.68683858439998,24.8526290792122));
#54450=CARTESIAN_POINT('Ctrl Pts',(-1.23788117676052,6.65281438131427,24.8613780935886));
#54451=CARTESIAN_POINT('Ctrl Pts',(-1.4300964145179,6.61704912302378,24.8705748044761));
#54452=CARTESIAN_POINT('Ctrl Pts',(-1.62076048992696,6.57294837083165,24.8797715153636));
#54453=CARTESIAN_POINT('Ctrl Pts',(-1.80915798961136,6.52067760042048,24.8889682262512));
#54454=CARTESIAN_POINT('Ctrl Pts',(-1.98840443003007,6.4709457857741,24.8977182239577));
#54455=CARTESIAN_POINT('Ctrl Pts',(-2.16559895952177,6.4138188847448,24.9064682216642));
#54456=CARTESIAN_POINT('Ctrl Pts',(-2.34013966242298,6.34949095285243,24.9152182193707));
#54457=CARTESIAN_POINT('Ctrl Pts',(-2.5146768255398,6.28516432556698,24.9239680396222));
#54458=CARTESIAN_POINT('Ctrl Pts',(-2.68656000078796,6.21363705879681,24.9327178598738));
#54459=CARTESIAN_POINT('Ctrl Pts',(-2.85520533840832,6.13515211510886,24.9414676801254));
#54460=CARTESIAN_POINT('Ctrl Pts',(-3.02384747998256,6.05666865881156,24.9502173345567));
#54461=CARTESIAN_POINT('Ctrl Pts',(-3.18925164684452,5.97122791039889,24.9589669889879));
#54462=CARTESIAN_POINT('Ctrl Pts',(-3.35085601829059,5.87912008251964,24.9677166434192));
#54463=CARTESIAN_POINT('Ctrl Pts',(-3.51245754191326,5.7870138777823,24.9764661436623));
#54464=CARTESIAN_POINT('Ctrl Pts',(-3.67025915510851,5.68824097061038,24.9852156439054));
#54465=CARTESIAN_POINT('Ctrl Pts',(-3.82372487928755,5.58313684656909,24.9939651441486));
#54466=CARTESIAN_POINT('Ctrl Pts',(-3.9771881030072,5.4780344350183,25.0027145018337));
#54467=CARTESIAN_POINT('Ctrl Pts',(-4.12631534262948,5.36660117496436,25.0114638595188));
#54468=CARTESIAN_POINT('Ctrl Pts',(-4.27060009886148,5.24921554097413,25.0202132172039));
#54469=CARTESIAN_POINT('Ctrl Pts',(-4.41488269594138,5.13183166360356,25.0289624439591));
#54470=CARTESIAN_POINT('Ctrl Pts',(-4.55432273235015,5.00849577139537,25.0377116707143));
#54471=CARTESIAN_POINT('Ctrl Pts',(-4.68844662480136,4.87962675277411,25.0464608974695));
#54472=CARTESIAN_POINT('Ctrl Pts',(-4.82256868835098,4.75075949139943,25.055210004921));
#54473=CARTESIAN_POINT('Ctrl Pts',(-4.95137454637813,4.61635945312579,25.0639591123725));
#54474=CARTESIAN_POINT('Ctrl Pts',(-5.07442674461039,4.47688309134635,25.072708219824));
#54475=CARTESIAN_POINT('Ctrl Pts',(-5.19747742838508,4.33740844616389,25.0814572195963));
#54476=CARTESIAN_POINT('Ctrl Pts',(-5.31477440450904,4.19285781736059,25.0902062193687));
#54477=CARTESIAN_POINT('Ctrl Pts',(-5.42591931531137,4.04372211999428,25.0989552191411));
#54478=CARTESIAN_POINT('Ctrl Pts',(-5.53707636462969,3.89457013500819,25.1077051744217));
#54479=CARTESIAN_POINT('Ctrl Pts',(-5.64207983273461,3.74083230916434,25.1164551297023));
#54480=CARTESIAN_POINT('Ctrl Pts',(-5.74057303468741,3.58303087251837,25.1252050849828));
#54481=CARTESIAN_POINT('Ctrl Pts',(-5.83906243363764,3.42523552887433,25.1339547024116));
#54482=CARTESIAN_POINT('Ctrl Pts',(-5.93104191768429,3.26337713156987,25.1427043198404));
#54483=CARTESIAN_POINT('Ctrl Pts',(-6.01619906699663,3.09800545291142,25.1514539372693));
#54484=CARTESIAN_POINT('Ctrl Pts',(-6.1013533809538,2.932639280396,25.1602032633746));
#54485=CARTESIAN_POINT('Ctrl Pts',(-6.17968568352828,2.76376031540248,25.16895258948));
#54486=CARTESIAN_POINT('Ctrl Pts',(-6.25092992694868,2.59194213831585,25.1777019155854));
#54487=CARTESIAN_POINT('Ctrl Pts',(-6.32217217691085,2.42012876880867,25.1864509968792));
#54488=CARTESIAN_POINT('Ctrl Pts',(-6.38632665483832,2.24537661647722,25.195200078173));
#54489=CARTESIAN_POINT('Ctrl Pts',(-6.44317547869332,2.06827917621512,25.2039491594668));
#54490=CARTESIAN_POINT('Ctrl Pts',(-6.50002944235916,1.89116572423491,25.2126990317818));
#54491=CARTESIAN_POINT('Ctrl Pts',(-6.54957634250377,1.71170683289277,25.2214489040967));
#54492=CARTESIAN_POINT('Ctrl Pts',(-6.59164787708374,1.53051209225456,25.2301987764117));
#54493=CARTESIAN_POINT('Ctrl Pts',(-6.63371649074992,1.34932993148116,25.2389480412465));
#54494=CARTESIAN_POINT('Ctrl Pts',(-6.6683107125711,1.16641244174083,25.2476973060813));
#54495=CARTESIAN_POINT('Ctrl Pts',(-6.69531304840322,0.982380875160746,
25.2564465709161));
#54496=CARTESIAN_POINT('Ctrl Pts',(-6.72231677033035,0.798339861796578,
25.2651962848717));
#54497=CARTESIAN_POINT('Ctrl Pts',(-6.74172778477883,0.613184940730891,
25.2739459988274));
#54498=CARTESIAN_POINT('Ctrl Pts',(-6.75348015835513,0.427545027691289,
25.282695712783));
#54499=CARTESIAN_POINT('Ctrl Pts',(-6.76249038365212,0.285219953548558,
25.2894038805853));
#54500=CARTESIAN_POINT('Ctrl Pts',(-6.76699999999992,0.142609995760042,
25.2961120483875));
#54501=CARTESIAN_POINT('Ctrl Pts',(-6.767,3.65565930388384E-12,25.3028202161898));
#54502=CARTESIAN_POINT('Ctrl Pts',(-6.7669985337519,-0.00445468289831136,
25.3028202161898));
#54503=CARTESIAN_POINT('Ctrl Pts',(-6.76686772084466,-0.203169332550661,
25.3121622732703));
#54504=CARTESIAN_POINT('Ctrl Pts',(-6.75797960988083,-0.401695375614664,
25.3215043303508));
#54505=CARTESIAN_POINT('Ctrl Pts',(-6.74040959930496,-0.599305793061871,
25.3308463874314));
#54506=CARTESIAN_POINT('Ctrl Pts',(-6.722962658811,-0.795532037736014,25.3401230075718));
#54507=CARTESIAN_POINT('Ctrl Pts',(-6.69695515512968,-0.990855271405463,
25.3493996277122));
#54508=CARTESIAN_POINT('Ctrl Pts',(-6.66251242258052,-1.18457469961173,
25.3586762478526));
#54509=CARTESIAN_POINT('Ctrl Pts',(-6.6277052533626,-1.38034386248957,25.3680510234032));
#54510=CARTESIAN_POINT('Ctrl Pts',(-6.58428339171561,-1.57447489642017,
25.3774257989537));
#54511=CARTESIAN_POINT('Ctrl Pts',(-6.53242827667237,-1.76625870419121,
25.3868005745043));
#54512=CARTESIAN_POINT('Ctrl Pts',(-6.4805731616291,-1.95804251196238,25.3961753500549));
#54513=CARTESIAN_POINT('Ctrl Pts',(-6.42028487035499,-2.14747891495456,
25.4055501256055));
#54514=CARTESIAN_POINT('Ctrl Pts',(-6.3517960376486,-2.33387576706891,25.4149249011561));
#54515=CARTESIAN_POINT('Ctrl Pts',(-6.28857685275979,-2.5059309268791,25.4235783654568));
#54516=CARTESIAN_POINT('Ctrl Pts',(-6.21832248720098,-2.67552548039541,
25.4322318297576));
#54517=CARTESIAN_POINT('Ctrl Pts',(-6.1412427471693,-2.84208137116805,25.4408852940583));
#54518=CARTESIAN_POINT('Ctrl Pts',(-6.06423401334421,-3.00848382989767,
25.4495307867484));
#54519=CARTESIAN_POINT('Ctrl Pts',(-5.98041257299404,-3.1718529340812,25.4581762794385));
#54520=CARTESIAN_POINT('Ctrl Pts',(-5.89003649211402,-3.33163009975075,
25.4668217721287));
#54521=CARTESIAN_POINT('Ctrl Pts',(-5.796941601983,-3.49621388717122,25.4757273496253));
#54522=CARTESIAN_POINT('Ctrl Pts',(-5.6968916447697,-3.65698593828745,25.4846329271219));
#54523=CARTESIAN_POINT('Ctrl Pts',(-5.59022108859942,-3.81336035283559,
25.4935385046184));
#54524=CARTESIAN_POINT('Ctrl Pts',(-5.48686230754852,-3.96487984851949,
25.5021675927909));
#54525=CARTESIAN_POINT('Ctrl Pts',(-5.3772880352706,-4.11227039426033,25.5107966809634));
#54526=CARTESIAN_POINT('Ctrl Pts',(-5.26184817134888,-4.25502559588923,
25.5194257691359));
#54527=CARTESIAN_POINT('Ctrl Pts',(-5.14085999989243,-4.40464194352013,
25.5284695912945));
#54528=CARTESIAN_POINT('Ctrl Pts',(-5.01342867388619,-4.54916609599658,
25.5375134134532));
#54529=CARTESIAN_POINT('Ctrl Pts',(-4.88000714049934,-4.68805069391058,
25.5465572356118));
#54530=CARTESIAN_POINT('Ctrl Pts',(-4.74658560711241,-4.82693529182466,
25.5556010577705));
#54531=CARTESIAN_POINT('Ctrl Pts',(-4.6071741083085,-4.96018003330942,25.5646448799291));
#54532=CARTESIAN_POINT('Ctrl Pts',(-4.46227354144581,-5.08727862823658,
25.5736887020878));
#54533=CARTESIAN_POINT('Ctrl Pts',(-4.32727511886633,-5.20569162135824,
25.5821144919376));
#54534=CARTESIAN_POINT('Ctrl Pts',(-4.1875714748537,-5.31871809721675,25.5905402817875));
#54535=CARTESIAN_POINT('Ctrl Pts',(-4.04362535160469,-5.42599143160583,
25.5989660716373));
#54536=CARTESIAN_POINT('Ctrl Pts',(-3.8996458280128,-5.53328965701711,25.6073938165538));
#54537=CARTESIAN_POINT('Ctrl Pts',(-3.75142212824965,-5.63483188122655,
25.6158215614703));
#54538=CARTESIAN_POINT('Ctrl Pts',(-3.59944737237399,-5.73029385053768,
25.6242493063868));
#54539=CARTESIAN_POINT('Ctrl Pts',(-3.44741677340041,-5.82579089733304,
25.6326801480768));
#54540=CARTESIAN_POINT('Ctrl Pts',(-3.29163265064257,-5.91520305821385,
25.6411109897667));
#54541=CARTESIAN_POINT('Ctrl Pts',(-3.13261452676403,-5.99825101397957,
25.6495418314567));
#54542=CARTESIAN_POINT('Ctrl Pts',(-2.97345028552638,-6.08137528021658,
25.657980420014));
#54543=CARTESIAN_POINT('Ctrl Pts',(-2.81104640017321,-6.15812350423278,
25.6664190085714));
#54544=CARTESIAN_POINT('Ctrl Pts',(-2.64594528120833,-6.22826320645261,
25.6748575971288));
#54545=CARTESIAN_POINT('Ctrl Pts',(-2.48075759051284,-6.29843968683267,
25.683300610509));
#54546=CARTESIAN_POINT('Ctrl Pts',(-2.31287015332307,-6.36200061214593,
25.6917436238893));
#54547=CARTESIAN_POINT('Ctrl Pts',(-2.14284304546279,-6.41876255071893,
25.7001866372696));
#54548=CARTESIAN_POINT('Ctrl Pts',(-1.97263731227475,-6.47558412166472,
25.7086385206239));
#54549=CARTESIAN_POINT('Ctrl Pts',(-1.80028773467195,-6.5255923401309,25.7170904039782));
#54550=CARTESIAN_POINT('Ctrl Pts',(-1.62636818537994,-6.56865401171229,
25.7255422873325));
#54551=CARTESIAN_POINT('Ctrl Pts',(-1.5789696136712,-6.58038967763747,25.7278456925614));
#54552=CARTESIAN_POINT('Ctrl Pts',(-1.53145448793498,-6.59160969352032,
25.7301490977903));
#54553=CARTESIAN_POINT('Ctrl Pts',(-1.48383452985272,-6.60231202595097,
25.7324525030192));
#54554=CARTESIAN_POINT('Ctrl Pts',(-1.31188570314621,-6.64095661067097,
25.7407697683526));
#54555=CARTESIAN_POINT('Ctrl Pts',(-1.13826014071322,-6.67291702549273,
25.749087033686));
#54556=CARTESIAN_POINT('Ctrl Pts',(-0.963512074390253,-6.69805445502679,
25.7574042990194));
#54557=CARTESIAN_POINT('Ctrl Pts',(-0.788911394614725,-6.72317068307331,
25.7657145493795));
#54558=CARTESIAN_POINT('Ctrl Pts',(-0.613190439782572,-6.74147534203104,
25.7740247997395));
#54559=CARTESIAN_POINT('Ctrl Pts',(-0.436914447371334,-6.75288047914949,
25.7823350500996));
#54560=CARTESIAN_POINT('Ctrl Pts',(-0.260754847280388,-6.76427808563172,
25.7906398133295));
#54561=CARTESIAN_POINT('Ctrl Pts',(-0.0840412858169509,-6.76878522558246,
25.7989445765594));
#54562=CARTESIAN_POINT('Ctrl Pts',(0.0926548189229739,-6.76636564815488,
25.8072493397893));
#54563=CARTESIAN_POINT('Ctrl Pts',(0.269266599297139,-6.76394722541789,
25.8155501397518));
#54564=CARTESIAN_POINT('Ctrl Pts',(0.445860592470569,-6.75460867784938,
25.8238509397144));
#54565=CARTESIAN_POINT('Ctrl Pts',(0.621864083055294,-6.73836583024444,
25.832151739677));
#54566=CARTESIAN_POINT('Ctrl Pts',(0.797815787426847,-6.72212776183772,
25.8404500972619));
#54567=CARTESIAN_POINT('Ctrl Pts',(0.973176989590091,-6.69898947466501,
25.8487484548469));
#54568=CARTESIAN_POINT('Ctrl Pts',(1.14737857352802,-6.6690187740783,25.8570468124318));
#54569=CARTESIAN_POINT('Ctrl Pts',(1.32159788207783,-6.6390450240415,25.8653460143556));
#54570=CARTESIAN_POINT('Ctrl Pts',(1.49465699260167,-6.60223752310994,25.8736452162794));
#54571=CARTESIAN_POINT('Ctrl Pts',(1.66599489619299,-6.5587155759233,25.8819444182031));
#54572=CARTESIAN_POINT('Ctrl Pts',(1.83735017019983,-6.51518921643622,25.8902444615087));
#54573=CARTESIAN_POINT('Ctrl Pts',(2.00698355202321,-6.46494713903994,25.8985445048142));
#54574=CARTESIAN_POINT('Ctrl Pts',(2.17434724937158,-6.40815909908222,25.9068445481197));
#54575=CARTESIAN_POINT('Ctrl Pts',(2.34175569696578,-6.35135587495501,25.9151468107177));
#54576=CARTESIAN_POINT('Ctrl Pts',(2.50689292103439,-6.28800331158205,25.9234490733155));
#54577=CARTESIAN_POINT('Ctrl Pts',(2.66922904968405,-6.21832013330954,25.9317513359135));
#54578=CARTESIAN_POINT('Ctrl Pts',(2.83163553567381,-6.14860675397758,25.9400571967561));
#54579=CARTESIAN_POINT('Ctrl Pts',(2.99123818721352,-6.0725574286115,25.9483630575987));
#54580=CARTESIAN_POINT('Ctrl Pts',(3.14752959060519,-5.99043792024129,25.9566689184413));
#54581=CARTESIAN_POINT('Ctrl Pts',(3.30400574146244,-5.90822134081843,25.9649845973974));
#54582=CARTESIAN_POINT('Ctrl Pts',(3.45716251556301,-5.81992040418544,25.9733002763535));
#54583=CARTESIAN_POINT('Ctrl Pts',(3.60651845478899,-5.72584610649522,25.9816159553096));
#54584=CARTESIAN_POINT('Ctrl Pts',(3.75596886045715,-5.63171230756086,25.9899368938665));
#54585=CARTESIAN_POINT('Ctrl Pts',(3.90161335059677,-5.53179806185756,25.9982578324233));
#54586=CARTESIAN_POINT('Ctrl Pts',(4.04300158438589,-5.42645622747048,26.0065787709802));
#54587=CARTESIAN_POINT('Ctrl Pts',(4.18459996488499,-5.3209578224882,26.0149120770291));
#54588=CARTESIAN_POINT('Ctrl Pts',(4.32192917608692,-5.2100159255991,26.023245383078));
#54589=CARTESIAN_POINT('Ctrl Pts',(4.45457291710652,-5.09402288237706,26.031578689127));
#54590=CARTESIAN_POINT('Ctrl Pts',(4.55220654180502,-5.00864515431748,26.0377124943787));
#54591=CARTESIAN_POINT('Ctrl Pts',(4.647302394389,-4.92053160836058,26.0438462996305));
#54592=CARTESIAN_POINT('Ctrl Pts',(4.73970804784577,-4.82985057959209,26.0499801048822));
#54593=CARTESIAN_POINT('Ctrl Pts',(4.86130372692857,-4.71052431696045,26.0580515181242));
#54594=CARTESIAN_POINT('Ctrl Pts',(4.97861389964261,-4.58638355881354,26.0661229313663));
#54595=CARTESIAN_POINT('Ctrl Pts',(5.09122289490461,-4.45777281098972,26.0741943446083));
#54596=CARTESIAN_POINT('Ctrl Pts',(5.20369051890032,-4.32932352330712,26.0822556248595));
#54597=CARTESIAN_POINT('Ctrl Pts',(5.31146846621601,-4.196415688837,26.0903169051108));
#54598=CARTESIAN_POINT('Ctrl Pts',(5.41417512671915,-4.05943305120502,26.098378185362));
#54599=CARTESIAN_POINT('Ctrl Pts',(5.51677537156268,-3.92259234300262,26.1064311132196));
#54600=CARTESIAN_POINT('Ctrl Pts',(5.61431456421166,-3.78168552932459,26.1144840410772));
#54601=CARTESIAN_POINT('Ctrl Pts',(5.70644896334461,-3.63713200595514,26.1225369689349));
#54602=CARTESIAN_POINT('Ctrl Pts',(5.79850807618911,-3.49269660240151,26.1305833164592));
#54603=CARTESIAN_POINT('Ctrl Pts',(5.88517098631676,-3.34462073299806,26.1386296639837));
#54604=CARTESIAN_POINT('Ctrl Pts',(5.96613524311391,-3.19335548614214,26.146676011508));
#54605=CARTESIAN_POINT('Ctrl Pts',(6.04705105193752,-3.04218075447116,26.1547175442012));
#54606=CARTESIAN_POINT('Ctrl Pts',(6.12227482020028,-2.88782077258248,26.1627590768943));
#54607=CARTESIAN_POINT('Ctrl Pts',(6.19154838686063,-2.73075403014691,26.1708006095875));
#54608=CARTESIAN_POINT('Ctrl Pts',(6.26215371965539,-2.57066772081876,26.1789967386357));
#54609=CARTESIAN_POINT('Ctrl Pts',(6.32657752879682,-2.40776985285506,26.187192867684));
#54610=CARTESIAN_POINT('Ctrl Pts',(6.38459630624366,-2.24259202850179,26.1953889967322));
#54611=CARTESIAN_POINT('Ctrl Pts',(6.4415010769077,-2.08058575006514,26.2034277535683));
#54612=CARTESIAN_POINT('Ctrl Pts',(6.49224444280832,-1.91638664810777,26.2114665104044));
#54613=CARTESIAN_POINT('Ctrl Pts',(6.53666485547006,-1.75051465782568,26.2195052672405));
#54614=CARTESIAN_POINT('Ctrl Pts',(6.58108956755827,-1.58462661288805,26.2275448021433));
#54615=CARTESIAN_POINT('Ctrl Pts',(6.61919001109639,-1.41706571796878,26.2355843370461));
#54616=CARTESIAN_POINT('Ctrl Pts',(6.65085514182505,-1.24836488354137,26.2436238719489));
#54617=CARTESIAN_POINT('Ctrl Pts',(6.68252960711064,-1.07961431783208,26.2516657768245));
#54618=CARTESIAN_POINT('Ctrl Pts',(6.70776491467035,-0.909723510592241,
26.2597076817));
#54619=CARTESIAN_POINT('Ctrl Pts',(6.72650156553943,-0.739233176200573,
26.2677495865755));
#54620=CARTESIAN_POINT('Ctrl Pts',(6.74587024640452,-0.562991813724064,
26.2760627632563));
#54621=CARTESIAN_POINT('Ctrl Pts',(6.75829412475733,-0.38611020372354,26.2843759399371));
#54622=CARTESIAN_POINT('Ctrl Pts',(6.76376593097555,-0.209187549759847,
26.2926891166179));
#54623=CARTESIAN_POINT('Ctrl Pts',(6.7690683740941,-0.0377409978145964,
26.3007449842285));
#54624=CARTESIAN_POINT('Ctrl Pts',(6.76784276946827,0.133743727256565,26.308800851839));
#54625=CARTESIAN_POINT('Ctrl Pts',(6.76013545925107,0.30472540520346,26.3168567194496));
#54626=CARTESIAN_POINT('Ctrl Pts',(6.75205888511553,0.483898963661559,26.3252985506655));
#54627=CARTESIAN_POINT('Ctrl Pts',(6.73686427849205,0.662519602094777,26.3337403818815));
#54628=CARTESIAN_POINT('Ctrl Pts',(6.71466525655449,0.839975887999223,26.3421822130974));
#54629=CARTESIAN_POINT('Ctrl Pts',(6.69246623461694,1.01743217390354,26.3506240443134));
#54630=CARTESIAN_POINT('Ctrl Pts',(6.66326295715326,1.19372366636151,26.3590658755293));
#54631=CARTESIAN_POINT('Ctrl Pts',(6.62722876856082,1.3682572306258,26.3675077067453));
#54632=CARTESIAN_POINT('Ctrl Pts',(6.59209409591994,1.53843394015663,26.3757388058167));
#54633=CARTESIAN_POINT('Ctrl Pts',(6.55034898385465,1.70750556831118,26.3839699048881));
#54634=CARTESIAN_POINT('Ctrl Pts',(6.50207382812475,1.87491998058988,26.3922010039595));
#54635=CARTESIAN_POINT('Ctrl Pts',(6.45385670486078,2.04213314087821,26.400422208273));
#54636=CARTESIAN_POINT('Ctrl Pts',(6.39912526794902,2.20769271110237,26.4086434125866));
#54637=CARTESIAN_POINT('Ctrl Pts',(6.33801114870739,2.37105539346107,26.4168646169001));
#54638=CARTESIAN_POINT('Ctrl Pts',(6.27695823368949,2.53425447228129,26.4250775878883));
#54639=CARTESIAN_POINT('Ctrl Pts',(6.20953549166139,2.69526071143631,26.4332905588765));
#54640=CARTESIAN_POINT('Ctrl Pts',(6.13592473550519,2.85354457477284,26.4415035298647));
#54641=CARTESIAN_POINT('Ctrl Pts',(6.06237293462631,3.01170166765429,26.4497099230373));
#54642=CARTESIAN_POINT('Ctrl Pts',(5.98264314217222,3.16714040415081,26.4579163162098));
#54643=CARTESIAN_POINT('Ctrl Pts',(5.89696581801861,3.31934980698331,26.4661227093823));
#54644=CARTESIAN_POINT('Ctrl Pts',(5.81134215802297,3.47146387316146,26.4743239624646));
#54645=CARTESIAN_POINT('Ctrl Pts',(5.71977856480075,3.62035232456767,26.482525215547));
#54646=CARTESIAN_POINT('Ctrl Pts',(5.62255212312826,3.76552740299495,26.4907264686293));
#54647=CARTESIAN_POINT('Ctrl Pts',(5.52535826973602,3.91065382175661,26.4989249728222));
#54648=CARTESIAN_POINT('Ctrl Pts',(5.42250554695334,4.05206904863729,26.5071234770151));
#54649=CARTESIAN_POINT('Ctrl Pts',(5.31431530047584,4.18931281800827,26.515321981208));
#54650=CARTESIAN_POINT('Ctrl Pts',(5.20614166420548,4.32653551664957,26.5235192267028));
#54651=CARTESIAN_POINT('Ctrl Pts',(5.09263235859772,4.45958775218417,26.5317164721977));
#54652=CARTESIAN_POINT('Ctrl Pts',(4.97415012139717,4.58804092939508,26.5399137176925));
#54653=CARTESIAN_POINT('Ctrl Pts',(4.85566455259991,4.71649771857513,26.5481111936853));
#54654=CARTESIAN_POINT('Ctrl Pts',(4.73220601761551,4.84035492916575,26.5563086696782));
#54655=CARTESIAN_POINT('Ctrl Pts',(4.60417537458037,4.95921950715107,26.564506145671));
#54656=CARTESIAN_POINT('Ctrl Pts',(4.47607211847807,5.07815149963482,26.5727082708936));
#54657=CARTESIAN_POINT('Ctrl Pts',(4.3433918367202,5.19208495826923,26.5809103961162));
#54658=CARTESIAN_POINT('Ctrl Pts',(4.2065703390607,5.30066552260513,26.5891125213388));
#54659=CARTESIAN_POINT('Ctrl Pts',(4.06970592182169,5.4092801476131,26.5973172194886));
#54660=CARTESIAN_POINT('Ctrl Pts',(3.92869798623901,5.51253831644174,26.6055219176385));
#54661=CARTESIAN_POINT('Ctrl Pts',(3.78401277938467,5.61012800972077,26.6137266157884));
#54662=CARTESIAN_POINT('Ctrl Pts',(3.63919306417103,5.70780842844307,26.6219389415355));
#54663=CARTESIAN_POINT('Ctrl Pts',(3.49068955190514,5.79980965362521,26.6301512672826));
#54664=CARTESIAN_POINT('Ctrl Pts',(3.33899528572142,5.88586437848598,26.6383635930298));
#54665=CARTESIAN_POINT('Ctrl Pts',(3.25986902722478,5.93075195779596,26.6426472790666));
#54666=CARTESIAN_POINT('Ctrl Pts',(3.1798750075793,5.97402235846659,26.6469309651035));
#54667=CARTESIAN_POINT('Ctrl Pts',(3.09908550384733,6.01564277861006,26.6512146511404));
#54668=CARTESIAN_POINT('Origin',(0.,0.,-63.6971797838103));
#54669=CARTESIAN_POINT('',(3.09908550384738,6.01564277861003,29.0457563580462));
#54670=CARTESIAN_POINT('',(3.09908550384705,6.0156427786102,28.6513967904261));
#54671=CARTESIAN_POINT('',(3.09908550384721,6.01564277861012,-63.6971797838103));
#54672=CARTESIAN_POINT('',(-6.76699784670241,0.00324515999788631,27.6971797838099));
#54673=CARTESIAN_POINT('Ctrl Pts',(-6.767,4.30010947876278E-12,27.6971797838099));
#54674=CARTESIAN_POINT('Ctrl Pts',(-6.76700000000012,-0.186007249555743,
27.7059292956227));
#54675=CARTESIAN_POINT('Ctrl Pts',(-6.7593263729427,-0.372014355811964,
27.7146788074354));
#54676=CARTESIAN_POINT('Ctrl Pts',(-6.74400518263396,-0.557389537582383,
27.7234283192481));
#54677=CARTESIAN_POINT('Ctrl Pts',(-6.72868405703772,-0.742763936378962,
27.7321777941054));
#54678=CARTESIAN_POINT('Ctrl Pts',(-6.70571545643614,-0.927506130401384,
27.7409272689626));
#54679=CARTESIAN_POINT('Ctrl Pts',(-6.67517739401632,-1.11098864009201,
27.7496767438198));
#54680=CARTESIAN_POINT('Ctrl Pts',(-6.64463945804457,-1.29447039004188,
27.7584261824483));
#54681=CARTESIAN_POINT('Ctrl Pts',(-6.60653217002804,-1.47669218338917,
27.7671756210768));
#54682=CARTESIAN_POINT('Ctrl Pts',(-6.56098496085573,-1.65703510627414,
27.7759250597053));
#54683=CARTESIAN_POINT('Ctrl Pts',(-6.51543793649655,-1.83737729739661,
27.7846744628319));
#54684=CARTESIAN_POINT('Ctrl Pts',(-6.46245112156998,-2.01584035544626,
27.7934238659586));
#54685=CARTESIAN_POINT('Ctrl Pts',(-6.40220448361822,-2.19181813797104,
27.8021732690852));
#54686=CARTESIAN_POINT('Ctrl Pts',(-6.34195808512075,-2.36779522106032,
27.8109226374368));
#54687=CARTESIAN_POINT('Ctrl Pts',(-6.27445201416452,-2.54128677725506,
27.8196720057883));
#54688=CARTESIAN_POINT('Ctrl Pts',(-6.19991555052815,-2.71170355428452,
27.8284213741398));
#54689=CARTESIAN_POINT('Ctrl Pts',(-6.12537937695205,-2.88211966813338,
27.837170708443));
#54690=CARTESIAN_POINT('Ctrl Pts',(-6.04381298028427,-3.04946076419718,
27.8459200427462));
#54691=CARTESIAN_POINT('Ctrl Pts',(-5.95549339308946,-3.21315848424378,
27.8546693770494));
#54692=CARTESIAN_POINT('Ctrl Pts',(-5.86717414225764,-3.37685558085162,
27.863418678031));
#54693=CARTESIAN_POINT('Ctrl Pts',(-5.7721018884401,-3.53690907700093,27.8721679790125));
#54694=CARTESIAN_POINT('Ctrl Pts',(-5.67059953311303,-3.69277537024097,
27.8809172799941));
#54695=CARTESIAN_POINT('Ctrl Pts',(-5.56909755592626,-3.84864108281145,
27.8896665483807));
#54696=CARTESIAN_POINT('Ctrl Pts',(-5.4611656815487,-4.0003193835496,27.8984158167673));
#54697=CARTESIAN_POINT('Ctrl Pts',(-5.34717048488266,-4.14729511918307,
27.907165085154));
#54698=CARTESIAN_POINT('Ctrl Pts',(-5.23317570343178,-4.29427031947334,
27.9159143216723));
#54699=CARTESIAN_POINT('Ctrl Pts',(-5.11311781951404,-4.43654276249722,
27.9246635581907));
#54700=CARTESIAN_POINT('Ctrl Pts',(-4.98740458929083,-4.57362924412558,
27.933412794709));
#54701=CARTESIAN_POINT('Ctrl Pts',(-4.86169180652574,-4.7107152378144,27.9421620000858));
#54702=CARTESIAN_POINT('Ctrl Pts',(-4.73032391141401,-4.84261509584657,
27.9509112054625));
#54703=CARTESIAN_POINT('Ctrl Pts',(-4.59374706947151,-4.96888084599762,
27.9596604108392));
#54704=CARTESIAN_POINT('Ctrl Pts',(-4.45717070231365,-5.09514615720865,
27.9684095858009));
#54705=CARTESIAN_POINT('Ctrl Pts',(-4.31538563497257,-5.21577720520669,
27.9771587607626));
#54706=CARTESIAN_POINT('Ctrl Pts',(-4.16887340951974,-5.33036429293527,
27.9859079357243));
#54707=CARTESIAN_POINT('Ctrl Pts',(-4.02236168122458,-5.44495099183725,
27.9946570809975));
#54708=CARTESIAN_POINT('Ctrl Pts',(-3.8711230526316,-5.55349359497943,28.0034062262707));
#54709=CARTESIAN_POINT('Ctrl Pts',(-3.71567116928981,-5.65562346357221,
28.012155371544));
#54710=CARTESIAN_POINT('Ctrl Pts',(-3.56021980053315,-5.75775299408924,
28.0209044878554));
#54711=CARTESIAN_POINT('Ctrl Pts',(-3.40055544442108,-5.85346967519865,
28.0296536041667));
#54712=CARTESIAN_POINT('Ctrl Pts',(-3.23722035886887,-5.94244843041359,
28.0384027204781));
#54713=CARTESIAN_POINT('Ctrl Pts',(-3.07388580043541,-6.03142689847425,
28.0471518085541));
#54714=CARTESIAN_POINT('Ctrl Pts',(-2.90688078789281,-6.11366734707874,
28.0559008966301));
#54715=CARTESIAN_POINT('Ctrl Pts',(-2.73677250610458,-6.188890470014,28.0646499847061));
#54716=CARTESIAN_POINT('Ctrl Pts',(-2.56666475917022,-6.26411335643298,
28.0733990452733));
#54717=CARTESIAN_POINT('Ctrl Pts',(-2.39345402457202,-6.33231884545214,
28.0821481058404));
#54718=CARTESIAN_POINT('Ctrl Pts',(-2.21772855944197,-6.39327529804837,
28.0908971664076));
#54719=CARTESIAN_POINT('Ctrl Pts',(-2.04200363223743,-6.45423156404654,
28.0996462001924));
#54720=CARTESIAN_POINT('Ctrl Pts',(-1.86376426061207,-6.50793874412403,
28.1083952339772));
#54721=CARTESIAN_POINT('Ctrl Pts',(-1.68361577621881,-6.55421443943263,
28.117144267762));
#54722=CARTESIAN_POINT('Ctrl Pts',(-1.50346782833454,-6.60048999692532,
28.1258932754909));
#54723=CARTESIAN_POINT('Ctrl Pts',(-1.32141105657673,-6.63933404265104,
28.1346422832197));
#54724=CARTESIAN_POINT('Ctrl Pts',(-1.13806375346868,-6.67061465631472,
28.1433912909486));
#54725=CARTESIAN_POINT('Ctrl Pts',(-0.954716981173318,-6.70189517941724,
28.152140273348));
#54726=CARTESIAN_POINT('Ctrl Pts',(-0.770079967445574,-6.72561226608966,
28.1608892557475));
#54727=CARTESIAN_POINT('Ctrl Pts',(-0.584779764076339,-6.74168536995957,
28.1696382381469));
#54728=CARTESIAN_POINT('Ctrl Pts',(-0.391489587596211,-6.75845153117854,
28.1787644685625));
#54729=CARTESIAN_POINT('Ctrl Pts',(-0.197478091808471,-6.76689985146385,
28.1878906989781));
#54730=CARTESIAN_POINT('Ctrl Pts',(-0.00346214753424312,-6.76699911434415,
28.1970169293937));
#54731=CARTESIAN_POINT('Ctrl Pts',(0.184490798481499,-6.76709527525944,
28.2058579651089));
#54732=CARTESIAN_POINT('Ctrl Pts',(0.372447602151712,-6.7593563379078,28.214699000824));
#54733=CARTESIAN_POINT('Ctrl Pts',(0.559756448191226,-6.74380914014538,
28.2235400365391));
#54734=CARTESIAN_POINT('Ctrl Pts',(0.745136131040457,-6.72842206873187,
28.2322900151524));
#54735=CARTESIAN_POINT('Ctrl Pts',(0.929880851942236,-6.70538686355763,
28.2410399937658));
#54736=CARTESIAN_POINT('Ctrl Pts',(1.11336305057191,-6.67478177303357,28.2497899723791));
#54737=CARTESIAN_POINT('Ctrl Pts',(1.29684337089858,-6.64417699581312,28.2585398614191));
#54738=CARTESIAN_POINT('Ctrl Pts',(1.47906091204931,-6.60600253548118,28.267289750459));
#54739=CARTESIAN_POINT('Ctrl Pts',(1.65939671094969,-6.56038806441276,28.276039639499));
#54740=CARTESIAN_POINT('Ctrl Pts',(1.83973072368907,-6.51477404513921,28.2847894418745));
#54741=CARTESIAN_POINT('Ctrl Pts',(2.01818275356783,-6.4617202328874,28.29353924425));
#54742=CARTESIAN_POINT('Ctrl Pts',(2.19414664033073,-6.40140683918195,28.3022890466255));
#54743=CARTESIAN_POINT('Ctrl Pts',(2.37010884270997,-6.34109402281595,28.311038765245));
#54744=CARTESIAN_POINT('Ctrl Pts',(2.54358267847536,-6.27352185699901,28.3197884838646));
#54745=CARTESIAN_POINT('Ctrl Pts',(2.71397890841464,-6.19891986435383,28.3285382024841));
#54746=CARTESIAN_POINT('Ctrl Pts',(2.88437356388674,-6.1243185610337,28.3372878402559));
#54747=CARTESIAN_POINT('Ctrl Pts',(3.05169040786914,-6.04268767582687,28.3460374780277));
#54748=CARTESIAN_POINT('Ctrl Pts',(3.21536112511806,-5.95430447954079,28.3547871157996));
#54749=CARTESIAN_POINT('Ctrl Pts',(3.37903038442588,-5.86592207055189,28.3635366756316));
#54750=CARTESIAN_POINT('Ctrl Pts',(3.53905332979713,-5.77078760703536,28.3722862354637));
#54751=CARTESIAN_POINT('Ctrl Pts',(3.69488643041626,-5.66922422085472,28.3810357952957));
#54752=CARTESIAN_POINT('Ctrl Pts',(3.85071819468482,-5.56766170563338,28.3897852800957));
#54753=CARTESIAN_POINT('Ctrl Pts',(4.0023599459897,-5.45967053456438,28.3985347648957));
#54754=CARTESIAN_POINT('Ctrl Pts',(4.14929662974053,-5.34561750206876,28.4072842496957));
#54755=CARTESIAN_POINT('Ctrl Pts',(4.29623210224798,-5.23156540974668,28.4160336623711));
#54756=CARTESIAN_POINT('Ctrl Pts',(4.43846235841872,-5.11145173172399,28.4247830750464));
#54757=CARTESIAN_POINT('Ctrl Pts',(4.57550431797185,-4.98568443006785,28.4335324877218));
#54758=CARTESIAN_POINT('Ctrl Pts',(4.71254519337256,-4.8599181233692,28.4422818311797));
#54759=CARTESIAN_POINT('Ctrl Pts',(4.84439764314752,-4.72849847631338,28.4510311746376));
#54760=CARTESIAN_POINT('Ctrl Pts',(4.97061384196461,-4.59187184425588,28.4597805180955));
#54761=CARTESIAN_POINT('Ctrl Pts',(5.09682908419996,-4.45524624767989,28.4685297952428));
#54762=CARTESIAN_POINT('Ctrl Pts',(5.21740796649975,-4.3134139555713,28.4772790723902));
#54763=CARTESIAN_POINT('Ctrl Pts',(5.33194095942069,-4.16685668163089,28.4860283495376));
#54764=CARTESIAN_POINT('Ctrl Pts',(5.44647312234952,-4.02030046975459,28.4947775632811));
#54765=CARTESIAN_POINT('Ctrl Pts',(5.5549593071211,-3.86901957035803,28.5035267770247));
#54766=CARTESIAN_POINT('Ctrl Pts',(5.6570310607962,-3.71352778058641,28.5122759907682));
#54767=CARTESIAN_POINT('Ctrl Pts',(5.75910210868564,-3.5580370659788,28.5210251440144));
#54768=CARTESIAN_POINT('Ctrl Pts',(5.85475865698382,-3.39833575881187,28.5297742972606));
#54769=CARTESIAN_POINT('Ctrl Pts',(5.943675830689,-3.23496624707019,28.5385234505068));
#54770=CARTESIAN_POINT('Ctrl Pts',(6.03259241909927,-3.07159781070396,28.5472725461619));
#54771=CARTESIAN_POINT('Ctrl Pts',(6.11476958470828,-2.90456146976127,28.556021641817));
#54772=CARTESIAN_POINT('Ctrl Pts',(6.18992823574258,-2.73442451648547,28.5647707374721));
#54773=CARTESIAN_POINT('Ctrl Pts',(6.26508641700816,-2.56428862662706,28.5735197784423));
#54774=CARTESIAN_POINT('Ctrl Pts',(6.33322605570187,-2.39105242531567,28.5822688194124));
#54775=CARTESIAN_POINT('Ctrl Pts',(6.39411573747667,-2.21530425354018,28.5910178603825));
#54776=CARTESIAN_POINT('Ctrl Pts',(6.45500505889026,-2.03955712188874,28.5997668495735));
#54777=CARTESIAN_POINT('Ctrl Pts',(6.50864441544832,-1.8612983202591,28.6085158387645));
#54778=CARTESIAN_POINT('Ctrl Pts',(6.55485164049813,-1.68113324012671,28.6172648279555));
#54779=CARTESIAN_POINT('Ctrl Pts',(6.60199852639029,-1.49730435913254,28.6261917348324));
#54780=CARTESIAN_POINT('Ctrl Pts',(6.64140767440941,-1.31149113174,28.6351186417092));
#54781=CARTESIAN_POINT('Ctrl Pts',(6.67293975269545,-1.12435050446772,28.6440455485861));
#54782=CARTESIAN_POINT('Ctrl Pts',(6.7038466483146,-0.940920291567091,28.6527954627701));
#54783=CARTESIAN_POINT('Ctrl Pts',(6.72718585889629,-0.756215114281222,
28.6615453769541));
#54784=CARTESIAN_POINT('Ctrl Pts',(6.74287810451837,-0.570862389378351,
28.6702952911381));
#54785=CARTESIAN_POINT('Ctrl Pts',(6.75857004154105,-0.385513309571343,
28.6790450332487));
#54786=CARTESIAN_POINT('Ctrl Pts',(6.76661529035546,-0.199516993262481,
28.6877947753593));
#54787=CARTESIAN_POINT('Ctrl Pts',(6.76698652348896,-0.0135052182083492,
28.6965445174699));
#54788=CARTESIAN_POINT('Ctrl Pts',(6.76735774981532,0.172503146034585,28.7052940991405));
#54789=CARTESIAN_POINT('Ctrl Pts',(6.76005524147502,0.358526681829154,28.7140436808111));
#54790=CARTESIAN_POINT('Ctrl Pts',(6.74510380214916,0.543933542110543,28.7227932624818));
#54791=CARTESIAN_POINT('Ctrl Pts',(6.73015261711027,0.729337249080307,28.7315426953437));
#54792=CARTESIAN_POINT('Ctrl Pts',(6.70755278444666,0.91412401585016,28.7402921282056));
#54793=CARTESIAN_POINT('Ctrl Pts',(6.67738106408364,1.09766621748927,28.7490415610676));
#54794=CARTESIAN_POINT('Ctrl Pts',(6.64720981677343,1.28120554142862,28.7577908567499));
#54795=CARTESIAN_POINT('Ctrl Pts',(6.60946696581625,1.46350005650159,28.7665401524323));
#54796=CARTESIAN_POINT('Ctrl Pts',(6.5642807001111,1.64393062206072,28.7752894481146));
#54797=CARTESIAN_POINT('Ctrl Pts',(6.51909508282871,1.82435859844187,28.7840386182446));
#54798=CARTESIAN_POINT('Ctrl Pts',(6.46646633415806,2.00292240086095,28.7927877883746));
#54799=CARTESIAN_POINT('Ctrl Pts',(6.40657319597352,2.17901557695983,28.8015369585046));
#54800=CARTESIAN_POINT('Ctrl Pts',(6.34668083768471,2.3551064600696,28.8102860147076));
#54801=CARTESIAN_POINT('Ctrl Pts',(6.27952437144077,2.52872650996053,28.8190350709107));
#54802=CARTESIAN_POINT('Ctrl Pts',(6.20533187335345,2.69928607997445,28.8277841271138));
#54803=CARTESIAN_POINT('Ctrl Pts',(6.12831449784469,2.87633970114936,28.8368663034026));
#54804=CARTESIAN_POINT('Ctrl Pts',(6.04371489463377,3.05009490561907,28.8459484796915));
#54805=CARTESIAN_POINT('Ctrl Pts',(5.9518426512072,3.21991584599208,28.8550306559803));
#54806=CARTESIAN_POINT('Ctrl Pts',(5.86333281335734,3.38352155904882,28.8637804363347));
#54807=CARTESIAN_POINT('Ctrl Pts',(5.76807337235938,3.54347560903412,28.8725302166892));
#54808=CARTESIAN_POINT('Ctrl Pts',(5.66638790086621,3.6992346717824,28.8812799970436));
#54809=CARTESIAN_POINT('Ctrl Pts',(5.56470608503021,3.85498813489362,28.8900294628378));
#54810=CARTESIAN_POINT('Ctrl Pts',(5.45659885767243,4.00654667255865,28.8987789286321));
#54811=CARTESIAN_POINT('Ctrl Pts',(5.34243340580811,4.1533955150582,28.9075283944264));
#54812=CARTESIAN_POINT('Ctrl Pts',(5.22827145140903,4.30023985883495,28.9162775921802));
#54813=CARTESIAN_POINT('Ctrl Pts',(5.10805181978403,4.44237456992682,28.9250267899341));
#54814=CARTESIAN_POINT('Ctrl Pts',(4.9821828128287,4.57931691626102,28.933775987688));
#54815=CARTESIAN_POINT('Ctrl Pts',(4.85631699296544,4.71625579511838,28.942524963906));
#54816=CARTESIAN_POINT('Ctrl Pts',(4.72480227792148,4.84800236135468,28.951273940124));
#54817=CARTESIAN_POINT('Ctrl Pts',(4.58808530848417,4.97410918678628,28.960022916342));
#54818=CARTESIAN_POINT('Ctrl Pts',(4.45135945057278,5.10022421088741,28.9687724613632));
#54819=CARTESIAN_POINT('Ctrl Pts',(4.3094308720835,5.2206985661173,28.9775220063844));
#54820=CARTESIAN_POINT('Ctrl Pts',(4.16278164322781,5.33512305301439,28.9862715514056));
#54821=CARTESIAN_POINT('Ctrl Pts',(4.01614103534698,5.44954081331201,28.9950205820729));
#54822=CARTESIAN_POINT('Ctrl Pts',(3.86478055833713,5.55790924068129,29.0037696127402));
#54823=CARTESIAN_POINT('Ctrl Pts',(3.70921425812244,5.65986029751099,29.0125186434074));
#54824=CARTESIAN_POINT('Ctrl Pts',(3.55364584530422,5.76181273884467,29.0212677928873));
#54825=CARTESIAN_POINT('Ctrl Pts',(3.39387173464656,5.85734747817882,29.0300169423671));
#54826=CARTESIAN_POINT('Ctrl Pts',(3.23043456092726,5.94614005448633,29.038766091847));
#54827=CARTESIAN_POINT('Ctrl Pts',(3.18690768806613,5.96978744811164,29.0410961805801));
#54828=CARTESIAN_POINT('Ctrl Pts',(3.14312114983002,5.99295688499238,29.0434262693131));
#54829=CARTESIAN_POINT('Ctrl Pts',(3.09908550384738,6.01564277861003,29.0457563580462));
#54830=CARTESIAN_POINT('Ctrl Pts',(3.09908550384735,6.01564277861005,27.0459166703402));
#54831=CARTESIAN_POINT('Ctrl Pts',(2.93605479406775,6.09963149402321,27.0545480454384));
#54832=CARTESIAN_POINT('Ctrl Pts',(2.76952358531319,6.1770322731653,27.0631794205365));
#54833=CARTESIAN_POINT('Ctrl Pts',(2.60004025099926,6.24756590146784,27.0718107956347));
#54834=CARTESIAN_POINT('Ctrl Pts',(2.43067166116671,6.31805177672946,27.0804363270747));
#54835=CARTESIAN_POINT('Ctrl Pts',(2.25835521155813,6.38167965649669,27.0890618585148));
#54836=CARTESIAN_POINT('Ctrl Pts',(2.08366127629973,6.43821750841403,27.0976873899548));
#54837=CARTESIAN_POINT('Ctrl Pts',(1.90910481826852,6.49471086727498,27.1063061334423));
#54838=CARTESIAN_POINT('Ctrl Pts',(1.73217489681239,6.54412523909033,27.1149248769297));
#54839=CARTESIAN_POINT('Ctrl Pts',(1.55345949011609,6.58627759911228,27.1235436204172));
#54840=CARTESIAN_POINT('Ctrl Pts',(1.46810051161555,6.60641062770436,27.1276601493368));
#54841=CARTESIAN_POINT('Ctrl Pts',(1.38233446969443,6.62488772612642,27.1317766782565));
#54842=CARTESIAN_POINT('Ctrl Pts',(1.29622666598318,6.64169296417669,27.1358932071761));
#54843=CARTESIAN_POINT('Ctrl Pts',(1.11997957221407,6.67609024570984,27.1443189970259));
#54844=CARTESIAN_POINT('Ctrl Pts',(0.942376881392607,6.70346498969645,27.1527447868757));
#54845=CARTESIAN_POINT('Ctrl Pts',(0.764002966958121,6.7237332239225,27.1611705767256));
#54846=CARTESIAN_POINT('Ctrl Pts',(0.585587663774305,6.74400616106078,27.1695983216421));
#54847=CARTESIAN_POINT('Ctrl Pts',(0.406401109563409,6.75716926324582,27.1780260665587));
#54848=CARTESIAN_POINT('Ctrl Pts',(0.227032608423332,6.76319045973958,27.1864538114752));
#54849=CARTESIAN_POINT('Ctrl Pts',(0.047598198358595,6.76921386872095,27.1948846531652));
#54850=CARTESIAN_POINT('Ctrl Pts',(-0.132017960781943,6.76809012829394,
27.2033154948552));
#54851=CARTESIAN_POINT('Ctrl Pts',(-0.31122635973812,6.75983928455434,27.2117463365451));
#54852=CARTESIAN_POINT('Ctrl Pts',(-0.490599428339162,6.75158085934247,
27.2201849251025));
#54853=CARTESIAN_POINT('Ctrl Pts',(-0.669563656796403,6.73618226199444,
27.2286235136598));
#54854=CARTESIAN_POINT('Ctrl Pts',(-0.847533326702103,6.71371553315519,
27.2370621022172));
#54855=CARTESIAN_POINT('Ctrl Pts',(-1.02559631603796,6.69123702375618,27.2455051155975));
#54856=CARTESIAN_POINT('Ctrl Pts',(-1.20266337921886,6.66168304044586,27.2539481289778));
#54857=CARTESIAN_POINT('Ctrl Pts',(-1.37815821303781,6.62517689875798,27.2623911423581));
#54858=CARTESIAN_POINT('Ctrl Pts',(-1.5538374164115,6.58863240482382,27.2708430257124));
#54859=CARTESIAN_POINT('Ctrl Pts',(-1.72794076836931,6.54512123785287,27.2792949090668));
#54860=CARTESIAN_POINT('Ctrl Pts',(-1.8999053223626,6.49481706948381,27.2877467924211));
#54861=CARTESIAN_POINT('Ctrl Pts',(-1.94677109608751,6.48110759437712,27.2900501976499));
#54862=CARTESIAN_POINT('Ctrl Pts',(-1.9934781158684,6.46689386041559,27.2923536028787));
#54863=CARTESIAN_POINT('Ctrl Pts',(-2.0400152289791,6.45218000876707,27.2946570081074));
#54864=CARTESIAN_POINT('Ctrl Pts',(-2.20805405808109,6.39905040451516,27.3029742734408));
#54865=CARTESIAN_POINT('Ctrl Pts',(-2.37417838005245,6.33930081292399,27.3112915387742));
#54866=CARTESIAN_POINT('Ctrl Pts',(-2.53783939289301,6.27309016481355,27.3196088041076));
#54867=CARTESIAN_POINT('Ctrl Pts',(-2.70136237026249,6.20693536029006,27.3279190544677));
#54868=CARTESIAN_POINT('Ctrl Pts',(-2.86242585707067,6.13433048632257,27.3362293048278));
#54869=CARTESIAN_POINT('Ctrl Pts',(-3.02049713478366,6.05548396569289,27.3445395551879));
#54870=CARTESIAN_POINT('Ctrl Pts',(-3.17846404046859,5.9766895062054,27.3528443184177));
#54871=CARTESIAN_POINT('Ctrl Pts',(-3.33344236368593,5.89166176691848,27.3611490816476));
#54872=CARTESIAN_POINT('Ctrl Pts',(-3.48492006132125,5.80065695987969,27.3694538448775));
#54873=CARTESIAN_POINT('Ctrl Pts',(-3.63632546952663,5.70969558290173,27.3777546448401));
#54874=CARTESIAN_POINT('Ctrl Pts',(-3.78423328394655,5.612763001541,27.3860554448027));
#54875=CARTESIAN_POINT('Ctrl Pts',(-3.92815654496965,5.51016108278262,27.3943562447653));
#54876=CARTESIAN_POINT('Ctrl Pts',(-4.07203745887423,5.40758935299843,27.4026546023502));
#54877=CARTESIAN_POINT('Ctrl Pts',(-4.21193587341536,5.29935181253114,27.4109529599351));
#54878=CARTESIAN_POINT('Ctrl Pts',(-4.34739409618035,5.18579343712187,27.4192513175201));
#54879=CARTESIAN_POINT('Ctrl Pts',(-4.48286610150874,5.07222350740843,27.4275505194438));
#54880=CARTESIAN_POINT('Ctrl Pts',(-4.61389674099209,4.9533318787011,27.4358497213676));
#54881=CARTESIAN_POINT('Ctrl Pts',(-4.74006124268781,4.82950395129447,27.4441489232914));
#54882=CARTESIAN_POINT('Ctrl Pts',(-4.86623853507252,4.7056634700832,27.4524489665969));
#54883=CARTESIAN_POINT('Ctrl Pts',(-4.98754845759794,4.57688593606884,27.4607490099025));
#54884=CARTESIAN_POINT('Ctrl Pts',(-5.10360304661759,4.44359369683545,27.469049053208));
#54885=CARTESIAN_POINT('Ctrl Pts',(-5.21968866668782,4.31026581749291,27.4773513158059));
#54886=CARTESIAN_POINT('Ctrl Pts',(-5.33051592409775,4.1724210893604,27.4856535784038));
#54887=CARTESIAN_POINT('Ctrl Pts',(-5.43573698275921,4.03051515990993,27.4939558410017));
#54888=CARTESIAN_POINT('Ctrl Pts',(-5.54100364478619,3.88854772767617,27.5022617018443));
#54889=CARTESIAN_POINT('Ctrl Pts',(-5.64065905844078,3.7425158654118,27.510567562687));
#54890=CARTESIAN_POINT('Ctrl Pts',(-5.7343984652765,3.5929045689295,27.5188734235296));
#54891=CARTESIAN_POINT('Ctrl Pts',(-5.82824867870474,3.44311642133918,27.5271891024857));
#54892=CARTESIAN_POINT('Ctrl Pts',(-5.91616872833246,3.2897406809609,27.5355047814418));
#54893=CARTESIAN_POINT('Ctrl Pts',(-5.99789904712273,3.13328837174689,27.5438204603979));
#54894=CARTESIAN_POINT('Ctrl Pts',(-6.07968105968878,2.9767371076932,27.5521413989548));
#54895=CARTESIAN_POINT('Ctrl Pts',(-6.15526538532918,2.81710570815055,27.5604623375116));
#54896=CARTESIAN_POINT('Ctrl Pts',(-6.22444041261873,2.65492571454622,27.5687832760684));
#54897=CARTESIAN_POINT('Ctrl Pts',(-6.29371825542564,2.49250467123652,27.5771165821174));
#54898=CARTESIAN_POINT('Ctrl Pts',(-6.35656763837977,2.32752778862264,27.5854498881663));
#54899=CARTESIAN_POINT('Ctrl Pts',(-6.41282623649688,2.16054360300765,27.5937831942152));
#54900=CARTESIAN_POINT('Ctrl Pts',(-6.45423588622814,2.03763338362067,27.599916999467));
#54901=CARTESIAN_POINT('Ctrl Pts',(-6.49207580302994,1.91363596890389,27.6060508047188));
#54902=CARTESIAN_POINT('Ctrl Pts',(-6.52629897085645,1.78877353038278,27.6121846099706));
#54903=CARTESIAN_POINT('Ctrl Pts',(-6.58230854197514,1.58442390191316,27.6222231839337));
#54904=CARTESIAN_POINT('Ctrl Pts',(-6.62877194642737,1.37723941178004,27.6322617578968));
#54905=CARTESIAN_POINT('Ctrl Pts',(-6.66543459182177,1.1680199921858,27.64230033186));
#54906=CARTESIAN_POINT('Ctrl Pts',(-6.70154781580039,0.96193590634854,27.6521884691195));
#54907=CARTESIAN_POINT('Ctrl Pts',(-6.72815180168886,0.753877410366474,
27.662076606379));
#54908=CARTESIAN_POINT('Ctrl Pts',(-6.7450473860383,0.544632683648273,27.6719647436385));
#54909=CARTESIAN_POINT('Ctrl Pts',(-6.75940879799794,0.366772619229647,
27.6803697570289));
#54910=CARTESIAN_POINT('Ctrl Pts',(-6.76675639309456,0.188055855418755,
27.6887747704194));
#54911=CARTESIAN_POINT('Ctrl Pts',(-6.76699404115812,0.00898036360930988,
27.6971797838099));
#54912=CARTESIAN_POINT('',(-6.767,3.80125455851782E-12,27.3028202161898));
#54913=CARTESIAN_POINT('Ctrl Pts',(3.09908550384733,6.01564277861006,26.6512146511404));
#54914=CARTESIAN_POINT('Ctrl Pts',(2.94396840926309,6.09555462791971,26.6594393944729));
#54915=CARTESIAN_POINT('Ctrl Pts',(2.78591789415201,6.1693808510076,26.6676641378053));
#54916=CARTESIAN_POINT('Ctrl Pts',(2.62545871930722,6.23692676830614,26.6758888811378));
#54917=CARTESIAN_POINT('Ctrl Pts',(2.56597851648579,6.26196519234493,26.6789376902947));
#54918=CARTESIAN_POINT('Ctrl Pts',(2.50616749398762,6.28614113728922,26.6819864994515));
#54919=CARTESIAN_POINT('Ctrl Pts',(2.44605286443358,6.30944644040951,26.6850353086083));
#54920=CARTESIAN_POINT('Ctrl Pts',(2.2698740956819,6.37774761168144,26.6939704953906));
#54921=CARTESIAN_POINT('Ctrl Pts',(2.09072110230475,6.43870896745376,26.702905682173));
#54922=CARTESIAN_POINT('Ctrl Pts',(1.90920164027248,6.4920904258013,26.7118408689553));
#54923=CARTESIAN_POINT('Ctrl Pts',(1.72795403824027,6.54539193523809,26.7207626735919));
#54924=CARTESIAN_POINT('Ctrl Pts',(1.54434728680086,6.59113612638472,26.7296844782285));
#54925=CARTESIAN_POINT('Ctrl Pts',(1.35900626864516,6.62913199157953,26.7386062828652));
#54926=CARTESIAN_POINT('Ctrl Pts',(1.17411734118709,6.66703517584826,26.7475063251045));
#54927=CARTESIAN_POINT('Ctrl Pts',(0.987502842551587,6.69722770356834,26.7564063673438));
#54928=CARTESIAN_POINT('Ctrl Pts',(0.799799258886218,6.71956919344426,26.7653064095831));
#54929=CARTESIAN_POINT('Ctrl Pts',(0.612384647647815,6.74187628826801,26.7741927500766));
#54930=CARTESIAN_POINT('Ctrl Pts',(0.423884551130265,6.7563564248753,26.7830790905699));
#54931=CARTESIAN_POINT('Ctrl Pts',(0.234944959542762,6.76292021733108,26.7919654310633));
#54932=CARTESIAN_POINT('Ctrl Pts',(0.046488453510159,6.76946722731531,26.8008290507353));
#54933=CARTESIAN_POINT('Ctrl Pts',(-0.142405047894484,6.76813827328685,
26.8096926704073));
#54934=CARTESIAN_POINT('Ctrl Pts',(-0.331085886631742,6.75889570386119,
26.8185562900792));
#54935=CARTESIAN_POINT('Ctrl Pts',(-0.51020143701945,6.75012169203915,26.8269705632327));
#54936=CARTESIAN_POINT('Ctrl Pts',(-0.689125089154248,6.73421643709939,
26.8353848363862));
#54937=CARTESIAN_POINT('Ctrl Pts',(-0.86729702919699,6.71119101673809,26.8437991095397));
#54938=CARTESIAN_POINT('Ctrl Pts',(-1.04114874807327,6.68872390487581,26.8520093577442));
#54939=CARTESIAN_POINT('Ctrl Pts',(-1.21411755445475,6.65949831652102,26.8602196059488));
#54940=CARTESIAN_POINT('Ctrl Pts',(-1.38564777503169,6.62361451501744,26.8684298541533));
#54941=CARTESIAN_POINT('Ctrl Pts',(-1.5572187717618,6.58772218321884,26.8766420540975));
#54942=CARTESIAN_POINT('Ctrl Pts',(-1.72735015295138,6.54516855778685,26.8848542540417));
#54943=CARTESIAN_POINT('Ctrl Pts',(-1.89549811119315,6.49610467206796,26.8930664539859));
#54944=CARTESIAN_POINT('Ctrl Pts',(-2.06371598399514,6.44702038598247,26.9012820684964));
#54945=CARTESIAN_POINT('Ctrl Pts',(-2.22994844946578,6.39142054646708,26.9094976830069));
#54946=CARTESIAN_POINT('Ctrl Pts',(-2.39366840240841,6.32950555567428,26.9177132975174));
#54947=CARTESIAN_POINT('Ctrl Pts',(-2.55757220568088,6.26752103706111,26.9259381378028));
#54948=CARTESIAN_POINT('Ctrl Pts',(-2.71895752803241,6.19920732882995,26.9341629780882));
#54949=CARTESIAN_POINT('Ctrl Pts',(-2.87731784303245,6.12481273429377,26.9423878183736));
#54950=CARTESIAN_POINT('Ctrl Pts',(-3.03577959331905,6.05037048743374,26.9506179269551));
#54951=CARTESIAN_POINT('Ctrl Pts',(-3.19121215847159,5.9698397530627,26.9588480355366));
#54952=CARTESIAN_POINT('Ctrl Pts',(-3.3431350941232,5.88351397911502,26.9670781441182));
#54953=CARTESIAN_POINT('Ctrl Pts',(-3.49526631845103,5.79706985120648,26.9753195363048));
#54954=CARTESIAN_POINT('Ctrl Pts',(-3.64387800078042,5.70481500142485,26.9835609284915));
#54955=CARTESIAN_POINT('Ctrl Pts',(-3.78851923208803,5.60708578747455,26.9918023206782));
#54956=CARTESIAN_POINT('Ctrl Pts',(-3.85147077077765,5.56455155060807,26.9953891839426));
#54957=CARTESIAN_POINT('Ctrl Pts',(-3.91367065011081,5.52098086674005,26.998976047207));
#54958=CARTESIAN_POINT('Ctrl Pts',(-3.97508375785953,5.47640375775941,27.0025629104715));
#54959=CARTESIAN_POINT('Ctrl Pts',(-4.11858185142801,5.37224472086962,27.0109439883749));
#54960=CARTESIAN_POINT('Ctrl Pts',(-4.25812341298019,5.26234050420493,27.0193250662783));
#54961=CARTESIAN_POINT('Ctrl Pts',(-4.39323229053872,5.14701846133933,27.0277061441818));
#54962=CARTESIAN_POINT('Ctrl Pts',(-4.52821375403582,5.03180517261425,27.0360793183324));
#54963=CARTESIAN_POINT('Ctrl Pts',(-4.6587706055261,4.91118445998857,27.0444524924829));
#54964=CARTESIAN_POINT('Ctrl Pts',(-4.78445752919904,4.78552558777932,27.0528256666335));
#54965=CARTESIAN_POINT('Ctrl Pts',(-4.91004744550775,4.65996370128369,27.061192378222));
#54966=CARTESIAN_POINT('Ctrl Pts',(-5.03077468462145,4.52937164579121,27.0695590898104));
#54967=CARTESIAN_POINT('Ctrl Pts',(-5.14622853284925,4.39415758566852,27.0779258013989));
#54968=CARTESIAN_POINT('Ctrl Pts',(-5.26161302402364,4.25902475323061,27.0862874868191));
#54969=CARTESIAN_POINT('Ctrl Pts',(-5.37173021773203,4.1192757098648,27.0946491722393));
#54970=CARTESIAN_POINT('Ctrl Pts',(-5.47620746828476,3.97535416841095,27.1030108576596));
#54971=CARTESIAN_POINT('Ctrl Pts',(-5.58064435175422,3.83148823420954,27.1113693123588));
#54972=CARTESIAN_POINT('Ctrl Pts',(-5.67944543449643,3.68345329071489,27.119727767058));
#54973=CARTESIAN_POINT('Ctrl Pts',(-5.77227923171137,3.53172499936697,27.1280862217571));
#54974=CARTESIAN_POINT('Ctrl Pts',(-5.86509355306056,3.38002853952784,27.1364429229124));
#54975=CARTESIAN_POINT('Ctrl Pts',(-5.95194290540346,3.22464056698319,27.1447996240677));
#54976=CARTESIAN_POINT('Ctrl Pts',(-6.03253975024757,3.06606476801829,27.1531563252229));
#54977=CARTESIAN_POINT('Ctrl Pts',(-6.1131321930474,2.9074976301578,27.1615125699513));
#54978=CARTESIAN_POINT('Ctrl Pts',(-6.1874726543895,2.74574331735602,27.1698688146796));
#54979=CARTESIAN_POINT('Ctrl Pts',(-6.25531996334364,2.58132933896365,27.178225059408));
#54980=CARTESIAN_POINT('Ctrl Pts',(-6.32317409415783,2.41689882919858,27.1865821443337));
#54981=CARTESIAN_POINT('Ctrl Pts',(-6.38453364155701,2.2498084366913,27.1949392292595));
#54982=CARTESIAN_POINT('Ctrl Pts',(-6.43920581269364,2.08060508068504,27.2032963141852));
#54983=CARTESIAN_POINT('Ctrl Pts',(-6.49391511153665,1.91128681919052,27.2116590743821));
#54984=CARTESIAN_POINT('Ctrl Pts',(-6.54192785242033,1.73985305173175,27.220021834579));
#54985=CARTESIAN_POINT('Ctrl Pts',(-6.58310103126158,1.56686623940997,27.2283845947759));
#54986=CARTESIAN_POINT('Ctrl Pts',(-6.62428763052127,1.39382304194932,27.2367500808187));
#54987=CARTESIAN_POINT('Ctrl Pts',(-6.65863015074845,1.2192261243188,27.2451155668615));
#54988=CARTESIAN_POINT('Ctrl Pts',(-6.68603679320054,1.04364792912585,27.2534810529043));
#54989=CARTESIAN_POINT('Ctrl Pts',(-6.71347283343644,0.867881399669266,
27.2618555122007));
#54990=CARTESIAN_POINT('Ctrl Pts',(-6.73395808035583,0.691131827904614,
27.2702299714969));
#54991=CARTESIAN_POINT('Ctrl Pts',(-6.74745253910463,0.513977852179009,
27.2786044307932));
#54992=CARTESIAN_POINT('Ctrl Pts',(-6.76045950490944,0.343223637627389,
27.2866763592587));
#54993=CARTESIAN_POINT('Ctrl Pts',(-6.76697195104396,0.172094006548877,
27.2947482877242));
#54994=CARTESIAN_POINT('Ctrl Pts',(-6.76699990953827,0.00110648500407755,
27.3028202161897));
#54995=CARTESIAN_POINT('Ctrl Pts',(-6.767,4.18591371480668E-12,27.3028202161898));
#54996=CARTESIAN_POINT('Ctrl Pts',(-6.76700000000012,-0.186007249555859,
27.3115697280026));
#54997=CARTESIAN_POINT('Ctrl Pts',(-6.75932637294269,-0.372014355812083,
27.3203192398153));
#54998=CARTESIAN_POINT('Ctrl Pts',(-6.74400518263395,-0.557389537582502,
27.329068751628));
#54999=CARTESIAN_POINT('Ctrl Pts',(-6.72868405703772,-0.742763936378955,
27.3378182264852));
#55000=CARTESIAN_POINT('Ctrl Pts',(-6.70571545643616,-0.92750613040125,
27.3465677013424));
#55001=CARTESIAN_POINT('Ctrl Pts',(-6.67517739401636,-1.11098864009176,
27.3553171761996));
#55002=CARTESIAN_POINT('Ctrl Pts',(-6.6446394580446,-1.29447039004176,27.3640666148281));
#55003=CARTESIAN_POINT('Ctrl Pts',(-6.60653217002805,-1.47669218338917,
27.3728160534567));
#55004=CARTESIAN_POINT('Ctrl Pts',(-6.5609849608557,-1.65703510627426,27.3815654920852));
#55005=CARTESIAN_POINT('Ctrl Pts',(-6.51543793649651,-1.83737729739674,
27.3903148952118));
#55006=CARTESIAN_POINT('Ctrl Pts',(-6.46245112156994,-2.01584035544639,
27.3990642983385));
#55007=CARTESIAN_POINT('Ctrl Pts',(-6.40220448361817,-2.19181813797117,
27.4078137014651));
#55008=CARTESIAN_POINT('Ctrl Pts',(-6.34195808512075,-2.36779522106032,
27.4165630698166));
#55009=CARTESIAN_POINT('Ctrl Pts',(-6.27445201416456,-2.54128677725495,
27.4253124381682));
#55010=CARTESIAN_POINT('Ctrl Pts',(-6.19991555052824,-2.71170355428429,
27.4340618065197));
#55011=CARTESIAN_POINT('Ctrl Pts',(-6.1253793769522,-2.88211966813304,27.4428111408229));
#55012=CARTESIAN_POINT('Ctrl Pts',(-6.0438129802845,-3.04946076419673,27.4515604751261));
#55013=CARTESIAN_POINT('Ctrl Pts',(-5.95549339308976,-3.21315848424322,
27.4603098094293));
#55014=CARTESIAN_POINT('Ctrl Pts',(-5.86717414225807,-3.37685558085085,
27.4690591104108));
#55015=CARTESIAN_POINT('Ctrl Pts',(-5.77210188844069,-3.53690907699995,
27.4778084113924));
#55016=CARTESIAN_POINT('Ctrl Pts',(-5.67059953311379,-3.6927753702398,27.4865577123739));
#55017=CARTESIAN_POINT('Ctrl Pts',(-5.56909755592719,-3.8486410828101,27.4953069807605));
#55018=CARTESIAN_POINT('Ctrl Pts',(-5.46116568154982,-4.00031938354806,
27.5040562491472));
#55019=CARTESIAN_POINT('Ctrl Pts',(-5.34717048488398,-4.14729511918137,
27.5128055175338));
#55020=CARTESIAN_POINT('Ctrl Pts',(-5.23317570343323,-4.29427031947158,
27.5215547540521));
#55021=CARTESIAN_POINT('Ctrl Pts',(-5.11311781951561,-4.4365427624954,27.5303039905705));
#55022=CARTESIAN_POINT('Ctrl Pts',(-4.98740458929254,-4.57362924412372,
27.5390532270888));
#55023=CARTESIAN_POINT('Ctrl Pts',(-4.86169180652732,-4.71071523781276,
27.5478024324655));
#55024=CARTESIAN_POINT('Ctrl Pts',(-4.73032391141546,-4.84261509584517,
27.5565516378423));
#55025=CARTESIAN_POINT('Ctrl Pts',(-4.5937470694728,-4.96888084599642,27.565300843219));
#55026=CARTESIAN_POINT('Ctrl Pts',(-4.45717070231507,-5.09514615720741,
27.5740500181807));
#55027=CARTESIAN_POINT('Ctrl Pts',(-4.31538563497412,-5.2157772052054,27.5827991931424));
#55028=CARTESIAN_POINT('Ctrl Pts',(-4.16887340952143,-5.33036429293395,
27.5915483681041));
#55029=CARTESIAN_POINT('Ctrl Pts',(-4.0223616812264,-5.4449509918359,27.6002975133773));
#55030=CARTESIAN_POINT('Ctrl Pts',(-3.87112305263356,-5.55349359497806,
27.6090466586505));
#55031=CARTESIAN_POINT('Ctrl Pts',(-3.71567116929191,-5.65562346357083,
27.6177958039238));
#55032=CARTESIAN_POINT('Ctrl Pts',(-3.56021980053529,-5.75775299408792,
27.6265449202351));
#55033=CARTESIAN_POINT('Ctrl Pts',(-3.40055544442325,-5.85346967519738,
27.6352940365465));
#55034=CARTESIAN_POINT('Ctrl Pts',(-3.23722035887108,-5.94244843041239,
27.6440431528579));
#55035=CARTESIAN_POINT('Ctrl Pts',(-3.07388580043764,-6.03142689847311,
27.6527922409339));
#55036=CARTESIAN_POINT('Ctrl Pts',(-2.90688078789508,-6.11366734707766,
27.6615413290099));
#55037=CARTESIAN_POINT('Ctrl Pts',(-2.73677250610687,-6.18889047001298,
27.6702904170859));
#55038=CARTESIAN_POINT('Ctrl Pts',(-2.56666475917254,-6.26411335643203,
27.679039477653));
#55039=CARTESIAN_POINT('Ctrl Pts',(-2.39345402457436,-6.33231884545125,
27.6877885382202));
#55040=CARTESIAN_POINT('Ctrl Pts',(-2.21772855944434,-6.39327529804755,
27.6965375987873));
#55041=CARTESIAN_POINT('Ctrl Pts',(-2.04200363223982,-6.45423156404578,
27.7052866325721));
#55042=CARTESIAN_POINT('Ctrl Pts',(-1.86376426061447,-6.50793874412334,
27.714035666357));
#55043=CARTESIAN_POINT('Ctrl Pts',(-1.68361577622123,-6.55421443943201,
27.7227847001418));
#55044=CARTESIAN_POINT('Ctrl Pts',(-1.50346782833673,-6.60048999692483,
27.7315337078706));
#55045=CARTESIAN_POINT('Ctrl Pts',(-1.32141105657867,-6.63933404265066,
27.7402827155995));
#55046=CARTESIAN_POINT('Ctrl Pts',(-1.13806375347037,-6.67061465631443,
27.7490317233284));
#55047=CARTESIAN_POINT('Ctrl Pts',(-0.954716981174895,-6.70189517941702,
27.7577807057278));
#55048=CARTESIAN_POINT('Ctrl Pts',(-0.770079967447028,-6.7256122660895,
27.7665296881273));
#55049=CARTESIAN_POINT('Ctrl Pts',(-0.584779764077667,-6.74168536995945,
27.7752786705267));
#55050=CARTESIAN_POINT('Ctrl Pts',(-0.391489587597413,-6.75845153117847,
27.7844049009423));
#55051=CARTESIAN_POINT('Ctrl Pts',(-0.197478091809546,-6.76689985146382,
27.793531131358));
#55052=CARTESIAN_POINT('Ctrl Pts',(-0.00346214753518824,-6.76699911434415,
27.8026573617736));
#55053=CARTESIAN_POINT('Ctrl Pts',(0.184490798480555,-6.76709527525946,
27.8114983974887));
#55054=CARTESIAN_POINT('Ctrl Pts',(0.372447602150772,-6.75935633790785,
27.8203394332039));
#55055=CARTESIAN_POINT('Ctrl Pts',(0.55975644819029,-6.74380914014546,27.829180468919));
#55056=CARTESIAN_POINT('Ctrl Pts',(0.745136131039397,-6.72842206873198,
27.8379304475323));
#55057=CARTESIAN_POINT('Ctrl Pts',(0.929880851941056,-6.70538686355779,
27.8466804261456));
#55058=CARTESIAN_POINT('Ctrl Pts',(1.11336305057062,-6.67478177303379,27.8554304047589));
#55059=CARTESIAN_POINT('Ctrl Pts',(1.29684337089742,-6.64417699581335,27.8641802937989));
#55060=CARTESIAN_POINT('Ctrl Pts',(1.47906091204828,-6.60600253548141,27.8729301828389));
#55061=CARTESIAN_POINT('Ctrl Pts',(1.65939671094879,-6.56038806441298,27.8816800718789));
#55062=CARTESIAN_POINT('Ctrl Pts',(1.83973072368831,-6.51477404513943,27.8904298742544));
#55063=CARTESIAN_POINT('Ctrl Pts',(2.01818275356719,-6.4617202328876,27.8991796766299));
#55064=CARTESIAN_POINT('Ctrl Pts',(2.19414664033022,-6.40140683918212,27.9079294790054));
#55065=CARTESIAN_POINT('Ctrl Pts',(2.37010884270947,-6.34109402281614,27.9166791976249));
#55066=CARTESIAN_POINT('Ctrl Pts',(2.54358267847486,-6.27352185699921,27.9254289162444));
#55067=CARTESIAN_POINT('Ctrl Pts',(2.71397890841415,-6.19891986435404,27.934178634864));
#55068=CARTESIAN_POINT('Ctrl Pts',(2.88437356388614,-6.12431856103397,27.9429282726358));
#55069=CARTESIAN_POINT('Ctrl Pts',(3.05169040786844,-6.04268767582723,27.9516779104076));
#55070=CARTESIAN_POINT('Ctrl Pts',(3.21536112511726,-5.95430447954122,27.9604275481794));
#55071=CARTESIAN_POINT('Ctrl Pts',(3.3790303844251,-5.86592207055234,27.9691771080115));
#55072=CARTESIAN_POINT('Ctrl Pts',(3.53905332979635,-5.77078760703584,27.9779266678435));
#55073=CARTESIAN_POINT('Ctrl Pts',(3.6948864304155,-5.66922422085521,27.9866762276756));
#55074=CARTESIAN_POINT('Ctrl Pts',(3.85071819468408,-5.56766170563389,27.9954257124756));
#55075=CARTESIAN_POINT('Ctrl Pts',(4.00235994598897,-5.45967053456491,28.0041751972756));
#55076=CARTESIAN_POINT('Ctrl Pts',(4.14929662973982,-5.34561750206932,28.0129246820756));
#55077=CARTESIAN_POINT('Ctrl Pts',(4.29623210224728,-5.23156540974726,28.0216740947509));
#55078=CARTESIAN_POINT('Ctrl Pts',(4.43846235841804,-5.11145173172458,28.0304235074263));
#55079=CARTESIAN_POINT('Ctrl Pts',(4.57550431797119,-4.98568443006845,28.0391729201016));
#55080=CARTESIAN_POINT('Ctrl Pts',(4.71254519337202,-4.85991812336973,28.0479222635595));
#55081=CARTESIAN_POINT('Ctrl Pts',(4.84439764314707,-4.72849847631384,28.0566716070174));
#55082=CARTESIAN_POINT('Ctrl Pts',(4.97061384196426,-4.59187184425625,28.0654209504753));
#55083=CARTESIAN_POINT('Ctrl Pts',(5.09682908419953,-4.45524624768036,28.0741702276227));
#55084=CARTESIAN_POINT('Ctrl Pts',(5.21740796649926,-4.31341395557189,28.0829195047701));
#55085=CARTESIAN_POINT('Ctrl Pts',(5.33194095942014,-4.16685668163159,28.0916687819174));
#55086=CARTESIAN_POINT('Ctrl Pts',(5.44647312234907,-4.0203004697552,28.100417995661));
#55087=CARTESIAN_POINT('Ctrl Pts',(5.55495930712074,-3.86901957035854,28.1091672094045));
#55088=CARTESIAN_POINT('Ctrl Pts',(5.65703106079593,-3.71352778058683,28.117916423148));
#55089=CARTESIAN_POINT('Ctrl Pts',(5.75910210868538,-3.55803706597922,28.1266655763942));
#55090=CARTESIAN_POINT('Ctrl Pts',(5.85475865698357,-3.3983357588123,28.1354147296404));
#55091=CARTESIAN_POINT('Ctrl Pts',(5.94367583068877,-3.23496624707062,28.1441638828866));
#55092=CARTESIAN_POINT('Ctrl Pts',(6.03259241909898,-3.07159781070451,28.1529129785417));
#55093=CARTESIAN_POINT('Ctrl Pts',(6.11476958470796,-2.90456146976195,28.1616620741969));
#55094=CARTESIAN_POINT('Ctrl Pts',(6.18992823574222,-2.73442451648627,28.170411169852));
#55095=CARTESIAN_POINT('Ctrl Pts',(6.26508641700778,-2.56428862662798,28.1791602108221));
#55096=CARTESIAN_POINT('Ctrl Pts',(6.33322605570147,-2.39105242531672,28.1879092517922));
#55097=CARTESIAN_POINT('Ctrl Pts',(6.39411573747626,-2.21530425354136,28.1966582927623));
#55098=CARTESIAN_POINT('Ctrl Pts',(6.45500505888992,-2.03955712188982,28.2054072819533));
#55099=CARTESIAN_POINT('Ctrl Pts',(6.50864441544805,-1.86129832026005,28.2141562711443));
#55100=CARTESIAN_POINT('Ctrl Pts',(6.55485164049792,-1.68113324012754,28.2229052603353));
#55101=CARTESIAN_POINT('Ctrl Pts',(6.60199852639014,-1.49730435913325,28.2318321672122));
#55102=CARTESIAN_POINT('Ctrl Pts',(6.6414076744093,-1.31149113174059,28.2407590740891));
#55103=CARTESIAN_POINT('Ctrl Pts',(6.67293975269537,-1.12435050446819,28.249685980966));
#55104=CARTESIAN_POINT('Ctrl Pts',(6.70384664831451,-0.940920291567684,
28.25843589515));
#55105=CARTESIAN_POINT('Ctrl Pts',(6.72718585889621,-0.756215114281942,
28.267185809334));
#55106=CARTESIAN_POINT('Ctrl Pts',(6.7428781045183,-0.5708623893792,28.275935723518));
#55107=CARTESIAN_POINT('Ctrl Pts',(6.75857004154099,-0.38551330957232,28.2846854656285));
#55108=CARTESIAN_POINT('Ctrl Pts',(6.76661529035543,-0.199516993263584,
28.2934352077391));
#55109=CARTESIAN_POINT('Ctrl Pts',(6.76698652348895,-0.013505218209579,
28.3021849498497));
#55110=CARTESIAN_POINT('Ctrl Pts',(6.76735774981535,0.172503146033357,28.3109345315204));
#55111=CARTESIAN_POINT('Ctrl Pts',(6.76005524147509,0.358526681827927,28.319684113191));
#55112=CARTESIAN_POINT('Ctrl Pts',(6.74510380214926,0.543933542109321,28.3284336948616));
#55113=CARTESIAN_POINT('Ctrl Pts',(6.73015261711039,0.729337249079217,28.3371831277236));
#55114=CARTESIAN_POINT('Ctrl Pts',(6.7075527844468,0.914124015849204,28.3459325605855));
#55115=CARTESIAN_POINT('Ctrl Pts',(6.67738106408378,1.09766621748845,28.3546819934474));
#55116=CARTESIAN_POINT('Ctrl Pts',(6.64720981677356,1.28120554142793,28.3634312891298));
#55117=CARTESIAN_POINT('Ctrl Pts',(6.60946696581638,1.46350005650103,28.3721805848121));
#55118=CARTESIAN_POINT('Ctrl Pts',(6.56428070011121,1.64393062206029,28.3809298804945));
#55119=CARTESIAN_POINT('Ctrl Pts',(6.5190950828288,1.82435859844156,28.3896790506245));
#55120=CARTESIAN_POINT('Ctrl Pts',(6.46646633415812,2.00292240086077,28.3984282207545));
#55121=CARTESIAN_POINT('Ctrl Pts',(6.40657319597354,2.17901557695978,28.4071773908845));
#55122=CARTESIAN_POINT('Ctrl Pts',(6.34668083768468,2.35510646006967,28.4159264470875));
#55123=CARTESIAN_POINT('Ctrl Pts',(6.2795243714407,2.52872650996072,28.4246755032906));
#55124=CARTESIAN_POINT('Ctrl Pts',(6.20533187335331,2.69928607997475,28.4334245594937));
#55125=CARTESIAN_POINT('Ctrl Pts',(6.12831449784455,2.87633970114966,28.4425067357825));
#55126=CARTESIAN_POINT('Ctrl Pts',(6.04371489463361,3.05009490561937,28.4515889120714));
#55127=CARTESIAN_POINT('Ctrl Pts',(5.95184265120704,3.21991584599238,28.4606710883602));
#55128=CARTESIAN_POINT('Ctrl Pts',(5.86333281335717,3.38352155904912,28.4694208687146));
#55129=CARTESIAN_POINT('Ctrl Pts',(5.7680733723592,3.54347560903441,28.4781706490691));
#55130=CARTESIAN_POINT('Ctrl Pts',(5.66638790086602,3.69923467178269,28.4869204294235));
#55131=CARTESIAN_POINT('Ctrl Pts',(5.56470608502994,3.85498813489401,28.4956698952178));
#55132=CARTESIAN_POINT('Ctrl Pts',(5.45659885767208,4.00654667255914,28.504419361012));
#55133=CARTESIAN_POINT('Ctrl Pts',(5.34243340580766,4.15339551505878,28.5131688268063));
#55134=CARTESIAN_POINT('Ctrl Pts',(5.22827145140856,4.30023985883551,28.5219180245602));
#55135=CARTESIAN_POINT('Ctrl Pts',(5.10805181978355,4.44237456992737,28.530667222314));
#55136=CARTESIAN_POINT('Ctrl Pts',(4.9821828128282,4.57931691626157,28.5394164200679));
#55137=CARTESIAN_POINT('Ctrl Pts',(4.85631699296501,4.71625579511881,28.5481653962859));
#55138=CARTESIAN_POINT('Ctrl Pts',(4.72480227792113,4.84800236135502,28.5569143725039));
#55139=CARTESIAN_POINT('Ctrl Pts',(4.58808530848391,4.97410918678653,28.5656633487219));
#55140=CARTESIAN_POINT('Ctrl Pts',(4.4513594505726,5.10022421088756,28.5744128937431));
#55141=CARTESIAN_POINT('Ctrl Pts',(4.30943087208342,5.22069856611737,28.5831624387643));
#55142=CARTESIAN_POINT('Ctrl Pts',(4.16278164322782,5.33512305301438,28.5919119837855));
#55143=CARTESIAN_POINT('Ctrl Pts',(4.01614103534699,5.449540813312,28.6006610144528));
#55144=CARTESIAN_POINT('Ctrl Pts',(3.86478055833715,5.55790924068128,28.6094100451201));
#55145=CARTESIAN_POINT('Ctrl Pts',(3.70921425812245,5.65986029751098,28.6181590757873));
#55146=CARTESIAN_POINT('Ctrl Pts',(3.55364584530423,5.76181273884466,28.6269082252672));
#55147=CARTESIAN_POINT('Ctrl Pts',(3.39387173464657,5.85734747817882,28.635657374747));
#55148=CARTESIAN_POINT('Ctrl Pts',(3.23043456092727,5.94614005448632,28.6444065242269));
#55149=CARTESIAN_POINT('Ctrl Pts',(3.18690768806603,5.9697874481117,28.64673661296));
#55150=CARTESIAN_POINT('Ctrl Pts',(3.1431211498298,5.9929568849925,28.6490667016931));
#55151=CARTESIAN_POINT('Ctrl Pts',(3.09908550384705,6.0156427786102,28.6513967904262));
#55152=CARTESIAN_POINT('Origin',(0.,0.,-63.6971797838103));
#55153=CARTESIAN_POINT('',(3.09908550384736,6.01564277861005,31.0457633158951));
#55154=CARTESIAN_POINT('',(3.09908550384718,6.01564277861014,30.6513967904261));
#55155=CARTESIAN_POINT('',(3.09908550384721,6.01564277861012,-63.6971797838103));
#55156=CARTESIAN_POINT('',(-6.76829295411965,-0.00242009354003358,29.6949426053424));
#55157=CARTESIAN_POINT('Ctrl Pts',(-6.7669982393656,-0.00488143655476046,
29.6971797838099));
#55158=CARTESIAN_POINT('Ctrl Pts',(-6.76685599634114,-0.20206894176599,
29.7064249492294));
#55159=CARTESIAN_POINT('Ctrl Pts',(-6.75809085851693,-0.398938330293628,
29.715670114649));
#55160=CARTESIAN_POINT('Ctrl Pts',(-6.74080995914764,-0.59478575525652,
29.7249152800685));
#55161=CARTESIAN_POINT('Ctrl Pts',(-6.72341233013775,-0.791956097449425,
29.7342228950639));
#55162=CARTESIAN_POINT('Ctrl Pts',(-6.69738357825563,-0.988090451151311,
29.7435305100593));
#55163=CARTESIAN_POINT('Ctrl Pts',(-6.6628831636456,-1.18248760991732,29.7528381250547));
#55164=CARTESIAN_POINT('Ctrl Pts',(-6.62827458067607,-1.3774942576415,29.7621749220022));
#55165=CARTESIAN_POINT('Ctrl Pts',(-6.58514122922429,-1.57075264470449,
29.7715117189497));
#55166=CARTESIAN_POINT('Ctrl Pts',(-6.53369301835144,-1.76157444973117,
29.7808485158971));
#55167=CARTESIAN_POINT('Ctrl Pts',(-6.48202976119589,-1.95319386305431,
29.7902243393422));
#55168=CARTESIAN_POINT('Ctrl Pts',(-6.4219820771575,-2.14235612770112,29.7996001627872));
#55169=CARTESIAN_POINT('Ctrl Pts',(-6.35381039694746,-2.32838623077066,
29.8089759862322));
#55170=CARTESIAN_POINT('Ctrl Pts',(-6.29103291597426,-2.4996963880076,29.8176099318254));
#55171=CARTESIAN_POINT('Ctrl Pts',(-6.22136680736831,-2.66835060517495,
29.8262438774186));
#55172=CARTESIAN_POINT('Ctrl Pts',(-6.14505012808121,-2.83383978435076,
29.8348778230117));
#55173=CARTESIAN_POINT('Ctrl Pts',(-6.07370575265772,-2.98854675323271,
29.8429492362537));
#55174=CARTESIAN_POINT('Ctrl Pts',(-5.99638391577799,-3.14084231455015,
29.8510206494958));
#55175=CARTESIAN_POINT('Ctrl Pts',(-5.91326881104139,-3.29021898486487,
29.8590920627378));
#55176=CARTESIAN_POINT('Ctrl Pts',(-5.83025805043447,-3.43940812514268,
29.867153342989));
#55177=CARTESIAN_POINT('Ctrl Pts',(-5.74146867235082,-3.58568534391104,
29.8752146232402));
#55178=CARTESIAN_POINT('Ctrl Pts',(-5.64713329442595,-3.72856199559374,
29.8832759034915));
#55179=CARTESIAN_POINT('Ctrl Pts',(-5.55289565856978,-3.87129061098495,
29.8913288313491));
#55180=CARTESIAN_POINT('Ctrl Pts',(-5.45312366189551,-4.01062536229669,
29.8993817592067));
#55181=CARTESIAN_POINT('Ctrl Pts',(-5.34809625418465,-4.14610123561595,
29.9074346870644));
#55182=CARTESIAN_POINT('Ctrl Pts',(-5.24315466809728,-4.28146640678951,
29.9154810345887));
#55183=CARTESIAN_POINT('Ctrl Pts',(-5.13296644561109,-4.41297868270579,
29.9235273821131));
#55184=CARTESIAN_POINT('Ctrl Pts',(-5.01785429461257,-4.54020123761472,
29.9315737296375));
#55185=CARTESIAN_POINT('Ctrl Pts',(-4.90281102524929,-4.66734766417798,
29.9396152623306));
#55186=CARTESIAN_POINT('Ctrl Pts',(-4.78284994244122,-4.79020920385607,
29.9476567950239));
#55187=CARTESIAN_POINT('Ctrl Pts',(-4.65833448314634,-4.90838148916012,
29.9556983277171));
#55188=CARTESIAN_POINT('Ctrl Pts',(-4.53142524683287,-5.02882560562792,
29.9638944567653));
#55189=CARTESIAN_POINT('Ctrl Pts',(-4.39978498217611,-5.14439802142215,
29.9720905858135));
#55190=CARTESIAN_POINT('Ctrl Pts',(-4.263838812226,-5.25470908646284,29.9802867148617));
#55191=CARTESIAN_POINT('Ctrl Pts',(-4.13050291712297,-5.3629020911085,29.9883254716978));
#55192=CARTESIAN_POINT('Ctrl Pts',(-3.99302528617483,-5.46603373152687,
29.9963642285339));
#55193=CARTESIAN_POINT('Ctrl Pts',(-3.8518409479282,-5.56377662310985,30.00440298537));
#55194=CARTESIAN_POINT('Ctrl Pts',(-3.71064294452981,-5.66152897517168,
30.0124425202728));
#55195=CARTESIAN_POINT('Ctrl Pts',(-3.56573782647819,-5.75389132716835,
30.0204820551756));
#55196=CARTESIAN_POINT('Ctrl Pts',(-3.41758986525397,-5.84057946722013,
30.0285215900784));
#55197=CARTESIAN_POINT('Ctrl Pts',(-3.26939823152485,-5.92729316204965,
30.036563494954));
#55198=CARTESIAN_POINT('Ctrl Pts',(-3.11796217398246,-6.00832912695545,
30.0446053998295));
#55199=CARTESIAN_POINT('Ctrl Pts',(-2.96377068943838,-6.08344904642309,
30.052647304705));
#55200=CARTESIAN_POINT('Ctrl Pts',(-2.80437797421315,-6.16110293221873,
30.0609604813858));
#55201=CARTESIAN_POINT('Ctrl Pts',(-2.64204107909781,-6.23243447639111,
30.0692736580666));
#55202=CARTESIAN_POINT('Ctrl Pts',(-2.4773216746203,-6.29723481541355,30.0775868347474));
#55203=CARTESIAN_POINT('Ctrl Pts',(-2.31770065773291,-6.3600294572605,30.085642702358));
#55204=CARTESIAN_POINT('Ctrl Pts',(-2.15584279267876,-6.41669112472147,
30.0936985699685));
#55205=CARTESIAN_POINT('Ctrl Pts',(-1.9922732365107,-6.46708097607284,30.101754437579));
#55206=CARTESIAN_POINT('Ctrl Pts',(-1.82086692101523,-6.51988504891404,
30.110196268795));
#55207=CARTESIAN_POINT('Ctrl Pts',(-1.64758133181649,-6.56580141985971,
30.118638100011));
#55208=CARTESIAN_POINT('Ctrl Pts',(-1.47303040899556,-6.60473091156441,
30.1270799312269));
#55209=CARTESIAN_POINT('Ctrl Pts',(-1.29847948617462,-6.6436604032691,30.1355217624429));
#55210=CARTESIAN_POINT('Ctrl Pts',(-1.12266369870626,-6.67560301751157,
30.1439635936588));
#55211=CARTESIAN_POINT('Ctrl Pts',(-0.94619989704853,-6.70052197629598,
30.1524054248748));
#55212=CARTESIAN_POINT('Ctrl Pts',(-0.774154575396528,-6.72481698886525,
30.1606358809414));
#55213=CARTESIAN_POINT('Ctrl Pts',(-0.600921132677589,-6.742517045862,30.1688663370079));
#55214=CARTESIAN_POINT('Ctrl Pts',(-0.427046353577607,-6.7535117096142,
30.1770967930745));
#55215=CARTESIAN_POINT('Ctrl Pts',(-0.253377974086122,-6.76449332205266,
30.1853174791047));
#55216=CARTESIAN_POINT('Ctrl Pts',(-0.0790701284325291,-6.76878536837594,
30.1935381651349));
#55217=CARTESIAN_POINT('Ctrl Pts',(0.0953214214695674,-6.76632860764307,
30.2017588511652));
#55218=CARTESIAN_POINT('Ctrl Pts',(0.269540946664971,-6.76387427032776,
30.2099714280805));
#55219=CARTESIAN_POINT('Ctrl Pts',(0.443843655654126,-6.75468438873625,
30.2181840049959));
#55220=CARTESIAN_POINT('Ctrl Pts',(0.617669798945825,-6.73875159205845,
30.2263965819113));
#55221=CARTESIAN_POINT('Ctrl Pts',(0.791359337635991,-6.72283131647384,
30.234602704816));
#55222=CARTESIAN_POINT('Ctrl Pts',(0.96457270116618,-6.70017871290767,30.2428088277206));
#55223=CARTESIAN_POINT('Ctrl Pts',(1.13675118480139,-6.67083845883354,30.2510149506253));
#55224=CARTESIAN_POINT('Ctrl Pts',(1.30882888172884,-6.64151537942346,30.259216269979));
#55225=CARTESIAN_POINT('Ctrl Pts',(1.47987255306294,-6.60551250809738,30.2674175893327));
#55226=CARTESIAN_POINT('Ctrl Pts',(1.64932956449011,-6.56292625188634,30.2756189086865));
#55227=CARTESIAN_POINT('Ctrl Pts',(1.81873796271549,-6.52035221266325,30.283817875276));
#55228=CARTESIAN_POINT('Ctrl Pts',(1.98656025945274,-6.47119863388872,30.2920168418655));
#55229=CARTESIAN_POINT('Ctrl Pts',(2.15225470193199,-6.41561288561051,30.300215808455));
#55230=CARTESIAN_POINT('Ctrl Pts',(2.31792726371152,-6.3600344776815,30.308413692334));
#55231=CARTESIAN_POINT('Ctrl Pts',(2.48147219072227,-6.29802570518288,30.3166115762129));
#55232=CARTESIAN_POINT('Ctrl Pts',(2.64236356024418,-6.22978360904243,30.3248094600919));
#55233=CARTESIAN_POINT('Ctrl Pts',(2.80326290971407,-6.16153812820596,30.3330077505724));
#55234=CARTESIAN_POINT('Ctrl Pts',(2.96150810930629,-6.08705884780282,30.3412060410529));
#55235=CARTESIAN_POINT('Ctrl Pts',(3.11659381819117,-6.00659071124483,30.3494043315335));
#55236=CARTESIAN_POINT('Ctrl Pts',(3.27171539076207,-5.92610396637015,30.3576045178748));
#55237=CARTESIAN_POINT('Ctrl Pts',(3.42367569916727,-5.8396257721012,30.3658047042161));
#55238=CARTESIAN_POINT('Ctrl Pts',(3.57199453607082,-5.74744674044747,30.3740048905575));
#55239=CARTESIAN_POINT('Ctrl Pts',(3.7204535967971,-5.65518056075196,30.3822128295316));
#55240=CARTESIAN_POINT('Ctrl Pts',(3.8652640028644,-5.55720296520223,30.3904207685057));
#55241=CARTESIAN_POINT('Ctrl Pts',(4.0059742741666,-5.45384810154402,30.3986287074798));
#55242=CARTESIAN_POINT('Ctrl Pts',(4.14675280828444,-5.35044309731018,30.4068406283738));
#55243=CARTESIAN_POINT('Ctrl Pts',(4.28342696142729,-5.24165584706851,30.4150525492677));
#55244=CARTESIAN_POINT('Ctrl Pts',(4.41557891651402,-5.12786035613656,30.4232644701617));
#55245=CARTESIAN_POINT('Ctrl Pts',(4.54791209707177,-5.01390881271615,30.4314876524042));
#55246=CARTESIAN_POINT('Ctrl Pts',(4.67571042355632,-4.89493554747051,30.4397108346468));
#55247=CARTESIAN_POINT('Ctrl Pts',(4.79859261712912,-4.77135178904615,30.4479340168894));
#55248=CARTESIAN_POINT('Ctrl Pts',(4.90817252212099,-4.66114626526002,30.4552670201722));
#55249=CARTESIAN_POINT('Ctrl Pts',(5.01384347551547,-4.54727504101347,30.462600023455));
#55250=CARTESIAN_POINT('Ctrl Pts',(5.11536292965119,-4.43005091369732,30.4699330267378));
#55251=CARTESIAN_POINT('Ctrl Pts',(5.23906330857525,-4.28721455694677,30.4788682135201));
#55252=CARTESIAN_POINT('Ctrl Pts',(5.35685635282951,-4.13910351529673,30.4878034003024));
#55253=CARTESIAN_POINT('Ctrl Pts',(5.46831113383627,-3.98620901905084,30.4967385870846));
#55254=CARTESIAN_POINT('Ctrl Pts',(5.5795989900604,-3.83354351146136,30.5056603917213));
#55255=CARTESIAN_POINT('Ctrl Pts',(5.68456737255042,-3.67610905247899,30.5145821963579));
#55256=CARTESIAN_POINT('Ctrl Pts',(5.78282577957969,-3.51442954162244,30.5235040009946));
#55257=CARTESIAN_POINT('Ctrl Pts',(5.88084451105185,-3.35314440543581,30.5324040432338));
#55258=CARTESIAN_POINT('Ctrl Pts',(5.97218579932985,-3.18763510392477,30.5413040854731));
#55259=CARTESIAN_POINT('Ctrl Pts',(6.05650289291878,-3.01845352922096,30.5502041277124));
#55260=CARTESIAN_POINT('Ctrl Pts',(6.14069017910248,-2.84953241203875,30.5590904682058));
#55261=CARTESIAN_POINT('Ctrl Pts',(6.21787472676923,-2.67695052902459,30.5679768086992));
#55262=CARTESIAN_POINT('Ctrl Pts',(6.28775458985052,-2.50128591284838,30.5768631491926));
#55263=CARTESIAN_POINT('Ctrl Pts',(6.3574557823198,-2.32607044043254,30.5857267688646));
#55264=CARTESIAN_POINT('Ctrl Pts',(6.41988946340562,-2.14778820223259,30.5945903885365));
#55265=CARTESIAN_POINT('Ctrl Pts',(6.47480115604427,-1.96703812613985,30.6034540082084));
#55266=CARTESIAN_POINT('Ctrl Pts',(6.52692906747278,-1.79545128362051,30.6118682813621));
#55267=CARTESIAN_POINT('Ctrl Pts',(6.57227855714262,-1.62164082876767,30.6202825545158));
#55268=CARTESIAN_POINT('Ctrl Pts',(6.61067131476496,-1.4461375343112,30.6286968276695));
#55269=CARTESIAN_POINT('Ctrl Pts',(6.6481331446317,-1.27488975308507,30.6369070758741));
#55270=CARTESIAN_POINT('Ctrl Pts',(6.67893452146936,-1.10219459339382,30.6451173240786));
#55271=CARTESIAN_POINT('Ctrl Pts',(6.70298249497128,-0.928608998507214,
30.6533275722831));
#55272=CARTESIAN_POINT('Ctrl Pts',(6.72703618515591,-0.754982138864243,
30.6615397722274));
#55273=CARTESIAN_POINT('Ctrl Pts',(6.74433322470396,-0.580464774897712,
30.6697519721716));
#55274=CARTESIAN_POINT('Ctrl Pts',(6.75483246138537,-0.405619795639249,
30.6779641721158));
#55275=CARTESIAN_POINT('Ctrl Pts',(6.76533606356442,-0.230702117253558,
30.6861797866263));
#55276=CARTESIAN_POINT('Ctrl Pts',(6.76903621060775,-0.0554569072121219,
30.6943954011368));
#55277=CARTESIAN_POINT('Ctrl Pts',(6.76594385974772,0.119552025253029,30.7026110156472));
#55278=CARTESIAN_POINT('Ctrl Pts',(6.76284803631324,0.294757485077517,30.7108358559327));
#55279=CARTESIAN_POINT('Ctrl Pts',(6.75294448632581,0.469725781350313,30.7190606962181));
#55280=CARTESIAN_POINT('Ctrl Pts',(6.73629620173029,0.643896329042222,30.7272855365035));
#55281=CARTESIAN_POINT('Ctrl Pts',(6.71963725332978,0.818178439024317,30.7355156450851));
#55282=CARTESIAN_POINT('Ctrl Pts',(6.69622500562402,0.991661429965108,30.7437457536666));
#55283=CARTESIAN_POINT('Ctrl Pts',(6.66617374553966,1.1637940514875,30.7519758622481));
#55284=CARTESIAN_POINT('Ctrl Pts',(6.63608128471658,1.33616266947545,30.7602172544348));
#55285=CARTESIAN_POINT('Ctrl Pts',(6.59933170541764,1.50717687313839,30.7684586466215));
#55286=CARTESIAN_POINT('Ctrl Pts',(6.55608964980781,1.67629875132178,30.7767000388082));
#55287=CARTESIAN_POINT('Ctrl Pts',(6.53726960857914,1.74990488949431,30.7802869020724));
#55288=CARTESIAN_POINT('Ctrl Pts',(6.51722038263344,1.82315281110361,30.7838737653366));
#55289=CARTESIAN_POINT('Ctrl Pts',(6.49595839816831,1.89599933788665,30.7874606286008));
#55290=CARTESIAN_POINT('Ctrl Pts',(6.44587287868093,2.06759931919429,30.795909976789));
#55291=CARTESIAN_POINT('Ctrl Pts',(6.3889402599342,2.23736201625861,30.8043593249772));
#55292=CARTESIAN_POINT('Ctrl Pts',(6.32531449620336,2.40472150656156,30.8128086731654));
#55293=CARTESIAN_POINT('Ctrl Pts',(6.26174807036031,2.57192491608725,30.821250141425));
#55294=CARTESIAN_POINT('Ctrl Pts',(6.19150106064262,2.73672927628151,30.8296916096846));
#55295=CARTESIAN_POINT('Ctrl Pts',(6.11477715678058,2.89858402033034,30.8381330779442));
#55296=CARTESIAN_POINT('Ctrl Pts',(6.03614647150604,3.06446126065405,30.8467843378588));
#55297=CARTESIAN_POINT('Ctrl Pts',(5.95071286114916,3.22724002553104,30.8554355977734));
#55298=CARTESIAN_POINT('Ctrl Pts',(5.85874871527526,3.38634795779472,30.8640868576881));
#55299=CARTESIAN_POINT('Ctrl Pts',(5.76914969626247,3.5413639644407,30.8725156251627));
#55300=CARTESIAN_POINT('Ctrl Pts',(5.67335207946818,3.6928953121624,30.8809443926373));
#55301=CARTESIAN_POINT('Ctrl Pts',(5.57165496922936,3.84043616062835,30.8893731601119));
#55302=CARTESIAN_POINT('Ctrl Pts',(5.4699998891518,3.98791603228148,30.8977984440809));
#55303=CARTESIAN_POINT('Ctrl Pts',(5.36245036500796,4.13140841832292,30.90622372805));
#55304=CARTESIAN_POINT('Ctrl Pts',(5.24934929153977,4.27043569386204,30.914649012019));
#55305=CARTESIAN_POINT('Ctrl Pts',(5.13627918007783,4.40942490996244,30.9230719895227));
#55306=CARTESIAN_POINT('Ctrl Pts',(5.01766075978946,4.54395119445761,30.9314949670265));
#55307=CARTESIAN_POINT('Ctrl Pts',(4.89387797507892,4.67356901789601,30.9399179445303));
#55308=CARTESIAN_POINT('Ctrl Pts',(4.76425403063248,4.80930334948289,30.948738392144));
#55309=CARTESIAN_POINT('Ctrl Pts',(4.62896675170893,4.93965443927406,30.9575588397578));
#55310=CARTESIAN_POINT('Ctrl Pts',(4.48850180617996,5.06415249927559,30.9663792873715));
#55311=CARTESIAN_POINT('Ctrl Pts',(4.3543598826087,5.18304628581148,30.974802683011));
#55312=CARTESIAN_POINT('Ctrl Pts',(4.21549649140343,5.29660220907103,30.9832260786504));
#55313=CARTESIAN_POINT('Ctrl Pts',(4.07236987403007,5.40445118481908,30.9916494742899));
#55314=CARTESIAN_POINT('Ctrl Pts',(3.92922778921737,5.5123118156144,31.0000737802307));
#55315=CARTESIAN_POINT('Ctrl Pts',(3.78182182859266,5.6144640722578,31.0084980861716));
#55316=CARTESIAN_POINT('Ctrl Pts',(3.63064085309637,5.71058105588456,31.0169223921125));
#55317=CARTESIAN_POINT('Ctrl Pts',(3.47939478624575,5.80673942292362,31.0253503251598));
#55318=CARTESIAN_POINT('Ctrl Pts',(3.32437074210901,5.89685715225192,31.033778258207));
#55319=CARTESIAN_POINT('Ctrl Pts',(3.16608450050147,5.98065196577132,31.0422061912543));
#55320=CARTESIAN_POINT('Ctrl Pts',(3.14381554134836,5.99244088223402,31.0433918994679));
#55321=CARTESIAN_POINT('Ctrl Pts',(3.12148205153332,6.00410472377132,31.0445776076815));
#55322=CARTESIAN_POINT('Ctrl Pts',(3.09908550384736,6.01564277861005,31.0457633158951));
#55323=CARTESIAN_POINT('Ctrl Pts',(3.09908550384738,6.01564277861003,29.0457563580462));
#55324=CARTESIAN_POINT('Ctrl Pts',(2.9337323201834,6.10082796552475,29.0545058059455));
#55325=CARTESIAN_POINT('Ctrl Pts',(2.7648650214443,6.17919158180189,29.0632552538448));
#55326=CARTESIAN_POINT('Ctrl Pts',(2.59305716434349,6.2504674659138,29.0720047017441));
#55327=CARTESIAN_POINT('Ctrl Pts',(2.42125069459278,6.32174277447227,29.0807540789915));
#55328=CARTESIAN_POINT('Ctrl Pts',(2.24650397871052,6.38593035557828,29.089503456239));
#55329=CARTESIAN_POINT('Ctrl Pts',(2.06941053323763,6.44281220003541,29.0982528334864));
#55330=CARTESIAN_POINT('Ctrl Pts',(1.89231845896674,6.49969360406688,29.107002142989));
#55331=CARTESIAN_POINT('Ctrl Pts',(1.71287996431495,6.54926929700883,29.1157514524916));
#55332=CARTESIAN_POINT('Ctrl Pts',(1.53170449173493,6.59137090065481,29.1245007619942));
#55333=CARTESIAN_POINT('Ctrl Pts',(1.35053036178147,6.63347219230088,29.1332500066588));
#55334=CARTESIAN_POINT('Ctrl Pts',(1.16761955878808,6.66809944062461,29.1419992513234));
#55335=CARTESIAN_POINT('Ctrl Pts',(0.983593309309987,6.69513503985399,29.150748495988));
#55336=CARTESIAN_POINT('Ctrl Pts',(0.799568362459552,6.72217044771219,29.1594976787211));
#55337=CARTESIAN_POINT('Ctrl Pts',(0.614428268438235,6.7416142723598,29.1682468614543));
#55338=CARTESIAN_POINT('Ctrl Pts',(0.42880181632998,6.75340047696804,29.1769960441875));
#55339=CARTESIAN_POINT('Ctrl Pts',(0.243176616522413,6.76518660206243,29.1857451678956));
#55340=CARTESIAN_POINT('Ctrl Pts',(0.0570653511650086,6.76931519233997,
29.1944942916037));
#55341=CARTESIAN_POINT('Ctrl Pts',(-0.128899900800564,6.76577222610794,
29.2032434153119));
#55342=CARTESIAN_POINT('Ctrl Pts',(-0.314863959942571,6.76222928260131,
29.2119924829011));
#55343=CARTESIAN_POINT('Ctrl Pts',(-0.500681721081245,6.75101488651272,
29.2207415504904));
#55344=CARTESIAN_POINT('Ctrl Pts',(-0.685722110173877,6.73216712415985,
29.2294906180797));
#55345=CARTESIAN_POINT('Ctrl Pts',(-0.870761373828091,6.71331947644139,
29.238239632456));
#55346=CARTESIAN_POINT('Ctrl Pts',(-1.05502298984381,6.6868385843999,29.2469886468324));
#55347=CARTESIAN_POINT('Ctrl Pts',(-1.23788117676088,6.65281438131421,29.2557376612087));
#55348=CARTESIAN_POINT('Ctrl Pts',(-1.43009641451812,6.61704912302373,29.2649343720962));
#55349=CARTESIAN_POINT('Ctrl Pts',(-1.62076048992706,6.57294837083162,29.2741310829838));
#55350=CARTESIAN_POINT('Ctrl Pts',(-1.80915798961134,6.52067760042049,29.2833277938713));
#55351=CARTESIAN_POINT('Ctrl Pts',(-1.98840443003017,6.47094578577408,29.2920777915778));
#55352=CARTESIAN_POINT('Ctrl Pts',(-2.16559895952199,6.41381888474473,29.3008277892843));
#55353=CARTESIAN_POINT('Ctrl Pts',(-2.34013966242332,6.3494909528523,29.3095777869908));
#55354=CARTESIAN_POINT('Ctrl Pts',(-2.51467682554025,6.28516432556681,29.3183276072424));
#55355=CARTESIAN_POINT('Ctrl Pts',(-2.68656000078853,6.21363705879656,29.327077427494));
#55356=CARTESIAN_POINT('Ctrl Pts',(-2.855205338409,6.13515211510854,29.3358272477456));
#55357=CARTESIAN_POINT('Ctrl Pts',(-3.02384747998346,6.05666865881112,29.3445769021769));
#55358=CARTESIAN_POINT('Ctrl Pts',(-3.18925164684563,5.9712279103983,29.3533265566081));
#55359=CARTESIAN_POINT('Ctrl Pts',(-3.35085601829191,5.87912008251889,29.3620762110394));
#55360=CARTESIAN_POINT('Ctrl Pts',(-3.51245754191456,5.78701387778151,29.3708257112825));
#55361=CARTESIAN_POINT('Ctrl Pts',(-3.67025915510978,5.68824097060956,29.3795752115256));
#55362=CARTESIAN_POINT('Ctrl Pts',(-3.8237248792888,5.58313684656823,29.3883247117688));
#55363=CARTESIAN_POINT('Ctrl Pts',(-3.97718810300842,5.47803443501741,29.3970740694539));
#55364=CARTESIAN_POINT('Ctrl Pts',(-4.12631534263068,5.36660117496343,29.405823427139));
#55365=CARTESIAN_POINT('Ctrl Pts',(-4.27060009886266,5.24921554097317,29.4145727848241));
#55366=CARTESIAN_POINT('Ctrl Pts',(-4.41488269594253,5.13183166360257,29.4233220115793));
#55367=CARTESIAN_POINT('Ctrl Pts',(-4.55432273235127,5.00849577139435,29.4320712383345));
#55368=CARTESIAN_POINT('Ctrl Pts',(-4.68844662480245,4.87962675277306,29.4408204650897));
#55369=CARTESIAN_POINT('Ctrl Pts',(-4.82256868835186,4.75075949139853,29.4495695725412));
#55370=CARTESIAN_POINT('Ctrl Pts',(-4.95137454637881,4.61635945312505,29.4583186799927));
#55371=CARTESIAN_POINT('Ctrl Pts',(-5.07442674461088,4.47688309134579,29.4670677874442));
#55372=CARTESIAN_POINT('Ctrl Pts',(-5.19747742838547,4.33740844616341,29.4758167872165));
#55373=CARTESIAN_POINT('Ctrl Pts',(-5.31477440450934,4.1928578173602,29.4845657869889));
#55374=CARTESIAN_POINT('Ctrl Pts',(-5.42591931531158,4.04372211999399,29.4933147867613));
#55375=CARTESIAN_POINT('Ctrl Pts',(-5.5370763646299,3.8945701350079,29.5020647420418));
#55376=CARTESIAN_POINT('Ctrl Pts',(-5.64207983273481,3.74083230916404,29.5108146973224));
#55377=CARTESIAN_POINT('Ctrl Pts',(-5.7405730346876,3.58303087251806,29.519564652603));
#55378=CARTESIAN_POINT('Ctrl Pts',(-5.83906243363776,3.42523552887413,29.5283142700318));
#55379=CARTESIAN_POINT('Ctrl Pts',(-5.93104191768434,3.26337713156978,29.5370638874606));
#55380=CARTESIAN_POINT('Ctrl Pts',(-6.01619906699662,3.09800545291144,29.5458135048894));
#55381=CARTESIAN_POINT('Ctrl Pts',(-6.10135338095391,2.93263928039579,29.5545628309948));
#55382=CARTESIAN_POINT('Ctrl Pts',(-6.17968568352848,2.76376031540203,29.5633121571002));
#55383=CARTESIAN_POINT('Ctrl Pts',(-6.25092992694897,2.59194213831516,29.5720614832056));
#55384=CARTESIAN_POINT('Ctrl Pts',(-6.32217217691122,2.42012876880773,29.5808105644994));
#55385=CARTESIAN_POINT('Ctrl Pts',(-6.38632665483874,2.24537661647603,29.5895596457932));
#55386=CARTESIAN_POINT('Ctrl Pts',(-6.44317547869378,2.06827917621368,29.598308727087));
#55387=CARTESIAN_POINT('Ctrl Pts',(-6.50002944235958,1.89116572423345,29.607058599402));
#55388=CARTESIAN_POINT('Ctrl Pts',(-6.54957634250415,1.71170683289131,29.6158084717169));
#55389=CARTESIAN_POINT('Ctrl Pts',(-6.59164787708408,1.53051209225308,29.6245583440319));
#55390=CARTESIAN_POINT('Ctrl Pts',(-6.63371649075019,1.3493299314798,29.6333076088667));
#55391=CARTESIAN_POINT('Ctrl Pts',(-6.66831071257131,1.16641244173959,29.6420568737015));
#55392=CARTESIAN_POINT('Ctrl Pts',(-6.69531304840338,0.982380875159628,
29.6508061385363));
#55393=CARTESIAN_POINT('Ctrl Pts',(-6.72231677033048,0.798339861795456,
29.6595558524919));
#55394=CARTESIAN_POINT('Ctrl Pts',(-6.74172778477893,0.613184940729765,
29.6683055664476));
#55395=CARTESIAN_POINT('Ctrl Pts',(-6.7534801583552,0.427545027690162,29.6770552804032));
#55396=CARTESIAN_POINT('Ctrl Pts',(-6.76249038365213,0.285219953548068,
29.6837634482055));
#55397=CARTESIAN_POINT('Ctrl Pts',(-6.76699999999991,0.142609995760195,
29.6904716160077));
#55398=CARTESIAN_POINT('Ctrl Pts',(-6.767,4.44901934821046E-12,29.6971797838099));
#55399=CARTESIAN_POINT('',(-6.767,9.60786626183482E-10,29.3028202161448));
#55400=CARTESIAN_POINT('Ctrl Pts',(3.09908550384705,6.0156427786102,28.6513967904262));
#55401=CARTESIAN_POINT('Ctrl Pts',(2.93373232018317,6.10082796552485,28.6601462383254));
#55402=CARTESIAN_POINT('Ctrl Pts',(2.76486502144419,6.17919158180193,28.6688956862247));
#55403=CARTESIAN_POINT('Ctrl Pts',(2.5930571643435,6.2504674659138,28.677645134124));
#55404=CARTESIAN_POINT('Ctrl Pts',(2.4212506945929,6.32174277447221,28.6863945113714));
#55405=CARTESIAN_POINT('Ctrl Pts',(2.24650397871076,6.38593035557819,28.6951438886188));
#55406=CARTESIAN_POINT('Ctrl Pts',(2.06941053323799,6.4428122000353,28.7038932658663));
#55407=CARTESIAN_POINT('Ctrl Pts',(1.89231845896711,6.49969360406677,28.7126425753689));
#55408=CARTESIAN_POINT('Ctrl Pts',(1.71287996431532,6.54926929700874,28.7213918848714));
#55409=CARTESIAN_POINT('Ctrl Pts',(1.5317044917353,6.59137090065473,28.730141194374));
#55410=CARTESIAN_POINT('Ctrl Pts',(1.35053036178209,6.63347219230075,28.7388904390386));
#55411=CARTESIAN_POINT('Ctrl Pts',(1.16761955878895,6.66809944062445,28.7476396837032));
#55412=CARTESIAN_POINT('Ctrl Pts',(0.983593309311117,6.69513503985382,28.7563889283678));
#55413=CARTESIAN_POINT('Ctrl Pts',(0.799568362460557,6.72217044771208,28.765138111101));
#55414=CARTESIAN_POINT('Ctrl Pts',(0.614428268439116,6.74161427235972,28.7738872938342));
#55415=CARTESIAN_POINT('Ctrl Pts',(0.428801816330733,6.75340047696799,28.7826364765673));
#55416=CARTESIAN_POINT('Ctrl Pts',(0.243176616523421,6.76518660206239,28.7913856002755));
#55417=CARTESIAN_POINT('Ctrl Pts',(0.057065351166272,6.76931519233996,28.8001347239836));
#55418=CARTESIAN_POINT('Ctrl Pts',(-0.128899900799046,6.76577222610797,
28.8088838476917));
#55419=CARTESIAN_POINT('Ctrl Pts',(-0.314863959940799,6.76222928260138,
28.817632915281));
#55420=CARTESIAN_POINT('Ctrl Pts',(-0.500681721079224,6.75101488651287,
28.8263819828702));
#55421=CARTESIAN_POINT('Ctrl Pts',(-0.685722110171609,6.73216712416008,
28.8351310504595));
#55422=CARTESIAN_POINT('Ctrl Pts',(-0.870761373825832,6.71331947644168,
28.8438800648358));
#55423=CARTESIAN_POINT('Ctrl Pts',(-1.05502298984156,6.68683858440026,28.8526290792122));
#55424=CARTESIAN_POINT('Ctrl Pts',(-1.23788117675864,6.65281438131462,28.8613780935885));
#55425=CARTESIAN_POINT('Ctrl Pts',(-1.43009641449636,6.61704912302784,28.8705748044751));
#55426=CARTESIAN_POINT('Ctrl Pts',(-1.62076048988609,6.57294837084113,28.8797715153617));
#55427=CARTESIAN_POINT('Ctrl Pts',(-1.8091579895517,6.52067760043703,28.8889682262483));
#55428=CARTESIAN_POINT('Ctrl Pts',(-1.98840442997098,6.47094578579226,28.8977182239548));
#55429=CARTESIAN_POINT('Ctrl Pts',(-2.16559895946333,6.41381888476454,28.9064682216613));
#55430=CARTESIAN_POINT('Ctrl Pts',(-2.34013966236525,6.34949095287371,28.9152182193678));
#55431=CARTESIAN_POINT('Ctrl Pts',(-2.51467682548265,6.28516432558985,28.9239680396194));
#55432=CARTESIAN_POINT('Ctrl Pts',(-2.68656000073147,6.21363705882123,28.932717859871));
#55433=CARTESIAN_POINT('Ctrl Pts',(-2.85520533835254,6.13515211513481,28.9414676801226));
#55434=CARTESIAN_POINT('Ctrl Pts',(-3.02384747992761,6.056668658839,28.9502173345538));
#55435=CARTESIAN_POINT('Ctrl Pts',(-3.18925164679046,5.97122791042776,28.9589669889851));
#55436=CARTESIAN_POINT('Ctrl Pts',(-3.35085601823748,5.87912008254991,28.9677166434163));
#55437=CARTESIAN_POINT('Ctrl Pts',(-3.51245754186099,5.78701387781403,28.9764661436595));
#55438=CARTESIAN_POINT('Ctrl Pts',(-3.67025915505712,5.68824097064353,28.9852156439026));
#55439=CARTESIAN_POINT('Ctrl Pts',(-3.82372487923712,5.58313684660363,28.9939651441457));
#55440=CARTESIAN_POINT('Ctrl Pts',(-3.97718810295761,5.4780344350543,29.0027145018308));
#55441=CARTESIAN_POINT('Ctrl Pts',(-4.1263153425808,5.36660117500178,29.011463859516));
#55442=CARTESIAN_POINT('Ctrl Pts',(-4.27060009881377,5.24921554101295,29.0202132172011));
#55443=CARTESIAN_POINT('Ctrl Pts',(-4.41488269589484,5.1318316636436,29.0289624439563));
#55444=CARTESIAN_POINT('Ctrl Pts',(-4.55432273230482,5.0084957714366,29.0377116707114));
#55445=CARTESIAN_POINT('Ctrl Pts',(-4.68844662475729,4.87962675281645,29.0464608974666));
#55446=CARTESIAN_POINT('Ctrl Pts',(-4.82256868830816,4.75075949144289,29.0552100049181));
#55447=CARTESIAN_POINT('Ctrl Pts',(-4.95137454633662,4.61635945317032,29.0639591123696));
#55448=CARTESIAN_POINT('Ctrl Pts',(-5.07442674457021,4.47688309139189,29.0727082198212));
#55449=CARTESIAN_POINT('Ctrl Pts',(-5.19747742834581,4.33740844621092,29.0814572195935));
#55450=CARTESIAN_POINT('Ctrl Pts',(-5.31477440447077,4.19285781740908,29.0902062193659));
#55451=CARTESIAN_POINT('Ctrl Pts',(-5.42591931527416,4.0437221200442,29.0989552191382));
#55452=CARTESIAN_POINT('Ctrl Pts',(-5.53707636459378,3.89457013505924,29.1077051744188));
#55453=CARTESIAN_POINT('Ctrl Pts',(-5.64207983270005,3.74083230921646,29.1164551296994));
#55454=CARTESIAN_POINT('Ctrl Pts',(-5.74057303465425,3.58303087257151,29.1252050849799));
#55455=CARTESIAN_POINT('Ctrl Pts',(-5.83906243360593,3.42523552892838,29.1339547024088));
#55456=CARTESIAN_POINT('Ctrl Pts',(-5.93104191765408,3.26337713162477,29.1427043198376));
#55457=CARTESIAN_POINT('Ctrl Pts',(-6.01619906696795,3.09800545296711,29.1514539372664));
#55458=CARTESIAN_POINT('Ctrl Pts',(-6.10135338092672,2.93263928045236,29.1602032633718));
#55459=CARTESIAN_POINT('Ctrl Pts',(-6.1796856835028,2.76376031545944,29.1689525894771));
#55460=CARTESIAN_POINT('Ctrl Pts',(-6.25092992692484,2.59194213837335,29.1777019155825));
#55461=CARTESIAN_POINT('Ctrl Pts',(-6.32217217688859,2.42012876886682,29.1864509968763));
#55462=CARTESIAN_POINT('Ctrl Pts',(-6.38632665481767,2.24537661653596,29.1952000781701));
#55463=CARTESIAN_POINT('Ctrl Pts',(-6.4431754786743,2.06827917627438,29.2039491594639));
#55464=CARTESIAN_POINT('Ctrl Pts',(-6.50002944234177,1.89116572429469,29.2126990317789));
#55465=CARTESIAN_POINT('Ctrl Pts',(-6.54957634248803,1.71170683295301,29.2214489040938));
#55466=CARTESIAN_POINT('Ctrl Pts',(-6.59164787706967,1.53051209231518,29.2301987764088));
#55467=CARTESIAN_POINT('Ctrl Pts',(-6.63371649073748,1.34932993154229,29.2389480412436));
#55468=CARTESIAN_POINT('Ctrl Pts',(-6.66831071256033,1.16641244180241,29.2476973060784));
#55469=CARTESIAN_POINT('Ctrl Pts',(-6.69531304839413,0.982380875222698,
29.2564465709132));
#55470=CARTESIAN_POINT('Ctrl Pts',(-6.72231677032296,0.798339861858778,
29.2651962848688));
#55471=CARTESIAN_POINT('Ctrl Pts',(-6.74172778477316,0.613184940793268,
29.2739459988245));
#55472=CARTESIAN_POINT('Ctrl Pts',(-6.75348015835118,0.427545027753774,
29.2826957127801));
#55473=CARTESIAN_POINT('Ctrl Pts',(-6.76249038363065,0.285219953908639,
29.2894038805684));
#55474=CARTESIAN_POINT('Ctrl Pts',(-6.76699999997976,0.142609996418872,
29.2961120483566));
#55475=CARTESIAN_POINT('Ctrl Pts',(-6.767,9.60595125194256E-10,29.3028202161448));
#55476=CARTESIAN_POINT('Ctrl Pts',(-6.767,3.94550158016225E-12,29.3028202161898));
#55477=CARTESIAN_POINT('Ctrl Pts',(-6.76700000000011,-0.1860072495561,29.3115697280026));
#55478=CARTESIAN_POINT('Ctrl Pts',(-6.75932637294268,-0.372014355812326,
29.3203192398153));
#55479=CARTESIAN_POINT('Ctrl Pts',(-6.74400518263393,-0.557389537582745,
29.329068751628));
#55480=CARTESIAN_POINT('Ctrl Pts',(-6.72868405703768,-0.742763936379325,
29.3378182264853));
#55481=CARTESIAN_POINT('Ctrl Pts',(-6.70571545643609,-0.927506130401745,
29.3465677013425));
#55482=CARTESIAN_POINT('Ctrl Pts',(-6.67517739401626,-1.11098864009237,
29.3553171761997));
#55483=CARTESIAN_POINT('Ctrl Pts',(-6.64463945804446,-1.2944703900425,29.3640666148282));
#55484=CARTESIAN_POINT('Ctrl Pts',(-6.60653217002786,-1.47669218339003,
29.3728160534567));
#55485=CARTESIAN_POINT('Ctrl Pts',(-6.56098496085545,-1.65703510627524,
29.3815654920852));
#55486=CARTESIAN_POINT('Ctrl Pts',(-6.51543793649624,-1.83737729739771,
29.3903148952119));
#55487=CARTESIAN_POINT('Ctrl Pts',(-6.46245112156964,-2.01584035544735,
29.3990642983385));
#55488=CARTESIAN_POINT('Ctrl Pts',(-6.40220448361785,-2.19181813797212,
29.4078137014651));
#55489=CARTESIAN_POINT('Ctrl Pts',(-6.34195808512043,-2.36779522106115,
29.4165630698167));
#55490=CARTESIAN_POINT('Ctrl Pts',(-6.27445201416427,-2.54128677725564,
29.4253124381682));
#55491=CARTESIAN_POINT('Ctrl Pts',(-6.19991555052799,-2.71170355428486,
29.4340618065197));
#55492=CARTESIAN_POINT('Ctrl Pts',(-6.12537937695189,-2.88211966813372,
29.4428111408229));
#55493=CARTESIAN_POINT('Ctrl Pts',(-6.0438129802841,-3.04946076419752,29.4515604751261));
#55494=CARTESIAN_POINT('Ctrl Pts',(-5.95549339308928,-3.21315848424411,
29.4603098094293));
#55495=CARTESIAN_POINT('Ctrl Pts',(-5.86717414225757,-3.37685558085172,
29.4690591104109));
#55496=CARTESIAN_POINT('Ctrl Pts',(-5.77210188844016,-3.53690907700082,
29.4778084113924));
#55497=CARTESIAN_POINT('Ctrl Pts',(-5.67059953311324,-3.69277537024064,
29.486557712374));
#55498=CARTESIAN_POINT('Ctrl Pts',(-5.56909755592647,-3.84864108281114,
29.4953069807606));
#55499=CARTESIAN_POINT('Ctrl Pts',(-5.46116568154892,-4.0003193835493,29.5040562491472));
#55500=CARTESIAN_POINT('Ctrl Pts',(-5.34717048488289,-4.14729511918278,
29.5128055175338));
#55501=CARTESIAN_POINT('Ctrl Pts',(-5.2331757034321,-4.29427031947295,29.5215547540522));
#55502=CARTESIAN_POINT('Ctrl Pts',(-5.11311781951445,-4.43654276249674,
29.5303039905706));
#55503=CARTESIAN_POINT('Ctrl Pts',(-4.98740458929134,-4.57362924412503,
29.5390532270889));
#55504=CARTESIAN_POINT('Ctrl Pts',(-4.86169180652617,-4.71071523781395,
29.5478024324656));
#55505=CARTESIAN_POINT('Ctrl Pts',(-4.73032391141436,-4.84261509584623,
29.5565516378423));
#55506=CARTESIAN_POINT('Ctrl Pts',(-4.59374706947177,-4.96888084599737,
29.5653008432191));
#55507=CARTESIAN_POINT('Ctrl Pts',(-4.45717070231383,-5.0951461572085,29.5740500181808));
#55508=CARTESIAN_POINT('Ctrl Pts',(-4.31538563497265,-5.21577720520662,
29.5827991931425));
#55509=CARTESIAN_POINT('Ctrl Pts',(-4.16887340951972,-5.33036429293528,
29.5915483681042));
#55510=CARTESIAN_POINT('Ctrl Pts',(-4.02236168122446,-5.44495099183735,
29.6002975133774));
#55511=CARTESIAN_POINT('Ctrl Pts',(-3.87112305263137,-5.55349359497959,
29.6090466586507));
#55512=CARTESIAN_POINT('Ctrl Pts',(-3.71567116928946,-5.65562346357244,
29.6177958039239));
#55513=CARTESIAN_POINT('Ctrl Pts',(-3.56021980053269,-5.75775299408953,
29.6265449202353));
#55514=CARTESIAN_POINT('Ctrl Pts',(-3.40055544442049,-5.85346967519899,
29.6352940365466));
#55515=CARTESIAN_POINT('Ctrl Pts',(-3.23722035886816,-5.94244843041397,
29.644043152858));
#55516=CARTESIAN_POINT('Ctrl Pts',(-3.07388580043446,-6.03142689847474,
29.652792240934));
#55517=CARTESIAN_POINT('Ctrl Pts',(-2.90688078789162,-6.11366734707931,
29.6615413290101));
#55518=CARTESIAN_POINT('Ctrl Pts',(-2.73677250610313,-6.18889047001464,
29.6702904170861));
#55519=CARTESIAN_POINT('Ctrl Pts',(-2.56666475916852,-6.26411335643368,
29.6790394776532));
#55520=CARTESIAN_POINT('Ctrl Pts',(-2.39345402457006,-6.33231884545289,
29.6877885382204));
#55521=CARTESIAN_POINT('Ctrl Pts',(-2.21772855943975,-6.39327529804914,
29.6965375987876));
#55522=CARTESIAN_POINT('Ctrl Pts',(-2.04200363223531,-6.45423156404721,
29.7052866325724));
#55523=CARTESIAN_POINT('Ctrl Pts',(-1.86376426061004,-6.50793874412461,
29.7140356663572));
#55524=CARTESIAN_POINT('Ctrl Pts',(-1.68361577621689,-6.55421443943312,
29.722784700142));
#55525=CARTESIAN_POINT('Ctrl Pts',(-1.50346782833187,-6.60048999692595,
29.7315337078709));
#55526=CARTESIAN_POINT('Ctrl Pts',(-1.32141105657328,-6.63933404265174,
29.7402827155998));
#55527=CARTESIAN_POINT('Ctrl Pts',(-1.13806375346445,-6.67061465631544,
29.7490317233287));
#55528=CARTESIAN_POINT('Ctrl Pts',(-0.954716981169325,-6.7018951794178,
29.7577807057281));
#55529=CARTESIAN_POINT('Ctrl Pts',(-0.770079967441817,-6.72561226609009,
29.7665296881275));
#55530=CARTESIAN_POINT('Ctrl Pts',(-0.584779764072827,-6.74168536995987,
29.7752786705269));
#55531=CARTESIAN_POINT('Ctrl Pts',(-0.391489587592689,-6.75845153117874,
29.7844049009426));
#55532=CARTESIAN_POINT('Ctrl Pts',(-0.197478091804947,-6.76689985146395,
29.7935311313582));
#55533=CARTESIAN_POINT('Ctrl Pts',(-0.00346214753071807,-6.76699911434415,
29.8026573617738));
#55534=CARTESIAN_POINT('Ctrl Pts',(0.184490798485026,-6.76709527525934,
29.8114983974889));
#55535=CARTESIAN_POINT('Ctrl Pts',(0.372447602155239,-6.75935633790761,
29.8203394332041));
#55536=CARTESIAN_POINT('Ctrl Pts',(0.559756448194746,-6.74380914014509,
29.8291804689192));
#55537=CARTESIAN_POINT('Ctrl Pts',(0.745136131043843,-6.72842206873149,
29.8379304475325));
#55538=CARTESIAN_POINT('Ctrl Pts',(0.929880851945483,-6.70538686355717,
29.8466804261458));
#55539=CARTESIAN_POINT('Ctrl Pts',(1.11336305057502,-6.67478177303306,29.8554304047591));
#55540=CARTESIAN_POINT('Ctrl Pts',(1.29684337090168,-6.64417699581252,29.8641802937991));
#55541=CARTESIAN_POINT('Ctrl Pts',(1.47906091205239,-6.60600253548049,29.8729301828391));
#55542=CARTESIAN_POINT('Ctrl Pts',(1.65939671095275,-6.56038806441198,29.881680071879));
#55543=CARTESIAN_POINT('Ctrl Pts',(1.83973072369224,-6.51477404513832,29.8904298742545));
#55544=CARTESIAN_POINT('Ctrl Pts',(2.0181827535711,-6.46172023288638,29.89917967663));
#55545=CARTESIAN_POINT('Ctrl Pts',(2.19414664033409,-6.40140683918079,29.9079294790055));
#55546=CARTESIAN_POINT('Ctrl Pts',(2.37010884271342,-6.34109402281466,29.9166791976251));
#55547=CARTESIAN_POINT('Ctrl Pts',(2.54358267847889,-6.27352185699758,29.9254289162446));
#55548=CARTESIAN_POINT('Ctrl Pts',(2.71397890841824,-6.19891986435225,29.9341786348642));
#55549=CARTESIAN_POINT('Ctrl Pts',(2.88437356389031,-6.12431856103202,29.942928272636));
#55550=CARTESIAN_POINT('Ctrl Pts',(3.05169040787266,-6.0426876758251,29.9516779104078));
#55551=CARTESIAN_POINT('Ctrl Pts',(3.21536112512153,-5.95430447953892,29.9604275481796));
#55552=CARTESIAN_POINT('Ctrl Pts',(3.37903038442942,-5.86592207054986,29.9691771080117));
#55553=CARTESIAN_POINT('Ctrl Pts',(3.53905332980071,-5.77078760703317,29.9779266678438));
#55554=CARTESIAN_POINT('Ctrl Pts',(3.69488643041989,-5.66922422085235,29.9866762276758));
#55555=CARTESIAN_POINT('Ctrl Pts',(3.8507181946885,-5.56766170563084,29.9954257124758));
#55556=CARTESIAN_POINT('Ctrl Pts',(4.00235994599341,-5.45967053456166,30.0041751972758));
#55557=CARTESIAN_POINT('Ctrl Pts',(4.14929662974426,-5.34561750206587,30.0129246820758));
#55558=CARTESIAN_POINT('Ctrl Pts',(4.29623210225173,-5.23156540974361,30.0216740947512));
#55559=CARTESIAN_POINT('Ctrl Pts',(4.43846235842249,-5.11145173172073,30.0304235074266));
#55560=CARTESIAN_POINT('Ctrl Pts',(4.57550431797562,-4.98568443006439,30.0391729201019));
#55561=CARTESIAN_POINT('Ctrl Pts',(4.71254519337633,-4.85991812336555,30.0479222635598));
#55562=CARTESIAN_POINT('Ctrl Pts',(4.84439764315127,-4.72849847630954,30.0566716070177));
#55563=CARTESIAN_POINT('Ctrl Pts',(4.97061384196834,-4.59187184425184,30.0654209504756));
#55564=CARTESIAN_POINT('Ctrl Pts',(5.09682908420349,-4.45524624767584,30.074170227623));
#55565=CARTESIAN_POINT('Ctrl Pts',(5.21740796650309,-4.31341395556726,30.0829195047704));
#55566=CARTESIAN_POINT('Ctrl Pts',(5.33194095942384,-4.16685668162686,30.0916687819177));
#55567=CARTESIAN_POINT('Ctrl Pts',(5.44647312235257,-4.02030046975047,30.1004179956613));
#55568=CARTESIAN_POINT('Ctrl Pts',(5.55495930712403,-3.86901957035382,30.1091672094048));
#55569=CARTESIAN_POINT('Ctrl Pts',(5.65703106079901,-3.71352778058213,30.1179164231483));
#55570=CARTESIAN_POINT('Ctrl Pts',(5.75910210868834,-3.55803706597444,30.1266655763945));
#55571=CARTESIAN_POINT('Ctrl Pts',(5.85475865698639,-3.39833575880744,30.1354147296407));
#55572=CARTESIAN_POINT('Ctrl Pts',(5.94367583069146,-3.23496624706568,30.1441638828869));
#55573=CARTESIAN_POINT('Ctrl Pts',(6.03259241910153,-3.07159781069949,30.152912978542));
#55574=CARTESIAN_POINT('Ctrl Pts',(6.11476958471038,-2.90456146975686,30.1616620741971));
#55575=CARTESIAN_POINT('Ctrl Pts',(6.1899282357445,-2.73442451648112,30.1704111698523));
#55576=CARTESIAN_POINT('Ctrl Pts',(6.26508641701002,-2.56428862662254,30.1791602108224));
#55577=CARTESIAN_POINT('Ctrl Pts',(6.33322605570365,-2.39105242531098,30.1879092517925));
#55578=CARTESIAN_POINT('Ctrl Pts',(6.39411573747835,-2.21530425353532,30.1966582927626));
#55579=CARTESIAN_POINT('Ctrl Pts',(6.45500505889193,-2.03955712188347,30.2054072819536));
#55580=CARTESIAN_POINT('Ctrl Pts',(6.50864441544996,-1.86129832025341,30.2141562711446));
#55581=CARTESIAN_POINT('Ctrl Pts',(6.5548516404997,-1.68113324012061,30.2229052603357));
#55582=CARTESIAN_POINT('Ctrl Pts',(6.60199852639166,-1.49730435912651,30.2318321672125));
#55583=CARTESIAN_POINT('Ctrl Pts',(6.64140767441058,-1.31149113173406,30.2407590740894));
#55584=CARTESIAN_POINT('Ctrl Pts',(6.67293975269643,-1.12435050446188,30.2496859809663));
#55585=CARTESIAN_POINT('Ctrl Pts',(6.70384664831542,-0.940920291561225,
30.2584358951503));
#55586=CARTESIAN_POINT('Ctrl Pts',(6.72718585889695,-0.756215114275331,
30.2671858093343));
#55587=CARTESIAN_POINT('Ctrl Pts',(6.74287810451887,-0.570862389372445,
30.2759357235183));
#55588=CARTESIAN_POINT('Ctrl Pts',(6.75857004154139,-0.385513309565421,
30.2846854656289));
#55589=CARTESIAN_POINT('Ctrl Pts',(6.76661529035564,-0.199516993256552,
30.2934352077394));
#55590=CARTESIAN_POINT('Ctrl Pts',(6.76698652348897,-0.0135052182024178,
30.30218494985));
#55591=CARTESIAN_POINT('Ctrl Pts',(6.76735774981517,0.172503146040519,30.3109345315207));
#55592=CARTESIAN_POINT('Ctrl Pts',(6.76005524147471,0.358526681835083,30.3196841131913));
#55593=CARTESIAN_POINT('Ctrl Pts',(6.74510380214869,0.543933542116461,30.328433694862));
#55594=CARTESIAN_POINT('Ctrl Pts',(6.73015261710962,0.729337249086341,30.3371831277239));
#55595=CARTESIAN_POINT('Ctrl Pts',(6.70755278444583,0.914124015856304,30.3459325605858));
#55596=CARTESIAN_POINT('Ctrl Pts',(6.67738106408262,1.09766621749552,30.3546819934478));
#55597=CARTESIAN_POINT('Ctrl Pts',(6.64720981677221,1.28120554143496,30.3634312891301));
#55598=CARTESIAN_POINT('Ctrl Pts',(6.60946696581483,1.46350005650802,30.3721805848125));
#55599=CARTESIAN_POINT('Ctrl Pts',(6.56428070010947,1.64393062206724,30.3809298804948));
#55600=CARTESIAN_POINT('Ctrl Pts',(6.5190950828269,1.82435859844834,30.3896790506248));
#55601=CARTESIAN_POINT('Ctrl Pts',(6.46646633415607,2.00292240086737,30.3984282207548));
#55602=CARTESIAN_POINT('Ctrl Pts',(6.40657319597136,2.1790155769662,30.4071773908848));
#55603=CARTESIAN_POINT('Ctrl Pts',(6.34668083768237,2.3551064600759,30.4159264470878));
#55604=CARTESIAN_POINT('Ctrl Pts',(6.27952437143826,2.52872650996677,30.4246755032909));
#55605=CARTESIAN_POINT('Ctrl Pts',(6.20533187335076,2.69928607998062,30.433424559494));
#55606=CARTESIAN_POINT('Ctrl Pts',(6.12831449784194,2.87633970115522,30.4425067357828));
#55607=CARTESIAN_POINT('Ctrl Pts',(6.04371489463096,3.05009490562461,30.4515889120717));
#55608=CARTESIAN_POINT('Ctrl Pts',(5.95184265120436,3.21991584599732,30.4606710883605));
#55609=CARTESIAN_POINT('Ctrl Pts',(5.86333281335429,3.3835215590541,30.4694208687149));
#55610=CARTESIAN_POINT('Ctrl Pts',(5.76807337235613,3.54347560903942,30.4781706490694));
#55611=CARTESIAN_POINT('Ctrl Pts',(5.66638790086274,3.69923467178772,30.4869204294238));
#55612=CARTESIAN_POINT('Ctrl Pts',(5.56470608502659,3.85498813489885,30.4956698952181));
#55613=CARTESIAN_POINT('Ctrl Pts',(5.45659885766867,4.00654667256377,30.5044193610123));
#55614=CARTESIAN_POINT('Ctrl Pts',(5.34243340580421,4.15339551506322,30.5131688268066));
#55615=CARTESIAN_POINT('Ctrl Pts',(5.22827145140507,4.30023985883976,30.5219180245604));
#55616=CARTESIAN_POINT('Ctrl Pts',(5.10805181978003,4.44237456993142,30.5306672223143));
#55617=CARTESIAN_POINT('Ctrl Pts',(4.98218281282465,4.57931691626542,30.5394164200682));
#55618=CARTESIAN_POINT('Ctrl Pts',(4.85631699296145,4.71625579512248,30.5481653962862));
#55619=CARTESIAN_POINT('Ctrl Pts',(4.72480227791756,4.84800236135849,30.5569143725042));
#55620=CARTESIAN_POINT('Ctrl Pts',(4.58808530848034,4.97410918678982,30.5656633487222));
#55621=CARTESIAN_POINT('Ctrl Pts',(4.45135945056885,5.10022421089084,30.5744128937434));
#55622=CARTESIAN_POINT('Ctrl Pts',(4.30943087207948,5.22069856612062,30.5831624387646));
#55623=CARTESIAN_POINT('Ctrl Pts',(4.16278164322369,5.3351230530176,30.5919119837858));
#55624=CARTESIAN_POINT('Ctrl Pts',(4.01614103534287,5.44954081331503,30.600661014453));
#55625=CARTESIAN_POINT('Ctrl Pts',(3.86478055833306,5.55790924068413,30.6094100451203));
#55626=CARTESIAN_POINT('Ctrl Pts',(3.70921425811839,5.65986029751364,30.6181590757875));
#55627=CARTESIAN_POINT('Ctrl Pts',(3.55364584530021,5.76181273884714,30.6269082252674));
#55628=CARTESIAN_POINT('Ctrl Pts',(3.39387173464259,5.85734747818112,30.6356573747472));
#55629=CARTESIAN_POINT('Ctrl Pts',(3.23043456092335,5.94614005448846,30.6444065242271));
#55630=CARTESIAN_POINT('Ctrl Pts',(3.18690768806344,5.96978744811307,30.6467366129601));
#55631=CARTESIAN_POINT('Ctrl Pts',(3.14312114982856,5.99295688499313,30.6490667016931));
#55632=CARTESIAN_POINT('Ctrl Pts',(3.09908550384718,6.01564277861014,30.6513967904261));
#55633=CARTESIAN_POINT('Origin',(0.,0.,-63.6971797838103));
#55634=CARTESIAN_POINT('',(3.09908550384727,6.01564277861009,33.045773705108));
#55635=CARTESIAN_POINT('',(3.09908550384731,6.01564277861007,32.651275857025));
#55636=CARTESIAN_POINT('',(3.09908550384721,6.01564277861012,-63.6971797838103));
#55637=CARTESIAN_POINT('',(-6.76699962134934,-0.00226377072112061,31.6971797837756));
#55638=CARTESIAN_POINT('Ctrl Pts',(-6.7669996213491,-0.00226377144942592,
31.6971797838099));
#55639=CARTESIAN_POINT('Ctrl Pts',(-6.76692578390497,-0.222983030274878,
31.7075764721537));
#55640=CARTESIAN_POINT('Ctrl Pts',(-6.75604897537786,-0.443454407875999,
31.7179731604974));
#55641=CARTESIAN_POINT('Ctrl Pts',(-6.73446647616864,-0.662759595449747,
31.7283698488412));
#55642=CARTESIAN_POINT('Ctrl Pts',(-6.72638873903325,-0.74483950846053,
31.7322610439574));
#55643=CARTESIAN_POINT('Ctrl Pts',(-6.71681185948521,-0.826756188685703,
31.7361522390737));
#55644=CARTESIAN_POINT('Ctrl Pts',(-6.70574275848478,-0.908461918315195,
31.7400434341899));
#55645=CARTESIAN_POINT('Ctrl Pts',(-6.68208302226691,-1.08310446701431,
31.7483606995234));
#55646=CARTESIAN_POINT('Ctrl Pts',(-6.65157362820262,-1.25699086935697,
31.7566779648568));
#55647=CARTESIAN_POINT('Ctrl Pts',(-6.6142774749381,-1.42955324648175,31.7649952301902));
#55648=CARTESIAN_POINT('Ctrl Pts',(-6.57701277810894,-1.60197008052,31.7733054805503));
#55649=CARTESIAN_POINT('Ctrl Pts',(-6.53297279979114,-1.77306477598608,
31.7816157309104));
#55650=CARTESIAN_POINT('Ctrl Pts',(-6.48227194989753,-1.94227685142251,
31.7899259812705));
#55651=CARTESIAN_POINT('Ctrl Pts',(-6.43160457699367,-2.11137719873351,
31.7982307445004));
#55652=CARTESIAN_POINT('Ctrl Pts',(-6.37428519571406,-2.27859707089379,
31.8065355077303));
#55653=CARTESIAN_POINT('Ctrl Pts',(-6.31047883354035,-2.44338819908734,
31.8148402709601));
#55654=CARTESIAN_POINT('Ctrl Pts',(-6.24670292156264,-2.60810068430576,
31.8231410709227));
#55655=CARTESIAN_POINT('Ctrl Pts',(-6.17644632359794,-2.77038641176818,
31.8314418708853));
#55656=CARTESIAN_POINT('Ctrl Pts',(-6.09992333431186,-2.92971403306153,
31.8397426708479));
#55657=CARTESIAN_POINT('Ctrl Pts',(-6.02342286069177,-3.08899477474999,
31.8480410284328));
#55658=CARTESIAN_POINT('Ctrl Pts',(-5.9406598213746,-3.24531883201725,31.8563393860177));
#55659=CARTESIAN_POINT('Ctrl Pts',(-5.85189598370829,-3.39817633383831,
31.8646377436027));
#55660=CARTESIAN_POINT('Ctrl Pts',(-5.76312311452502,-3.55104938855971,
31.8729369455265));
#55661=CARTESIAN_POINT('Ctrl Pts',(-5.6683483951749,-3.70045487852671,31.8812361474502));
#55662=CARTESIAN_POINT('Ctrl Pts',(-5.56787904463112,-3.84590846801606,
31.889535349374));
#55663=CARTESIAN_POINT('Ctrl Pts',(-5.46739950839948,-3.99137680374247,
31.8978353926796));
#55664=CARTESIAN_POINT('Ctrl Pts',(-5.36122438758727,-4.13289215376013,
31.9061354359852));
#55665=CARTESIAN_POINT('Ctrl Pts',(-5.24970359036488,-4.27000014207378,
31.9144354792907));
#55666=CARTESIAN_POINT('Ctrl Pts',(-5.13815297435195,-4.40714479076368,
31.9227377418887));
#55667=CARTESIAN_POINT('Ctrl Pts',(-5.02125405265445,-4.53987945904959,
31.9310400044865));
#55668=CARTESIAN_POINT('Ctrl Pts',(-4.89939639549994,-4.66778362392284,
31.9393422670845));
#55669=CARTESIAN_POINT('Ctrl Pts',(-4.77748592458961,-4.79574322314046,
31.9476481279271));
#55670=CARTESIAN_POINT('Ctrl Pts',(-4.65061267477801,-4.91886789471148,
31.9559539887697));
#55671=CARTESIAN_POINT('Ctrl Pts',(-4.51920248849852,-5.0367745500418,31.9642598496123));
#55672=CARTESIAN_POINT('Ctrl Pts',(-4.38763696610762,-5.15482057935726,
31.9725755285685));
#55673=CARTESIAN_POINT('Ctrl Pts',(-4.25152405140372,-5.26763603625039,
31.9808912075246));
#55674=CARTESIAN_POINT('Ctrl Pts',(-4.11132294846449,-5.37487791614184,
31.9892068864807));
#55675=CARTESIAN_POINT('Ctrl Pts',(-3.97103316944413,-5.48218762566831,
31.9975278250376));
#55676=CARTESIAN_POINT('Ctrl Pts',(-3.82665032953597,-5.58391652786719,
32.0058487635944));
#55677=CARTESIAN_POINT('Ctrl Pts',(-3.67866203664944,-5.67976536664273,
32.0141697021512));
#55678=CARTESIAN_POINT('Ctrl Pts',(-3.53045378732077,-5.77575666648157,
32.0225030082002));
#55679=CARTESIAN_POINT('Ctrl Pts',(-3.378629674649,-5.86585025973974,32.0308363142491));
#55680=CARTESIAN_POINT('Ctrl Pts',(-3.22370246671382,-5.94979255151835,
32.039169620298));
#55681=CARTESIAN_POINT('Ctrl Pts',(-3.10966689474783,-6.01157903423296,
32.0453034255497));
#55682=CARTESIAN_POINT('Ctrl Pts',(-2.99395061897389,-6.07003381744407,
32.0514372308013));
#55683=CARTESIAN_POINT('Ctrl Pts',(-2.87676452165102,-6.1250726434035,32.057571036053));
#55684=CARTESIAN_POINT('Ctrl Pts',(-2.72256050327969,-6.19749768633331,
32.065642449295));
#55685=CARTESIAN_POINT('Ctrl Pts',(-2.56533592850153,-6.26422877010482,
32.073713862537));
#55686=CARTESIAN_POINT('Ctrl Pts',(-2.40555850139185,-6.32499622896184,
32.0817852757791));
#55687=CARTESIAN_POINT('Ctrl Pts',(-2.24598166160797,-6.38568739930746,
32.0898465560303));
#55688=CARTESIAN_POINT('Ctrl Pts',(-2.08385869058967,-6.44042971072414,
32.0979078362815));
#55689=CARTESIAN_POINT('Ctrl Pts',(-1.91968221119545,-6.48899909138688,
32.1059691165327));
#55690=CARTESIAN_POINT('Ctrl Pts',(-1.75567583711146,-6.53751814870492,
32.1140220443904));
#55691=CARTESIAN_POINT('Ctrl Pts',(-1.58962054337844,-6.57987689829311,
32.122074972248));
#55692=CARTESIAN_POINT('Ctrl Pts',(-1.42202918432237,-6.61589918294826,
32.1301279001056));
#55693=CARTESIAN_POINT('Ctrl Pts',(-1.2545747701153,-6.65189203251583,32.13817424763));
#55694=CARTESIAN_POINT('Ctrl Pts',(-1.0855871515895,-6.68155864466435,32.1462205951543));
#55695=CARTESIAN_POINT('Ctrl Pts',(-0.915594511135806,-6.70477260547873,
32.1542669426787));
#55696=CARTESIAN_POINT('Ctrl Pts',(-0.745703592099352,-6.72797267535649,
32.1623084753719));
#55697=CARTESIAN_POINT('Ctrl Pts',(-0.574809216937471,-6.74472773006746,
32.1703500080651));
#55698=CARTESIAN_POINT('Ctrl Pts',(-0.403449829011714,-6.75496241554832,
32.1783915407582));
#55699=CARTESIAN_POINT('Ctrl Pts',(-0.228796101835591,-6.76539386017091,
32.1865876698065));
#55700=CARTESIAN_POINT('Ctrl Pts',(-0.0536596877783217,-6.76905159753581,
32.1947837988547));
#55701=CARTESIAN_POINT('Ctrl Pts',(0.12138325107208,-6.76591125469136,32.202979927903));
#55702=CARTESIAN_POINT('Ctrl Pts',(0.293065225942237,-6.76283120893318,
32.2110186847391));
#55703=CARTESIAN_POINT('Ctrl Pts',(0.464656896194815,-6.75321180321184,
32.2190574415752));
#55704=CARTESIAN_POINT('Ctrl Pts',(0.635614615127708,-6.73708268177229,
32.2270961984113));
#55705=CARTESIAN_POINT('Ctrl Pts',(0.806588880960806,-6.72095199920426,
32.2351357333141));
#55706=CARTESIAN_POINT('Ctrl Pts',(0.976928701445892,-6.6983103813075,32.2431752682168));
#55707=CARTESIAN_POINT('Ctrl Pts',(1.14609585613162,-6.66923933357905,32.2512148031196));
#55708=CARTESIAN_POINT('Ctrl Pts',(1.31531287956567,-6.64015971600284,32.2592567079951));
#55709=CARTESIAN_POINT('Ctrl Pts',(1.48335618123837,-6.604646959209,32.2672986128707));
#55710=CARTESIAN_POINT('Ctrl Pts',(1.6496981771387,-6.56283360480405,32.2753405177462));
#55711=CARTESIAN_POINT('Ctrl Pts',(1.82165126819941,-6.51960979052532,32.283653694427));
#55712=CARTESIAN_POINT('Ctrl Pts',(1.99178584450771,-6.46965298263884,32.2919668711078));
#55713=CARTESIAN_POINT('Ctrl Pts',(2.15953768467293,-6.41316505233395,32.3002800477887));
#55714=CARTESIAN_POINT('Ctrl Pts',(2.32209727743496,-6.35842553390429,32.3083359153992));
#55715=CARTESIAN_POINT('Ctrl Pts',(2.48241911867582,-6.29755337063983,32.3163917830097));
#55716=CARTESIAN_POINT('Ctrl Pts',(2.6400120116576,-6.23078049511484,32.3244476506202));
#55717=CARTESIAN_POINT('Ctrl Pts',(2.8051553168492,-6.16080847320002,32.3328894818362));
#55718=CARTESIAN_POINT('Ctrl Pts',(2.9673013085468,-6.08435661958424,32.3413313130522));
#55719=CARTESIAN_POINT('Ctrl Pts',(3.12591640348562,-6.0017443829623,32.3497731442682));
#55720=CARTESIAN_POINT('Ctrl Pts',(3.28453149842456,-5.9191321463403,32.3582149754842));
#55721=CARTESIAN_POINT('Ctrl Pts',(3.43961533894103,-5.83035983005544,32.3666568067001));
#55722=CARTESIAN_POINT('Ctrl Pts',(3.59067229527634,-5.73579649812778,32.3750986379161));
#55723=CARTESIAN_POINT('Ctrl Pts',(3.73794693401972,-5.64360093900966,32.3833290939827));
#55724=CARTESIAN_POINT('Ctrl Pts',(3.88188396889984,-5.54559457348232,32.3915595500493));
#55725=CARTESIAN_POINT('Ctrl Pts',(4.02199394598704,-5.44204499232077,32.3997900061158));
#55726=CARTESIAN_POINT('Ctrl Pts',(4.16193760427525,-5.33861833061388,32.408010692146));
#55727=CARTESIAN_POINT('Ctrl Pts',(4.29806296529143,-5.22966176676282,32.4162313781762));
#55728=CARTESIAN_POINT('Ctrl Pts',(4.42990667331544,-5.11548784239737,32.4244520642064));
#55729=CARTESIAN_POINT('Ctrl Pts',(4.56162032701516,-5.00142654238699,32.4326646411218));
#55730=CARTESIAN_POINT('Ctrl Pts',(4.68906046970116,-4.88215836424707,32.4408772180372));
#55731=CARTESIAN_POINT('Ctrl Pts',(4.81179409502263,-4.75803810273787,32.4490897949526));
#55732=CARTESIAN_POINT('Ctrl Pts',(4.93443126777576,-4.6340153835116,32.4572959178573));
#55733=CARTESIAN_POINT('Ctrl Pts',(5.05236903921426,-4.50514842955538,32.465502040762));
#55734=CARTESIAN_POINT('Ctrl Pts',(5.16520871727372,-4.371831184641,32.4737081636666));
#55735=CARTESIAN_POINT('Ctrl Pts',(5.27798234329545,-4.23859197854988,32.4819094830203));
#55736=CARTESIAN_POINT('Ctrl Pts',(5.38566358986551,-4.10090794394812,32.4901108023741));
#55737=CARTESIAN_POINT('Ctrl Pts',(5.48789171907028,-3.95920869363562,32.4983121217278));
#55738=CARTESIAN_POINT('Ctrl Pts',(5.59009052144693,-3.81755009348067,32.5065110883173));
#55739=CARTESIAN_POINT('Ctrl Pts',(5.68683910978897,-3.67187886007352,32.5147100549069));
#55740=CARTESIAN_POINT('Ctrl Pts',(5.77781788769589,-3.5226565907879,32.5229090214964));
#55741=CARTESIAN_POINT('Ctrl Pts',(5.86878465144408,-3.37345402697724,32.5311069053753));
#55742=CARTESIAN_POINT('Ctrl Pts',(5.95398293492057,-3.22070166689604,32.5393047892543));
#55743=CARTESIAN_POINT('Ctrl Pts',(6.03313723726971,-3.06488891744376,32.5475026731332));
#55744=CARTESIAN_POINT('Ctrl Pts',(6.1122954655424,-2.90906843993472,32.5557009636137));
#55745=CARTESIAN_POINT('Ctrl Pts',(6.18540895299778,-2.75018759037932,32.5638992540943));
#55746=CARTESIAN_POINT('Ctrl Pts',(6.25224879121642,-2.58875917240922,32.5720975445748));
#55747=CARTESIAN_POINT('Ctrl Pts',(6.31910408619757,-2.42729342399688,32.5802977309161));
#55748=CARTESIAN_POINT('Ctrl Pts',(6.37968270524256,-2.26327926506783,32.5884979172574));
#55749=CARTESIAN_POINT('Ctrl Pts',(6.43380437632073,-2.097248255986,32.5966981035988));
#55750=CARTESIAN_POINT('Ctrl Pts',(6.4879772151923,-1.93106027761251,32.6049060425729));
#55751=CARTESIAN_POINT('Ctrl Pts',(6.53568079862508,-1.76285198096014,32.613113981547));
#55752=CARTESIAN_POINT('Ctrl Pts',(6.5767848671248,-1.5931697372089,32.6213219205211));
#55753=CARTESIAN_POINT('Ctrl Pts',(6.61790887645348,-1.42340517546032,32.629533841415));
#55754=CARTESIAN_POINT('Ctrl Pts',(6.65242691673485,-1.25216559228056,32.637745762309));
#55755=CARTESIAN_POINT('Ctrl Pts',(6.68026014890569,-1.08000617727054,32.645957683203));
#55756=CARTESIAN_POINT('Ctrl Pts',(6.70813154994514,-0.907610672896134,
32.6541808654455));
#55757=CARTESIAN_POINT('Ctrl Pts',(6.72929977907265,-0.734293171843731,
32.6624040476881));
#55758=CARTESIAN_POINT('Ctrl Pts',(6.74373792122086,-0.560613815284455,
32.6706272299306));
#55759=CARTESIAN_POINT('Ctrl Pts',(6.75661310027526,-0.405735660546783,
32.6779602332134));
#55760=CARTESIAN_POINT('Ctrl Pts',(6.76413715051455,-0.250569959535481,
32.6852932364962));
#55761=CARTESIAN_POINT('Ctrl Pts',(6.76632591716136,-0.0955122125724868,
32.6926262397789));
#55762=CARTESIAN_POINT('Ctrl Pts',(6.76899290612317,0.093424008744249,32.7015614265612));
#55763=CARTESIAN_POINT('Ctrl Pts',(6.7637437604845,0.282591998645421,32.7104966133435));
#55764=CARTESIAN_POINT('Ctrl Pts',(6.75056509323352,0.471338436812814,32.7194318001257));
#55765=CARTESIAN_POINT('Ctrl Pts',(6.73740616354918,0.659802191205731,32.7283536047623));
#55766=CARTESIAN_POINT('Ctrl Pts',(6.71634142687637,0.847845396523924,32.7372754093989));
#55767=CARTESIAN_POINT('Ctrl Pts',(6.68740946285743,1.03481576915162,32.7461972140355));
#55768=CARTESIAN_POINT('Ctrl Pts',(6.65854807076005,1.22133007669985,32.7550972562748));
#55769=CARTESIAN_POINT('Ctrl Pts',(6.6218577907849,1.40677651960491,32.763997298514));
#55770=CARTESIAN_POINT('Ctrl Pts',(6.57742870056266,1.59050956897928,32.7728973407533));
#55771=CARTESIAN_POINT('Ctrl Pts',(6.53306800957807,1.77395975862261,32.7817836812467));
#55772=CARTESIAN_POINT('Ctrl Pts',(6.480992334127,1.95570156660659,32.7906700217401));
#55773=CARTESIAN_POINT('Ctrl Pts',(6.42134286456127,2.13509831524173,32.7995563622334));
#55774=CARTESIAN_POINT('Ctrl Pts',(6.36184590827701,2.3140363777055,32.8084199819053));
#55775=CARTESIAN_POINT('Ctrl Pts',(6.29481388053628,2.49064110088217,32.8172836015772));
#55776=CARTESIAN_POINT('Ctrl Pts',(6.22043774472953,2.66429038656529,32.8261472212491));
#55777=CARTESIAN_POINT('Ctrl Pts',(6.14983215175829,2.8291364175092,32.834561494403));
#55778=CARTESIAN_POINT('Ctrl Pts',(6.07260860983294,2.99131895356997,32.8429757675569));
#55779=CARTESIAN_POINT('Ctrl Pts',(5.98897247047364,3.15031708688329,32.8513900407107));
#55780=CARTESIAN_POINT('Ctrl Pts',(5.90736429702192,3.30545991558551,32.8596002889153));
#55781=CARTESIAN_POINT('Ctrl Pts',(5.81972826442297,3.45742132116671,32.8678105371198));
#55782=CARTESIAN_POINT('Ctrl Pts',(5.72635188422313,3.60571533791206,32.8760207853244));
#55783=CARTESIAN_POINT('Ctrl Pts',(5.63295330659624,3.75404460710146,32.8842329852686));
#55784=CARTESIAN_POINT('Ctrl Pts',(5.53381185236988,3.89870444934127,32.8924451852128));
#55785=CARTESIAN_POINT('Ctrl Pts',(5.42925849200748,4.03923770369667,32.900657385157));
#55786=CARTESIAN_POINT('Ctrl Pts',(5.32466165920383,4.1798293906421,32.9088729996675));
#55787=CARTESIAN_POINT('Ctrl Pts',(5.21464864961048,4.31629078610236,32.917088614178));
#55788=CARTESIAN_POINT('Ctrl Pts',(5.09959089478538,4.44819757944969,32.9253042286885));
#55789=CARTESIAN_POINT('Ctrl Pts',(4.98440393514553,4.58025249834339,32.933529068974));
#55790=CARTESIAN_POINT('Ctrl Pts',(4.86416114944602,4.70774233123302,32.9417539092594));
#55791=CARTESIAN_POINT('Ctrl Pts',(4.73927170448295,4.83027874051667,32.9499787495448));
#55792=CARTESIAN_POINT('Ctrl Pts',(4.61430226348916,4.9528936386299,32.9582088581263));
#55793=CARTESIAN_POINT('Ctrl Pts',(4.48468049291367,5.07054854962502,32.9664389667079));
#55794=CARTESIAN_POINT('Ctrl Pts',(4.35084879418545,5.1828953076572,32.9746690752895));
#55795=CARTESIAN_POINT('Ctrl Pts',(4.21683361014447,5.29539609481873,32.9829104674762));
#55796=CARTESIAN_POINT('Ctrl Pts',(4.07859724970943,5.40257397540435,32.9911518596628));
#55797=CARTESIAN_POINT('Ctrl Pts',(3.93661205132688,5.50412341407313,32.9993932518496));
#55798=CARTESIAN_POINT('Ctrl Pts',(3.87481648565114,5.54832030979238,33.0029801151137));
#55799=CARTESIAN_POINT('Ctrl Pts',(3.81231114292086,5.59145163960211,33.0065669783779));
#55800=CARTESIAN_POINT('Ctrl Pts',(3.74913639406064,5.63349494530083,33.0101538416421));
#55801=CARTESIAN_POINT('Ctrl Pts',(3.60032663912576,5.7325290393108,33.0186027908339));
#55802=CARTESIAN_POINT('Ctrl Pts',(3.4474616679766,5.82574900357178,33.0270517400257));
#55803=CARTESIAN_POINT('Ctrl Pts',(3.29102360987895,5.91282103561569,33.0355006892175));
#55804=CARTESIAN_POINT('Ctrl Pts',(3.22761964408248,5.94811111917128,33.0389250278477));
#55805=CARTESIAN_POINT('Ctrl Pts',(3.16362910304274,5.98239177950754,33.0423493664778));
#55806=CARTESIAN_POINT('Ctrl Pts',(3.09908550384727,6.01564277861009,33.045773705108));
#55807=CARTESIAN_POINT('Ctrl Pts',(3.09908550384736,6.01564277861005,31.0457633158951));
#55808=CARTESIAN_POINT('Ctrl Pts',(2.93978214379508,6.09771127104242,31.0541970845775));
#55809=CARTESIAN_POINT('Ctrl Pts',(2.77728693821518,6.1734119192158,31.06263085326));
#55810=CARTESIAN_POINT('Ctrl Pts',(2.61214130867702,6.24251606193393,31.0710646219425));
#55811=CARTESIAN_POINT('Ctrl Pts',(2.44685001542714,6.31168115670966,31.0795058294778));
#55812=CARTESIAN_POINT('Ctrl Pts',(2.2789039384388,6.37423800109378,31.0879470370132));
#55813=CARTESIAN_POINT('Ctrl Pts',(2.10886249709093,6.43000684046008,31.0963882445486));
#55814=CARTESIAN_POINT('Ctrl Pts',(2.0511158617316,6.44894612258902,31.0992549065204));
#55815=CARTESIAN_POINT('Ctrl Pts',(1.99312768629269,6.46710296868331,31.1021215684921));
#55816=CARTESIAN_POINT('Ctrl Pts',(1.93492021400103,6.48447166432626,31.1049882304639));
#55817=CARTESIAN_POINT('Ctrl Pts',(1.76961003393245,6.5337990460395,31.1131295976818));
#55818=CARTESIAN_POINT('Ctrl Pts',(1.60220166882337,6.57686372138172,31.1212709648996));
#55819=CARTESIAN_POINT('Ctrl Pts',(1.43321504134359,6.61348498488252,31.1294123321175));
#55820=CARTESIAN_POINT('Ctrl Pts',(1.26437592633729,6.65007428080551,31.137546592541));
#55821=CARTESIAN_POINT('Ctrl Pts',(1.09396164660413,6.68023128374515,31.1456808529645));
#55822=CARTESIAN_POINT('Ctrl Pts',(0.922507776869986,6.70382490833512,31.1538151133879));
#55823=CARTESIAN_POINT('Ctrl Pts',(0.751170866772573,6.72740243820665,31.1619438249128));
#55824=CARTESIAN_POINT('Ctrl Pts',(0.578796139762534,6.74442545419302,31.1700725364376));
#55825=CARTESIAN_POINT('Ctrl Pts',(0.405929832819718,6.75481383687419,31.1782012479625));
#55826=CARTESIAN_POINT('Ctrl Pts',(0.233145962624057,6.76519726552763,31.186326083055));
#55827=CARTESIAN_POINT('Ctrl Pts',(0.0598713439351249,6.76895233946947,
31.1944509181475));
#55828=CARTESIAN_POINT('Ctrl Pts',(-0.113342202082167,6.76605073475119,
31.2025757532401));
#55829=CARTESIAN_POINT('Ctrl Pts',(-0.2865072564816,6.76314994234529,31.2106983137623));
#55830=CARTESIAN_POINT('Ctrl Pts',(-0.459610906599376,6.75359619007722,
31.2188208742844));
#55831=CARTESIAN_POINT('Ctrl Pts',(-0.632100897357243,6.73741326144984,
31.2269434348066));
#55832=CARTESIAN_POINT('Ctrl Pts',(-0.804600055510615,6.72122947274179,
31.2350664270218));
#55833=CARTESIAN_POINT('Ctrl Pts',(-0.976485124324183,6.69841583412734,
31.2431894192369));
#55834=CARTESIAN_POINT('Ctrl Pts',(-1.14720834676363,6.66904805868993,31.2513124114521));
#55835=CARTESIAN_POINT('Ctrl Pts',(-1.23435734910002,6.65405670429983,31.2554589514332));
#55836=CARTESIAN_POINT('Ctrl Pts',(-1.32120370627018,6.6373583099481,31.2596054914143));
#55837=CARTESIAN_POINT('Ctrl Pts',(-1.40767548398425,6.61896810173532,31.2637520313953));
#55838=CARTESIAN_POINT('Ctrl Pts',(-1.59502034743857,6.57912491662224,31.2727356904237));
#55839=CARTESIAN_POINT('Ctrl Pts',(-1.78051361467214,6.53135738162034,31.281719349452));
#55840=CARTESIAN_POINT('Ctrl Pts',(-1.9635166759737,6.47586992327465,31.2907030084804));
#55841=CARTESIAN_POINT('Ctrl Pts',(-2.14683413459578,6.42028713806337,31.2997021013398));
#55842=CARTESIAN_POINT('Ctrl Pts',(-2.32765260758264,6.3569579904057,31.3087011941992));
#55843=CARTESIAN_POINT('Ctrl Pts',(-2.5053511830219,6.28613589176457,31.3177002870585));
#55844=CARTESIAN_POINT('Ctrl Pts',(-2.68346641196309,6.21514773509321,31.3267204802759));
#55845=CARTESIAN_POINT('Ctrl Pts',(-2.8584468837172,6.13663156412673,31.3357406734933));
#55846=CARTESIAN_POINT('Ctrl Pts',(-3.02969160558259,6.05088900700239,31.3447608667106));
#55847=CARTESIAN_POINT('Ctrl Pts',(-3.20110975560926,5.96505961406868,31.3537901951323));
#55848=CARTESIAN_POINT('Ctrl Pts',(-3.36878438653771,5.87198932674126,31.362819523554));
#55849=CARTESIAN_POINT('Ctrl Pts',(-3.53214007237226,5.77202525194945,31.3718488519757));
#55850=CARTESIAN_POINT('Ctrl Pts',(-3.69572605679668,5.67192024796167,31.3808909099305));
#55851=CARTESIAN_POINT('Ctrl Pts',(-3.8549807173307,5.56490214844779,31.3899329678852));
#55852=CARTESIAN_POINT('Ctrl Pts',(-4.0093565897801,5.45136209914429,31.39897502584));
#55853=CARTESIAN_POINT('Ctrl Pts',(-4.14332802850144,5.35282906081172,31.4068219613356));
#55854=CARTESIAN_POINT('Ctrl Pts',(-4.27362554592084,5.2493849196875,31.4146688968313));
#55855=CARTESIAN_POINT('Ctrl Pts',(-4.39991149110694,5.14130993720716,31.422515832327));
#55856=CARTESIAN_POINT('Ctrl Pts',(-4.53917744008327,5.02212672189731,31.4311692966278));
#55857=CARTESIAN_POINT('Ctrl Pts',(-4.67368667760506,4.89720573293097,31.4398227609286));
#55858=CARTESIAN_POINT('Ctrl Pts',(-4.80297040682896,4.7669449620407,31.4484762252294));
#55859=CARTESIAN_POINT('Ctrl Pts',(-4.93213503929425,4.63680418796427,31.4571217179196));
#55860=CARTESIAN_POINT('Ctrl Pts',(-5.05608355122076,4.50133365812178,31.4657672106098));
#55861=CARTESIAN_POINT('Ctrl Pts',(-5.17438220667066,4.36096982095613,31.4744127033));
#55862=CARTESIAN_POINT('Ctrl Pts',(-5.29623967409301,4.21638337870418,31.4833182807965));
#55863=CARTESIAN_POINT('Ctrl Pts',(-5.41210179073021,4.06660482120568,31.492223858293));
#55864=CARTESIAN_POINT('Ctrl Pts',(-5.52153582322863,3.91215172926651,31.5011294357896));
#55865=CARTESIAN_POINT('Ctrl Pts',(-5.62757228362368,3.76249390534837,31.5097585239621));
#55866=CARTESIAN_POINT('Ctrl Pts',(-5.72757361259153,3.60844771641768,31.5183876121346));
#55867=CARTESIAN_POINT('Ctrl Pts',(-5.82118697962478,3.45051751890161,31.5270167003072));
#55868=CARTESIAN_POINT('Ctrl Pts',(-5.91929962214053,3.28499682989753,31.5360605224657));
#55869=CARTESIAN_POINT('Ctrl Pts',(-6.0103949046184,3.11520983685613,31.5451043446242));
#55870=CARTESIAN_POINT('Ctrl Pts',(-6.0941174845633,2.9417717593892,31.5541481667827));
#55871=CARTESIAN_POINT('Ctrl Pts',(-6.1778400645082,2.76833368192228,31.5631919889412));
#55872=CARTESIAN_POINT('Ctrl Pts',(-6.25418974322116,2.5912448519767,31.5722358110998));
#55873=CARTESIAN_POINT('Ctrl Pts',(-6.32286637598467,2.41115113409395,31.5812796332583));
#55874=CARTESIAN_POINT('Ctrl Pts',(-6.38454938399387,2.24939710225573,31.5894024857074));
#55875=CARTESIAN_POINT('Ctrl Pts',(-6.44003201479634,2.08524629932887,31.5975253381565));
#55876=CARTESIAN_POINT('Ctrl Pts',(-6.48913545647371,1.91922120338844,31.6056481906056));
#55877=CARTESIAN_POINT('Ctrl Pts',(-6.53825536735526,1.75314042293563,31.6137737674445));
#55878=CARTESIAN_POINT('Ctrl Pts',(-6.58099170619849,1.58518444405631,31.6218993442833));
#55879=CARTESIAN_POINT('Ctrl Pts',(-6.61721562648338,1.41589065701564,31.6300249211222));
#55880=CARTESIAN_POINT('Ctrl Pts',(-6.65344540730411,1.24656948055111,31.6381518125685));
#55881=CARTESIAN_POINT('Ctrl Pts',(-6.68316060146275,1.07591042487806,31.6462787040148));
#55882=CARTESIAN_POINT('Ctrl Pts',(-6.70628368056084,0.904460168190584,
31.6544055954611));
#55883=CARTESIAN_POINT('Ctrl Pts',(-6.72942557385929,0.732870410208039,
31.6625390993903));
#55884=CARTESIAN_POINT('Ctrl Pts',(-6.74596459569385,0.560488529650756,
31.6706726033194));
#55885=CARTESIAN_POINT('Ctrl Pts',(-6.75587513796982,0.387866111127572,
31.6788061072486));
#55886=CARTESIAN_POINT('Ctrl Pts',(-6.76333781332565,0.257880785127765,
31.6849306660909));
#55887=CARTESIAN_POINT('Ctrl Pts',(-6.76704311804857,0.127759179243045,
31.6910552249333));
#55888=CARTESIAN_POINT('Ctrl Pts',(-6.76699962134934,-0.00226377072111077,
31.6971797837756));
#55889=CARTESIAN_POINT('',(-6.767,4.09441144183509E-12,31.3028202161898));
#55890=CARTESIAN_POINT('Ctrl Pts',(3.09908550384718,6.01564277861014,30.6513967904261));
#55891=CARTESIAN_POINT('Ctrl Pts',(2.93373232018331,6.10082796552479,30.6601462383254));
#55892=CARTESIAN_POINT('Ctrl Pts',(2.76486502144433,6.17919158180187,30.6688956862247));
#55893=CARTESIAN_POINT('Ctrl Pts',(2.59305716434363,6.25046746591374,30.677645134124));
#55894=CARTESIAN_POINT('Ctrl Pts',(2.42125069459292,6.32174277447221,30.6863945113714));
#55895=CARTESIAN_POINT('Ctrl Pts',(2.24650397871066,6.38593035557823,30.6951438886189));
#55896=CARTESIAN_POINT('Ctrl Pts',(2.06941053323777,6.44281220003537,30.7038932658663));
#55897=CARTESIAN_POINT('Ctrl Pts',(1.892318458967,6.4996936040668,30.7126425753689));
#55898=CARTESIAN_POINT('Ctrl Pts',(1.71287996431534,6.54926929700873,30.7213918848714));
#55899=CARTESIAN_POINT('Ctrl Pts',(1.53170449173545,6.59137090065469,30.730141194374));
#55900=CARTESIAN_POINT('Ctrl Pts',(1.35053036178223,6.63347219230072,30.7388904390386));
#55901=CARTESIAN_POINT('Ctrl Pts',(1.1676195587891,6.66809944062442,30.7476396837032));
#55902=CARTESIAN_POINT('Ctrl Pts',(0.983593309311263,6.6951350398538,30.7563889283678));
#55903=CARTESIAN_POINT('Ctrl Pts',(0.799568362460831,6.72217044771204,30.765138111101));
#55904=CARTESIAN_POINT('Ctrl Pts',(0.614428268439518,6.74161427235968,30.7738872938341));
#55905=CARTESIAN_POINT('Ctrl Pts',(0.428801816331264,6.75340047696796,30.7826364765673));
#55906=CARTESIAN_POINT('Ctrl Pts',(0.243176616523825,6.76518660206238,30.7913856002754));
#55907=CARTESIAN_POINT('Ctrl Pts',(0.0570653511665475,6.76931519233996,
30.8001347239836));
#55908=CARTESIAN_POINT('Ctrl Pts',(-0.128899900798899,6.76577222610797,
30.8088838476917));
#55909=CARTESIAN_POINT('Ctrl Pts',(-0.31486395994078,6.76222928260138,30.817632915281));
#55910=CARTESIAN_POINT('Ctrl Pts',(-0.500681721079332,6.75101488651286,
30.8263819828702));
#55911=CARTESIAN_POINT('Ctrl Pts',(-0.685722110171844,6.73216712416006,
30.8351310504595));
#55912=CARTESIAN_POINT('Ctrl Pts',(-0.870761373826321,6.71331947644162,
30.8438800648358));
#55913=CARTESIAN_POINT('Ctrl Pts',(-1.0550229898423,6.68683858440015,30.8526290792122));
#55914=CARTESIAN_POINT('Ctrl Pts',(-1.23788117675963,6.65281438131444,30.8613780935886));
#55915=CARTESIAN_POINT('Ctrl Pts',(-1.43009641451701,6.61704912302397,30.8705748044761));
#55916=CARTESIAN_POINT('Ctrl Pts',(-1.62076048992608,6.57294837083187,30.8797715153636));
#55917=CARTESIAN_POINT('Ctrl Pts',(-1.80915798961049,6.52067760042072,30.8889682262512));
#55918=CARTESIAN_POINT('Ctrl Pts',(-1.98840443002933,6.47094578577433,30.8977182239577));
#55919=CARTESIAN_POINT('Ctrl Pts',(-2.16559895952116,6.41381888474501,30.9064682216642));
#55920=CARTESIAN_POINT('Ctrl Pts',(-2.3401396624225,6.34949095285261,30.9152182193707));
#55921=CARTESIAN_POINT('Ctrl Pts',(-2.51467682553944,6.28516432556713,30.9239680396223));
#55922=CARTESIAN_POINT('Ctrl Pts',(-2.68656000078773,6.21363705879691,30.9327178598739));
#55923=CARTESIAN_POINT('Ctrl Pts',(-2.85520533840821,6.13515211510891,30.9414676801255));
#55924=CARTESIAN_POINT('Ctrl Pts',(-3.02384747998257,6.05666865881156,30.9502173345567));
#55925=CARTESIAN_POINT('Ctrl Pts',(-3.18925164684464,5.97122791039883,30.958966988988));
#55926=CARTESIAN_POINT('Ctrl Pts',(-3.35085601829082,5.87912008251951,30.9677166434192));
#55927=CARTESIAN_POINT('Ctrl Pts',(-3.51245754191338,5.78701387778223,30.9764661436623));
#55928=CARTESIAN_POINT('Ctrl Pts',(-3.67025915510852,5.68824097061037,30.9852156439055));
#55929=CARTESIAN_POINT('Ctrl Pts',(-3.82372487928746,5.58313684656915,30.9939651441486));
#55930=CARTESIAN_POINT('Ctrl Pts',(-3.97718810300689,5.47803443501851,31.0027145018337));
#55931=CARTESIAN_POINT('Ctrl Pts',(-4.12631534262898,5.36660117496473,31.0114638595188));
#55932=CARTESIAN_POINT('Ctrl Pts',(-4.2706000988608,5.24921554097468,31.0202132172039));
#55933=CARTESIAN_POINT('Ctrl Pts',(-4.41488269594072,5.13183166360413,31.0289624439591));
#55934=CARTESIAN_POINT('Ctrl Pts',(-4.55432273234951,5.00849577139596,31.0377116707143));
#55935=CARTESIAN_POINT('Ctrl Pts',(-4.68844662480073,4.87962675277471,31.0464608974695));
#55936=CARTESIAN_POINT('Ctrl Pts',(-4.82256868835018,4.75075949140023,31.0552100049209));
#55937=CARTESIAN_POINT('Ctrl Pts',(-4.95137454637718,4.61635945312679,31.0639591123724));
#55938=CARTESIAN_POINT('Ctrl Pts',(-5.0744267446093,4.47688309134758,31.0727082198239));
#55939=CARTESIAN_POINT('Ctrl Pts',(-5.19747742838395,4.33740844616524,31.0814572195963));
#55940=CARTESIAN_POINT('Ctrl Pts',(-5.31477440450787,4.19285781736207,31.0902062193687));
#55941=CARTESIAN_POINT('Ctrl Pts',(-5.42591931531016,4.0437221199959,31.098955219141));
#55942=CARTESIAN_POINT('Ctrl Pts',(-5.53707636462853,3.89457013500984,31.1077051744216));
#55943=CARTESIAN_POINT('Ctrl Pts',(-5.6420798327335,3.74083230916602,31.1164551297022));
#55944=CARTESIAN_POINT('Ctrl Pts',(-5.74057303468635,3.58303087252008,31.1252050849828));
#55945=CARTESIAN_POINT('Ctrl Pts',(-5.83906243363655,3.42523552887618,31.1339547024116));
#55946=CARTESIAN_POINT('Ctrl Pts',(-5.93104191768319,3.26337713157186,31.1427043198404));
#55947=CARTESIAN_POINT('Ctrl Pts',(-6.01619906699553,3.09800545291355,31.1514539372692));
#55948=CARTESIAN_POINT('Ctrl Pts',(-6.10135338095288,2.93263928039793,31.1602032633746));
#55949=CARTESIAN_POINT('Ctrl Pts',(-6.17968568352752,2.76376031540419,31.16895258948));
#55950=CARTESIAN_POINT('Ctrl Pts',(-6.25092992694807,2.59194213831734,31.1777019155854));
#55951=CARTESIAN_POINT('Ctrl Pts',(-6.32217217691038,2.42012876880994,31.1864509968792));
#55952=CARTESIAN_POINT('Ctrl Pts',(-6.38632665483796,2.24537661647826,31.195200078173));
#55953=CARTESIAN_POINT('Ctrl Pts',(-6.44317547869306,2.06827917621592,31.2039491594668));
#55954=CARTESIAN_POINT('Ctrl Pts',(-6.50002944235893,1.89116572423572,31.2126990317817));
#55955=CARTESIAN_POINT('Ctrl Pts',(-6.54957634250356,1.71170683289359,31.2214489040967));
#55956=CARTESIAN_POINT('Ctrl Pts',(-6.59164787708355,1.53051209225537,31.2301987764117));
#55957=CARTESIAN_POINT('Ctrl Pts',(-6.63371649074972,1.3493299314821,31.2389480412465));
#55958=CARTESIAN_POINT('Ctrl Pts',(-6.66831071257091,1.16641244174191,31.2476973060813));
#55959=CARTESIAN_POINT('Ctrl Pts',(-6.69531304840304,0.982380875161951,
31.256446570916));
#55960=CARTESIAN_POINT('Ctrl Pts',(-6.72231677033021,0.798339861797786,
31.2651962848717));
#55961=CARTESIAN_POINT('Ctrl Pts',(-6.74172778477872,0.613184940732099,
31.2739459988273));
#55962=CARTESIAN_POINT('Ctrl Pts',(-6.75348015835506,0.427545027692498,
31.282695712783));
#55963=CARTESIAN_POINT('Ctrl Pts',(-6.76249038365209,0.285219953549511,
31.2894038805853));
#55964=CARTESIAN_POINT('Ctrl Pts',(-6.76699999999992,0.142609995760739,
31.2961120483875));
#55965=CARTESIAN_POINT('Ctrl Pts',(-6.767,4.09441144960993E-12,31.3028202161898));
#55966=CARTESIAN_POINT('Ctrl Pts',(-6.76699999999999,3.85398425696932E-7,
31.3028286423802));
#55967=CARTESIAN_POINT('Ctrl Pts',(-6.76700001009724,-0.177291765525944,
31.3111296342103));
#55968=CARTESIAN_POINT('Ctrl Pts',(-6.76002823219753,-0.35452500436781,
31.3194306260403));
#55969=CARTESIAN_POINT('Ctrl Pts',(-6.7461245034264,-0.531124452713244,
31.3277316178704));
#55970=CARTESIAN_POINT('Ctrl Pts',(-6.73221366727717,-0.707814176054133,
31.3360368530433));
#55971=CARTESIAN_POINT('Ctrl Pts',(-6.71136384379665,-0.883869119375745,
31.3443420882161));
#55972=CARTESIAN_POINT('Ctrl Pts',(-6.68366659620006,-1.05872084651222,
31.352647323389));
#55973=CARTESIAN_POINT('Ctrl Pts',(-6.65593315543186,-1.23380105983825,
31.3609634113659));
#55974=CARTESIAN_POINT('Ctrl Pts',(-6.62133446535324,-1.40767457409,31.3692794993429));
#55975=CARTESIAN_POINT('Ctrl Pts',(-6.58001323514508,-1.5797831576883,31.3775955873198));
#55976=CARTESIAN_POINT('Ctrl Pts',(-6.53866348691055,-1.75201052277253,
31.385917414681));
#55977=CARTESIAN_POINT('Ctrl Pts',(-6.49058203898741,-1.92247019636217,
31.3942392420421));
#55978=CARTESIAN_POINT('Ctrl Pts',(-6.43596117186355,-2.09062019369009,
31.4025610694033));
#55979=CARTESIAN_POINT('Ctrl Pts',(-6.38125239988589,-2.25904080555985,
31.4108962896133));
#55980=CARTESIAN_POINT('Ctrl Pts',(-6.31998329308616,-2.42514398813847,
31.4192315098233));
#55981=CARTESIAN_POINT('Ctrl Pts',(-6.25239444022301,-2.58840737981261,
31.4275667300333));
#55982=CARTESIAN_POINT('Ctrl Pts',(-6.19730143494457,-2.72148658619436,
31.4343609322068));
#55983=CARTESIAN_POINT('Ctrl Pts',(-6.13801039301637,-2.85267932733502,
31.4411551343802));
#55984=CARTESIAN_POINT('Ctrl Pts',(-6.07467368380669,-2.98171572006227,
31.4479493365537));
#55985=CARTESIAN_POINT('Ctrl Pts',(-5.99591537686446,-3.14217065925854,
31.4563978313822));
#55986=CARTESIAN_POINT('Ctrl Pts',(-5.91072768780452,-3.29964212496179,
31.4648463262106));
#55987=CARTESIAN_POINT('Ctrl Pts',(-5.81935924605262,-3.45359913212027,
31.473294821039));
#55988=CARTESIAN_POINT('Ctrl Pts',(-5.7280742640647,-3.60741550849602,31.4817355986582));
#55989=CARTESIAN_POINT('Ctrl Pts',(-5.63061995245565,-3.75772353995931,
31.4901763762773));
#55990=CARTESIAN_POINT('Ctrl Pts',(-5.52729130552716,-3.90401585855436,
31.4986171538965));
#55991=CARTESIAN_POINT('Ctrl Pts',(-5.42404115359031,-4.05019704422869,
31.5070515193658));
#55992=CARTESIAN_POINT('Ctrl Pts',(-5.31492575410719,-4.19236832701484,
31.5154858848351));
#55993=CARTESIAN_POINT('Ctrl Pts',(-5.20028415625305,-4.33005007987478,
31.5239202503044));
#55994=CARTESIAN_POINT('Ctrl Pts',(-5.08571204217955,-4.46764838441495,
31.532349503741));
#55995=CARTESIAN_POINT('Ctrl Pts',(-4.96562062041456,-4.60076232855225,
31.5407787571776));
#55996=CARTESIAN_POINT('Ctrl Pts',(-4.84039031513101,-4.72894391986053,
31.5492080106142));
#55997=CARTESIAN_POINT('Ctrl Pts',(-4.71521670143398,-4.8570674835392,31.5576334481394));
#55998=CARTESIAN_POINT('Ctrl Pts',(-4.58490907565386,-4.98026290865399,
31.5660588856645));
#55999=CARTESIAN_POINT('Ctrl Pts',(-4.44988621019408,-5.0981174678821,31.5744843231897));
#56000=CARTESIAN_POINT('Ctrl Pts',(-4.31489300562593,-5.21594613763365,
31.5829079098729));
#56001=CARTESIAN_POINT('Ctrl Pts',(-4.17518687582563,-5.32843605967748,
31.5913314965561));
#56002=CARTESIAN_POINT('Ctrl Pts',(-4.03122170360776,-5.43521302032972,
31.5997550832393));
#56003=CARTESIAN_POINT('Ctrl Pts',(-3.88727264033771,-5.54197803320001,
31.6081777273673));
#56004=CARTESIAN_POINT('Ctrl Pts',(-3.73906575244608,-5.64303116049174,
31.6166003714953));
#56005=CARTESIAN_POINT('Ctrl Pts',(-3.58708634329544,-5.73803978425937,
31.6250230156233));
#56006=CARTESIAN_POINT('Ctrl Pts',(-3.43510274693006,-5.83305102562837,
31.6334458918052));
#56007=CARTESIAN_POINT('Ctrl Pts',(-3.27934670499372,-5.9220172550498,31.6418687679872));
#56008=CARTESIAN_POINT('Ctrl Pts',(-3.12033102343843,-6.00465014003045,
31.6502916441691));
#56009=CARTESIAN_POINT('Ctrl Pts',(-2.96128878538232,-6.08729682516123,
31.6587159270181));
#56010=CARTESIAN_POINT('Ctrl Pts',(-2.7989861184597,-6.16360790392657,31.6671402098671));
#56011=CARTESIAN_POINT('Ctrl Pts',(-2.63395918026583,-6.23334164286648,
31.675564492716));
#56012=CARTESIAN_POINT('Ctrl Pts',(-2.46882078897949,-6.30312247739538,
31.6839944650142));
#56013=CARTESIAN_POINT('Ctrl Pts',(-2.30095475736142,-6.36631696590148,
31.6924244373123));
#56014=CARTESIAN_POINT('Ctrl Pts',(-2.13091686438916,-6.42273168652263,
31.7008544096105));
#56015=CARTESIAN_POINT('Ctrl Pts',(-1.96081818561475,-6.47916657449581,
31.7092873954877));
#56016=CARTESIAN_POINT('Ctrl Pts',(-1.78854641571458,-6.52881676278467,
31.7177203813648));
#56017=CARTESIAN_POINT('Ctrl Pts',(-1.61467169920262,-6.5715389600758,31.726153367242));
#56018=CARTESIAN_POINT('Ctrl Pts',(-1.44063701901058,-6.61430046152821,
31.7345941114148));
#56019=CARTESIAN_POINT('Ctrl Pts',(-1.26499677117063,-6.65012116395491,
31.7430348555876));
#56020=CARTESIAN_POINT('Ctrl Pts',(-1.08833156359738,-6.67890884858281,
31.7514755997604));
#56021=CARTESIAN_POINT('Ctrl Pts',(-0.99064865201976,-6.69482632826462,
31.7561427126459));
#56022=CARTESIAN_POINT('Ctrl Pts',(-0.892652510235858,-6.70859453374112,
31.7608098255314));
#56023=CARTESIAN_POINT('Ctrl Pts',(-0.794441887477484,-6.72020469088712,
31.7654769384169));
#56024=CARTESIAN_POINT('Ctrl Pts',(-0.623122109235702,-6.74045758707839,
31.7736183056347));
#56025=CARTESIAN_POINT('Ctrl Pts',(-0.450809018270542,-6.75418076647741,
31.7817596728526));
#56026=CARTESIAN_POINT('Ctrl Pts',(-0.27804582147657,-6.7612853453437,31.7899010400705));
#56027=CARTESIAN_POINT('Ctrl Pts',(-0.105433433813596,-6.76838372245299,
31.7980353004939));
#56028=CARTESIAN_POINT('Ctrl Pts',(0.0676279143409377,-6.7688749843508,
31.8061695609174));
#56029=CARTESIAN_POINT('Ctrl Pts',(0.24058810366446,-6.76272181627894,31.8143038213409));
#56030=CARTESIAN_POINT('Ctrl Pts',(0.413430305793929,-6.7565728456761,31.8224325328657));
#56031=CARTESIAN_POINT('Ctrl Pts',(0.586171122158248,-6.74378848230862,
31.8305612443905));
#56032=CARTESIAN_POINT('Ctrl Pts',(0.758258667673219,-6.72438345076323,
31.8386899559153));
#56033=CARTESIAN_POINT('Ctrl Pts',(0.930264147817969,-6.70498767311878,
31.8468147910079));
#56034=CARTESIAN_POINT('Ctrl Pts',(1.10161661451117,-6.6789775554696,31.8549396261004));
#56035=CARTESIAN_POINT('Ctrl Pts',(1.27176756200563,-6.64641980830509,31.8630644611929));
#56036=CARTESIAN_POINT('Ctrl Pts',(1.44187087526515,-6.61387117577321,31.871187021715));
#56037=CARTESIAN_POINT('Ctrl Pts',(1.61077298025001,-6.57477863431058,31.8793095822372));
#56038=CARTESIAN_POINT('Ctrl Pts',(1.77793387804411,-6.52926030460596,31.8874321427593));
#56039=CARTESIAN_POINT('Ctrl Pts',(1.94510366000662,-6.48373955572009,31.8955551349745));
#56040=CARTESIAN_POINT('Ctrl Pts',(2.11053169567993,-6.43179242874369,31.9036781271897));
#56041=CARTESIAN_POINT('Ctrl Pts',(2.27369132140218,-6.37358743369701,31.9118011194049));
#56042=CARTESIAN_POINT('Ctrl Pts',(2.35697933811328,-6.34387555749811,31.915947659386));
#56043=CARTESIAN_POINT('Ctrl Pts',(2.43967650322425,-6.31253381200568,31.9200941993671));
#56044=CARTESIAN_POINT('Ctrl Pts',(2.52171455836815,-6.27958953165843,31.9242407393482));
#56045=CARTESIAN_POINT('Ctrl Pts',(2.69945356923415,-6.20821431692009,31.9332243983766));
#56046=CARTESIAN_POINT('Ctrl Pts',(2.87400969861641,-6.12934957648348,31.9422080574049));
#56047=CARTESIAN_POINT('Ctrl Pts',(3.04478884474696,-6.04330620529065,31.9511917164333));
#56048=CARTESIAN_POINT('Ctrl Pts',(3.21586138764105,-5.9571150124978,31.9601908092926));
#56049=CARTESIAN_POINT('Ctrl Pts',(3.38314376436154,-5.86372064674218,31.969189902152));
#56050=CARTESIAN_POINT('Ctrl Pts',(3.54606770778625,-5.76347922801806,31.9781889950114));
#56051=CARTESIAN_POINT('Ctrl Pts',(3.70937366232987,-5.66300277117907,31.9872091882288));
#56052=CARTESIAN_POINT('Ctrl Pts',(3.86830053205349,-5.55564726513335,31.9962293814461));
#56053=CARTESIAN_POINT('Ctrl Pts',(4.02230794127331,-5.4418129171784,32.0052495746635));
#56054=CARTESIAN_POINT('Ctrl Pts',(4.17647132155895,-5.32786328344164,32.0142789030851));
#56055=CARTESIAN_POINT('Ctrl Pts',(4.32570509960904,-5.20742184651481,32.0233082315069));
#56056=CARTESIAN_POINT('Ctrl Pts',(4.46950188560458,-5.08092923534437,32.0323375599285));
#56057=CARTESIAN_POINT('Ctrl Pts',(4.61350139608383,-4.95425829508879,32.0413796178833));
#56058=CARTESIAN_POINT('Ctrl Pts',(4.75204840847654,-4.82151928092027,32.050421675838));
#56059=CARTESIAN_POINT('Ctrl Pts',(4.88467063155627,-4.68319141411193,32.0594637337928));
#56060=CARTESIAN_POINT('Ctrl Pts',(4.9997636817242,-4.56314685638631,32.0673106692885));
#56061=CARTESIAN_POINT('Ctrl Pts',(5.11039516174533,-4.43889385236908,32.0751576047843));
#56062=CARTESIAN_POINT('Ctrl Pts',(5.21628047439694,-4.31076640661788,32.08300454028));
#56063=CARTESIAN_POINT('Ctrl Pts',(5.33304895981509,-4.16946968277394,32.0916580045808));
#56064=CARTESIAN_POINT('Ctrl Pts',(5.44414737920278,-4.02333573848796,32.1003114688816));
#56065=CARTESIAN_POINT('Ctrl Pts',(5.5491821175239,-3.87283705138145,32.1089649331824));
#56066=CARTESIAN_POINT('Ctrl Pts',(5.6541200973669,-3.72247700434923,32.1176104258726));
#56067=CARTESIAN_POINT('Ctrl Pts',(5.75300536396091,-3.56776048255794,32.1262559185628));
#56068=CARTESIAN_POINT('Ctrl Pts',(5.84548543773335,-3.40919183931433,32.134901411253));
#56069=CARTESIAN_POINT('Ctrl Pts',(5.94074761576993,-3.24585293064452,32.1438069887495));
#56070=CARTESIAN_POINT('Ctrl Pts',(6.02921298958072,-3.07842675588515,32.152712566246));
#56071=CARTESIAN_POINT('Ctrl Pts',(6.11054397824642,-2.90749742732757,32.1616181437425));
#56072=CARTESIAN_POINT('Ctrl Pts',(6.18934990325549,-2.74187490054964,32.1702472319151));
#56073=CARTESIAN_POINT('Ctrl Pts',(6.26145764313278,-2.57296377608173,32.1788763200876));
#56074=CARTESIAN_POINT('Ctrl Pts',(6.32660606909151,-2.40132143757027,32.1875054082601));
#56075=CARTESIAN_POINT('Ctrl Pts',(6.39488567946284,-2.22142957027925,32.1965492304186));
#56076=CARTESIAN_POINT('Ctrl Pts',(6.45552035026923,-2.03853777114086,32.2055930525772));
#56077=CARTESIAN_POINT('Ctrl Pts',(6.50826548648449,-1.85331307593585,32.2146368747357));
#56078=CARTESIAN_POINT('Ctrl Pts',(6.56101062269975,-1.66808838073083,32.2236806968943));
#56079=CARTESIAN_POINT('Ctrl Pts',(6.60586608548287,-1.48053115055913,32.2327245190528));
#56080=CARTESIAN_POINT('Ctrl Pts',(6.64264691453548,-1.29132914813085,32.2417683412113));
#56081=CARTESIAN_POINT('Ctrl Pts',(6.67691423322725,-1.11505673988637,32.2501941310611));
#56082=CARTESIAN_POINT('Ctrl Pts',(6.70415801674973,-0.937433912934323,
32.2586199209109));
#56083=CARTESIAN_POINT('Ctrl Pts',(6.72429472379184,-0.759045102470971,
32.2670457107607));
#56084=CARTESIAN_POINT('Ctrl Pts',(6.74443610322751,-0.580614899801526,
32.2754734556772));
#56085=CARTESIAN_POINT('Ctrl Pts',(6.7574670809708,-0.401418688658511,32.2839012005938));
#56086=CARTESIAN_POINT('Ctrl Pts',(6.76335602080805,-0.222045796626584,
32.2923289455103));
#56087=CARTESIAN_POINT('Ctrl Pts',(6.7692471245352,-0.0426069940570784,
32.3007597872002));
#56088=CARTESIAN_POINT('Ctrl Pts',(6.76799094678658,0.137008287681627,32.3091906288901));
#56089=CARTESIAN_POINT('Ctrl Pts',(6.75960796831947,0.316210554270361,32.31762147058));
#56090=CARTESIAN_POINT('Ctrl Pts',(6.75121728696513,0.495577484869227,32.3260600591374));
#56091=CARTESIAN_POINT('Ctrl Pts',(6.73568673686856,0.674530310722837,32.3344986476947));
#56092=CARTESIAN_POINT('Ctrl Pts',(6.71308879052693,0.852483366700916,32.342937236252));
#56093=CARTESIAN_POINT('Ctrl Pts',(6.69047899482105,1.03052973339614,32.3513802496322));
#56094=CARTESIAN_POINT('Ctrl Pts',(6.66079446146052,1.20757495719898,32.3598232630124));
#56095=CARTESIAN_POINT('Ctrl Pts',(6.6241589308752,1.38304282598419,32.3682662763926));
#56096=CARTESIAN_POINT('Ctrl Pts',(6.58748491211128,1.55869503599674,32.3767181597469));
#56097=CARTESIAN_POINT('Ctrl Pts',(6.54384538413784,1.73276625823651,32.3851700431012));
#56098=CARTESIAN_POINT('Ctrl Pts',(6.49341443362765,1.9046936743624,32.3936219264555));
#56099=CARTESIAN_POINT('Ctrl Pts',(6.47967040637978,1.95154932685327,32.3959253316847));
#56100=CARTESIAN_POINT('Ctrl Pts',(6.46542223746913,1.99824585363452,32.3982287369138));
#56101=CARTESIAN_POINT('Ctrl Pts',(6.45067407628573,2.04477210503648,32.400532142143));
#56102=CARTESIAN_POINT('Ctrl Pts',(6.39741524044961,2.21278857533894,32.4088502422396));
#56103=CARTESIAN_POINT('Ctrl Pts',(6.33753650125075,2.37888527235834,32.4171683423362));
#56104=CARTESIAN_POINT('Ctrl Pts',(6.27119724463434,2.54251334684612,32.4254864424328));
#56105=CARTESIAN_POINT('Ctrl Pts',(6.20491570892634,2.70599905071382,32.4337973050607));
#56106=CARTESIAN_POINT('Ctrl Pts',(6.1321849867042,2.86702009110896,32.4421081676886));
#56107=CARTESIAN_POINT('Ctrl Pts',(6.05321394639003,3.02504378798543,32.4504190303165));
#56108=CARTESIAN_POINT('Ctrl Pts',(5.97369014889362,3.18417357049868,32.4587880647626));
#56109=CARTESIAN_POINT('Ctrl Pts',(5.88783843755256,3.34026354500124,32.4671570992088));
#56110=CARTESIAN_POINT('Ctrl Pts',(5.79592159995018,3.49278997468084,32.475526133655));
#56111=CARTESIAN_POINT('Ctrl Pts',(5.70475335629834,3.64407419057747,32.48382700857));
#56112=CARTESIAN_POINT('Ctrl Pts',(5.60761859757572,3.791852389679,32.492127883485));
#56113=CARTESIAN_POINT('Ctrl Pts',(5.50481991256358,3.93563803343798,32.5004287584001));
#56114=CARTESIAN_POINT('Ctrl Pts',(5.40204866565804,4.0793852992175,32.5087274177197));
#56115=CARTESIAN_POINT('Ctrl Pts',(5.29361670686519,4.21914185041018,32.5170260770393));
#56116=CARTESIAN_POINT('Ctrl Pts',(5.17986971979655,4.35445044591563,32.525324736359));
#56117=CARTESIAN_POINT('Ctrl Pts',(5.0661342121998,4.48974538592779,32.5336225581687));
#56118=CARTESIAN_POINT('Ctrl Pts',(4.94708496951385,4.62059299913685,32.5419203799785));
#56119=CARTESIAN_POINT('Ctrl Pts',(4.82310781680742,4.74656928606875,32.5502182017882));
#56120=CARTESIAN_POINT('Ctrl Pts',(4.69728322650426,4.87442280056793,32.558639673058));
#56121=CARTESIAN_POINT('Ctrl Pts',(4.56638293228499,4.9972583754097,32.5670611443277));
#56122=CARTESIAN_POINT('Ctrl Pts',(4.43084893714561,5.11467170952307,32.5754826155974));
#56123=CARTESIAN_POINT('Ctrl Pts',(4.29722719054381,5.23042845942507,32.5837852683663));
#56124=CARTESIAN_POINT('Ctrl Pts',(4.15910193248385,5.34091477065818,32.5920879211352));
#56125=CARTESIAN_POINT('Ctrl Pts',(4.01692982274302,5.44578403897527,32.600390573904));
#56126=CARTESIAN_POINT('Ctrl Pts',(3.87170579500402,5.55290446898655,32.6088714544242));
#56127=CARTESIAN_POINT('Ctrl Pts',(3.72225951820408,5.65416374958702,32.6173523349444));
#56128=CARTESIAN_POINT('Ctrl Pts',(3.56910845987579,5.74923941070844,32.6258332154645));
#56129=CARTESIAN_POINT('Ctrl Pts',(3.4159574015475,5.84431507182986,32.6343140959847));
#56130=CARTESIAN_POINT('Ctrl Pts',(3.25910190906719,5.93320694589108,32.6427949765049));
#56131=CARTESIAN_POINT('Ctrl Pts',(3.09908550384733,6.01564277861006,32.651275857025));
#56132=CARTESIAN_POINT('Origin',(0.,0.,-63.6971797838103));
#56133=CARTESIAN_POINT('',(3.09908550384718,6.01564277861013,35.0459194627137));
#56134=CARTESIAN_POINT('',(3.09908550384707,6.01564277861019,34.6514623413619));
#56135=CARTESIAN_POINT('',(3.09908550384721,6.01564277861012,-63.6971797838103));
#56136=CARTESIAN_POINT('',(-6.76699913328736,0.0034249216301115,33.6971797837708));
#56137=CARTESIAN_POINT('Ctrl Pts',(-6.76699913328778,0.00342492080084751,
33.6971797838099));
#56138=CARTESIAN_POINT('Ctrl Pts',(-6.76708965214103,-0.175423302883435,
33.7056048624315));
#56139=CARTESIAN_POINT('Ctrl Pts',(-6.76008560640622,-0.354407685060025,
33.7140299410532));
#56140=CARTESIAN_POINT('Ctrl Pts',(-6.74598121021841,-0.532941377057729,
33.7224550196748));
#56141=CARTESIAN_POINT('Ctrl Pts',(-6.73188987970641,-0.711309683504007,
33.730872293684));
#56142=CARTESIAN_POINT('Ctrl Pts',(-6.71071134395962,-0.889227800981069,
33.7392895676932));
#56143=CARTESIAN_POINT('Ctrl Pts',(-6.68249185780763,-1.06611048692654,
33.7477068417025));
#56144=CARTESIAN_POINT('Ctrl Pts',(-6.65428790377499,-1.24289581592602,
33.75611948281));
#56145=CARTESIAN_POINT('Ctrl Pts',(-6.61905077549059,-1.41864652062158,
33.7645321239175));
#56146=CARTESIAN_POINT('Ctrl Pts',(-6.57687846791906,-1.5927832929255,33.7729447650251));
#56147=CARTESIAN_POINT('Ctrl Pts',(-6.53472619505594,-1.7668373384436,33.7813534095571));
#56148=CARTESIAN_POINT('Ctrl Pts',(-6.48564539169211,-1.93927865689273,
33.7897620540891));
#56149=CARTESIAN_POINT('Ctrl Pts',(-6.4297850314648,-2.10953868159635,33.7981706986212));
#56150=CARTESIAN_POINT('Ctrl Pts',(-6.41693674348431,-2.14869972209187,
33.8001047478474));
#56151=CARTESIAN_POINT('Ctrl Pts',(-6.40373000543813,-2.18774541800157,
33.8020387970736));
#56152=CARTESIAN_POINT('Ctrl Pts',(-6.39016700662022,-2.2266689532803,33.8039728462998));
#56153=CARTESIAN_POINT('Ctrl Pts',(-6.33107907016831,-2.39624143573127,
33.8123986361496));
#56154=CARTESIAN_POINT('Ctrl Pts',(-6.26524208101887,-2.56344664873282,
33.8208244259994));
#56155=CARTESIAN_POINT('Ctrl Pts',(-6.19287793451735,-2.72773750353075,
33.8292502158492));
#56156=CARTESIAN_POINT('Ctrl Pts',(-6.12049699709923,-2.89206647933437,
33.8376779607657));
#56157=CARTESIAN_POINT('Ctrl Pts',(-6.04158601622402,-3.0534794452517,33.8461057056822));
#56158=CARTESIAN_POINT('Ctrl Pts',(-5.95641420385625,-3.21145120344363,
33.8545334505988));
#56159=CARTESIAN_POINT('Ctrl Pts',(-5.8712110951206,-3.36948100833108,33.8629642922887));
#56160=CARTESIAN_POINT('Ctrl Pts',(-5.77974272506954,-3.52406679259694,
33.8713951339787));
#56161=CARTESIAN_POINT('Ctrl Pts',(-5.6823234274213,-3.67470943969439,33.8798259756686));
#56162=CARTESIAN_POINT('Ctrl Pts',(-5.58481461387319,-3.82549050815637,
33.888264564226));
#56163=CARTESIAN_POINT('Ctrl Pts',(-5.48134412803832,-3.97232092199644,
33.8967031527833));
#56164=CARTESIAN_POINT('Ctrl Pts',(-5.37226930641004,-4.11473103609514,
33.9051417413406));
#56165=CARTESIAN_POINT('Ctrl Pts',(-5.26313729076524,-4.25721582376466,
33.9135847547209));
#56166=CARTESIAN_POINT('Ctrl Pts',(-5.14839528601612,-4.3952754309605,33.9220277681012));
#56167=CARTESIAN_POINT('Ctrl Pts',(-5.02844017602248,-4.52847417969485,
33.9304707814815));
#56168=CARTESIAN_POINT('Ctrl Pts',(-4.90835904482523,-4.66181286299838,
33.9389226648358));
#56169=CARTESIAN_POINT('Ctrl Pts',(-4.78305409559201,-4.79028024606345,
33.9473745481901));
#56170=CARTESIAN_POINT('Ctrl Pts',(-4.65295898004466,-4.91347755973524,
33.9558264315445));
#56171=CARTESIAN_POINT('Ctrl Pts',(-4.61750395104761,-4.94705271980343,
33.9581298367734));
#56172=CARTESIAN_POINT('Ctrl Pts',(-4.58169333105088,-4.98023668318396,
33.9604332420023));
#56173=CARTESIAN_POINT('Ctrl Pts',(-4.54553631636656,-5.01302190266437,
33.9627366472312));
#56174=CARTESIAN_POINT('Ctrl Pts',(-4.41497853130123,-5.13140461970047,
33.9710539125646));
#56175=CARTESIAN_POINT('Ctrl Pts',(-4.27966702246925,-5.24479818046762,
33.979371177898));
#56176=CARTESIAN_POINT('Ctrl Pts',(-4.14001558193193,-5.3528086068307,33.9876884432314));
#56177=CARTESIAN_POINT('Ctrl Pts',(-4.00048192663891,-5.46072793471025,
33.9959986935915));
#56178=CARTESIAN_POINT('Ctrl Pts',(-3.85661590630194,-5.56327296237675,
34.0043089439516));
#56179=CARTESIAN_POINT('Ctrl Pts',(-3.70886596052665,-5.66008854054835,
34.0126191943117));
#56180=CARTESIAN_POINT('Ctrl Pts',(-3.56121357176315,-5.75684019288599,
34.0209239575415));
#56181=CARTESIAN_POINT('Ctrl Pts',(-3.40968265759789,-5.84786974395474,
34.0292287207714));
#56182=CARTESIAN_POINT('Ctrl Pts',(-3.2547525207898,-5.93286398195783,34.0375334840013));
#56183=CARTESIAN_POINT('Ctrl Pts',(-3.09989632101333,-6.01781765831298,
34.0458342839639));
#56184=CARTESIAN_POINT('Ctrl Pts',(-2.94164443581863,-6.09674159465641,
34.0541350839265));
#56185=CARTESIAN_POINT('Ctrl Pts',(-2.78050296652484,-6.16936724900914,
34.0624358838891));
#56186=CARTESIAN_POINT('Ctrl Pts',(-2.61940891053195,-6.24197153442426,
34.070734241474));
#56187=CARTESIAN_POINT('Ctrl Pts',(-2.455427281904,-6.3082810890148,34.0790325990589));
#56188=CARTESIAN_POINT('Ctrl Pts',(-2.2890866732251,-6.36807437161841,34.0873309566438));
#56189=CARTESIAN_POINT('Ctrl Pts',(-2.12272913977065,-6.42787373805144,
34.0956301585676));
#56190=CARTESIAN_POINT('Ctrl Pts',(-1.95401247144154,-6.48115538299653,
34.1039293604914));
#56191=CARTESIAN_POINT('Ctrl Pts',(-1.7834835928178,-6.52774656938746,34.1122285624152));
#56192=CARTESIAN_POINT('Ctrl Pts',(-1.61293742579809,-6.57434247924156,
34.1205286057207));
#56193=CARTESIAN_POINT('Ctrl Pts',(-1.44057901785703,-6.61424648633407,
34.1288286490263));
#56194=CARTESIAN_POINT('Ctrl Pts',(-1.26696866307933,-6.64733626400643,
34.1371286923318));
#56195=CARTESIAN_POINT('Ctrl Pts',(-1.09331188780462,-6.68043488933036,
34.1454309549297));
#56196=CARTESIAN_POINT('Ctrl Pts',(-0.918402840289488,-6.70671558864302,
34.1537332175277));
#56197=CARTESIAN_POINT('Ctrl Pts',(-0.742810361132624,-6.72610747515932,
34.1620354801256));
#56198=CARTESIAN_POINT('Ctrl Pts',(-0.567141779263084,-6.74550776622218,
34.1703413409682));
#56199=CARTESIAN_POINT('Ctrl Pts',(-0.390789520997402,-6.75801325588428,
34.1786472018108));
#56200=CARTESIAN_POINT('Ctrl Pts',(-0.214326073743895,-6.76360505456325,
34.1869530626534));
#56201=CARTESIAN_POINT('Ctrl Pts',(-0.0376540342455185,-6.76920346314278,
34.1952687416095));
#56202=CARTESIAN_POINT('Ctrl Pts',(0.139129108747934,-6.7678718413669,34.2035844205656));
#56203=CARTESIAN_POINT('Ctrl Pts',(0.315451153998915,-6.75964344987521,
34.2119000995217));
#56204=CARTESIAN_POINT('Ctrl Pts',(0.491884721539005,-6.75140985399143,
34.2202210380786));
#56205=CARTESIAN_POINT('Ctrl Pts',(0.667856263612172,-6.73627081892348,
34.2285419766354));
#56206=CARTESIAN_POINT('Ctrl Pts',(0.842800017963015,-6.71431136675397,
34.2368629151922));
#56207=CARTESIAN_POINT('Ctrl Pts',(1.01800379292136,-6.69231927603664,34.2451962212412));
#56208=CARTESIAN_POINT('Ctrl Pts',(1.19217638426054,-6.6634865661243,34.2535295272901));
#56209=CARTESIAN_POINT('Ctrl Pts',(1.36476218204342,-6.6279493952854,34.261862833339));
#56210=CARTESIAN_POINT('Ctrl Pts',(1.49179551870497,-6.60179193942767,34.2679966385907));
#56211=CARTESIAN_POINT('Ctrl Pts',(1.61796939998943,-6.57200318582296,34.2741304438425));
#56212=CARTESIAN_POINT('Ctrl Pts',(1.74306822618047,-6.5386544608872,34.2802642490942));
#56213=CARTESIAN_POINT('Ctrl Pts',(1.90768452566187,-6.49477120587597,34.2883356623363));
#56214=CARTESIAN_POINT('Ctrl Pts',(2.07094537377384,-6.44458654756956,34.2964070755783));
#56215=CARTESIAN_POINT('Ctrl Pts',(2.23231929035817,-6.3881953309127,34.3044784888204));
#56216=CARTESIAN_POINT('Ctrl Pts',(2.39349061535627,-6.33187490875766,34.3125397690716));
#56217=CARTESIAN_POINT('Ctrl Pts',(2.55277937468498,-6.26936355344841,34.3206010493228));
#56218=CARTESIAN_POINT('Ctrl Pts',(2.70966438187405,-6.200807039217,34.328662329574));
#56219=CARTESIAN_POINT('Ctrl Pts',(2.86638683853874,-6.13232155725017,34.3367152574316));
#56220=CARTESIAN_POINT('Ctrl Pts',(3.0207101604859,-6.05780352891701,34.3447681852893));
#56221=CARTESIAN_POINT('Ctrl Pts',(3.17212853550339,-5.97744841502168,34.3528211131469));
#56222=CARTESIAN_POINT('Ctrl Pts',(3.32342318119117,-5.89715896214258,34.3608674606713));
#56223=CARTESIAN_POINT('Ctrl Pts',(3.47181727672117,-5.81104209095456,34.3689138081957));
#56224=CARTESIAN_POINT('Ctrl Pts',(3.61682531321139,-5.71934119053177,34.3769601557201));
#56225=CARTESIAN_POINT('Ctrl Pts',(3.76174657875115,-5.62769516275246,34.3850016884132));
#56226=CARTESIAN_POINT('Ctrl Pts',(3.90328550435128,-5.53047195636487,34.3930432211064));
#56227=CARTESIAN_POINT('Ctrl Pts',(4.04098160901787,-5.42796063320096,34.4010847537995));
#56228=CARTESIAN_POINT('Ctrl Pts',(4.18132488515081,-5.32347855675891,34.4092808828478));
#56229=CARTESIAN_POINT('Ctrl Pts',(4.31767573316271,-5.21350315579193,34.417477011896));
#56230=CARTESIAN_POINT('Ctrl Pts',(4.44957764152242,-5.0983867852551,34.4256731409443));
#56231=CARTESIAN_POINT('Ctrl Pts',(4.57894692808211,-4.98548074080972,34.4337118977804));
#56232=CARTESIAN_POINT('Ctrl Pts',(4.70403629602601,-4.86762963010654,34.4417506546165));
#56233=CARTESIAN_POINT('Ctrl Pts',(4.82444889387516,-4.74520619893243,34.4497894114526));
#56234=CARTESIAN_POINT('Ctrl Pts',(4.94487314639105,-4.62277091846417,34.4578289463554));
#56235=CARTESIAN_POINT('Ctrl Pts',(5.06061946550275,-4.49576270252504,34.4658684812581));
#56236=CARTESIAN_POINT('Ctrl Pts',(5.17132854583285,-4.36459048148327,34.4739080161609));
#56237=CARTESIAN_POINT('Ctrl Pts',(5.28207026206822,-4.2333795922115,34.4819499210365));
#56238=CARTESIAN_POINT('Ctrl Pts',(5.38777154306417,-4.09800253976918,34.489991825912));
#56239=CARTESIAN_POINT('Ctrl Pts',(5.48811408449555,-3.95890045284818,34.4980337307875));
#56240=CARTESIAN_POINT('Ctrl Pts',(5.59184140885884,-3.81510613506593,34.5063469074683));
#56241=CARTESIAN_POINT('Ctrl Pts',(5.68984188934675,-3.66733143312462,34.5146600841492));
#56242=CARTESIAN_POINT('Ctrl Pts',(5.78181383338206,-3.51609411081556,34.52297326083));
#56243=CARTESIAN_POINT('Ctrl Pts',(5.8709390659472,-3.36953787929622,34.5310291284405));
#56244=CARTESIAN_POINT('Ctrl Pts',(5.9544032765479,-3.21973054106396,34.5390849960511));
#56245=CARTESIAN_POINT('Ctrl Pts',(6.0319800003596,-3.06716583758716,34.5471408636616));
#56246=CARTESIAN_POINT('Ctrl Pts',(6.11327349230423,-2.90729162682223,34.5555826948775));
#56247=CARTESIAN_POINT('Ctrl Pts',(6.18810126641518,-2.74438977672137,34.5640245260935));
#56248=CARTESIAN_POINT('Ctrl Pts',(6.25626078166885,-2.57904828022903,34.5724663573094));
#56249=CARTESIAN_POINT('Ctrl Pts',(6.32442029692256,-2.41370678373658,34.5809081885254));
#56250=CARTESIAN_POINT('Ctrl Pts',(6.38591147500212,-2.2459261032453,34.5893500197414));
#56251=CARTESIAN_POINT('Ctrl Pts',(6.44059276114633,-2.07630775297631,34.5977918509573));
#56252=CARTESIAN_POINT('Ctrl Pts',(6.49390488167561,-1.91093647934403,34.6060223070239));
#56253=CARTESIAN_POINT('Ctrl Pts',(6.54092172979095,-1.74326855251469,34.6142527630904));
#56254=CARTESIAN_POINT('Ctrl Pts',(6.58144113511989,-1.57382387354869,34.622483219157));
#56255=CARTESIAN_POINT('Ctrl Pts',(6.6219124415271,-1.40458033540115,34.6307039051872));
#56256=CARTESIAN_POINT('Ctrl Pts',(6.65590158058441,-1.23356459009026,34.6389245912175));
#56257=CARTESIAN_POINT('Ctrl Pts',(6.68325529423569,-1.06131412506884,34.6471452772477));
#56258=CARTESIAN_POINT('Ctrl Pts',(6.71058202541813,-0.889233572727791,
34.6553578541631));
#56259=CARTESIAN_POINT('Ctrl Pts',(6.7312863103825,-0.715921077884259,34.6635704310785));
#56260=CARTESIAN_POINT('Ctrl Pts',(6.74526531879975,-0.541926912966403,
34.671783007994));
#56261=CARTESIAN_POINT('Ctrl Pts',(6.75923334154567,-0.368069484693473,
34.6799891308986));
#56262=CARTESIAN_POINT('Ctrl Pts',(6.76648658607982,-0.19353180911163,34.6881952538032));
#56263=CARTESIAN_POINT('Ctrl Pts',(6.76697368452304,-0.0188720155952667,
34.6964013767079));
#56264=CARTESIAN_POINT('Ctrl Pts',(6.76746049783745,0.155685538749563,34.7046026960616));
#56265=CARTESIAN_POINT('Ctrl Pts',(6.76118905412521,0.330364711065663,34.7128040154154));
#56266=CARTESIAN_POINT('Ctrl Pts',(6.74815999195772,0.504604521324516,34.7210053347691));
#56267=CARTESIAN_POINT('Ctrl Pts',(6.73513466751953,0.678794346309399,34.7292043013586));
#56268=CARTESIAN_POINT('Ctrl Pts',(6.71535560884039,0.852544702931206,34.7374032679482));
#56269=CARTESIAN_POINT('Ctrl Pts',(6.68887552707403,1.02529663186323,34.7456022345377));
#56270=CARTESIAN_POINT('Ctrl Pts',(6.6623989421221,1.19802574812267,34.7538001184166));
#56271=CARTESIAN_POINT('Ctrl Pts',(6.62922314998981,1.36975634479695,34.7619980022955));
#56272=CARTESIAN_POINT('Ctrl Pts',(6.58945250612212,1.53993657972039,34.7701958861745));
#56273=CARTESIAN_POINT('Ctrl Pts',(6.5496798896958,1.71012525530406,34.778394176655));
#56274=CARTESIAN_POINT('Ctrl Pts',(6.50331185145674,1.87876306670202,34.7865924671355));
#56275=CARTESIAN_POINT('Ctrl Pts',(6.45050346000626,2.04531027290415,34.794790757616));
#56276=CARTESIAN_POINT('Ctrl Pts',(6.39768285657577,2.21189599327224,34.8029909439574));
#56277=CARTESIAN_POINT('Ctrl Pts',(6.33841904198215,2.37638980377696,34.8111911302987));
#56278=CARTESIAN_POINT('Ctrl Pts',(6.27291637400521,2.53826893073554,34.81939131664));
#56279=CARTESIAN_POINT('Ctrl Pts',(6.2073517783952,2.70030110170723,34.8275992556141));
#56280=CARTESIAN_POINT('Ctrl Pts',(6.13553667985029,2.85971331753786,34.8358071945882));
#56281=CARTESIAN_POINT('Ctrl Pts',(6.05772323735311,3.01600367699247,34.8440151335623));
#56282=CARTESIAN_POINT('Ctrl Pts',(5.97987204519757,3.17236985763538,34.8522270544562));
#56283=CARTESIAN_POINT('Ctrl Pts',(5.89601687931091,3.32561084793011,34.8604389753502));
#56284=CARTESIAN_POINT('Ctrl Pts',(5.80645491842284,3.47525111039811,34.8686508962442));
#56285=CARTESIAN_POINT('Ctrl Pts',(5.71677013749364,3.62509658078034,34.8768740784867));
#56286=CARTESIAN_POINT('Ctrl Pts',(5.62136311756674,3.77133115481839,34.8850972607293));
#56287=CARTESIAN_POINT('Ctrl Pts',(5.52057395244849,3.91350894154431,34.8933204429718));
#56288=CARTESIAN_POINT('Ctrl Pts',(5.43069545323876,4.04029564601689,34.9006534462547));
#56289=CARTESIAN_POINT('Ctrl Pts',(5.33653768861316,4.16385664902198,34.9079864495375));
#56290=CARTESIAN_POINT('Ctrl Pts',(5.23836745235498,4.28389955929269,34.9153194528204));
#56291=CARTESIAN_POINT('Ctrl Pts',(5.11872529153638,4.43019841445657,34.9242563403282));
#56292=CARTESIAN_POINT('Ctrl Pts',(4.9928749510221,4.57157535941286,34.9331932278359));
#56293=CARTESIAN_POINT('Ctrl Pts',(4.86122711320063,4.70752163605044,34.9421301153437));
#56294=CARTESIAN_POINT('Ctrl Pts',(4.72987446156941,4.8431630883617,34.9510469641952));
#56295=CARTESIAN_POINT('Ctrl Pts',(4.59275043899065,4.97339799229441,34.9599638130466));
#56296=CARTESIAN_POINT('Ctrl Pts',(4.45030382908657,5.09775291955362,34.9688806618981));
#56297=CARTESIAN_POINT('Ctrl Pts',(4.30806194981394,5.22192911835591,34.977784695056));
#56298=CARTESIAN_POINT('Ctrl Pts',(4.16051293739821,5.34024202984869,34.9866887282139));
#56299=CARTESIAN_POINT('Ctrl Pts',(4.00814202564201,5.45225517582242,34.9955927613719));
#56300=CARTESIAN_POINT('Ctrl Pts',(3.85613176909673,5.56400319163239,35.004475719077));
#56301=CARTESIAN_POINT('Ctrl Pts',(3.69932259696003,5.6694810461941,35.0133586767822));
#56302=CARTESIAN_POINT('Ctrl Pts',(3.53823190768989,5.76829298557252,35.0222416344873));
#56303=CARTESIAN_POINT('Ctrl Pts',(3.39510098981263,5.85608852263642,35.0301342438961));
#56304=CARTESIAN_POINT('Ctrl Pts',(3.24859059684888,5.93862207051218,35.0380268533049));
#56305=CARTESIAN_POINT('Ctrl Pts',(3.0990855038472,6.01564277861013,35.0459194627137));
#56306=CARTESIAN_POINT('Ctrl Pts',(3.09908550384727,6.01564277861009,33.045773705108));
#56307=CARTESIAN_POINT('Ctrl Pts',(2.94004160920022,6.09757760195576,33.0542117246657));
#56308=CARTESIAN_POINT('Ctrl Pts',(2.77763778918707,6.17325722407048,33.0626497442234));
#56309=CARTESIAN_POINT('Ctrl Pts',(2.61239456112603,6.24241008401396,33.071087763781));
#56310=CARTESIAN_POINT('Ctrl Pts',(2.44726656488396,6.3115147204391,33.0795198991136));
#56311=CARTESIAN_POINT('Ctrl Pts',(2.27930341468169,6.37410154006354,33.0879520344462));
#56312=CARTESIAN_POINT('Ctrl Pts',(2.10904802773521,6.42994598863056,33.0963841697788));
#56313=CARTESIAN_POINT('Ctrl Pts',(1.93888523470524,6.48576006602225,33.1048117192687));
#56314=CARTESIAN_POINT('Ctrl Pts',(1.76643300670117,6.53483897979737,33.1132392687585));
#56315=CARTESIAN_POINT('Ctrl Pts',(1.59225231329541,6.57700703746054,33.1216668182484));
#56316=CARTESIAN_POINT('Ctrl Pts',(1.4148392827628,6.61995762374779,33.1302507609674));
#56317=CARTESIAN_POINT('Ctrl Pts',(1.23563333481011,6.65573821405969,33.1388347036864));
#56318=CARTESIAN_POINT('Ctrl Pts',(1.05524239882421,6.68421666911866,33.1474186464055));
#56319=CARTESIAN_POINT('Ctrl Pts',(0.878232759112823,6.71216131634816,33.155841689391));
#56320=CARTESIAN_POINT('Ctrl Pts',(0.700082505122222,6.73307510953281,33.1642647323764));
#56321=CARTESIAN_POINT('Ctrl Pts',(0.52137539127125,6.74688496280889,33.1726877753619));
#56322=CARTESIAN_POINT('Ctrl Pts',(0.342677693318895,6.76069408845766,33.1811103745457));
#56323=CARTESIAN_POINT('Ctrl Pts',(0.163423526398336,6.767399994887,33.1895329737295));
#56324=CARTESIAN_POINT('Ctrl Pts',(-0.0157991414938836,6.76698155658253,
33.1979555729133));
#56325=CARTESIAN_POINT('Ctrl Pts',(-0.195037358157048,6.76656308197572,
33.2063789028141));
#56326=CARTESIAN_POINT('Ctrl Pts',(-0.374243736950611,6.75901903164635,
33.214802232715));
#56327=CARTESIAN_POINT('Ctrl Pts',(-0.55283084576014,6.74438040563966,33.2232255626159));
#56328=CARTESIAN_POINT('Ctrl Pts',(-0.737382501555146,6.72925287103703,
33.2319302193566));
#56329=CARTESIAN_POINT('Ctrl Pts',(-0.921272425447512,6.70654868286527,
33.2406348760974));
#56330=CARTESIAN_POINT('Ctrl Pts',(-1.10385876102418,6.67636014874199,33.2493395328382));
#56331=CARTESIAN_POINT('Ctrl Pts',(-1.28070950995677,6.64711992738579,33.2577707500974));
#56332=CARTESIAN_POINT('Ctrl Pts',(-1.45633700072461,6.61085854578323,33.2662019673566));
#56333=CARTESIAN_POINT('Ctrl Pts',(-1.63016890437465,6.56771180421385,33.2746331846158));
#56334=CARTESIAN_POINT('Ctrl Pts',(-1.81245732814894,6.52246607344448,33.2834745610973));
#56335=CARTESIAN_POINT('Ctrl Pts',(-1.99277069739514,6.46964844903224,33.2923159375789));
#56336=CARTESIAN_POINT('Ctrl Pts',(-2.17046753907376,6.40947421102754,33.3011573140604));
#56337=CARTESIAN_POINT('Ctrl Pts',(-2.34816438075237,6.34929997302284,33.309998690542));
#56338=CARTESIAN_POINT('Ctrl Pts',(-2.52324431328163,6.28176930052493,33.3188400670235));
#56339=CARTESIAN_POINT('Ctrl Pts',(-2.69509059764972,6.20715519948229,33.3276814435051));
#56340=CARTESIAN_POINT('Ctrl Pts',(-2.85333108305194,6.13844861318482,33.335822810723));
#56341=CARTESIAN_POINT('Ctrl Pts',(-3.00914418974486,6.0635994130988,33.3439641779408));
#56342=CARTESIAN_POINT('Ctrl Pts',(-3.16201576885751,5.98280413163397,33.3521055451587));
#56343=CARTESIAN_POINT('Ctrl Pts',(-3.31475390270805,5.90207937830507,33.3602398055821));
#56344=CARTESIAN_POINT('Ctrl Pts',(-3.4645552986537,5.81541904518829,33.3683740660056));
#56345=CARTESIAN_POINT('Ctrl Pts',(-3.61092578394971,5.72306770734081,33.3765083264291));
#56346=CARTESIAN_POINT('Ctrl Pts',(-3.75719642058769,5.6307793682402,33.3846370379539));
#56347=CARTESIAN_POINT('Ctrl Pts',(-3.90004049800891,5.53280794827193,33.3927657494787));
#56348=CARTESIAN_POINT('Ctrl Pts',(-4.03898850387016,5.42944388179901,33.4008944610035));
#56349=CARTESIAN_POINT('Ctrl Pts',(-4.17787024799543,5.32612910773903,33.4090192960961));
#56350=CARTESIAN_POINT('Ctrl Pts',(-4.31285932734706,5.2174270262601,33.4171441311886));
#56351=CARTESIAN_POINT('Ctrl Pts',(-4.44351530932409,5.1036712958225,33.4252689662811));
#56352=CARTESIAN_POINT('Ctrl Pts',(-4.57413471379273,4.98994741162049,33.4333915268032));
#56353=CARTESIAN_POINT('Ctrl Pts',(-4.70042316178427,4.87117293721467,33.4415140873254));
#56354=CARTESIAN_POINT('Ctrl Pts',(-4.82197344176443,4.74772167749106,33.4496366478476));
#56355=CARTESIAN_POINT('Ctrl Pts',(-4.94353018182662,4.62426385665328,33.4577596400628));
#56356=CARTESIAN_POINT('Ctrl Pts',(-5.06034799119233,4.49612901204469,33.465882632278));
#56357=CARTESIAN_POINT('Ctrl Pts',(-5.17205653826282,4.3637277831016,33.4740056244932));
#56358=CARTESIAN_POINT('Ctrl Pts',(-5.22908034727287,4.29614099059608,33.4781521644744));
#56359=CARTESIAN_POINT('Ctrl Pts',(-5.28477340689579,4.22744303401794,33.4822987044556));
#56360=CARTESIAN_POINT('Ctrl Pts',(-5.33909048514278,4.1576918826986,33.4864452444368));
#56361=CARTESIAN_POINT('Ctrl Pts',(-5.45677079513745,4.00657298281193,33.4954289034652));
#56362=CARTESIAN_POINT('Ctrl Pts',(-5.56793181226996,3.85058350284633,33.5044125624936));
#56363=CARTESIAN_POINT('Ctrl Pts',(-5.67221657546274,3.69029106183317,33.5133962215221));
#56364=CARTESIAN_POINT('Ctrl Pts',(-5.77668049877385,3.52972324010454,33.5223953143816));
#56365=CARTESIAN_POINT('Ctrl Pts',(-5.87424442618288,3.36483788239926,33.531394407241));
#56366=CARTESIAN_POINT('Ctrl Pts',(-5.96459647945295,3.19622868976822,33.5403935001005));
#56367=CARTESIAN_POINT('Ctrl Pts',(-6.05516038303925,3.02722415569794,33.549413693318));
#56368=CARTESIAN_POINT('Ctrl Pts',(-6.13847846550649,2.85447852845012,33.5584338865355));
#56369=CARTESIAN_POINT('Ctrl Pts',(-6.21428513635634,2.67860957290544,33.5674540797529));
#56370=CARTESIAN_POINT('Ctrl Pts',(-6.29016858044267,2.50256250600508,33.5764834081747));
#56371=CARTESIAN_POINT('Ctrl Pts',(-6.35852532659879,2.3233860134179,33.5855127365965));
#56372=CARTESIAN_POINT('Ctrl Pts',(-6.41913862994282,2.14171619258383,33.5945420650183));
#56373=CARTESIAN_POINT('Ctrl Pts',(-6.47983738582691,1.95979025392109,33.6035841229731));
#56374=CARTESIAN_POINT('Ctrl Pts',(-6.53277079511993,1.77536418551779,33.6126261809279));
#56375=CARTESIAN_POINT('Ctrl Pts',(-6.57777186379046,1.58908977340066,33.6216682388828));
#56376=CARTESIAN_POINT('Ctrl Pts',(-6.61682497369461,1.42743594375495,33.6295151743779));
#56377=CARTESIAN_POINT('Ctrl Pts',(-6.64990483474276,1.26439037905654,33.6373621098731));
#56378=CARTESIAN_POINT('Ctrl Pts',(-6.67693357879417,1.10038492554693,33.6452090453682));
#56379=CARTESIAN_POINT('Ctrl Pts',(-6.70999996181544,0.899744187930262,
33.6548088171568));
#56380=CARTESIAN_POINT('Ctrl Pts',(-6.73402868125974,0.697549037419545,
33.6644085889453));
#56381=CARTESIAN_POINT('Ctrl Pts',(-6.74890395273286,0.494554786436053,
33.6740083607339));
#56382=CARTESIAN_POINT('Ctrl Pts',(-6.7608723347487,0.33122917942572,33.6817321684129));
#56383=CARTESIAN_POINT('Ctrl Pts',(-6.76691614885309,0.167386511247601,
33.6894559760919));
#56384=CARTESIAN_POINT('Ctrl Pts',(-6.76699913328736,0.003424921630116,
33.6971797837708));
#56385=CARTESIAN_POINT('',(-6.76699785065912,-0.00539343812502433,33.3028202162135));
#56386=CARTESIAN_POINT('Ctrl Pts',(3.09908550384733,6.01564277861006,32.651275857025));
#56387=CARTESIAN_POINT('Ctrl Pts',(2.94207978962374,6.09652759023844,32.6595971707146));
#56388=CARTESIAN_POINT('Ctrl Pts',(2.78203138935587,6.1711970514421,32.6679184844042));
#56389=CARTESIAN_POINT('Ctrl Pts',(2.61947314133681,6.23944304099453,32.6762397980938));
#56390=CARTESIAN_POINT('Ctrl Pts',(2.45667623468372,6.30778922536847,32.6845733286557));
#56391=CARTESIAN_POINT('Ctrl Pts',(2.2913624423339,6.36969297089404,32.6929068592175));
#56392=CARTESIAN_POINT('Ctrl Pts',(2.12408121548847,6.4249955634233,32.7012403897794));
#56393=CARTESIAN_POINT('Ctrl Pts',(2.0115413906263,6.46220083860589,32.7068468411883));
#56394=CARTESIAN_POINT('Ctrl Pts',(1.89811138804103,6.49641945309301,32.7124532925971));
#56395=CARTESIAN_POINT('Ctrl Pts',(1.78396096288937,6.52761612557654,32.7180597440059));
#56396=CARTESIAN_POINT('Ctrl Pts',(1.61962256307724,6.57252889071599,32.7261311572479));
#56397=CARTESIAN_POINT('Ctrl Pts',(1.45328462129516,6.61131411443873,32.73420257049));
#56398=CARTESIAN_POINT('Ctrl Pts',(1.28545415222779,6.64378631674141,32.742273983732));
#56399=CARTESIAN_POINT('Ctrl Pts',(1.11783438041326,6.6762177528837,32.7503352639832));
#56400=CARTESIAN_POINT('Ctrl Pts',(0.9487261711101,6.70235186732054,32.7583965442345));
#56401=CARTESIAN_POINT('Ctrl Pts',(0.778653271254402,6.72205237134945,32.7664578244857));
#56402=CARTESIAN_POINT('Ctrl Pts',(0.608756586064406,6.74173246343894,32.7745107523433));
#56403=CARTESIAN_POINT('Ctrl Pts',(0.437897566757396,6.75499216799324,32.7825636802009));
#56404=CARTESIAN_POINT('Ctrl Pts',(0.266611676714297,6.76174587024975,32.7906166080585));
#56405=CARTESIAN_POINT('Ctrl Pts',(0.0954657504538968,6.76849405381635,
32.7986629555829));
#56406=CARTESIAN_POINT('Ctrl Pts',(-0.0761059815110598,6.7687468016881,
32.8067093031072));
#56407=CARTESIAN_POINT('Ctrl Pts',(-0.247561483685967,6.76247013389303,
32.8147556506315));
#56408=CARTESIAN_POINT('Ctrl Pts',(-0.418914389086828,6.75619722197549,
32.8227971833247));
#56409=CARTESIAN_POINT('Ctrl Pts',(-0.590150831376489,6.74340268594741,
32.8308387160178));
#56410=CARTESIAN_POINT('Ctrl Pts',(-0.760727420740435,6.72410460889282,
32.8388802487109));
#56411=CARTESIAN_POINT('Ctrl Pts',(-0.934583300258403,6.70443553137261,
32.8470763777592));
#56412=CARTESIAN_POINT('Ctrl Pts',(-1.1077533020177,6.67801029604354,32.8552725068074));
#56413=CARTESIAN_POINT('Ctrl Pts',(-1.27966561724474,6.64490367936524,32.8634686358557));
#56414=CARTESIAN_POINT('Ctrl Pts',(-1.44827707896115,6.61243273612164,32.8715073926918));
#56415=CARTESIAN_POINT('Ctrl Pts',(-1.61567833783162,6.57353475680192,32.8795461495279));
#56416=CARTESIAN_POINT('Ctrl Pts',(-1.78133888071629,6.52833216005807,32.887584906364));
#56417=CARTESIAN_POINT('Ctrl Pts',(-1.9470154577899,6.4831251881808,32.8956244412668));
#56418=CARTESIAN_POINT('Ctrl Pts',(-2.11095062305154,6.4316124820358,32.9036639761696));
#56419=CARTESIAN_POINT('Ctrl Pts',(-2.27262810136108,6.37396662314009,32.9117035110723));
#56420=CARTESIAN_POINT('Ctrl Pts',(-2.43435324053951,6.31630377083411,32.9197454159479));
#56421=CARTESIAN_POINT('Ctrl Pts',(-2.59381901643189,6.25250429237782,32.9277873208234));
#56422=CARTESIAN_POINT('Ctrl Pts',(-2.75052838345207,6.18278922589348,32.9358292256989));
#56423=CARTESIAN_POINT('Ctrl Pts',(-2.91252391507618,6.11072251110747,32.9441424023798));
#56424=CARTESIAN_POINT('Ctrl Pts',(-3.07157342616548,6.03233431217328,32.9524555790606));
#56425=CARTESIAN_POINT('Ctrl Pts',(-3.22715566352832,5.9479202519332,32.9607687557414));
#56426=CARTESIAN_POINT('Ctrl Pts',(-3.3779223264858,5.86611897188471,32.968824623352));
#56427=CARTESIAN_POINT('Ctrl Pts',(-3.5254328760615,5.7786595481313,32.9768804909625));
#56428=CARTESIAN_POINT('Ctrl Pts',(-3.66924315661712,5.6858546989541,32.9849363585731));
#56429=CARTESIAN_POINT('Ctrl Pts',(-3.81994351246532,5.58860348894737,32.9933781897891));
#56430=CARTESIAN_POINT('Ctrl Pts',(-3.96657991269236,5.4854823239354,33.001820021005));
#56431=CARTESIAN_POINT('Ctrl Pts',(-4.10868144830041,5.37689740988165,33.010261852221));
#56432=CARTESIAN_POINT('Ctrl Pts',(-4.25078298390857,5.26831249582783,33.018703683437));
#56433=CARTESIAN_POINT('Ctrl Pts',(-4.38834935454169,5.15426419290825,33.027145514653));
#56434=CARTESIAN_POINT('Ctrl Pts',(-4.52095554968078,5.0352010801765,33.035587345869));
#56435=CARTESIAN_POINT('Ctrl Pts',(-4.64913029779636,4.92011683039282,33.0437470671294));
#56436=CARTESIAN_POINT('Ctrl Pts',(-4.77311108384849,4.79995272957011,33.0519067883899));
#56437=CARTESIAN_POINT('Ctrl Pts',(-4.89246522808437,4.67504791333579,33.0600665096504));
#56438=CARTESIAN_POINT('Ctrl Pts',(-5.01167597079469,4.55029316764418,33.0682164271752));
#56439=CARTESIAN_POINT('Ctrl Pts',(-5.1262708878455,4.42080930722444,33.0763663447));
#56440=CARTESIAN_POINT('Ctrl Pts',(-5.23585041703899,4.28697555514289,33.0845162622248));
#56441=CARTESIAN_POINT('Ctrl Pts',(-5.34532132898999,4.15327446153514,33.0926581014017));
#56442=CARTESIAN_POINT('Ctrl Pts',(-5.44978652130772,4.015232342053,33.1007999405785));
#56443=CARTESIAN_POINT('Ctrl Pts',(-5.54888336725751,3.8732650795644,33.1089417797553));
#56444=CARTESIAN_POINT('Ctrl Pts',(-5.64789321709116,3.73142244869587,33.1170764712941));
#56445=CARTESIAN_POINT('Ctrl Pts',(-5.74154390171591,3.585661838549,33.1252111628329));
#56446=CARTESIAN_POINT('Ctrl Pts',(-5.82951327604952,3.43643186522917,33.1333458543717));
#56447=CARTESIAN_POINT('Ctrl Pts',(-5.9174395202893,3.28727505717624,33.1414765575906));
#56448=CARTESIAN_POINT('Ctrl Pts',(-5.99968981356505,3.13465258587875,33.1496072608095));
#56449=CARTESIAN_POINT('Ctrl Pts',(-6.07598537388288,2.97904191584499,33.1577379640283));
#56450=CARTESIAN_POINT('Ctrl Pts',(-6.15225804036006,2.82347793956205,33.165866227485));
#56451=CARTESIAN_POINT('Ctrl Pts',(-6.22257937066534,2.66492787772565,33.1739944909416));
#56452=CARTESIAN_POINT('Ctrl Pts',(-6.28671661044567,2.50389361993405,33.1821227543983));
#56453=CARTESIAN_POINT('Ctrl Pts',(-6.35084680440882,2.34287705261287,33.1902501249219));
#56454=CARTESIAN_POINT('Ctrl Pts',(-6.40879412622396,2.17937717268235,33.1983774954456));
#56455=CARTESIAN_POINT('Ctrl Pts',(-6.46037404997259,2.013915622473,33.2065048659692));
#56456=CARTESIAN_POINT('Ctrl Pts',(-6.51197711765053,1.84837982960984,33.2146358832468));
#56457=CARTESIAN_POINT('Ctrl Pts',(-6.55720696619344,1.68088095613857,33.2227669005244));
#56458=CARTESIAN_POINT('Ctrl Pts',(-6.59592887245198,1.51195612024768,33.230897917802));
#56459=CARTESIAN_POINT('Ctrl Pts',(-6.63465877599399,1.34299639610026,33.2390306143886));
#56460=CARTESIAN_POINT('Ctrl Pts',(-6.66687798578942,1.17261048116098,33.2471633109753));
#56461=CARTESIAN_POINT('Ctrl Pts',(-6.69250301964037,1.00134526118841,33.255296007562));
#56462=CARTESIAN_POINT('Ctrl Pts',(-6.71815280979513,0.829914582163535,
33.2634365611337));
#56463=CARTESIAN_POINT('Ctrl Pts',(-6.7371956485091,0.657603263896057,33.2715771147054));
#56464=CARTESIAN_POINT('Ctrl Pts',(-6.74959992417062,0.484963775591544,
33.2797176682771));
#56465=CARTESIAN_POINT('Ctrl Pts',(-6.76133419466654,0.321649245237541,
33.2874185175813));
#56466=CARTESIAN_POINT('Ctrl Pts',(-6.76712811155804,0.158041329314807,
33.2951193668855));
#56467=CARTESIAN_POINT('Ctrl Pts',(-6.76699785065953,-0.00539343761909804,
33.3028202161897));
#56468=CARTESIAN_POINT('Ctrl Pts',(-6.76699785065912,-0.00539343812484117,
33.3028202162135));
#56469=CARTESIAN_POINT('Ctrl Pts',(-6.7668025852718,-0.250387526453958,
33.3143640424755));
#56470=CARTESIAN_POINT('Ctrl Pts',(-6.75329908010437,-0.494887213932031,
33.3259078687374));
#56471=CARTESIAN_POINT('Ctrl Pts',(-6.72666862041688,-0.737711509398421,
33.3374516949994));
#56472=CARTESIAN_POINT('Ctrl Pts',(-6.71462409806051,-0.847536975790543,
33.3426727792435));
#56473=CARTESIAN_POINT('Ctrl Pts',(-6.69989494559919,-0.95702010800004,
33.3478938634877));
#56474=CARTESIAN_POINT('Ctrl Pts',(-6.68250099372052,-1.06605322049339,
33.3531149477319));
#56475=CARTESIAN_POINT('Ctrl Pts',(-6.65273357345905,-1.25264879719985,
33.3620501345141));
#56476=CARTESIAN_POINT('Ctrl Pts',(-6.61512750839485,-1.4381154136122,33.3709853212964));
#56477=CARTESIAN_POINT('Ctrl Pts',(-6.5697816277517,-1.62180712899415,33.3799205080786));
#56478=CARTESIAN_POINT('Ctrl Pts',(-6.52450366120969,-1.80522373101277,
33.3888423127152));
#56479=CARTESIAN_POINT('Ctrl Pts',(-6.47150907061117,-1.98687048590991,
33.3977641173518));
#56480=CARTESIAN_POINT('Ctrl Pts',(-6.410947704516,-2.16611138447704,33.4066859219884));
#56481=CARTESIAN_POINT('Ctrl Pts',(-6.35053406195511,-2.34491507198488,
33.4155859642277));
#56482=CARTESIAN_POINT('Ctrl Pts',(-6.28259056378408,-2.52132437130597,
33.4244860064669));
#56483=CARTESIAN_POINT('Ctrl Pts',(-6.20731663576343,-2.6947187577509,33.4333860487062));
#56484=CARTESIAN_POINT('Ctrl Pts',(-6.13215859306182,-2.86784620098825,
33.4422723891995));
#56485=CARTESIAN_POINT('Ctrl Pts',(-6.04969273412608,-3.03796775415776,
33.4511587296929));
#56486=CARTESIAN_POINT('Ctrl Pts',(-5.9601673228959,-3.20448037645481,33.4600450701862));
#56487=CARTESIAN_POINT('Ctrl Pts',(-5.87087081251491,-3.37056725504265,
33.4689086898581));
#56488=CARTESIAN_POINT('Ctrl Pts',(-5.77455088954403,-3.53306338862778,
33.47777230953));
#56489=CARTESIAN_POINT('Ctrl Pts',(-5.67150235408961,-3.69138863404492,
33.4866359292019));
#56490=CARTESIAN_POINT('Ctrl Pts',(-5.5736779259755,-3.84168748614078,33.4950502023558));
#56491=CARTESIAN_POINT('Ctrl Pts',(-5.46979023457897,-3.98822757624349,
33.5034644755097));
#56492=CARTESIAN_POINT('Ctrl Pts',(-5.36013090501699,-4.13053092000069,
33.5118787486636));
#56493=CARTESIAN_POINT('Ctrl Pts',(-5.25313053823785,-4.26938376577987,
33.5200889968682));
#56494=CARTESIAN_POINT('Ctrl Pts',(-5.14073706316906,-4.40406876775802,
33.5282992450727));
#56495=CARTESIAN_POINT('Ctrl Pts',(-5.02331705709524,-4.53415645339859,
33.5365094932772));
#56496=CARTESIAN_POINT('Ctrl Pts',(-4.90586913794518,-4.66427506347535,
33.5447216932215));
#56497=CARTESIAN_POINT('Ctrl Pts',(-4.78339254569706,-4.78979391566198,
33.5529338931657));
#56498=CARTESIAN_POINT('Ctrl Pts',(-4.65629173412285,-4.91031936708187,
33.5611460931099));
#56499=CARTESIAN_POINT('Ctrl Pts',(-4.52913807505962,-5.03089493200921,
33.5693617076204));
#56500=CARTESIAN_POINT('Ctrl Pts',(-4.39735662427768,-5.14647271517083,
33.5775773221309));
#56501=CARTESIAN_POINT('Ctrl Pts',(-4.2613860649639,-5.25669837496232,33.5857929366414));
#56502=CARTESIAN_POINT('Ctrl Pts',(-4.12526281667301,-5.36704781333742,
33.5940177769268));
#56503=CARTESIAN_POINT('Ctrl Pts',(-3.98494134067954,-5.47203289979203,
33.6022426172123));
#56504=CARTESIAN_POINT('Ctrl Pts',(-3.84089132867578,-5.57134120309492,
33.6104674574977));
#56505=CARTESIAN_POINT('Ctrl Pts',(-3.69674904763208,-5.67071311681809,
33.6186975660792));
#56506=CARTESIAN_POINT('Ctrl Pts',(-3.54887376960743,-5.76440080884536,
33.6269276746607));
#56507=CARTESIAN_POINT('Ctrl Pts',(-3.39776104093056,-5.85213712319991,
33.6351577832422));
#56508=CARTESIAN_POINT('Ctrl Pts',(-3.24644113438345,-5.93999372538798,
33.6433991754289));
#56509=CARTESIAN_POINT('Ctrl Pts',(-3.09187522516354,-6.0218824861561,33.6516405676156));
#56510=CARTESIAN_POINT('Ctrl Pts',(-2.93458104387901,-6.09758338171,33.6598819598023));
#56511=CARTESIAN_POINT('Ctrl Pts',(-2.86612261989647,-6.13053033474645,
33.6634688230666));
#56512=CARTESIAN_POINT('Ctrl Pts',(-2.79714763125209,-6.16230580362811,
33.6670556863308));
#56513=CARTESIAN_POINT('Ctrl Pts',(-2.72769970169662,-6.19289458471272,
33.670642549595));
#56514=CARTESIAN_POINT('Ctrl Pts',(-2.56412210465004,-6.26494337491329,
33.6790910444234));
#56515=CARTESIAN_POINT('Ctrl Pts',(-2.39754655500624,-6.33056952167647,
33.6875395392518));
#56516=CARTESIAN_POINT('Ctrl Pts',(-2.228505189376,-6.38952686988045,33.6959880340803));
#56517=CARTESIAN_POINT('Ctrl Pts',(-2.05961823321371,-6.44843036397165,
33.7044288116994));
#56518=CARTESIAN_POINT('Ctrl Pts',(-1.88827026407826,-6.50067709254612,
33.7128695893186));
#56519=CARTESIAN_POINT('Ctrl Pts',(-1.71501368446944,-6.54606882503404,
33.7213103669378));
#56520=CARTESIAN_POINT('Ctrl Pts',(-1.54188872154352,-6.59142607508399,
33.7297447324071));
#56521=CARTESIAN_POINT('Ctrl Pts',(-1.36685835996665,-6.629938626022,33.7381790978764));
#56522=CARTESIAN_POINT('Ctrl Pts',(-1.19049084534923,-6.66145783947776,
33.7466134633457));
#56523=CARTESIAN_POINT('Ctrl Pts',(-1.0142302263253,-6.69295794927355,33.7550427167824));
#56524=CARTESIAN_POINT('Ctrl Pts',(-0.836634397506523,-6.71747311379963,
33.763471970219));
#56525=CARTESIAN_POINT('Ctrl Pts',(-0.658282890031881,-6.73490554029463,
33.7719012236556));
#56526=CARTESIAN_POINT('Ctrl Pts',(-0.480012122038219,-6.75233007515424,
33.7803266611808));
#56527=CARTESIAN_POINT('Ctrl Pts',(-0.30098668883616,-6.76267823310201,
33.7887520987061));
#56528=CARTESIAN_POINT('Ctrl Pts',(-0.121792753588958,-6.7659038956501,
33.7971775362313));
#56529=CARTESIAN_POINT('Ctrl Pts',(0.0573618175695597,-6.76912884960688,
33.8056011229145));
#56530=CARTESIAN_POINT('Ctrl Pts',(0.236684483945418,-6.76523441908685,
33.8140247095977));
#56531=CARTESIAN_POINT('Ctrl Pts',(0.415587019380714,-6.7542265604081,33.8224482962809));
#56532=CARTESIAN_POINT('Ctrl Pts',(0.594469536560332,-6.74321993345103,
33.8308709404089));
#56533=CARTESIAN_POINT('Ctrl Pts',(0.77293168381078,-6.7251014855954,33.8392935845369));
#56534=CARTESIAN_POINT('Ctrl Pts',(0.950387979692742,-6.69992923007815,
33.8477162286649));
#56535=CARTESIAN_POINT('Ctrl Pts',(1.12784916470806,-6.67475628103513,33.8561391048468));
#56536=CARTESIAN_POINT('Ctrl Pts',(1.30430411306229,-6.64252918407661,33.8645619810287));
#56537=CARTESIAN_POINT('Ctrl Pts',(1.47917481759715,-6.60335754438501,33.8729848572107));
#56538=CARTESIAN_POINT('Ctrl Pts',(1.65407472651038,-6.56417936281214,33.8814091400597));
#56539=CARTESIAN_POINT('Ctrl Pts',(1.82738953895219,-6.51805439971197,33.8898334229087));
#56540=CARTESIAN_POINT('Ctrl Pts',(1.99855338766498,-6.46514294943684,33.8982577057577));
#56541=CARTESIAN_POINT('Ctrl Pts',(2.16983283411233,-6.41219576472462,33.9066876780558));
#56542=CARTESIAN_POINT('Ctrl Pts',(2.33895809519942,-6.35245303285671,33.915117650354));
#56543=CARTESIAN_POINT('Ctrl Pts',(2.50537940031931,-6.28612464563468,33.9235476226521));
#56544=CARTESIAN_POINT('Ctrl Pts',(2.67186019836991,-6.21977254708468,33.9319806085293));
#56545=CARTESIAN_POINT('Ctrl Pts',(2.83563480565612,-6.14683022802284,33.9404135944065));
#56546=CARTESIAN_POINT('Ctrl Pts',(2.99617474068942,-6.06755518501931,33.9488465802837));
#56547=CARTESIAN_POINT('Ctrl Pts',(3.15686237148472,-5.98820720945927,33.9572873244566));
#56548=CARTESIAN_POINT('Ctrl Pts',(3.31430908801181,-5.90251502289283,33.9657280686294));
#56549=CARTESIAN_POINT('Ctrl Pts',(3.46801128996304,-5.81078193470456,33.9741688128022));
#56550=CARTESIAN_POINT('Ctrl Pts',(3.55299734244075,-5.76006026027348,33.9788359256875));
#56551=CARTESIAN_POINT('Ctrl Pts',(3.63683908351056,-5.70749249695703,33.9835030385727));
#56552=CARTESIAN_POINT('Ctrl Pts',(3.719455311038,-5.65313551838192,33.988170151458));
#56553=CARTESIAN_POINT('Ctrl Pts',(3.86357204079958,-5.55831455854855,33.9963115186759));
#56554=CARTESIAN_POINT('Ctrl Pts',(4.00424412887687,-5.4578581470722,34.0044528858937));
#56555=CARTESIAN_POINT('Ctrl Pts',(4.14099873769758,-5.3520480616664,34.0125942531116));
#56556=CARTESIAN_POINT('Ctrl Pts',(4.27763397014559,-5.24633034041782,34.020728513535));
#56557=CARTESIAN_POINT('Ctrl Pts',(4.41035824268065,-5.13526847007893,34.0288627739585));
#56558=CARTESIAN_POINT('Ctrl Pts',(4.53872663540292,-5.01918813445801,34.036997034382));
#56559=CARTESIAN_POINT('Ctrl Pts',(4.66700745984418,-4.90318698464938,34.0451257459068));
#56560=CARTESIAN_POINT('Ctrl Pts',(4.79093805008766,-4.78217442998399,34.0532544574315));
#56561=CARTESIAN_POINT('Ctrl Pts',(4.91010564445792,-4.65651710619241,34.0613831689563));
#56562=CARTESIAN_POINT('Ctrl Pts',(5.02921641000494,-4.53091970605607,34.0695080040488));
#56563=CARTESIAN_POINT('Ctrl Pts',(5.14356845145161,-4.40068221268763,34.0776328391413));
#56564=CARTESIAN_POINT('Ctrl Pts',(5.25278506741071,-4.2662088598177,34.0857576742338));
#56565=CARTESIAN_POINT('Ctrl Pts',(5.36197110787203,-4.13177315313985,34.093880234756));
#56566=CARTESIAN_POINT('Ctrl Pts',(5.46602435649172,-3.9931042333415,34.1020027952782));
#56567=CARTESIAN_POINT('Ctrl Pts',(5.56460772447092,-3.85064018998901,34.1101253558003));
#56568=CARTESIAN_POINT('Ctrl Pts',(5.66319633190043,-3.70816857504213,34.1182483480155));
#56569=CARTESIAN_POINT('Ctrl Pts',(5.75631426641379,-3.56190173238892,34.1263713402307));
#56570=CARTESIAN_POINT('Ctrl Pts',(5.8436670886332,-3.41230771725313,34.1344943324458));
#56571=CARTESIAN_POINT('Ctrl Pts',(5.88825804233793,-3.33594453133714,34.1386408724271));
#56572=CARTESIAN_POINT('Ctrl Pts',(5.9313474338422,-3.25871480604756,34.1427874124084));
#56573=CARTESIAN_POINT('Ctrl Pts',(5.9729006403841,-3.18068340771275,34.1469339523897));
#56574=CARTESIAN_POINT('Ctrl Pts',(6.06292746776206,-3.01162499290993,34.1559176114181));
#56575=CARTESIAN_POINT('Ctrl Pts',(6.14569643807502,-2.83888592048222,34.1649012704466));
#56576=CARTESIAN_POINT('Ctrl Pts',(6.22095320011086,-2.66308660806038,34.173884929475));
#56577=CARTESIAN_POINT('Ctrl Pts',(6.29633925246657,-2.48698527428227,34.1828840223345));
#56578=CARTESIAN_POINT('Ctrl Pts',(6.36418720716324,-2.30781341220419,34.1918831151939));
#56579=CARTESIAN_POINT('Ctrl Pts',(6.42429160021571,-2.12620940534979,34.2008822080534));
#56580=CARTESIAN_POINT('Ctrl Pts',(6.48453692127384,-1.94417958784817,34.2099024012709));
#56581=CARTESIAN_POINT('Ctrl Pts',(6.5370022773313,-1.75970644342602,34.2189225944883));
#56582=CARTESIAN_POINT('Ctrl Pts',(6.58153193264677,-1.57344412660599,34.2279427877058));
#56583=CARTESIAN_POINT('Ctrl Pts',(6.62610668538862,-1.38699317254946,34.2369721161276));
#56584=CARTESIAN_POINT('Ctrl Pts',(6.66272963199257,-1.19874965998421,34.2460014445494));
#56585=CARTESIAN_POINT('Ctrl Pts',(6.69129630227897,-1.00937742946224,34.2550307729711));
#56586=CARTESIAN_POINT('Ctrl Pts',(6.71990324581237,-0.819738222266482,
34.264072830926));
#56587=CARTESIAN_POINT('Ctrl Pts',(6.74043116743781,-0.628967351954016,
34.2731148888808));
#56588=CARTESIAN_POINT('Ctrl Pts',(6.75282730103158,-0.437735585076878,
34.2821569468356));
#56589=CARTESIAN_POINT('Ctrl Pts',(6.76358499150263,-0.271779632703956,
34.2900038823307));
#56590=CARTESIAN_POINT('Ctrl Pts',(6.76821926374527,-0.105476725647189,
34.2978508178259));
#56591=CARTESIAN_POINT('Ctrl Pts',(6.76672744690542,0.0607343337573115,
34.305697753321));
#56592=CARTESIAN_POINT('Ctrl Pts',(6.76508229718105,0.244029005904913,34.3143512176217));
#56593=CARTESIAN_POINT('Ctrl Pts',(6.75598423759691,0.427373527978166,34.3230046819225));
#56594=CARTESIAN_POINT('Ctrl Pts',(6.73943635421743,0.610152954145541,34.3316581462232));
#56595=CARTESIAN_POINT('Ctrl Pts',(6.72290371482327,0.792764003075407,34.3403036389133));
#56596=CARTESIAN_POINT('Ctrl Pts',(6.69893496700205,0.974810692669004,34.3489491316035));
#56597=CARTESIAN_POINT('Ctrl Pts',(6.66758519465642,1.15568017721104,34.3575946242936));
#56598=CARTESIAN_POINT('Ctrl Pts',(6.63529231822572,1.34199080970958,34.3665002017902));
#56599=CARTESIAN_POINT('Ctrl Pts',(6.59516738389635,1.52705197798527,34.3754057792868));
#56600=CARTESIAN_POINT('Ctrl Pts',(6.54732823285542,1.71019940686877,34.3843113567834));
#56601=CARTESIAN_POINT('Ctrl Pts',(6.50097433243883,1.88766070154679,34.3929404449559));
#56602=CARTESIAN_POINT('Ctrl Pts',(6.44737810572147,2.0633249796476,34.4015695331283));
#56603=CARTESIAN_POINT('Ctrl Pts',(6.38669867572393,2.23659764497467,34.4101986213008));
#56604=CARTESIAN_POINT('Ctrl Pts',(6.32310285162108,2.41819819637104,34.4192424434595));
#56605=CARTESIAN_POINT('Ctrl Pts',(6.25172622432653,2.59717124063413,34.4282862656181));
#56606=CARTESIAN_POINT('Ctrl Pts',(6.17281117396229,2.7728489339678,34.4373300877768));
#56607=CARTESIAN_POINT('Ctrl Pts',(6.09389612359799,2.94852662730158,34.4463739099354));
#56608=CARTESIAN_POINT('Ctrl Pts',(6.00744277645742,3.12090860402851,34.4554177320941));
#56609=CARTESIAN_POINT('Ctrl Pts',(5.91375248523791,3.28934956235157,34.4644615542527));
#56610=CARTESIAN_POINT('Ctrl Pts',(5.8264647554555,3.44627968459813,34.4728873441025));
#56611=CARTESIAN_POINT('Ctrl Pts',(5.73293380946965,3.59972040454659,34.4813131339524));
#56612=CARTESIAN_POINT('Ctrl Pts',(5.63347206019072,3.74917078125957,34.4897389238022));
#56613=CARTESIAN_POINT('Ctrl Pts',(5.5339872324399,3.89865583548771,34.4981666687187));
#56614=CARTESIAN_POINT('Ctrl Pts',(5.42856904122757,4.04414842440703,34.5065944136352));
#56615=CARTESIAN_POINT('Ctrl Pts',(5.31757276197332,4.18517728670118,34.5150221585518));
#56616=CARTESIAN_POINT('Ctrl Pts',(5.20653569715525,4.32625797002665,34.5234530002417));
#56617=CARTESIAN_POINT('Ctrl Pts',(5.08991666237077,4.46287139595117,34.5318838419316));
#56618=CARTESIAN_POINT('Ctrl Pts',(4.96811091470667,4.59457973477144,34.5403146836216));
#56619=CARTESIAN_POINT('Ctrl Pts',(4.84619324310758,4.72640909674403,34.548753272179));
#56620=CARTESIAN_POINT('Ctrl Pts',(4.71907956199458,4.85332412320422,34.5571918607363));
#56621=CARTESIAN_POINT('Ctrl Pts',(4.58720244125173,4.97492339267392,34.5656304492937));
#56622=CARTESIAN_POINT('Ctrl Pts',(4.4552561699748,5.0965864234267,34.574073462674));
#56623=CARTESIAN_POINT('Ctrl Pts',(4.31854172632411,5.21292791942066,34.5825164760543));
#56624=CARTESIAN_POINT('Ctrl Pts',(4.17752481791164,5.32358670406825,34.5909594894345));
#56625=CARTESIAN_POINT('Ctrl Pts',(4.03635976140795,5.43436174348208,34.5994113727888));
#56626=CARTESIAN_POINT('Ctrl Pts',(3.89088347633704,5.53944194759298,34.6078632561432));
#56627=CARTESIAN_POINT('Ctrl Pts',(3.74159156531282,5.63850880626961,34.6163151394975));
#56628=CARTESIAN_POINT('Ctrl Pts',(3.70090480307715,5.66550765501338,34.6186185447264));
#56629=CARTESIAN_POINT('Ctrl Pts',(3.65993479012726,5.69206013077368,34.6209219499552));
#56630=CARTESIAN_POINT('Ctrl Pts',(3.61869188063002,5.71816037489877,34.6232253551841));
#56631=CARTESIAN_POINT('Ctrl Pts',(3.46974835597489,5.81241808856974,34.6315438103483));
#56632=CARTESIAN_POINT('Ctrl Pts',(3.31697584700636,5.90094381771582,34.6398622655126));
#56633=CARTESIAN_POINT('Ctrl Pts',(3.16084977546522,5.98342023402514,34.6481807206768));
#56634=CARTESIAN_POINT('Ctrl Pts',(3.14031925885143,5.99426585012609,34.6492745942385));
#56635=CARTESIAN_POINT('Ctrl Pts',(3.11973079513912,6.00500692051147,34.6503684678002));
#56636=CARTESIAN_POINT('Ctrl Pts',(3.09908550384707,6.01564277861019,34.6514623413619));
#56637=CARTESIAN_POINT('Origin',(0.,0.,-63.6971797838103));
#56638=CARTESIAN_POINT('',(3.09908550384717,6.01564277861014,37.0457563580462));
#56639=CARTESIAN_POINT('',(3.09908550384717,6.01564277861014,36.651532120892));
#56640=CARTESIAN_POINT('',(3.09908550384721,6.01564277861012,-63.6971797838103));
#56641=CARTESIAN_POINT('',(-6.767,4.50145461541613E-12,35.6971797838099));
#56642=CARTESIAN_POINT('Ctrl Pts',(-6.767,4.88611405695858E-12,35.6971797838098));
#56643=CARTESIAN_POINT('Ctrl Pts',(-6.76700000000014,-0.186007249555188,
35.7059292956226));
#56644=CARTESIAN_POINT('Ctrl Pts',(-6.75932637294273,-0.372014355811442,
35.7146788074353));
#56645=CARTESIAN_POINT('Ctrl Pts',(-6.744005182634,-0.557389537581891,35.7234283192481));
#56646=CARTESIAN_POINT('Ctrl Pts',(-6.72868405703777,-0.742763936378502,
35.7321777941053));
#56647=CARTESIAN_POINT('Ctrl Pts',(-6.7057154564362,-0.927506130400955,
35.7409272689625));
#56648=CARTESIAN_POINT('Ctrl Pts',(-6.67517739401639,-1.11098864009162,
35.7496767438197));
#56649=CARTESIAN_POINT('Ctrl Pts',(-6.64463945804465,-1.29447039004152,
35.7584261824482));
#56650=CARTESIAN_POINT('Ctrl Pts',(-6.60653217002812,-1.47669218338883,
35.7671756210767));
#56651=CARTESIAN_POINT('Ctrl Pts',(-6.56098496085581,-1.65703510627383,
35.7759250597052));
#56652=CARTESIAN_POINT('Ctrl Pts',(-6.51543793649669,-1.83737729739609,
35.7846744628318));
#56653=CARTESIAN_POINT('Ctrl Pts',(-6.46245112157021,-2.01584035544553,
35.7934238659585));
#56654=CARTESIAN_POINT('Ctrl Pts',(-6.40220448361854,-2.1918181379701,35.8021732690851));
#56655=CARTESIAN_POINT('Ctrl Pts',(-6.34195808512117,-2.36779522105917,
35.8109226374366));
#56656=CARTESIAN_POINT('Ctrl Pts',(-6.27445201416505,-2.54128677725371,
35.8196720057882));
#56657=CARTESIAN_POINT('Ctrl Pts',(-6.19991555052882,-2.71170355428299,
35.8284213741397));
#56658=CARTESIAN_POINT('Ctrl Pts',(-6.1253793769528,-2.88211966813178,35.8371707084429));
#56659=CARTESIAN_POINT('Ctrl Pts',(-6.04381298028511,-3.04946076419551,
35.8459200427461));
#56660=CARTESIAN_POINT('Ctrl Pts',(-5.9554933930904,-3.21315848424205,35.8546693770492));
#56661=CARTESIAN_POINT('Ctrl Pts',(-5.86717414225866,-3.37685558084983,
35.8634186780308));
#56662=CARTESIAN_POINT('Ctrl Pts',(-5.77210188844123,-3.53690907699909,
35.8721679790124));
#56663=CARTESIAN_POINT('Ctrl Pts',(-5.67059953311426,-3.69277537023907,
35.8809172799939));
#56664=CARTESIAN_POINT('Ctrl Pts',(-5.56909755592753,-3.84864108280962,
35.8896665483805));
#56665=CARTESIAN_POINT('Ctrl Pts',(-5.46116568155,-4.00031938354783,35.8984158167672));
#56666=CARTESIAN_POINT('Ctrl Pts',(-5.34717048488399,-4.14729511918136,
35.9071650851538));
#56667=CARTESIAN_POINT('Ctrl Pts',(-5.23317570343298,-4.29427031947189,
35.9159143216722));
#56668=CARTESIAN_POINT('Ctrl Pts',(-5.11311781951509,-4.43654276249602,
35.9246635581906));
#56669=CARTESIAN_POINT('Ctrl Pts',(-4.98740458929172,-4.57362924412462,
35.9334127947089));
#56670=CARTESIAN_POINT('Ctrl Pts',(-4.86169180652671,-4.71071523781338,
35.9421620000856));
#56671=CARTESIAN_POINT('Ctrl Pts',(-4.73032391141508,-4.84261509584552,
35.9509112054623));
#56672=CARTESIAN_POINT('Ctrl Pts',(-4.59374706947268,-4.96888084599653,
35.959660410839));
#56673=CARTESIAN_POINT('Ctrl Pts',(-4.45717070231474,-5.09514615720771,
35.9684095858007));
#56674=CARTESIAN_POINT('Ctrl Pts',(-4.31538563497356,-5.21577720520587,
35.9771587607625));
#56675=CARTESIAN_POINT('Ctrl Pts',(-4.16887340952063,-5.33036429293457,
35.9859079357242));
#56676=CARTESIAN_POINT('Ctrl Pts',(-4.02236168122556,-5.44495099183652,
35.9946570809974));
#56677=CARTESIAN_POINT('Ctrl Pts',(-3.87112305263268,-5.55349359497867,
36.0034062262706));
#56678=CARTESIAN_POINT('Ctrl Pts',(-3.71567116929099,-5.65562346357143,
36.0121553715439));
#56679=CARTESIAN_POINT('Ctrl Pts',(-3.56021980053412,-5.75775299408865,
36.0209044878552));
#56680=CARTESIAN_POINT('Ctrl Pts',(-3.40055544442181,-5.85346967519823,
36.0296536041666));
#56681=CARTESIAN_POINT('Ctrl Pts',(-3.23722035886936,-5.94244843041332,
36.038402720478));
#56682=CARTESIAN_POINT('Ctrl Pts',(-3.07388580043576,-6.03142689847407,
36.047151808554));
#56683=CARTESIAN_POINT('Ctrl Pts',(-2.90688078789303,-6.11366734707864,
36.05590089663));
#56684=CARTESIAN_POINT('Ctrl Pts',(-2.73677250610466,-6.18889047001396,
36.064649984706));
#56685=CARTESIAN_POINT('Ctrl Pts',(-2.56666475917026,-6.26411335643296,
36.0733990452732));
#56686=CARTESIAN_POINT('Ctrl Pts',(-2.39345402457205,-6.33231884545213,
36.0821481058404));
#56687=CARTESIAN_POINT('Ctrl Pts',(-2.21772855944197,-6.39327529804837,
36.0908971664075));
#56688=CARTESIAN_POINT('Ctrl Pts',(-2.04200363223764,-6.45423156404647,
36.0996462001923));
#56689=CARTESIAN_POINT('Ctrl Pts',(-1.86376426061249,-6.5079387441239,36.1083952339771));
#56690=CARTESIAN_POINT('Ctrl Pts',(-1.68361577621946,-6.55421443943246,
36.1171442677619));
#56691=CARTESIAN_POINT('Ctrl Pts',(-1.50346782833442,-6.60048999692537,
36.1258932754908));
#56692=CARTESIAN_POINT('Ctrl Pts',(-1.32141105657582,-6.63933404265124,
36.1346422832197));
#56693=CARTESIAN_POINT('Ctrl Pts',(-1.13806375346697,-6.67061465631501,
36.1433912909486));
#56694=CARTESIAN_POINT('Ctrl Pts',(-0.954716981171831,-6.70189517941744,
36.152140273348));
#56695=CARTESIAN_POINT('Ctrl Pts',(-0.770079967444305,-6.7256122660898,
36.1608892557474));
#56696=CARTESIAN_POINT('Ctrl Pts',(-0.584779764075293,-6.74168536995966,
36.1696382381469));
#56697=CARTESIAN_POINT('Ctrl Pts',(-0.391489587595131,-6.7584515311786,
36.1787644685625));
#56698=CARTESIAN_POINT('Ctrl Pts',(-0.197478091807359,-6.76689985146388,
36.1878906989781));
#56699=CARTESIAN_POINT('Ctrl Pts',(-0.00346214753309966,-6.76699911434415,
36.1970169293937));
#56700=CARTESIAN_POINT('Ctrl Pts',(0.184490798482673,-6.7670952752594,36.2058579651089));
#56701=CARTESIAN_POINT('Ctrl Pts',(0.372447602152916,-6.75935633790774,
36.214699000824));
#56702=CARTESIAN_POINT('Ctrl Pts',(0.559756448192457,-6.74380914014528,
36.2235400365391));
#56703=CARTESIAN_POINT('Ctrl Pts',(0.745136131041587,-6.72842206873174,
36.2322900151524));
#56704=CARTESIAN_POINT('Ctrl Pts',(0.929880851943267,-6.70538686355748,
36.2410399937657));
#56705=CARTESIAN_POINT('Ctrl Pts',(1.11336305057284,-6.67478177303342,36.249789972379));
#56706=CARTESIAN_POINT('Ctrl Pts',(1.29684337089954,-6.64417699581294,36.258539861419));
#56707=CARTESIAN_POINT('Ctrl Pts',(1.47906091205029,-6.60600253548096,36.267289750459));
#56708=CARTESIAN_POINT('Ctrl Pts',(1.6593967109507,-6.5603880644125,36.276039639499));
#56709=CARTESIAN_POINT('Ctrl Pts',(1.8397307236901,-6.51477404513892,36.2847894418745));
#56710=CARTESIAN_POINT('Ctrl Pts',(2.01818275356888,-6.46172023288707,36.29353924425));
#56711=CARTESIAN_POINT('Ctrl Pts',(2.19414664033179,-6.40140683918158,36.3022890466255));
#56712=CARTESIAN_POINT('Ctrl Pts',(2.37010884271118,-6.3410940228155,36.311038765245));
#56713=CARTESIAN_POINT('Ctrl Pts',(2.54358267847669,-6.27352185699847,36.3197884838646));
#56714=CARTESIAN_POINT('Ctrl Pts',(2.7139789084161,-6.19891986435319,36.3285382024841));
#56715=CARTESIAN_POINT('Ctrl Pts',(2.8843735638881,-6.12431856103305,36.3372878402559));
#56716=CARTESIAN_POINT('Ctrl Pts',(3.0516904078704,-6.04268767582624,36.3460374780277));
#56717=CARTESIAN_POINT('Ctrl Pts',(3.21536112511921,-5.95430447954017,36.3547871157996));
#56718=CARTESIAN_POINT('Ctrl Pts',(3.37903038442716,-5.86592207055116,36.3635366756316));
#56719=CARTESIAN_POINT('Ctrl Pts',(3.53905332979852,-5.77078760703452,36.3722862354637));
#56720=CARTESIAN_POINT('Ctrl Pts',(3.69488643041776,-5.66922422085374,36.3810357952958));
#56721=CARTESIAN_POINT('Ctrl Pts',(3.85071819468642,-5.56766170563228,36.3897852800958));
#56722=CARTESIAN_POINT('Ctrl Pts',(4.0023599459914,-5.45967053456314,36.3985347648958));
#56723=CARTESIAN_POINT('Ctrl Pts',(4.14929662974232,-5.34561750206738,36.4072842496958));
#56724=CARTESIAN_POINT('Ctrl Pts',(4.29623210224975,-5.23156540974523,36.4160336623711));
#56725=CARTESIAN_POINT('Ctrl Pts',(4.43846235842047,-5.11145173172247,36.4247830750465));
#56726=CARTESIAN_POINT('Ctrl Pts',(4.57550431797358,-4.98568443006626,36.4335324877218));
#56727=CARTESIAN_POINT('Ctrl Pts',(4.71254519337427,-4.85991812336754,36.4422818311797));
#56728=CARTESIAN_POINT('Ctrl Pts',(4.8443976431492,-4.72849847631166,36.4510311746376));
#56729=CARTESIAN_POINT('Ctrl Pts',(4.97061384196626,-4.59187184425409,36.4597805180955));
#56730=CARTESIAN_POINT('Ctrl Pts',(5.0968290842015,-4.45524624767812,36.4685297952429));
#56731=CARTESIAN_POINT('Ctrl Pts',(5.21740796650117,-4.31341395556957,36.4772790723902));
#56732=CARTESIAN_POINT('Ctrl Pts',(5.33194095942201,-4.1668566816292,36.4860283495376));
#56733=CARTESIAN_POINT('Ctrl Pts',(5.44647312235089,-4.02030046975274,36.4947775632811));
#56734=CARTESIAN_POINT('Ctrl Pts',(5.55495930712251,-3.86901957035601,36.5035267770247));
#56735=CARTESIAN_POINT('Ctrl Pts',(5.65703106079764,-3.71352778058422,36.5122759907682));
#56736=CARTESIAN_POINT('Ctrl Pts',(5.75910210868711,-3.55803706597644,36.5210251440144));
#56737=CARTESIAN_POINT('Ctrl Pts',(5.8547586569853,-3.39833575880934,36.5297742972606));
#56738=CARTESIAN_POINT('Ctrl Pts',(5.94367583069048,-3.23496624706747,36.5385234505068));
#56739=CARTESIAN_POINT('Ctrl Pts',(6.03259241910056,-3.0715978107014,36.547272546162));
#56740=CARTESIAN_POINT('Ctrl Pts',(6.11476958470941,-2.90456146975888,36.5560216418171));
#56741=CARTESIAN_POINT('Ctrl Pts',(6.18992823574355,-2.73442451648326,36.5647707374722));
#56742=CARTESIAN_POINT('Ctrl Pts',(6.26508641700904,-2.56428862662491,36.5735197784423));
#56743=CARTESIAN_POINT('Ctrl Pts',(6.33322605570266,-2.39105242531359,36.5822688194124));
#56744=CARTESIAN_POINT('Ctrl Pts',(6.39411573747736,-2.21530425353817,36.5910178603825));
#56745=CARTESIAN_POINT('Ctrl Pts',(6.45500505889099,-2.03955712188645,36.5997668495735));
#56746=CARTESIAN_POINT('Ctrl Pts',(6.50864441544907,-1.86129832025651,36.6085158387645));
#56747=CARTESIAN_POINT('Ctrl Pts',(6.55485164049888,-1.68113324012382,36.6172648279555));
#56748=CARTESIAN_POINT('Ctrl Pts',(6.60199852639096,-1.4973043591296,36.6261917348324));
#56749=CARTESIAN_POINT('Ctrl Pts',(6.64140767441001,-1.31149113173701,36.6351186417093));
#56750=CARTESIAN_POINT('Ctrl Pts',(6.67293975269596,-1.12435050446469,36.6440455485862));
#56751=CARTESIAN_POINT('Ctrl Pts',(6.70384664831501,-0.940920291564142,
36.6527954627702));
#56752=CARTESIAN_POINT('Ctrl Pts',(6.72718585889661,-0.756215114278357,
36.6615453769542));
#56753=CARTESIAN_POINT('Ctrl Pts',(6.7428781045186,-0.570862389375578,36.6702952911382));
#56754=CARTESIAN_POINT('Ctrl Pts',(6.75857004154121,-0.385513309568533,
36.6790450332488));
#56755=CARTESIAN_POINT('Ctrl Pts',(6.76661529035555,-0.199516993259636,
36.6877947753593));
#56756=CARTESIAN_POINT('Ctrl Pts',(6.76698652348896,-0.013505218205474,
36.6965445174699));
#56757=CARTESIAN_POINT('Ctrl Pts',(6.76735774981525,0.172503146037491,36.7052940991406));
#56758=CARTESIAN_POINT('Ctrl Pts',(6.76005524147487,0.358526681832086,36.7140436808112));
#56759=CARTESIAN_POINT('Ctrl Pts',(6.74510380214892,0.543933542113499,36.7227932624819));
#56760=CARTESIAN_POINT('Ctrl Pts',(6.73015261710994,0.729337249083414,36.7315426953438));
#56761=CARTESIAN_POINT('Ctrl Pts',(6.70755278444622,0.914124015853416,36.7402921282057));
#56762=CARTESIAN_POINT('Ctrl Pts',(6.67738106408309,1.09766621749267,36.7490415610676));
#56763=CARTESIAN_POINT('Ctrl Pts',(6.64720981677277,1.28120554143203,36.75779085675));
#56764=CARTESIAN_POINT('Ctrl Pts',(6.60946696581549,1.46350005650501,36.7665401524323));
#56765=CARTESIAN_POINT('Ctrl Pts',(6.56428070011024,1.64393062206415,36.7752894481147));
#56766=CARTESIAN_POINT('Ctrl Pts',(6.51909508282775,1.8243585984453,36.7840386182447));
#56767=CARTESIAN_POINT('Ctrl Pts',(6.466466334157,2.00292240086438,36.7927877883747));
#56768=CARTESIAN_POINT('Ctrl Pts',(6.40657319597236,2.17901557696326,36.8015369585047));
#56769=CARTESIAN_POINT('Ctrl Pts',(6.34668083768339,2.35510646007314,36.8102860147077));
#56770=CARTESIAN_POINT('Ctrl Pts',(6.27952437143931,2.52872650996418,36.8190350709108));
#56771=CARTESIAN_POINT('Ctrl Pts',(6.20533187335181,2.69928607997821,36.8277841271139));
#56772=CARTESIAN_POINT('Ctrl Pts',(6.12831449784299,2.87633970115298,36.8368663034027));
#56773=CARTESIAN_POINT('Ctrl Pts',(6.043714894632,3.05009490562255,36.8459484796916));
#56774=CARTESIAN_POINT('Ctrl Pts',(5.95184265120539,3.21991584599543,36.8550306559804));
#56775=CARTESIAN_POINT('Ctrl Pts',(5.86333281335542,3.38352155905215,36.8637804363349));
#56776=CARTESIAN_POINT('Ctrl Pts',(5.76807337235736,3.54347560903741,36.8725302166893));
#56777=CARTESIAN_POINT('Ctrl Pts',(5.66638790086408,3.69923467178567,36.8812799970437));
#56778=CARTESIAN_POINT('Ctrl Pts',(5.56470608502797,3.85498813489685,36.890029462838));
#56779=CARTESIAN_POINT('Ctrl Pts',(5.45659885767009,4.00654667256184,36.8987789286322));
#56780=CARTESIAN_POINT('Ctrl Pts',(5.34243340580566,4.15339551506135,36.9075283944265));
#56781=CARTESIAN_POINT('Ctrl Pts',(5.22827145140647,4.30023985883805,36.9162775921804));
#56782=CARTESIAN_POINT('Ctrl Pts',(5.10805181978138,4.44237456992987,36.9250267899342));
#56783=CARTESIAN_POINT('Ctrl Pts',(4.98218281282593,4.57931691626403,36.9337759876881));
#56784=CARTESIAN_POINT('Ctrl Pts',(4.85631699296275,4.71625579512114,36.9425249639061));
#56785=CARTESIAN_POINT('Ctrl Pts',(4.72480227791888,4.84800236135721,36.9512739401241));
#56786=CARTESIAN_POINT('Ctrl Pts',(4.58808530848167,4.97410918678859,36.9600229163421));
#56787=CARTESIAN_POINT('Ctrl Pts',(4.45135945057028,5.10022421088958,36.9687724613633));
#56788=CARTESIAN_POINT('Ctrl Pts',(4.30943087208103,5.22069856611934,36.9775220063845));
#56789=CARTESIAN_POINT('Ctrl Pts',(4.16278164322535,5.33512305301631,36.9862715514057));
#56790=CARTESIAN_POINT('Ctrl Pts',(4.01614103534455,5.44954081331379,36.995020582073));
#56791=CARTESIAN_POINT('Ctrl Pts',(3.86478055833474,5.55790924068295,37.0037696127402));
#56792=CARTESIAN_POINT('Ctrl Pts',(3.70921425812008,5.65986029751254,37.0125186434075));
#56793=CARTESIAN_POINT('Ctrl Pts',(3.5536458453018,5.76181273884617,37.0212677928873));
#56794=CARTESIAN_POINT('Ctrl Pts',(3.39387173464407,5.85734747818027,37.0300169423672));
#56795=CARTESIAN_POINT('Ctrl Pts',(3.23043456092471,5.94614005448772,37.038766091847));
#56796=CARTESIAN_POINT('Ctrl Pts',(3.18690768806435,5.96978744811259,37.0410961805801));
#56797=CARTESIAN_POINT('Ctrl Pts',(3.14312114982902,5.9929568849929,37.0434262693131));
#56798=CARTESIAN_POINT('Ctrl Pts',(3.09908550384717,6.01564277861014,37.0457563580462));
#56799=CARTESIAN_POINT('Ctrl Pts',(3.0990855038472,6.01564277861013,35.0459194627137));
#56800=CARTESIAN_POINT('Ctrl Pts',(2.93136712737222,6.1020464445842,35.0547735800526));
#56801=CARTESIAN_POINT('Ctrl Pts',(2.75987960907094,6.18151138996883,35.0636276973915));
#56802=CARTESIAN_POINT('Ctrl Pts',(2.58519441278919,6.25372359863174,35.0724818147303));
#56803=CARTESIAN_POINT('Ctrl Pts',(2.57466267638231,6.25807725860514,35.0730156277375));
#56804=CARTESIAN_POINT('Ctrl Pts',(2.56411932536443,6.26240456914106,35.0735494407446));
#56805=CARTESIAN_POINT('Ctrl Pts',(2.55356448819932,6.26670546655955,35.0740832537517));
#56806=CARTESIAN_POINT('Ctrl Pts',(2.39122705594141,6.33285491371824,35.0822935019562));
#56807=CARTESIAN_POINT('Ctrl Pts',(2.2263263371004,6.39268881649299,35.0905037501607));
#56808=CARTESIAN_POINT('Ctrl Pts',(2.05939522783671,6.44602050070921,35.0987139983652));
#56809=CARTESIAN_POINT('Ctrl Pts',(1.89242443572067,6.49936486292991,35.1069261983094));
#56810=CARTESIAN_POINT('Ctrl Pts',(1.72342263064715,6.54620381877281,35.1151383982535));
#56811=CARTESIAN_POINT('Ctrl Pts',(1.55293741088268,6.5864007164673,35.1233505981977));
#56812=CARTESIAN_POINT('Ctrl Pts',(1.3823813047447,6.62661432770628,35.1315662127081));
#56813=CARTESIAN_POINT('Ctrl Pts',(1.21034090129479,6.66018029723885,35.1397818272185));
#56814=CARTESIAN_POINT('Ctrl Pts',(1.03737360229679,6.68701316054169,35.1479974417289));
#56815=CARTESIAN_POINT('Ctrl Pts',(0.86421206860269,6.71387615597401,35.1562222820143));
#56816=CARTESIAN_POINT('Ctrl Pts',(0.690121912293478,6.73399088885896,35.1644471222997));
#56817=CARTESIAN_POINT('Ctrl Pts',(0.515666242315641,6.74732371585476,35.1726719625851));
#56818=CARTESIAN_POINT('Ctrl Pts',(0.341098827417393,6.76066508298967,35.1809020711666));
#56819=CARTESIAN_POINT('Ctrl Pts',(0.166165786911986,6.76721587130811,35.1891321797481));
#56820=CARTESIAN_POINT('Ctrl Pts',(-0.00857021009941388,6.76699457303601,
35.1973622883296));
#56821=CARTESIAN_POINT('Ctrl Pts',(-0.183545772844242,6.76677297136059,
35.2056036805162));
#56822=CARTESIAN_POINT('Ctrl Pts',(-0.358323397887863,6.75976075224408,
35.2138450727029));
#56823=CARTESIAN_POINT('Ctrl Pts',(-0.532344962192309,6.74602830124722,
35.2220864648896));
#56824=CARTESIAN_POINT('Ctrl Pts',(-0.608083568257796,6.74005158967977,
35.2256733281542));
#56825=CARTESIAN_POINT('Ctrl Pts',(-0.683679079804085,6.73280258171049,
35.2292601914188));
#56826=CARTESIAN_POINT('Ctrl Pts',(-0.759086148045756,6.72429009039951,
35.2328470546835));
#56827=CARTESIAN_POINT('Ctrl Pts',(-0.936699895508152,6.70423977526012,
35.2412955495119));
#56828=CARTESIAN_POINT('Ctrl Pts',(-1.11367249075454,6.67713063639898,35.2497440443403));
#56829=CARTESIAN_POINT('Ctrl Pts',(-1.28942021218734,6.6430177266362,35.2581925391687));
#56830=CARTESIAN_POINT('Ctrl Pts',(-1.46500739828611,6.6089359770348,35.2666333167879));
#56831=CARTESIAN_POINT('Ctrl Pts',(-1.63937161501225,6.56786327199708,35.2750740944071));
#56832=CARTESIAN_POINT('Ctrl Pts',(-1.81193574336636,6.51990627708033,35.2835148720262));
#56833=CARTESIAN_POINT('Ctrl Pts',(-1.98436878106708,6.47198571333764,35.2919492374956));
#56834=CARTESIAN_POINT('Ctrl Pts',(-2.1550041363007,6.41719137423499,35.3003836029649));
#56835=CARTESIAN_POINT('Ctrl Pts',(-2.32327595385652,6.35568075364332,35.3088179684342));
#56836=CARTESIAN_POINT('Ctrl Pts',(-2.49144578258572,6.29420741437486,35.3172472218708));
#56837=CARTESIAN_POINT('Ctrl Pts',(-2.65725461732566,6.22602602375008,35.3256764753074));
#56838=CARTESIAN_POINT('Ctrl Pts',(-2.82015243589234,6.15134369372502,35.3341057287439));
#56839=CARTESIAN_POINT('Ctrl Pts',(-2.98297651084329,6.07669517228681,35.3425311662692));
#56840=CARTESIAN_POINT('Ctrl Pts',(-3.14289189476114,5.99555171849709,35.3509566037945));
#56841=CARTESIAN_POINT('Ctrl Pts',(-3.29936883688705,5.90816843684898,35.3593820413198));
#56842=CARTESIAN_POINT('Ctrl Pts',(-3.45581140523587,5.82080435095844,35.367805628003));
#56843=CARTESIAN_POINT('Ctrl Pts',(-3.60881674564846,5.72720333028828,35.3762292146862));
#56844=CARTESIAN_POINT('Ctrl Pts',(-3.75787952875216,5.62766651885002,35.3846528013694));
#56845=CARTESIAN_POINT('Ctrl Pts',(-3.9069256325118,5.52814084505919,35.3930754454974));
#56846=CARTESIAN_POINT('Ctrl Pts',(-4.05202978121308,5.42268088970375,35.4014980896254));
#56847=CARTESIAN_POINT('Ctrl Pts',(-4.19271521254371,5.31163140160389,35.4099207337534));
#56848=CARTESIAN_POINT('Ctrl Pts',(-4.33340451992718,5.20057885395709,35.4183436099354));
#56849=CARTESIAN_POINT('Ctrl Pts',(-4.46967460576564,5.08393667340918,35.4267664861174));
#56850=CARTESIAN_POINT('Ctrl Pts',(-4.60108112797115,4.96209043184702,35.4351893622993));
#56851=CARTESIAN_POINT('Ctrl Pts',(-4.73250959579531,4.84022384128615,35.4436136451484));
#56852=CARTESIAN_POINT('Ctrl Pts',(-4.85907263658495,4.71315168407173,35.4520379279974));
#56853=CARTESIAN_POINT('Ctrl Pts',(-4.98036190608001,4.58129722725639,35.4604622108465));
#56854=CARTESIAN_POINT('Ctrl Pts',(-5.10173308986262,4.44935372081668,35.4688921831446));
#56855=CARTESIAN_POINT('Ctrl Pts',(-5.21782315931491,4.31262170655697,35.4773221554428));
#56856=CARTESIAN_POINT('Ctrl Pts',(-5.32826263794759,4.17155921221932,35.485752127741));
#56857=CARTESIAN_POINT('Ctrl Pts',(-5.43874159691134,4.03044629031673,35.4941851136182));
#56858=CARTESIAN_POINT('Ctrl Pts',(-5.54356573661601,3.88500006782507,35.5026180994954));
#56859=CARTESIAN_POINT('Ctrl Pts',(-5.6424079327895,3.73570899830195,35.5110510853726));
#56860=CARTESIAN_POINT('Ctrl Pts',(-5.74134106318118,3.58628058190456,35.5194918295454));
#56861=CARTESIAN_POINT('Ctrl Pts',(-5.8342810755705,3.43300053271089,35.5279325737182));
#56862=CARTESIAN_POINT('Ctrl Pts',(-5.92094540033487,3.27638437400945,35.536373317891));
#56863=CARTESIAN_POINT('Ctrl Pts',(-5.96886442009193,3.18978711702404,35.5410404307761));
#56864=CARTESIAN_POINT('Ctrl Pts',(-6.01486560565325,3.10217034801432,35.5457075436612));
#56865=CARTESIAN_POINT('Ctrl Pts',(-6.05890740361888,3.01362407648538,35.5503746565462));
#56866=CARTESIAN_POINT('Ctrl Pts',(-6.13625931929622,2.85810763425941,35.5585716452936));
#56867=CARTESIAN_POINT('Ctrl Pts',(-6.20771484785789,2.69942007259873,35.5667686340411));
#56868=CARTESIAN_POINT('Ctrl Pts',(-6.27300523970475,2.53804930264105,35.5749656227885));
#56869=CARTESIAN_POINT('Ctrl Pts',(-6.33823577321284,2.37682647767103,35.5831550965232));
#56870=CARTESIAN_POINT('Ctrl Pts',(-6.39731228980008,2.21292567422031,35.5913445702578));
#56871=CARTESIAN_POINT('Ctrl Pts',(-6.45001232168374,2.04685858088142,35.5995340439925));
#56872=CARTESIAN_POINT('Ctrl Pts',(-6.50266850996351,1.88092964646957,35.6077167045236));
#56873=CARTESIAN_POINT('Ctrl Pts',(-6.5489586750115,1.71283835509394,35.6158993650547));
#56874=CARTESIAN_POINT('Ctrl Pts',(-6.58870881764961,1.54311539303654,35.6240820255859));
#56875=CARTESIAN_POINT('Ctrl Pts',(-6.62843926318373,1.37347653258509,35.6322606314217));
#56876=CARTESIAN_POINT('Ctrl Pts',(-6.66163605740798,1.20220796131236,35.6404392372576));
#56877=CARTESIAN_POINT('Ctrl Pts',(-6.68817524503397,1.02985479156765,35.6486178430935));
#56878=CARTESIAN_POINT('Ctrl Pts',(-6.7147089798616,0.857537033874542,35.6567947685355));
#56879=CARTESIAN_POINT('Ctrl Pts',(-6.73458777152393,0.684135476315733,
35.6649716939774));
#56880=CARTESIAN_POINT('Ctrl Pts',(-6.74773887873612,0.510204884720826,
35.6731486194194));
#56881=CARTESIAN_POINT('Ctrl Pts',(-6.76057309465491,0.340465353942477,
35.6811285122894));
#56882=CARTESIAN_POINT('Ctrl Pts',(-6.76700010762539,0.17022232465388,35.6891084051592));
#56883=CARTESIAN_POINT('Ctrl Pts',(-6.76699999999865,-4.27847436253801E-6,
35.6970882980292));
#56884=CARTESIAN_POINT('',(-6.76699909143212,0.00350664467830086,35.3028202162169));
#56885=CARTESIAN_POINT('Ctrl Pts',(3.09908550384707,6.01564277861019,34.6514623413619));
#56886=CARTESIAN_POINT('Ctrl Pts',(2.94225676158109,6.09643641939472,34.6597717816335));
#56887=CARTESIAN_POINT('Ctrl Pts',(2.78214665864428,6.17115516241344,34.668081221905));
#56888=CARTESIAN_POINT('Ctrl Pts',(2.61926119430939,6.239532017386,34.6763906621765));
#56889=CARTESIAN_POINT('Ctrl Pts',(2.45647935227009,6.30786537328572,34.6846948162595));
#56890=CARTESIAN_POINT('Ctrl Pts',(2.29092598676088,6.3698647463026,34.6929989703425));
#56891=CARTESIAN_POINT('Ctrl Pts',(2.12312973459856,6.42531004155157,34.7013031244254));
#56892=CARTESIAN_POINT('Ctrl Pts',(1.95540951419974,6.48073021345291,34.7096035157338));
#56893=CARTESIAN_POINT('Ctrl Pts',(1.78544876220221,6.52960211728033,34.7179039070422));
#56894=CARTESIAN_POINT('Ctrl Pts',(1.61379425525372,6.57175449189257,34.7262042983505));
#56895=CARTESIAN_POINT('Ctrl Pts',(1.44218611769813,6.61389547979521,34.7345024474567));
#56896=CARTESIAN_POINT('Ctrl Pts',(1.26888547465544,6.64932047391046,34.7428005965629));
#56897=CARTESIAN_POINT('Ctrl Pts',(1.09445258014889,6.67790854607979,34.7510987456691));
#56898=CARTESIAN_POINT('Ctrl Pts',(0.919996881133932,6.70650035571466,34.7593979796349));
#56899=CARTESIAN_POINT('Ctrl Pts',(0.744408977038477,6.72825339445515,34.7676972136008));
#56900=CARTESIAN_POINT('Ctrl Pts',(0.568258187685816,6.74309807374385,34.7759964475667));
#56901=CARTESIAN_POINT('Ctrl Pts',(0.392085688931662,6.75794458253955,34.7842967043574));
#56902=CARTESIAN_POINT('Ctrl Pts',(0.215350513402237,6.76588100520434,34.7925969611481));
#56903=CARTESIAN_POINT('Ctrl Pts',(0.0386258614192862,6.76688976139183,
34.8008972179388));
#56904=CARTESIAN_POINT('Ctrl Pts',(-0.138149907699033,6.76789880935937,
34.8091998755567));
#56905=CARTESIAN_POINT('Ctrl Pts',(-0.314914799295381,6.76197619512784,
34.8175025331745));
#56906=CARTESIAN_POINT('Ctrl Pts',(-0.491096662607798,6.74915647084697,
34.8258051907924));
#56907=CARTESIAN_POINT('Ctrl Pts',(-0.667358736770107,6.73633091009143,
34.8341116283864));
#56908=CARTESIAN_POINT('Ctrl Pts',(-0.843036906908127,6.71660200630864,
34.8424180659803));
#56909=CARTESIAN_POINT('Ctrl Pts',(-1.01756499031653,6.69005609023438,34.8507245035742));
#56910=CARTESIAN_POINT('Ctrl Pts',(-1.19230029145033,6.66347865611306,34.8590408034269));
#56911=CARTESIAN_POINT('Ctrl Pts',(-1.36588243360027,6.63006809193622,34.8673571032795));
#56912=CARTESIAN_POINT('Ctrl Pts',(-1.53775512353514,6.58996192553807,34.8756734031321));
#56913=CARTESIAN_POINT('Ctrl Pts',(-1.70973991161785,6.54982960124961,34.88399512701));
#56914=CARTESIAN_POINT('Ctrl Pts',(-1.88001268926494,6.50299305821419,34.8923168508878));
#56915=CARTESIAN_POINT('Ctrl Pts',(-2.04803300333657,6.44963951064276,34.9006385747657));
#56916=CARTESIAN_POINT('Ctrl Pts',(-2.21629673150151,6.39620866881391,34.9089723544767));
#56917=CARTESIAN_POINT('Ctrl Pts',(-2.38230114892681,6.33624207514864,34.9173061341877));
#56918=CARTESIAN_POINT('Ctrl Pts',(-2.54552526514105,6.26997528898867,34.9256399138987));
#56919=CARTESIAN_POINT('Ctrl Pts',(-2.64419250444711,6.22991772274334,34.9306775949482));
#56920=CARTESIAN_POINT('Ctrl Pts',(-2.74184424504694,6.18755892995849,34.9357152759977));
#56921=CARTESIAN_POINT('Ctrl Pts',(-2.83836998641614,6.14295896292756,34.9407529570472));
#56922=CARTESIAN_POINT('Ctrl Pts',(-2.9930243084011,6.07150053573624,34.9488243702892));
#56923=CARTESIAN_POINT('Ctrl Pts',(-3.14526281607396,5.99406642673338,34.9568957835312));
#56924=CARTESIAN_POINT('Ctrl Pts',(-3.29457816194719,5.91084120365458,34.9649671967732));
#56925=CARTESIAN_POINT('Ctrl Pts',(-3.44370605477106,5.82772046295003,34.9730284770245));
#56926=CARTESIAN_POINT('Ctrl Pts',(-3.58991776608896,5.73882325340684,34.9810897572757));
#56927=CARTESIAN_POINT('Ctrl Pts',(-3.73272482197509,5.64438255289372,34.989151037527));
#56928=CARTESIAN_POINT('Ctrl Pts',(-3.87538391367902,5.55003970357521,34.9972039653846));
#56929=CARTESIAN_POINT('Ctrl Pts',(-4.01464506153743,5.45016499736433,35.0052568932422));
#56930=CARTESIAN_POINT('Ctrl Pts',(-4.15004345744367,5.3450377268387,35.0133098210999));
#56931=CARTESIAN_POINT('Ctrl Pts',(-4.28533121451376,5.239996359538,35.0213561686242));
#56932=CARTESIAN_POINT('Ctrl Pts',(-4.41676220883512,5.12971119814665,35.0294025161487));
#56933=CARTESIAN_POINT('Ctrl Pts',(-4.54389985272087,5.01450527255115,35.037448863673));
#56934=CARTESIAN_POINT('Ctrl Pts',(-4.67096141906987,4.8993682847051,35.0454903963662));
#56935=CARTESIAN_POINT('Ctrl Pts',(-4.79373447361304,4.77931664415647,35.0535319290593));
#56936=CARTESIAN_POINT('Ctrl Pts',(-4.91181491694693,4.65471408591953,35.0615734617525));
#56937=CARTESIAN_POINT('Ctrl Pts',(-5.03216542580734,4.52771607620914,35.0697695908007));
#56938=CARTESIAN_POINT('Ctrl Pts',(-5.14764074695656,4.39599063152631,35.077965719849));
#56939=CARTESIAN_POINT('Ctrl Pts',(-5.25785154387946,4.25996316210885,35.0861618488972));
#56940=CARTESIAN_POINT('Ctrl Pts',(-5.3659462056352,4.12654752855294,35.0942006057333));
#56941=CARTESIAN_POINT('Ctrl Pts',(-5.46897645068472,3.98899389220856,35.1022393625694));
#56942=CARTESIAN_POINT('Ctrl Pts',(-5.56661521527149,3.8477375228968,35.1102781194055));
#56943=CARTESIAN_POINT('Ctrl Pts',(-5.66426343025872,3.70646748146143,35.1183176543083));
#56944=CARTESIAN_POINT('Ctrl Pts',(-5.75651891325343,3.56149430062665,35.1263571892111));
#56945=CARTESIAN_POINT('Ctrl Pts',(-5.84309779477765,3.4132824613068,35.1343967241139));
#56946=CARTESIAN_POINT('Ctrl Pts',(-5.92970219887138,3.26502693065132,35.1424386289894));
#56947=CARTESIAN_POINT('Ctrl Pts',(-6.01062648235128,3.11353116346445,35.1504805338649));
#56948=CARTESIAN_POINT('Ctrl Pts',(-6.08563269032308,2.95928433214369,35.1585224387404));
#56949=CARTESIAN_POINT('Ctrl Pts',(-6.16316902887444,2.79983440316903,35.1668356154213));
#56950=CARTESIAN_POINT('Ctrl Pts',(-6.23438085666861,2.63744495680056,35.1751487921021));
#56951=CARTESIAN_POINT('Ctrl Pts',(-6.29905972437611,2.47267781741632,35.1834619687829));
#56952=CARTESIAN_POINT('Ctrl Pts',(-6.36173665468294,2.31301054311053,35.1915178363935));
#56953=CARTESIAN_POINT('Ctrl Pts',(-6.41827896296015,2.15111094331454,35.199573704004));
#56954=CARTESIAN_POINT('Ctrl Pts',(-6.46854819473955,1.98750427731154,35.2076295716145));
#56955=CARTESIAN_POINT('Ctrl Pts',(-6.52122586902032,1.81605907401727,35.2160714028305));
#56956=CARTESIAN_POINT('Ctrl Pts',(-6.56701445761997,1.64273967608754,35.2245132340464));
#56957=CARTESIAN_POINT('Ctrl Pts',(-6.60581523590073,1.46816009656367,35.2329550652623));
#56958=CARTESIAN_POINT('Ctrl Pts',(-6.64461601418148,1.2935805170398,35.2413968964783));
#56959=CARTESIAN_POINT('Ctrl Pts',(-6.67642898426788,1.11774122489512,35.2498387276942));
#56960=CARTESIAN_POINT('Ctrl Pts',(-6.70121782300071,0.941259097537779,
35.2582805589102));
#56961=CARTESIAN_POINT('Ctrl Pts',(-6.74481367139252,0.630881989878215,
35.2731271113367));
#56962=CARTESIAN_POINT('Ctrl Pts',(-6.76683634641136,0.317566188239821,
35.2879736637632));
#56963=CARTESIAN_POINT('Ctrl Pts',(-6.76699909143182,0.00350664525299999,
35.3028202161897));
#56964=CARTESIAN_POINT('Ctrl Pts',(-6.76699909143212,0.00350664467849019,
35.3028202162169));
#56965=CARTESIAN_POINT('Ctrl Pts',(-6.76708746338061,-0.167030421380243,
35.3108820234392));
#56966=CARTESIAN_POINT('Ctrl Pts',(-6.7607250453901,-0.337839588124926,
35.3189438306615));
#56967=CARTESIAN_POINT('Ctrl Pts',(-6.74787647786183,-0.508381785195997,
35.3270056378839));
#56968=CARTESIAN_POINT('Ctrl Pts',(-6.73504143045245,-0.678744526403567,
35.3350589619355));
#56969=CARTESIAN_POINT('Ctrl Pts',(-6.71573384360594,-0.848840487435429,
35.3431122859871));
#56970=CARTESIAN_POINT('Ctrl Pts',(-6.68997033672216,-1.01812862339572,
35.3511656100387));
#56971=CARTESIAN_POINT('Ctrl Pts',(-6.66422827530273,-1.18727584442923,
35.359212230528));
#56972=CARTESIAN_POINT('Ctrl Pts',(-6.63204104580464,-1.35561621114065,
35.3672588510172));
#56973=CARTESIAN_POINT('Ctrl Pts',(-6.5934772201377,-1.52261194909446,35.3753054715065));
#56974=CARTESIAN_POINT('Ctrl Pts',(-6.55343892722467,-1.6959926797608,35.383659750226));
#56975=CARTESIAN_POINT('Ctrl Pts',(-6.50652679565116,-1.86792351633893,
35.3920140289454));
#56976=CARTESIAN_POINT('Ctrl Pts',(-6.45287643485501,-2.03781125634661,
35.4003683076649));
#56977=CARTESIAN_POINT('Ctrl Pts',(-6.40124942677632,-2.20129190392644,
35.4084075157623));
#56978=CARTESIAN_POINT('Ctrl Pts',(-6.34338328244956,-2.36288035711749,
35.4164467238596));
#56979=CARTESIAN_POINT('Ctrl Pts',(-6.27945022569185,-2.52206143126186,
35.424485931957));
#56980=CARTESIAN_POINT('Ctrl Pts',(-6.21552446196669,-2.68122434715111,
35.4325242229982));
#56981=CARTESIAN_POINT('Ctrl Pts',(-6.1455333021718,-2.83798008325793,35.4405625140394));
#56982=CARTESIAN_POINT('Ctrl Pts',(-6.06969761707096,-2.99183218735997,
35.4486008050806));
#56983=CARTESIAN_POINT('Ctrl Pts',(-5.99385551476963,-3.14569731039626,
35.4566397763204));
#56984=CARTESIAN_POINT('Ctrl Pts',(-5.91216806867525,-3.29665797700334,
35.4646787475601));
#56985=CARTESIAN_POINT('Ctrl Pts',(-5.82490265043725,-3.44424129714065,
35.4727177187999));
#56986=CARTESIAN_POINT('Ctrl Pts',(-5.73761250544533,-3.59186643517689,
35.4807589678912));
#56987=CARTESIAN_POINT('Ctrl Pts',(-5.64474143370571,-3.73611200072254,
35.4888002169825));
#56988=CARTESIAN_POINT('Ctrl Pts',(-5.54660067049607,-3.87653324531759,
35.4968414660737));
#56989=CARTESIAN_POINT('Ctrl Pts',(-5.44836692289814,-4.01708753334031,
35.504890333922));
#56990=CARTESIAN_POINT('Ctrl Pts',(-5.34485373119514,-4.15380996054235,
35.5129392017703));
#56991=CARTESIAN_POINT('Ctrl Pts',(-5.2364135956204,-4.2862876309928,35.5209880696185));
#56992=CARTESIAN_POINT('Ctrl Pts',(-5.12791246737458,-4.41883981414038,
35.5290414645909));
#56993=CARTESIAN_POINT('Ctrl Pts',(-5.01447912353585,-4.54714220666268,
35.5370948595632));
#56994=CARTESIAN_POINT('Ctrl Pts',(-4.89650322992137,-4.67081846354251,
35.5451482545356));
#56995=CARTESIAN_POINT('Ctrl Pts',(-4.77838336477845,-4.79464564837203,
35.5532114774444));
#56996=CARTESIAN_POINT('Ctrl Pts',(-4.65571015313716,-4.91383517099587,
35.5612747003532));
#56997=CARTESIAN_POINT('Ctrl Pts',(-4.52890706630093,-5.0280502965672,35.569337923262));
#56998=CARTESIAN_POINT('Ctrl Pts',(-4.49498985568179,-5.05860048715442,
35.5714946690991));
#56999=CARTESIAN_POINT('Ctrl Pts',(-4.46077733722195,-5.08879502042966,
35.5736514149362));
#57000=CARTESIAN_POINT('Ctrl Pts',(-4.42627796346472,-5.11862797926813,
35.5758081607733));
#57001=CARTESIAN_POINT('Ctrl Pts',(-4.28335043668362,-5.24222300604602,
35.5847433475556));
#57002=CARTESIAN_POINT('Ctrl Pts',(-4.13515258213284,-5.3599068105399,35.5936785343379));
#57003=CARTESIAN_POINT('Ctrl Pts',(-3.98217594772205,-5.47124882649145,
35.6026137211202));
#57004=CARTESIAN_POINT('Ctrl Pts',(-3.82942842498542,-5.58242408654738,
35.6115355257568));
#57005=CARTESIAN_POINT('Ctrl Pts',(-3.67191661173363,-5.68727635826303,
35.6204573303934));
#57006=CARTESIAN_POINT('Ctrl Pts',(-3.51016469527428,-5.78541552630838,
35.6293791350301));
#57007=CARTESIAN_POINT('Ctrl Pts',(-3.34880733009906,-5.88331530964891,
35.6382791772694));
#57008=CARTESIAN_POINT('Ctrl Pts',(-3.18323072427315,-5.97453453697728,
35.6471792195087));
#57009=CARTESIAN_POINT('Ctrl Pts',(-3.01398702545083,-6.05872686382329,
35.656079261748));
#57010=CARTESIAN_POINT('Ctrl Pts',(-2.84500387979123,-6.14278957534426,
35.6649656022415));
#57011=CARTESIAN_POINT('Ctrl Pts',(-2.67236513267249,-6.21984685103397,
35.6738519427349));
#57012=CARTESIAN_POINT('Ctrl Pts',(-2.49664903924339,-6.28959717111081,
35.6827382832283));
#57013=CARTESIAN_POINT('Ctrl Pts',(-2.32138222119325,-6.35916915179441,
35.6916019029003));
#57014=CARTESIAN_POINT('Ctrl Pts',(-2.14305399679716,-6.42147136183039,
35.7004655225722));
#57015=CARTESIAN_POINT('Ctrl Pts',(-1.96226348141899,-6.47624976583589,
35.7093291422441));
#57016=CARTESIAN_POINT('Ctrl Pts',(-1.79063824971273,-6.52825114577708,
35.7177434153976));
#57017=CARTESIAN_POINT('Ctrl Pts',(-1.61679440425823,-6.57347246625104,
35.7261576885511));
#57018=CARTESIAN_POINT('Ctrl Pts',(-1.44126284911579,-6.61173580837579,
35.7345719617046));
#57019=CARTESIAN_POINT('Ctrl Pts',(-1.26998749245017,-6.64907136074594,
35.7427822099092));
#57020=CARTESIAN_POINT('Ctrl Pts',(-1.09726966871086,-6.67974539469198,
35.7509924581137));
#57021=CARTESIAN_POINT('Ctrl Pts',(-0.923666389551918,-6.70366537058736,
35.7592027063182));
#57022=CARTESIAN_POINT('Ctrl Pts',(-0.750021841432833,-6.72759103273784,
35.7674149062624));
#57023=CARTESIAN_POINT('Ctrl Pts',(-0.575491771160288,-6.74475938948673,
35.7756271062066));
#57024=CARTESIAN_POINT('Ctrl Pts',(-0.400639097955959,-6.75512970365404,
35.7838393061508));
#57025=CARTESIAN_POINT('Ctrl Pts',(-0.225713722424808,-6.76550432971406,
35.7920549206613));
#57026=CARTESIAN_POINT('Ctrl Pts',(-0.0504658317656606,-6.76907526098659,
35.8002705351718));
#57027=CARTESIAN_POINT('Ctrl Pts',(0.124540773021885,-6.76585387041836,
35.8084861496823));
#57028=CARTESIAN_POINT('Ctrl Pts',(0.299743902554118,-6.76262886236976,
35.8167109899677));
#57029=CARTESIAN_POINT('Ctrl Pts',(0.474704849010942,-6.75259630448826,
35.8249358302531));
#57030=CARTESIAN_POINT('Ctrl Pts',(0.648863073961833,-6.73581960204167,
35.8331606705385));
#57031=CARTESIAN_POINT('Ctrl Pts',(0.823132853310406,-6.71903215353392,
35.8413907791201));
#57032=CARTESIAN_POINT('Ctrl Pts',(0.996598534377933,-6.69549199677668,
35.8496208877016));
#57033=CARTESIAN_POINT('Ctrl Pts',(1.16870895120514,-6.66531382512279,35.8578509962831));
#57034=CARTESIAN_POINT('Ctrl Pts',(1.34105533405454,-6.63509427873253,35.8660923884698));
#57035=CARTESIAN_POINT('Ctrl Pts',(1.51204239440781,-6.59821861433577,35.8743337806565));
#57036=CARTESIAN_POINT('Ctrl Pts',(1.6811323426534,-6.55485187067448,35.8825751728432));
#57037=CARTESIAN_POINT('Ctrl Pts',(1.75472458411031,-6.53597756203677,35.8861620361076));
#57038=CARTESIAN_POINT('Ctrl Pts',(1.82795770277806,-6.51587433314231,35.889748899372));
#57039=CARTESIAN_POINT('Ctrl Pts',(1.90078853251695,-6.49455864202119,35.8933357626364));
#57040=CARTESIAN_POINT('Ctrl Pts',(2.07233420990709,-6.44435168041547,35.9017842574648));
#57041=CARTESIAN_POINT('Ctrl Pts',(2.24203792725608,-6.38730035969397,35.9102327522933));
#57042=CARTESIAN_POINT('Ctrl Pts',(2.40933404653316,-6.32355900203486,35.9186812471217));
#57043=CARTESIAN_POINT('Ctrl Pts',(2.57647735052358,-6.25987586840322,35.9271220247409));
#57044=CARTESIAN_POINT('Ctrl Pts',(2.74121713001409,-6.18951499698267,35.9355628023601));
#57045=CARTESIAN_POINT('Ctrl Pts',(2.9030031012906,-6.11268042628577,35.9440035799792));
#57046=CARTESIAN_POINT('Ctrl Pts',(3.06466616968524,-6.03590422400049,35.9524379454486));
#57047=CARTESIAN_POINT('Ctrl Pts',(3.22337960295659,-5.95266426873485,35.9608723109179));
#57048=CARTESIAN_POINT('Ctrl Pts',(3.37861292937405,-5.86321274332311,35.9693066763872));
#57049=CARTESIAN_POINT('Ctrl Pts',(3.53375216953899,-5.7738154340968,35.9777359298238));
#57050=CARTESIAN_POINT('Ctrl Pts',(3.68541522000411,-5.67821422683876,35.9861651832604));
#57051=CARTESIAN_POINT('Ctrl Pts',(3.83309571509002,-5.57670747295916,35.994594436697));
#57052=CARTESIAN_POINT('Ctrl Pts',(3.98070935542008,-5.47524667104664,36.0030198742223));
#57053=CARTESIAN_POINT('Ctrl Pts',(4.12434376104425,-5.36788584193663,36.0114453117475));
#57054=CARTESIAN_POINT('Ctrl Pts',(4.2635207662896,-5.25496714313395,36.0198707492728));
#57055=CARTESIAN_POINT('Ctrl Pts',(4.40266719808954,-5.14207324953286,36.0282943359559));
#57056=CARTESIAN_POINT('Ctrl Pts',(4.53735792143644,-5.02362412834757,36.0367179226392));
#57057=CARTESIAN_POINT('Ctrl Pts',(4.66714672430506,-4.9000031075305,36.0451415093223));
#57058=CARTESIAN_POINT('Ctrl Pts',(4.79692100448706,-4.77639591925757,36.0535641534504));
#57059=CARTESIAN_POINT('Ctrl Pts',(4.92179421629,-4.64761821494519,36.0619867975784));
#57060=CARTESIAN_POINT('Ctrl Pts',(5.04135576816381,-4.51409138352354,36.0704094417064));
#57061=CARTESIAN_POINT('Ctrl Pts',(5.16092061410174,-4.38056087327758,36.0788323178883));
#57062=CARTESIAN_POINT('Ctrl Pts',(5.27517328622964,-4.24228122369439,36.0872551940703));
#57063=CARTESIAN_POINT('Ctrl Pts',(5.38374213261956,-4.09970848347257,36.0956780702522));
#57064=CARTESIAN_POINT('Ctrl Pts',(5.49232911060918,-3.95711193281213,36.1041023531012));
#57065=CARTESIAN_POINT('Ctrl Pts',(5.5952301688979,-3.81022112766847,36.1125266359502));
#57066=CARTESIAN_POINT('Ctrl Pts',(5.69211558349487,-3.65952308151415,36.1209509187992));
#57067=CARTESIAN_POINT('Ctrl Pts',(5.78906643091869,-3.50872325947127,36.1293808910974));
#57068=CARTESIAN_POINT('Ctrl Pts',(5.8799933358985,-3.35411133916849,36.1378108633956));
#57069=CARTESIAN_POINT('Ctrl Pts',(5.96461082667901,-3.19620191575306,36.1462408356937));
#57070=CARTESIAN_POINT('Ctrl Pts',(6.04925856684666,-3.03823604226759,36.1546738215709));
#57071=CARTESIAN_POINT('Ctrl Pts',(6.12759224339033,-2.87697061193304,36.1631068074481));
#57072=CARTESIAN_POINT('Ctrl Pts',(6.19937332638077,-2.71294293345043,36.1715397933253));
#57073=CARTESIAN_POINT('Ctrl Pts',(6.27122044753022,-2.54876435050299,36.1799805374981));
#57074=CARTESIAN_POINT('Ctrl Pts',(6.33650280265216,-2.3818187501014,36.1884212816709));
#57075=CARTESIAN_POINT('Ctrl Pts',(6.39503039802752,-2.21266247048754,36.1968620258438));
#57076=CARTESIAN_POINT('Ctrl Pts',(6.42739186864194,-2.11913144573141,36.2015291387289));
#57077=CARTESIAN_POINT('Ctrl Pts',(6.45768910090555,-2.02492483767073,36.2061962516141));
#57078=CARTESIAN_POINT('Ctrl Pts',(6.48589658976253,-1.9301384476008,36.2108633644992));
#57079=CARTESIAN_POINT('Ctrl Pts',(6.53510206876611,-1.76479194156975,36.219004731717));
#57080=CARTESIAN_POINT('Ctrl Pts',(6.57804329603186,-1.59735186879326,36.2271460989349));
#57081=CARTESIAN_POINT('Ctrl Pts',(6.61453994949666,-1.42833828504062,36.2352874661527));
#57082=CARTESIAN_POINT('Ctrl Pts',(6.65100474415887,-1.25947223729159,36.2434217265761));
#57083=CARTESIAN_POINT('Ctrl Pts',(6.68103608615913,-1.08903576801106,36.2515559869996));
#57084=CARTESIAN_POINT('Ctrl Pts',(6.70450328506581,-0.91756454843337,36.2596902474231));
#57085=CARTESIAN_POINT('Ctrl Pts',(6.72795447549683,-0.746210300329624,
36.2678189589478));
#57086=CARTESIAN_POINT('Ctrl Pts',(6.74485038860386,-0.573823068480533,
36.2759476704725));
#57087=CARTESIAN_POINT('Ctrl Pts',(6.75511130774931,-0.400949148792437,
36.2840763819973));
#57088=CARTESIAN_POINT('Ctrl Pts',(6.76536733365211,-0.228157669480848,
36.2922012170898));
#57089=CARTESIAN_POINT('Ctrl Pts',(6.76899464479822,-0.054880329140094,
36.3003260521822));
#57090=CARTESIAN_POINT('Ctrl Pts',(6.76596532412493,0.118331030330624,36.3084508872747));
#57091=CARTESIAN_POINT('Ctrl Pts',(6.76293685151845,0.291493898795741,36.3165734477968));
#57092=CARTESIAN_POINT('Ctrl Pts',(6.75325546613401,0.464590457522918,36.324696008319));
#57093=CARTESIAN_POINT('Ctrl Pts',(6.73694535866609,0.637068469120464,36.3328185688411));
#57094=CARTESIAN_POINT('Ctrl Pts',(6.72063438435824,0.80955564747711,36.3409415610562));
#57095=CARTESIAN_POINT('Ctrl Pts',(6.697694014737,0.981423848227725,36.3490645532714));
#57096=CARTESIAN_POINT('Ctrl Pts',(6.66820036674673,1.15212537031294,36.3571875454865));
#57097=CARTESIAN_POINT('Ctrl Pts',(6.65314475825274,1.23926329528894,36.361334085468));
#57098=CARTESIAN_POINT('Ctrl Pts',(6.63638233341226,1.32609731651731,36.3654806254495));
#57099=CARTESIAN_POINT('Ctrl Pts',(6.61792837136154,1.41255551095451,36.369627165431));
#57100=CARTESIAN_POINT('Ctrl Pts',(6.5779470607922,1.59987094563239,36.3786108244594));
#57101=CARTESIAN_POINT('Ctrl Pts',(6.53004276773826,1.78532894167697,36.3875944834879));
#57102=CARTESIAN_POINT('Ctrl Pts',(6.4744203895597,1.96829104028181,36.3965781425163));
#57103=CARTESIAN_POINT('Ctrl Pts',(6.41870245272483,2.15156746583332,36.4055772353757));
#57104=CARTESIAN_POINT('Ctrl Pts',(6.35523999814356,2.33233919474975,36.4145763282352));
#57105=CARTESIAN_POINT('Ctrl Pts',(6.28428689503124,2.50998550213713,36.4235754210947));
#57106=CARTESIAN_POINT('Ctrl Pts',(6.21316742671953,2.68804834047318,36.4325956143121));
#57107=CARTESIAN_POINT('Ctrl Pts',(6.13452225753113,2.86297087179123,36.4416158075296));
#57108=CARTESIAN_POINT('Ctrl Pts',(6.04865345865544,3.03415232595458,36.4506360007471));
#57109=CARTESIAN_POINT('Ctrl Pts',(5.96269769611887,3.20550714420504,36.4596653291689));
#57110=CARTESIAN_POINT('Ctrl Pts',(5.86950380139162,3.37311310539593,36.4686946575907));
#57111=CARTESIAN_POINT('Ctrl Pts',(5.76941930559148,3.53639503962275,36.4777239860125));
#57112=CARTESIAN_POINT('Ctrl Pts',(5.66919371082616,3.6999071684643,36.4867660439674));
#57113=CARTESIAN_POINT('Ctrl Pts',(5.56205821605885,3.8590828773121,36.4958081019222));
#57114=CARTESIAN_POINT('Ctrl Pts',(5.44840437058529,4.01337499052694,36.504850159877));
#57115=CARTESIAN_POINT('Ctrl Pts',(5.34977257695484,4.14727374077163,36.5126970953721));
#57116=CARTESIAN_POINT('Ctrl Pts',(5.24623239078634,4.27749494957618,36.5205440308672));
#57117=CARTESIAN_POINT('Ctrl Pts',(5.13806432240161,4.40370117274819,36.5283909663623));
#57118=CARTESIAN_POINT('Ctrl Pts',(5.01876243282036,4.54289789804959,36.5370455928705));
#57119=CARTESIAN_POINT('Ctrl Pts',(4.89372473713899,4.67733240286398,36.5457002193786));
#57120=CARTESIAN_POINT('Ctrl Pts',(4.76334973590017,4.80653599731654,36.5543548458869));
#57121=CARTESIAN_POINT('Ctrl Pts',(4.6331375630723,4.93557822635569,36.5629986634281));
#57122=CARTESIAN_POINT('Ctrl Pts',(4.49760160300558,5.05940236966045,36.5716424809694));
#57123=CARTESIAN_POINT('Ctrl Pts',(4.35717837145664,5.17757526640709,36.5802862985107));
#57124=CARTESIAN_POINT('Ctrl Pts',(4.21686407093436,5.29565649246061,36.5889234107517));
#57125=CARTESIAN_POINT('Ctrl Pts',(4.07167029085023,5.40809501883335,36.5975605229928));
#57126=CARTESIAN_POINT('Ctrl Pts',(3.92206895355486,5.51449581771182,36.6061976352339));
#57127=CARTESIAN_POINT('Ctrl Pts',(3.7726101150563,5.62079526732366,36.6148265204221));
#57128=CARTESIAN_POINT('Ctrl Pts',(3.61875234417994,5.72106829015106,36.6234554056104));
#57129=CARTESIAN_POINT('Ctrl Pts',(3.46099924771643,5.81496115269108,36.6320842907986));
#57130=CARTESIAN_POINT('Ctrl Pts',(3.34248430827023,5.88549990703454,36.6385669008298));
#57131=CARTESIAN_POINT('Ctrl Pts',(3.2217715316867,5.95243847868828,36.6450495108609));
#57132=CARTESIAN_POINT('Ctrl Pts',(3.09908550384717,6.01564277861014,36.651532120892));
#57133=CARTESIAN_POINT('Origin',(0.,0.,-63.6971797838103));
#57134=CARTESIAN_POINT('',(3.09908550384713,6.01564277861016,39.0456530966623));
#57135=CARTESIAN_POINT('',(3.09908550384735,6.01564277861005,38.6513967904261));
#57136=CARTESIAN_POINT('',(3.09908550384721,6.01564277861012,-63.6971797838103));
#57137=CARTESIAN_POINT('',(-6.76700535807815,-1.06911827047406E-5,37.6971705070289));
#57138=CARTESIAN_POINT('Ctrl Pts',(-6.76699974905361,-0.00184290760892239,
37.6971797838099));
#57139=CARTESIAN_POINT('Ctrl Pts',(-6.76693552975974,-0.237650684080379,
37.7082773287428));
#57140=CARTESIAN_POINT('Ctrl Pts',(-6.75454167359002,-0.473079103425044,
37.7193748736757));
#57141=CARTESIAN_POINT('Ctrl Pts',(-6.72996025036087,-0.707053059227286,
37.7304724186087));
#57142=CARTESIAN_POINT('Ctrl Pts',(-6.70499092345331,-0.944719208002343,
37.7417450867825));
#57143=CARTESIAN_POINT('Ctrl Pts',(-6.66744627003892,-1.18088516299746,
37.7530177549562));
#57144=CARTESIAN_POINT('Ctrl Pts',(-6.61752558591685,-1.4144412747569,37.76429042313));
#57145=CARTESIAN_POINT('Ctrl Pts',(-6.6045686968806,-1.47506064881043,37.7672162386159));
#57146=CARTESIAN_POINT('Ctrl Pts',(-6.59077834990439,-1.53550427290328,
37.7701420541018));
#57147=CARTESIAN_POINT('Ctrl Pts',(-6.57615859055703,-1.59575286051536,
37.7730678695877));
#57148=CARTESIAN_POINT('Ctrl Pts',(-6.53547768294063,-1.76340043722524,
37.7812092368056));
#57149=CARTESIAN_POINT('Ctrl Pts',(-6.48832991777303,-1.92970502288278,
37.7893506040235));
#57150=CARTESIAN_POINT('Ctrl Pts',(-6.4348211596328,-2.09412646312059,37.7974919712414));
#57151=CARTESIAN_POINT('Ctrl Pts',(-6.38135911056881,-2.25840437594618,
37.8056262316649));
#57152=CARTESIAN_POINT('Ctrl Pts',(-6.32154723368755,-2.42080206973341,
37.8137604920884));
#57153=CARTESIAN_POINT('Ctrl Pts',(-6.25554214140539,-2.58079087046999,
37.8218947525119));
#57154=CARTESIAN_POINT('Ctrl Pts',(-6.18958207541336,-2.74067053262482,
37.8300234640367));
#57155=CARTESIAN_POINT('Ctrl Pts',(-6.11743734447345,-2.89814423640583,
37.8381521755615));
#57156=CARTESIAN_POINT('Ctrl Pts',(-6.03931395731611,-3.05269977642199,
37.8462808870864));
#57157=CARTESIAN_POINT('Ctrl Pts',(-5.96122782575807,-3.20718161175793,
37.8544057221789));
#57158=CARTESIAN_POINT('Ctrl Pts',(-5.87716888032726,-3.35874772853615,
37.8625305572714));
#57159=CARTESIAN_POINT('Ctrl Pts',(-5.7873906840792,-3.50690719435706,37.870655392364));
#57160=CARTESIAN_POINT('Ctrl Pts',(-5.6976376214887,-3.65502518252044,37.8787779528862));
#57161=CARTESIAN_POINT('Ctrl Pts',(-5.60216868744704,-3.79973810695931,
37.8869005134084));
#57162=CARTESIAN_POINT('Ctrl Pts',(-5.50128267391272,-3.94058091424447,
37.8950230739306));
#57163=CARTESIAN_POINT('Ctrl Pts',(-5.40039129854866,-4.08143120695922,
37.9031460661458));
#57164=CARTESIAN_POINT('Ctrl Pts',(-5.29408247852451,-4.21841067174524,
37.911269058361));
#57165=CARTESIAN_POINT('Ctrl Pts',(-5.18269759614329,-4.35108430473722,
37.9193920505762));
#57166=CARTESIAN_POINT('Ctrl Pts',(-5.12583900809701,-4.41881015120421,
37.9235385905571));
#57167=CARTESIAN_POINT('Ctrl Pts',(-5.06765836793178,-4.48541449969006,
37.9276851305381));
#57168=CARTESIAN_POINT('Ctrl Pts',(-5.00820507123816,-4.55084288505156,
37.931831670519));
#57169=CARTESIAN_POINT('Ctrl Pts',(-4.87939692081389,-4.69259632468153,
37.9408153295474));
#57170=CARTESIAN_POINT('Ctrl Pts',(-4.74467664467028,-4.82875776116382,
37.9497989885758));
#57171=CARTESIAN_POINT('Ctrl Pts',(-4.60454258261437,-4.95887856323292,
37.9587826476041));
#57172=CARTESIAN_POINT('Ctrl Pts',(-4.46416777172448,-5.08922291146144,
37.9677817404635));
#57173=CARTESIAN_POINT('Ctrl Pts',(-4.31836076045437,-5.21350572033224,
37.9767808333229));
#57174=CARTESIAN_POINT('Ctrl Pts',(-4.16765328480797,-5.33131832642072,
37.9857799261823));
#57175=CARTESIAN_POINT('Ctrl Pts',(-4.01659244224615,-5.44940717014791,
37.9948001193997));
#57176=CARTESIAN_POINT('Ctrl Pts',(-3.8606083345819,-5.56099530909942,38.003820312617));
#57177=CARTESIAN_POINT('Ctrl Pts',(-3.70026431117455,-5.6657155794699,38.0128405058344));
#57178=CARTESIAN_POINT('Ctrl Pts',(-3.5397578992929,-5.77054190533639,38.021869834256));
#57179=CARTESIAN_POINT('Ctrl Pts',(-3.3748829539253,-5.86848634177909,38.0308991626777));
#57180=CARTESIAN_POINT('Ctrl Pts',(-3.20622922738068,-5.95922672345078,
38.0399284910994));
#57181=CARTESIAN_POINT('Ctrl Pts',(-3.03733773307671,-6.05009503077033,
38.0489705490541));
#57182=CARTESIAN_POINT('Ctrl Pts',(-2.86465701626704,-6.13373886238583,
38.0580126070089));
#57183=CARTESIAN_POINT('Ctrl Pts',(-2.68880078161175,-6.20988239476434,
38.0670546649636));
#57184=CARTESIAN_POINT('Ctrl Pts',(-2.53618812011712,-6.27596175302345,
38.0749016004593));
#57185=CARTESIAN_POINT('Ctrl Pts',(-2.38118432692681,-6.33639318090253,
38.082748535955));
#57186=CARTESIAN_POINT('Ctrl Pts',(-2.22420161295688,-6.39102622314445,
38.0905954714507));
#57187=CARTESIAN_POINT('Ctrl Pts',(-2.05108380003152,-6.45127459410962,
38.0992489357516));
#57188=CARTESIAN_POINT('Ctrl Pts',(-1.87540633154713,-6.50452321409249,
38.1079024000524));
#57189=CARTESIAN_POINT('Ctrl Pts',(-1.6977491900116,-6.5505676614943,38.1165558643532));
#57190=CARTESIAN_POINT('Ctrl Pts',(-1.52025570704185,-6.59656969254202,
38.1252013570434));
#57191=CARTESIAN_POINT('Ctrl Pts',(-1.34078648166763,-6.63538071170318,
38.1338468497336));
#57192=CARTESIAN_POINT('Ctrl Pts',(-1.15993705013949,-6.66684595890093,
38.1424923424238));
#57193=CARTESIAN_POINT('Ctrl Pts',(-0.973647073918563,-6.69925778404589,
38.1513979199203));
#57194=CARTESIAN_POINT('Ctrl Pts',(-0.785892855662658,-6.72387484896148,
38.1603034974169));
#57195=CARTESIAN_POINT('Ctrl Pts',(-0.597339508404085,-6.7405841372762,
38.1692090749134));
#57196=CARTESIAN_POINT('Ctrl Pts',(-0.41464013159659,-6.75677465633291,
38.1778381630859));
#57197=CARTESIAN_POINT('Ctrl Pts',(-0.231190833158081,-6.76554101372821,
38.1864672512585));
#57198=CARTESIAN_POINT('Ctrl Pts',(-0.0476050447402823,-6.76683254999821,
38.1950963394311));
#57199=CARTESIAN_POINT('Ctrl Pts',(0.144804302351395,-6.76818616049604,
38.2041401615896));
#57200=CARTESIAN_POINT('Ctrl Pts',(0.337363249713542,-6.76132866194586,
38.2131839837481));
#57201=CARTESIAN_POINT('Ctrl Pts',(0.529361336727085,-6.74626308226847,
38.2222278059066));
#57202=CARTESIAN_POINT('Ctrl Pts',(0.721359423740628,-6.73119750259109,
38.2312716280651));
#57203=CARTESIAN_POINT('Ctrl Pts',(0.912796263558366,-6.70792383739874,
38.2403154502236));
#57204=CARTESIAN_POINT('Ctrl Pts',(1.10296273536256,-6.67650823442925,38.2493592723821));
#57205=CARTESIAN_POINT('Ctrl Pts',(1.28013370354561,-6.6472394956166,38.2577850622319));
#57206=CARTESIAN_POINT('Ctrl Pts',(1.45612444654051,-6.61091662712941,38.2662108520816));
#57207=CARTESIAN_POINT('Ctrl Pts',(1.63035802345081,-6.56766486015917,38.2746366419314));
#57208=CARTESIAN_POINT('Ctrl Pts',(1.80463202841247,-6.52440305732393,38.2830643868479));
#57209=CARTESIAN_POINT('Ctrl Pts',(1.97714773261153,-6.47420923027956,38.2914921317644));
#57210=CARTESIAN_POINT('Ctrl Pts',(2.14734168613832,-6.41725896960475,38.2999198766809));
#57211=CARTESIAN_POINT('Ctrl Pts',(2.31759817740396,-6.36028778256648,38.3083507183708));
#57212=CARTESIAN_POINT('Ctrl Pts',(2.48553090271921,-6.29655531686225,38.3167815600607));
#57213=CARTESIAN_POINT('Ctrl Pts',(2.65059440674841,-6.22628607525498,38.3252124017506));
#57214=CARTESIAN_POINT('Ctrl Pts',(2.81580958306958,-6.15595226518363,38.333650990308));
#57215=CARTESIAN_POINT('Ctrl Pts',(2.97814996550125,-6.07906980880263,38.3420895788653));
#57216=CARTESIAN_POINT('Ctrl Pts',(3.13709179542038,-5.995910612001,38.3505281674226));
#57217=CARTESIAN_POINT('Ctrl Pts',(3.29611696741091,-5.91270781019166,38.3589711808028));
#57218=CARTESIAN_POINT('Ctrl Pts',(3.4517397430259,-5.82322186435422,38.3674141941831));
#57219=CARTESIAN_POINT('Ctrl Pts',(3.60346308000267,-5.72776944639514,38.3758572075634));
#57220=CARTESIAN_POINT('Ctrl Pts',(3.7553458129201,-5.63221674901792,38.3843090909176));
#57221=CARTESIAN_POINT('Ctrl Pts',(3.90332064776322,-5.53068524126354,38.3927609742719));
#57222=CARTESIAN_POINT('Ctrl Pts',(4.04692063169226,-5.42353412460764,38.4012128576262));
#57223=CARTESIAN_POINT('Ctrl Pts',(4.08605616397931,-5.39433206015927,38.4035162628554));
#57224=CARTESIAN_POINT('Ctrl Pts',(4.12486695453269,-5.36471283553297,38.4058196680846));
#57225=CARTESIAN_POINT('Ctrl Pts',(4.16334399683875,-5.33468422345566,38.4081230733138));
#57226=CARTESIAN_POINT('Ctrl Pts',(4.30227906829076,-5.2262552197038,38.4164403386472));
#57227=CARTESIAN_POINT('Ctrl Pts',(4.43710985544817,-5.11229047568035,38.4247576039807));
#57228=CARTESIAN_POINT('Ctrl Pts',(4.56737751684648,-4.99313044277889,38.4330748693141));
#57229=CARTESIAN_POINT('Ctrl Pts',(4.69753530749622,-4.87407091219607,38.4413851196742));
#57230=CARTESIAN_POINT('Ctrl Pts',(4.82313738498907,-4.7498250565862,38.4496953700342));
#57231=CARTESIAN_POINT('Ctrl Pts',(4.94375725112098,-4.62077409553732,38.4580056203943));
#57232=CARTESIAN_POINT('Ctrl Pts',(5.0642974738146,-4.49180834484874,38.4663103836242));
#57233=CARTESIAN_POINT('Ctrl Pts',(5.1798618035169,-4.35804406405578,38.4746151468541));
#57234=CARTESIAN_POINT('Ctrl Pts',(5.29005979439378,-4.21990004286102,38.482919910084));
#57235=CARTESIAN_POINT('Ctrl Pts',(5.4002051956809,-4.08182194789,38.4912207100466));
#57236=CARTESIAN_POINT('Ctrl Pts',(5.50498914544803,-3.93936854931038,38.4995215100092));
#57237=CARTESIAN_POINT('Ctrl Pts',(5.60406063640611,-3.7929926685249,38.5078223099718));
#57238=CARTESIAN_POINT('Ctrl Pts',(5.70310297716192,-3.64665985650209,38.5161206675567));
#57239=CARTESIAN_POINT('Ctrl Pts',(5.79643601471079,-3.49640715050521,38.5244190251416));
#57240=CARTESIAN_POINT('Ctrl Pts',(5.88375121247998,-3.34271755756306,38.5327173827266));
#57241=CARTESIAN_POINT('Ctrl Pts',(5.97107529437035,-3.18901232705722,38.5410165846503));
#57242=CARTESIAN_POINT('Ctrl Pts',(6.05238013469612,-3.03186980957788,38.5493157865741));
#57243=CARTESIAN_POINT('Ctrl Pts',(6.12740215452806,-2.87179940745953,38.5576149884979));
#57244=CARTESIAN_POINT('Ctrl Pts',(6.20243178017074,-2.71171277723661,38.5659150318034));
#57245=CARTESIAN_POINT('Ctrl Pts',(6.271177167546,-2.54869798562367,38.574215075109));
#57246=CARTESIAN_POINT('Ctrl Pts',(6.33342212535606,-2.38328621488279,38.5825151184145));
#57247=CARTESIAN_POINT('Ctrl Pts',(6.39568372642389,-2.21783021580864,38.5908173810124));
#57248=CARTESIAN_POINT('Ctrl Pts',(6.45144131116843,-2.04997628585027,38.5991196436104));
#57249=CARTESIAN_POINT('Ctrl Pts',(6.50052791371773,-1.88027281078482,38.6074219062083));
#57250=CARTESIAN_POINT('Ctrl Pts',(6.54963579066124,-1.71049578533208,38.6157277670509));
#57251=CARTESIAN_POINT('Ctrl Pts',(6.59206682652152,-1.53886795115879,38.6240336278935));
#57252=CARTESIAN_POINT('Ctrl Pts',(6.62770466654014,-1.36595016494823,38.6323394887361));
#57253=CARTESIAN_POINT('Ctrl Pts',(6.663384633,-1.19282797771456,38.6406551676923));
#57254=CARTESIAN_POINT('Ctrl Pts',(6.69225528955528,-1.01841313301012,38.6489708466484));
#57255=CARTESIAN_POINT('Ctrl Pts',(6.71425171482333,-0.84327510931606,38.6572865256045));
#57256=CARTESIAN_POINT('Ctrl Pts',(6.7362620526552,-0.66802631221671,38.6656074641614));
#57257=CARTESIAN_POINT('Ctrl Pts',(6.75138945862924,-0.492053770065858,
38.6739284027182));
#57258=CARTESIAN_POINT('Ctrl Pts',(6.75962111215635,-0.31592945429344,38.682249341275));
#57259=CARTESIAN_POINT('Ctrl Pts',(6.76786500047033,-0.13954336323383,38.690582647324));
#57260=CARTESIAN_POINT('Ctrl Pts',(6.76919265107294,0.0369946045765517,
38.6989159533729));
#57261=CARTESIAN_POINT('Ctrl Pts',(6.76364336208099,0.213113750325444,38.7072492594219));
#57262=CARTESIAN_POINT('Ctrl Pts',(6.7595587577521,0.342747839696261,38.7133830646735));
#57263=CARTESIAN_POINT('Ctrl Pts',(6.75174943541119,0.472155075365261,38.719516869925));
#57264=CARTESIAN_POINT('Ctrl Pts',(6.7402488642125,0.601110845420475,38.7256506751766));
#57265=CARTESIAN_POINT('Ctrl Pts',(6.72511537711008,0.770802458923698,38.7337220884187));
#57266=CARTESIAN_POINT('Ctrl Pts',(6.70354158783764,0.940234380567401,38.7417935016607));
#57267=CARTESIAN_POINT('Ctrl Pts',(6.6755302075295,1.10886674057852,38.7498649149027));
#57268=CARTESIAN_POINT('Ctrl Pts',(6.64755399318921,1.27728739662912,38.7579261951539));
#57269=CARTESIAN_POINT('Ctrl Pts',(6.61315632898602,1.44491012506535,38.7659874754051));
#57270=CARTESIAN_POINT('Ctrl Pts',(6.57239186503604,1.61119650335027,38.7740487556564));
#57271=CARTESIAN_POINT('Ctrl Pts',(6.53166963765862,1.77731059023224,38.782101683514));
#57272=CARTESIAN_POINT('Ctrl Pts',(6.48459382625072,1.94209072320865,38.7901546113716));
#57273=CARTESIAN_POINT('Ctrl Pts',(6.43127066286263,2.10500514512495,38.7982075392292));
#57274=CARTESIAN_POINT('Ctrl Pts',(6.37799107172432,2.26778644388363,38.8062538867536));
#57275=CARTESIAN_POINT('Ctrl Pts',(6.31847440459218,2.42870471327798,38.814300234278));
#57276=CARTESIAN_POINT('Ctrl Pts',(6.25287758452075,2.58724001843625,38.8223465818024));
#57277=CARTESIAN_POINT('Ctrl Pts',(6.18732001674569,2.74568045809988,38.8303881144955));
#57278=CARTESIAN_POINT('Ctrl Pts',(6.11568968104562,2.90174042839282,38.8384296471887));
#57279=CARTESIAN_POINT('Ctrl Pts',(6.03819277572227,3.05491685700534,38.8464711798819));
#57280=CARTESIAN_POINT('Ctrl Pts',(5.95920601273738,3.21103806224841,38.8546673089301));
#57281=CARTESIAN_POINT('Ctrl Pts',(5.87412494248754,3.36416335100427,38.8628634379783));
#57282=CARTESIAN_POINT('Ctrl Pts',(5.78321880480353,3.51378275591518,38.8710595670266));
#57283=CARTESIAN_POINT('Ctrl Pts',(5.69405813743866,3.66052934896659,38.8790983238627));
#57284=CARTESIAN_POINT('Ctrl Pts',(5.5992942870446,3.80390315035634,38.8871370806988));
#57285=CARTESIAN_POINT('Ctrl Pts',(5.499226770835,3.94344949542043,38.8951758375349));
#57286=CARTESIAN_POINT('Ctrl Pts',(5.39914956914746,4.08300934709585,38.9032153724377));
#57287=CARTESIAN_POINT('Ctrl Pts',(5.29376789705891,4.21874070121749,38.9112549073404));
#57288=CARTESIAN_POINT('Ctrl Pts',(5.18342333543849,4.35021971004129,38.9192944422432));
#57289=CARTESIAN_POINT('Ctrl Pts',(5.07304624536894,4.48173747753329,38.9273363471187));
#57290=CARTESIAN_POINT('Ctrl Pts',(4.9577035936448,4.60900011865569,38.9353782519943));
#57291=CARTESIAN_POINT('Ctrl Pts',(4.83777568693623,4.73161868739322,38.9434201568698));
#57292=CARTESIAN_POINT('Ctrl Pts',(4.71380233822566,4.85837346030382,38.9517333335506));
#57293=CARTESIAN_POINT('Ctrl Pts',(4.58492928649313,4.98016505790788,38.9600465102315));
#57294=CARTESIAN_POINT('Ctrl Pts',(4.45161518447419,5.09660781788818,38.9683596869123));
#57295=CARTESIAN_POINT('Ctrl Pts',(4.32242741453802,5.20944644680479,38.9764155545228));
#57296=CARTESIAN_POINT('Ctrl Pts',(4.18906974925552,5.31726224411553,38.9844714221333));
#57297=CARTESIAN_POINT('Ctrl Pts',(4.05199001561559,5.41974777211556,38.9925272897439));
#57298=CARTESIAN_POINT('Ctrl Pts',(3.90834267302436,5.52714347066523,39.0009691209599));
#57299=CARTESIAN_POINT('Ctrl Pts',(3.76060823317765,5.62868530356234,39.0094109521758));
#57300=CARTESIAN_POINT('Ctrl Pts',(3.60933147526002,5.72407331379476,39.0178527833918));
#57301=CARTESIAN_POINT('Ctrl Pts',(3.45805471734239,5.81946132402718,39.0262946146078));
#57302=CARTESIAN_POINT('Ctrl Pts',(3.30323608358605,5.90869535548226,39.0347364458238));
#57303=CARTESIAN_POINT('Ctrl Pts',(3.14544408829463,5.9915332334397,39.0431782770398));
#57304=CARTESIAN_POINT('Ctrl Pts',(3.13002457736035,5.99962819137834,39.0440032169139));
#57305=CARTESIAN_POINT('Ctrl Pts',(3.114571560116,6.00766480946192,39.0448281567881));
#57306=CARTESIAN_POINT('Ctrl Pts',(3.09908550384713,6.01564277861016,39.0456530966623));
#57307=CARTESIAN_POINT('Ctrl Pts',(3.09908550384717,6.01564277861014,37.0457563580462));
#57308=CARTESIAN_POINT('Ctrl Pts',(2.93373232018327,6.10082796552481,37.0545058059455));
#57309=CARTESIAN_POINT('Ctrl Pts',(2.76486502144427,6.1791915818019,37.0632552538448));
#57310=CARTESIAN_POINT('Ctrl Pts',(2.59305716434354,6.25046746591378,37.072004701744));
#57311=CARTESIAN_POINT('Ctrl Pts',(2.42125069459281,6.32174277447226,37.0807540789915));
#57312=CARTESIAN_POINT('Ctrl Pts',(2.24650397871051,6.38593035557828,37.0895034562389));
#57313=CARTESIAN_POINT('Ctrl Pts',(2.06941053323759,6.44281220003542,37.0982528334863));
#57314=CARTESIAN_POINT('Ctrl Pts',(1.8923184589668,6.49969360406686,37.1070021429889));
#57315=CARTESIAN_POINT('Ctrl Pts',(1.71287996431511,6.54926929700879,37.1157514524915));
#57316=CARTESIAN_POINT('Ctrl Pts',(1.53170449173519,6.59137090065475,37.1245007619941));
#57317=CARTESIAN_POINT('Ctrl Pts',(1.35053036178182,6.63347219230081,37.1332500066587));
#57318=CARTESIAN_POINT('Ctrl Pts',(1.16761955878853,6.66809944062453,37.1419992513233));
#57319=CARTESIAN_POINT('Ctrl Pts',(0.983593309310534,6.69513503985391,37.1507484959879));
#57320=CARTESIAN_POINT('Ctrl Pts',(0.799568362460071,6.72217044771213,37.159497678721));
#57321=CARTESIAN_POINT('Ctrl Pts',(0.614428268438726,6.74161427235976,37.1682468614542));
#57322=CARTESIAN_POINT('Ctrl Pts',(0.428801816330442,6.75340047696801,37.1769960441874));
#57323=CARTESIAN_POINT('Ctrl Pts',(0.243176616522973,6.76518660206241,37.1857451678955));
#57324=CARTESIAN_POINT('Ctrl Pts',(0.0570653511656652,6.76931519233997,
37.1944942916036));
#57325=CARTESIAN_POINT('Ctrl Pts',(-0.12889990079981,6.76577222610796,37.2032434153118));
#57326=CARTESIAN_POINT('Ctrl Pts',(-0.314863959941719,6.76222928260134,
37.211992482901));
#57327=CARTESIAN_POINT('Ctrl Pts',(-0.500681721080297,6.75101488651279,
37.2207415504903));
#57328=CARTESIAN_POINT('Ctrl Pts',(-0.685722110172835,6.73216712415996,
37.2294906180796));
#57329=CARTESIAN_POINT('Ctrl Pts',(-0.870761373827337,6.71331947644149,
37.2382396324559));
#57330=CARTESIAN_POINT('Ctrl Pts',(-1.05502298984334,6.68683858439998,37.2469886468323));
#57331=CARTESIAN_POINT('Ctrl Pts',(-1.23788117676069,6.65281438131424,37.2557376612086));
#57332=CARTESIAN_POINT('Ctrl Pts',(-1.43009641451797,6.61704912302376,37.2649343720962));
#57333=CARTESIAN_POINT('Ctrl Pts',(-1.62076048992694,6.57294837083165,37.2741310829837));
#57334=CARTESIAN_POINT('Ctrl Pts',(-1.80915798961124,6.52067760042051,37.2833277938712));
#57335=CARTESIAN_POINT('Ctrl Pts',(-1.98840443003011,6.4709457857741,37.2920777915777));
#57336=CARTESIAN_POINT('Ctrl Pts',(-2.16559895952196,6.41381888474474,37.3008277892843));
#57337=CARTESIAN_POINT('Ctrl Pts',(-2.34013966242332,6.34949095285231,37.3095777869908));
#57338=CARTESIAN_POINT('Ctrl Pts',(-2.51467682554016,6.28516432556684,37.3183276072424));
#57339=CARTESIAN_POINT('Ctrl Pts',(-2.68656000078835,6.21363705879664,37.3270774274939));
#57340=CARTESIAN_POINT('Ctrl Pts',(-2.85520533840873,6.13515211510866,37.3358272477455));
#57341=CARTESIAN_POINT('Ctrl Pts',(-3.02384747998311,6.05666865881129,37.3445769021768));
#57342=CARTESIAN_POINT('Ctrl Pts',(-3.1892516468452,5.97122791039853,37.353326556608));
#57343=CARTESIAN_POINT('Ctrl Pts',(-3.3508560182914,5.87912008251918,37.3620762110393));
#57344=CARTESIAN_POINT('Ctrl Pts',(-3.51245754191397,5.78701387778187,37.3708257112824));
#57345=CARTESIAN_POINT('Ctrl Pts',(-3.67025915510912,5.68824097060998,37.3795752115256));
#57346=CARTESIAN_POINT('Ctrl Pts',(-3.82372487928807,5.58313684656873,37.3883247117687));
#57347=CARTESIAN_POINT('Ctrl Pts',(-3.97718810300773,5.47803443501791,37.3970740694538));
#57348=CARTESIAN_POINT('Ctrl Pts',(-4.12631534263003,5.36660117496393,37.4058234271389));
#57349=CARTESIAN_POINT('Ctrl Pts',(-4.27060009886204,5.24921554097367,37.414572784824));
#57350=CARTESIAN_POINT('Ctrl Pts',(-4.41488269594185,5.13183166360315,37.4233220115792));
#57351=CARTESIAN_POINT('Ctrl Pts',(-4.55432273235054,5.00849577139502,37.4320712383344));
#57352=CARTESIAN_POINT('Ctrl Pts',(-4.68844662480167,4.87962675277381,37.4408204650896));
#57353=CARTESIAN_POINT('Ctrl Pts',(-4.82256868835112,4.75075949139928,37.4495695725411));
#57354=CARTESIAN_POINT('Ctrl Pts',(-4.95137454637811,4.6163594531258,37.4583186799926));
#57355=CARTESIAN_POINT('Ctrl Pts',(-5.07442674461022,4.47688309134654,37.467067787444));
#57356=CARTESIAN_POINT('Ctrl Pts',(-5.19747742838477,4.33740844616425,37.4758167872164));
#57357=CARTESIAN_POINT('Ctrl Pts',(-5.3147744045086,4.19285781736114,37.4845657869888));
#57358=CARTESIAN_POINT('Ctrl Pts',(-5.42591931531081,4.04372211999502,37.4933147867611));
#57359=CARTESIAN_POINT('Ctrl Pts',(-5.53707636462918,3.89457013500892,37.5020647420417));
#57360=CARTESIAN_POINT('Ctrl Pts',(-5.64207983273414,3.74083230916506,37.5108146973223));
#57361=CARTESIAN_POINT('Ctrl Pts',(-5.74057303468697,3.58303087251908,37.5195646526029));
#57362=CARTESIAN_POINT('Ctrl Pts',(-5.83906243363723,3.42523552887503,37.5283142700317));
#57363=CARTESIAN_POINT('Ctrl Pts',(-5.93104191768392,3.26337713157055,37.5370638874605));
#57364=CARTESIAN_POINT('Ctrl Pts',(-6.01619906699629,3.09800545291209,37.5458135048893));
#57365=CARTESIAN_POINT('Ctrl Pts',(-6.10135338095361,2.93263928039642,37.5545628309947));
#57366=CARTESIAN_POINT('Ctrl Pts',(-6.17968568352821,2.76376031540264,37.5633121571001));
#57367=CARTESIAN_POINT('Ctrl Pts',(-6.25092992694873,2.59194213831574,37.5720614832055));
#57368=CARTESIAN_POINT('Ctrl Pts',(-6.32217217691096,2.42012876880842,37.5808105644993));
#57369=CARTESIAN_POINT('Ctrl Pts',(-6.38632665483847,2.24537661647681,37.5895596457931));
#57370=CARTESIAN_POINT('Ctrl Pts',(-6.4431754786935,2.06827917621456,37.5983087270869));
#57371=CARTESIAN_POINT('Ctrl Pts',(-6.50002944235933,1.89116572423431,37.6070585994019));
#57372=CARTESIAN_POINT('Ctrl Pts',(-6.54957634250394,1.71170683289215,37.6158084717168));
#57373=CARTESIAN_POINT('Ctrl Pts',(-6.59164787708389,1.5305120922539,37.6245583440318));
#57374=CARTESIAN_POINT('Ctrl Pts',(-6.63371649075,1.34932993148071,37.6333076088666));
#57375=CARTESIAN_POINT('Ctrl Pts',(-6.66831071257113,1.16641244174061,37.6420568737014));
#57376=CARTESIAN_POINT('Ctrl Pts',(-6.69531304840322,0.982380875160746,
37.6508061385361));
#57377=CARTESIAN_POINT('Ctrl Pts',(-6.72231677033035,0.798339861796548,
37.6595558524918));
#57378=CARTESIAN_POINT('Ctrl Pts',(-6.74172778477884,0.613184940730828,
37.6683055664475));
#57379=CARTESIAN_POINT('Ctrl Pts',(-6.75348015835514,0.427545027691196,
37.6770552804031));
#57380=CARTESIAN_POINT('Ctrl Pts',(-6.76249038365209,0.285219953548953,
37.6837634482053));
#57381=CARTESIAN_POINT('Ctrl Pts',(-6.7669999999999,0.142609995760929,37.6904716160076));
#57382=CARTESIAN_POINT('Ctrl Pts',(-6.767,5.0320187747232E-12,37.6971797838098));
#57383=CARTESIAN_POINT('',(-6.76702302174747,7.20323096178367E-5,37.3028600550208));
#57384=CARTESIAN_POINT('Ctrl Pts',(3.09908550384717,6.01564277861014,36.651532120892));
#57385=CARTESIAN_POINT('Ctrl Pts',(2.9359801966848,6.09966992444147,36.6601504462137));
#57386=CARTESIAN_POINT('Ctrl Pts',(2.76938649977694,6.17709521451719,36.6687687715353));
#57387=CARTESIAN_POINT('Ctrl Pts',(2.59985511119712,6.2476429476069,36.6773870968569));
#57388=CARTESIAN_POINT('Ctrl Pts',(2.53580837858245,6.27429495485829,36.6806429870026));
#57389=CARTESIAN_POINT('Ctrl Pts',(2.47134262033588,6.29996584594057,36.6838988771483));
#57390=CARTESIAN_POINT('Ctrl Pts',(2.40648839577786,6.32464248799776,36.687154767294));
#57391=CARTESIAN_POINT('Ctrl Pts',(2.2386547028249,6.38850219789888,36.6955805571438));
#57392=CARTESIAN_POINT('Ctrl Pts',(2.06829126929335,6.44567205805835,36.7040063469937));
#57393=CARTESIAN_POINT('Ctrl Pts',(1.89595968604162,6.49596997136725,36.7124321368435));
#57394=CARTESIAN_POINT('Ctrl Pts',(1.72358811606418,6.54627955548439,36.7208598817601));
#57395=CARTESIAN_POINT('Ctrl Pts',(1.54924780404718,6.58971392062384,36.7292876266766));
#57396=CARTESIAN_POINT('Ctrl Pts',(1.37351402332003,6.62614127737579,36.7377153715932));
#57397=CARTESIAN_POINT('Ctrl Pts',(1.19771566924371,6.66258201935405,36.7461462132833));
#57398=CARTESIAN_POINT('Ctrl Pts',(1.02052314996444,6.69201055192431,36.7545770549733));
#57399=CARTESIAN_POINT('Ctrl Pts',(0.842520801187833,6.71434640896386,36.7630078966634));
#57400=CARTESIAN_POINT('Ctrl Pts',(0.66435489097534,6.73670278980476,36.7714464852207));
#57401=CARTESIAN_POINT('Ctrl Pts',(0.485377993719001,6.75195343293511,36.7798850737781));
#57402=CARTESIAN_POINT('Ctrl Pts',(0.306179548867013,6.76006975436316,36.7883236623354));
#57403=CARTESIAN_POINT('Ctrl Pts',(0.126887140270615,6.76819033163145,36.7967666757157));
#57404=CARTESIAN_POINT('Ctrl Pts',(-0.0526267164854606,6.76916911916001,
36.8052096890959));
#57405=CARTESIAN_POINT('Ctrl Pts',(-0.231773143031693,6.76302966207965,
36.8136527024761));
#57406=CARTESIAN_POINT('Ctrl Pts',(-0.411107775386743,6.75688375507167,
36.8221045858305));
#57407=CARTESIAN_POINT('Ctrl Pts',(-0.590073875790865,6.74360468431347,
36.8305564691848));
#57408=CARTESIAN_POINT('Ctrl Pts',(-0.768087167234132,6.72326788872274,
36.8390083525391));
#57409=CARTESIAN_POINT('Ctrl Pts',(-0.816601413007557,6.71772546943745,
36.8413117577678));
#57410=CARTESIAN_POINT('Ctrl Pts',(-0.865044943110747,6.71165914262081,
36.8436151629966));
#57411=CARTESIAN_POINT('Ctrl Pts',(-0.913406063142955,6.70507109312151,
36.8459185682254));
#57412=CARTESIAN_POINT('Ctrl Pts',(-1.0880311191712,6.68128259293446,36.8542358335588));
#57413=CARTESIAN_POINT('Ctrl Pts',(-1.26189497854287,6.65064499429759,36.8625530988922));
#57414=CARTESIAN_POINT('Ctrl Pts',(-1.43442980892838,6.61322161455804,36.8708703642256));
#57415=CARTESIAN_POINT('Ctrl Pts',(-1.60681911946091,6.5758297985596,36.8791806145857));
#57416=CARTESIAN_POINT('Ctrl Pts',(-1.77788129611543,6.53166367777585,36.8874908649458));
#57417=CARTESIAN_POINT('Ctrl Pts',(-1.94705594194545,6.48083807535221,36.895801115306));
#57418=CARTESIAN_POINT('Ctrl Pts',(-2.11611888436437,6.43004603229046,36.9041058785358));
#57419=CARTESIAN_POINT('Ctrl Pts',(-2.28329644737229,6.37260336920495,36.9124106417657));
#57420=CARTESIAN_POINT('Ctrl Pts',(-2.44804048398312,6.30867551779133,36.9207154049956));
#57421=CARTESIAN_POINT('Ctrl Pts',(-2.61270590009155,6.24477817455208,36.9290162049581));
#57422=CARTESIAN_POINT('Ctrl Pts',(-2.77493978065457,6.17440193642565,36.9373170049207));
#57423=CARTESIAN_POINT('Ctrl Pts',(-2.9342109354109,6.09776148980223,36.9456178048833));
#57424=CARTESIAN_POINT('Ctrl Pts',(-3.09343522717903,6.02114359340362,36.9539161624683));
#57425=CARTESIAN_POINT('Ctrl Pts',(-3.24969821770864,5.93826531308279,36.9622145200533));
#57426=CARTESIAN_POINT('Ctrl Pts',(-3.40249022912408,5.84938879206325,36.9705128776383));
#57427=CARTESIAN_POINT('Ctrl Pts',(-3.55529778677459,5.76050322806251,36.9788120795621));
#57428=CARTESIAN_POINT('Ctrl Pts',(-3.70463335522753,5.66561837228997,36.9871112814859));
#57429=CARTESIAN_POINT('Ctrl Pts',(-3.85001282541519,5.56504180075394,36.9954104834097));
#57430=CARTESIAN_POINT('Ctrl Pts',(-3.99540703432518,5.46445503266016,37.0037105267152));
#57431=CARTESIAN_POINT('Ctrl Pts',(-4.13684405903616,5.35817559621645,37.0120105700207));
#57432=CARTESIAN_POINT('Ctrl Pts',(-4.2738697816766,5.24655373452628,37.0203106133263));
#57433=CARTESIAN_POINT('Ctrl Pts',(-4.41093214269751,5.13490202702205,37.0286128759242));
#57434=CARTESIAN_POINT('Ctrl Pts',(-4.54358058100991,5.01790526692851,37.0369151385221));
#57435=CARTESIAN_POINT('Ctrl Pts',(-4.67139486096394,4.89595333443444,37.04521740112));
#57436=CARTESIAN_POINT('Ctrl Pts',(-4.79926453630584,4.77394854732503,37.0535232619627));
#57437=CARTESIAN_POINT('Ctrl Pts',(-4.92229562607523,4.64698454763409,37.0618291228053));
#57438=CARTESIAN_POINT('Ctrl Pts',(-5.04010535577153,4.51548746014461,37.0701349836479));
#57439=CARTESIAN_POINT('Ctrl Pts',(-5.15805434487977,4.38383493382063,37.0784506626041));
#57440=CARTESIAN_POINT('Ctrl Pts',(-5.27076941002723,4.24763887311402,37.0867663415602));
#57441=CARTESIAN_POINT('Ctrl Pts',(-5.37790788531592,4.10735873488752,37.0950820205163));
#57442=CARTESIAN_POINT('Ctrl Pts',(-5.48511412483643,3.96698987059153,37.1034029590731));
#57443=CARTESIAN_POINT('Ctrl Pts',(-5.5867365405815,3.82253206145575,37.1117238976299));
#57444=CARTESIAN_POINT('Ctrl Pts',(-5.68247623606807,3.67447313590965,37.1200448361867));
#57445=CARTESIAN_POINT('Ctrl Pts',(-5.77835823039775,3.52619414893853,37.1283781422357));
#57446=CARTESIAN_POINT('Ctrl Pts',(-5.86833985364039,3.37430364820411,37.1367114482846));
#57447=CARTESIAN_POINT('Ctrl Pts',(-5.95216788904884,3.21931458863154,37.1450447543335));
#57448=CARTESIAN_POINT('Ctrl Pts',(-6.01387027232919,3.10523349020892,37.1511785595852));
#57449=CARTESIAN_POINT('Ctrl Pts',(-6.07223971776672,2.98947414502033,37.1573123648368));
#57450=CARTESIAN_POINT('Ctrl Pts',(-6.12719212312746,2.87224749739378,37.1634461700884));
#57451=CARTESIAN_POINT('Ctrl Pts',(-6.20505480737424,2.70614773543547,37.1721372280759));
#57452=CARTESIAN_POINT('Ctrl Pts',(-6.27626917716232,2.53664610066104,37.1808282860633));
#57453=CARTESIAN_POINT('Ctrl Pts',(-6.34053998751404,2.36428459935251,37.1895193440508));
#57454=CARTESIAN_POINT('Ctrl Pts',(-6.40466935798327,2.19230241161351,37.1981912757472));
#57455=CARTESIAN_POINT('Ctrl Pts',(-6.46188552719803,2.01747317717048,37.2068632074437));
#57456=CARTESIAN_POINT('Ctrl Pts',(-6.51193941222511,1.84036248916058,37.2155351391402));
#57457=CARTESIAN_POINT('Ctrl Pts',(-6.56184040138734,1.66379280794372,37.2241805813345));
#57458=CARTESIAN_POINT('Ctrl Pts',(-6.60462265583713,1.48495585292723,37.2328260235288));
#57459=CARTESIAN_POINT('Ctrl Pts',(-6.64008566687456,1.30443525579736,37.2414714657231));
#57460=CARTESIAN_POINT('Ctrl Pts',(-6.67548350019386,1.12424643874622,37.2501010183981));
#57461=CARTESIAN_POINT('Ctrl Pts',(-6.70358884369664,0.942380433296196,
37.2587305710732));
#57462=CARTESIAN_POINT('Ctrl Pts',(-6.72425049383304,0.759436828305091,
37.2673601237483));
#57463=CARTESIAN_POINT('Ctrl Pts',(-6.74486050175704,0.576950476846289,
37.2759681075173));
#57464=CARTESIAN_POINT('Ctrl Pts',(-6.75806388383551,0.393392188113838,
37.2845760912862));
#57465=CARTESIAN_POINT('Ctrl Pts',(-6.76376022331584,0.209372016971024,
37.2931840750552));
#57466=CARTESIAN_POINT('Ctrl Pts',(-6.76588579776919,0.14070536252861,37.2963961221));
#57467=CARTESIAN_POINT('Ctrl Pts',(-6.76696660310004,0.0719745239661936,
37.2996081691449));
#57468=CARTESIAN_POINT('Ctrl Pts',(-6.76699923788744,0.00321160876916168,
37.3028202161897));
#57469=CARTESIAN_POINT('Ctrl Pts',(-6.767,4.91316042210608E-12,37.3028202161897));
#57470=CARTESIAN_POINT('Ctrl Pts',(-6.76700000000014,-0.186007249555132,
37.3115697280025));
#57471=CARTESIAN_POINT('Ctrl Pts',(-6.75932637294273,-0.372014355811356,
37.3203192398152));
#57472=CARTESIAN_POINT('Ctrl Pts',(-6.74400518263401,-0.557389537581778,
37.3290687516279));
#57473=CARTESIAN_POINT('Ctrl Pts',(-6.7286840570378,-0.742763936378232,
37.3378182264851));
#57474=CARTESIAN_POINT('Ctrl Pts',(-6.70571545643626,-0.927506130400532,
37.3465677013423));
#57475=CARTESIAN_POINT('Ctrl Pts',(-6.67517739401648,-1.11098864009104,
37.3553171761995));
#57476=CARTESIAN_POINT('Ctrl Pts',(-6.64463945804472,-1.29447039004117,
37.3640666148281));
#57477=CARTESIAN_POINT('Ctrl Pts',(-6.60653217002815,-1.47669218338871,
37.3728160534566));
#57478=CARTESIAN_POINT('Ctrl Pts',(-6.56098496085578,-1.65703510627393,
37.3815654920851));
#57479=CARTESIAN_POINT('Ctrl Pts',(-6.5154379364966,-1.83737729739641,37.3903148952118));
#57480=CARTESIAN_POINT('Ctrl Pts',(-6.46245112157005,-2.01584035544606,
37.3990642983384));
#57481=CARTESIAN_POINT('Ctrl Pts',(-6.40220448361828,-2.19181813797084,
37.407813701465));
#57482=CARTESIAN_POINT('Ctrl Pts',(-6.34195808512091,-2.36779522105988,
37.4165630698166));
#57483=CARTESIAN_POINT('Ctrl Pts',(-6.27445201416478,-2.54128677725439,
37.4253124381681));
#57484=CARTESIAN_POINT('Ctrl Pts',(-6.19991555052854,-2.71170355428363,
37.4340618065196));
#57485=CARTESIAN_POINT('Ctrl Pts',(-6.12537937695241,-2.88211966813262,
37.4428111408228));
#57486=CARTESIAN_POINT('Ctrl Pts',(-6.0438129802846,-3.04946076419655,37.451560475126));
#57487=CARTESIAN_POINT('Ctrl Pts',(-5.95549339308974,-3.21315848424326,
37.4603098094292));
#57488=CARTESIAN_POINT('Ctrl Pts',(-5.86717414225799,-3.376855580851,37.4690591104108));
#57489=CARTESIAN_POINT('Ctrl Pts',(-5.77210188844054,-3.53690907700021,
37.4778084113923));
#57490=CARTESIAN_POINT('Ctrl Pts',(-5.67059953311356,-3.69277537024016,
37.4865577123739));
#57491=CARTESIAN_POINT('Ctrl Pts',(-5.56909755592688,-3.84864108281055,
37.4953069807605));
#57492=CARTESIAN_POINT('Ctrl Pts',(-5.46116568154942,-4.00031938354862,
37.5040562491471));
#57493=CARTESIAN_POINT('Ctrl Pts',(-5.34717048488348,-4.14729511918202,
37.5128055175337));
#57494=CARTESIAN_POINT('Ctrl Pts',(-5.23317570343271,-4.2942703194722,37.5215547540521));
#57495=CARTESIAN_POINT('Ctrl Pts',(-5.11311781951508,-4.43654276249601,
37.5303039905704));
#57496=CARTESIAN_POINT('Ctrl Pts',(-4.987404589292,-4.57362924412431,37.5390532270888));
#57497=CARTESIAN_POINT('Ctrl Pts',(-4.86169180652702,-4.71071523781306,
37.5478024324655));
#57498=CARTESIAN_POINT('Ctrl Pts',(-4.73032391141542,-4.84261509584519,
37.5565516378422));
#57499=CARTESIAN_POINT('Ctrl Pts',(-4.59374706947305,-4.96888084599619,
37.5653008432189));
#57500=CARTESIAN_POINT('Ctrl Pts',(-4.45717070231523,-5.09514615720727,
37.5740500181806));
#57501=CARTESIAN_POINT('Ctrl Pts',(-4.31538563497419,-5.21577720520535,
37.5827991931423));
#57502=CARTESIAN_POINT('Ctrl Pts',(-4.16887340952139,-5.33036429293397,
37.591548368104));
#57503=CARTESIAN_POINT('Ctrl Pts',(-4.02236168122617,-5.44495099183609,
37.6002975133773));
#57504=CARTESIAN_POINT('Ctrl Pts',(-3.87112305263311,-5.55349359497838,
37.6090466586505));
#57505=CARTESIAN_POINT('Ctrl Pts',(-3.71567116929123,-5.65562346357127,
37.6177958039237));
#57506=CARTESIAN_POINT('Ctrl Pts',(-3.5602198005346,-5.75775299408835,37.6265449202351));
#57507=CARTESIAN_POINT('Ctrl Pts',(-3.40055544442255,-5.85346967519779,
37.6352940365465));
#57508=CARTESIAN_POINT('Ctrl Pts',(-3.23722035887036,-5.94244843041277,
37.6440431528578));
#57509=CARTESIAN_POINT('Ctrl Pts',(-3.07388580043715,-6.03142689847335,
37.6527922409338));
#57510=CARTESIAN_POINT('Ctrl Pts',(-2.9068807878948,-6.11366734707778,37.6615413290098));
#57511=CARTESIAN_POINT('Ctrl Pts',(-2.73677250610683,-6.188890470013,37.6702904170858));
#57512=CARTESIAN_POINT('Ctrl Pts',(-2.56666475917226,-6.26411335643215,
37.679039477653));
#57513=CARTESIAN_POINT('Ctrl Pts',(-2.39345402457385,-6.33231884545146,
37.6877885382202));
#57514=CARTESIAN_POINT('Ctrl Pts',(-2.21772855944357,-6.39327529804781,
37.6965375987873));
#57515=CARTESIAN_POINT('Ctrl Pts',(-2.04200363223892,-6.45423156404607,
37.7052866325721));
#57516=CARTESIAN_POINT('Ctrl Pts',(-1.86376426061344,-6.50793874412364,
37.7140356663569));
#57517=CARTESIAN_POINT('Ctrl Pts',(-1.68361577622007,-6.5542144394323,37.7227847001417));
#57518=CARTESIAN_POINT('Ctrl Pts',(-1.50346782833494,-6.60048999692525,
37.7315337078706));
#57519=CARTESIAN_POINT('Ctrl Pts',(-1.32141105657625,-6.63933404265116,
37.7402827155996));
#57520=CARTESIAN_POINT('Ctrl Pts',(-1.1380637534673,-6.67061465631496,37.7490317233285));
#57521=CARTESIAN_POINT('Ctrl Pts',(-0.954716981172442,-6.70189517941735,
37.7577807057279));
#57522=CARTESIAN_POINT('Ctrl Pts',(-0.770079967445198,-6.72561226608969,
37.7665296881273));
#57523=CARTESIAN_POINT('Ctrl Pts',(-0.584779764076472,-6.74168536995955,
37.7752786705267));
#57524=CARTESIAN_POINT('Ctrl Pts',(-0.391489587596343,-6.75845153117853,
37.7844049009423));
#57525=CARTESIAN_POINT('Ctrl Pts',(-0.197478091808605,-6.76689985146384,
37.793531131358));
#57526=CARTESIAN_POINT('Ctrl Pts',(-0.00346214753437534,-6.76699911434415,
37.8026573617736));
#57527=CARTESIAN_POINT('Ctrl Pts',(0.184490798481368,-6.76709527525944,
37.8114983974887));
#57528=CARTESIAN_POINT('Ctrl Pts',(0.372447602151582,-6.75935633790781,
37.8203394332038));
#57529=CARTESIAN_POINT('Ctrl Pts',(0.559756448191097,-6.74380914014539,
37.8291804689189));
#57530=CARTESIAN_POINT('Ctrl Pts',(0.745136131040202,-6.72842206873189,
37.8379304475323));
#57531=CARTESIAN_POINT('Ctrl Pts',(0.929880851941859,-6.70538686355767,
37.8466804261456));
#57532=CARTESIAN_POINT('Ctrl Pts',(1.11336305057141,-6.67478177303366,37.8554304047589));
#57533=CARTESIAN_POINT('Ctrl Pts',(1.29684337089809,-6.64417699581322,37.8641802937988));
#57534=CARTESIAN_POINT('Ctrl Pts',(1.47906091204882,-6.60600253548129,37.8729301828389));
#57535=CARTESIAN_POINT('Ctrl Pts',(1.6593967109492,-6.56038806441288,37.8816800718788));
#57536=CARTESIAN_POINT('Ctrl Pts',(1.83973072368859,-6.51477404513934,37.8904298742543));
#57537=CARTESIAN_POINT('Ctrl Pts',(2.01818275356735,-6.46172023288755,37.8991796766298));
#57538=CARTESIAN_POINT('Ctrl Pts',(2.19414664033026,-6.40140683918211,37.9079294790053));
#57539=CARTESIAN_POINT('Ctrl Pts',(2.37010884270963,-6.34109402281608,37.9166791976248));
#57540=CARTESIAN_POINT('Ctrl Pts',(2.54358267847514,-6.2735218569991,37.9254289162444));
#57541=CARTESIAN_POINT('Ctrl Pts',(2.71397890841454,-6.19891986435387,37.9341786348639));
#57542=CARTESIAN_POINT('Ctrl Pts',(2.88437356388664,-6.12431856103374,37.9429282726357));
#57543=CARTESIAN_POINT('Ctrl Pts',(3.05169040786905,-6.04268767582692,37.9516779104076));
#57544=CARTESIAN_POINT('Ctrl Pts',(3.21536112511797,-5.95430447954084,37.9604275481794));
#57545=CARTESIAN_POINT('Ctrl Pts',(3.37903038442591,-5.86592207055188,37.9691771080115));
#57546=CARTESIAN_POINT('Ctrl Pts',(3.53905332979726,-5.77078760703528,37.9779266678435));
#57547=CARTESIAN_POINT('Ctrl Pts',(3.6948864304165,-5.66922422085456,37.9866762276756));
#57548=CARTESIAN_POINT('Ctrl Pts',(3.85071819468506,-5.56766170563322,37.9954257124756));
#57549=CARTESIAN_POINT('Ctrl Pts',(4.00235994598994,-5.4596705345642,38.0041751972756));
#57550=CARTESIAN_POINT('Ctrl Pts',(4.14929662974076,-5.34561750206858,38.0129246820756));
#57551=CARTESIAN_POINT('Ctrl Pts',(4.29623210224831,-5.23156540974642,38.0216740947509));
#57552=CARTESIAN_POINT('Ctrl Pts',(4.43846235841914,-5.11145173172363,38.0304235074263));
#57553=CARTESIAN_POINT('Ctrl Pts',(4.57550431797236,-4.98568443006738,38.0391729201016));
#57554=CARTESIAN_POINT('Ctrl Pts',(4.71254519337315,-4.85991812336863,38.0479222635595));
#57555=CARTESIAN_POINT('Ctrl Pts',(4.84439764314818,-4.72849847631271,38.0566716070175));
#57556=CARTESIAN_POINT('Ctrl Pts',(4.97061384196533,-4.59187184425509,38.0654209504754));
#57557=CARTESIAN_POINT('Ctrl Pts',(5.09682908420066,-4.45524624767908,38.0741702276227));
#57558=CARTESIAN_POINT('Ctrl Pts',(5.21740796650043,-4.31341395557047,38.0829195047701));
#57559=CARTESIAN_POINT('Ctrl Pts',(5.33194095942135,-4.16685668163004,38.0916687819174));
#57560=CARTESIAN_POINT('Ctrl Pts',(5.44647312235024,-4.02030046975362,38.100417995661));
#57561=CARTESIAN_POINT('Ctrl Pts',(5.55495930712187,-3.86901957035693,38.1091672094045));
#57562=CARTESIAN_POINT('Ctrl Pts',(5.657031060797,-3.71352778058519,38.1179164231481));
#57563=CARTESIAN_POINT('Ctrl Pts',(5.75910210868641,-3.55803706597755,38.1266655763943));
#57564=CARTESIAN_POINT('Ctrl Pts',(5.85475865698456,-3.3983357588106,38.1354147296405));
#57565=CARTESIAN_POINT('Ctrl Pts',(5.94367583068971,-3.2349662470689,38.1441638828866));
#57566=CARTESIAN_POINT('Ctrl Pts',(6.03259241909987,-3.07159781070276,38.1529129785418));
#57567=CARTESIAN_POINT('Ctrl Pts',(6.1147695847088,-2.90456146976017,38.1616620741969));
#57568=CARTESIAN_POINT('Ctrl Pts',(6.18992823574302,-2.73442451648447,38.170411169852));
#57569=CARTESIAN_POINT('Ctrl Pts',(6.26508641700858,-2.56428862662605,38.1791602108221));
#57570=CARTESIAN_POINT('Ctrl Pts',(6.33322605570226,-2.39105242531465,38.1879092517923));
#57571=CARTESIAN_POINT('Ctrl Pts',(6.39411573747703,-2.21530425353914,38.1966582927624));
#57572=CARTESIAN_POINT('Ctrl Pts',(6.45500505889067,-2.03955712188745,38.2054072819534));
#57573=CARTESIAN_POINT('Ctrl Pts',(6.50864441544877,-1.86129832025755,38.2141562711444));
#57574=CARTESIAN_POINT('Ctrl Pts',(6.5548516404986,-1.6811332401249,38.2229052603354));
#57575=CARTESIAN_POINT('Ctrl Pts',(6.60199852639071,-1.49730435913071,38.2318321672123));
#57576=CARTESIAN_POINT('Ctrl Pts',(6.64140767440978,-1.31149113173816,38.2407590740892));
#57577=CARTESIAN_POINT('Ctrl Pts',(6.67293975269576,-1.12435050446587,38.249685980966));
#57578=CARTESIAN_POINT('Ctrl Pts',(6.70384664831484,-0.940920291565358,
38.25843589515));
#57579=CARTESIAN_POINT('Ctrl Pts',(6.72718585889647,-0.756215114279608,
38.267185809334));
#57580=CARTESIAN_POINT('Ctrl Pts',(6.7428781045185,-0.57086238937686,38.275935723518));
#57581=CARTESIAN_POINT('Ctrl Pts',(6.75857004154112,-0.385513309569975,
38.2846854656286));
#57582=CARTESIAN_POINT('Ctrl Pts',(6.7666152903555,-0.199516993261237,38.2934352077392));
#57583=CARTESIAN_POINT('Ctrl Pts',(6.76698652348896,-0.0135052182072312,
38.3021849498497));
#57584=CARTESIAN_POINT('Ctrl Pts',(6.76735774981529,0.172503146035705,38.3109345315204));
#57585=CARTESIAN_POINT('Ctrl Pts',(6.76005524147496,0.358526681830274,38.319684113191));
#57586=CARTESIAN_POINT('Ctrl Pts',(6.74510380214907,0.543933542111663,38.3284336948617));
#57587=CARTESIAN_POINT('Ctrl Pts',(6.73015261711013,0.729337249081553,38.3371831277236));
#57588=CARTESIAN_POINT('Ctrl Pts',(6.70755278444648,0.914124015851531,38.3459325605855));
#57589=CARTESIAN_POINT('Ctrl Pts',(6.6773810640834,1.09766621749077,38.3546819934475));
#57590=CARTESIAN_POINT('Ctrl Pts',(6.64720981677314,1.2812055414301,38.3634312891298));
#57591=CARTESIAN_POINT('Ctrl Pts',(6.60946696581592,1.46350005650307,38.3721805848122));
#57592=CARTESIAN_POINT('Ctrl Pts',(6.56428070011073,1.64393062206219,38.3809298804945));
#57593=CARTESIAN_POINT('Ctrl Pts',(6.5190950828283,1.82435859844333,38.3896790506245));
#57594=CARTESIAN_POINT('Ctrl Pts',(6.46646633415761,2.0029224008624,38.3984282207545));
#57595=CARTESIAN_POINT('Ctrl Pts',(6.40657319597303,2.17901557696127,38.4071773908845));
#57596=CARTESIAN_POINT('Ctrl Pts',(6.34668083768422,2.3551064600709,38.4159264470875));
#57597=CARTESIAN_POINT('Ctrl Pts',(6.2795243714403,2.5287265099617,38.4246755032906));
#57598=CARTESIAN_POINT('Ctrl Pts',(6.20533187335299,2.6992860799755,38.4334245594937));
#57599=CARTESIAN_POINT('Ctrl Pts',(6.12831449784421,2.87633970115039,38.4425067357825));
#57600=CARTESIAN_POINT('Ctrl Pts',(6.04371489463325,3.05009490562009,38.4515889120714));
#57601=CARTESIAN_POINT('Ctrl Pts',(5.95184265120665,3.21991584599309,38.4606710883602));
#57602=CARTESIAN_POINT('Ctrl Pts',(5.8633328133567,3.38352155904993,38.4694208687146));
#57603=CARTESIAN_POINT('Ctrl Pts',(5.76807337235865,3.54347560903532,38.4781706490691));
#57604=CARTESIAN_POINT('Ctrl Pts',(5.66638790086537,3.69923467178369,38.4869204294235));
#57605=CARTESIAN_POINT('Ctrl Pts',(5.56470608502933,3.85498813489489,38.4956698952177));
#57606=CARTESIAN_POINT('Ctrl Pts',(5.45659885767152,4.00654667255989,38.504419361012));
#57607=CARTESIAN_POINT('Ctrl Pts',(5.34243340580716,4.15339551505942,38.5131688268063));
#57608=CARTESIAN_POINT('Ctrl Pts',(5.22827145140797,4.30023985883624,38.5219180245601));
#57609=CARTESIAN_POINT('Ctrl Pts',(5.10805181978285,4.44237456992818,38.530667222314));
#57610=CARTESIAN_POINT('Ctrl Pts',(4.98218281282739,4.57931691626244,38.5394164200679));
#57611=CARTESIAN_POINT('Ctrl Pts',(4.85631699296418,4.71625579511967,38.5481653962859));
#57612=CARTESIAN_POINT('Ctrl Pts',(4.72480227792028,4.84800236135585,38.5569143725039));
#57613=CARTESIAN_POINT('Ctrl Pts',(4.58808530848303,4.97410918678734,38.5656633487219));
#57614=CARTESIAN_POINT('Ctrl Pts',(4.45135945057161,5.10022421088843,38.5744128937431));
#57615=CARTESIAN_POINT('Ctrl Pts',(4.3094308720823,5.22069856611829,38.5831624387643));
#57616=CARTESIAN_POINT('Ctrl Pts',(4.16278164322658,5.33512305301535,38.5919119837855));
#57617=CARTESIAN_POINT('Ctrl Pts',(4.01614103534572,5.44954081331294,38.6006610144528));
#57618=CARTESIAN_POINT('Ctrl Pts',(3.86478055833585,5.55790924068218,38.6094100451201));
#57619=CARTESIAN_POINT('Ctrl Pts',(3.70921425812113,5.65986029751185,38.6181590757873));
#57620=CARTESIAN_POINT('Ctrl Pts',(3.55364584530289,5.76181273884549,38.6269082252672));
#57621=CARTESIAN_POINT('Ctrl Pts',(3.39387173464521,5.85734747817961,38.635657374747));
#57622=CARTESIAN_POINT('Ctrl Pts',(3.23043456092589,5.94614005448708,38.6444065242269));
#57623=CARTESIAN_POINT('Ctrl Pts',(3.1869076880652,5.96978744811214,38.6467366129599));
#57624=CARTESIAN_POINT('Ctrl Pts',(3.14312114982954,5.99295688499263,38.649066701693));
#57625=CARTESIAN_POINT('Ctrl Pts',(3.09908550384735,6.01564277861005,38.6513967904261));
#57626=CARTESIAN_POINT('Origin',(0.,0.,-63.6971797838103));
#57627=CARTESIAN_POINT('',(3.09908550384737,6.01564277861004,41.0460412338187));
#57628=CARTESIAN_POINT('',(3.0990855038471,6.01564277861018,40.6514943894097));
#57629=CARTESIAN_POINT('',(3.09908550384721,6.01564277861012,-63.6971797838103));
#57630=CARTESIAN_POINT('',(-6.76699998768905,-0.000408186690650814,39.6971797838371));
#57631=CARTESIAN_POINT('Ctrl Pts',(-6.76699998768905,-0.000408186690462319,
39.6971797838371));
#57632=CARTESIAN_POINT('Ctrl Pts',(-6.7669893069887,-0.177474957546841,
39.7055509473628));
#57633=CARTESIAN_POINT('Ctrl Pts',(-6.76002454313562,-0.354721736622949,
39.7139221108885));
#57634=CARTESIAN_POINT('Ctrl Pts',(-6.74608922499918,-0.531572354764644,
39.7222932744142));
#57635=CARTESIAN_POINT('Ctrl Pts',(-6.73216752127865,-0.708250194800711,
39.7306562595474));
#57636=CARTESIAN_POINT('Ctrl Pts',(-6.71128886035345,-0.884532305404253,
39.7390192446805));
#57637=CARTESIAN_POINT('Ctrl Pts',(-6.68348879857372,-1.05984266725754,
39.7473822298137));
#57638=CARTESIAN_POINT('Ctrl Pts',(-6.65571106829061,-1.23501220414491,
39.7557384970491));
#57639=CARTESIAN_POINT('Ctrl Pts',(-6.62102307112024,-1.40921121080189,
39.7640947642845));
#57640=CARTESIAN_POINT('Ctrl Pts',(-6.57951218369061,-1.58186864962514,
39.7724510315198));
#57641=CARTESIAN_POINT('Ctrl Pts',(-6.53802743766386,-1.75441735775269,
39.7808020364117));
#57642=CARTESIAN_POINT('Ctrl Pts',(-6.48972844551703,-1.92542610070345,
39.7891530413036));
#57643=CARTESIAN_POINT('Ctrl Pts',(-6.43475374173362,-2.09433361316798,
39.7975040461954));
#57644=CARTESIAN_POINT('Ctrl Pts',(-6.3798024647024,-2.26316914790154,39.8058514924156));
#57645=CARTESIAN_POINT('Ctrl Pts',(-6.31818125176635,-2.42990491138873,
39.8141989386358));
#57646=CARTESIAN_POINT('Ctrl Pts',(-6.25007870163198,-2.59399406772768,
39.822546384856));
#57647=CARTESIAN_POINT('Ctrl Pts',(-6.18199193246221,-2.75804520074498,
39.8308918967763));
#57648=CARTESIAN_POINT('Ctrl Pts',(-6.10742695007066,-2.91945063234419,
39.8392374086966));
#57649=CARTESIAN_POINT('Ctrl Pts',(-6.02662089271538,-3.07768250725875,
39.8475829206169));
#57650=CARTESIAN_POINT('Ctrl Pts',(-5.94582084388802,-3.23590261646329,
39.8559278119867));
#57651=CARTESIAN_POINT('Ctrl Pts',(-5.85878080098072,-3.3909493341977,39.8642727033565));
#57652=CARTESIAN_POINT('Ctrl Pts',(-5.76578446894041,-3.54231823213635,
39.8726175947263));
#57653=CARTESIAN_POINT('Ctrl Pts',(-5.67278041850855,-3.69369969319868,
39.8809631786948));
#57654=CARTESIAN_POINT('Ctrl Pts',(-5.57381927358222,-3.84140243443189,
39.8893087626633));
#57655=CARTESIAN_POINT('Ctrl Pts',(-5.46922891738796,-3.98494969218023,
39.8976543466318));
#57656=CARTESIAN_POINT('Ctrl Pts',(-5.36457065941219,-4.12859014317207,
39.9060053486908));
#57657=CARTESIAN_POINT('Ctrl Pts',(-5.25427608820586,-4.26806944150156,
39.9143563507499));
#57658=CARTESIAN_POINT('Ctrl Pts',(-5.13871494445318,-4.40294193916449,
39.9227073528089));
#57659=CARTESIAN_POINT('Ctrl Pts',(-5.02311737044658,-4.53785695491938,
39.9310609874927));
#57660=CARTESIAN_POINT('Ctrl Pts',(-4.90225014228802,-4.66816201893523,
39.9394146221764));
#57661=CARTESIAN_POINT('Ctrl Pts',(-4.77652120601833,-4.79344700277965,
39.9477682568602));
#57662=CARTESIAN_POINT('Ctrl Pts',(-4.65066169959826,-4.91886209572755,
39.9561305668368));
#57663=CARTESIAN_POINT('Ctrl Pts',(-4.51993064258537,-5.03924645202986,
39.9644928768133));
#57664=CARTESIAN_POINT('Ctrl Pts',(-4.38477143172748,-5.15422821492283,
39.9728551867899));
#57665=CARTESIAN_POINT('Ctrl Pts',(-4.26136283552805,-5.25921357150409,
39.9804904854029));
#57666=CARTESIAN_POINT('Ctrl Pts',(-4.1342631326172,-5.35969524653657,39.9881257840159));
#57667=CARTESIAN_POINT('Ctrl Pts',(-4.00383178889481,-5.4554211575492,39.9957610826289));
#57668=CARTESIAN_POINT('Ctrl Pts',(-3.8647554384088,-5.55749179464177,40.0039024498467));
#57669=CARTESIAN_POINT('Ctrl Pts',(-3.72159612305646,-5.65437077790788,
40.0120438170646));
#57670=CARTESIAN_POINT('Ctrl Pts',(-3.57478265544449,-5.74571300765477,
40.0201851842825));
#57671=CARTESIAN_POINT('Ctrl Pts',(-3.42809734482381,-5.83697550258215,
40.0283194447059));
#57672=CARTESIAN_POINT('Ctrl Pts',(-3.27776453996345,-5.92271067241397,
40.0364537051294));
#57673=CARTESIAN_POINT('Ctrl Pts',(-3.1242444878253,-6.00261487855861,40.0445879655529));
#57674=CARTESIAN_POINT('Ctrl Pts',(-2.970829161522,-6.08246457693975,40.0527166770777));
#57675=CARTESIAN_POINT('Ctrl Pts',(-2.81423124013008,-6.15649106274397,
40.0608453886025));
#57676=CARTESIAN_POINT('Ctrl Pts',(-2.65493815887967,-6.2244351046922,40.0689741001273));
#57677=CARTESIAN_POINT('Ctrl Pts',(-2.49572104155544,-6.29234674538266,
40.0770989352198));
#57678=CARTESIAN_POINT('Ctrl Pts',(-2.33381165978804,-6.3541815750316,40.0852237703124));
#57679=CARTESIAN_POINT('Ctrl Pts',(-2.16972013415191,-6.40972725936571,
40.0933486054049));
#57680=CARTESIAN_POINT('Ctrl Pts',(-2.00567454639833,-6.46525739352979,
40.1014711659271));
#57681=CARTESIAN_POINT('Ctrl Pts',(-1.83944837825209,-6.51450177280169,
40.1095937264492));
#57682=CARTESIAN_POINT('Ctrl Pts',(-1.67156969058518,-6.55729698652707,
40.1177162869714));
#57683=CARTESIAN_POINT('Ctrl Pts',(-1.50368208060156,-6.60009447470703,
40.1258392791865));
#57684=CARTESIAN_POINT('Ctrl Pts',(-1.33414212939293,-6.63644201839307,
40.1339622714017));
#57685=CARTESIAN_POINT('Ctrl Pts',(-1.16349113385735,-6.66622662241806,
40.1420852636169));
#57686=CARTESIAN_POINT('Ctrl Pts',(-1.07637900115297,-6.68143075509968,
40.146231803598));
#57687=CARTESIAN_POINT('Ctrl Pts',(-0.988977531711366,-6.69492554177188,
40.1503783435792));
#57688=CARTESIAN_POINT('Ctrl Pts',(-0.901359588944638,-6.70670111839029,
40.1545248835603));
#57689=CARTESIAN_POINT('Ctrl Pts',(-0.711531509107533,-6.73221341676049,
40.1635085425886));
#57690=CARTESIAN_POINT('Ctrl Pts',(-0.520780911100196,-6.74964037716923,
40.172492201617));
#57691=CARTESIAN_POINT('Ctrl Pts',(-0.329777953790215,-6.75895964636526,
40.1814758606454));
#57692=CARTESIAN_POINT('Ctrl Pts',(-0.138446855423123,-6.76829492596703,
40.1904749535048));
#57693=CARTESIAN_POINT('Ctrl Pts',(0.0531372298977748,-6.76949466268849,
40.1994740463642));
#57694=CARTESIAN_POINT('Ctrl Pts',(0.244304328232994,-6.76258858686573,
40.2084731392236));
#57695=CARTESIAN_POINT('Ctrl Pts',(0.435919659992452,-6.75566631822506,
40.2174933324409));
#57696=CARTESIAN_POINT('Ctrl Pts',(0.627115808575196,-6.7406002183414,40.2265135256583));
#57697=CARTESIAN_POINT('Ctrl Pts',(0.817225335351815,-6.71747212508241,
40.2355337188757));
#57698=CARTESIAN_POINT('Ctrl Pts',(1.00752739562876,-6.69432060883759,40.2445630472974));
#57699=CARTESIAN_POINT('Ctrl Pts',(1.19674039916342,-6.66309082283544,40.2535923757191));
#57700=CARTESIAN_POINT('Ctrl Pts',(1.38420568205252,-6.62391603432392,40.2626217041408));
#57701=CARTESIAN_POINT('Ctrl Pts',(1.57193525320336,-6.58468601725702,40.2716637620956));
#57702=CARTESIAN_POINT('Ctrl Pts',(1.75791194283566,-6.53748865039368,40.2807058200503));
#57703=CARTESIAN_POINT('Ctrl Pts',(1.94148860172122,-6.48250808016362,40.2897478780051));
#57704=CARTESIAN_POINT('Ctrl Pts',(2.10080125023388,-6.4347944965672,40.2975948135007));
#57705=CARTESIAN_POINT('Ctrl Pts',(2.25830651812223,-6.38122002535534,40.3054417489963));
#57706=CARTESIAN_POINT('Ctrl Pts',(2.4135921446991,-6.32193498535431,40.3132886844919));
#57707=CARTESIAN_POINT('Ctrl Pts',(2.58483843909759,-6.25655647198356,40.3219421487927));
#57708=CARTESIAN_POINT('Ctrl Pts',(2.75353582436312,-6.18417428724513,40.3305956130935));
#57709=CARTESIAN_POINT('Ctrl Pts',(2.91910892899455,-6.10500549227143,40.3392490773943));
#57710=CARTESIAN_POINT('Ctrl Pts',(3.0845295069299,-6.02590962795127,40.3478945700845));
#57711=CARTESIAN_POINT('Ctrl Pts',(3.24683127136244,-5.94003975356798,40.3565400627747));
#57712=CARTESIAN_POINT('Ctrl Pts',(3.4054589288059,-5.84766094128381,40.3651855554648));
#57713=CARTESIAN_POINT('Ctrl Pts',(3.56885862701655,-5.75250307101346,40.3740911329614));
#57714=CARTESIAN_POINT('Ctrl Pts',(3.72835940075996,-5.6504386328712,40.382996710458));
#57715=CARTESIAN_POINT('Ctrl Pts',(3.88337960349927,-5.54180943872359,40.3919022879545));
#57716=CARTESIAN_POINT('Ctrl Pts',(4.03358693126474,-5.43655282905661,40.4005313761271));
#57717=CARTESIAN_POINT('Ctrl Pts',(4.17958744935665,-5.32513315917595,40.4091604642996));
#57718=CARTESIAN_POINT('Ctrl Pts',(4.32087920515903,-5.20790667105549,40.4177895524722));
#57719=CARTESIAN_POINT('Ctrl Pts',(4.46896177036093,-5.08504600610086,40.4268333746307));
#57720=CARTESIAN_POINT('Ctrl Pts',(4.61187149305091,-4.9558067525573,40.4358771967892));
#57721=CARTESIAN_POINT('Ctrl Pts',(4.74906675487989,-4.82064870714457,40.4449210189478));
#57722=CARTESIAN_POINT('Ctrl Pts',(4.88626201670897,-4.68549066173174,40.4539648411063));
#57723=CARTESIAN_POINT('Ctrl Pts',(5.01774251887779,-4.54441407019152,40.4630086632648));
#57724=CARTESIAN_POINT('Ctrl Pts',(5.14300831224654,-4.39792615901666,40.4720524854234));
#57725=CARTESIAN_POINT('Ctrl Pts',(5.25971375290996,-4.26144886728546,40.4804782752732));
#57726=CARTESIAN_POINT('Ctrl Pts',(5.37097391419248,-4.12033448493361,40.488904065123));
#57727=CARTESIAN_POINT('Ctrl Pts',(5.47642802186094,-3.97505032941425,40.4973298549728));
#57728=CARTESIAN_POINT('Ctrl Pts',(5.58190659843003,-3.8297324630832,40.5057575998893));
#57729=CARTESIAN_POINT('Ctrl Pts',(5.6815762405327,-3.68024316275739,40.5141853448058));
#57730=CARTESIAN_POINT('Ctrl Pts',(5.77511892322488,-3.52707958835775,40.5226130897223));
#57731=CARTESIAN_POINT('Ctrl Pts',(5.86869597815981,-3.37385973402892,40.5310439314122));
#57732=CARTESIAN_POINT('Ctrl Pts',(5.95614141199291,-3.21696319640461,40.5394747731021));
#57733=CARTESIAN_POINT('Ctrl Pts',(6.03718246284654,-3.05691297067781,40.5479056147921));
#57734=CARTESIAN_POINT('Ctrl Pts',(6.11829798008194,-2.89671567922214,40.5563442033494));
#57735=CARTESIAN_POINT('Ctrl Pts',(6.19299720718392,-2.73335920601794,40.5647827919068));
#57736=CARTESIAN_POINT('Ctrl Pts',(6.26105450610643,-2.5673888430786,40.5732213804641));
#57737=CARTESIAN_POINT('Ctrl Pts',(6.32914749126888,-2.40133145261552,40.5816643938444));
#57738=CARTESIAN_POINT('Ctrl Pts',(6.39059148392767,-2.23265774820703,40.5901074072246));
#57739=CARTESIAN_POINT('Ctrl Pts',(6.44521011227507,-2.06193006880136,40.5985504206049));
#57740=CARTESIAN_POINT('Ctrl Pts',(6.49988612129841,-1.89102302806892,40.6070023039592));
#57741=CARTESIAN_POINT('Ctrl Pts',(6.54772234890497,-1.71805801963597,40.6154541873135));
#57742=CARTESIAN_POINT('Ctrl Pts',(6.58859283013561,-1.54361054631202,40.6239060706678));
#57743=CARTESIAN_POINT('Ctrl Pts',(6.59973132746635,-1.49606809862198,40.6262094758968));
#57744=CARTESIAN_POINT('Ctrl Pts',(6.61035274938802,-1.44841559263421,40.6285128811259));
#57745=CARTESIAN_POINT('Ctrl Pts',(6.62045521010196,-1.40066477468157,40.630816286355));
#57746=CARTESIAN_POINT('Ctrl Pts',(6.65693374423811,-1.22824343179927,40.6391335516884));
#57747=CARTESIAN_POINT('Ctrl Pts',(6.68670754520988,-1.05422956792178,40.6474508170218));
#57748=CARTESIAN_POINT('Ctrl Pts',(6.7096447804503,-0.879179117231563,40.6557680823552));
#57749=CARTESIAN_POINT('Ctrl Pts',(6.73256266989776,-0.70427630812673,40.6640783327153));
#57750=CARTESIAN_POINT('Ctrl Pts',(6.74865543694662,-0.52833899725857,40.6723885830754));
#57751=CARTESIAN_POINT('Ctrl Pts',(6.75784224608755,-0.351933483764263,
40.6806988334355));
#57752=CARTESIAN_POINT('Ctrl Pts',(6.76702298932,-0.175644448111405,40.6890035966654));
#57753=CARTESIAN_POINT('Ctrl Pts',(6.76930684277377,0.00111182795543882,
40.6973083598952));
#57754=CARTESIAN_POINT('Ctrl Pts',(6.76466474650015,0.17776351554252,40.7056131231251));
#57755=CARTESIAN_POINT('Ctrl Pts',(6.76002486556583,0.354330899961088,40.7139139230877));
#57756=CARTESIAN_POINT('Ctrl Pts',(6.74846563108645,0.530793448378331,40.7222147230503));
#57757=CARTESIAN_POINT('Ctrl Pts',(6.73001007095392,0.706578689785423,40.7305155230129));
#57758=CARTESIAN_POINT('Ctrl Pts',(6.71155994107486,0.88231220919593,40.7388138805979));
#57759=CARTESIAN_POINT('Ctrl Pts',(6.68621756648536,1.0573684733161,40.7471122381828));
#57760=CARTESIAN_POINT('Ctrl Pts',(6.65405790624388,1.23117926410141,40.7554105957677));
#57761=CARTESIAN_POINT('Ctrl Pts',(6.62189497383071,1.40500773973616,40.7637097976915));
#57762=CARTESIAN_POINT('Ctrl Pts',(6.58291342568409,1.57759014545674,40.7720089996153));
#57763=CARTESIAN_POINT('Ctrl Pts',(6.5372396140938,1.74836701751169,40.7803082015391));
#57764=CARTESIAN_POINT('Ctrl Pts',(6.49156117204478,1.91916120310433,40.7886082448446));
#57765=CARTESIAN_POINT('Ctrl Pts',(6.43918920361854,2.08814915383814,40.7969082881502));
#57766=CARTESIAN_POINT('Ctrl Pts',(6.38030034156562,2.2547852561647,40.8052083314557));
#57767=CARTESIAN_POINT('Ctrl Pts',(6.32139573361864,2.42146591419026,40.8135105940537));
#57768=CARTESIAN_POINT('Ctrl Pts',(6.25597087498801,2.5857931424035,40.8218128566516));
#57769=CARTESIAN_POINT('Ctrl Pts',(6.18425113812239,2.74723986223118,40.8301151192496));
#57770=CARTESIAN_POINT('Ctrl Pts',(6.11250031754195,2.90875655392457,40.8384209800922));
#57771=CARTESIAN_POINT('Ctrl Pts',(6.03444932246879,3.06738993135616,40.8467268409348));
#57772=CARTESIAN_POINT('Ctrl Pts',(5.95037027780558,3.22263596408405,40.8550327017774));
#57773=CARTESIAN_POINT('Ctrl Pts',(5.86619184577965,3.37806550857552,40.8633483807335));
#57774=CARTESIAN_POINT('Ctrl Pts',(5.77597129333123,3.53009940209645,40.8716640596897));
#57775=CARTESIAN_POINT('Ctrl Pts',(5.68002564840435,3.6782601367316,40.8799797386458));
#57776=CARTESIAN_POINT('Ctrl Pts',(5.58401931862118,3.82651458185144,40.8883006772027));
#57777=CARTESIAN_POINT('Ctrl Pts',(5.4822808751195,3.97089069870037,40.8966216157595));
#57778=CARTESIAN_POINT('Ctrl Pts',(5.37516881303009,4.11094262079012,40.9049425543164));
#57779=CARTESIAN_POINT('Ctrl Pts',(5.26789754923871,4.25120270341684,40.9132758603653));
#57780=CARTESIAN_POINT('Ctrl Pts',(5.1552369273305,4.38712547930825,40.9216091664143));
#57781=CARTESIAN_POINT('Ctrl Pts',(5.03758449860262,4.51829961594388,40.9299424724632));
#57782=CARTESIAN_POINT('Ctrl Pts',(4.95098536484261,4.61485152504757,40.9360762777148));
#57783=CARTESIAN_POINT('Ctrl Pts',(4.861682553003,4.70883144820397,40.9422100829664));
#57784=CARTESIAN_POINT('Ctrl Pts',(4.76984630227297,4.80008908799544,40.948343888218));
#57785=CARTESIAN_POINT('Ctrl Pts',(4.6479513616092,4.9212160340442,40.9564853336847));
#57786=CARTESIAN_POINT('Ctrl Pts',(4.52121319054477,5.03792146431372,40.9646267791515));
#57787=CARTESIAN_POINT('Ctrl Pts',(4.3899908637469,5.14978341449607,40.9727682246182));
#57788=CARTESIAN_POINT('Ctrl Pts',(4.26006191464205,5.26054281029919,40.9808294248689));
#57789=CARTESIAN_POINT('Ctrl Pts',(4.12573706105073,5.36655348541563,40.9888906251197));
#57790=CARTESIAN_POINT('Ctrl Pts',(3.98740513822656,5.46743900410827,40.9969518253704));
#57791=CARTESIAN_POINT('Ctrl Pts',(3.84700767776288,5.56983092010883,41.0051333934452));
#57792=CARTESIAN_POINT('Ctrl Pts',(3.70248276567876,5.66694309843023,41.0133149615198));
#57793=CARTESIAN_POINT('Ctrl Pts',(3.55427531661674,5.75842130915141,41.0214965295946));
#57794=CARTESIAN_POINT('Ctrl Pts',(3.40606786755482,5.84989951987252,41.0296780976693));
#57795=CARTESIAN_POINT('Ctrl Pts',(3.25417819184764,5.9357435028679,41.037859665744));
#57796=CARTESIAN_POINT('Ctrl Pts',(3.09908550384737,6.01564277861004,41.0460412338188));
#57797=CARTESIAN_POINT('Ctrl Pts',(3.09908550384713,6.01564277861016,39.0456530966623));
#57798=CARTESIAN_POINT('Ctrl Pts',(2.9446003203866,6.09522908555046,39.0538824990093));
#57799=CARTESIAN_POINT('Ctrl Pts',(2.78682478641158,6.16897536872828,39.0621119013562));
#57800=CARTESIAN_POINT('Ctrl Pts',(2.62623941930812,6.23659807206398,39.0703413037032));
#57801=CARTESIAN_POINT('Ctrl Pts',(2.46584144851121,6.30414186257548,39.078561102687));
#57802=CARTESIAN_POINT('Ctrl Pts',(2.30264050108509,6.36557616480819,39.0867809016708));
#57803=CARTESIAN_POINT('Ctrl Pts',(2.13714233615255,6.42066286570354,39.0950007006546));
#57804=CARTESIAN_POINT('Ctrl Pts',(1.97180409788713,6.47569633439248,39.103212556559));
#57805=CARTESIAN_POINT('Ctrl Pts',(1.80417340096941,6.52439430504693,39.1114244124634));
#57806=CARTESIAN_POINT('Ctrl Pts',(1.63477675133519,6.56656637621931,39.1196362683678));
#57807=CARTESIAN_POINT('Ctrl Pts',(1.46550982262301,6.60870615277448,39.12784183578));
#57808=CARTESIAN_POINT('Ctrl Pts',(1.29447998119713,6.6443298975055,39.1360474031922));
#57809=CARTESIAN_POINT('Ctrl Pts',(1.12222978257994,6.67329673512954,39.1442529706043));
#57810=CARTESIAN_POINT('Ctrl Pts',(0.950076953392023,6.70224719840702,39.1524538995811));
#57811=CARTESIAN_POINT('Ctrl Pts',(0.776705493949861,6.7245481917699,39.1606548285579));
#57812=CARTESIAN_POINT('Ctrl Pts',(0.602669155930628,6.74010970893574,39.1688557575347));
#57813=CARTESIAN_POINT('Ctrl Pts',(0.428678188946208,6.75566716923539,39.1770545485406));
#57814=CARTESIAN_POINT('Ctrl Pts',(0.254023044948438,6.76448861684865,39.1852533395464));
#57815=CARTESIAN_POINT('Ctrl Pts',(0.0792638848705898,6.7665357633397,39.1934521305523));
#57816=CARTESIAN_POINT('Ctrl Pts',(-0.0954753772327584,6.76858267674387,
39.2016499880486));
#57817=CARTESIAN_POINT('Ctrl Pts',(-0.270318273336021,6.76385682026826,
39.209847845545));
#57818=CARTESIAN_POINT('Ctrl Pts',(-0.444703345564633,6.75237202281122,
39.2180457030413));
#57819=CARTESIAN_POINT('Ctrl Pts',(-0.619100239948408,6.74088644676082,
39.2262441162982));
#57820=CARTESIAN_POINT('Ctrl Pts',(-0.793038890761985,6.7226410404945,39.2344425295551));
#57821=CARTESIAN_POINT('Ctrl Pts',(-0.965961612094605,6.69770163294541,
39.242640942812));
#57822=CARTESIAN_POINT('Ctrl Pts',(-1.1389274682706,6.67275600436631,39.2508414011285));
#57823=CARTESIAN_POINT('Ctrl Pts',(-1.31087653538488,6.64111309994968,39.2590418594451));
#57824=CARTESIAN_POINT('Ctrl Pts',(-1.48125993131168,6.60289012598957,39.2672423177616));
#57825=CARTESIAN_POINT('Ctrl Pts',(-1.6518057834008,6.56463070741214,39.275450595003));
#57826=CARTESIAN_POINT('Ctrl Pts',(-1.82078263170728,6.51977876420005,39.2836588722445));
#57827=CARTESIAN_POINT('Ctrl Pts',(-1.98765450752797,6.46850203360127,39.2918671494859));
#57828=CARTESIAN_POINT('Ctrl Pts',(-2.15461006186638,6.41719959009677,39.3000795427983));
#57829=CARTESIAN_POINT('Ctrl Pts',(-2.31945820115124,6.35946605453715,39.3082919361107));
#57830=CARTESIAN_POINT('Ctrl Pts',(-2.48168172307127,6.29551783615725,39.3165043294231));
#57831=CARTESIAN_POINT('Ctrl Pts',(-2.64412359806743,6.2314835433904,39.3247277766278));
#57832=CARTESIAN_POINT('Ctrl Pts',(-2.80393346830925,6.16121799693371,39.3329512238325));
#57833=CARTESIAN_POINT('Ctrl Pts',(-2.96061653670768,6.0849846937008,39.3411746710371));
#57834=CARTESIAN_POINT('Ctrl Pts',(-3.08466060653792,6.02463171946898,39.347685073659));
#57835=CARTESIAN_POINT('Ctrl Pts',(-3.20674532188333,5.96053928021444,39.3541954762809));
#57836=CARTESIAN_POINT('Ctrl Pts',(-3.32663794447513,5.89285745512127,39.3607058789027));
#57837=CARTESIAN_POINT('Ctrl Pts',(-3.49118429266487,5.79996769328983,39.369641065685));
#57838=CARTESIAN_POINT('Ctrl Pts',(-3.65194238196678,5.70012322094762,39.3785762524673));
#57839=CARTESIAN_POINT('Ctrl Pts',(-3.80834113109411,5.59364164290284,39.3875114392495));
#57840=CARTESIAN_POINT('Ctrl Pts',(-3.9645056432784,5.48731954132109,39.3964332438862));
#57841=CARTESIAN_POINT('Ctrl Pts',(-4.11632362974265,5.37438031348778,39.4053550485228));
#57842=CARTESIAN_POINT('Ctrl Pts',(-4.2632510875454,5.25518593053975,39.4142768531594));
#57843=CARTESIAN_POINT('Ctrl Pts',(-4.40982015443415,5.13628229095915,39.4231768953987));
#57844=CARTESIAN_POINT('Ctrl Pts',(-4.55152230097991,5.01115411069876,39.432076937638));
#57845=CARTESIAN_POINT('Ctrl Pts',(-4.68784530566999,4.88020444142536,39.4409769798773));
#57846=CARTESIAN_POINT('Ctrl Pts',(-4.82395843909019,4.74945637109297,39.4498633203707));
#57847=CARTESIAN_POINT('Ctrl Pts',(-4.95470876426148,4.61290486721666,39.4587496608641));
#57848=CARTESIAN_POINT('Ctrl Pts',(-5.07961745791228,4.47099267291648,39.4676360013575));
#57849=CARTESIAN_POINT('Ctrl Pts',(-5.20420678183671,4.32944332332579,39.4764996210295));
#57850=CARTESIAN_POINT('Ctrl Pts',(-5.3229841079977,4.18256082681411,39.4853632407014));
#57851=CARTESIAN_POINT('Ctrl Pts',(-5.43550828445764,4.03082357460512,39.4942268603733));
#57852=CARTESIAN_POINT('Ctrl Pts',(-5.54232798026772,3.88677873345232,39.502641133527));
#57853=CARTESIAN_POINT('Ctrl Pts',(-5.64351257316431,3.73835929877524,39.5110554066807));
#57854=CARTESIAN_POINT('Ctrl Pts',(-5.73871556846863,3.58600510655183,39.5194696798344));
#57855=CARTESIAN_POINT('Ctrl Pts',(-5.83161013071872,3.4373451200848,39.527679928039));
#57856=CARTESIAN_POINT('Ctrl Pts',(-5.91871951545199,3.28508121074497,39.5358901762436));
#57857=CARTESIAN_POINT('Ctrl Pts',(-5.99976880637994,3.12970657889686,39.5441004244481));
#57858=CARTESIAN_POINT('Ctrl Pts',(-6.08083736434019,2.9742950114011,39.5523126243924));
#57859=CARTESIAN_POINT('Ctrl Pts',(-6.15584279376882,2.81577156373658,39.5605248243366));
#57860=CARTESIAN_POINT('Ctrl Pts',(-6.22455695618284,2.65465246298565,39.5687370242809));
#57861=CARTESIAN_POINT('Ctrl Pts',(-6.29329968938915,2.49346637021739,39.5769526387914));
#57862=CARTESIAN_POINT('Ctrl Pts',(-6.35574580469699,2.32968280140303,39.5851682533019));
#57863=CARTESIAN_POINT('Ctrl Pts',(-6.4117159255237,2.16383638253583,39.5933838678123));
#57864=CARTESIAN_POINT('Ctrl Pts',(-6.46774889834276,1.9978037254098,39.6016087080978));
#57865=CARTESIAN_POINT('Ctrl Pts',(-6.51729123776591,1.82970392883746,39.6098335483833));
#57866=CARTESIAN_POINT('Ctrl Pts',(-6.56021365311348,1.66008608978676,39.6180583886687));
#57867=CARTESIAN_POINT('Ctrl Pts',(-6.60316356176015,1.49035960461389,39.6262884972503));
#57868=CARTESIAN_POINT('Ctrl Pts',(-6.6394850198573,1.31911348591226,39.6345186058319));
#57869=CARTESIAN_POINT('Ctrl Pts',(-6.66910018189931,1.14690529852754,39.6427487144135));
#57870=CARTESIAN_POINT('Ctrl Pts',(-6.69875594678292,0.974461011075437,
39.6509901066002));
#57871=CARTESIAN_POINT('Ctrl Pts',(-6.72168700417267,0.801052372189292,
39.659231498787));
#57872=CARTESIAN_POINT('Ctrl Pts',(-6.73786741612785,0.627241327307671,
39.6674728909737));
#57873=CARTESIAN_POINT('Ctrl Pts',(-6.74490954249729,0.551594344656564,
39.6710597542378));
#57874=CARTESIAN_POINT('Ctrl Pts',(-6.75067362222021,0.475871132458775,
39.6746466175018));
#57875=CARTESIAN_POINT('Ctrl Pts',(-6.75516059642061,0.400117878338753,
39.6782334807659));
#57876=CARTESIAN_POINT('Ctrl Pts',(-6.7630608671859,0.266738190342119,39.6845489151139));
#57877=CARTESIAN_POINT('Ctrl Pts',(-6.76700804548976,0.133175820827996,
39.6908643494619));
#57878=CARTESIAN_POINT('Ctrl Pts',(-6.76699998768909,-0.00040818611676218,
39.6971797838099));
#57879=CARTESIAN_POINT('',(-6.76699837066092,-0.00360871217654551,39.3028202161897));
#57880=CARTESIAN_POINT('Ctrl Pts',(3.09908550384735,6.01564277861005,38.6513967904261));
#57881=CARTESIAN_POINT('Ctrl Pts',(2.93373232018349,6.1008279655247,38.6601462383254));
#57882=CARTESIAN_POINT('Ctrl Pts',(2.76486502144451,6.17919158180179,38.6688956862246));
#57883=CARTESIAN_POINT('Ctrl Pts',(2.59305716434381,6.25046746591367,38.6776451341239));
#57884=CARTESIAN_POINT('Ctrl Pts',(2.42125069459311,6.32174277447214,38.6863945113713));
#57885=CARTESIAN_POINT('Ctrl Pts',(2.24650397871084,6.38593035557817,38.6951438886188));
#57886=CARTESIAN_POINT('Ctrl Pts',(2.06941053323796,6.44281220003531,38.7038932658662));
#57887=CARTESIAN_POINT('Ctrl Pts',(1.89231845896707,6.49969360406678,38.7126425753688));
#57888=CARTESIAN_POINT('Ctrl Pts',(1.71287996431528,6.54926929700875,38.7213918848714));
#57889=CARTESIAN_POINT('Ctrl Pts',(1.53170449173527,6.59137090065474,38.730141194374));
#57890=CARTESIAN_POINT('Ctrl Pts',(1.35053036178192,6.63347219230079,38.7388904390386));
#57891=CARTESIAN_POINT('Ctrl Pts',(1.16761955878866,6.6680994406245,38.7476396837031));
#57892=CARTESIAN_POINT('Ctrl Pts',(0.983593309310698,6.69513503985388,38.7563889283677));
#57893=CARTESIAN_POINT('Ctrl Pts',(0.79956836246001,6.72217044771214,38.7651381111009));
#57894=CARTESIAN_POINT('Ctrl Pts',(0.614428268438438,6.74161427235979,38.7738872938341));
#57895=CARTESIAN_POINT('Ctrl Pts',(0.428801816329926,6.75340047696804,38.7826364765673));
#57896=CARTESIAN_POINT('Ctrl Pts',(0.243176616522485,6.76518660206243,38.7913856002754));
#57897=CARTESIAN_POINT('Ctrl Pts',(0.0570653511652053,6.76931519233997,
38.8001347239836));
#57898=CARTESIAN_POINT('Ctrl Pts',(-0.128899900800241,6.76577222610795,
38.8088838476917));
#57899=CARTESIAN_POINT('Ctrl Pts',(-0.314863959942378,6.76222928260132,
38.817632915281));
#57900=CARTESIAN_POINT('Ctrl Pts',(-0.500681721081183,6.75101488651273,
38.8263819828702));
#57901=CARTESIAN_POINT('Ctrl Pts',(-0.685722110173944,6.73216712415984,
38.8351310504595));
#57902=CARTESIAN_POINT('Ctrl Pts',(-0.870761373828287,6.71331947644136,
38.8438800648359));
#57903=CARTESIAN_POINT('Ctrl Pts',(-1.05502298984414,6.68683858439985,38.8526290792122));
#57904=CARTESIAN_POINT('Ctrl Pts',(-1.23788117676133,6.65281438131412,38.8613780935886));
#57905=CARTESIAN_POINT('Ctrl Pts',(-1.43009641451857,6.61704912302363,38.8705748044761));
#57906=CARTESIAN_POINT('Ctrl Pts',(-1.62076048992751,6.57294837083151,38.8797715153636));
#57907=CARTESIAN_POINT('Ctrl Pts',(-1.80915798961178,6.52067760042036,38.8889682262511));
#57908=CARTESIAN_POINT('Ctrl Pts',(-1.98840443003049,6.47094578577397,38.8977182239576));
#57909=CARTESIAN_POINT('Ctrl Pts',(-2.16559895952219,6.41381888474466,38.9064682216642));
#57910=CARTESIAN_POINT('Ctrl Pts',(-2.3401396624234,6.34949095285228,38.9152182193707));
#57911=CARTESIAN_POINT('Ctrl Pts',(-2.51467682554033,6.28516432556678,38.9239680396223));
#57912=CARTESIAN_POINT('Ctrl Pts',(-2.68656000078861,6.21363705879653,38.9327178598738));
#57913=CARTESIAN_POINT('Ctrl Pts',(-2.85520533840908,6.1351521151085,38.9414676801254));
#57914=CARTESIAN_POINT('Ctrl Pts',(-3.02384747998342,6.05666865881114,38.9502173345567));
#57915=CARTESIAN_POINT('Ctrl Pts',(-3.18925164684548,5.97122791039838,38.9589669889879));
#57916=CARTESIAN_POINT('Ctrl Pts',(-3.35085601829165,5.87912008251904,38.9677166434192));
#57917=CARTESIAN_POINT('Ctrl Pts',(-3.5124575419142,5.78701387778173,38.9764661436623));
#57918=CARTESIAN_POINT('Ctrl Pts',(-3.67025915510932,5.68824097060985,38.9852156439055));
#57919=CARTESIAN_POINT('Ctrl Pts',(-3.82372487928825,5.58313684656861,38.9939651441486));
#57920=CARTESIAN_POINT('Ctrl Pts',(-3.97718810300799,5.47803443501773,39.0027145018337));
#57921=CARTESIAN_POINT('Ctrl Pts',(-4.12631534263035,5.36660117496369,39.0114638595188));
#57922=CARTESIAN_POINT('Ctrl Pts',(-4.27060009886244,5.24921554097335,39.020213217204));
#57923=CARTESIAN_POINT('Ctrl Pts',(-4.41488269594222,5.13183166360283,39.0289624439591));
#57924=CARTESIAN_POINT('Ctrl Pts',(-4.55432273235087,5.00849577139471,39.0377116707143));
#57925=CARTESIAN_POINT('Ctrl Pts',(-4.68844662480197,4.87962675277352,39.0464608974695));
#57926=CARTESIAN_POINT('Ctrl Pts',(-4.82256868835139,4.750759491399,39.055210004921));
#57927=CARTESIAN_POINT('Ctrl Pts',(-4.95137454637836,4.61635945312553,39.0639591123725));
#57928=CARTESIAN_POINT('Ctrl Pts',(-5.07442674461044,4.47688309134629,39.0727082198239));
#57929=CARTESIAN_POINT('Ctrl Pts',(-5.19747742838505,4.33740844616392,39.0814572195963));
#57930=CARTESIAN_POINT('Ctrl Pts',(-5.31477440450893,4.19285781736072,39.0902062193687));
#57931=CARTESIAN_POINT('Ctrl Pts',(-5.42591931531119,4.04372211999451,39.0989552191411));
#57932=CARTESIAN_POINT('Ctrl Pts',(-5.53707636462952,3.89457013500843,39.1077051744216));
#57933=CARTESIAN_POINT('Ctrl Pts',(-5.64207983273445,3.74083230916458,39.1164551297022));
#57934=CARTESIAN_POINT('Ctrl Pts',(-5.74057303468726,3.58303087251862,39.1252050849828));
#57935=CARTESIAN_POINT('Ctrl Pts',(-5.83906243363743,3.42523552887469,39.1339547024116));
#57936=CARTESIAN_POINT('Ctrl Pts',(-5.93104191768403,3.26337713157034,39.1427043198404));
#57937=CARTESIAN_POINT('Ctrl Pts',(-6.01619906699632,3.09800545291201,39.1514539372692));
#57938=CARTESIAN_POINT('Ctrl Pts',(-6.10135338095369,2.93263928039626,39.1602032633746));
#57939=CARTESIAN_POINT('Ctrl Pts',(-6.17968568352833,2.76376031540238,39.16895258948));
#57940=CARTESIAN_POINT('Ctrl Pts',(-6.25092992694887,2.5919421383154,39.1777019155854));
#57941=CARTESIAN_POINT('Ctrl Pts',(-6.32217217691103,2.42012876880821,39.1864509968792));
#57942=CARTESIAN_POINT('Ctrl Pts',(-6.38632665483849,2.24537661647675,39.195200078173));
#57943=CARTESIAN_POINT('Ctrl Pts',(-6.44317547869347,2.06827917621465,39.2039491594668));
#57944=CARTESIAN_POINT('Ctrl Pts',(-6.50002944235934,1.89116572423431,39.2126990317818));
#57945=CARTESIAN_POINT('Ctrl Pts',(-6.54957634250397,1.71170683289204,39.2214489040967));
#57946=CARTESIAN_POINT('Ctrl Pts',(-6.59164787708394,1.53051209225369,39.2301987764117));
#57947=CARTESIAN_POINT('Ctrl Pts',(-6.63371649075009,1.34932993148028,39.2389480412465));
#57948=CARTESIAN_POINT('Ctrl Pts',(-6.66831071257125,1.16641244173996,39.2476973060813));
#57949=CARTESIAN_POINT('Ctrl Pts',(-6.69531304840335,0.982380875159863,
39.2564465709161));
#57950=CARTESIAN_POINT('Ctrl Pts',(-6.72231677033045,0.79833986179569,39.2651962848717));
#57951=CARTESIAN_POINT('Ctrl Pts',(-6.74172778477891,0.613184940729997,
39.2739459988274));
#57952=CARTESIAN_POINT('Ctrl Pts',(-6.75348015835519,0.427545027690393,
39.282695712783));
#57953=CARTESIAN_POINT('Ctrl Pts',(-6.76249038365212,0.285219953548298,
39.2894038805853));
#57954=CARTESIAN_POINT('Ctrl Pts',(-6.7669999999999,0.142609995760424,39.2961120483875));
#57955=CARTESIAN_POINT('Ctrl Pts',(-6.767,4.67741087612267E-12,39.3028202161897));
#57956=CARTESIAN_POINT('Ctrl Pts',(-6.76699724104549,-0.00611062049019318,
39.3028202161897));
#57957=CARTESIAN_POINT('Ctrl Pts',(-6.76678101224438,-0.245565795769802,
39.3141020673561));
#57958=CARTESIAN_POINT('Ctrl Pts',(-6.75385175166444,-0.484454529984376,
39.3253839185225));
#57959=CARTESIAN_POINT('Ctrl Pts',(-6.72840805681548,-0.721674456372541,
39.3366657696888));
#57960=CARTESIAN_POINT('Ctrl Pts',(-6.70195509449772,-0.968304114958578,
39.3483951346868));
#57961=CARTESIAN_POINT('Ctrl Pts',(-6.66197504121415,-1.21313061101869,
39.3601244996846));
#57962=CARTESIAN_POINT('Ctrl Pts',(-6.6087384623976,-1.45494499402095,39.3718538646825));
#57963=CARTESIAN_POINT('Ctrl Pts',(-6.58712569453163,-1.55311580519366,
39.3766157041649));
#57964=CARTESIAN_POINT('Ctrl Pts',(-6.56332857647657,-1.65079044562883,
39.3813775436472));
#57965=CARTESIAN_POINT('Ctrl Pts',(-6.53736745489185,-1.7478889437607,39.3861393831296));
#57966=CARTESIAN_POINT('Ctrl Pts',(-6.4933628341328,-1.91247284174916,39.3942107963716));
#57967=CARTESIAN_POINT('Ctrl Pts',(-6.44305781121587,-2.0756966424793,39.4022822096136));
#57968=CARTESIAN_POINT('Ctrl Pts',(-6.38654762293997,-2.23702893587005,
39.4103536228556));
#57969=CARTESIAN_POINT('Ctrl Pts',(-6.33010837852473,-2.39815868992951,
39.4184149031069));
#57970=CARTESIAN_POINT('Ctrl Pts',(-6.26747959072336,-2.55740131402768,
39.4264761833581));
#57971=CARTESIAN_POINT('Ctrl Pts',(-6.19880741801831,-2.71423572932072,
39.4345374636094));
#57972=CARTESIAN_POINT('Ctrl Pts',(-6.13020639741324,-2.87090764650779,
39.442590391467));
#57973=CARTESIAN_POINT('Ctrl Pts',(-6.05557460105233,-3.0251759816103,39.4506433193246));
#57974=CARTESIAN_POINT('Ctrl Pts',(-5.97510786264064,-3.17653506667407,
39.4586962471822));
#57975=CARTESIAN_POINT('Ctrl Pts',(-5.89470687645742,-3.32777047085628,
39.4667425947065));
#57976=CARTESIAN_POINT('Ctrl Pts',(-5.80848061223211,-3.47610102889844,
39.4747889422309));
#57977=CARTESIAN_POINT('Ctrl Pts',(-5.71667281695634,-3.6210414115103,39.4828352897553));
#57978=CARTESIAN_POINT('Ctrl Pts',(-5.62491995828841,-3.76589506365514,
39.4908768224485));
#57979=CARTESIAN_POINT('Ctrl Pts',(-5.52759241645241,-3.90736226452003,
39.4989183551416));
#57980=CARTESIAN_POINT('Ctrl Pts',(-5.42497959273133,-4.04498274637218,
39.5069598878348));
#57981=CARTESIAN_POINT('Ctrl Pts',(-5.32039406441056,-4.18524894586192,
39.515156016883));
#57982=CARTESIAN_POINT('Ctrl Pts',(-5.21031815682281,-4.32151866788484,
39.5233521459313));
#57983=CARTESIAN_POINT('Ctrl Pts',(-5.09510456143018,-4.45333566083822,
39.5315482749795));
#57984=CARTESIAN_POINT('Ctrl Pts',(-4.98210315892401,-4.58262166243479,
39.5395870318156));
#57985=CARTESIAN_POINT('Ctrl Pts',(-4.86415984724632,-4.70762410039903,
39.5476257886517));
#57986=CARTESIAN_POINT('Ctrl Pts',(-4.74164766469593,-4.8279463981991,39.5556645454878));
#57987=CARTESIAN_POINT('Ctrl Pts',(-4.61912362426101,-4.948280341926,39.5637040803906));
#57988=CARTESIAN_POINT('Ctrl Pts',(-4.49203009881134,-5.06393298172611,
39.5717436152934));
#57989=CARTESIAN_POINT('Ctrl Pts',(-4.36077628353313,-5.17454531383918,
39.5797831501962));
#57990=CARTESIAN_POINT('Ctrl Pts',(-4.22948377597157,-5.2851902533373,39.5878250550717));
#57991=CARTESIAN_POINT('Ctrl Pts',(-4.094028822871,-5.39079168710017,39.5958669599473));
#57992=CARTESIAN_POINT('Ctrl Pts',(-3.9548527875009,-5.49103163614965,39.6039088648228));
#57993=CARTESIAN_POINT('Ctrl Pts',(-3.8109820268197,-5.59465290745577,39.6122220415036));
#57994=CARTESIAN_POINT('Ctrl Pts',(-3.66313510567491,-5.69254440155902,
39.6205352181844));
#57995=CARTESIAN_POINT('Ctrl Pts',(-3.51183001016619,-5.78440480773054,
39.6288483948653));
#57996=CARTESIAN_POINT('Ctrl Pts',(-3.36520810316052,-5.87342195474662,
39.6369042624758));
#57997=CARTESIAN_POINT('Ctrl Pts',(-3.21533926440627,-5.9567756841761,39.6449601300863));
#57998=CARTESIAN_POINT('Ctrl Pts',(-3.06271740221846,-6.03423989530978,
39.6530159976969));
#57999=CARTESIAN_POINT('Ctrl Pts',(-2.90278329421852,-6.11541548399668,
39.6614578289128));
#58000=CARTESIAN_POINT('Ctrl Pts',(-2.73982631511816,-6.19012312421717,
39.6698996601288));
#58001=CARTESIAN_POINT('Ctrl Pts',(-2.57443460704302,-6.25816070855161,
39.6783414913447));
#58002=CARTESIAN_POINT('Ctrl Pts',(-2.40904289896788,-6.32619829288606,
39.6867833225607));
#58003=CARTESIAN_POINT('Ctrl Pts',(-2.24121692436823,-6.38756574335857,
39.6952251537767));
#58004=CARTESIAN_POINT('Ctrl Pts',(-2.07155830167522,-6.44212194876506,
39.7036669849926));
#58005=CARTESIAN_POINT('Ctrl Pts',(-1.90614776400091,-6.49531212045522,
39.7118974410592));
#58006=CARTESIAN_POINT('Ctrl Pts',(-1.73844521549067,-6.54220532803548,
39.7201278971258));
#58007=CARTESIAN_POINT('Ctrl Pts',(-1.56897070613128,-6.58259978453057,
39.7283583531923));
#58008=CARTESIAN_POINT('Ctrl Pts',(-1.39969737300103,-6.62294629042551,
39.7365790392226));
#58009=CARTESIAN_POINT('Ctrl Pts',(-1.22865661273056,-6.65680932401883,
39.7447997252528));
#58010=CARTESIAN_POINT('Ctrl Pts',(-1.05638602562939,-6.68403602360542,
39.753020411283));
#58011=CARTESIAN_POINT('Ctrl Pts',(-0.884285371057839,-6.71123586601336,
39.7612329881984));
#58012=CARTESIAN_POINT('Ctrl Pts',(-0.710957657292857,-6.73181235564676,
39.7694455651138));
#58013=CARTESIAN_POINT('Ctrl Pts',(-0.53695323243361,-6.7456630679407,39.7776581420292));
#58014=CARTESIAN_POINT('Ctrl Pts',(-0.363085552281877,-6.7595028953873,
39.7858642649339));
#58015=CARTESIAN_POINT('Ctrl Pts',(-0.188542576060101,-6.76662744487597,
39.7940703878385));
#58016=CARTESIAN_POINT('Ctrl Pts',(-0.0138824708663815,-6.76698576007092,
39.8022765107431));
#58017=CARTESIAN_POINT('Ctrl Pts',(0.160675394972847,-6.76734386552185,
39.8104778300969));
#58018=CARTESIAN_POINT('Ctrl Pts',(0.335349895637805,-6.76094362610986,
39.8186791494506));
#58019=CARTESIAN_POINT('Ctrl Pts',(0.509580051723304,-6.74778609403749,
39.8268804688043));
#58020=CARTESIAN_POINT('Ctrl Pts',(0.683760225305153,-6.73463233654932,
39.8350794353939));
#58021=CARTESIAN_POINT('Ctrl Pts',(0.857495950865726,-6.71472517069232,
39.8432784019833));
#58022=CARTESIAN_POINT('Ctrl Pts',(1.03022830809612,-6.68811771974727,39.8514773685729));
#58023=CARTESIAN_POINT('Ctrl Pts',(1.20293785523847,-6.6615137824363,39.8596752524518));
#58024=CARTESIAN_POINT('Ctrl Pts',(1.37464394349423,-6.6282113760114,39.8678731363308));
#58025=CARTESIAN_POINT('Ctrl Pts',(1.54479480779287,-6.58831526278276,39.8760710202097));
#58026=CARTESIAN_POINT('Ctrl Pts',(1.71495411129512,-6.54841717077237,39.8842693106903));
#58027=CARTESIAN_POINT('Ctrl Pts',(1.88355768798516,-6.50192480225152,39.8924676011708));
#58028=CARTESIAN_POINT('Ctrl Pts',(2.05006591133739,-6.44899362375033,39.9006658916513));
#58029=CARTESIAN_POINT('Ctrl Pts',(2.21661263984078,-6.39605020487453,39.9088660779927));
#58030=CARTESIAN_POINT('Ctrl Pts',(2.38106270823189,-6.33666511902945,39.917066264334));
#58031=CARTESIAN_POINT('Ctrl Pts',(2.54289349365061,-6.2710431093997,39.9252664506754));
#58032=CARTESIAN_POINT('Ctrl Pts',(2.70487727737897,-6.20535905930884,39.9334743896495));
#58033=CARTESIAN_POINT('Ctrl Pts',(2.86423649795181,-6.13342643977186,39.9416823286236));
#58034=CARTESIAN_POINT('Ctrl Pts',(3.02046944019675,-6.05549777977315,39.9498902675977));
#58035=CARTESIAN_POINT('Ctrl Pts',(3.17677817577527,-5.97753131422052,39.9581021884916));
#58036=CARTESIAN_POINT('Ctrl Pts',(3.32995729490357,-5.89356318088711,39.9663141093856));
#58037=CARTESIAN_POINT('Ctrl Pts',(3.47953147935324,-5.80389090905316,39.9745260302796));
#58038=CARTESIAN_POINT('Ctrl Pts',(3.6293107811016,-5.71409566590411,39.9827492125221));
#58039=CARTESIAN_POINT('Ctrl Pts',(3.77547496826922,-5.61858084776005,39.9909723947647));
#58040=CARTESIAN_POINT('Ctrl Pts',(3.91757840077306,-5.51768687710678,39.9991955770072));
#58041=CARTESIAN_POINT('Ctrl Pts',(4.04429880004363,-5.42771491780995,40.0065285802901));
#58042=CARTESIAN_POINT('Ctrl Pts',(4.16779034346317,-5.33346607268934,40.0138615835729));
#58043=CARTESIAN_POINT('Ctrl Pts',(4.28776083656118,-5.23520735104658,40.0211945868557));
#58044=CARTESIAN_POINT('Ctrl Pts',(4.43394361090994,-5.11548014010676,40.030129773638));
#58045=CARTESIAN_POINT('Ctrl Pts',(4.57520177472949,-4.98955074287292,40.0390649604202));
#58046=CARTESIAN_POINT('Ctrl Pts',(4.71102716015007,-4.85782997812073,40.0480001472025));
#58047=CARTESIAN_POINT('Ctrl Pts',(4.84664912116181,-4.7263064903254,40.0569219518391));
#58048=CARTESIAN_POINT('Ctrl Pts',(4.97685435412913,-4.5890091214301,40.0658437564758));
#58049=CARTESIAN_POINT('Ctrl Pts',(5.10116897555833,-4.44638775668533,40.0747655611124));
#58050=CARTESIAN_POINT('Ctrl Pts',(5.22518036414416,-4.3041142792724,40.0836656033517));
#58051=CARTESIAN_POINT('Ctrl Pts',(5.34332964903508,-4.15654291920981,40.092565645591));
#58052=CARTESIAN_POINT('Ctrl Pts',(5.45518130116827,-4.00415858469467,40.1014656878302));
#58053=CARTESIAN_POINT('Ctrl Pts',(5.56686075603846,-3.85200884810301,40.1103520283236));
#58054=CARTESIAN_POINT('Ctrl Pts',(5.67226176565813,-3.69506112459502,40.1192383688171));
#58055=CARTESIAN_POINT('Ctrl Pts',(5.77098851009418,-3.53383369959043,40.1281247093105));
#58056=CARTESIAN_POINT('Ctrl Pts',(5.86946282747804,-3.37301850496838,40.1369883289824));
#58057=CARTESIAN_POINT('Ctrl Pts',(5.96129679718971,-3.20794566347558,40.1458519486543));
#58058=CARTESIAN_POINT('Ctrl Pts',(6.04613782496832,-3.03916212161961,40.1547155683262));
#58059=CARTESIAN_POINT('Ctrl Pts',(6.1266777859317,-2.87893516270284,40.1631298414799));
#58060=CARTESIAN_POINT('Ctrl Pts',(6.20091602757362,-2.71536458494684,40.1715441146336));
#58061=CARTESIAN_POINT('Ctrl Pts',(6.26858660046434,-2.54894312068333,40.1799583877873));
#58062=CARTESIAN_POINT('Ctrl Pts',(6.3346163322578,-2.38655695812284,40.1881686359919));
#58063=CARTESIAN_POINT('Ctrl Pts',(6.39432863137815,-2.22161216636013,40.1963788841964));
#58064=CARTESIAN_POINT('Ctrl Pts',(6.44753721662558,-2.05464177905252,40.204589132401));
#58065=CARTESIAN_POINT('Ctrl Pts',(6.50075845061444,-1.88763169955526,40.2128013323452));
#58066=CARTESIAN_POINT('Ctrl Pts',(6.54747278245295,-1.71859540432895,40.2210135322894));
#58067=CARTESIAN_POINT('Ctrl Pts',(6.58754396417207,-1.54808059224971,40.2292257322336));
#58068=CARTESIAN_POINT('Ctrl Pts',(6.62763180716421,-1.37749488149171,40.2374413467441));
#58069=CARTESIAN_POINT('Ctrl Pts',(6.66107091582961,-1.20542977537698,40.2456569612546));
#58070=CARTESIAN_POINT('Ctrl Pts',(6.68777623666107,-1.03244273853398,40.2538725757651));
#58071=CARTESIAN_POINT('Ctrl Pts',(6.71451154639715,-0.859261444831786,
40.2620974160506));
#58072=CARTESIAN_POINT('Ctrl Pts',(6.73449791071248,-0.685156504510114,
40.270322256336));
#58073=CARTESIAN_POINT('Ctrl Pts',(6.74770210147544,-0.510691051168863,
40.2785470966214));
#58074=CARTESIAN_POINT('Ctrl Pts',(6.76091474998158,-0.336113846640106,
40.286777205203));
#58075=CARTESIAN_POINT('Ctrl Pts',(6.7673365519278,-0.161176023548126,40.2950073137846));
#58076=CARTESIAN_POINT('Ctrl Pts',(6.76698641441174,0.0135597627938511,
40.3032374223661));
#58077=CARTESIAN_POINT('Ctrl Pts',(6.76663579685176,0.188535114580424,40.3114788145528));
#58078=CARTESIAN_POINT('Ctrl Pts',(6.75949470964332,0.363307521746561,40.3197202067395));
#58079=CARTESIAN_POINT('Ctrl Pts',(6.74563394985275,0.537318913303875,40.3279615989262));
#58080=CARTESIAN_POINT('Ctrl Pts',(6.73960139503915,0.613053091921744,40.3315484621904));
#58081=CARTESIAN_POINT('Ctrl Pts',(6.73229664967877,0.688643237948223,40.3351353254546));
#58082=CARTESIAN_POINT('Ctrl Pts',(6.72372856026666,0.764044009108428,40.3387221887188));
#58083=CARTESIAN_POINT('Ctrl Pts',(6.70354713635535,0.941644271294464,40.3471707476174));
#58084=CARTESIAN_POINT('Ctrl Pts',(6.67630725626448,1.11859816690005,40.355619306516));
#58085=CARTESIAN_POINT('Ctrl Pts',(6.64206440465825,1.29432200181096,40.3640678654146));
#58086=CARTESIAN_POINT('Ctrl Pts',(6.6078528846049,1.46988505278098,40.3725086940437));
#58087=CARTESIAN_POINT('Ctrl Pts',(6.56665122883549,1.64421996076122,40.3809495226729));
#58088=CARTESIAN_POINT('Ctrl Pts',(6.51856653089795,1.81674967517736,40.389390351302));
#58089=CARTESIAN_POINT('Ctrl Pts',(6.47051843501161,1.98914806004979,40.397824754776));
#58090=CARTESIAN_POINT('Ctrl Pts',(6.41559783096888,2.15974367059655,40.4062591582501));
#58091=CARTESIAN_POINT('Ctrl Pts',(6.35396263276272,2.32797076043817,40.4146935617241));
#58092=CARTESIAN_POINT('Ctrl Pts',(6.29236488592939,2.49609563051501,40.4231228402047));
#58093=CARTESIAN_POINT('Ctrl Pts',(6.22406079385863,2.66185453694141,40.4315521186853));
#58094=CARTESIAN_POINT('Ctrl Pts',(6.14925787681769,2.82469760583246,40.4399813971658));
#58095=CARTESIAN_POINT('Ctrl Pts',(6.07104937984889,2.99495449103902,40.4487944385093));
#58096=CARTESIAN_POINT('Ctrl Pts',(5.98573656891452,3.16202346297437,40.4576074798528));
#58097=CARTESIAN_POINT('Ctrl Pts',(5.89361308808811,3.32529904939639,40.4664205211963));
#58098=CARTESIAN_POINT('Ctrl Pts',(5.80556200177603,3.48135690374288,40.4748439747723));
#58099=CARTESIAN_POINT('Ctrl Pts',(5.71128960475681,3.63394921250901,40.4832674283484));
#58100=CARTESIAN_POINT('Ctrl Pts',(5.61109946859779,3.78257210816946,40.4916908819245));
#58101=CARTESIAN_POINT('Ctrl Pts',(5.51092010916819,3.93117901753833,40.5001134294505));
#58102=CARTESIAN_POINT('Ctrl Pts',(5.40482446599098,4.07581708866082,40.5085359769765));
#58103=CARTESIAN_POINT('Ctrl Pts',(5.29315957063137,4.2160112381057,40.5169585245025));
#58104=CARTESIAN_POINT('Ctrl Pts',(5.18149111520029,4.35620985718439,40.525381340554));
#58105=CARTESIAN_POINT('Ctrl Pts',(5.06425326169615,4.49196401166464,40.5338041566055));
#58106=CARTESIAN_POINT('Ctrl Pts',(4.94183370014266,4.6228312407154,40.542226972657));
#58107=CARTESIAN_POINT('Ctrl Pts',(4.81939316380426,4.75372089193421,40.5506512318337));
#58108=CARTESIAN_POINT('Ctrl Pts',(4.69176937762932,4.87972170546081,40.5590754910104));
#58109=CARTESIAN_POINT('Ctrl Pts',(4.55938754390115,5.00042740418447,40.5674997501871));
#58110=CARTESIAN_POINT('Ctrl Pts',(4.42692011906221,5.1212111448459,40.5759294560455));
#58111=CARTESIAN_POINT('Ctrl Pts',(4.28968874691289,5.23669270582208,40.5843591619038));
#58112=CARTESIAN_POINT('Ctrl Pts',(4.14815314656469,5.34650488381386,40.5927888677621));
#58113=CARTESIAN_POINT('Ctrl Pts',(4.00656615436389,5.4563569348217,40.6012216344631));
#58114=CARTESIAN_POINT('Ctrl Pts',(3.86067208477238,5.56053529876295,40.6096544011641));
#58115=CARTESIAN_POINT('Ctrl Pts',(3.7109608657171,5.65871526524495,40.618087167865));
#58116=CARTESIAN_POINT('Ctrl Pts',(3.56112336055373,5.75697804960752,40.6265270478692));
#58117=CARTESIAN_POINT('Ctrl Pts',(3.40746255645117,5.84923215213074,40.6349669278733));
#58118=CARTESIAN_POINT('Ctrl Pts',(3.25049509572416,5.93519760687656,40.6434068078774));
#58119=CARTESIAN_POINT('Ctrl Pts',(3.20035666026769,5.96265663172346,40.6461026683882));
#58120=CARTESIAN_POINT('Ctrl Pts',(3.1498810270518,5.9894743913875,40.6487985288989));
#58121=CARTESIAN_POINT('Ctrl Pts',(3.0990855038471,6.01564277861018,40.6514943894097));
#58122=CARTESIAN_POINT('Origin',(0.,0.,-63.6971797838103));
#58123=CARTESIAN_POINT('',(3.09908550384712,6.01564277861017,43.045630740225));
#58124=CARTESIAN_POINT('',(3.09908550384717,6.01564277861014,42.6514898562653));
#58125=CARTESIAN_POINT('',(3.09908550384721,6.01564277861012,-63.6971797838103));
#58126=CARTESIAN_POINT('',(-6.76699843322197,0.00460486387876293,41.6971797837852));
#58127=CARTESIAN_POINT('Ctrl Pts',(-6.76699843322233,0.00460486335559169,
41.6971797838098));
#58128=CARTESIAN_POINT('Ctrl Pts',(-6.7671159111045,-0.168032755431752,
41.7052849047448));
#58129=CARTESIAN_POINT('Ctrl Pts',(-6.76062274111126,-0.340827023646455,
41.7133900256798));
#58130=CARTESIAN_POINT('Ctrl Pts',(-6.74750964751565,-0.513227587609325,
41.7214951466149));
#58131=CARTESIAN_POINT('Ctrl Pts',(-6.73636368628527,-0.659765853962388,
41.7283843953685));
#58132=CARTESIAN_POINT('Ctrl Pts',(-6.72043584051447,-0.80601946530117,
41.7352736441221));
#58133=CARTESIAN_POINT('Ctrl Pts',(-6.69975003711939,-0.951650377039166,
41.7421628928757));
#58134=CARTESIAN_POINT('Ctrl Pts',(-6.6750977729527,-1.12520572021015,41.7503731410802));
#58135=CARTESIAN_POINT('Ctrl Pts',(-6.64369867344581,-1.29779320395664,
41.7585833892847));
#58136=CARTESIAN_POINT('Ctrl Pts',(-6.60565998398111,-1.46885846017602,
41.7667936374892));
#58137=CARTESIAN_POINT('Ctrl Pts',(-6.56761225196154,-1.6399643820174,41.7750058374335));
#58138=CARTESIAN_POINT('Ctrl Pts',(-6.52292186269664,-1.80954700792686,
41.7832180373777));
#58139=CARTESIAN_POINT('Ctrl Pts',(-6.47174667829002,-1.97706447341561,
41.7914302373219));
#58140=CARTESIAN_POINT('Ctrl Pts',(-6.42055021565599,-2.14465159131042,
41.7996458518324));
#58141=CARTESIAN_POINT('Ctrl Pts',(-6.36286369011821,-2.31017149797406,
41.8078614663428));
#58142=CARTESIAN_POINT('Ctrl Pts',(-6.29889411857824,-2.47309965083101,
41.8160770808533));
#58143=CARTESIAN_POINT('Ctrl Pts',(-6.23485271201375,-2.63621076486114,
41.8243019211387));
#58144=CARTESIAN_POINT('Ctrl Pts',(-6.16451429729534,-2.79672398057163,
41.8325267614242));
#58145=CARTESIAN_POINT('Ctrl Pts',(-6.08813352982892,-2.95413593508708,
41.8407516017096));
#58146=CARTESIAN_POINT('Ctrl Pts',(-6.01170383782557,-3.11164871743182,
41.8489817102912));
#58147=CARTESIAN_POINT('Ctrl Pts',(-5.92922424502312,-3.26605596551176,
41.8572118188727));
#58148=CARTESIAN_POINT('Ctrl Pts',(-5.84099421978324,-3.41688096433849,
41.8654419274543));
#58149=CARTESIAN_POINT('Ctrl Pts',(-5.75264322982504,-3.56791274655275,
41.873683319641));
#58150=CARTESIAN_POINT('Ctrl Pts',(-5.65852625106592,-3.71535217052858,
41.8819247118277));
#58151=CARTESIAN_POINT('Ctrl Pts',(-5.55898528670911,-3.8587525940583,41.8901661040144));
#58152=CARTESIAN_POINT('Ctrl Pts',(-5.5156625300379,-3.92116410167497,41.8937529672786));
#58153=CARTESIAN_POINT('Ctrl Pts',(-5.47131286370705,-3.98281097164823,
41.8973398305428));
#58154=CARTESIAN_POINT('Ctrl Pts',(-5.4259667489167,-4.04365847218213,41.900926693807));
#58155=CARTESIAN_POINT('Ctrl Pts',(-5.31915854685407,-4.18697862567439,
41.9093751886355));
#58156=CARTESIAN_POINT('Ctrl Pts',(-5.20657598901216,-4.32618844051475,
41.9178236834639));
#58157=CARTESIAN_POINT('Ctrl Pts',(-5.08856073177413,-4.46081143728877,
41.9262721782923));
#58158=CARTESIAN_POINT('Ctrl Pts',(-4.97065327461787,-4.59531146377573,
41.9347129559115));
#58159=CARTESIAN_POINT('Ctrl Pts',(-4.84732322849867,-4.72523277418302,
41.9431537335307));
#58160=CARTESIAN_POINT('Ctrl Pts',(-4.71895350609851,-4.85013059693042,
41.9515945111499));
#58161=CARTESIAN_POINT('Ctrl Pts',(-4.59068130147954,-4.97493353937175,
41.9600288766192));
#58162=CARTESIAN_POINT('Ctrl Pts',(-4.45737729080423,-5.09472036999594,
41.9684632420884));
#58163=CARTESIAN_POINT('Ctrl Pts',(-4.31946261697925,-5.20908165615772,
41.9768976075577));
#58164=CARTESIAN_POINT('Ctrl Pts',(-4.18163153264475,-5.32337362843594,
41.9853268609944));
#58165=CARTESIAN_POINT('Ctrl Pts',(-4.03919561271726,-5.43224640014772,
41.993756114431));
#58166=CARTESIAN_POINT('Ctrl Pts',(-3.89261088277409,-5.53532921471783,
42.0021853678677));
#58167=CARTESIAN_POINT('Ctrl Pts',(-3.74609251153582,-5.63836536384008,
42.0106108053929));
#58168=CARTESIAN_POINT('Ctrl Pts',(-3.59542934765794,-5.73561659085825,
42.0190362429182));
#58169=CARTESIAN_POINT('Ctrl Pts',(-3.4411086590045,-5.82675383012911,42.0274616804434));
#58170=CARTESIAN_POINT('Ctrl Pts',(-3.2868218704568,-5.91787104899911,42.0358852671266));
#58171=CARTESIAN_POINT('Ctrl Pts',(-3.12887944457916,-6.00287678629404,
42.0443088538097));
#58172=CARTESIAN_POINT('Ctrl Pts',(-2.96779611359637,-6.08148626802053,
42.0527324404929));
#58173=CARTESIAN_POINT('Ctrl Pts',(-2.80673080699336,-6.16008695375836,
42.0611550846209));
#58174=CARTESIAN_POINT('Ctrl Pts',(-2.64252559549371,-6.23229266454623,
42.0695777287489));
#58175=CARTESIAN_POINT('Ctrl Pts',(-2.47571848383332,-6.29786527236063,
42.078000372877));
#58176=CARTESIAN_POINT('Ctrl Pts',(-2.3089067764376,-6.36343968677877,42.0864232490589));
#58177=CARTESIAN_POINT('Ctrl Pts',(-2.13949333638898,-6.42238051225617,
42.0948461252408));
#58178=CARTESIAN_POINT('Ctrl Pts',(-1.96803509669743,-6.47449819354111,
42.1032690014228));
#58179=CARTESIAN_POINT('Ctrl Pts',(-1.79654822252821,-6.5266245787681,42.1116932842718));
#58180=CARTESIAN_POINT('Ctrl Pts',(-1.62301618700375,-6.57192545160094,
42.1201175671208));
#58181=CARTESIAN_POINT('Ctrl Pts',(-1.44801034699811,-6.61026134392479,
42.1285418499698));
#58182=CARTESIAN_POINT('Ctrl Pts',(-1.27288631451881,-6.64862312689289,
42.1369718222679));
#58183=CARTESIAN_POINT('Ctrl Pts',(-1.09628681462513,-6.6800104585119,42.1454017945661));
#58184=CARTESIAN_POINT('Ctrl Pts',(-0.918793647272057,-6.70433495834841,
42.1538317668642));
#58185=CARTESIAN_POINT('Ctrl Pts',(-0.741237028976705,-6.72866815380096,
42.1622647527414));
#58186=CARTESIAN_POINT('Ctrl Pts',(-0.562786437325949,-6.74593344387162,
42.1706977386186));
#58187=CARTESIAN_POINT('Ctrl Pts',(-0.384028615301828,-6.75609436158417,
42.1791307244958));
#58188=CARTESIAN_POINT('Ctrl Pts',(-0.205106337170434,-6.76626462727912,
42.1875714686686));
#58189=CARTESIAN_POINT('Ctrl Pts',(-0.0258765972778607,-6.76931744920169,
42.1960122128414));
#58190=CARTESIAN_POINT('Ctrl Pts',(0.15307292701594,-6.76526848536071,42.2044529570142));
#58191=CARTESIAN_POINT('Ctrl Pts',(0.252018898312637,-6.76302970511487,
42.2091200698995));
#58192=CARTESIAN_POINT('Ctrl Pts',(0.350879241127732,-6.75862063444282,
42.2137871827848));
#58193=CARTESIAN_POINT('Ctrl Pts',(0.449555269248574,-6.75205072995537,
42.21845429567));
#58194=CARTESIAN_POINT('Ctrl Pts',(0.621686906146081,-6.74059011043894,
42.2265956628879));
#58195=CARTESIAN_POINT('Ctrl Pts',(0.793599377061357,-6.72252829119632,
42.2347370301057));
#58196=CARTESIAN_POINT('Ctrl Pts',(0.964742383957024,-6.69787736022368,
42.2428783973235));
#58197=CARTESIAN_POINT('Ctrl Pts',(1.1357359960245,-6.67324794763887,42.251012657747));
#58198=CARTESIAN_POINT('Ctrl Pts',(1.30596112122551,-6.642040924175,42.2591469181704));
#58199=CARTESIAN_POINT('Ctrl Pts',(1.47487010898186,-6.60432034062793,42.2672811785939));
#58200=CARTESIAN_POINT('Ctrl Pts',(1.64366387312816,-6.56662548870041,42.2754098901187));
#58201=CARTESIAN_POINT('Ctrl Pts',(1.81114293157273,-6.5224260026454,42.2835386016436));
#58202=CARTESIAN_POINT('Ctrl Pts',(1.9767674269714,-6.47183741604074,42.2916673131684));
#58203=CARTESIAN_POINT('Ctrl Pts',(2.14231293910877,-6.42127295419821,42.2997921482609));
#58204=CARTESIAN_POINT('Ctrl Pts',(2.30600530002384,-6.36432556584715,42.3079169833535));
#58205=CARTESIAN_POINT('Ctrl Pts',(2.46731749392409,-6.30116127266841,42.316041818446));
#58206=CARTESIAN_POINT('Ctrl Pts',(2.62858452802384,-6.23801466251046,42.3241643789682));
#58207=CARTESIAN_POINT('Ctrl Pts',(2.78747238206722,-6.16865474826588,42.3322869394903));
#58208=CARTESIAN_POINT('Ctrl Pts',(2.94347181719057,-6.09329653483275,42.3404095000125));
#58209=CARTESIAN_POINT('Ctrl Pts',(3.09947954327883,-6.01793431630626,42.3485324922277));
#58210=CARTESIAN_POINT('Ctrl Pts',(3.25259821245427,-5.93657331743266,42.3566554844428));
#58211=CARTESIAN_POINT('Ctrl Pts',(3.40234092262927,-5.84947563856814,42.364778476658));
#58212=CARTESIAN_POINT('Ctrl Pts',(3.47878001283058,-5.80501492777115,42.3689250166392));
#58213=CARTESIAN_POINT('Ctrl Pts',(3.55433978964625,-5.75906009934237,42.3730715566205));
#58214=CARTESIAN_POINT('Ctrl Pts',(3.62895815416705,-5.71165052461235,42.3772180966017));
#58215=CARTESIAN_POINT('Ctrl Pts',(3.79062208292333,-5.60893562110648,42.3862017556301));
#58216=CARTESIAN_POINT('Ctrl Pts',(3.94778550942087,-5.49944065792936,42.3951854146585));
#58217=CARTESIAN_POINT('Ctrl Pts',(4.099921306424,-5.38358006173685,42.404169073687));
#58218=CARTESIAN_POINT('Ctrl Pts',(4.25231847111563,-5.26752041826676,42.4131681665465));
#58219=CARTESIAN_POINT('Ctrl Pts',(4.39967055226727,-5.14507342852191,42.4221672594059));
#58220=CARTESIAN_POINT('Ctrl Pts',(4.54148410181434,-5.01669324884108,42.4311663522654));
#58221=CARTESIAN_POINT('Ctrl Pts',(4.68363016450503,-4.88801205351497,42.4401865454829));
#58222=CARTESIAN_POINT('Ctrl Pts',(4.8202115342865,-4.75336999460394,42.4492067387004));
#58223=CARTESIAN_POINT('Ctrl Pts',(4.95077025594302,-4.61325946299034,42.4582269319178));
#58224=CARTESIAN_POINT('Ctrl Pts',(5.08146120099783,-4.47300703437904,42.4672562603396));
#58225=CARTESIAN_POINT('Ctrl Pts',(5.20611715428203,-4.32727524803248,42.4762855887614));
#58226=CARTESIAN_POINT('Ctrl Pts',(5.32431999048377,-4.17659019284092,42.4853149171832));
#58227=CARTESIAN_POINT('Ctrl Pts',(5.44268946885848,-4.02569270209503,42.494356975138));
#58228=CARTESIAN_POINT('Ctrl Pts',(5.55458749173169,-3.86982816795383,42.5033990330928));
#58229=CARTESIAN_POINT('Ctrl Pts',(5.65963750572569,-3.70955419205369,42.5124410910476));
#58230=CARTESIAN_POINT('Ctrl Pts',(5.7508026683128,-3.57046422418131,42.5202880265428));
#58231=CARTESIAN_POINT('Ctrl Pts',(5.83681107249541,-3.42805394440939,42.5281349620379));
#58232=CARTESIAN_POINT('Ctrl Pts',(5.91744409407256,-3.28270382360727,42.535981897533));
#58233=CARTESIAN_POINT('Ctrl Pts',(6.00636479109011,-3.12241423256244,42.5446353618338));
#58234=CARTESIAN_POINT('Ctrl Pts',(6.08882553004275,-2.95840747967115,42.5532888261345));
#58235=CARTESIAN_POINT('Ctrl Pts',(6.16452586860145,-2.79122013021967,42.5619422904353));
#58236=CARTESIAN_POINT('Ctrl Pts',(6.24015647166431,-2.62418679451417,42.5705877831254));
#58237=CARTESIAN_POINT('Ctrl Pts',(6.30903897070218,-2.45397898214835,42.5792332758155));
#58238=CARTESIAN_POINT('Ctrl Pts',(6.37091920020569,-2.28115706264398,42.5878787685056));
#58239=CARTESIAN_POINT('Ctrl Pts',(6.43466099018841,-2.10313609236246,42.5967843460022));
#58240=CARTESIAN_POINT('Ctrl Pts',(6.4909724624241,-1.9223415557936,42.6056899234988));
#58241=CARTESIAN_POINT('Ctrl Pts',(6.53962870314262,-1.73940950469785,42.6145955009954));
#58242=CARTESIAN_POINT('Ctrl Pts',(6.58677432525006,-1.5621569010248,42.6232245891679));
#58243=CARTESIAN_POINT('Ctrl Pts',(6.62673282869204,-1.38289783675792,42.6318536773404));
#58244=CARTESIAN_POINT('Ctrl Pts',(6.65934956475971,-1.20222808748369,42.6404827655129));
#58245=CARTESIAN_POINT('Ctrl Pts',(6.69353393679229,-1.01287493113444,42.6495265876715));
#58246=CARTESIAN_POINT('Ctrl Pts',(6.71965330256688,-0.821972463292397,
42.6585704098301));
#58247=CARTESIAN_POINT('Ctrl Pts',(6.73758934643241,-0.630221230077622,
42.6676142319888));
#58248=CARTESIAN_POINT('Ctrl Pts',(6.75552539029795,-0.43846999686272,42.6766580541474));
#58249=CARTESIAN_POINT('Ctrl Pts',(6.76527804188348,-0.245870378693191,
42.685701876306));
#58250=CARTESIAN_POINT('Ctrl Pts',(6.76679140733531,-0.053132378198996,
42.6947456984647));
#58251=CARTESIAN_POINT('Ctrl Pts',(6.76820135315682,0.126434386798115,42.7031714883145));
#58252=CARTESIAN_POINT('Ctrl Pts',(6.76245923937044,0.306042628603557,42.7115972781643));
#58253=CARTESIAN_POINT('Ctrl Pts',(6.7495899555549,0.485102496254617,42.7200230680141));
#58254=CARTESIAN_POINT('Ctrl Pts',(6.73671768563253,0.66420391181936,42.7284508129306));
#58255=CARTESIAN_POINT('Ctrl Pts',(6.71671497212188,0.842756368876598,42.7368785578472));
#58256=CARTESIAN_POINT('Ctrl Pts',(6.68965862793557,1.02017471135446,42.7453063027637));
#58257=CARTESIAN_POINT('Ctrl Pts',(6.66259234190026,1.19765824617164,42.7537371444536));
#58258=CARTESIAN_POINT('Ctrl Pts',(6.62846730721728,1.37400650792871,42.7621679861436));
#58259=CARTESIAN_POINT('Ctrl Pts',(6.58741160309024,1.54864371999245,42.7705988278335));
#58260=CARTESIAN_POINT('Ctrl Pts',(6.54631817401137,1.72344140136376,42.7790374163909));
#58261=CARTESIAN_POINT('Ctrl Pts',(6.49828142794358,1.89652456892985,42.7874760049483));
#58262=CARTESIAN_POINT('Ctrl Pts',(6.44347985555778,2.0673307309236,42.7959145935056));
#58263=CARTESIAN_POINT('Ctrl Pts',(6.3886495476493,2.23822645612015,42.8043576068859));
#58264=CARTESIAN_POINT('Ctrl Pts',(6.32704744756299,2.40684248162703,42.8128006202662));
#58265=CARTESIAN_POINT('Ctrl Pts',(6.25890071606799,2.5726349967307,42.8212436336465));
#58266=CARTESIAN_POINT('Ctrl Pts',(6.19068239168181,2.73860168842704,42.8296955170008));
#58267=CARTESIAN_POINT('Ctrl Pts',(6.11590583448472,2.90173864103937,42.8381474003551));
#58268=CARTESIAN_POINT('Ctrl Pts',(6.03484524762624,3.06152443028029,42.8465992837094));
#58269=CARTESIAN_POINT('Ctrl Pts',(6.01275367681282,3.10507110585712,42.8489026889383));
#58270=CARTESIAN_POINT('Ctrl Pts',(5.99019562670143,3.14836903081173,42.8512060941672));
#58271=CARTESIAN_POINT('Ctrl Pts',(5.96717721818493,3.19140800380879,42.8535094993961));
#58272=CARTESIAN_POINT('Ctrl Pts',(5.88406764621074,3.34680322244131,42.8618261048869));
#58273=CARTESIAN_POINT('Ctrl Pts',(5.79480385367624,3.49910004449492,42.8701427103777));
#58274=CARTESIAN_POINT('Ctrl Pts',(5.69964289076411,3.64778835978216,42.8784593158685));
#58275=CARTESIAN_POINT('Ctrl Pts',(5.60455801142871,3.79635779503183,42.8867692720246));
#58276=CARTESIAN_POINT('Ctrl Pts',(5.50358554028747,3.94132417917203,42.8950792281806));
#58277=CARTESIAN_POINT('Ctrl Pts',(5.3970282457195,4.08220223836423,42.9033891843367));
#58278=CARTESIAN_POINT('Ctrl Pts',(5.2905384442719,4.22299106575071,42.9116938769877));
#58279=CARTESIAN_POINT('Ctrl Pts',(5.17847107612982,4.35969645089914,42.9199985696386));
#58280=CARTESIAN_POINT('Ctrl Pts',(5.06117210616261,4.49186218753443,42.9283032622896));
#58281=CARTESIAN_POINT('Ctrl Pts',(4.94392795336888,4.6239661593297,42.9366040739194));
#58282=CARTESIAN_POINT('Ctrl Pts',(4.82145730117771,4.75153445063336,42.9449048855492));
#58283=CARTESIAN_POINT('Ctrl Pts',(4.69414639063808,4.87414389029084,42.953205697179));
#58284=CARTESIAN_POINT('Ctrl Pts',(4.56686135994001,4.9967284058247,42.9615048214147));
#58285=CARTESIAN_POINT('Ctrl Pts',(4.43473827917861,5.11435583460496,42.9698039456503));
#58286=CARTESIAN_POINT('Ctrl Pts',(4.29820050075553,5.22663959493143,42.978103069886));
#58287=CARTESIAN_POINT('Ctrl Pts',(4.16168176791428,5.33890769285611,42.9864010364812));
#58288=CARTESIAN_POINT('Ctrl Pts',(4.02074983493964,5.44583338904462,42.9946990030764));
#58289=CARTESIAN_POINT('Ctrl Pts',(3.87586141588145,5.54707015323237,43.0029969696717));
#58290=CARTESIAN_POINT('Ctrl Pts',(3.73093540160447,5.64833318603651,43.0112970893988));
#58291=CARTESIAN_POINT('Ctrl Pts',(3.58205113465018,5.74390413726842,43.0195972091258));
#58292=CARTESIAN_POINT('Ctrl Pts',(3.42969509580122,5.8334792833983,43.0278973288529));
#58293=CARTESIAN_POINT('Ctrl Pts',(3.32119094562956,5.89727245615832,43.0338084659769));
#58294=CARTESIAN_POINT('Ctrl Pts',(3.21092656187111,5.95802549407168,43.039719603101));
#58295=CARTESIAN_POINT('Ctrl Pts',(3.09908550384712,6.01564277861017,43.045630740225));
#58296=CARTESIAN_POINT('Ctrl Pts',(3.09908550384737,6.01564277861004,41.0460412338188));
#58297=CARTESIAN_POINT('Ctrl Pts',(2.94665044189545,6.0941729221307,41.0540826047719));
#58298=CARTESIAN_POINT('Ctrl Pts',(2.79112159957602,6.16696026658,41.0621239757251));
#58299=CARTESIAN_POINT('Ctrl Pts',(2.63298169230085,6.23375459959795,41.0701653466782));
#58300=CARTESIAN_POINT('Ctrl Pts',(2.47261853433126,6.30148797798289,41.07831976932));
#58301=CARTESIAN_POINT('Ctrl Pts',(2.30957067502836,6.36305836293058,41.0864741919618));
#58302=CARTESIAN_POINT('Ctrl Pts',(2.14436518815934,6.41825419719493,41.0946286146036));
#58303=CARTESIAN_POINT('Ctrl Pts',(1.98150303802598,6.4726671129949,41.1026673718489));
#58304=CARTESIAN_POINT('Ctrl Pts',(1.81654443640663,6.52088502335897,41.1107061290943));
#58305=CARTESIAN_POINT('Ctrl Pts',(1.65001184703235,6.56275474969566,41.1187448863396));
#58306=CARTESIAN_POINT('Ctrl Pts',(1.48346194172913,6.60462882961388,41.1267844794487));
#58307=CARTESIAN_POINT('Ctrl Pts',(1.31533808499582,6.64015332005647,41.1348240725577));
#58308=CARTESIAN_POINT('Ctrl Pts',(1.14617489316087,6.66922575073656,41.1428636656668));
#58309=CARTESIAN_POINT('Ctrl Pts',(0.976960617147773,6.69830696075696,41.1509056865853));
#58310=CARTESIAN_POINT('Ctrl Pts',(0.806706749164652,6.72093216955925,41.1589477075039));
#58311=CARTESIAN_POINT('Ctrl Pts',(0.635954870452851,6.73705057148507,41.1669897284225));
#58312=CARTESIAN_POINT('Ctrl Pts',(0.460996292000625,6.75356607169003,41.1752298752273));
#58313=CARTESIAN_POINT('Ctrl Pts',(0.285515264690243,6.76324998340181,41.1834700220322));
#58314=CARTESIAN_POINT('Ctrl Pts',(0.110095320071505,6.76610434596588,41.1917101688371));
#58315=CARTESIAN_POINT('Ctrl Pts',(-0.0614046923037506,6.76889492497402,
41.1997661814079));
#58316=CARTESIAN_POINT('Ctrl Pts',(-0.232845954937012,6.76515801909524,
41.2078221939787));
#58317=CARTESIAN_POINT('Ctrl Pts',(-0.403688049607549,6.75494818326566,
41.2158782065494));
#58318=CARTESIAN_POINT('Ctrl Pts',(-0.580387485856322,6.74438830199777,
41.2242104204714));
#58319=CARTESIAN_POINT('Ctrl Pts',(-0.756445492117974,6.726903815481,41.2325426343933));
#58320=CARTESIAN_POINT('Ctrl Pts',(-0.931275858727255,6.70261249625486,
41.2408748483153));
#58321=CARTESIAN_POINT('Ctrl Pts',(-1.10610622533641,6.67832117702874,41.2492070622372));
#58322=CARTESIAN_POINT('Ctrl Pts',(-1.27970854145619,6.64722318059881,41.2575392761591));
#58323=CARTESIAN_POINT('Ctrl Pts',(-1.45151475646483,6.60949271213494,41.2658714900811));
#58324=CARTESIAN_POINT('Ctrl Pts',(-1.62122277378632,6.57222303015461,41.2741019461476));
#58325=CARTESIAN_POINT('Ctrl Pts',(-1.78974282827711,6.5283583640965,41.2823324022142));
#58326=CARTESIAN_POINT('Ctrl Pts',(-1.95652396937399,6.47798602632524,41.2905628582808));
#58327=CARTESIAN_POINT('Ctrl Pts',(-2.12310713142855,6.42767348348718,41.298783544311));
#58328=CARTESIAN_POINT('Ctrl Pts',(-2.2879551505189,6.37086875375443,41.3070042303412));
#58329=CARTESIAN_POINT('Ctrl Pts',(-2.45052652895091,6.30771026053891,41.3152249163714));
#58330=CARTESIAN_POINT('Ctrl Pts',(-2.61293754242438,6.24461406862908,41.3234374932868));
#58331=CARTESIAN_POINT('Ctrl Pts',(-2.77307605571986,6.17517672389178,41.3316500702022));
#58332=CARTESIAN_POINT('Ctrl Pts',(-2.9304149349874,6.09958665065124,41.3398626471176));
#58333=CARTESIAN_POINT('Ctrl Pts',(-3.08763016648538,6.02405598131646,41.3480687700223));
#58334=CARTESIAN_POINT('Ctrl Pts',(-3.24204982444864,5.94238236875823,41.3562748929269));
#58335=CARTESIAN_POINT('Ctrl Pts',(-3.39316591702405,5.85480264906908,41.3644810158316));
#58336=CARTESIAN_POINT('Ctrl Pts',(-3.54419355201104,5.76727419520257,41.3726823351853));
#58337=CARTESIAN_POINT('Ctrl Pts',(-3.69192116456413,5.67384670065939,41.3808836545391));
#58338=CARTESIAN_POINT('Ctrl Pts',(-3.83586450333802,5.57480336083986,41.3890849738928));
#58339=CARTESIAN_POINT('Ctrl Pts',(-3.97976654817822,5.47578843420806,41.3972839404823));
#58340=CARTESIAN_POINT('Ctrl Pts',(-4.11988618443246,5.37116107103508,41.4054829070719));
#58341=CARTESIAN_POINT('Ctrl Pts',(-4.25576714244758,5.26124842877274,41.4136818736614));
#58342=CARTESIAN_POINT('Ctrl Pts',(-4.39163015676819,5.15135030097146,41.4218797575403));
#58343=CARTESIAN_POINT('Ctrl Pts',(-4.52325532839601,5.03616850895693,41.4300776414193));
#58344=CARTESIAN_POINT('Ctrl Pts',(-4.65021855588829,4.91607123447904,41.4382755252982));
#58345=CARTESIAN_POINT('Ctrl Pts',(-4.77718808054846,4.79596800337327,41.4464738157788));
#58346=CARTESIAN_POINT('Ctrl Pts',(-4.89949493984377,4.67094905051927,41.4546721062593));
#58347=CARTESIAN_POINT('Ctrl Pts',(-5.01675103656091,4.54142026652072,41.4628703967399));
#58348=CARTESIAN_POINT('Ctrl Pts',(-5.13403424883809,4.41186152889402,41.4710705830812));
#58349=CARTESIAN_POINT('Ctrl Pts',(-5.2462641316202,4.27779114877439,41.4792707694225));
#58350=CARTESIAN_POINT('Ctrl Pts',(-5.35309207785388,4.1396490438222,41.4874709557639));
#58351=CARTESIAN_POINT('Ctrl Pts',(-5.46002102152844,4.00137633634913,41.495678894738));
#58352=CARTESIAN_POINT('Ctrl Pts',(-5.56153760556237,3.85902449722819,41.5038868337121));
#58353=CARTESIAN_POINT('Ctrl Pts',(-5.65733533659436,3.7130642183136,41.5120947726862));
#58354=CARTESIAN_POINT('Ctrl Pts',(-5.753179542008,3.56703312964564,41.5203066935801));
#58355=CARTESIAN_POINT('Ctrl Pts',(-5.84329917803921,3.4173904179821,41.5285186144741));
#58356=CARTESIAN_POINT('Ctrl Pts',(-5.92743320698998,3.2646323800196,41.5367305353681));
#58357=CARTESIAN_POINT('Ctrl Pts',(-6.0116826124331,3.11166485860769,41.5449537176106));
#58358=CARTESIAN_POINT('Ctrl Pts',(-6.08992984596416,2.95557379371224,41.5531768998532));
#58359=CARTESIAN_POINT('Ctrl Pts',(-6.16196110076714,2.79687761488281,41.5614000820957));
#58360=CARTESIAN_POINT('Ctrl Pts',(-6.22619480158398,2.65536067338867,41.5687330853785));
#58361=CARTESIAN_POINT('Ctrl Pts',(-6.28548608766533,2.51177254889014,41.5760660886612));
#58362=CARTESIAN_POINT('Ctrl Pts',(-6.33971681340106,2.36649101538121,41.583399091944));
#58363=CARTESIAN_POINT('Ctrl Pts',(-6.41039570506891,2.177145628077,41.5929561933397));
#58364=CARTESIAN_POINT('Ctrl Pts',(-6.47261128120862,1.98456975275513,41.6025132947355));
#58365=CARTESIAN_POINT('Ctrl Pts',(-6.52610743942796,1.78947218169021,41.6120703961312));
#58366=CARTESIAN_POINT('Ctrl Pts',(-6.57946562461814,1.59487779073682,41.6216028486125));
#58367=CARTESIAN_POINT('Ctrl Pts',(-6.62414924673454,1.39777480200119,41.6311353010937));
#58368=CARTESIAN_POINT('Ctrl Pts',(-6.65995207290432,1.19888589391044,41.640667753575));
#58369=CARTESIAN_POINT('Ctrl Pts',(-6.6955405052461,1.00118796873682,41.6501431239989));
#58370=CARTESIAN_POINT('Ctrl Pts',(-6.7223541321133,0.801725566272196,41.6596184944227));
#58371=CARTESIAN_POINT('Ctrl Pts',(-6.7402386003398,0.601225923001824,41.6690938648466));
#58372=CARTESIAN_POINT('Ctrl Pts',(-6.75790903440202,0.403125779288352,
41.6784558378261));
#58373=CARTESIAN_POINT('Ctrl Pts',(-6.76686273816051,0.204013205259285,
41.6878178108057));
#58374=CARTESIAN_POINT('Ctrl Pts',(-6.76699843322198,0.00460486387857811,
41.6971797837852));
#58375=CARTESIAN_POINT('',(-6.76699994849255,0.000834926224110294,41.302820216214));
#58376=CARTESIAN_POINT('Ctrl Pts',(3.0990855038471,6.01564277861018,40.6514943894097));
#58377=CARTESIAN_POINT('Ctrl Pts',(3.069218343977,6.03102947718936,40.6530795231337));
#58378=CARTESIAN_POINT('Ctrl Pts',(3.0392405925958,6.04619167767068,40.6546646568578));
#58379=CARTESIAN_POINT('Ctrl Pts',(3.00915580109585,6.06112781293475,40.6562497905818));
#58380=CARTESIAN_POINT('Ctrl Pts',(2.85463802662748,6.13784093824151,40.6643911577997));
#58381=CARTESIAN_POINT('Ctrl Pts',(2.69698790972868,6.20873922885997,40.6725325250175));
#58382=CARTESIAN_POINT('Ctrl Pts',(2.53668708341959,6.27355621962633,40.6806738922354));
#58383=CARTESIAN_POINT('Ctrl Pts',(2.37652618754003,6.33831663008947,40.6888081526589));
#58384=CARTESIAN_POINT('Ctrl Pts',(2.21371952507958,6.39700617108109,40.6969424130824));
#58385=CARTESIAN_POINT('Ctrl Pts',(2.04877258900682,6.44940461426745,40.7050766735058));
#58386=CARTESIAN_POINT('Ctrl Pts',(1.88393817377604,6.50176731312848,40.7132053850307));
#58387=CARTESIAN_POINT('Ctrl Pts',(1.71696673922693,6.5478473481717,40.7213340965555));
#58388=CARTESIAN_POINT('Ctrl Pts',(1.54838294991314,6.58747290244281,40.7294628080803));
#58389=CARTESIAN_POINT('Ctrl Pts',(1.37987955509287,6.62707956001941,40.7375876431729));
#58390=CARTESIAN_POINT('Ctrl Pts',(1.20976569224582,6.66023778266953,40.7457124782654));
#58391=CARTESIAN_POINT('Ctrl Pts',(1.03858033438825,6.68682584557292,40.7538373133579));
#58392=CARTESIAN_POINT('Ctrl Pts',(0.867442900351693,6.71340646507353,40.7619598738801));
#58393=CARTESIAN_POINT('Ctrl Pts',(0.695234930307182,6.73342053311475,40.7700824344022));
#58394=CARTESIAN_POINT('Ctrl Pts',(0.522504683473259,6.74679760002837,40.7782049949244));
#58395=CARTESIAN_POINT('Ctrl Pts',(0.349765256474587,6.76017537789841,40.7863279871396));
#58396=CARTESIAN_POINT('Ctrl Pts',(0.176503861899764,6.76691541779922,40.7944509793548));
#58397=CARTESIAN_POINT('Ctrl Pts',(0.00327315476795207,6.76699920839791,
40.80257397157));
#58398=CARTESIAN_POINT('Ctrl Pts',(-0.0851558420898549,6.76704198094505,
40.806720511551));
#58399=CARTESIAN_POINT('Ctrl Pts',(-0.173576807295014,6.76535111136654,
40.8108670515321));
#58400=CARTESIAN_POINT('Ctrl Pts',(-0.26191626517331,6.76192937481882,40.8150135915132));
#58401=CARTESIAN_POINT('Ctrl Pts',(-0.453307538849495,6.75451603392019,
40.8239972505416));
#58402=CARTESIAN_POINT('Ctrl Pts',(-0.644221361093534,6.73897891496851,
40.8329809095699));
#58403=CARTESIAN_POINT('Ctrl Pts',(-0.833993664631919,6.71541090085736,
40.8419645685983));
#58404=CARTESIAN_POINT('Ctrl Pts',(-1.02409199497715,6.69180239714766,40.8509636614577));
#58405=CARTESIAN_POINT('Ctrl Pts',(-1.21304464953948,6.66013545144486,40.859962754317));
#58406=CARTESIAN_POINT('Ctrl Pts',(-1.40019667346197,6.62055422722494,40.8689618471764));
#58407=CARTESIAN_POINT('Ctrl Pts',(-1.58778751658146,6.58088019609508,40.8779820403938));
#58408=CARTESIAN_POINT('Ctrl Pts',(-1.77356904672516,6.53325480731981,40.8870022336112));
#58409=CARTESIAN_POINT('Ctrl Pts',(-1.95689774113366,6.47787312555178,40.8960224268285));
#58410=CARTESIAN_POINT('Ctrl Pts',(-2.14041210175138,6.4224353559632,40.9050517552502));
#58411=CARTESIAN_POINT('Ctrl Pts',(-2.32146843701564,6.35922567552714,40.9140810836719));
#58412=CARTESIAN_POINT('Ctrl Pts',(-2.49944068700665,6.28848831215704,40.9231104120936));
#58413=CARTESIAN_POINT('Ctrl Pts',(-2.67766384199675,6.21765122336294,40.9321524700483));
#58414=CARTESIAN_POINT('Ctrl Pts',(-2.85279399561198,6.1392653201658,40.9411945280031));
#58415=CARTESIAN_POINT('Ctrl Pts',(-3.0242251558089,6.05362298189875,40.9502365859578));
#58416=CARTESIAN_POINT('Ctrl Pts',(-3.17299762140804,5.97930031028507,40.9580835214535));
#58417=CARTESIAN_POINT('Ctrl Pts',(-3.31898456659371,5.89951343658971,40.9659304569492));
#58418=CARTESIAN_POINT('Ctrl Pts',(-3.4618056093732,5.81448113961274,40.9737773924449));
#58419=CARTESIAN_POINT('Ctrl Pts',(-3.61930617705035,5.72070899802823,40.9824308567457));
#58420=CARTESIAN_POINT('Ctrl Pts',(-3.77309473582241,5.62047393602927,40.9910843210465));
#58421=CARTESIAN_POINT('Ctrl Pts',(-3.92264165196769,5.51408845324848,40.9997377853474));
#58422=CARTESIAN_POINT('Ctrl Pts',(-4.07205080481473,5.40780097325753,41.0083832780376));
#58423=CARTESIAN_POINT('Ctrl Pts',(-4.21722586162392,5.29537454867129,41.0170287707278));
#58424=CARTESIAN_POINT('Ctrl Pts',(-4.35766520130469,5.17716553659801,41.025674263418));
#58425=CARTESIAN_POINT('Ctrl Pts',(-4.50232941743482,5.05540040931979,41.0345798409145));
#58426=CARTESIAN_POINT('Ctrl Pts',(-4.64196825079845,4.92749950011744,41.043485418411));
#58427=CARTESIAN_POINT('Ctrl Pts',(-4.77606727526543,4.79389928785938,41.0523909959076));
#58428=CARTESIAN_POINT('Ctrl Pts',(-4.90600295955243,4.66444692927855,41.0610200840801));
#58429=CARTESIAN_POINT('Ctrl Pts',(-5.03073741675548,4.52964407580015,41.0696491722527));
#58430=CARTESIAN_POINT('Ctrl Pts',(-5.14983720867053,4.38992775842525,41.0782782604253));
#58431=CARTESIAN_POINT('Ctrl Pts',(-5.27466121274285,4.24349635087574,41.0873220825838));
#58432=CARTESIAN_POINT('Ctrl Pts',(-5.3932953083213,4.09166774730639,41.0963659047423));
#58433=CARTESIAN_POINT('Ctrl Pts',(-5.50528473431925,3.93498780100669,41.1054097269008));
#58434=CARTESIAN_POINT('Ctrl Pts',(-5.6172741603172,3.778307854707,41.1144535490593));
#58435=CARTESIAN_POINT('Ctrl Pts',(-5.72261866449503,3.61677685901155,41.1234973712178));
#58436=CARTESIAN_POINT('Ctrl Pts',(-5.82091267018917,3.45098025002046,41.1325411933763));
#58437=CARTESIAN_POINT('Ctrl Pts',(-5.91248950805211,3.29651376884917,41.1409669832261));
#58438=CARTESIAN_POINT('Ctrl Pts',(-5.99790663143424,3.13841251196621,41.1493927730758));
#58439=CARTESIAN_POINT('Ctrl Pts',(-6.07688873477558,2.97719873457545,41.1578185629256));
#58440=CARTESIAN_POINT('Ctrl Pts',(-6.15588916462177,2.81594755016529,41.166246307842));
#58441=CARTESIAN_POINT('Ctrl Pts',(-6.22845145147225,2.65158270296457,41.1746740527584));
#58442=CARTESIAN_POINT('Ctrl Pts',(-6.29434752276427,2.48464851894011,41.1831017976749));
#58443=CARTESIAN_POINT('Ctrl Pts',(-6.36026780755679,2.31765299497734,41.1915326393648));
#58444=CARTESIAN_POINT('Ctrl Pts',(-6.41951687104965,2.14808655993829,41.1999634810547));
#58445=CARTESIAN_POINT('Ctrl Pts',(-6.47191566315663,1.97651123168777,41.2083943227446));
#58446=CARTESIAN_POINT('Ctrl Pts',(-6.52436260306527,1.80477824761083,41.2168329113019));
#58447=CARTESIAN_POINT('Ctrl Pts',(-6.56994659882727,1.63103299962583,41.2252714998592));
#58448=CARTESIAN_POINT('Ctrl Pts',(-6.60853884934117,1.45585139239845,41.2337100884165));
#58449=CARTESIAN_POINT('Ctrl Pts',(-6.6471513359257,1.28057792767814,41.2421531017967));
#58450=CARTESIAN_POINT('Ctrl Pts',(-6.67876470189843,1.10386692665057,41.2505961151769));
#58451=CARTESIAN_POINT('Ctrl Pts',(-6.70330160567991,0.926302641305302,
41.2590391285571));
#58452=CARTESIAN_POINT('Ctrl Pts',(-6.72786428718906,0.748551812301852,
41.2674910119114));
#58453=CARTESIAN_POINT('Ctrl Pts',(-6.74533561831508,0.569946237354676,
41.2759428952657));
#58454=CARTESIAN_POINT('Ctrl Pts',(-6.75569017492979,0.391074494639017,
41.2843947786199));
#58455=CARTESIAN_POINT('Ctrl Pts',(-6.75851211873265,0.342326293760333,
41.2866981838493));
#58456=CARTESIAN_POINT('Ctrl Pts',(-6.7608057738674,0.293558321921608,41.2890015890787));
#58457=CARTESIAN_POINT('Ctrl Pts',(-6.76257129648251,0.244782474844337,
41.291304994308));
#58458=CARTESIAN_POINT('Ctrl Pts',(-6.7655133731944,0.163502131810913,41.2951434016019));
#58459=CARTESIAN_POINT('Ctrl Pts',(-6.76698991274409,0.0821736906038927,
41.2989818088958));
#58460=CARTESIAN_POINT('Ctrl Pts',(-6.76699994849249,0.000834926739618518,
41.3028202161897));
#58461=CARTESIAN_POINT('Ctrl Pts',(-6.76699994849255,0.000834926224295111,
41.302820216214));
#58462=CARTESIAN_POINT('Ctrl Pts',(-6.76702159771241,-0.174630001529597,
41.311100473087));
#58463=CARTESIAN_POINT('Ctrl Pts',(-6.76021436775829,-0.350273550115445,
41.3193807299599));
#58464=CARTESIAN_POINT('Ctrl Pts',(-6.74656269657631,-0.52552904883085,
41.3276609868328));
#58465=CARTESIAN_POINT('Ctrl Pts',(-6.73292255833172,-0.700636491629351,
41.3359342485414));
#58466=CARTESIAN_POINT('Ctrl Pts',(-6.71244952477012,-0.875356188557083,
41.3442075102499));
#58467=CARTESIAN_POINT('Ctrl Pts',(-6.68518007513384,-1.04912171030509,
41.3524807719585));
#58468=CARTESIAN_POINT('Ctrl Pts',(-6.65792847524227,-1.2227734904762,41.3607486182439));
#58469=CARTESIAN_POINT('Ctrl Pts',(-6.62388937715619,-1.39547199333365,
41.3690164645292));
#58470=CARTESIAN_POINT('Ctrl Pts',(-6.58315107345072,-1.56665597503876,
41.3772843108146));
#58471=CARTESIAN_POINT('Ctrl Pts',(-6.54243168849149,-1.73776045941543,
41.3855483175369));
#58472=CARTESIAN_POINT('Ctrl Pts',(-6.49501937864736,-1.90735148248255,
41.3938123242592));
#58473=CARTESIAN_POINT('Ctrl Pts',(-6.44105354449972,-2.07487788481336,
41.4020763309816));
#58474=CARTESIAN_POINT('Ctrl Pts',(-6.3847966610295,-2.24951640273799,41.4106911753644));
#58475=CARTESIAN_POINT('Ctrl Pts',(-6.32141771498079,-2.42191077070381,
41.4193060197474));
#58476=CARTESIAN_POINT('Ctrl Pts',(-6.25113255705074,-2.59145340575136,
41.4279208641303));
#58477=CARTESIAN_POINT('Ctrl Pts',(-6.18371954334532,-2.75406782274516,
41.4361836700989));
#58478=CARTESIAN_POINT('Ctrl Pts',(-6.10995370878172,-2.91405860628642,
41.4444464760676));
#58479=CARTESIAN_POINT('Ctrl Pts',(-6.03007486180251,-3.07090966344785,
41.4527092820363));
#58480=CARTESIAN_POINT('Ctrl Pts',(-5.95018477644512,-3.22778278842283,
41.4609732505222));
#58481=CARTESIAN_POINT('Ctrl Pts',(-5.8641801242536,-3.38151499281869,41.4692372190082));
#58482=CARTESIAN_POINT('Ctrl Pts',(-5.77234689493559,-3.53161440767922,
41.4775011874941));
#58483=CARTESIAN_POINT('Ctrl Pts',(-5.68048491395558,-3.68176081650563,
41.4857677433096));
#58484=CARTESIAN_POINT('Ctrl Pts',(-5.58279090321834,-3.82827186915964,
41.4940342991251));
#58485=CARTESIAN_POINT('Ctrl Pts',(-5.47959449987094,-3.97068421269989,
41.5023008549406));
#58486=CARTESIAN_POINT('Ctrl Pts',(-5.37634799565992,-4.11316569606644,
41.5105714240896));
#58487=CARTESIAN_POINT('Ctrl Pts',(-5.26759398206475,-4.25154422045178,
41.5188419932387));
#58488=CARTESIAN_POINT('Ctrl Pts',(-5.15370280173387,-4.38538897150531,
41.5271125623877));
#58489=CARTESIAN_POINT('Ctrl Pts',(-5.03967715035149,-4.51939175274485,
41.5353928965785));
#58490=CARTESIAN_POINT('Ctrl Pts',(-4.92050244578517,-4.64884980091141,
41.5436732307692));
#58491=CARTESIAN_POINT('Ctrl Pts',(-4.79658706322744,-4.77336794568355,
41.55195356496));
#58492=CARTESIAN_POINT('Ctrl Pts',(-4.67258598133548,-4.89797220665761,
41.5602396257935));
#58493=CARTESIAN_POINT('Ctrl Pts',(-4.5438379418359,-5.01762951397747,41.5685256866271));
#58494=CARTESIAN_POINT('Ctrl Pts',(-4.41078491776607,-5.13198454880833,
41.5768117474606));
#58495=CARTESIAN_POINT('Ctrl Pts',(-4.27755089760805,-5.24649514428211,
41.5851090800755));
#58496=CARTESIAN_POINT('Ctrl Pts',(-4.1400004714568,-5.35568884362025,41.5934064126903));
#58497=CARTESIAN_POINT('Ctrl Pts',(-3.99860590072931,-5.45925268243308,
41.6017037453052));
#58498=CARTESIAN_POINT('Ctrl Pts',(-3.95811173010324,-5.48891246171598,
41.6040800289271));
#58499=CARTESIAN_POINT('Ctrl Pts',(-3.91730242562021,-5.51811076410782,
41.6064563125491));
#58500=CARTESIAN_POINT('Ctrl Pts',(-3.87618945569539,-5.54684093007505,
41.608832596171));
#58501=CARTESIAN_POINT('Ctrl Pts',(-3.73654292242446,-5.64442736289563,
41.616904009413));
#58502=CARTESIAN_POINT('Ctrl Pts',(-3.59295179309453,-5.73691623808197,
41.6249754226551));
#58503=CARTESIAN_POINT('Ctrl Pts',(-3.44583111845353,-5.82396230268511,
41.6330468358971));
#58504=CARTESIAN_POINT('Ctrl Pts',(-3.29889514163395,-5.91089908816394,
41.6411081161483));
#58505=CARTESIAN_POINT('Ctrl Pts',(-3.14843875307453,-5.9924064714656,41.6491693963995));
#58506=CARTESIAN_POINT('Ctrl Pts',(-2.9949093108269,-6.06817989350368,41.6572306766507));
#58507=CARTESIAN_POINT('Ctrl Pts',(-2.84153894236072,-6.14387480574846,
41.6652836045084));
#58508=CARTESIAN_POINT('Ctrl Pts',(-2.685102188131,-6.21384741588624,41.673336532366));
#58509=CARTESIAN_POINT('Ctrl Pts',(-2.52607448894336,-6.27783694247545,
41.6813894602236));
#58510=CARTESIAN_POINT('Ctrl Pts',(-2.36717673693423,-6.34177418095085,
41.689435807748));
#58511=CARTESIAN_POINT('Ctrl Pts',(-2.20569259806756,-6.3997379281198,41.6974821552723));
#58512=CARTESIAN_POINT('Ctrl Pts',(-2.04212107476457,-6.45151381584217,
41.7055285027967));
#58513=CARTESIAN_POINT('Ctrl Pts',(-1.87864743056523,-6.50325872153675,
41.7135700354899));
#58514=CARTESIAN_POINT('Ctrl Pts',(-1.71308924313668,-6.54882302659542,
41.721611568183));
#58515=CARTESIAN_POINT('Ctrl Pts',(-1.54596430700804,-6.58804093501681,
41.7296531008761));
#58516=CARTESIAN_POINT('Ctrl Pts',(-1.37562643785263,-6.6280127974329,41.7378492299244));
#58517=CARTESIAN_POINT('Ctrl Pts',(-1.20366133405153,-6.66139161775555,
41.7460453589726));
#58518=CARTESIAN_POINT('Ctrl Pts',(-1.03063262690695,-6.68805542653131,
41.7542414880209));
#58519=CARTESIAN_POINT('Ctrl Pts',(-0.860926208888125,-6.71420726892063,
41.7622802448569));
#58520=CARTESIAN_POINT('Ctrl Pts',(-0.690197047214644,-6.73389959282415,
41.770319001693));
#58521=CARTESIAN_POINT('Ctrl Pts',(-0.518985914405807,-6.74706918748047,
41.7783577585291));
#58522=CARTESIAN_POINT('Ctrl Pts',(-0.347758210168852,-6.76024005681436,
41.7863972934319));
#58523=CARTESIAN_POINT('Ctrl Pts',(-0.17604881429155,-6.76688691105645,
41.7944368283347));
#58524=CARTESIAN_POINT('Ctrl Pts',(-0.00440196878264766,-6.76699856824803,
41.8024763632375));
#58525=CARTESIAN_POINT('Ctrl Pts',(0.167295476462347,-6.76711025835501,
41.810518268113));
#58526=CARTESIAN_POINT('Ctrl Pts',(0.338929961368386,-6.76068291650286,
41.8185601729886));
#58527=CARTESIAN_POINT('Ctrl Pts',(0.509959049061346,-6.74775746217071,
41.8266020778641));
#58528=CARTESIAN_POINT('Ctrl Pts',(0.686757338217968,-6.73439600276446,
41.8349152545449));
#58529=CARTESIAN_POINT('Ctrl Pts',(0.862908237529732,-6.71409040300712,
41.8432284312257));
#58530=CARTESIAN_POINT('Ctrl Pts',(1.03782141959566,-6.68694367413308,41.8515416079066));
#58531=CARTESIAN_POINT('Ctrl Pts',(1.20732069672647,-6.66063718958876,41.8595974755171));
#58532=CARTESIAN_POINT('Ctrl Pts',(1.37565738690412,-6.62790690117781,41.8676533431277));
#58533=CARTESIAN_POINT('Ctrl Pts',(1.54230801372537,-6.58889785857988,41.8757092107382));
#58534=CARTESIAN_POINT('Ctrl Pts',(1.71694301664174,-6.54801985891198,41.8841510419542));
#58535=CARTESIAN_POINT('Ctrl Pts',(1.88972595164476,-6.50024679205816,41.8925928731701));
#58536=CARTESIAN_POINT('Ctrl Pts',(2.06007669451811,-6.44580274385614,41.9010347043861));
#58537=CARTESIAN_POINT('Ctrl Pts',(2.23042743739158,-6.39135869565408,41.9094765356021));
#58538=CARTESIAN_POINT('Ctrl Pts',(2.39834558410787,-6.33024390422619,41.9179183668181));
#58539=CARTESIAN_POINT('Ctrl Pts',(2.56327997653748,-6.26273780082497,41.9263601980341));
#58540=CARTESIAN_POINT('Ctrl Pts',(2.72408457402659,-6.19692198384718,41.9345906541006));
#58541=CARTESIAN_POINT('Ctrl Pts',(2.88258802821156,-6.12481253435969,41.9428211101672));
#58542=CARTESIAN_POINT('Ctrl Pts',(3.03826251800127,-6.04658993745306,41.9510515662337));
#58543=CARTESIAN_POINT('Ctrl Pts',(3.19375221299813,-5.9684601953784,41.959272252264));
#58544=CARTESIAN_POINT('Ctrl Pts',(3.34641931321335,-5.88423191491491,41.9674929382942));
#58545=CARTESIAN_POINT('Ctrl Pts',(3.49575407391469,-5.79413431452092,41.9757136243244));
#58546=CARTESIAN_POINT('Ctrl Pts',(3.64494152662763,-5.70412558892214,41.9839262012398));
#58547=CARTESIAN_POINT('Ctrl Pts',(3.79080288120831,-5.60825925737429,41.9921387781551));
#58548=CARTESIAN_POINT('Ctrl Pts',(3.93285111718936,-5.50681133597497,42.0003513550705));
#58549=CARTESIAN_POINT('Ctrl Pts',(4.07478772184563,-5.4054431393662,42.0085574779751));
#58550=CARTESIAN_POINT('Ctrl Pts',(4.21291688604373,-5.29850229706694,42.0167636008798));
#58551=CARTESIAN_POINT('Ctrl Pts',(4.34677874850116,-5.18630923794356,42.0249697237844));
#58552=CARTESIAN_POINT('Ctrl Pts',(4.4805622533377,-5.07418185235132,42.0331710431382));
#58553=CARTESIAN_POINT('Ctrl Pts',(4.61008315853134,-4.95680860427007,42.041372362492));
#58554=CARTESIAN_POINT('Ctrl Pts',(4.7349129404829,-4.83455152481051,42.0495736818457));
#58555=CARTESIAN_POINT('Ctrl Pts',(4.85970691172722,-4.71232951801079,42.0577726484352));
#58556=CARTESIAN_POINT('Ctrl Pts',(4.97981218176148,-4.58522671828342,42.0659716150247));
#58557=CARTESIAN_POINT('Ctrl Pts',(5.09483533201472,-4.45364367003631,42.0741705816143));
#58558=CARTESIAN_POINT('Ctrl Pts',(5.2098432929413,-4.3220779979252,42.0823684654932));
#58559=CARTESIAN_POINT('Ctrl Pts',(5.31977023414561,-4.18603352499365,42.0905663493722));
#58560=CARTESIAN_POINT('Ctrl Pts',(5.42426146289995,-4.0459456968796,42.0987642332511));
#58561=CARTESIAN_POINT('Ctrl Pts',(5.52875787424774,-3.90585092063919,42.1069625237317));
#58562=CARTESIAN_POINT('Ctrl Pts',(5.62781782156914,-3.7617126771366,42.1151608142122));
#58563=CARTESIAN_POINT('Ctrl Pts',(5.72112854872728,-3.6139973891714,42.1233591046927));
#58564=CARTESIAN_POINT('Ctrl Pts',(5.81446085406098,-3.46624794193519,42.131559291034));
#58565=CARTESIAN_POINT('Ctrl Pts',(5.90204109975462,-3.31492010583429,42.1397594773754));
#58566=CARTESIAN_POINT('Ctrl Pts',(5.98360126929088,-3.16050705585996,42.1479596637167));
#58567=CARTESIAN_POINT('Ctrl Pts',(6.06523854756767,-3.00594802046318,42.1561676026908));
#58568=CARTESIAN_POINT('Ctrl Pts',(6.14084421097973,-2.84829826120235,42.1643755416649));
#58569=CARTESIAN_POINT('Ctrl Pts',(6.21019700957568,-2.68807405073917,42.172583480639));
#58570=CARTESIAN_POINT('Ctrl Pts',(6.27958345331552,-2.52777211065692,42.180795401533));
#58571=CARTESIAN_POINT('Ctrl Pts',(6.34271085472138,-2.36489356343775,42.189007322427));
#58572=CARTESIAN_POINT('Ctrl Pts',(6.39940713655381,-2.1999721136015,42.1972192433209));
#58573=CARTESIAN_POINT('Ctrl Pts',(6.45618116835496,-2.03482450012359,42.2054424255635));
#58574=CARTESIAN_POINT('Ctrl Pts',(6.5065063521424,-1.86762872872908,42.213665607806));
#58575=CARTESIAN_POINT('Ctrl Pts',(6.55026093701272,-1.69893221084457,42.2218887900486));
#58576=CARTESIAN_POINT('Ctrl Pts',(6.58927898440913,-1.54849749069047,42.2292217933313));
#58577=CARTESIAN_POINT('Ctrl Pts',(6.62307268442447,-1.39686968340749,42.2365547966141));
#58578=CARTESIAN_POINT('Ctrl Pts',(6.6515904139959,-1.24444122578685,42.2438877998968));
#58579=CARTESIAN_POINT('Ctrl Pts',(6.68633896523764,-1.05870876566714,42.252822986679));
#58580=CARTESIAN_POINT('Ctrl Pts',(6.71332601968396,-0.871402116491395,
42.2617581734613));
#58581=CARTESIAN_POINT('Ctrl Pts',(6.73242731649758,-0.683162812276314,
42.2706933602435));
#58582=CARTESIAN_POINT('Ctrl Pts',(6.75150000547755,-0.495205432307076,
42.2796151648801));
#58583=CARTESIAN_POINT('Ctrl Pts',(6.76271047669215,-0.306318440875435,
42.2885369695166));
#58584=CARTESIAN_POINT('Ctrl Pts',(6.76598585572273,-0.117151185056005,
42.2974587741532));
#58585=CARTESIAN_POINT('Ctrl Pts',(6.76925324532711,0.0715546469659966,
42.3063588163924));
#58586=CARTESIAN_POINT('Ctrl Pts',(6.76462416870618,0.260539121144108,42.3152588586317));
#58587=CARTESIAN_POINT('Ctrl Pts',(6.75207764811812,0.449150791810227,42.3241589008709));
#58588=CARTESIAN_POINT('Ctrl Pts',(6.73955044308297,0.637472092036088,42.3330452413643));
#58589=CARTESIAN_POINT('Ctrl Pts',(6.7191301250787,0.825421477125606,42.3419315818577));
#58590=CARTESIAN_POINT('Ctrl Pts',(6.69084758979494,1.0123475342664,42.350817922351));
#58591=CARTESIAN_POINT('Ctrl Pts',(6.66263736801696,1.19879565410852,42.3596815420229));
#58592=CARTESIAN_POINT('Ctrl Pts',(6.62660508041631,1.38422541235042,42.3685451616948));
#58593=CARTESIAN_POINT('Ctrl Pts',(6.58283314977905,1.56799130168828,42.3774087813667));
#58594=CARTESIAN_POINT('Ctrl Pts',(6.54128026343128,1.74244106899538,42.3858230545206));
#58595=CARTESIAN_POINT('Ctrl Pts',(6.49275295455914,1.91539120841361,42.3942373276746));
#58596=CARTESIAN_POINT('Ctrl Pts',(6.43736502764553,2.08629348387188,42.4026516008285));
#58597=CARTESIAN_POINT('Ctrl Pts',(6.3833201185753,2.2530518092276,42.4108618490331));
#58598=CARTESIAN_POINT('Ctrl Pts',(6.32279423564831,2.41769979886549,42.4190720972376));
#58599=CARTESIAN_POINT('Ctrl Pts',(6.25598808775781,2.57970968247056,42.4272823454422));
#58600=CARTESIAN_POINT('Ctrl Pts',(6.18916605871436,2.74175807905419,42.4354945453863));
#58601=CARTESIAN_POINT('Ctrl Pts',(6.11606092603107,2.9011667911064,42.4437067453305));
#58602=CARTESIAN_POINT('Ctrl Pts',(6.03692112188408,3.05742904548085,42.4519189452747));
#58603=CARTESIAN_POINT('Ctrl Pts',(5.95774841204665,3.21375627243673,42.4601345597852));
#58604=CARTESIAN_POINT('Ctrl Pts',(5.87253619262379,3.3669341180665,42.4683501742958));
#58605=CARTESIAN_POINT('Ctrl Pts',(5.78157835265737,3.51648130267796,42.4765657888063));
#58606=CARTESIAN_POINT('Ctrl Pts',(5.6905183710241,3.66619642222185,42.4847906290917));
#58607=CARTESIAN_POINT('Ctrl Pts',(5.593700066994,3.81227243328368,42.4930154693771));
#58608=CARTESIAN_POINT('Ctrl Pts',(5.49146063118123,3.95425709029986,42.5012403096626));
#58609=CARTESIAN_POINT('Ctrl Pts',(5.38915570745532,4.09633269342515,42.5094704182442));
#58610=CARTESIAN_POINT('Ctrl Pts',(5.281422948332,4.23431143852898,42.5177005268258));
#58611=CARTESIAN_POINT('Ctrl Pts',(5.1686391247196,4.36777501691855,42.5259306354074));
#58612=CARTESIAN_POINT('Ctrl Pts',(5.0557006727549,4.50142157592145,42.5341720275941));
#58613=CARTESIAN_POINT('Ctrl Pts',(4.93769756359107,4.63054034164055,42.5424134197808));
#58614=CARTESIAN_POINT('Ctrl Pts',(4.81504331682191,4.75474992582456,42.5506548119675));
#58615=CARTESIAN_POINT('Ctrl Pts',(4.76166107241942,4.80880909258559,42.5542416752316));
#58616=CARTESIAN_POINT('Ctrl Pts',(4.70739823009763,4.86193887165618,42.5578285384958));
#58617=CARTESIAN_POINT('Ctrl Pts',(4.65229075505896,4.91411026844056,42.5614154017599));
#58618=CARTESIAN_POINT('Ctrl Pts',(4.52249896975261,5.03698686051487,42.5698633552613));
#58619=CARTESIAN_POINT('Ctrl Pts',(4.38772373593038,5.15482456114658,42.5783113087626));
#58620=CARTESIAN_POINT('Ctrl Pts',(4.24838326576361,5.26721260508628,42.586759262264));
#58621=CARTESIAN_POINT('Ctrl Pts',(4.10915498731491,5.37951015839015,42.5952004137902));
#58622=CARTESIAN_POINT('Ctrl Pts',(3.96536905461369,5.48636658937178,42.6036415653164));
#58623=CARTESIAN_POINT('Ctrl Pts',(3.81747902898346,5.58740931588796,42.6120827168425));
#58624=CARTESIAN_POINT('Ctrl Pts',(3.66971391030278,5.68836670237739,42.6205167390273));
#58625=CARTESIAN_POINT('Ctrl Pts',(3.51785188528157,5.78351998852695,42.628950761212));
#58626=CARTESIAN_POINT('Ctrl Pts',(3.36237800086015,5.87253805260823,42.6373847833968));
#58627=CARTESIAN_POINT('Ctrl Pts',(3.27570640570748,5.92216270590637,42.6420864743529));
#58628=CARTESIAN_POINT('Ctrl Pts',(3.18791291542018,5.96988146038011,42.6467881653091));
#58629=CARTESIAN_POINT('Ctrl Pts',(3.09908550384717,6.01564277861014,42.6514898562653));
#58630=CARTESIAN_POINT('Origin',(0.,0.,-63.6971797838103));
#58631=CARTESIAN_POINT('',(3.09908550384733,6.01564277861006,45.0456868593144));
#58632=CARTESIAN_POINT('',(3.09908550384713,6.01564277861016,44.6513967904261));
#58633=CARTESIAN_POINT('',(3.09908550384721,6.01564277861012,-63.6971797838103));
#58634=CARTESIAN_POINT('',(-6.76699891035573,-0.00384021409550919,43.6971797838495));
#58635=CARTESIAN_POINT('Ctrl Pts',(-6.76699891035574,-0.00384021409532003,
43.6971797838495));
#58636=CARTESIAN_POINT('Ctrl Pts',(-6.76688889412393,-0.197704332677314,
43.7062639835883));
#58637=CARTESIAN_POINT('Ctrl Pts',(-6.75844393087704,-0.391285946385338,
43.7153481833271));
#58638=CARTESIAN_POINT('Ctrl Pts',(-6.74176126980812,-0.583904085372994,
43.7244323830658));
#58639=CARTESIAN_POINT('Ctrl Pts',(-6.72503138903265,-0.777067423472387,
43.7335422953239));
#58640=CARTESIAN_POINT('Ctrl Pts',(-6.70001720613928,-0.969261620986978,
43.7426522075821));
#58641=CARTESIAN_POINT('Ctrl Pts',(-6.66686713123509,-1.1598153536047,43.7517621198402));
#58642=CARTESIAN_POINT('Ctrl Pts',(-6.63357584368091,-1.35118080678795,
43.7609108384918));
#58643=CARTESIAN_POINT('Ctrl Pts',(-6.59207929180269,-1.54089158702463,
43.7700595571434));
#58644=CARTESIAN_POINT('Ctrl Pts',(-6.54257710767204,-1.72828637388765,
43.779208275795));
#58645=CARTESIAN_POINT('Ctrl Pts',(-6.49408878146193,-1.91184311416213,
43.7881696188585));
#58646=CARTESIAN_POINT('Ctrl Pts',(-6.43791966665236,-2.09317765977988,
43.7971309619219));
#58647=CARTESIAN_POINT('Ctrl Pts',(-6.37430158871318,-2.2716884152825,43.8060923049854));
#58648=CARTESIAN_POINT('Ctrl Pts',(-6.31086919860206,-2.44967813532555,
43.8150274917677));
#58649=CARTESIAN_POINT('Ctrl Pts',(-6.23993743073889,-2.62512261726111,
43.82396267855));
#58650=CARTESIAN_POINT('Ctrl Pts',(-6.16172172418814,-2.79740493916558,
43.8328978653323));
#58651=CARTESIAN_POINT('Ctrl Pts',(-6.08362316056912,-2.96942923544882,
43.841819669969));
#58652=CARTESIAN_POINT('Ctrl Pts',(-5.99826253221266,-3.13830058685223,
43.8507414746057));
#58653=CARTESIAN_POINT('Ctrl Pts',(-5.90590361626398,-3.30342117741593,
43.8596632792425));
#58654=CARTESIAN_POINT('Ctrl Pts',(-5.81376998561476,-3.46813899969992,
43.8685633214818));
#58655=CARTESIAN_POINT('Ctrl Pts',(-5.71467226302677,-3.62912409593327,
43.8774633637211));
#58656=CARTESIAN_POINT('Ctrl Pts',(-5.60892012914344,-3.78580295114386,
43.8863634059605));
#58657=CARTESIAN_POINT('Ctrl Pts',(-5.50333080222544,-3.94224059695269,
43.8952497464539));
#58658=CARTESIAN_POINT('Ctrl Pts',(-5.39110764306521,-4.09438501285902,
43.9041360869474));
#58659=CARTESIAN_POINT('Ctrl Pts',(-5.27260514316644,-4.24168881511302,
43.9130224274408));
#58660=CARTESIAN_POINT('Ctrl Pts',(-5.15440563347442,-4.3886159872576,43.9218860471127));
#58661=CARTESIAN_POINT('Ctrl Pts',(-5.02995898159621,-4.53072704181745,
43.9307496667846));
#58662=CARTESIAN_POINT('Ctrl Pts',(-4.89966123547151,-4.66750562695085,
43.9396132864566));
#58663=CARTESIAN_POINT('Ctrl Pts',(-4.77596901178222,-4.79735013962594,
43.94802755961));
#58664=CARTESIAN_POINT('Ctrl Pts',(-4.64700432697074,-4.92238917552397,
43.9564418327634));
#58665=CARTESIAN_POINT('Ctrl Pts',(-4.51314140094846,-5.04220623289498,
43.9648561059167));
#58666=CARTESIAN_POINT('Ctrl Pts',(-4.38252431400659,-5.15911802815295,
43.9730663541212));
#58667=CARTESIAN_POINT('Ctrl Pts',(-4.24736849838787,-5.27094489657062,
43.9812766023257));
#58668=CARTESIAN_POINT('Ctrl Pts',(-4.10811297565561,-5.37733175276085,
43.9894868505303));
#58669=CARTESIAN_POINT('Ctrl Pts',(-3.96882434910982,-5.48374389922739,
43.9976990504744));
#58670=CARTESIAN_POINT('Ctrl Pts',(-3.8254343566595,-5.58471324094904,44.0059112504186));
#58671=CARTESIAN_POINT('Ctrl Pts',(-3.67841269500965,-5.6799268520987,44.0141234503628));
#58672=CARTESIAN_POINT('Ctrl Pts',(-3.53132990294273,-5.77518005229731,
44.0223390648732));
#58673=CARTESIAN_POINT('Ctrl Pts',(-3.38061273190973,-5.86467256084481,
44.0305546793837));
#58674=CARTESIAN_POINT('Ctrl Pts',(-3.22675733264959,-5.94813635655674,
44.0387702938941));
#58675=CARTESIAN_POINT('Ctrl Pts',(-3.07272916052049,-6.03169387845254,
44.0469951341795));
#58676=CARTESIAN_POINT('Ctrl Pts',(-2.91555603440391,-6.10920899587778,
44.0552199744649));
#58677=CARTESIAN_POINT('Ctrl Pts',(-2.75575691486018,-6.18046056748203,
44.0634448147503));
#58678=CARTESIAN_POINT('Ctrl Pts',(-2.59585543842534,-6.25175777819479,
44.0716749233318));
#58679=CARTESIAN_POINT('Ctrl Pts',(-2.43332494512286,-6.31678331344898,
44.0799050319133));
#58680=CARTESIAN_POINT('Ctrl Pts',(-2.26870152245154,-6.37536527596859,
44.0881351404949));
#58681=CARTESIAN_POINT('Ctrl Pts',(-2.10385239854164,-6.43402755525774,
44.0963765326815));
#58682=CARTESIAN_POINT('Ctrl Pts',(-1.93690495258762,-6.48622851044388,
44.1046179248682));
#58683=CARTESIAN_POINT('Ctrl Pts',(-1.76840845069959,-6.53184664176175,
44.1128593170549));
#58684=CARTESIAN_POINT('Ctrl Pts',(-1.69507449217272,-6.55170081150803,
44.1164461803194));
#58685=CARTESIAN_POINT('Ctrl Pts',(-1.62144721854119,-6.57030871465975,
44.1200330435839));
#58686=CARTESIAN_POINT('Ctrl Pts',(-1.54757229995239,-6.58766339276834,
44.1236199068484));
#58687=CARTESIAN_POINT('Ctrl Pts',(-1.37356737653549,-6.62854058753074,
44.1320684016769));
#58688=CARTESIAN_POINT('Ctrl Pts',(-1.19779126771295,-6.66255476759419,
44.1405168965053));
#58689=CARTESIAN_POINT('Ctrl Pts',(-1.02081218703135,-6.68956138164591,
44.1489653913337));
#58690=CARTESIAN_POINT('Ctrl Pts',(-0.843994766459049,-6.71654332672453,
44.1574061689529));
#58691=CARTESIAN_POINT('Ctrl Pts',(-0.665976892409825,-6.73653041487473,
44.1658469465721));
#58692=CARTESIAN_POINT('Ctrl Pts',(-0.487337925993888,-6.7494289199819,
44.1742877241913));
#58693=CARTESIAN_POINT('Ctrl Pts',(-0.30883466506351,-6.76231762656675,
44.1827220896606));
#58694=CARTESIAN_POINT('Ctrl Pts',(-0.129711583760677,-6.76812846110855,
44.1911564551299));
#58695=CARTESIAN_POINT('Ctrl Pts',(0.0494454626071732,-6.76681935226792,
44.1995908205993));
#58696=CARTESIAN_POINT('Ctrl Pts',(0.22849392265844,-6.76551103687253,44.2080200740359));
#58697=CARTESIAN_POINT('Ctrl Pts',(0.407575974118805,-6.75709138424464,
44.2164493274725));
#58698=CARTESIAN_POINT('Ctrl Pts',(0.58610397752143,-6.74157037547882,44.2248785809091));
#58699=CARTESIAN_POINT('Ctrl Pts',(0.76455116154374,-6.7260563930522,44.2333040184344));
#58700=CARTESIAN_POINT('Ctrl Pts',(0.942444466007396,-6.70344749362747,
44.2417294559597));
#58701=CARTESIAN_POINT('Ctrl Pts',(1.11919919384768,-6.673805673264,44.2501548934849));
#58702=CARTESIAN_POINT('Ctrl Pts',(1.29591509342742,-6.64417036441135,44.2585784801681));
#58703=CARTESIAN_POINT('Ctrl Pts',(1.47149258608872,-6.60750526743822,44.2670020668513));
#58704=CARTESIAN_POINT('Ctrl Pts',(1.64535448228701,-6.5639239504749,44.2754256535345));
#58705=CARTESIAN_POINT('Ctrl Pts',(1.81919692425085,-6.52034751003241,44.2838482976625));
#58706=CARTESIAN_POINT('Ctrl Pts',(1.99132382911603,-6.46985647344597,44.2922709417905));
#58707=CARTESIAN_POINT('Ctrl Pts',(2.16117023800555,-6.41261508297193,44.3006935859185));
#58708=CARTESIAN_POINT('Ctrl Pts',(2.33102132636682,-6.3553721154291,44.3091164621004));
#58709=CARTESIAN_POINT('Ctrl Pts',(2.49859147766921,-6.29137853005043,44.3175393382824));
#58710=CARTESIAN_POINT('Ctrl Pts',(2.66333252815353,-6.22084792005715,44.3259622144643));
#58711=CARTESIAN_POINT('Ctrl Pts',(2.82810109130764,-6.15030553106053,44.3343864973133));
#58712=CARTESIAN_POINT('Ctrl Pts',(2.99003930545369,-6.07322407264201,44.3428107801623));
#58713=CARTESIAN_POINT('Ctrl Pts',(3.1486202233711,-5.98986474713566,44.3512350630113));
#58714=CARTESIAN_POINT('Ctrl Pts',(3.30730824097709,-5.90644912382299,44.3596650353095));
#58715=CARTESIAN_POINT('Ctrl Pts',(3.46263413618509,-5.81674731655718,44.3680950076077));
#58716=CARTESIAN_POINT('Ctrl Pts',(3.61409586825149,-5.72106633898678,44.3765249799058));
#58717=CARTESIAN_POINT('Ctrl Pts',(3.76561174544246,-5.62535115701121,44.384957965783));
#58718=CARTESIAN_POINT('Ctrl Pts',(3.91326042653645,-5.52365272598554,44.3933909516602));
#58719=CARTESIAN_POINT('Ctrl Pts',(4.05656951705068,-5.41632096107083,44.4018239375374));
#58720=CARTESIAN_POINT('Ctrl Pts',(4.20001045105504,-5.30889045158634,44.4102646817103));
#58721=CARTESIAN_POINT('Ctrl Pts',(4.33910355456252,-5.19581645837651,44.4187054258831));
#58722=CARTESIAN_POINT('Ctrl Pts',(4.47340928254556,-5.07748937870235,44.4271461700559));
#58723=CARTESIAN_POINT('Ctrl Pts',(4.54767050652973,-5.01206317611936,44.431813282941));
#58724=CARTESIAN_POINT('Ctrl Pts',(4.62046872254336,-4.94503163854069,44.4364803958261));
#58725=CARTESIAN_POINT('Ctrl Pts',(4.69173451581017,-4.87646554721301,44.4411475087112));
#58726=CARTESIAN_POINT('Ctrl Pts',(4.81605141307395,-4.75685804211657,44.449288875929));
#58727=CARTESIAN_POINT('Ctrl Pts',(4.93594998097428,-4.63234113408405,44.4574302431468));
#58728=CARTESIAN_POINT('Ctrl Pts',(5.05101697431889,-4.50327841967855,44.4655716103647));
#58729=CARTESIAN_POINT('Ctrl Pts',(5.16598352292975,-4.37432836720682,44.4737058707881));
#58730=CARTESIAN_POINT('Ctrl Pts',(5.27612665022993,-4.24084067836807,44.4818401312116));
#58731=CARTESIAN_POINT('Ctrl Pts',(5.38106859648469,-4.10321700132059,44.489974391635));
#58732=CARTESIAN_POINT('Ctrl Pts',(5.48593895513416,-3.96568720617469,44.4981031031598));
#58733=CARTESIAN_POINT('Ctrl Pts',(5.58561497575892,-3.82402733007337,44.5062318146846));
#58734=CARTESIAN_POINT('Ctrl Pts',(5.67975801198224,-3.67867339204279,44.5143605262093));
#58735=CARTESIAN_POINT('Ctrl Pts',(5.77385615313152,-3.53338877061884,44.5224853613018));
#58736=CARTESIAN_POINT('Ctrl Pts',(5.86242636564597,-3.38441390187614,44.5306101963943));
#58737=CARTESIAN_POINT('Ctrl Pts',(5.94517233844275,-3.23221516397272,44.5387350314868));
#58738=CARTESIAN_POINT('Ctrl Pts',(6.0278951462725,-3.0800590345326,44.5468575920089));
#58739=CARTESIAN_POINT('Ctrl Pts',(6.10479678808972,-2.92468115530904,44.5549801525311));
#58740=CARTESIAN_POINT('Ctrl Pts',(6.1756260950989,-2.76657393422506,44.5631027130532));
#58741=CARTESIAN_POINT('Ctrl Pts',(6.246459166502,-2.60845831015246,44.5712257052683));
#58742=CARTESIAN_POINT('Ctrl Pts',(6.31121910514574,-2.44761338690518,44.5793486974835));
#58743=CARTESIAN_POINT('Ctrl Pts',(6.36970215766022,-2.28455322168226,44.5874716896986));
#58744=CARTESIAN_POINT('Ctrl Pts',(6.39955597372514,-2.20131597651837,44.5916182296801));
#58745=CARTESIAN_POINT('Ctrl Pts',(6.42777494090506,-2.11750180098473,44.5957647696615));
#58746=CARTESIAN_POINT('Ctrl Pts',(6.45433689979305,-2.03318080454491,44.5999113096429));
#58747=CARTESIAN_POINT('Ctrl Pts',(6.5118845377867,-1.85049570218309,44.6088949686714));
#58748=CARTESIAN_POINT('Ctrl Pts',(6.56162305658886,-1.66552119221636,44.6178786276999));
#58749=CARTESIAN_POINT('Ctrl Pts',(6.60341601288126,-1.47891377734583,44.6268622867283));
#58750=CARTESIAN_POINT('Ctrl Pts',(6.64528076902984,-1.29198577291342,44.6358613795878));
#58751=CARTESIAN_POINT('Ctrl Pts',(6.67917262709894,-1.10341948994128,44.6448604724474));
#58752=CARTESIAN_POINT('Ctrl Pts',(6.70500649420441,-0.913880141307793,
44.6538595653069));
#58753=CARTESIAN_POINT('Ctrl Pts',(6.730900934509,-0.72389637586825,44.6628797585243));
#58754=CARTESIAN_POINT('Ctrl Pts',(6.74869954840513,-0.532935217663735,
44.6718999517418));
#58755=CARTESIAN_POINT('Ctrl Pts',(6.75836901832327,-0.341668277965887,
44.6809201449593));
#58756=CARTESIAN_POINT('Ctrl Pts',(6.76804828100098,-0.150207632597564,
44.6899494733811));
#58757=CARTESIAN_POINT('Ctrl Pts',(6.76958194657552,0.0415591739957861,
44.6989788018029));
#58758=CARTESIAN_POINT('Ctrl Pts',(6.76298886987241,0.232960395736803,44.7080081302247));
#58759=CARTESIAN_POINT('Ctrl Pts',(6.75638649826011,0.42463145462011,44.7170501881796));
#58760=CARTESIAN_POINT('Ctrl Pts',(6.74163448406952,0.615935658974207,44.7260922461344));
#58761=CARTESIAN_POINT('Ctrl Pts',(6.71880378020087,0.806203921572273,44.7351343040893));
#58762=CARTESIAN_POINT('Ctrl Pts',(6.69899069545212,0.971323719610178,44.7429812395843));
#58763=CARTESIAN_POINT('Ctrl Pts',(6.67309419700013,1.13566332147699,44.7508281750793));
#58764=CARTESIAN_POINT('Ctrl Pts',(6.6411920100604,1.29879085518415,44.7586751105743));
#58765=CARTESIAN_POINT('Ctrl Pts',(6.60601083188276,1.47868506870226,44.767328574875));
#58766=CARTESIAN_POINT('Ctrl Pts',(6.56349363194616,1.65726355612998,44.7759820391758));
#58767=CARTESIAN_POINT('Ctrl Pts',(6.51375604940836,1.83392233445042,44.7846355034765));
#58768=CARTESIAN_POINT('Ctrl Pts',(6.46406428535748,2.01041837390193,44.7932809961666));
#58769=CARTESIAN_POINT('Ctrl Pts',(6.40716548729329,2.18499793983939,44.8019264888567));
#58770=CARTESIAN_POINT('Ctrl Pts',(6.34322602845369,2.35706863539178,44.8105719815468));
#58771=CARTESIAN_POINT('Ctrl Pts',(6.27736306075519,2.53431578243841,44.8194775590434));
#58772=CARTESIAN_POINT('Ctrl Pts',(6.20402925680783,2.70890043112542,44.82838313654));
#58773=CARTESIAN_POINT('Ctrl Pts',(6.12346210347251,2.88019111646017,44.8372887140366));
#58774=CARTESIAN_POINT('Ctrl Pts',(6.04539629918276,3.04616378105642,44.8459178022091));
#58775=CARTESIAN_POINT('Ctrl Pts',(5.96053968343559,3.20904364133053,44.8545468903816));
#58776=CARTESIAN_POINT('Ctrl Pts',(5.86915756771335,3.36827529239419,44.8631759785541));
#58777=CARTESIAN_POINT('Ctrl Pts',(5.77338341561825,3.53515998582456,44.8722198007128));
#58778=CARTESIAN_POINT('Ctrl Pts',(5.67044115448376,3.6980368238629,44.8812636228714));
#58779=CARTESIAN_POINT('Ctrl Pts',(5.56069135782519,3.85629363806859,44.8903074450301));
#58780=CARTESIAN_POINT('Ctrl Pts',(5.45094156116662,4.01455045227428,44.8993512671887));
#58781=CARTESIAN_POINT('Ctrl Pts',(5.33438442010266,4.16818690627899,44.9083950893474));
#58782=CARTESIAN_POINT('Ctrl Pts',(5.21143435583699,4.31662379120557,44.9174389115061));
#58783=CARTESIAN_POINT('Ctrl Pts',(5.09689635502667,4.45490484170802,44.9258639685886));
#58784=CARTESIAN_POINT('Ctrl Pts',(4.97686061622874,4.58861306477576,44.9342890256711));
#58785=CARTESIAN_POINT('Ctrl Pts',(4.85172589363782,4.71731330876001,44.9427140827536));
#58786=CARTESIAN_POINT('Ctrl Pts',(4.72427403878008,4.84839670812998,44.951295147467));
#58787=CARTESIAN_POINT('Ctrl Pts',(4.59153275331571,4.97428458065801,44.9598762121804));
#58788=CARTESIAN_POINT('Ctrl Pts',(4.45396213209447,5.09455693126188,44.9684572768938));
#58789=CARTESIAN_POINT('Ctrl Pts',(4.31877156467922,5.21274849845961,44.9768898840692));
#58790=CARTESIAN_POINT('Ctrl Pts',(4.17891768344854,5.32551707867113,44.9853224912446));
#58791=CARTESIAN_POINT('Ctrl Pts',(4.03487008848478,5.43250516511958,44.99375509842));
#58792=CARTESIAN_POINT('Ctrl Pts',(3.88701851851171,5.54231856779246,45.0024103919024));
#58793=CARTESIAN_POINT('Ctrl Pts',(3.73474899182892,5.64604174992405,45.0110656853848));
#58794=CARTESIAN_POINT('Ctrl Pts',(3.57860057541301,5.74333587052452,45.0197209788672));
#58795=CARTESIAN_POINT('Ctrl Pts',(3.4224521589971,5.84062999112499,45.0283762723496));
#58796=CARTESIAN_POINT('Ctrl Pts',(3.26242519189843,5.93149488651081,45.037031565832));
#58797=CARTESIAN_POINT('Ctrl Pts',(3.09908550384733,6.01564277861006,45.0456868593144));
#58798=CARTESIAN_POINT('Ctrl Pts',(3.09908550384712,6.01564277861017,43.045630740225));
#58799=CARTESIAN_POINT('Ctrl Pts',(2.9419576178338,6.09659052961784,43.0539354227508));
#58800=CARTESIAN_POINT('Ctrl Pts',(2.78171701424298,6.17134687375159,43.0622401052765));
#58801=CARTESIAN_POINT('Ctrl Pts',(2.61889088468052,6.23968745484398,43.0705447878023));
#58802=CARTESIAN_POINT('Ctrl Pts',(2.4546986312921,6.30860141869969,43.078919147257));
#58803=CARTESIAN_POINT('Ctrl Pts',(2.28787760231696,6.37099133390253,43.0872935067117));
#58804=CARTESIAN_POINT('Ctrl Pts',(2.11898561054603,6.42667791182185,43.0956678661665));
#58805=CARTESIAN_POINT('Ctrl Pts',(1.95120332122819,6.4819986018653,43.1039872020104));
#58806=CARTESIAN_POINT('Ctrl Pts',(1.7813775537115,6.5307037424505,43.1123065378543));
#58807=CARTESIAN_POINT('Ctrl Pts',(1.61006699785046,6.57266865606603,43.1206258736982));
#58808=CARTESIAN_POINT('Ctrl Pts',(1.43705688468038,6.61504989998473,43.1290277449583));
#58809=CARTESIAN_POINT('Ctrl Pts',(1.26253272416397,6.65055639756547,43.1374296162185));
#58810=CARTESIAN_POINT('Ctrl Pts',(1.08707678624679,6.67911319419003,43.1458314874786));
#58811=CARTESIAN_POINT('Ctrl Pts',(0.911620848329616,6.70766999081459,43.1542333587388));
#58812=CARTESIAN_POINT('Ctrl Pts',(0.735233496888212,6.72927709584685,43.162635229999));
#58813=CARTESIAN_POINT('Ctrl Pts',(0.558498370545718,6.74391344621932,43.1710371012591));
#58814=CARTESIAN_POINT('Ctrl Pts',(0.388714498010424,6.75797412729302,43.1791085145012));
#58815=CARTESIAN_POINT('Ctrl Pts',(0.21808693188033,6.76564472910105,43.1871799277432));
#58816=CARTESIAN_POINT('Ctrl Pts',(0.0471480780741471,6.7668357493539,43.1952513409852));
#58817=CARTESIAN_POINT('Ctrl Pts',(-0.123576176159475,6.76802527437947,
43.2033126212365));
#58818=CARTESIAN_POINT('Ctrl Pts',(-0.294610572263851,6.76275140100793,
43.2113739014877));
#58819=CARTESIAN_POINT('Ctrl Pts',(-0.465415262605885,6.75097605041919,
43.2194351817389));
#58820=CARTESIAN_POINT('Ctrl Pts',(-0.636042980065169,6.73921290041894,
43.2274881095966));
#58821=CARTESIAN_POINT('Ctrl Pts',(-0.806441096464912,6.72096170399405,
43.2355410374542));
#58822=CARTESIAN_POINT('Ctrl Pts',(-0.976067524947408,6.69623634489876,
43.2435939653119));
#58823=CARTESIAN_POINT('Ctrl Pts',(-1.1455553456542,6.67153118977202,43.2516403128363));
#58824=CARTESIAN_POINT('Ctrl Pts',(-1.31427236631446,6.6403624549363,43.2596866603607));
#58825=CARTESIAN_POINT('Ctrl Pts',(-1.48167949414037,6.60279598932482,43.2677330078851));
#58826=CARTESIAN_POINT('Ctrl Pts',(-1.64898644768527,6.56525200300518,43.2757745405783));
#58827=CARTESIAN_POINT('Ctrl Pts',(-1.81498470576385,6.52131798844838,43.2838160732714));
#58828=CARTESIAN_POINT('Ctrl Pts',(-1.97914337764906,6.47111122533896,43.2918576059646));
#58829=CARTESIAN_POINT('Ctrl Pts',(-2.14645795690911,6.41993925038819,43.3000537350128));
#58830=CARTESIAN_POINT('Ctrl Pts',(-2.31186110747613,6.36225094694745,43.3082498640611));
#58831=CARTESIAN_POINT('Ctrl Pts',(-2.47480438153987,6.29822453339916,43.3164459931093));
#58832=CARTESIAN_POINT('Ctrl Pts',(-2.63461901483382,6.23542747803655,43.3244847499454));
#58833=CARTESIAN_POINT('Ctrl Pts',(-2.79206702665504,6.16653366234927,43.3325235067815));
#58834=CARTESIAN_POINT('Ctrl Pts',(-2.94664929054513,6.09176057954758,43.3405622636176));
#58835=CARTESIAN_POINT('Ctrl Pts',(-3.10124651636469,6.0169802595017,43.3486017985203));
#58836=CARTESIAN_POINT('Ctrl Pts',(-3.25297710568235,5.93631970179732,43.3566413334231));
#58837=CARTESIAN_POINT('Ctrl Pts',(-3.4013651148282,5.85004310715996,43.3646808683259));
#58838=CARTESIAN_POINT('Ctrl Pts',(-3.54979686724296,5.76374107906406,43.3727227732014));
#58839=CARTESIAN_POINT('Ctrl Pts',(-3.69488375546739,5.67181990632548,43.380764678077));
#58840=CARTESIAN_POINT('Ctrl Pts',(-3.83617761333508,5.57458790575113,43.3888065829525));
#58841=CARTESIAN_POINT('Ctrl Pts',(-3.98223763549984,5.47407604788741,43.3971197596333));
#58842=CARTESIAN_POINT('Ctrl Pts',(-4.12424389634693,5.3678890496725,43.4054329363142));
#58843=CARTESIAN_POINT('Ctrl Pts',(-4.26173808893117,5.25641298428437,43.413746112995));
#58844=CARTESIAN_POINT('Ctrl Pts',(-4.39497656745786,5.14838732105241,43.4218019806055));
#58845=CARTESIAN_POINT('Ctrl Pts',(-4.52397790198581,5.03539542431061,43.429857848216));
#58846=CARTESIAN_POINT('Ctrl Pts',(-4.6483627099482,4.91782605596854,43.4379137158265));
#58847=CARTESIAN_POINT('Ctrl Pts',(-4.77870690195993,4.7946238372015,43.4463555470425));
#58848=CARTESIAN_POINT('Ctrl Pts',(-4.90398098136119,4.66639508233387,43.4547973782585));
#58849=CARTESIAN_POINT('Ctrl Pts',(-5.02379638349647,4.5336253591544,43.4632392094745));
#58850=CARTESIAN_POINT('Ctrl Pts',(-5.14361178563174,4.40085563597493,43.4716810406904));
#58851=CARTESIAN_POINT('Ctrl Pts',(-5.25796828117685,4.26354535356909,43.4801228719063));
#58852=CARTESIAN_POINT('Ctrl Pts',(-5.36653018699977,4.12221333169697,43.4885647031223));
#58853=CARTESIAN_POINT('Ctrl Pts',(-5.47831305615991,3.97668807779401,43.497256998151));
#58854=CARTESIAN_POINT('Ctrl Pts',(-5.58432744583572,3.82641131247741,43.5059492931796));
#58855=CARTESIAN_POINT('Ctrl Pts',(-5.68415610484355,3.67187395967915,43.5146415882083));
#58856=CARTESIAN_POINT('Ctrl Pts',(-5.78007555539817,3.52338816293602,43.522993500089));
#58857=CARTESIAN_POINT('Ctrl Pts',(-5.87028426080624,3.37096942442776,43.5313454119698));
#58858=CARTESIAN_POINT('Ctrl Pts',(-5.9544518841414,3.21508814178476,43.5396973238505));
#58859=CARTESIAN_POINT('Ctrl Pts',(-6.03853035496607,3.05937197260385,43.5480403891715));
#58860=CARTESIAN_POINT('Ctrl Pts',(-6.11658032902696,2.90020086545064,43.5563834544924));
#58861=CARTESIAN_POINT('Ctrl Pts',(-6.18831481050102,2.73807392269341,43.5647265198134));
#58862=CARTESIAN_POINT('Ctrl Pts',(-6.25998471771382,2.5760929240811,43.5730620748371));
#58863=CARTESIAN_POINT('Ctrl Pts',(-6.32535032107552,2.41116170357753,43.5813976298608));
#58864=CARTESIAN_POINT('Ctrl Pts',(-6.38417050338549,2.24380390936968,43.5897331848846));
#58865=CARTESIAN_POINT('Ctrl Pts',(-6.44294708442541,2.07657017143119,43.5980625610633));
#58866=CARTESIAN_POINT('Ctrl Pts',(-6.4951877993785,1.90691376699399,43.6063919372421));
#58867=CARTESIAN_POINT('Ctrl Pts',(-6.54069953748574,1.73537850635929,43.6147213134209));
#58868=CARTESIAN_POINT('Ctrl Pts',(-6.58618145098423,1.56395565567086,43.6230452312191));
#58869=CARTESIAN_POINT('Ctrl Pts',(-6.62494309208294,1.39065673491937,43.6313691490173));
#58870=CARTESIAN_POINT('Ctrl Pts',(-6.65684108440876,1.21604102600513,43.6396930668155));
#58871=CARTESIAN_POINT('Ctrl Pts',(-6.68872682337062,1.04149239434806,43.6480137870459));
#58872=CARTESIAN_POINT('Ctrl Pts',(-6.71375410681703,0.865628319988322,
43.6563345072763));
#58873=CARTESIAN_POINT('Ctrl Pts',(-6.73183049171232,0.689019035188684,
43.6646552275067));
#58874=CARTESIAN_POINT('Ctrl Pts',(-6.74990324280198,0.512445253273955,
43.6729742750641));
#58875=CARTESIAN_POINT('Ctrl Pts',(-6.76102784515868,0.335126900850402,
43.6812933226216));
#58876=CARTESIAN_POINT('Ctrl Pts',(-6.76516359776396,0.157640399293324,
43.689612370179));
#58877=CARTESIAN_POINT('Ctrl Pts',(-6.76641762556073,0.103823590662527,
43.6921348413893));
#58878=CARTESIAN_POINT('Ctrl Pts',(-6.76702945930099,0.0499913483530002,
43.6946573125995));
#58879=CARTESIAN_POINT('Ctrl Pts',(-6.76699891035622,-0.00384021324774086,
43.6971797838098));
#58880=CARTESIAN_POINT('',(-6.76699984387958,0.000602726414096441,43.3028202161897));
#58881=CARTESIAN_POINT('Ctrl Pts',(3.09908550384717,6.01564277861014,42.6514898562653));
#58882=CARTESIAN_POINT('Ctrl Pts',(2.93987777019309,6.09766200708263,42.6599168220883));
#58883=CARTESIAN_POINT('Ctrl Pts',(2.77734729302395,6.17339041892882,42.6683437879113));
#58884=CARTESIAN_POINT('Ctrl Pts',(2.61202061225415,6.24256656521654,42.6767707537343));
#58885=CARTESIAN_POINT('Ctrl Pts',(2.44674469261368,6.31172147198447,42.6851951321813));
#58886=CARTESIAN_POINT('Ctrl Pts',(2.27867458764138,6.37432799404581,42.6936195106282));
#58887=CARTESIAN_POINT('Ctrl Pts',(2.10835819139115,6.43017221672902,42.7020438890751));
#58888=CARTESIAN_POINT('Ctrl Pts',(1.93807135869421,6.48600674596116,42.7104668052168));
#58889=CARTESIAN_POINT('Ctrl Pts',(1.76553932864102,6.5350812117948,42.7188897213584));
#58890=CARTESIAN_POINT('Ctrl Pts',(1.59132692617963,6.57723099898549,42.7273126375001));
#58891=CARTESIAN_POINT('Ctrl Pts',(1.4171204692445,6.61937934768694,42.7357352661842));
#58892=CARTESIAN_POINT('Ctrl Pts',(1.24123407831885,6.65460341070326,42.7441578948684));
#58893=CARTESIAN_POINT('Ctrl Pts',(1.06424495043908,6.68278921450205,42.7525805235525));
#58894=CARTESIAN_POINT('Ctrl Pts',(0.88723718228041,6.7109779867953,42.7610040392976));
#58895=CARTESIAN_POINT('Ctrl Pts',(0.709126774946567,6.73212697011826,42.7694275550427));
#58896=CARTESIAN_POINT('Ctrl Pts',(0.530498633683403,6.74617374514325,42.7778510707878));
#58897=CARTESIAN_POINT('Ctrl Pts',(0.35175453806,6.76022963846729,42.7862800545592));
#58898=CARTESIAN_POINT('Ctrl Pts',(0.17249236956393,6.76717408219812,42.7947090383307));
#58899=CARTESIAN_POINT('Ctrl Pts',(-0.00669927327009474,6.766996683887,
42.8031380221021));
#58900=CARTESIAN_POINT('Ctrl Pts',(-0.185944842087931,6.76681923218958,
42.8115695424943));
#58901=CARTESIAN_POINT('Ctrl Pts',(-0.365119509352608,6.75951567108584,
42.8200010628864));
#58902=CARTESIAN_POINT('Ctrl Pts',(-0.543636598857979,6.74512774144287,
42.8284325832786));
#58903=CARTESIAN_POINT('Ctrl Pts',(-0.722332975389522,6.73072536181572,
42.836872571556));
#58904=CARTESIAN_POINT('Ctrl Pts',(-0.90037012165086,6.70922442470045,42.8453125598334));
#58905=CARTESIAN_POINT('Ctrl Pts',(-1.07716704268992,6.68071853636588,42.8537525481108));
#58906=CARTESIAN_POINT('Ctrl Pts',(-1.25305966353853,6.6523584530606,42.8621493666148));
#58907=CARTESIAN_POINT('Ctrl Pts',(-1.42772440839463,6.61706502585254,42.8705461851189));
#58908=CARTESIAN_POINT('Ctrl Pts',(-1.60060127131946,6.57498019542649,42.8789430036229));
#58909=CARTESIAN_POINT('Ctrl Pts',(-1.76821880692063,6.53417568611933,42.8870843708408));
#58910=CARTESIAN_POINT('Ctrl Pts',(-1.93448858358166,6.48690531125586,42.8952257380586));
#58911=CARTESIAN_POINT('Ctrl Pts',(-2.09887052513986,6.43327533366163,42.9033671052764));
#58912=CARTESIAN_POINT('Ctrl Pts',(-2.26310897376519,6.379692170959,42.9115013656999));
#58913=CARTESIAN_POINT('Ctrl Pts',(-2.42546252190072,6.31976056852021,42.9196356261233));
#58914=CARTESIAN_POINT('Ctrl Pts',(-2.58540261115405,6.25363752852992,42.9277698865468));
#58915=CARTESIAN_POINT('Ctrl Pts',(-2.74523359505533,6.18755959528923,42.9358985980716));
#58916=CARTESIAN_POINT('Ctrl Pts',(-2.90265406105496,6.11529877278384,42.9440273095964));
#58917=CARTESIAN_POINT('Ctrl Pts',(-3.05715195579901,6.03706144735618,42.9521560211212));
#58918=CARTESIAN_POINT('Ctrl Pts',(-3.21157617335267,5.95886143186294,42.9602808562137));
#58919=CARTESIAN_POINT('Ctrl Pts',(-3.36308026916501,5.87469075398754,42.9684056913062));
#58920=CARTESIAN_POINT('Ctrl Pts',(-3.51117349793127,5.78480333869917,42.9765305263987));
#58921=CARTESIAN_POINT('Ctrl Pts',(-3.65922526758303,5.69494108764467,42.9846530869209));
#58922=CARTESIAN_POINT('Ctrl Pts',(-3.80386775991283,5.59936547737208,42.992775647443));
#58923=CARTESIAN_POINT('Ctrl Pts',(-3.94463614192823,5.49837564265971,43.0008982079652));
#58924=CARTESIAN_POINT('Ctrl Pts',(-4.08541200541813,5.39738044059949,43.0090212001803));
#58925=CARTESIAN_POINT('Ctrl Pts',(-4.22231304754953,5.29097064945622,43.0171441923955));
#58926=CARTESIAN_POINT('Ctrl Pts',(-4.35490451628916,5.17948797218454,43.0252671846107));
#58927=CARTESIAN_POINT('Ctrl Pts',(-4.42258842041516,5.12257946282197,43.029413724592));
#58928=CARTESIAN_POINT('Ctrl Pts',(-4.48914985206684,5.06434972862147,43.0335602645733));
#58929=CARTESIAN_POINT('Ctrl Pts',(-4.55453438253697,5.00484820531937,43.0377068045546));
#58930=CARTESIAN_POINT('Ctrl Pts',(-4.69619280862793,4.8759355698629,43.046690463583));
#58931=CARTESIAN_POINT('Ctrl Pts',(-4.83225487386259,4.74111493348462,43.0556741226114));
#58932=CARTESIAN_POINT('Ctrl Pts',(-4.96227231454179,4.60088496664849,43.0646577816398));
#58933=CARTESIAN_POINT('Ctrl Pts',(-5.09251312380689,4.4604140862147,43.0736568744992));
#58934=CARTESIAN_POINT('Ctrl Pts',(-5.21668838999999,4.31451547627411,43.0826559673587));
#58935=CARTESIAN_POINT('Ctrl Pts',(-5.33438984187612,4.16372117400876,43.0916550602181));
#58936=CARTESIAN_POINT('Ctrl Pts',(-5.45236727076581,4.01257330124332,43.1006752534355));
#58937=CARTESIAN_POINT('Ctrl Pts',(-5.56384036654162,3.8565069579234,43.109695446653));
#58938=CARTESIAN_POINT('Ctrl Pts',(-5.66844238087631,3.69608576397861,43.1187156398704));
#58939=CARTESIAN_POINT('Ctrl Pts',(-5.77315033094328,3.53550210340483,43.1277449682922));
#58940=CARTESIAN_POINT('Ctrl Pts',(-5.87097317237599,3.37055498480376,43.1367742967139));
#58941=CARTESIAN_POINT('Ctrl Pts',(-5.96158917476093,3.20183439786841,43.1458036251357));
#58942=CARTESIAN_POINT('Ctrl Pts',(-6.05233292744388,3.03287594891427,43.1548456830905));
#58943=CARTESIAN_POINT('Ctrl Pts',(-6.13584941245282,2.86013360535714,43.1638877410453));
#58944=CARTESIAN_POINT('Ctrl Pts',(-6.21186325883687,2.68422127506519,43.1729297990001));
#58945=CARTESIAN_POINT('Ctrl Pts',(-6.27783007217801,2.53155993231266,43.1807767344954));
#58946=CARTESIAN_POINT('Ctrl Pts',(-6.33814719360531,2.37651162294236,43.1886236699907));
#58947=CARTESIAN_POINT('Ctrl Pts',(-6.39266447184091,2.21948866869443,43.196470605486));
#58948=CARTESIAN_POINT('Ctrl Pts',(-6.45445102698719,2.04152843781232,43.2053638431604));
#58949=CARTESIAN_POINT('Ctrl Pts',(-6.50883338074033,1.8608973894608,43.2142570808348));
#58950=CARTESIAN_POINT('Ctrl Pts',(-6.55560081224318,1.67820945966723,43.2231503185091));
#58951=CARTESIAN_POINT('Ctrl Pts',(-6.6023193763613,1.49571242086473,43.2320342636213));
#58952=CARTESIAN_POINT('Ctrl Pts',(-6.64143882873939,1.31116304398865,43.2409182087335));
#58953=CARTESIAN_POINT('Ctrl Pts',(-6.67279818559416,1.12519037248425,43.2498021538456));
#58954=CARTESIAN_POINT('Ctrl Pts',(-6.70410369344196,0.939537045656859,
43.25867084381));
#58955=CARTESIAN_POINT('Ctrl Pts',(-6.72767566198704,0.752465562753678,
43.2675395337744));
#58956=CARTESIAN_POINT('Ctrl Pts',(-6.74340410743541,0.564614951824003,
43.2764082237388));
#58957=CARTESIAN_POINT('Ctrl Pts',(-6.75901782205446,0.37813461340171,43.2852122212224));
#58958=CARTESIAN_POINT('Ctrl Pts',(-6.76690201965948,0.190886734716022,
43.2940162187061));
#58959=CARTESIAN_POINT('Ctrl Pts',(-6.76699909195969,0.00350562643901177,
43.3028202161897));
#58960=CARTESIAN_POINT('Ctrl Pts',(-6.767,5.35191256783216E-12,43.3028202161897));
#58961=CARTESIAN_POINT('Ctrl Pts',(-6.76700000000015,-0.18600724955472,
43.3115697280024));
#58962=CARTESIAN_POINT('Ctrl Pts',(-6.75932637294276,-0.372014355810972,
43.3203192398152));
#58963=CARTESIAN_POINT('Ctrl Pts',(-6.74400518263404,-0.557389537581421,
43.3290687516279));
#58964=CARTESIAN_POINT('Ctrl Pts',(-6.72868405703783,-0.742763936377903,
43.3378182264851));
#58965=CARTESIAN_POINT('Ctrl Pts',(-6.7057154564363,-0.927506130400228,
43.3465677013423));
#58966=CARTESIAN_POINT('Ctrl Pts',(-6.67517739401653,-1.11098864009077,
43.3553171761995));
#58967=CARTESIAN_POINT('Ctrl Pts',(-6.64463945804479,-1.2944703900408,43.364066614828));
#58968=CARTESIAN_POINT('Ctrl Pts',(-6.60653217002826,-1.47669218338824,
43.3728160534566));
#58969=CARTESIAN_POINT('Ctrl Pts',(-6.56098496085593,-1.65703510627337,
43.3815654920851));
#58970=CARTESIAN_POINT('Ctrl Pts',(-6.51543793649679,-1.83737729739575,
43.3903148952117));
#58971=CARTESIAN_POINT('Ctrl Pts',(-6.46245112157028,-2.01584035544531,
43.3990642983383));
#58972=CARTESIAN_POINT('Ctrl Pts',(-6.40220448361857,-2.19181813797001,
43.407813701465));
#58973=CARTESIAN_POINT('Ctrl Pts',(-6.34195808512125,-2.36779522105895,
43.4165630698165));
#58974=CARTESIAN_POINT('Ctrl Pts',(-6.27445201416518,-2.54128677725338,
43.425312438168));
#58975=CARTESIAN_POINT('Ctrl Pts',(-6.19991555052901,-2.71170355428254,
43.4340618065196));
#58976=CARTESIAN_POINT('Ctrl Pts',(-6.12537937695296,-2.88211966813145,
43.4428111408228));
#58977=CARTESIAN_POINT('Ctrl Pts',(-6.04381298028522,-3.0494607641953,43.4515604751259));
#58978=CARTESIAN_POINT('Ctrl Pts',(-5.95549339309045,-3.21315848424195,
43.4603098094291));
#58979=CARTESIAN_POINT('Ctrl Pts',(-5.86717414225866,-3.37685558084984,
43.4690591104107));
#58980=CARTESIAN_POINT('Ctrl Pts',(-5.77210188844116,-3.53690907699921,
43.4778084113923));
#58981=CARTESIAN_POINT('Ctrl Pts',(-5.67059953311412,-3.6927753702393,43.4865577123738));
#58982=CARTESIAN_POINT('Ctrl Pts',(-5.56909755592737,-3.84864108280984,
43.4953069807604));
#58983=CARTESIAN_POINT('Ctrl Pts',(-5.46116568154984,-4.00031938354804,
43.5040562491471));
#58984=CARTESIAN_POINT('Ctrl Pts',(-5.34717048488383,-4.14729511918157,
43.5128055175337));
#58985=CARTESIAN_POINT('Ctrl Pts',(-5.23317570343297,-4.29427031947189,
43.5215547540521));
#58986=CARTESIAN_POINT('Ctrl Pts',(-5.11311781951525,-4.43654276249582,
43.5303039905704));
#58987=CARTESIAN_POINT('Ctrl Pts',(-4.98740458929206,-4.57362924412424,
43.5390532270888));
#58988=CARTESIAN_POINT('Ctrl Pts',(-4.86169180652698,-4.71071523781311,
43.5478024324655));
#58989=CARTESIAN_POINT('Ctrl Pts',(-4.73032391141527,-4.84261509584534,
43.5565516378422));
#58990=CARTESIAN_POINT('Ctrl Pts',(-4.59374706947278,-4.96888084599644,
43.5653008432189));
#58991=CARTESIAN_POINT('Ctrl Pts',(-4.45717070231475,-5.09514615720771,
43.5740500181806));
#58992=CARTESIAN_POINT('Ctrl Pts',(-4.31538563497346,-5.21577720520596,
43.5827991931423));
#58993=CARTESIAN_POINT('Ctrl Pts',(-4.16887340952043,-5.33036429293473,
43.591548368104));
#58994=CARTESIAN_POINT('Ctrl Pts',(-4.02236168122516,-5.44495099183683,
43.6002975133773));
#58995=CARTESIAN_POINT('Ctrl Pts',(-3.87112305263206,-5.55349359497911,
43.6090466586506));
#58996=CARTESIAN_POINT('Ctrl Pts',(-3.71567116929015,-5.65562346357199,
43.6177958039238));
#58997=CARTESIAN_POINT('Ctrl Pts',(-3.56021980053348,-5.75775299408904,
43.6265449202352));
#58998=CARTESIAN_POINT('Ctrl Pts',(-3.40055544442138,-5.85346967519847,
43.6352940365465));
#58999=CARTESIAN_POINT('Ctrl Pts',(-3.23722035886915,-5.94244843041343,
43.6440431528579));
#59000=CARTESIAN_POINT('Ctrl Pts',(-3.07388580043589,-6.03142689847399,
43.6527922409339));
#59001=CARTESIAN_POINT('Ctrl Pts',(-2.90688078789351,-6.1136673470784,43.6615413290099));
#59002=CARTESIAN_POINT('Ctrl Pts',(-2.7367725061055,-6.18889047001359,43.6702904170859));
#59003=CARTESIAN_POINT('Ctrl Pts',(-2.56666475917112,-6.26411335643261,
43.6790394776531));
#59004=CARTESIAN_POINT('Ctrl Pts',(-2.39345402457291,-6.33231884545181,
43.6877885382202));
#59005=CARTESIAN_POINT('Ctrl Pts',(-2.21772855944284,-6.39327529804807,
43.6965375987874));
#59006=CARTESIAN_POINT('Ctrl Pts',(-2.04200363223816,-6.45423156404631,
43.7052866325722));
#59007=CARTESIAN_POINT('Ctrl Pts',(-1.86376426061265,-6.50793874412387,
43.714035666357));
#59008=CARTESIAN_POINT('Ctrl Pts',(-1.68361577621924,-6.55421443943252,
43.7227847001418));
#59009=CARTESIAN_POINT('Ctrl Pts',(-1.5034678283347,-6.60048999692529,43.7315337078707));
#59010=CARTESIAN_POINT('Ctrl Pts',(-1.32141105657661,-6.63933404265107,
43.7402827155996));
#59011=CARTESIAN_POINT('Ctrl Pts',(-1.13806375346827,-6.67061465631479,
43.7490317233284));
#59012=CARTESIAN_POINT('Ctrl Pts',(-0.954716981172886,-6.7018951794173,
43.7577807057279));
#59013=CARTESIAN_POINT('Ctrl Pts',(-0.770079967445112,-6.72561226608972,
43.7665296881273));
#59014=CARTESIAN_POINT('Ctrl Pts',(-0.584779764075847,-6.74168536995961,
43.7752786705267));
#59015=CARTESIAN_POINT('Ctrl Pts',(-0.391489587595688,-6.75845153117857,
43.7844049009424));
#59016=CARTESIAN_POINT('Ctrl Pts',(-0.197478091807917,-6.76689985146386,
43.793531131358));
#59017=CARTESIAN_POINT('Ctrl Pts',(-0.00346214753366012,-6.76699911434415,
43.8026573617736));
#59018=CARTESIAN_POINT('Ctrl Pts',(0.184490798482111,-6.76709527525942,
43.8114983974887));
#59019=CARTESIAN_POINT('Ctrl Pts',(0.372447602152351,-6.75935633790777,
43.8203394332039));
#59020=CARTESIAN_POINT('Ctrl Pts',(0.559756448191892,-6.74380914014532,
43.829180468919));
#59021=CARTESIAN_POINT('Ctrl Pts',(0.745136131041022,-6.7284220687318,43.8379304475323));
#59022=CARTESIAN_POINT('Ctrl Pts',(0.929880851942699,-6.70538686355756,
43.8466804261456));
#59023=CARTESIAN_POINT('Ctrl Pts',(1.11336305057228,-6.67478177303351,43.8554304047589));
#59024=CARTESIAN_POINT('Ctrl Pts',(1.29684337089884,-6.64417699581307,43.8641802937989));
#59025=CARTESIAN_POINT('Ctrl Pts',(1.47906091204948,-6.60600253548114,43.8729301828389));
#59026=CARTESIAN_POINT('Ctrl Pts',(1.65939671094976,-6.56038806441274,43.8816800718788));
#59027=CARTESIAN_POINT('Ctrl Pts',(1.8397307236893,-6.51477404513915,43.8904298742543));
#59028=CARTESIAN_POINT('Ctrl Pts',(2.0181827535682,-6.46172023288729,43.8991796766298));
#59029=CARTESIAN_POINT('Ctrl Pts',(2.19414664033124,-6.40140683918177,43.9079294790053));
#59030=CARTESIAN_POINT('Ctrl Pts',(2.37010884271063,-6.34109402281571,43.9166791976249));
#59031=CARTESIAN_POINT('Ctrl Pts',(2.54358267847615,-6.27352185699869,43.9254289162444));
#59032=CARTESIAN_POINT('Ctrl Pts',(2.71397890841557,-6.19891986435342,43.934178634864));
#59033=CARTESIAN_POINT('Ctrl Pts',(2.88437356388768,-6.12431856103325,43.9429282726358));
#59034=CARTESIAN_POINT('Ctrl Pts',(3.0516904078701,-6.04268767582639,43.9516779104076));
#59035=CARTESIAN_POINT('Ctrl Pts',(3.21536112511903,-5.95430447954027,43.9604275481794));
#59036=CARTESIAN_POINT('Ctrl Pts',(3.37903038442686,-5.86592207055133,43.9691771080115));
#59037=CARTESIAN_POINT('Ctrl Pts',(3.53905332979811,-5.77078760703476,43.9779266678436));
#59038=CARTESIAN_POINT('Ctrl Pts',(3.69488643041726,-5.66922422085407,43.9866762276756));
#59039=CARTESIAN_POINT('Ctrl Pts',(3.85071819468582,-5.56766170563269,43.9954257124756));
#59040=CARTESIAN_POINT('Ctrl Pts',(4.00235994599071,-5.45967053456364,44.0041751972756));
#59041=CARTESIAN_POINT('Ctrl Pts',(4.14929662974154,-5.34561750206798,44.0129246820756));
#59042=CARTESIAN_POINT('Ctrl Pts',(4.29623210224898,-5.23156540974586,44.021674094751));
#59043=CARTESIAN_POINT('Ctrl Pts',(4.43846235841972,-5.11145173172312,44.0304235074263));
#59044=CARTESIAN_POINT('Ctrl Pts',(4.57550431797285,-4.98568443006693,44.0391729201017));
#59045=CARTESIAN_POINT('Ctrl Pts',(4.71254519337365,-4.85991812336815,44.0479222635596));
#59046=CARTESIAN_POINT('Ctrl Pts',(4.84439764314869,-4.72849847631219,44.0566716070175));
#59047=CARTESIAN_POINT('Ctrl Pts',(4.97061384196585,-4.59187184425454,44.0654209504754));
#59048=CARTESIAN_POINT('Ctrl Pts',(5.09682908420118,-4.45524624767849,44.0741702276228));
#59049=CARTESIAN_POINT('Ctrl Pts',(5.21740796650095,-4.31341395556985,44.0829195047701));
#59050=CARTESIAN_POINT('Ctrl Pts',(5.33194095942187,-4.16685668162939,44.0916687819175));
#59051=CARTESIAN_POINT('Ctrl Pts',(5.44647312235076,-4.02030046975292,44.100417995661));
#59052=CARTESIAN_POINT('Ctrl Pts',(5.55495930712237,-3.8690195703562,44.1091672094046));
#59053=CARTESIAN_POINT('Ctrl Pts',(5.65703106079751,-3.71352778058442,44.1179164231481));
#59054=CARTESIAN_POINT('Ctrl Pts',(5.75910210868684,-3.55803706597686,44.1266655763943));
#59055=CARTESIAN_POINT('Ctrl Pts',(5.85475865698491,-3.39833575880998,44.1354147296405));
#59056=CARTESIAN_POINT('Ctrl Pts',(5.94367583069,-3.23496624706836,44.1441638828867));
#59057=CARTESIAN_POINT('Ctrl Pts',(6.03259241910016,-3.07159781070219,44.1529129785418));
#59058=CARTESIAN_POINT('Ctrl Pts',(6.11476958470909,-2.90456146975957,44.1616620741969));
#59059=CARTESIAN_POINT('Ctrl Pts',(6.1899282357433,-2.73442451648384,44.170411169852));
#59060=CARTESIAN_POINT('Ctrl Pts',(6.26508641700885,-2.56428862662538,44.1791602108222));
#59061=CARTESIAN_POINT('Ctrl Pts',(6.33322605570253,-2.39105242531395,44.1879092517923));
#59062=CARTESIAN_POINT('Ctrl Pts',(6.39411573747728,-2.21530425353841,44.1966582927624));
#59063=CARTESIAN_POINT('Ctrl Pts',(6.45500505889096,-2.03955712188657,44.2054072819534));
#59064=CARTESIAN_POINT('Ctrl Pts',(6.50864441544907,-1.86129832025651,44.2141562711444));
#59065=CARTESIAN_POINT('Ctrl Pts',(6.55485164049891,-1.6811332401237,44.2229052603354));
#59066=CARTESIAN_POINT('Ctrl Pts',(6.60199852639099,-1.49730435912947,44.2318321672123));
#59067=CARTESIAN_POINT('Ctrl Pts',(6.64140767441003,-1.31149113173689,44.2407590740892));
#59068=CARTESIAN_POINT('Ctrl Pts',(6.67293975269598,-1.12435050446457,44.2496859809661));
#59069=CARTESIAN_POINT('Ctrl Pts',(6.70384664831503,-0.940920291564023,
44.2584358951501));
#59070=CARTESIAN_POINT('Ctrl Pts',(6.72718585889662,-0.756215114278239,
44.2671858093341));
#59071=CARTESIAN_POINT('Ctrl Pts',(6.74287810451862,-0.570862389375461,
44.2759357235181));
#59072=CARTESIAN_POINT('Ctrl Pts',(6.75857004154122,-0.385513309568418,
44.2846854656287));
#59073=CARTESIAN_POINT('Ctrl Pts',(6.76661529035555,-0.199516993259524,
44.2934352077393));
#59074=CARTESIAN_POINT('Ctrl Pts',(6.76698652348896,-0.0135052182053635,
44.3021849498498));
#59075=CARTESIAN_POINT('Ctrl Pts',(6.76735774981525,0.1725031460376,44.3109345315205));
#59076=CARTESIAN_POINT('Ctrl Pts',(6.76005524147486,0.358526681832194,44.3196841131911));
#59077=CARTESIAN_POINT('Ctrl Pts',(6.74510380214892,0.543933542113605,44.3284336948618));
#59078=CARTESIAN_POINT('Ctrl Pts',(6.73015261710993,0.72933724908339,44.3371831277237));
#59079=CARTESIAN_POINT('Ctrl Pts',(6.70755278444624,0.914124015853262,44.3459325605856));
#59080=CARTESIAN_POINT('Ctrl Pts',(6.67738106408313,1.09766621749239,44.3546819934475));
#59081=CARTESIAN_POINT('Ctrl Pts',(6.64720981677282,1.28120554143175,44.3634312891299));
#59082=CARTESIAN_POINT('Ctrl Pts',(6.60946696581555,1.46350005650473,44.3721805848122));
#59083=CARTESIAN_POINT('Ctrl Pts',(6.56428070011031,1.64393062206387,44.3809298804946));
#59084=CARTESIAN_POINT('Ctrl Pts',(6.51909508282779,1.82435859844514,44.3896790506246));
#59085=CARTESIAN_POINT('Ctrl Pts',(6.46646633415702,2.00292240086435,44.3984282207546));
#59086=CARTESIAN_POINT('Ctrl Pts',(6.40657319597233,2.17901557696335,44.4071773908846));
#59087=CARTESIAN_POINT('Ctrl Pts',(6.34668083768341,2.35510646007311,44.4159264470876));
#59088=CARTESIAN_POINT('Ctrl Pts',(6.27952437143936,2.52872650996403,44.4246755032907));
#59089=CARTESIAN_POINT('Ctrl Pts',(6.20533187335193,2.69928607997793,44.4334245594938));
#59090=CARTESIAN_POINT('Ctrl Pts',(6.12831449784312,2.87633970115271,44.4425067357826));
#59091=CARTESIAN_POINT('Ctrl Pts',(6.04371489463214,3.05009490562228,44.4515889120715));
#59092=CARTESIAN_POINT('Ctrl Pts',(5.95184265120553,3.21991584599516,44.4606710883603));
#59093=CARTESIAN_POINT('Ctrl Pts',(5.86333281335551,3.383521559052,44.4694208687147));
#59094=CARTESIAN_POINT('Ctrl Pts',(5.76807337235739,3.54347560903737,44.4781706490692));
#59095=CARTESIAN_POINT('Ctrl Pts',(5.66638790086404,3.69923467178573,44.4869204294236));
#59096=CARTESIAN_POINT('Ctrl Pts',(5.56470608502793,3.85498813489691,44.4956698952178));
#59097=CARTESIAN_POINT('Ctrl Pts',(5.45659885767004,4.0065466725619,44.5044193610121));
#59098=CARTESIAN_POINT('Ctrl Pts',(5.34243340580562,4.15339551506141,44.5131688268064));
#59099=CARTESIAN_POINT('Ctrl Pts',(5.22827145140643,4.30023985883811,44.5219180245603));
#59100=CARTESIAN_POINT('Ctrl Pts',(5.10805181978133,4.44237456992993,44.5306672223142));
#59101=CARTESIAN_POINT('Ctrl Pts',(4.98218281282589,4.57931691626407,44.539416420068));
#59102=CARTESIAN_POINT('Ctrl Pts',(4.85631699296262,4.71625579512128,44.548165396286));
#59103=CARTESIAN_POINT('Ctrl Pts',(4.72480227791865,4.84800236135743,44.556914372504));
#59104=CARTESIAN_POINT('Ctrl Pts',(4.58808530848134,4.97410918678889,44.565663348722));
#59105=CARTESIAN_POINT('Ctrl Pts',(4.45135945056995,5.10022421088987,44.5744128937432));
#59106=CARTESIAN_POINT('Ctrl Pts',(4.30943087208069,5.22069856611962,44.5831624387644));
#59107=CARTESIAN_POINT('Ctrl Pts',(4.16278164322501,5.33512305301658,44.5919119837856));
#59108=CARTESIAN_POINT('Ctrl Pts',(4.0161410353442,5.44954081331405,44.6006610144529));
#59109=CARTESIAN_POINT('Ctrl Pts',(3.86478055833438,5.5579092406832,44.6094100451201));
#59110=CARTESIAN_POINT('Ctrl Pts',(3.70921425811972,5.65986029751278,44.6181590757874));
#59111=CARTESIAN_POINT('Ctrl Pts',(3.55364584530143,5.76181273884639,44.6269082252673));
#59112=CARTESIAN_POINT('Ctrl Pts',(3.3938717346437,5.85734747818048,44.6356573747471));
#59113=CARTESIAN_POINT('Ctrl Pts',(3.23043456092433,5.94614005448792,44.644406524227));
#59114=CARTESIAN_POINT('Ctrl Pts',(3.18690768806409,5.96978744811273,44.64673661296));
#59115=CARTESIAN_POINT('Ctrl Pts',(3.14312114982886,5.99295688499298,44.649066701693));
#59116=CARTESIAN_POINT('Ctrl Pts',(3.09908550384713,6.01564277861016,44.6513967904261));
#59117=CARTESIAN_POINT('Origin',(0.,0.,-63.6971797838103));
#59118=CARTESIAN_POINT('',(3.09908550384709,6.01564277861018,47.0459139429101));
#59119=CARTESIAN_POINT('',(3.09908550384732,6.01564277861007,46.6512066495886));
#59120=CARTESIAN_POINT('',(3.09908550384721,6.01564277861012,-63.6971797838103));
#59121=CARTESIAN_POINT('',(-6.76699846313023,-0.00456070095142003,45.6971797837712));
#59122=CARTESIAN_POINT('Ctrl Pts',(-6.76699846312968,-0.00456070176632315,
45.6971797838098));
#59123=CARTESIAN_POINT('Ctrl Pts',(-6.76693165203006,-0.103692509023912,
45.7018724945944));
#59124=CARTESIAN_POINT('Ctrl Pts',(-6.76468666223142,-0.202774974724137,
45.7065652053789));
#59125=CARTESIAN_POINT('Ctrl Pts',(-6.76026920478145,-0.301743730479347,
45.7112579161634));
#59126=CARTESIAN_POINT('Ctrl Pts',(-6.7525215102958,-0.475323146217892,
45.7194883722299));
#59127=CARTESIAN_POINT('Ctrl Pts',(-6.73807283924028,-0.648858023399886,
45.7277188282965));
#59128=CARTESIAN_POINT('Ctrl Pts',(-6.71691515652579,-0.821790593785403,
45.735949284363));
#59129=CARTESIAN_POINT('Ctrl Pts',(-6.69578258922741,-0.994517883019688,
45.7441699703932));
#59130=CARTESIAN_POINT('Ctrl Pts',(-6.66795691146689,-1.16664393675678,
45.7523906564234));
#59131=CARTESIAN_POINT('Ctrl Pts',(-6.63348206267254,-1.33761157448703,
45.7606113424536));
#59132=CARTESIAN_POINT('Ctrl Pts',(-6.59904122083407,-1.50841056495365,
45.768823919369));
#59133=CARTESIAN_POINT('Ctrl Pts',(-6.55796434037573,-1.67805306604469,
45.7770364962844));
#59134=CARTESIAN_POINT('Ctrl Pts',(-6.51034707987385,-1.84598751338629,
45.7852490731998));
#59135=CARTESIAN_POINT('Ctrl Pts',(-6.4627672403075,-2.01378998622826,45.7934551961044));
#59136=CARTESIAN_POINT('Ctrl Pts',(-6.40865735556372,-2.17988673552435,
45.8016613190091));
#59137=CARTESIAN_POINT('Ctrl Pts',(-6.34816405334433,-2.34373679235253,
45.8098674419137));
#59138=CARTESIAN_POINT('Ctrl Pts',(-6.28770616159362,-2.5074909376154,45.8180687612674));
#59139=CARTESIAN_POINT('Ctrl Pts',(-6.22087241996648,-2.66900067486691,
45.8262700806211));
#59140=CARTESIAN_POINT('Ctrl Pts',(-6.14785918808317,-2.82774051205223,
45.8344713999748));
#59141=CARTESIAN_POINT('Ctrl Pts',(-6.07486690196608,-2.98643481053948,
45.8426703665643));
#59142=CARTESIAN_POINT('Ctrl Pts',(-5.99569880272875,-3.14236046478394,
45.8508693331539));
#59143=CARTESIAN_POINT('Ctrl Pts',(-5.91059934396207,-3.29501204780121,
45.8590682997434));
#59144=CARTESIAN_POINT('Ctrl Pts',(-5.82551112296334,-3.44764347248739,
45.8672661836223));
#59145=CARTESIAN_POINT('Ctrl Pts',(-5.73449327625604,-3.59700137351191,
45.8754640675012));
#59146=CARTESIAN_POINT('Ctrl Pts',(-5.63783617155951,-3.74260501558143,
45.8836619513802));
#59147=CARTESIAN_POINT('Ctrl Pts',(-5.54117427282915,-3.88821587935274,
45.8918602418607));
#59148=CARTESIAN_POINT('Ctrl Pts',(-5.43887275720035,-4.03007181438313,
45.9000585323412));
#59149=CARTESIAN_POINT('Ctrl Pts',(-5.33126529469141,-4.16772112282227,
45.9082568228217));
#59150=CARTESIAN_POINT('Ctrl Pts',(-5.22363294787663,-4.3054022627665,45.916457009163));
#59151=CARTESIAN_POINT('Ctrl Pts',(-5.11069243117124,-4.43887455614888,
45.9246571955044));
#59152=CARTESIAN_POINT('Ctrl Pts',(-4.99281768431763,-4.5677194059142,45.9328573818457));
#59153=CARTESIAN_POINT('Ctrl Pts',(-4.87483149613951,-4.6966860683756,45.9410653208198));
#59154=CARTESIAN_POINT('Ctrl Pts',(-4.75190200018331,-4.82101628175486,
45.9492732597938));
#59155=CARTESIAN_POINT('Ctrl Pts',(-4.6244406487371,-4.94032769017481,45.9574811987679));
#59156=CARTESIAN_POINT('Ctrl Pts',(-4.4969174619275,-5.05969698017386,45.9656931196619));
#59157=CARTESIAN_POINT('Ctrl Pts',(-4.36485830718876,-5.17404237624267,
45.9739050405559));
#59158=CARTESIAN_POINT('Ctrl Pts',(-4.22870762648803,-5.28302193916342,
45.9821169614498));
#59159=CARTESIAN_POINT('Ctrl Pts',(-4.09237023669766,-5.3921509502902,45.9903401436924));
#59160=CARTESIAN_POINT('Ctrl Pts',(-3.95193039624666,-5.49589920959848,
45.9985633259349));
#59161=CARTESIAN_POINT('Ctrl Pts',(-3.80786241885848,-5.59396753646687,
46.0067865081775));
#59162=CARTESIAN_POINT('Ctrl Pts',(-3.67939014133803,-5.68141973461536,
46.0141195114605));
#59163=CARTESIAN_POINT('Ctrl Pts',(-3.54803325774793,-5.76435570532466,
46.0214525147435));
#59164=CARTESIAN_POINT('Ctrl Pts',(-3.41414382398665,-5.84259453916955,
46.0287855180265));
#59165=CARTESIAN_POINT('Ctrl Pts',(-3.25100096796157,-5.93792772900352,
46.0377207048088));
#59166=CARTESIAN_POINT('Ctrl Pts',(-3.08375932500652,-6.02648457399728,
46.0466558915912));
#59167=CARTESIAN_POINT('Ctrl Pts',(-2.91298097454007,-6.10793179742273,
46.0555910783735));
#59168=CARTESIAN_POINT('Ctrl Pts',(-2.74245839721137,-6.18925703810364,
46.0645128830101));
#59169=CARTESIAN_POINT('Ctrl Pts',(-2.56840991414264,-6.26349379274193,
46.0734346876467));
#59170=CARTESIAN_POINT('Ctrl Pts',(-2.3914222851357,-6.33035452831485,46.0823564922834));
#59171=CARTESIAN_POINT('Ctrl Pts',(-2.21486637092911,-6.39705217469747,
46.0912565345227));
#59172=CARTESIAN_POINT('Ctrl Pts',(-2.03538586065373,-6.45640961957508,
46.100156576762));
#59173=CARTESIAN_POINT('Ctrl Pts',(-1.85358698663192,-6.50818748062691,
46.1090566190013));
#59174=CARTESIAN_POINT('Ctrl Pts',(-1.67206799464952,-6.5598856289004,46.1179429594947));
#59175=CARTESIAN_POINT('Ctrl Pts',(-1.48823800567415,-6.60402739933049,
46.1268292999881));
#59176=CARTESIAN_POINT('Ctrl Pts',(-1.30272071005423,-6.64042225702521,
46.1357156404815));
#59177=CARTESIAN_POINT('Ctrl Pts',(-1.11767774977619,-6.67672405942173,
46.1445792601535));
#59178=CARTESIAN_POINT('Ctrl Pts',(-0.930956344206983,-6.70531842414489,
46.1534428798254));
#59179=CARTESIAN_POINT('Ctrl Pts',(-0.743191996133971,-6.72606531761939,
46.1623064994974));
#59180=CARTESIAN_POINT('Ctrl Pts',(-0.564946474366039,-6.74576043487875,
46.1707207726509));
#59181=CARTESIAN_POINT('Ctrl Pts',(-0.385761376642811,-6.75838387267933,
46.1791350458044));
#59182=CARTESIAN_POINT('Ctrl Pts',(-0.206191209780811,-6.76385793648929,
46.1875493189579));
#59183=CARTESIAN_POINT('Ctrl Pts',(-0.0309751675667889,-6.76919926802764,
46.1957595671624));
#59184=CARTESIAN_POINT('Ctrl Pts',(0.144439133819563,-6.76772758024457,
46.203969815367));
#59185=CARTESIAN_POINT('Ctrl Pts',(0.31948715555248,-6.7594538949117,46.2121800635715));
#59186=CARTESIAN_POINT('Ctrl Pts',(0.494576789690166,-6.75117824275887,
46.2203922635157));
#59187=CARTESIAN_POINT('Ctrl Pts',(0.669299615144041,-6.73609738839269,
46.22860446346));
#59188=CARTESIAN_POINT('Ctrl Pts',(0.843094771168033,-6.71427436189713,
46.2368166634042));
#59189=CARTESIAN_POINT('Ctrl Pts',(1.01696218981099,-6.69244226156381,46.2450322779147));
#59190=CARTESIAN_POINT('Ctrl Pts',(1.18990081770612,-6.66386244854279,46.2532478924251));
#59191=CARTESIAN_POINT('Ctrl Pts',(1.36135846933956,-6.6286493434151,46.2614635069356));
#59192=CARTESIAN_POINT('Ctrl Pts',(1.53300866039976,-6.59339669551396,46.2696883472211));
#59193=CARTESIAN_POINT('Ctrl Pts',(1.70317420470409,-6.5514959492847,46.2779131875065));
#59194=CARTESIAN_POINT('Ctrl Pts',(1.87131565199657,-6.50311208042678,46.2861380277919));
#59195=CARTESIAN_POINT('Ctrl Pts',(2.03956479973073,-6.45469722001899,46.2943681363734));
#59196=CARTESIAN_POINT('Ctrl Pts',(2.20578692882527,-6.39979107020287,46.302598244955));
#59197=CARTESIAN_POINT('Ctrl Pts',(2.36946119459583,-6.33860731133461,46.3108283535366));
#59198=CARTESIAN_POINT('Ctrl Pts',(2.53335986029653,-6.277339668594,46.3190697457233));
#59199=CARTESIAN_POINT('Ctrl Pts',(2.69470335810053,-6.20977736290887,46.32731113791));
#59200=CARTESIAN_POINT('Ctrl Pts',(2.85299321245167,-6.13618111936933,46.3355525300967));
#59201=CARTESIAN_POINT('Ctrl Pts',(2.92188497865142,-6.10415016436032,46.339139393361));
#59202=CARTESIAN_POINT('Ctrl Pts',(2.99019866156302,-6.07097682855361,46.3427262566253));
#59203=CARTESIAN_POINT('Ctrl Pts',(3.05789483861246,-6.03668519603162,46.3463131198896));
#59204=CARTESIAN_POINT('Ctrl Pts',(3.21734635921982,-5.9559147125559,46.3547616147181));
#59205=CARTESIAN_POINT('Ctrl Pts',(3.37373376537696,-5.86875288562713,46.3632101095465));
#59206=CARTESIAN_POINT('Ctrl Pts',(3.52652924162476,-5.77545500441008,46.3716586043749));
#59207=CARTESIAN_POINT('Ctrl Pts',(3.67918514808085,-5.68224234538789,46.3800993819941));
#59208=CARTESIAN_POINT('Ctrl Pts',(3.82825538147023,-5.58290497733933,46.3885401596133));
#59209=CARTESIAN_POINT('Ctrl Pts',(3.97323632479801,-5.47774425355051,46.3969809372325));
#59210=CARTESIAN_POINT('Ctrl Pts',(4.11810713140899,-5.372663416515,46.4054153027018));
#59211=CARTESIAN_POINT('Ctrl Pts',(4.2588945717964,-5.26176823770797,46.413849668171));
#59212=CARTESIAN_POINT('Ctrl Pts',(4.39512332186689,-5.14540377284249,46.4222840336404));
#59213=CARTESIAN_POINT('Ctrl Pts',(4.53126950427668,-5.02910983597972,46.430713287077));
#59214=CARTESIAN_POINT('Ctrl Pts',(4.66286225216365,-4.90735343816392,46.4391425405136));
#59215=CARTESIAN_POINT('Ctrl Pts',(4.78945839401117,-4.78052060889146,46.4475717939502));
#59216=CARTESIAN_POINT('Ctrl Pts',(4.9159972259603,-4.65374519666545,46.4559972314755));
#59217=CARTESIAN_POINT('Ctrl Pts',(5.0375437270808,-4.52189817102035,46.4644226690007));
#59218=CARTESIAN_POINT('Ctrl Pts',(5.15369047056232,-4.38540346303908,46.4728481065259));
#59219=CARTESIAN_POINT('Ctrl Pts',(5.26981169972771,-4.24893873927454,46.4812716932091));
#59220=CARTESIAN_POINT('Ctrl Pts',(5.38053531837965,-4.10782862079312,46.4896952798923));
#59221=CARTESIAN_POINT('Ctrl Pts',(5.48549285196325,-3.96253166183693,46.4981188665755));
#59222=CARTESIAN_POINT('Ctrl Pts',(5.59043864134923,-3.81725096084852,46.5065415107035));
#59223=CARTESIAN_POINT('Ctrl Pts',(5.6896194367138,-3.66778462355201,46.5149641548315));
#59224=CARTESIAN_POINT('Ctrl Pts',(5.78270875119717,-3.5146220990069,46.5233867989595));
#59225=CARTESIAN_POINT('Ctrl Pts',(5.87580063040251,-3.36145535465102,46.5318096751414));
#59226=CARTESIAN_POINT('Ctrl Pts',(5.96280052129554,-3.20459250512422,46.5402325513233));
#59227=CARTESIAN_POINT('Ctrl Pts',(6.04342656492772,-3.04454994282011,46.5486554275053));
#59228=CARTESIAN_POINT('Ctrl Pts',(6.12406607355669,-2.88448065251981,46.5570797103543));
#59229=CARTESIAN_POINT('Ctrl Pts',(6.19832946325092,-2.72123088871047,46.5655039932032));
#59230=CARTESIAN_POINT('Ctrl Pts',(6.26598176415498,-2.55533980739887,46.5739282760522));
#59231=CARTESIAN_POINT('Ctrl Pts',(6.33367975492169,-2.38933668938462,46.5823582483504));
#59232=CARTESIAN_POINT('Ctrl Pts',(6.3947576090331,-2.22068899836572,46.5907882206486));
#59233=CARTESIAN_POINT('Ctrl Pts',(6.44902891123204,-2.04995490245353,46.5992181929467));
#59234=CARTESIAN_POINT('Ctrl Pts',(6.5033196145456,-1.87915977185763,46.6076511788239));
#59235=CARTESIAN_POINT('Ctrl Pts',(6.55079881906786,-1.70627706873265,46.6160841647011));
#59236=CARTESIAN_POINT('Ctrl Pts',(6.5913304168321,-1.5318786949834,46.6245171505783));
#59237=CARTESIAN_POINT('Ctrl Pts',(6.6318993034193,-1.35731987579298,46.6329578947512));
#59238=CARTESIAN_POINT('Ctrl Pts',(6.66550774326317,-1.18124292626535,46.641398638924));
#59239=CARTESIAN_POINT('Ctrl Pts',(6.69207082851838,-1.00422956842213,46.6498393830968));
#59240=CARTESIAN_POINT('Ctrl Pts',(6.70675826779258,-0.906354155266412,
46.6545064959821));
#59241=CARTESIAN_POINT('Ctrl Pts',(6.71929266270581,-0.808192573016185,
46.6591736088674));
#59242=CARTESIAN_POINT('Ctrl Pts',(6.72966648202166,-0.709843673462194,
46.6638407217526));
#59243=CARTESIAN_POINT('Ctrl Pts',(6.74776269580049,-0.538282683526237,
46.6719820889705));
#59244=CARTESIAN_POINT('Ctrl Pts',(6.7593172142716,-0.365810598614877,46.6801234561884));
#59245=CARTESIAN_POINT('Ctrl Pts',(6.76424799388039,-0.192971700736592,
46.6882648234062));
#59246=CARTESIAN_POINT('Ctrl Pts',(6.76917446929359,-0.0202836780708488,
46.6963990838297));
#59247=CARTESIAN_POINT('Ctrl Pts',(6.76748870466451,0.152770156792283,46.7045333442532));
#59248=CARTESIAN_POINT('Ctrl Pts',(6.75916030829398,0.325639258664043,46.7126676046766));
#59249=CARTESIAN_POINT('Ctrl Pts',(6.75083759325464,0.49839043547832,46.7207963162014));
#59250=CARTESIAN_POINT('Ctrl Pts',(6.73588128581851,0.670956766066609,46.7289250277262));
#59251=CARTESIAN_POINT('Ctrl Pts',(6.71431305172587,0.842786594235866,46.7370537392511));
#59252=CARTESIAN_POINT('Ctrl Pts',(6.69275510312545,1.0145344799358,46.7451785743436));
#59253=CARTESIAN_POINT('Ctrl Pts',(6.66459155230309,1.18554620019801,46.7533034094361));
#59254=CARTESIAN_POINT('Ctrl Pts',(6.62989600427889,1.35527413184449,46.7614282445286));
#59255=CARTESIAN_POINT('Ctrl Pts',(6.59521016937061,1.52495454768074,46.7695508050508));
#59256=CARTESIAN_POINT('Ctrl Pts',(6.55399605363946,1.693351532603,46.777673365573));
#59257=CARTESIAN_POINT('Ctrl Pts',(6.50637856122733,1.8599266162947,46.7857959260951));
#59258=CARTESIAN_POINT('Ctrl Pts',(6.45875853806897,2.02651055302006,46.7939189183103));
#59259=CARTESIAN_POINT('Ctrl Pts',(6.40473455520926,2.1912720420392,46.8020419105255));
#59260=CARTESIAN_POINT('Ctrl Pts',(6.34448173438675,2.35368658109632,46.8101649027407));
#59261=CARTESIAN_POINT('Ctrl Pts',(6.31372450553582,2.43659425377132,46.8143114427218));
#59262=CARTESIAN_POINT('Ctrl Pts',(6.28134496883979,2.51889061900879,46.8184579827029));
#59263=CARTESIAN_POINT('Ctrl Pts',(6.24737131521594,2.6005077676902,46.822604522684));
#59264=CARTESIAN_POINT('Ctrl Pts',(6.17376591854954,2.7773348664176,46.8315881817124));
#59265=CARTESIAN_POINT('Ctrl Pts',(6.09271162714002,2.95088512263563,46.8405718407408));
#59266=CARTESIAN_POINT('Ctrl Pts',(6.00452678470492,3.12056839241848,46.8495554997691));
#59267=CARTESIAN_POINT('Ctrl Pts',(5.91619044164476,3.29054317626114,46.8585545926285));
#59268=CARTESIAN_POINT('Ctrl Pts',(5.82069917312599,3.4566374830664,46.867553685488));
#59269=CARTESIAN_POINT('Ctrl Pts',(5.71841621935872,3.61828757040884,46.8765527783473));
#59270=CARTESIAN_POINT('Ctrl Pts',(5.61589344064769,3.78031668203322,46.8855729715647));
#59271=CARTESIAN_POINT('Ctrl Pts',(5.50654724276295,3.93788052181485,46.894593164782));
#59272=CARTESIAN_POINT('Ctrl Pts',(5.39078459887529,4.0904437911465,46.9036133579994));
#59273=CARTESIAN_POINT('Ctrl Pts',(5.27490471632333,4.24316156899073,46.9126426864211));
#59274=CARTESIAN_POINT('Ctrl Pts',(5.15259555508884,4.39086847241206,46.9216720148428));
#59275=CARTESIAN_POINT('Ctrl Pts',(5.02430409185478,4.53306269453351,46.9307013432645));
#59276=CARTESIAN_POINT('Ctrl Pts',(4.89583176351692,4.67545738184644,46.9397434012193));
#59277=CARTESIAN_POINT('Ctrl Pts',(4.76136042990209,4.81232367046866,46.948785459174));
#59278=CARTESIAN_POINT('Ctrl Pts',(4.62137521545124,4.94319533480248,46.9578275171288));
#59279=CARTESIAN_POINT('Ctrl Pts',(4.49989236789182,5.0567692040892,46.9656744526244));
#59280=CARTESIAN_POINT('Ctrl Pts',(4.37425753037591,5.16582891700249,46.97352138812));
#59281=CARTESIAN_POINT('Ctrl Pts',(4.24480826106292,5.27009410037544,46.9813683236157));
#59282=CARTESIAN_POINT('Ctrl Pts',(4.10203802238213,5.38508868624877,46.9900227475423));
#59283=CARTESIAN_POINT('Ctrl Pts',(3.95450121372337,5.49435153419774,46.9986771714689));
#59284=CARTESIAN_POINT('Ctrl Pts',(3.8026753874517,5.59749487696675,47.0073315953956));
#59285=CARTESIAN_POINT('Ctrl Pts',(3.65101725419665,5.70052429696837,47.0159764604316));
#59286=CARTESIAN_POINT('Ctrl Pts',(3.4950798062013,5.7974475277724,47.0246213254677));
#59287=CARTESIAN_POINT('Ctrl Pts',(3.33537168233416,5.88791854059509,47.0332661905038));
#59288=CARTESIAN_POINT('Ctrl Pts',(3.25748541499414,5.9320393362103,47.0374821079726));
#59289=CARTESIAN_POINT('Ctrl Pts',(3.17870283742253,5.97462622669391,47.0416980254413));
#59290=CARTESIAN_POINT('Ctrl Pts',(3.09908550384709,6.01564277861018,47.0459139429101));
#59291=CARTESIAN_POINT('Ctrl Pts',(3.09908550384733,6.01564277861006,45.0456868593144));
#59292=CARTESIAN_POINT('Ctrl Pts',(2.93958034937513,6.0978152297023,45.0541389626605));
#59293=CARTESIAN_POINT('Ctrl Pts',(2.77691659048998,6.17358242935526,45.0625910660065));
#59294=CARTESIAN_POINT('Ctrl Pts',(2.61164101840684,6.24272538167225,45.0710431693525));
#59295=CARTESIAN_POINT('Ctrl Pts',(2.57801047698548,6.25679470173318,45.0727630170475));
#59296=CARTESIAN_POINT('Ctrl Pts',(2.54427184984424,6.27058990954399,45.0744828647424));
#59297=CARTESIAN_POINT('Ctrl Pts',(2.51042982486944,6.28410941139682,45.0762027124373));
#59298=CARTESIAN_POINT('Ctrl Pts',(2.34676818089706,6.34949036601073,45.0845199777707));
#59299=CARTESIAN_POINT('Ctrl Pts',(2.18039267880978,6.40853692688432,45.0928372431041));
#59300=CARTESIAN_POINT('Ctrl Pts',(2.01182858200964,6.461024280763,45.1011545084375));
#59301=CARTESIAN_POINT('Ctrl Pts',(1.84340665605461,6.51346736559745,45.1094647587976));
#59302=CARTESIAN_POINT('Ctrl Pts',(1.67280014357719,6.5593621627641,45.1177750091577));
#59303=CARTESIAN_POINT('Ctrl Pts',(1.50055322763242,6.59853233765221,45.1260852595178));
#59304=CARTESIAN_POINT('Ctrl Pts',(1.32842004367123,6.63767664907761,45.1343900227476));
#59305=CARTESIAN_POINT('Ctrl Pts',(1.15464895255644,6.67010510892785,45.1426947859775));
#59306=CARTESIAN_POINT('Ctrl Pts',(0.979798425707771,6.69569145383661,45.1509995492073));
#59307=CARTESIAN_POINT('Ctrl Pts',(0.805031342462777,6.72126558821983,45.1593003491699));
#59308=CARTESIAN_POINT('Ctrl Pts',(0.629186193557567,6.74000406473415,45.1676011491325));
#59309=CARTESIAN_POINT('Ctrl Pts',(0.452830976215294,6.75183183343453,45.1759019490951));
#59310=CARTESIAN_POINT('Ctrl Pts',(0.276527648575783,6.7636561220031,45.18420030668));
#59311=CARTESIAN_POINT('Ctrl Pts',(0.0997148982905996,6.76857373261156,
45.192498664265));
#59312=CARTESIAN_POINT('Ctrl Pts',(-0.0770346015696344,6.76656151011435,
45.2007970218499));
#59313=CARTESIAN_POINT('Ctrl Pts',(-0.253802085286102,6.76454908287813,
45.2090962237737));
#59314=CARTESIAN_POINT('Ctrl Pts',(-0.430505957846561,6.75560541012814,
45.2173954256975));
#59315=CARTESIAN_POINT('Ctrl Pts',(-0.606573397413491,6.73975947000709,
45.2256946276213));
#59316=CARTESIAN_POINT('Ctrl Pts',(-0.782658686881366,6.72391192340808,
45.2339946709268));
#59317=CARTESIAN_POINT('Ctrl Pts',(-0.958107068082406,6.70116074533084,
45.2422947142323));
#59318=CARTESIAN_POINT('Ctrl Pts',(-1.1323507814872,6.67158682081447,45.2505947575379));
#59319=CARTESIAN_POINT('Ctrl Pts',(-1.30664108473885,6.64200498872665,45.2588970201358));
#59320=CARTESIAN_POINT('Ctrl Pts',(-1.47972573516905,6.60559683243518,45.2671992827337));
#59321=CARTESIAN_POINT('Ctrl Pts',(-1.65104691460278,6.56249442558092,45.2755015453317));
#59322=CARTESIAN_POINT('Ctrl Pts',(-1.82244234554509,6.51937333791474,45.2838074061743));
#59323=CARTESIAN_POINT('Ctrl Pts',(-1.99207244505875,6.4695523021355,45.2921132670169));
#59324=CARTESIAN_POINT('Ctrl Pts',(-2.15939412250235,6.41321339296474,45.3004191278595));
#59325=CARTESIAN_POINT('Ctrl Pts',(-2.32691358597379,6.35680788722844,45.3087348068156));
#59326=CARTESIAN_POINT('Ctrl Pts',(-2.49211884542283,6.29386922571135,45.3170504857718));
#59327=CARTESIAN_POINT('Ctrl Pts',(-2.65448527687942,6.2246282551515,45.3253661647279));
#59328=CARTESIAN_POINT('Ctrl Pts',(-2.8169544038108,6.15534349022921,45.3336871032847));
#59329=CARTESIAN_POINT('Ctrl Pts',(-2.9765808080228,6.07974861552979,45.3420080418416));
#59330=CARTESIAN_POINT('Ctrl Pts',(-3.13286396257183,5.9981207383662,45.3503289803984));
#59331=CARTESIAN_POINT('Ctrl Pts',(-3.28937940229686,5.91637153689312,45.3586622864473));
#59332=CARTESIAN_POINT('Ctrl Pts',(-3.44254136015966,5.82857158587743,45.3669955924963));
#59333=CARTESIAN_POINT('Ctrl Pts',(-3.59187666795456,5.73504237143926,45.3753288985452));
#59334=CARTESIAN_POINT('Ctrl Pts',(-3.70179627127209,5.66619934763298,45.3814627037969));
#59335=CARTESIAN_POINT('Ctrl Pts',(-3.80964325951199,5.59425321995921,45.3875965090487));
#59336=CARTESIAN_POINT('Ctrl Pts',(-3.91524047656804,5.51934606730211,45.3937303143004));
#59337=CARTESIAN_POINT('Ctrl Pts',(-4.0532153760656,5.42147126389677,45.4017448357692));
#59338=CARTESIAN_POINT('Ctrl Pts',(-4.18778596920639,5.31822896559392,45.4097593572381));
#59339=CARTESIAN_POINT('Ctrl Pts',(-4.31849079120842,5.2098873583071,45.4177738787069));
#59340=CARTESIAN_POINT('Ctrl Pts',(-4.44903199527607,5.10168137440218,45.4257783674973));
#59341=CARTESIAN_POINT('Ctrl Pts',(-4.57571676755245,4.98838901765393,45.4337828562878));
#59342=CARTESIAN_POINT('Ctrl Pts',(-4.69811078084983,4.87032279123906,45.4417873450782));
#59343=CARTESIAN_POINT('Ctrl Pts',(-4.82037907632526,4.75237783733117,45.4497836120049));
#59344=CARTESIAN_POINT('Ctrl Pts',(-4.93836511173299,4.62966902965933,45.4577798789316));
#59345=CARTESIAN_POINT('Ctrl Pts',(-5.05166609793072,4.50255023681218,45.4657761458583));
#59346=CARTESIAN_POINT('Ctrl Pts',(-5.16487609682491,4.37553352777365,45.473765991316));
#59347=CARTESIAN_POINT('Ctrl Pts',(-5.27340828304388,4.24411416140957,45.4817558367738));
#59348=CARTESIAN_POINT('Ctrl Pts',(-5.3768954784377,4.10868397591689,45.4897456822315));
#59349=CARTESIAN_POINT('Ctrl Pts',(-5.48032271791807,3.97333225269628,45.4977308987254));
#59350=CARTESIAN_POINT('Ctrl Pts',(-5.57871055502915,3.83397463479472,45.5057161152193));
#59351=CARTESIAN_POINT('Ctrl Pts',(-5.67173112246984,3.69103712720518,45.5137013317132));
#59352=CARTESIAN_POINT('Ctrl Pts',(-5.76473112548316,3.54813121937979,45.5216847828836));
#59353=CARTESIAN_POINT('Ctrl Pts',(-5.85236600804091,3.40164730950946,45.5296682340538));
#59354=CARTESIAN_POINT('Ctrl Pts',(-5.93435038671638,3.25204158763063,45.5376516852241));
#59355=CARTESIAN_POINT('Ctrl Pts',(-6.01632816088129,3.10244791771323,45.5456344932623));
#59356=CARTESIAN_POINT('Ctrl Pts',(-6.09265615419054,2.94973326750943,45.5536173013006));
#59357=CARTESIAN_POINT('Ctrl Pts',(-6.1630944028326,2.79437942695215,45.5616001093388));
#59358=CARTESIAN_POINT('Ctrl Pts',(-6.23354122773228,2.63900667118072,45.5695838893293));
#59359=CARTESIAN_POINT('Ctrl Pts',(-6.2980967247161,2.4809944302798,45.5775676693197));
#59360=CARTESIAN_POINT('Ctrl Pts',(-6.35656873276757,2.32084530841711,45.5855514493102));
#59361=CARTESIAN_POINT('Ctrl Pts',(-6.41505969468335,2.16064427377041,45.5935378172653));
#59362=CARTESIAN_POINT('Ctrl Pts',(-6.46746311446471,1.99830533514858,45.6015241852202));
#59363=CARTESIAN_POINT('Ctrl Pts',(-6.51363649930655,1.83434690146154,45.6095105531753));
#59364=CARTESIAN_POINT('Ctrl Pts',(-6.5598607569089,1.67020782218919,45.6175057203246));
#59365=CARTESIAN_POINT('Ctrl Pts',(-6.59984117190231,1.50444604950245,45.6255008874739));
#59366=CARTESIAN_POINT('Ctrl Pts',(-6.63348610337766,1.33759153566978,45.6334960546232));
#59367=CARTESIAN_POINT('Ctrl Pts',(-6.66715123024904,1.17063686728674,45.6414960208777));
#59368=CARTESIAN_POINT('Ctrl Pts',(-6.69447324239003,1.00258852399637,45.6494959871323));
#59369=CARTESIAN_POINT('Ctrl Pts',(-6.71541239859187,0.833981604616404,
45.6574959533868));
#59370=CARTESIAN_POINT('Ctrl Pts',(-6.73638267762508,0.665124077013908,
45.6655078103593));
#59371=CARTESIAN_POINT('Ctrl Pts',(-6.75095112627625,0.495706690858887,
45.6735196673318));
#59372=CARTESIAN_POINT('Ctrl Pts',(-6.75913011130805,0.326265441640491,
45.6815315243043));
#59373=CARTESIAN_POINT('Ctrl Pts',(-6.76445500583179,0.215951414099029,
45.6867476107933));
#59374=CARTESIAN_POINT('Ctrl Pts',(-6.76707272562536,0.105627227563015,
45.6919636972822));
#59375=CARTESIAN_POINT('Ctrl Pts',(-6.76699846313023,-0.00456070095141469,
45.6971797837712));
#59376=CARTESIAN_POINT('',(-6.7669992409897,-0.00233727624500557,45.3028202161897));
#59377=CARTESIAN_POINT('Ctrl Pts',(3.09908550384713,6.01564277861016,44.6513967904261));
#59378=CARTESIAN_POINT('Ctrl Pts',(2.93373232018324,6.10082796552483,44.6601462383254));
#59379=CARTESIAN_POINT('Ctrl Pts',(2.76486502144423,6.17919158180192,44.6688956862247));
#59380=CARTESIAN_POINT('Ctrl Pts',(2.59305716434351,6.2504674659138,44.677645134124));
#59381=CARTESIAN_POINT('Ctrl Pts',(2.42125069459277,6.32174277447227,44.6863945113714));
#59382=CARTESIAN_POINT('Ctrl Pts',(2.24650397871048,6.38593035557829,44.6951438886188));
#59383=CARTESIAN_POINT('Ctrl Pts',(2.06941053323756,6.44281220003544,44.7038932658662));
#59384=CARTESIAN_POINT('Ctrl Pts',(1.89231845896665,6.49969360406691,44.7126425753688));
#59385=CARTESIAN_POINT('Ctrl Pts',(1.71287996431483,6.54926929700887,44.7213918848714));
#59386=CARTESIAN_POINT('Ctrl Pts',(1.53170449173479,6.59137090065485,44.730141194374));
#59387=CARTESIAN_POINT('Ctrl Pts',(1.35053036178141,6.63347219230089,44.7388904390386));
#59388=CARTESIAN_POINT('Ctrl Pts',(1.16761955878812,6.6680994406246,44.7476396837032));
#59389=CARTESIAN_POINT('Ctrl Pts',(0.98359330931013,6.69513503985397,44.7563889283678));
#59390=CARTESIAN_POINT('Ctrl Pts',(0.799568362459666,6.72217044771218,44.7651381111009));
#59391=CARTESIAN_POINT('Ctrl Pts',(0.614428268438323,6.74161427235979,44.7738872938341));
#59392=CARTESIAN_POINT('Ctrl Pts',(0.42880181633004,6.75340047696803,44.7826364765673));
#59393=CARTESIAN_POINT('Ctrl Pts',(0.243176616522572,6.76518660206243,44.7913856002754));
#59394=CARTESIAN_POINT('Ctrl Pts',(0.0570653511652667,6.76931519233997,
44.8001347239836));
#59395=CARTESIAN_POINT('Ctrl Pts',(-0.128899900800206,6.76577222610795,
44.8088838476917));
#59396=CARTESIAN_POINT('Ctrl Pts',(-0.314863959942114,6.76222928260132,
44.8176329152809));
#59397=CARTESIAN_POINT('Ctrl Pts',(-0.500681721080689,6.75101488651276,
44.8263819828702));
#59398=CARTESIAN_POINT('Ctrl Pts',(-0.685722110173223,6.73216712415992,
44.8351310504595));
#59399=CARTESIAN_POINT('Ctrl Pts',(-0.870761373827468,6.71331947644147,
44.8438800648358));
#59400=CARTESIAN_POINT('Ctrl Pts',(-1.05502298984322,6.68683858439999,44.8526290792122));
#59401=CARTESIAN_POINT('Ctrl Pts',(-1.23788117676032,6.65281438131431,44.8613780935885));
#59402=CARTESIAN_POINT('Ctrl Pts',(-1.43009641451759,6.61704912302384,44.8705748044761));
#59403=CARTESIAN_POINT('Ctrl Pts',(-1.62076048992657,6.57294837083175,44.8797715153636));
#59404=CARTESIAN_POINT('Ctrl Pts',(-1.80915798961087,6.52067760042062,44.8889682262511));
#59405=CARTESIAN_POINT('Ctrl Pts',(-1.98840443002961,6.47094578577424,44.8977182239576));
#59406=CARTESIAN_POINT('Ctrl Pts',(-2.16559895952135,6.41381888474494,44.9064682216641));
#59407=CARTESIAN_POINT('Ctrl Pts',(-2.34013966242259,6.34949095285257,44.9152182193706));
#59408=CARTESIAN_POINT('Ctrl Pts',(-2.51467682553956,6.28516432556709,44.9239680396222));
#59409=CARTESIAN_POINT('Ctrl Pts',(-2.68656000078787,6.21363705879685,44.9327178598738));
#59410=CARTESIAN_POINT('Ctrl Pts',(-2.85520533840837,6.13515211510883,44.9414676801254));
#59411=CARTESIAN_POINT('Ctrl Pts',(-3.02384747998275,6.05666865881147,44.9502173345567));
#59412=CARTESIAN_POINT('Ctrl Pts',(-3.18925164684484,5.97122791039872,44.9589669889879));
#59413=CARTESIAN_POINT('Ctrl Pts',(-3.35085601829104,5.87912008251938,44.9677166434192));
#59414=CARTESIAN_POINT('Ctrl Pts',(-3.51245754191351,5.78701387778214,44.9764661436623));
#59415=CARTESIAN_POINT('Ctrl Pts',(-3.67025915510856,5.68824097061034,44.9852156439054));
#59416=CARTESIAN_POINT('Ctrl Pts',(-3.82372487928742,5.58313684656918,44.9939651441486));
#59417=CARTESIAN_POINT('Ctrl Pts',(-3.97718810300709,5.47803443501838,45.0027145018337));
#59418=CARTESIAN_POINT('Ctrl Pts',(-4.1263153426294,5.36660117496442,45.0114638595188));
#59419=CARTESIAN_POINT('Ctrl Pts',(-4.27060009886142,5.24921554097418,45.0202132172039));
#59420=CARTESIAN_POINT('Ctrl Pts',(-4.41488269594124,5.13183166360367,45.0289624439591));
#59421=CARTESIAN_POINT('Ctrl Pts',(-4.55432273234995,5.00849577139556,45.0377116707143));
#59422=CARTESIAN_POINT('Ctrl Pts',(-4.68844662480109,4.87962675277437,45.0464608974695));
#59423=CARTESIAN_POINT('Ctrl Pts',(-4.82256868835036,4.75075949140003,45.0552100049209));
#59424=CARTESIAN_POINT('Ctrl Pts',(-4.95137454637721,4.61635945312676,45.0639591123724));
#59425=CARTESIAN_POINT('Ctrl Pts',(-5.07442674460918,4.47688309134772,45.0727082198239));
#59426=CARTESIAN_POINT('Ctrl Pts',(-5.19747742838393,4.33740844616527,45.0814572195962));
#59427=CARTESIAN_POINT('Ctrl Pts',(-5.31477440450794,4.19285781736198,45.0902062193686));
#59428=CARTESIAN_POINT('Ctrl Pts',(-5.42591931531033,4.04372211999568,45.098955219141));
#59429=CARTESIAN_POINT('Ctrl Pts',(-5.53707636462871,3.89457013500959,45.1077051744216));
#59430=CARTESIAN_POINT('Ctrl Pts',(-5.64207983273368,3.74083230916574,45.1164551297022));
#59431=CARTESIAN_POINT('Ctrl Pts',(-5.74057303468654,3.58303087251978,45.1252050849828));
#59432=CARTESIAN_POINT('Ctrl Pts',(-5.83906243363682,3.42523552887573,45.1339547024116));
#59433=CARTESIAN_POINT('Ctrl Pts',(-5.93104191768352,3.26337713157127,45.1427043198404));
#59434=CARTESIAN_POINT('Ctrl Pts',(-6.01619906699591,3.09800545291282,45.1514539372692));
#59435=CARTESIAN_POINT('Ctrl Pts',(-6.10135338095319,2.93263928039728,45.1602032633746));
#59436=CARTESIAN_POINT('Ctrl Pts',(-6.17968568352777,2.76376031540362,45.1689525894799));
#59437=CARTESIAN_POINT('Ctrl Pts',(-6.25092992694826,2.59194213831687,45.1777019155853));
#59438=CARTESIAN_POINT('Ctrl Pts',(-6.32217217691047,2.42012876880967,45.1864509968791));
#59439=CARTESIAN_POINT('Ctrl Pts',(-6.38632665483798,2.2453766164782,45.1952000781729));
#59440=CARTESIAN_POINT('Ctrl Pts',(-6.44317547869301,2.06827917621609,45.2039491594667));
#59441=CARTESIAN_POINT('Ctrl Pts',(-6.50002944235889,1.89116572423585,45.2126990317817));
#59442=CARTESIAN_POINT('Ctrl Pts',(-6.54957634250353,1.7117068328937,45.2214489040967));
#59443=CARTESIAN_POINT('Ctrl Pts',(-6.59164787708353,1.53051209225546,45.2301987764116));
#59444=CARTESIAN_POINT('Ctrl Pts',(-6.63371649074977,1.34932993148191,45.2389480412464));
#59445=CARTESIAN_POINT('Ctrl Pts',(-6.668310712571,1.16641244174144,45.2476973060812));
#59446=CARTESIAN_POINT('Ctrl Pts',(-6.69531304840315,0.982380875161198,
45.256446570916));
#59447=CARTESIAN_POINT('Ctrl Pts',(-6.7223167703303,0.798339861797004,45.2651962848717));
#59448=CARTESIAN_POINT('Ctrl Pts',(-6.7417277847788,0.61318494073129,45.2739459988274));
#59449=CARTESIAN_POINT('Ctrl Pts',(-6.75348015835511,0.427545027691661,
45.282695712783));
#59450=CARTESIAN_POINT('Ctrl Pts',(-6.76249038365207,0.28521995354942,45.2894038805852));
#59451=CARTESIAN_POINT('Ctrl Pts',(-6.76699999999988,0.142609995761396,
45.2961120483875));
#59452=CARTESIAN_POINT('Ctrl Pts',(-6.767,5.50082243727984E-12,45.3028202161897));
#59453=CARTESIAN_POINT('Ctrl Pts',(-6.76699857274565,-0.0043950492956634,
45.3028202161897));
#59454=CARTESIAN_POINT('Ctrl Pts',(-6.76686460262846,-0.210667045539541,
45.3125155163845));
#59455=CARTESIAN_POINT('Ctrl Pts',(-6.75729411431099,-0.416736582006849,
45.3222108165793));
#59456=CARTESIAN_POINT('Ctrl Pts',(-6.73837284507612,-0.621788067383695,
45.3319061167741));
#59457=CARTESIAN_POINT('Ctrl Pts',(-6.72034007666234,-0.817210789971848,
45.3411461471835));
#59458=CARTESIAN_POINT('Ctrl Pts',(-6.69381460588411,-1.01170871981791,
45.3503861775929));
#59459=CARTESIAN_POINT('Ctrl Pts',(-6.65892323893038,-1.20458718988415,
45.3596262080024));
#59460=CARTESIAN_POINT('Ctrl Pts',(-6.62398604063929,-1.39771901426128,
45.3688783755961));
#59461=CARTESIAN_POINT('Ctrl Pts',(-6.58066101984478,-1.58922693698234,
45.3781305431897));
#59462=CARTESIAN_POINT('Ctrl Pts',(-6.52912587635335,-1.77842747693941,
45.3873827107835));
#59463=CARTESIAN_POINT('Ctrl Pts',(-6.4775270261816,-1.96786190269752,45.3966463157157));
#59464=CARTESIAN_POINT('Ctrl Pts',(-6.41769781049481,-2.15498305559458,
45.405909920648));
#59465=CARTESIAN_POINT('Ctrl Pts',(-6.34986606512067,-2.33912162040134,
45.4151735255802));
#59466=CARTESIAN_POINT('Ctrl Pts',(-6.34012656891899,-2.36556081701386,
45.4165036232293));
#59467=CARTESIAN_POINT('Ctrl Pts',(-6.33022217370865,-2.39193855499759,
45.4178337208783));
#59468=CARTESIAN_POINT('Ctrl Pts',(-6.32015363622328,-2.41825288473594,
45.4191638185273));
#59469=CARTESIAN_POINT('Ctrl Pts',(-6.25464887440804,-2.58945092659074,
45.427817282828));
#59470=CARTESIAN_POINT('Ctrl Pts',(-6.18214232253387,-2.75809489593996,
45.4364707471288));
#59471=CARTESIAN_POINT('Ctrl Pts',(-6.10285146591681,-2.92360958148606,
45.4451242114295));
#59472=CARTESIAN_POINT('Ctrl Pts',(-6.02363365239697,-3.08897179415212,
45.4537697041196));
#59473=CARTESIAN_POINT('Ctrl Pts',(-5.93764413027185,-3.25121019943543,
45.4624151968098));
#59474=CARTESIAN_POINT('Ctrl Pts',(-5.84514838106999,-3.40976969944817,
45.4710606895));
#59475=CARTESIAN_POINT('Ctrl Pts',(-5.74987005603456,-3.57309918983049,
45.4799662669965));
#59476=CARTESIAN_POINT('Ctrl Pts',(-5.64768803982555,-3.73252466433785,
45.4888718444931));
#59477=CARTESIAN_POINT('Ctrl Pts',(-5.5389445730861,-3.88746472862199,45.4977774219897));
#59478=CARTESIAN_POINT('Ctrl Pts',(-5.4335772386222,-4.0375944059699,45.5064065101622));
#59479=CARTESIAN_POINT('Ctrl Pts',(-5.32204994745615,-4.18351273053596,
45.5150355983347));
#59480=CARTESIAN_POINT('Ctrl Pts',(-5.20471931157317,-4.32471801251102,
45.5236646865071));
#59481=CARTESIAN_POINT('Ctrl Pts',(-5.08174949327091,-4.47270994775557,
45.5327085086658));
#59482=CARTESIAN_POINT('Ctrl Pts',(-4.95240490224127,-4.6155243387253,45.5417523308244));
#59483=CARTESIAN_POINT('Ctrl Pts',(-4.81714573443428,-4.75261990624347,
45.5507961529831));
#59484=CARTESIAN_POINT('Ctrl Pts',(-4.68188656662729,-4.88971547376163,
45.5598399751417));
#59485=CARTESIAN_POINT('Ctrl Pts',(-4.54071306800496,-5.02109191921025,
45.5688837973004));
#59486=CARTESIAN_POINT('Ctrl Pts',(-4.39413283355317,-5.14624966758221,
45.577927619459));
#59487=CARTESIAN_POINT('Ctrl Pts',(-4.25756952768939,-5.26285444677407,
45.5863534093088));
#59488=CARTESIAN_POINT('Ctrl Pts',(-4.11637314747104,-5.37401052896704,
45.5947791991586));
#59489=CARTESIAN_POINT('Ctrl Pts',(-3.9710112762364,-5.47935748459648,45.6032049890084));
#59490=CARTESIAN_POINT('Ctrl Pts',(-3.82561567615772,-5.58472888426344,
45.6116327339249));
#59491=CARTESIAN_POINT('Ctrl Pts',(-3.67605292636013,-5.68428827529069,
45.6200604788414));
#59492=CARTESIAN_POINT('Ctrl Pts',(-3.52282042112096,-5.77771799939502,
45.6284882237579));
#59493=CARTESIAN_POINT('Ctrl Pts',(-3.36953161062352,-5.87118205423574,
45.6369190654479));
#59494=CARTESIAN_POINT('Ctrl Pts',(-3.21257063890073,-5.95851177868701,
45.6453499071378));
#59495=CARTESIAN_POINT('Ctrl Pts',(-3.05246070212078,-6.03943479656899,
45.6537807488278));
#59496=CARTESIAN_POINT('Ctrl Pts',(-2.89220364474537,-6.12043217237539,
45.6622193373851));
#59497=CARTESIAN_POINT('Ctrl Pts',(-2.72879213744786,-6.19501093041115,
45.6706579259424));
#59498=CARTESIAN_POINT('Ctrl Pts',(-2.56277163846469,-6.26294583475548,
45.6790965144998));
#59499=CARTESIAN_POINT('Ctrl Pts',(-2.39666408566866,-6.33091636116146,
45.6875395278801));
#59500=CARTESIAN_POINT('Ctrl Pts',(-2.22794512218614,-6.39223596776628,
45.6959825412603));
#59501=CARTESIAN_POINT('Ctrl Pts',(-2.05717721685793,-6.44672869744343,
45.7044255546406));
#59502=CARTESIAN_POINT('Ctrl Pts',(-1.88622990794259,-6.50127867553127,
45.7128774379949));
#59503=CARTESIAN_POINT('Ctrl Pts',(-1.7132296751096,-6.548987356646,45.7213293213492));
#59504=CARTESIAN_POINT('Ctrl Pts',(-1.53875211389063,-6.58972920020217,
45.7297812047035));
#59505=CARTESIAN_POINT('Ctrl Pts',(-1.49120146630198,-6.60083263970188,
45.7320846099324));
#59506=CARTESIAN_POINT('Ctrl Pts',(-1.44354114170434,-6.61141892278309,
45.7343880151614));
#59507=CARTESIAN_POINT('Ctrl Pts',(-1.39578288781783,-6.62148617230867,
45.7366914203903));
#59508=CARTESIAN_POINT('Ctrl Pts',(-1.22333469483533,-6.65783756390512,
45.7450086857237));
#59509=CARTESIAN_POINT('Ctrl Pts',(-1.0492989249379,-6.68748304993526,45.753325951057));
#59510=CARTESIAN_POINT('Ctrl Pts',(-0.874231609361912,-6.71029120777873,
45.7616432163904));
#59511=CARTESIAN_POINT('Ctrl Pts',(-0.699311949595541,-6.7330801286961,
45.7699534667505));
#59512=CARTESIAN_POINT('Ctrl Pts',(-0.523362820761848,-6.74904316629383,
45.7782637171106));
#59513=CARTESIAN_POINT('Ctrl Pts',(-0.346950581447075,-6.75809990263784,
45.7865739674707));
#59514=CARTESIAN_POINT('Ctrl Pts',(-0.170654824414324,-6.76715065895846,
45.7948787307005));
#59515=CARTESIAN_POINT('Ctrl Pts',(0.00610308757387329,-6.76930418286158,
45.8031834939304));
#59516=CARTESIAN_POINT('Ctrl Pts',(0.182751304352238,-6.76453183603696,
45.8114882571603));
#59517=CARTESIAN_POINT('Ctrl Pts',(0.359315219618329,-6.75976176671087,
45.8197890571229));
#59518=CARTESIAN_POINT('Ctrl Pts',(0.535769197016702,-6.7480724230201,45.8280898570855));
#59519=CARTESIAN_POINT('Ctrl Pts',(0.711540782673459,-6.72948725495431,
45.8363906570481));
#59520=CARTESIAN_POINT('Ctrl Pts',(0.887260650351361,-6.71090755527708,
45.844689014633));
#59521=CARTESIAN_POINT('Ctrl Pts',(1.06229818101648,-6.68543611212831,45.852987372218));
#59522=CARTESIAN_POINT('Ctrl Pts',(1.23608521204884,-6.65314830351422,45.8612857298029));
#59523=CARTESIAN_POINT('Ctrl Pts',(1.40988992551327,-6.62085720968962,45.8695849317267));
#59524=CARTESIAN_POINT('Ctrl Pts',(1.58244354178506,-6.58174842075848,45.8778841336504));
#59525=CARTESIAN_POINT('Ctrl Pts',(1.75318669042906,-6.53594870148951,45.8861833355742));
#59526=CARTESIAN_POINT('Ctrl Pts',(1.92394714919171,-6.49014433899719,45.8944833788797));
#59527=CARTESIAN_POINT('Ctrl Pts',(2.09289643820234,-6.43764778375086,45.9027834221853));
#59528=CARTESIAN_POINT('Ctrl Pts',(2.25948907429872,-6.37863607075406,45.9110834654909));
#59529=CARTESIAN_POINT('Ctrl Pts',(2.42612625447195,-6.31960857901492,45.9193857280888));
#59530=CARTESIAN_POINT('Ctrl Pts',(2.590405197851,-6.25406257363528,45.9276879906866));
#59531=CARTESIAN_POINT('Ctrl Pts',(2.75179899218133,-6.18222381563704,45.9359902532846));
#59532=CARTESIAN_POINT('Ctrl Pts',(2.91326273543907,-6.11035392233964,45.9442961141272));
#59533=CARTESIAN_POINT('Ctrl Pts',(3.07183851986749,-6.03218598223624,45.9526019749698));
#59534=CARTESIAN_POINT('Ctrl Pts',(3.22702251580944,-5.94799249179578,45.9609078358124));
#59535=CARTESIAN_POINT('Ctrl Pts',(3.38238995018334,-5.86369947870948,45.9692235147685));
#59536=CARTESIAN_POINT('Ctrl Pts',(3.53435727943124,-5.77336685058202,45.9775391937246));
#59537=CARTESIAN_POINT('Ctrl Pts',(3.68244722952413,-5.67731198735547,45.9858548726807));
#59538=CARTESIAN_POINT('Ctrl Pts',(3.83063084533104,-5.58119637019292,45.9941758112376));
#59539=CARTESIAN_POINT('Ctrl Pts',(3.97493190742218,-5.4793515005047,46.0024967497944));
#59540=CARTESIAN_POINT('Ctrl Pts',(4.11490481376219,-5.37213620207798,46.0108176883513));
#59541=CARTESIAN_POINT('Ctrl Pts',(4.25508576319729,-5.26476154850811,46.0191509944002));
#59542=CARTESIAN_POINT('Ctrl Pts',(4.39092543330336,-5.15200073634286,46.0274843004491));
#59543=CARTESIAN_POINT('Ctrl Pts',(4.52201278480097,-5.03425162006197,46.035817606498));
#59544=CARTESIAN_POINT('Ctrl Pts',(4.61850081492207,-4.94758131855199,46.0419514117498));
#59545=CARTESIAN_POINT('Ctrl Pts',(4.71241486627321,-4.85820923611743,46.0480852170016));
#59546=CARTESIAN_POINT('Ctrl Pts',(4.8036047670012,-4.76630572272104,46.0542190222533));
#59547=CARTESIAN_POINT('Ctrl Pts',(4.92360064917607,-4.64537080474297,46.0622904354954));
#59548=CARTESIAN_POINT('Ctrl Pts',(5.03924729246588,-4.51967888634194,46.0703618487374));
#59549=CARTESIAN_POINT('Ctrl Pts',(5.15013365027661,-4.38957997811733,46.0784332619794));
#59550=CARTESIAN_POINT('Ctrl Pts',(5.26088079944952,-4.25964439829626,46.0864945422307));
#59551=CARTESIAN_POINT('Ctrl Pts',(5.36687931527553,-4.12531311737569,46.0945558224819));
#59552=CARTESIAN_POINT('Ctrl Pts',(5.46775273160348,-3.9869749266885,46.1026171027331));
#59553=CARTESIAN_POINT('Ctrl Pts',(5.5685216317191,-3.8487800699364,46.1106700305908));
#59554=CARTESIAN_POINT('Ctrl Pts',(5.66417578187042,-3.70658686404281,46.1187229584484));
#59555=CARTESIAN_POINT('Ctrl Pts',(5.75437705612355,-3.56081924505567,46.126775886306));
#59556=CARTESIAN_POINT('Ctrl Pts',(5.84450462371335,-3.41517073796477,46.1348222338304));
#59557=CARTESIAN_POINT('Ctrl Pts',(5.92918798858885,-3.26595394666839,46.1428685813548));
#59558=CARTESIAN_POINT('Ctrl Pts',(6.00813073389935,-3.11362394716736,46.1509149288792));
#59559=CARTESIAN_POINT('Ctrl Pts',(6.08702624088287,-2.96138509998561,46.1589564615723));
#59560=CARTESIAN_POINT('Ctrl Pts',(6.16018779544525,-2.80603708340868,46.1669979942655));
#59561=CARTESIAN_POINT('Ctrl Pts',(6.22736363127136,-2.64806178249655,46.1750395269586));
#59562=CARTESIAN_POINT('Ctrl Pts',(6.29583090490721,-2.48704944789376,46.1832356560069));
#59563=CARTESIAN_POINT('Ctrl Pts',(6.3580797627172,-2.32330812057301,46.1914317850551));
#59564=CARTESIAN_POINT('Ctrl Pts',(6.41389379559058,-2.15737233200129,46.1996279141033));
#59565=CARTESIAN_POINT('Ctrl Pts',(6.4686361545347,-1.99462264286348,46.2076666709394));
#59566=CARTESIAN_POINT('Ctrl Pts',(6.51718845418104,-1.82976237334537,46.2157054277755));
#59567=CARTESIAN_POINT('Ctrl Pts',(6.55939608412578,-1.66331356381034,46.2237441846116));
#59568=CARTESIAN_POINT('Ctrl Pts',(6.60160779932296,-1.49684864378987,46.2317837195144));
#59569=CARTESIAN_POINT('Ctrl Pts',(6.63747353013455,-1.32879523960759,46.2398232544172));
#59570=CARTESIAN_POINT('Ctrl Pts',(6.66688933868066,-1.1596876932115,46.24786278932));
#59571=CARTESIAN_POINT('Ctrl Pts',(6.6963138187065,-0.990530295639011,46.2559046941956));
#59572=CARTESIAN_POINT('Ctrl Pts',(6.71928452786946,-0.820318505058142,
46.2639465990711));
#59573=CARTESIAN_POINT('Ctrl Pts',(6.73574917293496,-0.649593780224284,
46.2719885039466));
#59574=CARTESIAN_POINT('Ctrl Pts',(6.75276920805537,-0.473110120780893,
46.2803016806274));
#59575=CARTESIAN_POINT('Ctrl Pts',(6.76283653056089,-0.29607875144971,46.2886148573082));
#59576=CARTESIAN_POINT('Ctrl Pts',(6.7659518508028,-0.119098919466973,46.296928033989));
#59577=CARTESIAN_POINT('Ctrl Pts',(6.76897074579287,0.0524030407257231,
46.3049839015996));
#59578=CARTESIAN_POINT('Ctrl Pts',(6.76546166354127,0.223856239532683,46.3130397692101));
#59579=CARTESIAN_POINT('Ctrl Pts',(6.75547814928279,0.39472012181132,46.3210956368206));
#59580=CARTESIAN_POINT('Ctrl Pts',(6.74501631619583,0.573770240908646,46.3295374680366));
#59581=CARTESIAN_POINT('Ctrl Pts',(6.72744444476342,0.752172701315157,46.3379792992525));
#59582=CARTESIAN_POINT('Ctrl Pts',(6.70288428426154,0.929317637731945,46.3464211304685));
#59583=CARTESIAN_POINT('Ctrl Pts',(6.67832412375965,1.10646257414873,46.3548629616844));
#59584=CARTESIAN_POINT('Ctrl Pts',(6.64677583983355,1.28234954782513,46.3633047929004));
#59585=CARTESIAN_POINT('Ctrl Pts',(6.60842066002361,1.4563877849574,46.3717466241164));
#59586=CARTESIAN_POINT('Ctrl Pts',(6.57102255228109,1.62608326744095,46.37997780736));
#59587=CARTESIAN_POINT('Ctrl Pts',(6.52702917216304,1.79458571382543,46.3882089906037));
#59588=CARTESIAN_POINT('Ctrl Pts',(6.47652826378856,1.96134409228671,46.3964401738473));
#59589=CARTESIAN_POINT('Ctrl Pts',(6.42608815898527,2.12790169208354,46.4046614466685));
#59590=CARTESIAN_POINT('Ctrl Pts',(6.36915623117908,2.2927190655902,46.4128827194897));
#59591=CARTESIAN_POINT('Ctrl Pts',(6.30587133907991,2.45525470266743,46.4211039923109));
#59592=CARTESIAN_POINT('Ctrl Pts',(6.24264994472732,2.6176272574299,46.4293170162076));
#59593=CARTESIAN_POINT('Ctrl Pts',(6.17308841055718,2.77772230349296,46.4375300401042));
#59594=CARTESIAN_POINT('Ctrl Pts',(6.09737558966443,2.93501276293041,46.4457430640009));
#59595=CARTESIAN_POINT('Ctrl Pts',(6.01845506532761,3.09896710230928,46.4543040467337));
#59596=CARTESIAN_POINT('Ctrl Pts',(5.9328507410126,3.25987364252657,46.4628650294665));
#59597=CARTESIAN_POINT('Ctrl Pts',(5.84083313343287,3.41715631884067,46.4714260121993));
#59598=CARTESIAN_POINT('Ctrl Pts',(5.75268393266127,3.56782685437153,46.4796270924661));
#59599=CARTESIAN_POINT('Ctrl Pts',(5.65864985070985,3.71517164022411,46.4878281727329));
#59600=CARTESIAN_POINT('Ctrl Pts',(5.55901639374952,3.85870778033581,46.4960292529997));
#59601=CARTESIAN_POINT('Ctrl Pts',(5.45941581825502,4.00219655002767,46.5042276267103));
#59602=CARTESIAN_POINT('Ctrl Pts',(5.35421975207708,4.14187888304339,46.5124260004211));
#59603=CARTESIAN_POINT('Ctrl Pts',(5.24375747124643,4.2773001511172,46.5206243741317));
#59604=CARTESIAN_POINT('Ctrl Pts',(5.13331158006555,4.41270132629472,46.5288215314229));
#59605=CARTESIAN_POINT('Ctrl Pts',(5.01760125753553,4.5438424184666,46.537018688714));
#59606=CARTESIAN_POINT('Ctrl Pts',(4.8969966066966,4.67030119307117,46.5452158460052));
#59607=CARTESIAN_POINT('Ctrl Pts',(4.77638794301987,4.79676417529583,46.5534132760376));
#59608=CARTESIAN_POINT('Ctrl Pts',(4.65088487507611,4.91854427121403,46.56161070607));
#59609=CARTESIAN_POINT('Ctrl Pts',(4.52089499289623,5.03525545163359,46.5698081361024));
#59610=CARTESIAN_POINT('Ctrl Pts',(4.3908347845312,5.1520297742912,46.5780100010491));
#59611=CARTESIAN_POINT('Ctrl Pts',(4.25628318015729,5.26372946396891,46.5862118659958));
#59612=CARTESIAN_POINT('Ctrl Pts',(4.11768199038142,5.37000782365245,46.5944137309424));
#59613=CARTESIAN_POINT('Ctrl Pts',(3.97903649457181,5.47632015687256,46.6026182177433));
#59614=CARTESIAN_POINT('Ctrl Pts',(3.83633912354135,5.57720749587675,46.6108227045441));
#59615=CARTESIAN_POINT('Ctrl Pts',(3.69006137002425,5.67236600418685,46.6190271913449));
#59616=CARTESIAN_POINT('Ctrl Pts',(3.54365877316924,5.76760572721022,46.6272386804102));
#59617=CARTESIAN_POINT('Ctrl Pts',(3.39366999761389,5.85710666947437,46.6354501694755));
#59618=CARTESIAN_POINT('Ctrl Pts',(3.24059241283144,5.94061022235084,46.6436616585408));
#59619=CARTESIAN_POINT('Ctrl Pts',(3.193708143015,5.96618550895636,46.6461766555567));
#59620=CARTESIAN_POINT('Ctrl Pts',(3.14653428003767,5.99119853883744,46.6486916525726));
#59621=CARTESIAN_POINT('Ctrl Pts',(3.09908550384732,6.01564277861007,46.6512066495885));
#59622=CARTESIAN_POINT('Origin',(0.,0.,-63.6971797838103));
#59623=CARTESIAN_POINT('',(3.09908550384708,6.01564277861019,49.0457563580462));
#59624=CARTESIAN_POINT('',(3.09908550384732,6.01564277861007,48.6513967904261));
#59625=CARTESIAN_POINT('',(3.09908550384721,6.01564277861012,-63.6971797838103));
#59626=CARTESIAN_POINT('',(-6.76699762275617,0.00351474313282491,47.6971797838098));
#59627=CARTESIAN_POINT('Ctrl Pts',(-6.767,5.76061319672769E-12,47.6971797838098));
#59628=CARTESIAN_POINT('Ctrl Pts',(-6.76700000000016,-0.186007249554285,
47.7059292956226));
#59629=CARTESIAN_POINT('Ctrl Pts',(-6.75932637294278,-0.37201435581051,
47.7146788074353));
#59630=CARTESIAN_POINT('Ctrl Pts',(-6.74400518263408,-0.557389537580933,
47.7234283192481));
#59631=CARTESIAN_POINT('Ctrl Pts',(-6.72868405703788,-0.742763936377517,
47.7321777941053));
#59632=CARTESIAN_POINT('Ctrl Pts',(-6.70571545643634,-0.927506130399944,
47.7409272689625));
#59633=CARTESIAN_POINT('Ctrl Pts',(-6.67517739401656,-1.11098864009058,
47.7496767438197));
#59634=CARTESIAN_POINT('Ctrl Pts',(-6.64463945804483,-1.29447039004059,
47.7584261824482));
#59635=CARTESIAN_POINT('Ctrl Pts',(-6.60653217002831,-1.476692183388,47.7671756210767));
#59636=CARTESIAN_POINT('Ctrl Pts',(-6.56098496085599,-1.65703510627311,
47.7759250597052));
#59637=CARTESIAN_POINT('Ctrl Pts',(-6.5154379364968,-1.83737729739572,47.7846744628319));
#59638=CARTESIAN_POINT('Ctrl Pts',(-6.46245112157023,-2.0158403554455,47.7934238659585));
#59639=CARTESIAN_POINT('Ctrl Pts',(-6.40220448361843,-2.19181813797041,
47.8021732690852));
#59640=CARTESIAN_POINT('Ctrl Pts',(-6.34195808512111,-2.36779522105933,
47.8109226374367));
#59641=CARTESIAN_POINT('Ctrl Pts',(-6.27445201416505,-2.54128677725372,
47.8196720057882));
#59642=CARTESIAN_POINT('Ctrl Pts',(-6.19991555052887,-2.71170355428285,
47.8284213741397));
#59643=CARTESIAN_POINT('Ctrl Pts',(-6.12537937695282,-2.88211966813174,
47.8371707084429));
#59644=CARTESIAN_POINT('Ctrl Pts',(-6.04381298028509,-3.04946076419556,
47.8459200427461));
#59645=CARTESIAN_POINT('Ctrl Pts',(-5.95549339309033,-3.21315848424218,
47.8546693770493));
#59646=CARTESIAN_POINT('Ctrl Pts',(-5.8671741422586,-3.37685558084993,47.8634186780308));
#59647=CARTESIAN_POINT('Ctrl Pts',(-5.77210188844118,-3.53690907699916,
47.8721679790124));
#59648=CARTESIAN_POINT('Ctrl Pts',(-5.67059953311423,-3.69277537023913,
47.880917279994));
#59649=CARTESIAN_POINT('Ctrl Pts',(-5.56909755592743,-3.84864108280976,
47.8896665483806));
#59650=CARTESIAN_POINT('Ctrl Pts',(-5.46116568154985,-4.00031938354804,
47.8984158167672));
#59651=CARTESIAN_POINT('Ctrl Pts',(-5.34717048488377,-4.14729511918165,
47.9071650851539));
#59652=CARTESIAN_POINT('Ctrl Pts',(-5.23317570343316,-4.29427031947164,
47.9159143216722));
#59653=CARTESIAN_POINT('Ctrl Pts',(-5.11311781951571,-4.43654276249527,
47.9246635581906));
#59654=CARTESIAN_POINT('Ctrl Pts',(-4.98740458929283,-4.57362924412341,
47.9334127947089));
#59655=CARTESIAN_POINT('Ctrl Pts',(-4.86169180652779,-4.71071523781227,
47.9421620000856));
#59656=CARTESIAN_POINT('Ctrl Pts',(-4.73032391141612,-4.84261509584451,
47.9509112054623));
#59657=CARTESIAN_POINT('Ctrl Pts',(-4.59374706947367,-4.96888084599561,
47.959660410839));
#59658=CARTESIAN_POINT('Ctrl Pts',(-4.45717070231578,-5.0951461572068,47.9684095858007));
#59659=CARTESIAN_POINT('Ctrl Pts',(-4.31538563497464,-5.21577720520498,
47.9771587607624));
#59660=CARTESIAN_POINT('Ctrl Pts',(-4.16887340952175,-5.33036429293369,
47.9859079357241));
#59661=CARTESIAN_POINT('Ctrl Pts',(-4.02236168122654,-5.44495099183581,
47.9946570809974));
#59662=CARTESIAN_POINT('Ctrl Pts',(-3.87112305263349,-5.55349359497811,
48.0034062262706));
#59663=CARTESIAN_POINT('Ctrl Pts',(-3.71567116929162,-5.65562346357102,
48.0121553715439));
#59664=CARTESIAN_POINT('Ctrl Pts',(-3.56021980053478,-5.75775299408824,
48.0209044878552));
#59665=CARTESIAN_POINT('Ctrl Pts',(-3.40055544442251,-5.85346967519782,
48.0296536041666));
#59666=CARTESIAN_POINT('Ctrl Pts',(-3.23722035887009,-5.94244843041292,
48.038402720478));
#59667=CARTESIAN_POINT('Ctrl Pts',(-3.07388580043665,-6.03142689847362,
48.047151808554));
#59668=CARTESIAN_POINT('Ctrl Pts',(-2.90688078789406,-6.11366734707814,
48.05590089663));
#59669=CARTESIAN_POINT('Ctrl Pts',(-2.73677250610585,-6.18889047001344,
48.064649984706));
#59670=CARTESIAN_POINT('Ctrl Pts',(-2.56666475917162,-6.2641133564324,48.0733990452732));
#59671=CARTESIAN_POINT('Ctrl Pts',(-2.39345402457356,-6.33231884545155,
48.0821481058403));
#59672=CARTESIAN_POINT('Ctrl Pts',(-2.21772855944364,-6.39327529804779,
48.0908971664075));
#59673=CARTESIAN_POINT('Ctrl Pts',(-2.04200363223899,-6.45423156404605,
48.0996462001923));
#59674=CARTESIAN_POINT('Ctrl Pts',(-1.86376426061351,-6.50793874412362,
48.1083952339771));
#59675=CARTESIAN_POINT('Ctrl Pts',(-1.68361577622014,-6.55421443943229,
48.1171442677619));
#59676=CARTESIAN_POINT('Ctrl Pts',(-1.50346782833576,-6.60048999692505,
48.1258932754908));
#59677=CARTESIAN_POINT('Ctrl Pts',(-1.32141105657782,-6.63933404265082,
48.1346422832196));
#59678=CARTESIAN_POINT('Ctrl Pts',(-1.13806375346965,-6.67061465631456,
48.1433912909485));
#59679=CARTESIAN_POINT('Ctrl Pts',(-0.954716981174169,-6.70189517941712,
48.152140273348));
#59680=CARTESIAN_POINT('Ctrl Pts',(-0.7700799674463,-6.72561226608958,48.1608892557474));
#59681=CARTESIAN_POINT('Ctrl Pts',(-0.584779764076936,-6.74168536995951,
48.1696382381468));
#59682=CARTESIAN_POINT('Ctrl Pts',(-0.39148958759668,-6.75845153117851,
48.1787644685625));
#59683=CARTESIAN_POINT('Ctrl Pts',(-0.197478091808809,-6.76689985146384,
48.1878906989781));
#59684=CARTESIAN_POINT('Ctrl Pts',(-0.00346214753445197,-6.76699911434415,
48.1970169293937));
#59685=CARTESIAN_POINT('Ctrl Pts',(0.184490798481292,-6.76709527525944,
48.2058579651088));
#59686=CARTESIAN_POINT('Ctrl Pts',(0.372447602151505,-6.75935633790781,
48.214699000824));
#59687=CARTESIAN_POINT('Ctrl Pts',(0.559756448191021,-6.7438091401454,48.2235400365391));
#59688=CARTESIAN_POINT('Ctrl Pts',(0.745136131040126,-6.7284220687319,48.2322900151524));
#59689=CARTESIAN_POINT('Ctrl Pts',(0.929880851941783,-6.70538686355768,
48.2410399937657));
#59690=CARTESIAN_POINT('Ctrl Pts',(1.11336305057134,-6.67478177303367,48.249789972379));
#59691=CARTESIAN_POINT('Ctrl Pts',(1.29684337089801,-6.64417699581324,48.258539861419));
#59692=CARTESIAN_POINT('Ctrl Pts',(1.47906091204875,-6.60600253548131,48.267289750459));
#59693=CARTESIAN_POINT('Ctrl Pts',(1.65939671094913,-6.5603880644129,48.276039639499));
#59694=CARTESIAN_POINT('Ctrl Pts',(1.83973072368852,-6.51477404513937,48.2847894418745));
#59695=CARTESIAN_POINT('Ctrl Pts',(2.01818275356728,-6.46172023288757,48.2935392442499));
#59696=CARTESIAN_POINT('Ctrl Pts',(2.19414664033019,-6.40140683918213,48.3022890466254));
#59697=CARTESIAN_POINT('Ctrl Pts',(2.37010884270956,-6.34109402281611,48.311038765245));
#59698=CARTESIAN_POINT('Ctrl Pts',(2.54358267847507,-6.27352185699913,48.3197884838645));
#59699=CARTESIAN_POINT('Ctrl Pts',(2.71397890841447,-6.1989198643539,48.3285382024841));
#59700=CARTESIAN_POINT('Ctrl Pts',(2.88437356388658,-6.12431856103377,48.3372878402559));
#59701=CARTESIAN_POINT('Ctrl Pts',(3.05169040786899,-6.04268767582695,48.3460374780277));
#59702=CARTESIAN_POINT('Ctrl Pts',(3.21536112511791,-5.95430447954088,48.3547871157995));
#59703=CARTESIAN_POINT('Ctrl Pts',(3.37903038442584,-5.86592207055191,48.3635366756316));
#59704=CARTESIAN_POINT('Ctrl Pts',(3.5390533297972,-5.77078760703532,48.3722862354637));
#59705=CARTESIAN_POINT('Ctrl Pts',(3.69488643041644,-5.6692242208546,48.3810357952957));
#59706=CARTESIAN_POINT('Ctrl Pts',(3.850718194685,-5.56766170563326,48.3897852800957));
#59707=CARTESIAN_POINT('Ctrl Pts',(4.00235994598988,-5.45967053456425,48.3985347648957));
#59708=CARTESIAN_POINT('Ctrl Pts',(4.1492966297407,-5.34561750206863,48.4072842496957));
#59709=CARTESIAN_POINT('Ctrl Pts',(4.29623210224804,-5.23156540974662,48.4160336623711));
#59710=CARTESIAN_POINT('Ctrl Pts',(4.43846235841869,-5.11145173172401,48.4247830750464));
#59711=CARTESIAN_POINT('Ctrl Pts',(4.57550431797173,-4.98568443006796,48.4335324877218));
#59712=CARTESIAN_POINT('Ctrl Pts',(4.71254519337245,-4.85991812336931,48.4422818311797));
#59713=CARTESIAN_POINT('Ctrl Pts',(4.84439764314741,-4.7284984763135,48.4510311746375));
#59714=CARTESIAN_POINT('Ctrl Pts',(4.9706138419645,-4.59187184425599,48.4597805180954));
#59715=CARTESIAN_POINT('Ctrl Pts',(5.09682908419994,-4.45524624767991,48.4685297952428));
#59716=CARTESIAN_POINT('Ctrl Pts',(5.21740796649981,-4.31341395557123,48.4772790723902));
#59717=CARTESIAN_POINT('Ctrl Pts',(5.33194095942083,-4.16685668163071,48.4860283495376));
#59718=CARTESIAN_POINT('Ctrl Pts',(5.44647312234966,-4.0203004697544,48.4947775632811));
#59719=CARTESIAN_POINT('Ctrl Pts',(5.55495930712123,-3.86901957035783,48.5035267770246));
#59720=CARTESIAN_POINT('Ctrl Pts',(5.65703106079633,-3.71352778058622,48.5122759907682));
#59721=CARTESIAN_POINT('Ctrl Pts',(5.75910210868577,-3.5580370659786,48.5210251440144));
#59722=CARTESIAN_POINT('Ctrl Pts',(5.85475865698394,-3.39833575881167,48.5297742972606));
#59723=CARTESIAN_POINT('Ctrl Pts',(5.94367583068912,-3.23496624706998,48.5385234505067));
#59724=CARTESIAN_POINT('Ctrl Pts',(6.03259241909938,-3.07159781070374,48.5472725461619));
#59725=CARTESIAN_POINT('Ctrl Pts',(6.11476958470839,-2.90456146976105,48.556021641817));
#59726=CARTESIAN_POINT('Ctrl Pts',(6.18992823574268,-2.73442451648525,48.5647707374721));
#59727=CARTESIAN_POINT('Ctrl Pts',(6.26508641700826,-2.56428862662683,48.5735197784422));
#59728=CARTESIAN_POINT('Ctrl Pts',(6.33322605570196,-2.39105242531544,48.5822688194124));
#59729=CARTESIAN_POINT('Ctrl Pts',(6.39411573747675,-2.21530425353994,48.5910178603825));
#59730=CARTESIAN_POINT('Ctrl Pts',(6.45500505889042,-2.03955712188826,48.5997668495735));
#59731=CARTESIAN_POINT('Ctrl Pts',(6.50864441544854,-1.86129832025836,48.6085158387645));
#59732=CARTESIAN_POINT('Ctrl Pts',(6.55485164049839,-1.68113324012572,48.6172648279555));
#59733=CARTESIAN_POINT('Ctrl Pts',(6.60199852639052,-1.49730435913154,48.6261917348324));
#59734=CARTESIAN_POINT('Ctrl Pts',(6.64140767440961,-1.31149113173899,48.6351186417092));
#59735=CARTESIAN_POINT('Ctrl Pts',(6.67293975269562,-1.1243505044667,48.6440455485861));
#59736=CARTESIAN_POINT('Ctrl Pts',(6.70384664831472,-0.940920291566195,
48.6527954627701));
#59737=CARTESIAN_POINT('Ctrl Pts',(6.72718585889637,-0.756215114280447,
48.6615453769542));
#59738=CARTESIAN_POINT('Ctrl Pts',(6.74287810451843,-0.570862389377701,
48.6702952911381));
#59739=CARTESIAN_POINT('Ctrl Pts',(6.75857004154109,-0.38551330957069,48.6790450332487));
#59740=CARTESIAN_POINT('Ctrl Pts',(6.76661529035548,-0.199516993261825,
48.6877947753593));
#59741=CARTESIAN_POINT('Ctrl Pts',(6.76698652348896,-0.013505218207691,
48.6965445174699));
#59742=CARTESIAN_POINT('Ctrl Pts',(6.76735774981531,0.172503146035245,48.7052940991405));
#59743=CARTESIAN_POINT('Ctrl Pts',(6.76005524147499,0.358526681829814,48.7140436808112));
#59744=CARTESIAN_POINT('Ctrl Pts',(6.74510380214911,0.543933542111204,48.7227932624818));
#59745=CARTESIAN_POINT('Ctrl Pts',(6.7301526171102,0.729337249080968,48.7315426953437));
#59746=CARTESIAN_POINT('Ctrl Pts',(6.70755278444657,0.914124015850821,48.7402921282056));
#59747=CARTESIAN_POINT('Ctrl Pts',(6.67738106408353,1.09766621748993,48.7490415610676));
#59748=CARTESIAN_POINT('Ctrl Pts',(6.6472098167733,1.28120554142928,48.7577908567499));
#59749=CARTESIAN_POINT('Ctrl Pts',(6.6094669658161,1.46350005650224,48.7665401524323));
#59750=CARTESIAN_POINT('Ctrl Pts',(6.56428070011094,1.64393062206138,48.7752894481146));
#59751=CARTESIAN_POINT('Ctrl Pts',(6.51909508282852,1.82435859844252,48.7840386182446));
#59752=CARTESIAN_POINT('Ctrl Pts',(6.46646633415786,2.00292240086159,48.7927877883746));
#59753=CARTESIAN_POINT('Ctrl Pts',(6.40657319597331,2.17901557696048,48.8015369585046));
#59754=CARTESIAN_POINT('Ctrl Pts',(6.34668083768443,2.35510646007035,48.8102860147076));
#59755=CARTESIAN_POINT('Ctrl Pts',(6.27952437144043,2.5287265099614,48.8190350709107));
#59756=CARTESIAN_POINT('Ctrl Pts',(6.20533187335302,2.69928607997543,48.8277841271138));
#59757=CARTESIAN_POINT('Ctrl Pts',(6.12831449784424,2.87633970115033,48.8368663034027));
#59758=CARTESIAN_POINT('Ctrl Pts',(6.04371489463328,3.05009490562002,48.8459484796915));
#59759=CARTESIAN_POINT('Ctrl Pts',(5.95184265120669,3.21991584599302,48.8550306559803));
#59760=CARTESIAN_POINT('Ctrl Pts',(5.86333281335674,3.38352155904987,48.8637804363348));
#59761=CARTESIAN_POINT('Ctrl Pts',(5.76807337235869,3.54347560903525,48.8725302166892));
#59762=CARTESIAN_POINT('Ctrl Pts',(5.66638790086541,3.69923467178363,48.8812799970436));
#59763=CARTESIAN_POINT('Ctrl Pts',(5.56470608502931,3.85498813489493,48.8900294628379));
#59764=CARTESIAN_POINT('Ctrl Pts',(5.45659885767141,4.00654667256004,48.8987789286322));
#59765=CARTESIAN_POINT('Ctrl Pts',(5.34243340580697,4.15339551505966,48.9075283944264));
#59766=CARTESIAN_POINT('Ctrl Pts',(5.22827145140793,4.30023985883628,48.9162775921803));
#59767=CARTESIAN_POINT('Ctrl Pts',(5.10805181978298,4.44237456992802,48.9250267899341));
#59768=CARTESIAN_POINT('Ctrl Pts',(4.9821828128277,4.57931691626211,48.933775987688));
#59769=CARTESIAN_POINT('Ctrl Pts',(4.8563169929645,4.71625579511934,48.942524963906));
#59770=CARTESIAN_POINT('Ctrl Pts',(4.7248022779206,4.84800236135553,48.951273940124));
#59771=CARTESIAN_POINT('Ctrl Pts',(4.58808530848337,4.97410918678703,48.9600229163421));
#59772=CARTESIAN_POINT('Ctrl Pts',(4.45135945057195,5.10022421088813,48.9687724613633));
#59773=CARTESIAN_POINT('Ctrl Pts',(4.30943087208266,5.220698566118,48.9775220063844));
#59774=CARTESIAN_POINT('Ctrl Pts',(4.16278164322694,5.33512305301507,48.9862715514057));
#59775=CARTESIAN_POINT('Ctrl Pts',(4.01614103534619,5.44954081331258,48.9950205820729));
#59776=CARTESIAN_POINT('Ctrl Pts',(3.86478055833644,5.55790924068177,49.0037696127402));
#59777=CARTESIAN_POINT('Ctrl Pts',(3.70921425812184,5.65986029751139,49.0125186434074));
#59778=CARTESIAN_POINT('Ctrl Pts',(3.55364584530371,5.76181273884498,49.0212677928873));
#59779=CARTESIAN_POINT('Ctrl Pts',(3.39387173464616,5.85734747817905,49.0300169423671));
#59780=CARTESIAN_POINT('Ctrl Pts',(3.23043456092697,5.94614005448649,49.0387660918469));
#59781=CARTESIAN_POINT('Ctrl Pts',(3.18690768806583,5.9697874481118,49.04109618058));
#59782=CARTESIAN_POINT('Ctrl Pts',(3.14312114982972,5.99295688499254,49.0434262693131));
#59783=CARTESIAN_POINT('Ctrl Pts',(3.09908550384708,6.01564277861019,49.0457563580462));
#59784=CARTESIAN_POINT('Ctrl Pts',(3.09908550384709,6.01564277861018,47.0459139429101));
#59785=CARTESIAN_POINT('Ctrl Pts',(2.93606339535898,6.09962706288626,47.0545463314129));
#59786=CARTESIAN_POINT('Ctrl Pts',(2.76953995568906,6.17702472520362,47.0631787199156));
#59787=CARTESIAN_POINT('Ctrl Pts',(2.60006334833904,6.24755628903206,47.0718111084183));
#59788=CARTESIAN_POINT('Ctrl Pts',(2.43070337527171,6.31803931283788,47.0804375560867));
#59789=CARTESIAN_POINT('Ctrl Pts',(2.25839456749121,6.3816655451314,47.0890640037551));
#59790=CARTESIAN_POINT('Ctrl Pts',(2.08370711628746,6.4382026726046,47.0976904514235));
#59791=CARTESIAN_POINT('Ctrl Pts',(1.90916134328403,6.4946939463063,47.1063099027131));
#59792=CARTESIAN_POINT('Ctrl Pts',(1.73224106521693,6.54410749540541,47.1149293540028));
#59793=CARTESIAN_POINT('Ctrl Pts',(1.55353408329108,6.58626000489299,47.1235488052924));
#59794=CARTESIAN_POINT('Ctrl Pts',(1.43892682911922,6.61329299105146,47.1290765783773));
#59795=CARTESIAN_POINT('Ctrl Pts',(1.32358510542547,6.63734061643636,47.1346043514622));
#59796=CARTESIAN_POINT('Ctrl Pts',(1.20766724045767,6.65836532764051,47.140132124547));
#59797=CARTESIAN_POINT('Ctrl Pts',(1.0309777209973,6.69041255453248,47.1485579143968));
#59798=CARTESIAN_POINT('Ctrl Pts',(0.853026240713427,6.71541981467453,47.1569837042466));
#59799=CARTESIAN_POINT('Ctrl Pts',(0.674398239450259,6.73331092514124,47.1654094940964));
#59800=CARTESIAN_POINT('Ctrl Pts',(0.495728790481579,6.75120618694745,47.1738372390129));
#59801=CARTESIAN_POINT('Ctrl Pts',(0.316382837402103,6.76198197381547,47.1822649839294));
#59802=CARTESIAN_POINT('Ctrl Pts',(0.136950059128389,6.76561406535318,47.1906927288458));
#59803=CARTESIAN_POINT('Ctrl Pts',(-0.0425486516889925,6.7692474915023,
47.1991235705357));
#59804=CARTESIAN_POINT('Ctrl Pts',(-0.222133920036509,6.76573198170366,
47.2075544122257));
#59805=CARTESIAN_POINT('Ctrl Pts',(-0.401216555870379,6.75509543050989,
47.2159852539156));
#59806=CARTESIAN_POINT('Ctrl Pts',(-0.580463745788857,6.74444910568319,
47.2244238424729));
#59807=CARTESIAN_POINT('Ctrl Pts',(-0.759207049298254,6.72666868617792,
47.2328624310302));
#59808=CARTESIAN_POINT('Ctrl Pts',(-0.936861759259506,6.70183400600442,
47.2413010195876));
#59809=CARTESIAN_POINT('Ctrl Pts',(-1.11460962349945,6.67698630362216,47.2497440329678));
#59810=CARTESIAN_POINT('Ctrl Pts',(-1.29126742893335,6.64507701701444,47.258187046348));
#59811=CARTESIAN_POINT('Ctrl Pts',(-1.46626056559307,6.6062371251558,47.2666300597283));
#59812=CARTESIAN_POINT('Ctrl Pts',(-1.64143754473994,6.5673564292836,47.2750819430825));
#59813=CARTESIAN_POINT('Ctrl Pts',(-1.81494604009456,6.52153066302154,47.2835338264368));
#59814=CARTESIAN_POINT('Ctrl Pts',(-1.98622546773283,6.46894097911934,47.2919857097911));
#59815=CARTESIAN_POINT('Ctrl Pts',(-2.03290452289036,6.45460862882231,47.2942891150203));
#59816=CARTESIAN_POINT('Ctrl Pts',(-2.07941812318807,6.43977417843863,47.2965925202495));
#59817=CARTESIAN_POINT('Ctrl Pts',(-2.12575517203482,6.42444191728489,47.2988959254787));
#59818=CARTESIAN_POINT('Ctrl Pts',(-2.29307159779326,6.36907932517157,47.3072131908121));
#59819=CARTESIAN_POINT('Ctrl Pts',(-2.45838553073322,6.30712282735392,47.3155304561456));
#59820=CARTESIAN_POINT('Ctrl Pts',(-2.6211503339279,6.23873864871335,47.323847721479));
#59821=CARTESIAN_POINT('Ctrl Pts',(-2.7837778575355,6.17041214686544,47.3321579718391));
#59822=CARTESIAN_POINT('Ctrl Pts',(-2.94386021593875,6.09566889944545,47.3404682221992));
#59823=CARTESIAN_POINT('Ctrl Pts',(-3.10086751331362,6.01472440473179,47.3487784725593));
#59824=CARTESIAN_POINT('Ctrl Pts',(-3.25777114119002,5.93383335642038,47.3570832357891));
#59825=CARTESIAN_POINT('Ctrl Pts',(-3.4116034457619,5.84674937864201,47.365387999019));
#59826=CARTESIAN_POINT('Ctrl Pts',(-3.56185584117991,5.75373547937795,47.3736927622489));
#59827=CARTESIAN_POINT('Ctrl Pts',(-3.71203653191623,5.66076596897052,47.3819935622115));
#59828=CARTESIAN_POINT('Ctrl Pts',(-3.85864042310634,5.56187235955357,47.3902943621741));
#59829=CARTESIAN_POINT('Ctrl Pts',(-4.0011846181465,5.4573629759718,47.3985951621367));
#59830=CARTESIAN_POINT('Ctrl Pts',(-4.14368687183637,5.35288434260519,47.4068935197216));
#59831=CARTESIAN_POINT('Ctrl Pts',(-4.28213153019121,5.24279343412293,47.4151918773066));
#59832=CARTESIAN_POINT('Ctrl Pts',(-4.4160655352711,5.12744129056499,47.4234902348915));
#59833=CARTESIAN_POINT('Ctrl Pts',(-4.55001316782912,5.01207741019077,47.4317894368153));
#59834=CARTESIAN_POINT('Ctrl Pts',(-4.67944896164117,4.89145144640008,47.440088638739));
#59835=CARTESIAN_POINT('Ctrl Pts',(-4.80395331463428,4.76595442181462,47.4483878406628));
#59836=CARTESIAN_POINT('Ctrl Pts',(-4.92847029000877,4.6404446742097,47.4566878839684));
#59837=CARTESIAN_POINT('Ctrl Pts',(-5.04805458255985,4.51006312818003,47.4649879272739));
#59838=CARTESIAN_POINT('Ctrl Pts',(-5.1623238872576,4.37523726020082,47.4732879705795));
#59839=CARTESIAN_POINT('Ctrl Pts',(-5.27662374565087,4.24037534204586,47.4815902331774));
#59840=CARTESIAN_POINT('Ctrl Pts',(-5.3856055587599,4.10106699889841,47.4898924957753));
#59841=CARTESIAN_POINT('Ctrl Pts',(-5.48892758899494,3.95777246980802,47.4981947583733));
#59842=CARTESIAN_POINT('Ctrl Pts',(-5.59229439954663,3.81441583610767,47.5065006192159));
#59843=CARTESIAN_POINT('Ctrl Pts',(-5.68999633505279,3.66706985528161,47.5148064800585));
#59844=CARTESIAN_POINT('Ctrl Pts',(-5.78173512256456,3.51622353847183,47.5231123409011));
#59845=CARTESIAN_POINT('Ctrl Pts',(-5.87358235179552,3.36519891067309,47.5314280198573));
#59846=CARTESIAN_POINT('Ctrl Pts',(-5.95945216866167,3.21066597756631,47.5397436988134));
#59847=CARTESIAN_POINT('Ctrl Pts',(-6.03909183422184,3.05313917433108,47.5480593777695));
#59848=CARTESIAN_POINT('Ctrl Pts',(-6.11878187123628,2.89551273664727,47.5563803163264));
#59849=CARTESIAN_POINT('Ctrl Pts',(-6.19223375406644,2.73488896844577,47.5647012548833));
#59850=CARTESIAN_POINT('Ctrl Pts',(-6.25924296835286,2.57180218195826,47.5730221934401));
#59851=CARTESIAN_POINT('Ctrl Pts',(-6.32635177908765,2.4084729979903,47.5813554994891));
#59852=CARTESIAN_POINT('Ctrl Pts',(-6.38699866499412,2.24267380630154,47.5896888055379));
#59853=CARTESIAN_POINT('Ctrl Pts',(-6.44102862009678,2.0749552561668,47.5980221115869));
#59854=CARTESIAN_POINT('Ctrl Pts',(-6.48079785698841,1.95150450114106,47.6041559168385));
#59855=CARTESIAN_POINT('Ctrl Pts',(-6.51698319977678,1.82701418374228,47.6102897220901));
#59856=CARTESIAN_POINT('Ctrl Pts',(-6.54954059514499,1.70170708188803,47.6164235273416));
#59857=CARTESIAN_POINT('Ctrl Pts',(-6.60381077106686,1.49283169781688,47.6266480150904));
#59858=CARTESIAN_POINT('Ctrl Pts',(-6.64813743337064,1.2811567617572,47.6368725028391));
#59859=CARTESIAN_POINT('Ctrl Pts',(-6.68226665206471,1.06752114297744,47.6470969905879));
#59860=CARTESIAN_POINT('Ctrl Pts',(-6.71580609236908,0.857577307251926,
47.6571447915518));
#59861=CARTESIAN_POINT('Ctrl Pts',(-6.73949747235133,0.645739900102742,
47.6671925925157));
#59862=CARTESIAN_POINT('Ctrl Pts',(-6.75314355816964,0.432829161161674,
47.6772403934795));
#59863=CARTESIAN_POINT('Ctrl Pts',(-6.76217023085786,0.291992031906009,
47.683886856923));
#59864=CARTESIAN_POINT('Ctrl Pts',(-6.76680235460557,0.150685748618224,
47.6905333203664));
#59865=CARTESIAN_POINT('Ctrl Pts',(-6.76699380863722,0.00915389892568289,
47.6971797838098));
#59866=CARTESIAN_POINT('',(-6.767,5.25875296000095E-12,47.3028202161897));
#59867=CARTESIAN_POINT('Ctrl Pts',(3.09908550384732,6.01564277861007,46.6512066495885));
#59868=CARTESIAN_POINT('Ctrl Pts',(2.94392541256584,6.09557677857692,46.6594308272786));
#59869=CARTESIAN_POINT('Ctrl Pts',(2.78582439819486,6.16942480198856,46.6676550049686));
#59870=CARTESIAN_POINT('Ctrl Pts',(2.62530703088028,6.23699061997135,46.6758791826586));
#59871=CARTESIAN_POINT('Ctrl Pts',(2.53816003698039,6.27367299288897,46.6803441970989));
#59872=CARTESIAN_POINT('Ctrl Pts',(2.45030109831904,6.30850451592851,46.6848092115392));
#59873=CARTESIAN_POINT('Ctrl Pts',(2.36181586475785,6.34145999127789,46.6892742259795));
#59874=CARTESIAN_POINT('Ctrl Pts',(2.18474318113969,6.40740901152872,46.6982094127618));
#59875=CARTESIAN_POINT('Ctrl Pts',(2.00479427769777,6.46597926066129,46.7071445995441));
#59876=CARTESIAN_POINT('Ctrl Pts',(1.82258005357805,6.51693877125598,46.7160797863264));
#59877=CARTESIAN_POINT('Ctrl Pts',(1.64063872999669,6.56782196026852,46.725001590963));
#59878=CARTESIAN_POINT('Ctrl Pts',(1.4564391036601,6.61111708534289,46.7339233955997));
#59879=CARTESIAN_POINT('Ctrl Pts',(1.27060854541588,6.64664147704058,46.7428452002363));
#59880=CARTESIAN_POINT('Ctrl Pts',(1.0852312719738,6.68207921632214,46.7517452424756));
#59881=CARTESIAN_POINT('Ctrl Pts',(0.898231259765142,6.70978400408473,46.7606452847149));
#59882=CARTESIAN_POINT('Ctrl Pts',(0.710246807896361,6.7296239472851,46.7695453269542));
#59883=CARTESIAN_POINT('Ctrl Pts',(0.522551760855276,6.74943334660119,46.7784316674476));
#59884=CARTESIAN_POINT('Ctrl Pts',(0.333875552927846,6.76140202678392,46.7873180079409));
#59885=CARTESIAN_POINT('Ctrl Pts',(0.144865307356764,6.76544921219016,46.7962043484343));
#59886=CARTESIAN_POINT('Ctrl Pts',(-0.0436616720093867,6.76948604964978,
46.8050679681062));
#59887=CARTESIAN_POINT('Ctrl Pts',(-0.232520727267387,6.76564180217864,
46.8139315877782));
#59888=CARTESIAN_POINT('Ctrl Pts',(-0.421061756595683,6.75388747293976,
46.8227952074501));
#59889=CARTESIAN_POINT('Ctrl Pts',(-0.600044585298222,6.74272903647544,
46.8312094806037));
#59890=CARTESIAN_POINT('Ctrl Pts',(-0.778740569150256,6.72444254463978,
46.8396237537572));
#59891=CARTESIAN_POINT('Ctrl Pts',(-0.956590091467695,6.69904652894021,
46.8480380269108));
#59892=CARTESIAN_POINT('Ctrl Pts',(-1.13012721043577,6.67426630271106,46.8562482751153));
#59893=CARTESIAN_POINT('Ctrl Pts',(-1.30269149555158,6.64273995661422,46.8644585233199));
#59894=CARTESIAN_POINT('Ctrl Pts',(-1.47372865793921,6.60457514475903,46.8726687715244));
#59895=CARTESIAN_POINT('Ctrl Pts',(-1.64480647927,6.56640126036723,46.8808809714686));
#59896=CARTESIAN_POINT('Ctrl Pts',(-1.81435610720646,6.52158584371817,46.8890931714128));
#59897=CARTESIAN_POINT('Ctrl Pts',(-1.98183579380467,6.47028715640926,46.897305371357));
#59898=CARTESIAN_POINT('Ctrl Pts',(-2.14938511710104,6.41896713952136,46.9055209858674));
#59899=CARTESIAN_POINT('Ctrl Pts',(-2.31486244436512,6.36115858572511,46.9137366003779));
#59900=CARTESIAN_POINT('Ctrl Pts',(-2.4777433858052,6.29706889863043,46.9219522148883));
#59901=CARTESIAN_POINT('Ctrl Pts',(-2.64080723540247,6.23290724162657,46.9301770551738));
#59902=CARTESIAN_POINT('Ctrl Pts',(-2.80126854436963,6.1624504937069,46.9384018954592));
#59903=CARTESIAN_POINT('Ctrl Pts',(-2.95862413773496,6.08595368135612,46.9466267357446));
#59904=CARTESIAN_POINT('Ctrl Pts',(-3.1160805228276,6.00940787013795,46.9548568443262));
#59905=CARTESIAN_POINT('Ctrl Pts',(-3.2704269136844,5.92681444959039,46.9630869529077));
#59906=CARTESIAN_POINT('Ctrl Pts',(-3.42118681625558,5.83847323949327,46.9713170614892));
#59907=CARTESIAN_POINT('Ctrl Pts',(-3.57215341296688,5.75001091224135,46.9795584536759));
#59908=CARTESIAN_POINT('Ctrl Pts',(-3.71952340093979,5.65578524653429,46.9877998458626));
#59909=CARTESIAN_POINT('Ctrl Pts',(-3.86285039025964,5.55613857480813,46.9960412380493));
#59910=CARTESIAN_POINT('Ctrl Pts',(-3.92522993744552,5.51276981160202,46.9996281013137));
#59911=CARTESIAN_POINT('Ctrl Pts',(-3.98684409001736,5.46837470281088,47.0032149645781));
#59912=CARTESIAN_POINT('Ctrl Pts',(-4.0476581386488,5.42298373523563,47.0068018278425));
#59913=CARTESIAN_POINT('Ctrl Pts',(-4.18954903877564,5.31707785671216,47.0151706713691));
#59914=CARTESIAN_POINT('Ctrl Pts',(-4.32742197024226,5.20549438136416,47.0235395148958));
#59915=CARTESIAN_POINT('Ctrl Pts',(-4.4608059996976,5.0885654985528,47.0319083584224));
#59916=CARTESIAN_POINT('Ctrl Pts',(-4.59406364738814,4.97174740620583,47.0402692724448));
#59917=CARTESIAN_POINT('Ctrl Pts',(-4.7228406120741,4.84959422392152,47.0486301864673));
#59918=CARTESIAN_POINT('Ctrl Pts',(-4.846697292323,4.72247968302553,47.0569911004898));
#59919=CARTESIAN_POINT('Ctrl Pts',(-4.97045817713752,4.59546345731638,47.0653455478655));
#59920=CARTESIAN_POINT('Ctrl Pts',(-5.08930612336192,4.46349376528868,47.0736999952414));
#59921=CARTESIAN_POINT('Ctrl Pts',(-5.20283660433539,4.32698281353044,47.0820544426171));
#59922=CARTESIAN_POINT('Ctrl Pts',(-5.31629902297498,4.19055370106239,47.0904038814421));
#59923=CARTESIAN_POINT('Ctrl Pts',(-5.42445011179671,4.04958901851922,47.0987533202671));
#59924=CARTESIAN_POINT('Ctrl Pts',(-5.52692385525375,3.90453604135331,47.107102759092));
#59925=CARTESIAN_POINT('Ctrl Pts',(-5.62935841990309,3.75953852232242,47.1154490056743));
#59926=CARTESIAN_POINT('Ctrl Pts',(-5.7261197672751,3.61045610331053,47.1237952522565));
#59927=CARTESIAN_POINT('Ctrl Pts',(-5.81688345084336,3.4577674761766,47.1321414988388));
#59928=CARTESIAN_POINT('Ctrl Pts',(-5.90762870315803,3.30510985530745,47.1404860505605));
#59929=CARTESIAN_POINT('Ctrl Pts',(-5.99237854344952,3.14884778015148,47.1488306022822));
#59930=CARTESIAN_POINT('Ctrl Pts',(-6.07085283775845,2.98948738453271,47.1571751540039));
#59931=CARTESIAN_POINT('Ctrl Pts',(-6.14932357433846,2.83013421371402,47.1655193274151));
#59932=CARTESIAN_POINT('Ctrl Pts',(-6.2215191806665,2.66768331008425,47.1738635008262));
#59933=CARTESIAN_POINT('Ctrl Pts',(-6.28720620812607,2.50266399992108,47.1822076742373));
#59934=CARTESIAN_POINT('Ctrl Pts',(-6.35290061801783,2.33762614357133,47.1905527854333));
#59935=CARTESIAN_POINT('Ctrl Pts',(-6.41208486491018,2.1700196241852,47.1988978966292));
#59936=CARTESIAN_POINT('Ctrl Pts',(-6.46457414151185,2.00039250370931,47.2072430078251));
#59937=CARTESIAN_POINT('Ctrl Pts',(-6.51709907580486,1.83065014995345,47.2155937881295));
#59938=CARTESIAN_POINT('Ctrl Pts',(-6.56291984934629,1.65888477997448,47.2239445684338));
#59939=CARTESIAN_POINT('Ctrl Pts',(-6.60190166241576,1.48565926099896,47.2322953487382));
#59940=CARTESIAN_POINT('Ctrl Pts',(-6.64089680252307,1.31237451996926,47.2406489839935));
#59941=CARTESIAN_POINT('Ctrl Pts',(-6.67304825266115,1.1376289709083,47.2490026192488));
#59942=CARTESIAN_POINT('Ctrl Pts',(-6.69827255134879,0.96199471300386,47.2573562545041));
#59943=CARTESIAN_POINT('Ctrl Pts',(-6.72352306873745,0.786177896917976,
47.265718572715));
#59944=CARTESIAN_POINT('Ctrl Pts',(-6.74183200456947,0.609470866823461,
47.2740808909259));
#59945=CARTESIAN_POINT('Ctrl Pts',(-6.75316778180667,0.432451050141371,
47.2824432091368));
#59946=CARTESIAN_POINT('Ctrl Pts',(-6.76237532477453,0.288665799764858,
47.2892355448211));
#59947=CARTESIAN_POINT('Ctrl Pts',(-6.7669832534489,0.144674329426934,47.2960278805054));
#59948=CARTESIAN_POINT('Ctrl Pts',(-6.76699995441783,0.00078543557435644,
47.3028202161897));
#59949=CARTESIAN_POINT('Ctrl Pts',(-6.767,5.64341228108853E-12,47.3028202161897));
#59950=CARTESIAN_POINT('Ctrl Pts',(-6.76700000000016,-0.186007249554274,
47.3115697280025));
#59951=CARTESIAN_POINT('Ctrl Pts',(-6.75932637294278,-0.37201435581037,
47.3203192398152));
#59952=CARTESIAN_POINT('Ctrl Pts',(-6.7440051826341,-0.557389537580667,
47.3290687516279));
#59953=CARTESIAN_POINT('Ctrl Pts',(-6.72868405703791,-0.742763936377251,
47.3378182264851));
#59954=CARTESIAN_POINT('Ctrl Pts',(-6.70571545643638,-0.927506130399682,
47.3465677013423));
#59955=CARTESIAN_POINT('Ctrl Pts',(-6.6751773940166,-1.11098864009032,47.3553171761995));
#59956=CARTESIAN_POINT('Ctrl Pts',(-6.64463945804486,-1.29447039004045,
47.3640666148281));
#59957=CARTESIAN_POINT('Ctrl Pts',(-6.60653217002831,-1.476692183388,47.3728160534566));
#59958=CARTESIAN_POINT('Ctrl Pts',(-6.56098496085596,-1.65703510627323,
47.3815654920851));
#59959=CARTESIAN_POINT('Ctrl Pts',(-6.51543793649677,-1.83737729739583,
47.3903148952117));
#59960=CARTESIAN_POINT('Ctrl Pts',(-6.46245112157019,-2.01584035544561,
47.3990642983384));
#59961=CARTESIAN_POINT('Ctrl Pts',(-6.40220448361839,-2.19181813797052,
47.407813701465));
#59962=CARTESIAN_POINT('Ctrl Pts',(-6.34195808512107,-2.36779522105944,
47.4165630698166));
#59963=CARTESIAN_POINT('Ctrl Pts',(-6.274452014165,-2.54128677725383,47.4253124381681));
#59964=CARTESIAN_POINT('Ctrl Pts',(-6.19991555052883,-2.71170355428296,
47.4340618065196));
#59965=CARTESIAN_POINT('Ctrl Pts',(-6.12537937695283,-2.88211966813172,
47.4428111408228));
#59966=CARTESIAN_POINT('Ctrl Pts',(-6.04381298028515,-3.04946076419543,
47.451560475126));
#59967=CARTESIAN_POINT('Ctrl Pts',(-5.95549339309045,-3.21315848424194,
47.4603098094292));
#59968=CARTESIAN_POINT('Ctrl Pts',(-5.86717414225874,-3.3768555808497,47.4690591104107));
#59969=CARTESIAN_POINT('Ctrl Pts',(-5.77210188844132,-3.53690907699893,
47.4778084113923));
#59970=CARTESIAN_POINT('Ctrl Pts',(-5.67059953311438,-3.6927753702389,47.4865577123739));
#59971=CARTESIAN_POINT('Ctrl Pts',(-5.56909755592773,-3.84864108280932,
47.4953069807605));
#59972=CARTESIAN_POINT('Ctrl Pts',(-5.4611656815503,-4.00031938354741,47.5040562491471));
#59973=CARTESIAN_POINT('Ctrl Pts',(-5.3471704848844,-4.14729511918083,47.5128055175337));
#59974=CARTESIAN_POINT('Ctrl Pts',(-5.23317570343366,-4.29427031947104,
47.5215547540521));
#59975=CARTESIAN_POINT('Ctrl Pts',(-5.11311781951606,-4.43654276249488,
47.5303039905704));
#59976=CARTESIAN_POINT('Ctrl Pts',(-4.98740458929301,-4.57362924412321,
47.5390532270888));
#59977=CARTESIAN_POINT('Ctrl Pts',(-4.86169180652789,-4.71071523781218,
47.5478024324655));
#59978=CARTESIAN_POINT('Ctrl Pts',(-4.73032391141613,-4.8426150958445,47.5565516378422));
#59979=CARTESIAN_POINT('Ctrl Pts',(-4.59374706947358,-4.96888084599569,
47.5653008432189));
#59980=CARTESIAN_POINT('Ctrl Pts',(-4.45717070231569,-5.09514615720688,
47.5740500181806));
#59981=CARTESIAN_POINT('Ctrl Pts',(-4.31538563497455,-5.21577720520505,
47.5827991931423));
#59982=CARTESIAN_POINT('Ctrl Pts',(-4.16887340952167,-5.33036429293376,
47.591548368104));
#59983=CARTESIAN_POINT('Ctrl Pts',(-4.02236168122665,-5.44495099183572,
47.6002975133772));
#59984=CARTESIAN_POINT('Ctrl Pts',(-3.87112305263381,-5.55349359497788,
47.6090466586505));
#59985=CARTESIAN_POINT('Ctrl Pts',(-3.71567116929217,-5.65562346357066,
47.6177958039237));
#59986=CARTESIAN_POINT('Ctrl Pts',(-3.56021980053566,-5.75775299408769,
47.6265449202351));
#59987=CARTESIAN_POINT('Ctrl Pts',(-3.40055544442373,-5.8534696751971,47.6352940365465));
#59988=CARTESIAN_POINT('Ctrl Pts',(-3.23722035887168,-5.94244843041206,
47.6440431528578));
#59989=CARTESIAN_POINT('Ctrl Pts',(-3.07388580043826,-6.03142689847279,
47.6527922409338));
#59990=CARTESIAN_POINT('Ctrl Pts',(-2.9068807878957,-6.11366734707737,47.6615413290098));
#59991=CARTESIAN_POINT('Ctrl Pts',(-2.7367725061075,-6.18889047001271,47.6702904170858));
#59992=CARTESIAN_POINT('Ctrl Pts',(-2.5666647591727,-6.26411335643197,47.679039477653));
#59993=CARTESIAN_POINT('Ctrl Pts',(-2.39345402457405,-6.33231884545138,
47.6877885382202));
#59994=CARTESIAN_POINT('Ctrl Pts',(-2.21772855944354,-6.39327529804783,
47.6965375987874));
#59995=CARTESIAN_POINT('Ctrl Pts',(-2.04200363223889,-6.45423156404608,
47.7052866325722));
#59996=CARTESIAN_POINT('Ctrl Pts',(-1.8637642606134,-6.50793874412365,47.714035666357));
#59997=CARTESIAN_POINT('Ctrl Pts',(-1.68361577622003,-6.55421443943231,
47.7227847001418));
#59998=CARTESIAN_POINT('Ctrl Pts',(-1.50346782833515,-6.6004899969252,47.7315337078707));
#59999=CARTESIAN_POINT('Ctrl Pts',(-1.32141105657671,-6.63933404265106,
47.7402827155996));
#60000=CARTESIAN_POINT('Ctrl Pts',(-1.13806375346802,-6.67061465631484,
47.7490317233285));
#60001=CARTESIAN_POINT('Ctrl Pts',(-0.954716981172404,-6.70189517941738,
47.7577807057279));
#60002=CARTESIAN_POINT('Ctrl Pts',(-0.770079967444401,-6.7256122660898,
47.7665296881274));
#60003=CARTESIAN_POINT('Ctrl Pts',(-0.584779764074905,-6.74168536995969,
47.7752786705268));
#60004=CARTESIAN_POINT('Ctrl Pts',(-0.391489587594772,-6.75845153117862,
47.7844049009424));
#60005=CARTESIAN_POINT('Ctrl Pts',(-0.197478091807028,-6.76689985146389,
47.7935311313581));
#60006=CARTESIAN_POINT('Ctrl Pts',(-0.00346214753279914,-6.76699911434415,
47.8026573617737));
#60007=CARTESIAN_POINT('Ctrl Pts',(0.184490798482945,-6.7670952752594,47.8114983974888));
#60008=CARTESIAN_POINT('Ctrl Pts',(0.37244760215316,-6.75935633790772,47.8203394332039));
#60009=CARTESIAN_POINT('Ctrl Pts',(0.559756448192672,-6.74380914014526,
47.8291804689191));
#60010=CARTESIAN_POINT('Ctrl Pts',(0.745136131041901,-6.72842206873171,
47.8379304475324));
#60011=CARTESIAN_POINT('Ctrl Pts',(0.929880851943675,-6.70538686355743,
47.8466804261457));
#60012=CARTESIAN_POINT('Ctrl Pts',(1.11336305057335,-6.67478177303334,47.855430404759));
#60013=CARTESIAN_POINT('Ctrl Pts',(1.29684337090001,-6.64417699581285,47.864180293799));
#60014=CARTESIAN_POINT('Ctrl Pts',(1.47906091205074,-6.60600253548086,47.8729301828389));
#60015=CARTESIAN_POINT('Ctrl Pts',(1.65939671095111,-6.5603880644124,47.8816800718789));
#60016=CARTESIAN_POINT('Ctrl Pts',(1.83973072369048,-6.51477404513881,47.8904298742544));
#60017=CARTESIAN_POINT('Ctrl Pts',(2.01818275356923,-6.46172023288696,47.8991796766299));
#60018=CARTESIAN_POINT('Ctrl Pts',(2.19414664033212,-6.40140683918147,47.9079294790054));
#60019=CARTESIAN_POINT('Ctrl Pts',(2.37010884271147,-6.34109402281539,47.9166791976249));
#60020=CARTESIAN_POINT('Ctrl Pts',(2.54358267847696,-6.27352185699836,47.9254289162445));
#60021=CARTESIAN_POINT('Ctrl Pts',(2.71397890841634,-6.19891986435309,47.934178634864));
#60022=CARTESIAN_POINT('Ctrl Pts',(2.88437356388842,-6.1243185610329,47.9429282726358));
#60023=CARTESIAN_POINT('Ctrl Pts',(3.0516904078708,-6.04268767582604,47.9516779104077));
#60024=CARTESIAN_POINT('Ctrl Pts',(3.2153611251197,-5.95430447953991,47.9604275481795));
#60025=CARTESIAN_POINT('Ctrl Pts',(3.37903038442761,-5.8659220705509,47.9691771080116));
#60026=CARTESIAN_POINT('Ctrl Pts',(3.53905332979894,-5.77078760703426,47.9779266678436));
#60027=CARTESIAN_POINT('Ctrl Pts',(3.69488643041815,-5.66922422085349,47.9866762276757));
#60028=CARTESIAN_POINT('Ctrl Pts',(3.85071819468668,-5.5676617056321,47.9954257124757));
#60029=CARTESIAN_POINT('Ctrl Pts',(4.00235994599152,-5.45967053456304,48.0041751972757));
#60030=CARTESIAN_POINT('Ctrl Pts',(4.14929662974231,-5.34561750206738,48.0129246820757));
#60031=CARTESIAN_POINT('Ctrl Pts',(4.29623210224982,-5.23156540974517,48.0216740947511));
#60032=CARTESIAN_POINT('Ctrl Pts',(4.43846235842062,-5.11145173172234,48.0304235074264));
#60033=CARTESIAN_POINT('Ctrl Pts',(4.5755043179738,-4.98568443006606,48.0391729201018));
#60034=CARTESIAN_POINT('Ctrl Pts',(4.71254519337456,-4.85991812336727,48.0479222635597));
#60035=CARTESIAN_POINT('Ctrl Pts',(4.84439764314955,-4.72849847631131,48.0566716070176));
#60036=CARTESIAN_POINT('Ctrl Pts',(4.97061384196666,-4.59187184425365,48.0654209504755));
#60037=CARTESIAN_POINT('Ctrl Pts',(5.09682908420178,-4.45524624767779,48.0741702276228));
#60038=CARTESIAN_POINT('Ctrl Pts',(5.21740796650135,-4.31341395556935,48.0829195047702));
#60039=CARTESIAN_POINT('Ctrl Pts',(5.33194095942208,-4.16685668162911,48.0916687819175));
#60040=CARTESIAN_POINT('Ctrl Pts',(5.44647312235095,-4.02030046975266,48.1004179956611));
#60041=CARTESIAN_POINT('Ctrl Pts',(5.55495930712255,-3.86901957035595,48.1091672094046));
#60042=CARTESIAN_POINT('Ctrl Pts',(5.65703106079766,-3.71352778058419,48.1179164231482));
#60043=CARTESIAN_POINT('Ctrl Pts',(5.75910210868704,-3.55803706597654,48.1266655763944));
#60044=CARTESIAN_POINT('Ctrl Pts',(5.85475865698516,-3.39833575880957,48.1354147296405));
#60045=CARTESIAN_POINT('Ctrl Pts',(5.94367583069028,-3.23496624706785,48.1441638828867));
#60046=CARTESIAN_POINT('Ctrl Pts',(6.03259241910048,-3.07159781070158,48.1529129785419));
#60047=CARTESIAN_POINT('Ctrl Pts',(6.11476958470943,-2.90456146975886,48.161662074197));
#60048=CARTESIAN_POINT('Ctrl Pts',(6.18992823574365,-2.73442451648303,48.1704111698521));
#60049=CARTESIAN_POINT('Ctrl Pts',(6.26508641700917,-2.56428862662459,48.1791602108222));
#60050=CARTESIAN_POINT('Ctrl Pts',(6.33322605570282,-2.39105242531317,48.1879092517924));
#60051=CARTESIAN_POINT('Ctrl Pts',(6.39411573747755,-2.21530425353765,48.1966582927625));
#60052=CARTESIAN_POINT('Ctrl Pts',(6.45500505889119,-2.03955712188583,48.2054072819535));
#60053=CARTESIAN_POINT('Ctrl Pts',(6.50864441544928,-1.86129832025579,48.2141562711445));
#60054=CARTESIAN_POINT('Ctrl Pts',(6.55485164049909,-1.681133240123,48.2229052603355));
#60055=CARTESIAN_POINT('Ctrl Pts',(6.60199852639114,-1.4973043591288,48.2318321672124));
#60056=CARTESIAN_POINT('Ctrl Pts',(6.64140767441016,-1.31149113173623,48.2407590740893));
#60057=CARTESIAN_POINT('Ctrl Pts',(6.67293975269609,-1.12435050446393,48.2496859809661));
#60058=CARTESIAN_POINT('Ctrl Pts',(6.70384664831511,-0.940920291563414,
48.2584358951501));
#60059=CARTESIAN_POINT('Ctrl Pts',(6.72718585889669,-0.756215114277657,
48.2671858093341));
#60060=CARTESIAN_POINT('Ctrl Pts',(6.74287810451866,-0.570862389374904,
48.2759357235181));
#60061=CARTESIAN_POINT('Ctrl Pts',(6.75857004154125,-0.385513309567886,
48.2846854656287));
#60062=CARTESIAN_POINT('Ctrl Pts',(6.76661529035556,-0.199516993259019,
48.2934352077393));
#60063=CARTESIAN_POINT('Ctrl Pts',(6.76698652348896,-0.013505218204885,
48.3021849498499));
#60064=CARTESIAN_POINT('Ctrl Pts',(6.76735774981523,0.172503146038051,48.3109345315205));
#60065=CARTESIAN_POINT('Ctrl Pts',(6.76005524147484,0.358526681832619,48.3196841131912));
#60066=CARTESIAN_POINT('Ctrl Pts',(6.74510380214888,0.543933542114002,48.3284336948618));
#60067=CARTESIAN_POINT('Ctrl Pts',(6.73015261710988,0.729337249083888,48.3371831277237));
#60068=CARTESIAN_POINT('Ctrl Pts',(6.70755278444616,0.914124015853858,48.3459325605857));
#60069=CARTESIAN_POINT('Ctrl Pts',(6.67738106408302,1.09766621749308,48.3546819934476));
#60070=CARTESIAN_POINT('Ctrl Pts',(6.64720981677269,1.28120554143241,48.36343128913));
#60071=CARTESIAN_POINT('Ctrl Pts',(6.60946696581541,1.46350005650536,48.3721805848123));
#60072=CARTESIAN_POINT('Ctrl Pts',(6.56428070011016,1.64393062206447,48.3809298804946));
#60073=CARTESIAN_POINT('Ctrl Pts',(6.51909508282766,1.82435859844559,48.3896790506246));
#60074=CARTESIAN_POINT('Ctrl Pts',(6.46646633415692,2.00292240086464,48.3984282207546));
#60075=CARTESIAN_POINT('Ctrl Pts',(6.40657319597228,2.1790155769635,48.4071773908846));
#60076=CARTESIAN_POINT('Ctrl Pts',(6.34668083768332,2.35510646007335,48.4159264470877));
#60077=CARTESIAN_POINT('Ctrl Pts',(6.27952437143923,2.52872650996436,48.4246755032908));
#60078=CARTESIAN_POINT('Ctrl Pts',(6.20533187335175,2.69928607997835,48.4334245594938));
#60079=CARTESIAN_POINT('Ctrl Pts',(6.12831449784293,2.8763397011531,48.4425067357827));
#60080=CARTESIAN_POINT('Ctrl Pts',(6.04371489463196,3.05009490562264,48.4515889120715));
#60081=CARTESIAN_POINT('Ctrl Pts',(5.95184265120535,3.21991584599549,48.4606710883604));
#60082=CARTESIAN_POINT('Ctrl Pts',(5.86333281335533,3.3835215590523,48.4694208687148));
#60083=CARTESIAN_POINT('Ctrl Pts',(5.76807337235722,3.54347560903765,48.4781706490692));
#60084=CARTESIAN_POINT('Ctrl Pts',(5.66638790086387,3.69923467178598,48.4869204294236));
#60085=CARTESIAN_POINT('Ctrl Pts',(5.56470608502771,3.85498813489724,48.4956698952179));
#60086=CARTESIAN_POINT('Ctrl Pts',(5.45659885766975,4.0065466725623,48.5044193610122));
#60087=CARTESIAN_POINT('Ctrl Pts',(5.34243340580525,4.15339551506188,48.5131688268064));
#60088=CARTESIAN_POINT('Ctrl Pts',(5.22827145140607,4.30023985883855,48.5219180245603));
#60089=CARTESIAN_POINT('Ctrl Pts',(5.10805181978097,4.44237456993034,48.5306672223142));
#60090=CARTESIAN_POINT('Ctrl Pts',(4.98218281282554,4.57931691626446,48.5394164200681));
#60091=CARTESIAN_POINT('Ctrl Pts',(4.8563169929621,4.71625579512182,48.5481653962861));
#60092=CARTESIAN_POINT('Ctrl Pts',(4.72480227791796,4.84800236135812,48.5569143725041));
#60093=CARTESIAN_POINT('Ctrl Pts',(4.58808530848046,4.97410918678971,48.5656633487221));
#60094=CARTESIAN_POINT('Ctrl Pts',(4.45135945056897,5.10022421089073,48.5744128937433));
#60095=CARTESIAN_POINT('Ctrl Pts',(4.3094308720796,5.22069856612052,48.5831624387645));
#60096=CARTESIAN_POINT('Ctrl Pts',(4.16278164322382,5.33512305301751,48.5919119837857));
#60097=CARTESIAN_POINT('Ctrl Pts',(4.0161410353432,5.44954081331478,48.600661014453));
#60098=CARTESIAN_POINT('Ctrl Pts',(3.8647805583336,5.55790924068374,48.6094100451202));
#60099=CARTESIAN_POINT('Ctrl Pts',(3.70921425811917,5.65986029751314,48.6181590757875));
#60100=CARTESIAN_POINT('Ctrl Pts',(3.55364584530089,5.76181273884673,48.6269082252673));
#60101=CARTESIAN_POINT('Ctrl Pts',(3.39387173464318,5.85734747818079,48.6356573747471));
#60102=CARTESIAN_POINT('Ctrl Pts',(3.23043456092383,5.9461400544882,48.644406524227));
#60103=CARTESIAN_POINT('Ctrl Pts',(3.18690768806381,5.96978744811287,48.64673661296));
#60104=CARTESIAN_POINT('Ctrl Pts',(3.14312114982882,5.992956884993,48.6490667016931));
#60105=CARTESIAN_POINT('Ctrl Pts',(3.09908550384732,6.01564277861007,48.6513967904261));
#60106=CARTESIAN_POINT('Origin',(0.,0.,-63.6971797838103));
#60107=CARTESIAN_POINT('',(3.0990855038473,6.01564277861008,51.0457613895064));
#60108=CARTESIAN_POINT('',(3.09908550384729,6.01564277861008,50.6513967904261));
#60109=CARTESIAN_POINT('',(3.09908550384721,6.01564277861012,-63.6971797838103));
#60110=CARTESIAN_POINT('',(-6.76800097367046,-0.00217352041212573,49.6954478291652));
#60111=CARTESIAN_POINT('Ctrl Pts',(-6.76699845293094,-0.00457580925307041,
49.6971797838098));
#60112=CARTESIAN_POINT('Ctrl Pts',(-6.7668662394862,-0.200101480569433,
49.7063448954362));
#60113=CARTESIAN_POINT('Ctrl Pts',(-6.75825574679544,-0.39532739586738,
49.7155100070625));
#60114=CARTESIAN_POINT('Ctrl Pts',(-6.74126887845904,-0.589561623852473,
49.7246751186889));
#60115=CARTESIAN_POINT('Ctrl Pts',(-6.72359310938338,-0.791673001445151,
49.7342119204967));
#60116=CARTESIAN_POINT('Ctrl Pts',(-6.69684755273203,-0.992710310089097,
49.7437487223045));
#60117=CARTESIAN_POINT('Ctrl Pts',(-6.66120365726185,-1.19191226039562,
49.7532855241123));
#60118=CARTESIAN_POINT('Ctrl Pts',(-6.62664155718862,-1.3850684137974,49.7625328831373));
#60119=CARTESIAN_POINT('Ctrl Pts',(-6.58371344390243,-1.57649885085553,
49.7717802421623));
#60120=CARTESIAN_POINT('Ctrl Pts',(-6.53262555518545,-1.76552891670967,
49.7810276011872));
#60121=CARTESIAN_POINT('Ctrl Pts',(-6.47913908640227,-1.96343395781248,
49.7907091243865));
#60122=CARTESIAN_POINT('Ctrl Pts',(-6.41670838137096,-2.15870756645148,
49.8003906475858));
#60123=CARTESIAN_POINT('Ctrl Pts',(-6.34562561425132,-2.35060089418804,
49.810072170785));
#60124=CARTESIAN_POINT('Ctrl Pts',(-6.27454284713163,-2.54249422192472,
49.8197536939843));
#60125=CARTESIAN_POINT('Ctrl Pts',(-6.19480817045469,-2.73100707998284,
49.8294352171836));
#60126=CARTESIAN_POINT('Ctrl Pts',(-6.10676825880042,-2.91541942665334,
49.8391167403829));
#60127=CARTESIAN_POINT('Ctrl Pts',(-6.03337004509734,-3.0691626162599,49.8471881536249));
#60128=CARTESIAN_POINT('Ctrl Pts',(-5.95402701160415,-3.22041501290717,
49.8552595668669));
#60129=CARTESIAN_POINT('Ctrl Pts',(-5.86893009352057,-3.36867163097988,
49.8633309801089));
#60130=CARTESIAN_POINT('Ctrl Pts',(-5.7839400075693,-3.51674212514829,49.8713922603602));
#60131=CARTESIAN_POINT('Ctrl Pts',(-5.69321059329911,-3.66182400471009,
49.8794535406114));
#60132=CARTESIAN_POINT('Ctrl Pts',(-5.59698095479664,-3.80343176508317,
49.8875148208626));
#60133=CARTESIAN_POINT('Ctrl Pts',(-5.50085102103002,-3.94489280387898,
49.8955677487202));
#60134=CARTESIAN_POINT('Ctrl Pts',(-5.39923241176125,-4.08288658088965,
49.9036206765778));
#60135=CARTESIAN_POINT('Ctrl Pts',(-5.29241024442235,-4.21695183808558,
49.9116736044354));
#60136=CARTESIAN_POINT('Ctrl Pts',(-5.18567536526842,-4.35090754580073,
49.9197199519598));
#60137=CARTESIAN_POINT('Ctrl Pts',(-5.07374562223461,-4.4809408327538,49.9277662994843));
#60138=CARTESIAN_POINT('Ctrl Pts',(-4.95694951160859,-4.60661920928607,
49.9358126470086));
#60139=CARTESIAN_POINT('Ctrl Pts',(-4.84022329027853,-4.73222238148827,
49.9438541797018));
#60140=CARTESIAN_POINT('Ctrl Pts',(-4.7186367515078,-4.85347555839493,49.9518957123949));
#60141=CARTESIAN_POINT('Ctrl Pts',(-4.5925586848118,-4.96997924810152,49.959937245088));
#60142=CARTESIAN_POINT('Ctrl Pts',(-4.46405680037926,-5.08872269066031,
49.9681333741363));
#60143=CARTESIAN_POINT('Ctrl Pts',(-4.33088918138524,-5.20253186350212,
49.9763295031845));
#60144=CARTESIAN_POINT('Ctrl Pts',(-4.19348610198228,-5.31102281227274,
49.9845256322328));
#60145=CARTESIAN_POINT('Ctrl Pts',(-4.05872127124951,-5.41743064833173,
49.9925643890689));
#60146=CARTESIAN_POINT('Ctrl Pts',(-3.91988247186705,-5.51872241528514,
50.000603145905));
#60147=CARTESIAN_POINT('Ctrl Pts',(-3.77740905344398,-5.6145765506367,50.0086419027411));
#60148=CARTESIAN_POINT('Ctrl Pts',(-3.63492184509992,-5.7104399636554,50.0166814376439));
#60149=CARTESIAN_POINT('Ctrl Pts',(-3.48879962705872,-5.80086448852888,
50.0247209725467));
#60150=CARTESIAN_POINT('Ctrl Pts',(-3.33951041435837,-5.88557212107642,
50.0327605074495));
#60151=CARTESIAN_POINT('Ctrl Pts',(-3.19017719272408,-5.9703047245682,50.040802412325));
#60152=CARTESIAN_POINT('Ctrl Pts',(-3.03767544277751,-6.04931689701847,
50.0488443172005));
#60153=CARTESIAN_POINT('Ctrl Pts',(-2.88249729151362,-6.12237685579846,
50.056886222076));
#60154=CARTESIAN_POINT('Ctrl Pts',(-2.72208462704745,-6.19790129373147,
50.0651993987568));
#60155=CARTESIAN_POINT('Ctrl Pts',(-2.55881223557885,-6.26706474429625,
50.0735125754377));
#60156=CARTESIAN_POINT('Ctrl Pts',(-2.39324451917611,-6.3296658420041,50.0818257521185));
#60157=CARTESIAN_POINT('Ctrl Pts',(-2.23280144727658,-6.3903293133544,50.089881619729));
#60158=CARTESIAN_POINT('Ctrl Pts',(-2.07020339565959,-6.44483056700669,
50.0979374873396));
#60159=CARTESIAN_POINT('Ctrl Pts',(-1.90597732370652,-6.49303776683276,
50.1059933549501));
#60160=CARTESIAN_POINT('Ctrl Pts',(-1.73388303818443,-6.54355461542096,
50.1144351861661));
#60161=CARTESIAN_POINT('Ctrl Pts',(-1.56000136607515,-6.58715934738382,
50.1228770173821));
#60162=CARTESIAN_POINT('Ctrl Pts',(-1.38494751372303,-6.6237609697386,50.1313188485981));
#60163=CARTESIAN_POINT('Ctrl Pts',(-1.20989366137104,-6.66036259209335,
50.1397606798141));
#60164=CARTESIAN_POINT('Ctrl Pts',(-1.0336680976857,-6.68996111286377,50.1482025110301));
#60165=CARTESIAN_POINT('Ctrl Pts',(-0.856888108185714,-6.71252797164004,
50.1566443422461));
#60166=CARTESIAN_POINT('Ctrl Pts',(-0.68453451572473,-6.73452977847151,
50.1648747983126));
#60167=CARTESIAN_POINT('Ctrl Pts',(-0.511080729655507,-6.74992139281732,
50.1731052543792));
#60168=CARTESIAN_POINT('Ctrl Pts',(-0.337074956830591,-6.75859966808788,
50.1813357104457));
#60169=CARTESIAN_POINT('Ctrl Pts',(-0.163275739111443,-6.76726764173433,
50.1895563964759));
#60170=CARTESIAN_POINT('Ctrl Pts',(0.011073806073178,-6.76923812693641,
50.1977770825062));
#60171=CARTESIAN_POINT('Ctrl Pts',(0.185417177203249,-6.76445928884179,
50.2059977685364));
#60172=CARTESIAN_POINT('Ctrl Pts',(0.359588571151644,-6.75968516472684,
50.2142103454518));
#60173=CARTESIAN_POINT('Ctrl Pts',(0.533753447251468,-6.74817498584979,
50.2224229223672));
#60174=CARTESIAN_POINT('Ctrl Pts',(0.707352007490277,-6.72992883599073,
50.2306354992826));
#60175=CARTESIAN_POINT('Ctrl Pts',(0.880814141978052,-6.71169702521774,
50.2388416221872));
#60176=CARTESIAN_POINT('Ctrl Pts',(1.05371049209146,-6.68673982442808,50.2470477450919));
#60177=CARTESIAN_POINT('Ctrl Pts',(1.22548299758562,-6.65510934715791,50.2552538679965));
#60178=CARTESIAN_POINT('Ctrl Pts',(1.39715495401562,-6.62349738516106,50.2634551873502));
#60179=CARTESIAN_POINT('Ctrl Pts',(1.56770402470165,-6.58521999320251,50.2716565067039));
#60180=CARTESIAN_POINT('Ctrl Pts',(1.73657890814165,-6.54038092895189,50.2798578260577));
#60181=CARTESIAN_POINT('Ctrl Pts',(1.90540534537897,-6.49555472796637,50.2880567926472));
#60182=CARTESIAN_POINT('Ctrl Pts',(2.07255820494615,-6.44417069224509,50.2962557592367));
#60183=CARTESIAN_POINT('Ctrl Pts',(2.23749774457196,-6.38638339305083,50.3044547258262));
#60184=CARTESIAN_POINT('Ctrl Pts',(2.40241550318638,-6.32860372493051,50.3126526097052));
#60185=CARTESIAN_POINT('Ctrl Pts',(2.56512018536469,-6.26442259518839,50.320850493584));
#60186=CARTESIAN_POINT('Ctrl Pts',(2.72508853892699,-6.19404403076123,50.329048377463));
#60187=CARTESIAN_POINT('Ctrl Pts',(2.8850648266572,-6.12366197567272,50.3372466679435));
#60188=CARTESIAN_POINT('Ctrl Pts',(3.04230418709739,-6.04708201790509,50.3454449584241));
#60189=CARTESIAN_POINT('Ctrl Pts',(3.1963045860293,-5.96455580855172,50.3536432489046));
#60190=CARTESIAN_POINT('Ctrl Pts',(3.35034059766838,-5.88201051495085,50.3618434352459));
#60191=CARTESIAN_POINT('Ctrl Pts',(3.50113583996505,-5.79351640037113,50.3700436215872));
#60192=CARTESIAN_POINT('Ctrl Pts',(3.64821401811469,-5.69937044576254,50.3782438079286));
#60193=CARTESIAN_POINT('Ctrl Pts',(3.79543124714156,-5.60513548354085,50.3864517469027));
#60194=CARTESIAN_POINT('Ctrl Pts',(3.93892408863219,-5.50523819941379,50.3946596858767));
#60195=CARTESIAN_POINT('Ctrl Pts',(4.07824555221077,-5.40001872365949,50.4028676248508));
#60196=CARTESIAN_POINT('Ctrl Pts',(4.21763460485237,-5.29474820274966,50.4110795457448));
#60197=CARTESIAN_POINT('Ctrl Pts',(4.35284796746005,-5.18415056929953,50.4192914666388));
#60198=CARTESIAN_POINT('Ctrl Pts',(4.48347284046371,-5.06860535934929,50.4275033875327));
#60199=CARTESIAN_POINT('Ctrl Pts',(4.61427684478724,-4.95290169744814,50.4357265697753));
#60200=CARTESIAN_POINT('Ctrl Pts',(4.74047952508958,-4.83223714764187,50.4439497520178));
#60201=CARTESIAN_POINT('Ctrl Pts',(4.86170511249005,-4.70702797943545,50.4521729342604));
#60202=CARTESIAN_POINT('Ctrl Pts',(4.96980774285222,-4.59537300032729,50.4595059375432));
#60203=CARTESIAN_POINT('Ctrl Pts',(5.07395295370794,-4.48010469957471,50.466838940826));
#60204=CARTESIAN_POINT('Ctrl Pts',(5.17390238428699,-4.36153907673305,50.4741719441088));
#60205=CARTESIAN_POINT('Ctrl Pts',(5.29568970614727,-4.21706812190195,50.4831071308911));
#60206=CARTESIAN_POINT('Ctrl Pts',(5.41149997648915,-4.06740161523908,50.4920423176734));
#60207=CARTESIAN_POINT('Ctrl Pts',(5.52090884644196,-3.91303648197649,50.5009775044556));
#60208=CARTESIAN_POINT('Ctrl Pts',(5.63015385575383,-3.7589025399298,50.5098993090923));
#60209=CARTESIAN_POINT('Ctrl Pts',(5.73301644565672,-3.60008422298872,50.5188211137288));
#60210=CARTESIAN_POINT('Ctrl Pts',(5.82911312558786,-3.43711058435707,50.5277429183655));
#60211=CARTESIAN_POINT('Ctrl Pts',(5.92497540292707,-3.27453447707966,50.5366429606048));
#60212=CARTESIAN_POINT('Ctrl Pts',(6.01410457781343,-3.10782349959165,50.5455430028441));
#60213=CARTESIAN_POINT('Ctrl Pts',(6.09616127880189,-2.93753411262517,50.5544430450834));
#60214=CARTESIAN_POINT('Ctrl Pts',(6.17809165229264,-2.7675068886738,50.5633293855768));
#60215=CARTESIAN_POINT('Ctrl Pts',(6.25297115939355,-2.59391247586209,50.5722157260702));
#60216=CARTESIAN_POINT('Ctrl Pts',(6.32050557821505,-2.41733287648855,50.5811020665635));
#60217=CARTESIAN_POINT('Ctrl Pts',(6.38786732331621,-2.24120476032747,50.5899656862355));
#60218=CARTESIAN_POINT('Ctrl Pts',(6.44792136267434,-2.06210692854757,50.5988293059074));
#60219=CARTESIAN_POINT('Ctrl Pts',(6.50042121744808,-1.88064164469226,50.6076929255793));
#60220=CARTESIAN_POINT('Ctrl Pts',(6.55025956057991,-1.70837585229585,50.6161071987331));
#60221=CARTESIAN_POINT('Ctrl Pts',(6.59329047212807,-1.53397690997897,50.6245214718868));
#60222=CARTESIAN_POINT('Ctrl Pts',(6.62934272568025,-1.35797791788763,50.6329357450406));
#60223=CARTESIAN_POINT('Ctrl Pts',(6.66452080281028,-1.18624645844818,50.6411459932451));
#60224=CARTESIAN_POINT('Ctrl Pts',(6.69301974338952,-1.01315644319117,50.6493562414497));
#60225=CARTESIAN_POINT('Ctrl Pts',(6.71475402192053,-0.839266003780745,
50.6575664896542));
#60226=CARTESIAN_POINT('Ctrl Pts',(6.73649346712284,-0.665334227146208,
50.6657786895984));
#60227=CARTESIAN_POINT('Ctrl Pts',(6.75146500234347,-0.490602000479054,
50.6739908895426));
#60228=CARTESIAN_POINT('Ctrl Pts',(6.75963497474576,-0.315632710906001,
50.6822030894868));
#60229=CARTESIAN_POINT('Ctrl Pts',(6.76780834415645,-0.140590670518497,
50.6904187039973));
#60230=CARTESIAN_POINT('Ctrl Pts',(6.76917450009466,0.0346882738773664,
50.6986343185078));
#60231=CARTESIAN_POINT('Ctrl Pts',(6.76375190681956,0.209640508954743,50.7068499330183));
#60232=CARTESIAN_POINT('Ctrl Pts',(6.75832322420992,0.384789207722648,50.7150747733037));
#60233=CARTESIAN_POINT('Ctrl Pts',(6.74609057688584,0.559610108482023,50.7232996135891));
#60234=CARTESIAN_POINT('Ctrl Pts',(6.72712441626983,0.733543514746242,50.7315244538745));
#60235=CARTESIAN_POINT('Ctrl Pts',(6.70814610716865,0.907588331403449,50.7397545624561));
#60236=CARTESIAN_POINT('Ctrl Pts',(6.6824257390876,1.08074416917431,50.7479846710376));
#60237=CARTESIAN_POINT('Ctrl Pts',(6.65008492957727,1.25246134846922,50.7562147796191));
#60238=CARTESIAN_POINT('Ctrl Pts',(6.61769978032081,1.424413954652,50.7644561718058));
#60239=CARTESIAN_POINT('Ctrl Pts',(6.57867613900747,1.59492361669999,50.7726975639925));
#60240=CARTESIAN_POINT('Ctrl Pts',(6.53318579632867,1.76345466362177,50.7809389561792));
#60241=CARTESIAN_POINT('Ctrl Pts',(6.5133872434463,1.83680365701936,50.7845258194435));
#60242=CARTESIAN_POINT('Ctrl Pts',(6.49236438504947,1.90977809710686,50.7881126827077));
#60243=CARTESIAN_POINT('Ctrl Pts',(6.47013422086513,1.98233502819023,50.791699545972));
#60244=CARTESIAN_POINT('Ctrl Pts',(6.4177676139473,2.15325415670859,50.8001489598886));
#60245=CARTESIAN_POINT('Ctrl Pts',(6.35857887499528,2.32224495408212,50.8085983738051));
#60246=CARTESIAN_POINT('Ctrl Pts',(6.29272948473869,2.48874358500435,50.8170477877217));
#60247=CARTESIAN_POINT('Ctrl Pts',(6.22694159651133,2.65508670949554,50.8254893100526));
#60248=CARTESIAN_POINT('Ctrl Pts',(6.15450558008233,2.81894199877421,50.8339308323836));
#60249=CARTESIAN_POINT('Ctrl Pts',(6.07563244337218,2.97976163695074,50.8423723547145));
#60250=CARTESIAN_POINT('Ctrl Pts',(5.99645077784254,3.14121035487719,50.8508468978308));
#60251=CARTESIAN_POINT('Ctrl Pts',(5.91078161542371,3.29959929415626,50.8593214409472));
#60252=CARTESIAN_POINT('Ctrl Pts',(5.81888763225979,3.4543936838661,50.8677959840635));
#60253=CARTESIAN_POINT('Ctrl Pts',(5.72748898892862,3.60835367915241,50.8762248465093));
#60254=CARTESIAN_POINT('Ctrl Pts',(5.62993263870237,3.7587574908774,50.8846537089551));
#60255=CARTESIAN_POINT('Ctrl Pts',(5.52652345996922,3.90510274466753,50.8930825714009));
#60256=CARTESIAN_POINT('Ctrl Pts',(5.4231575139961,4.05138681521149,50.9015079099526));
#60257=CARTESIAN_POINT('Ctrl Pts',(5.31394380953577,4.19361543853159,50.9099332485044));
#60258=CARTESIAN_POINT('Ctrl Pts',(5.19923068858017,4.33131495586804,50.9183585870561));
#60259=CARTESIAN_POINT('Ctrl Pts',(5.08454951973867,4.4689761184753,50.9267815788198));
#60260=CARTESIAN_POINT('Ctrl Pts',(4.96437220194532,4.60211043464504,50.9352045705836));
#60261=CARTESIAN_POINT('Ctrl Pts',(4.83908775559834,4.73027680940748,50.9436275623473));
#60262=CARTESIAN_POINT('Ctrl Pts',(4.71249200090834,4.85978465664652,50.9521387146105));
#60263=CARTESIAN_POINT('Ctrl Pts',(4.58068181891687,4.98421970695032,50.9606498668738));
#60264=CARTESIAN_POINT('Ctrl Pts',(4.44409769073168,5.10316418658398,50.9691610191371));
#60265=CARTESIAN_POINT('Ctrl Pts',(4.30892535712618,5.22087920292743,50.9775841963274));
#60266=CARTESIAN_POINT('Ctrl Pts',(4.16907757488618,5.33321641597437,50.9860073735178));
#60267=CARTESIAN_POINT('Ctrl Pts',(4.02501557564025,5.43981053124586,50.9944305507081));
#60268=CARTESIAN_POINT('Ctrl Pts',(3.87869661362397,5.54807461466279,51.0029856905079));
#60269=CARTESIAN_POINT('Ctrl Pts',(3.72803056266511,5.65041392478799,51.0115408303076));
#60270=CARTESIAN_POINT('Ctrl Pts',(3.57353246629222,5.74649064319742,51.0200959701073));
#60271=CARTESIAN_POINT('Ctrl Pts',(3.41903436991944,5.84256736160677,51.028651109907));
#60272=CARTESIAN_POINT('Ctrl Pts',(3.26070454339456,5.93238131494943,51.0372062497067));
#60273=CARTESIAN_POINT('Ctrl Pts',(3.0990855038473,6.01564277861008,51.0457613895064));
#60274=CARTESIAN_POINT('Ctrl Pts',(3.09908550384708,6.01564277861019,49.0457563580462));
#60275=CARTESIAN_POINT('Ctrl Pts',(2.93373232018321,6.10082796552484,49.0545058059455));
#60276=CARTESIAN_POINT('Ctrl Pts',(2.76486502144422,6.17919158180192,49.0632552538448));
#60277=CARTESIAN_POINT('Ctrl Pts',(2.59305716434353,6.25046746591379,49.0720047017441));
#60278=CARTESIAN_POINT('Ctrl Pts',(2.42125069459282,6.32174277447225,49.0807540789915));
#60279=CARTESIAN_POINT('Ctrl Pts',(2.24650397871055,6.38593035557827,49.0895034562389));
#60280=CARTESIAN_POINT('Ctrl Pts',(2.06941053323766,6.4428122000354,49.0982528334864));
#60281=CARTESIAN_POINT('Ctrl Pts',(1.89231845896677,6.49969360406687,49.107002142989));
#60282=CARTESIAN_POINT('Ctrl Pts',(1.71287996431498,6.54926929700883,49.1157514524915));
#60283=CARTESIAN_POINT('Ctrl Pts',(1.53170449173496,6.59137090065481,49.1245007619941));
#60284=CARTESIAN_POINT('Ctrl Pts',(1.35053036178162,6.63347219230085,49.1332500066587));
#60285=CARTESIAN_POINT('Ctrl Pts',(1.16761955878835,6.66809944062456,49.1419992513233));
#60286=CARTESIAN_POINT('Ctrl Pts',(0.98359330931039,6.69513503985393,49.1507484959879));
#60287=CARTESIAN_POINT('Ctrl Pts',(0.799568362459827,6.72217044771216,49.1594976787211));
#60288=CARTESIAN_POINT('Ctrl Pts',(0.614428268438384,6.74161427235979,49.1682468614543));
#60289=CARTESIAN_POINT('Ctrl Pts',(0.42880181633,6.75340047696804,49.1769960441874));
#60290=CARTESIAN_POINT('Ctrl Pts',(0.243176616522559,6.76518660206243,49.1857451678956));
#60291=CARTESIAN_POINT('Ctrl Pts',(0.0570653511652789,6.76931519233997,
49.1944942916037));
#60292=CARTESIAN_POINT('Ctrl Pts',(-0.128899900800167,6.76577222610795,
49.2032434153118));
#60293=CARTESIAN_POINT('Ctrl Pts',(-0.314863959942176,6.76222928260132,
49.2119924829011));
#60294=CARTESIAN_POINT('Ctrl Pts',(-0.500681721080852,6.75101488651275,
49.2207415504904));
#60295=CARTESIAN_POINT('Ctrl Pts',(-0.685722110173486,6.73216712415989,
49.2294906180796));
#60296=CARTESIAN_POINT('Ctrl Pts',(-0.870761373827704,6.71331947644144,
49.238239632456));
#60297=CARTESIAN_POINT('Ctrl Pts',(-1.05502298984343,6.68683858439996,49.2469886468323));
#60298=CARTESIAN_POINT('Ctrl Pts',(-1.2378811767605,6.65281438131428,49.2557376612087));
#60299=CARTESIAN_POINT('Ctrl Pts',(-1.43009641451775,6.61704912302381,49.2649343720962));
#60300=CARTESIAN_POINT('Ctrl Pts',(-1.62076048992669,6.57294837083171,49.2741310829837));
#60301=CARTESIAN_POINT('Ctrl Pts',(-1.80915798961097,6.52067760042059,49.2833277938713));
#60302=CARTESIAN_POINT('Ctrl Pts',(-1.9884044300298,6.47094578577419,49.2920777915778));
#60303=CARTESIAN_POINT('Ctrl Pts',(-2.16559895952163,6.41381888474485,49.3008277892843));
#60304=CARTESIAN_POINT('Ctrl Pts',(-2.34013966242297,6.34949095285244,49.3095777869908));
#60305=CARTESIAN_POINT('Ctrl Pts',(-2.51467682553978,6.28516432556699,49.3183276072424));
#60306=CARTESIAN_POINT('Ctrl Pts',(-2.68656000078795,6.21363705879681,49.327077427494));
#60307=CARTESIAN_POINT('Ctrl Pts',(-2.85520533840831,6.13515211510886,49.3358272477455));
#60308=CARTESIAN_POINT('Ctrl Pts',(-3.02384747998279,6.05666865881146,49.3445769021768));
#60309=CARTESIAN_POINT('Ctrl Pts',(-3.18925164684496,5.97122791039866,49.3533265566081));
#60310=CARTESIAN_POINT('Ctrl Pts',(-3.35085601829125,5.87912008251926,49.3620762110393));
#60311=CARTESIAN_POINT('Ctrl Pts',(-3.5124575419138,5.78701387778197,49.3708257112825));
#60312=CARTESIAN_POINT('Ctrl Pts',(-3.67025915510894,5.6882409706101,49.3795752115256));
#60313=CARTESIAN_POINT('Ctrl Pts',(-3.82372487928787,5.58313684656887,49.3883247117687));
#60314=CARTESIAN_POINT('Ctrl Pts',(-3.97718810300761,5.478034435018,49.3970740694538));
#60315=CARTESIAN_POINT('Ctrl Pts',(-4.12631534262999,5.36660117496397,49.4058234271389));
#60316=CARTESIAN_POINT('Ctrl Pts',(-4.27060009886208,5.24921554097364,49.4145727848241));
#60317=CARTESIAN_POINT('Ctrl Pts',(-4.41488269594197,5.13183166360305,49.4233220115793));
#60318=CARTESIAN_POINT('Ctrl Pts',(-4.55432273235073,5.00849577139485,49.4320712383344));
#60319=CARTESIAN_POINT('Ctrl Pts',(-4.68844662480192,4.87962675277357,49.4408204650896));
#60320=CARTESIAN_POINT('Ctrl Pts',(-4.82256868835143,4.75075949139896,49.4495695725411));
#60321=CARTESIAN_POINT('Ctrl Pts',(-4.95137454637849,4.6163594531254,49.4583186799926));
#60322=CARTESIAN_POINT('Ctrl Pts',(-5.07442674461065,4.47688309134605,49.4670677874441));
#60323=CARTESIAN_POINT('Ctrl Pts',(-5.19747742838542,4.33740844616348,49.4758167872165));
#60324=CARTESIAN_POINT('Ctrl Pts',(-5.31477440450945,4.19285781736007,49.4845657869889));
#60325=CARTESIAN_POINT('Ctrl Pts',(-5.42591931531184,4.04372211999365,49.4933147867613));
#60326=CARTESIAN_POINT('Ctrl Pts',(-5.53707636463015,3.89457013500754,49.5020647420418));
#60327=CARTESIAN_POINT('Ctrl Pts',(-5.64207983273505,3.74083230916368,49.5108146973224));
#60328=CARTESIAN_POINT('Ctrl Pts',(-5.74057303468783,3.5830308725177,49.519564652603));
#60329=CARTESIAN_POINT('Ctrl Pts',(-5.83906243363804,3.42523552887364,49.5283142700318));
#60330=CARTESIAN_POINT('Ctrl Pts',(-5.93104191768467,3.26337713156918,49.5370638874606));
#60331=CARTESIAN_POINT('Ctrl Pts',(-6.01619906699699,3.09800545291071,49.5458135048894));
#60332=CARTESIAN_POINT('Ctrl Pts',(-6.10135338095426,2.93263928039505,49.5545628309948));
#60333=CARTESIAN_POINT('Ctrl Pts',(-6.17968568352882,2.76376031540128,49.5633121571002));
#60334=CARTESIAN_POINT('Ctrl Pts',(-6.25092992694929,2.5919421383144,49.5720614832056));
#60335=CARTESIAN_POINT('Ctrl Pts',(-6.32217217691152,2.42012876880696,49.5808105644994));
#60336=CARTESIAN_POINT('Ctrl Pts',(-6.38632665483902,2.24537661647525,49.5895596457932));
#60337=CARTESIAN_POINT('Ctrl Pts',(-6.44317547869404,2.06827917621289,49.598308727087));
#60338=CARTESIAN_POINT('Ctrl Pts',(-6.50002944235986,1.89116572423253,49.607058599402));
#60339=CARTESIAN_POINT('Ctrl Pts',(-6.54957634250443,1.71170683289025,49.6158084717169));
#60340=CARTESIAN_POINT('Ctrl Pts',(-6.59164787708436,1.53051209225189,49.6245583440319));
#60341=CARTESIAN_POINT('Ctrl Pts',(-6.63371649075043,1.3493299314786,49.6333076088667));
#60342=CARTESIAN_POINT('Ctrl Pts',(-6.66831071257153,1.16641244173839,49.6420568737015));
#60343=CARTESIAN_POINT('Ctrl Pts',(-6.69531304840356,0.982380875158415,
49.6508061385363));
#60344=CARTESIAN_POINT('Ctrl Pts',(-6.72231677033063,0.798339861794236,
49.6595558524919));
#60345=CARTESIAN_POINT('Ctrl Pts',(-6.74172778477905,0.613184940728539,
49.6683055664476));
#60346=CARTESIAN_POINT('Ctrl Pts',(-6.75348015835528,0.427545027688932,
49.6770552804032));
#60347=CARTESIAN_POINT('Ctrl Pts',(-6.76249038365213,0.285219953547603,
49.6837634482054));
#60348=CARTESIAN_POINT('Ctrl Pts',(-6.76699999999988,0.142609995760499,
49.6904716160076));
#60349=CARTESIAN_POINT('Ctrl Pts',(-6.767,5.52185849906123E-12,49.6971797838098));
#60350=CARTESIAN_POINT('',(-6.767,7.5280007819922E-10,49.3028202161545));
#60351=CARTESIAN_POINT('Ctrl Pts',(3.09908550384732,6.01564277861007,48.6513967904261));
#60352=CARTESIAN_POINT('Ctrl Pts',(2.93373232018345,6.10082796552472,48.6601462383254));
#60353=CARTESIAN_POINT('Ctrl Pts',(2.76486502144447,6.17919158180181,48.6688956862247));
#60354=CARTESIAN_POINT('Ctrl Pts',(2.59305716434378,6.25046746591368,48.677645134124));
#60355=CARTESIAN_POINT('Ctrl Pts',(2.42125069459307,6.32174277447215,48.6863945113714));
#60356=CARTESIAN_POINT('Ctrl Pts',(2.24650397871081,6.38593035557818,48.6951438886188));
#60357=CARTESIAN_POINT('Ctrl Pts',(2.06941053323792,6.44281220003532,48.7038932658662));
#60358=CARTESIAN_POINT('Ctrl Pts',(1.89231845896703,6.49969360406679,48.7126425753688));
#60359=CARTESIAN_POINT('Ctrl Pts',(1.71287996431524,6.54926929700876,48.7213918848714));
#60360=CARTESIAN_POINT('Ctrl Pts',(1.53170449173523,6.59137090065474,48.730141194374));
#60361=CARTESIAN_POINT('Ctrl Pts',(1.35053036178189,6.6334721923008,48.7388904390386));
#60362=CARTESIAN_POINT('Ctrl Pts',(1.16761955878862,6.66809944062451,48.7476396837032));
#60363=CARTESIAN_POINT('Ctrl Pts',(0.983593309310659,6.69513503985389,48.7563889283678));
#60364=CARTESIAN_POINT('Ctrl Pts',(0.799568362460224,6.72217044771211,48.765138111101));
#60365=CARTESIAN_POINT('Ctrl Pts',(0.61442826843891,6.74161427235974,48.7738872938341));
#60366=CARTESIAN_POINT('Ctrl Pts',(0.428801816330655,6.75340047696799,48.7826364765673));
#60367=CARTESIAN_POINT('Ctrl Pts',(0.243176616523087,6.76518660206241,48.7913856002754));
#60368=CARTESIAN_POINT('Ctrl Pts',(0.0570653511656807,6.76931519233997,
48.8001347239836));
#60369=CARTESIAN_POINT('Ctrl Pts',(-0.128899900799894,6.76577222610795,
48.8088838476917));
#60370=CARTESIAN_POINT('Ctrl Pts',(-0.314863959941646,6.76222928260134,
48.817632915281));
#60371=CARTESIAN_POINT('Ctrl Pts',(-0.500681721080068,6.7510148865128,48.8263819828702));
#60372=CARTESIAN_POINT('Ctrl Pts',(-0.685722110172451,6.73216712416,48.8351310504594));
#60373=CARTESIAN_POINT('Ctrl Pts',(-0.870761373826543,6.71331947644158,
48.8438800648358));
#60374=CARTESIAN_POINT('Ctrl Pts',(-1.05502298984215,6.68683858440016,48.8526290792122));
#60375=CARTESIAN_POINT('Ctrl Pts',(-1.2378811767591,6.65281438131454,48.8613780935885));
#60376=CARTESIAN_POINT('Ctrl Pts',(-1.4300964145011,6.61704912302695,48.8705748044753));
#60377=CARTESIAN_POINT('Ctrl Pts',(-1.62076048989504,6.57294837083906,48.8797715153621));
#60378=CARTESIAN_POINT('Ctrl Pts',(-1.80915798956474,6.52067760043342,48.8889682262489));
#60379=CARTESIAN_POINT('Ctrl Pts',(-1.98840442998381,6.47094578578832,48.8977182239554));
#60380=CARTESIAN_POINT('Ctrl Pts',(-2.16559895947592,6.41381888476028,48.9064682216619));
#60381=CARTESIAN_POINT('Ctrl Pts',(-2.3401396623776,6.34949095286916,48.9152182193684));
#60382=CARTESIAN_POINT('Ctrl Pts',(-2.51467682549499,6.28516432558492,48.92396803962));
#60383=CARTESIAN_POINT('Ctrl Pts',(-2.68656000074379,6.21363705881591,48.9327178598716));
#60384=CARTESIAN_POINT('Ctrl Pts',(-2.85520533836482,6.1351521151291,48.9414676801232));
#60385=CARTESIAN_POINT('Ctrl Pts',(-3.02384747993973,6.05666865883295,48.9502173345544));
#60386=CARTESIAN_POINT('Ctrl Pts',(-3.18925164680241,5.97122791042138,48.9589669889857));
#60387=CARTESIAN_POINT('Ctrl Pts',(-3.35085601824925,5.8791200825432,48.9677166434169));
#60388=CARTESIAN_POINT('Ctrl Pts',(-3.51245754187268,5.78701387780694,48.9764661436601));
#60389=CARTESIAN_POINT('Ctrl Pts',(-3.67025915506873,5.68824097063605,48.9852156439032));
#60390=CARTESIAN_POINT('Ctrl Pts',(-3.82372487924861,5.58313684659576,48.9939651441464));
#60391=CARTESIAN_POINT('Ctrl Pts',(-3.97718810296909,5.47803443504597,49.0027145018315));
#60392=CARTESIAN_POINT('Ctrl Pts',(-4.12631534259225,5.36660117499298,49.0114638595166));
#60393=CARTESIAN_POINT('Ctrl Pts',(-4.27060009882517,5.24921554100367,49.0202132172017));
#60394=CARTESIAN_POINT('Ctrl Pts',(-4.41488269590598,5.13183166363402,49.0289624439569));
#60395=CARTESIAN_POINT('Ctrl Pts',(-4.5543227323157,5.0084957714267,49.0377116707121));
#60396=CARTESIAN_POINT('Ctrl Pts',(-4.68844662476788,4.87962675280627,49.0464608974673));
#60397=CARTESIAN_POINT('Ctrl Pts',(-4.82256868831839,4.75075949143251,49.0552100049188));
#60398=CARTESIAN_POINT('Ctrl Pts',(-4.95137454634646,4.61635945315975,49.0639591123703));
#60399=CARTESIAN_POINT('Ctrl Pts',(-5.07442674457968,4.47688309138116,49.0727082198218));
#60400=CARTESIAN_POINT('Ctrl Pts',(-5.19747742835516,4.33740844619973,49.0814572195941));
#60401=CARTESIAN_POINT('Ctrl Pts',(-5.31477440447996,4.19285781739744,49.0902062193665));
#60402=CARTESIAN_POINT('Ctrl Pts',(-5.42591931528317,4.04372212003211,49.0989552191389));
#60403=CARTESIAN_POINT('Ctrl Pts',(-5.53707636460246,3.8945701350469,49.1077051744195));
#60404=CARTESIAN_POINT('Ctrl Pts',(-5.64207983270839,3.74083230920389,49.1164551297));
#60405=CARTESIAN_POINT('Ctrl Pts',(-5.74057303466223,3.58303087255872,49.1252050849806));
#60406=CARTESIAN_POINT('Ctrl Pts',(-5.83906243361357,3.42523552891537,49.1339547024094));
#60407=CARTESIAN_POINT('Ctrl Pts',(-5.93104191766135,3.26337713161155,49.1427043198382));
#60408=CARTESIAN_POINT('Ctrl Pts',(-6.01619906697486,3.0980054529537,49.151453937267));
#60409=CARTESIAN_POINT('Ctrl Pts',(-6.10135338093331,2.93263928043865,49.1602032633724));
#60410=CARTESIAN_POINT('Ctrl Pts',(-6.17968568350907,2.76376031544544,49.1689525894778));
#60411=CARTESIAN_POINT('Ctrl Pts',(-6.25092992693076,2.59194213835907,49.1777019155832));
#60412=CARTESIAN_POINT('Ctrl Pts',(-6.32217217689402,2.42012876885261,49.186450996877));
#60413=CARTESIAN_POINT('Ctrl Pts',(-6.38632665482262,2.24537661652185,49.1952000781708));
#60414=CARTESIAN_POINT('Ctrl Pts',(-6.44317547867879,2.06827917626039,49.2039491594646));
#60415=CARTESIAN_POINT('Ctrl Pts',(-6.50002944234587,1.89116572428058,49.2126990317795));
#60416=CARTESIAN_POINT('Ctrl Pts',(-6.54957634249174,1.71170683293879,49.2214489040945));
#60417=CARTESIAN_POINT('Ctrl Pts',(-6.59164787707299,1.53051209230087,49.2301987764094));
#60418=CARTESIAN_POINT('Ctrl Pts',(-6.63371649074038,1.34932993152801,49.2389480412442));
#60419=CARTESIAN_POINT('Ctrl Pts',(-6.66831071256281,1.16641244178818,49.247697306079));
#60420=CARTESIAN_POINT('Ctrl Pts',(-6.69531304839621,0.982380875208539,
49.2564465709138));
#60421=CARTESIAN_POINT('Ctrl Pts',(-6.72231677032465,0.798339861844562,
49.2651962848694));
#60422=CARTESIAN_POINT('Ctrl Pts',(-6.74172778477446,0.613184940779011,
49.2739459988251));
#60423=CARTESIAN_POINT('Ctrl Pts',(-6.75348015835208,0.427545027739492,
49.2826957127808));
#60424=CARTESIAN_POINT('Ctrl Pts',(-6.76249038363532,0.285219953829973,
49.289403880572));
#60425=CARTESIAN_POINT('Ctrl Pts',(-6.76699999998414,0.142609996275572,
49.2961120483633));
#60426=CARTESIAN_POINT('Ctrl Pts',(-6.767,7.52800906917709E-10,49.3028202161545));
#60427=CARTESIAN_POINT('Ctrl Pts',(-6.767,5.40600529812716E-12,49.3028202161897));
#60428=CARTESIAN_POINT('Ctrl Pts',(-6.76700000000015,-0.186007249554668,
49.3115697280025));
#60429=CARTESIAN_POINT('Ctrl Pts',(-6.75932637294276,-0.372014355810922,
49.3203192398152));
#60430=CARTESIAN_POINT('Ctrl Pts',(-6.74400518263404,-0.557389537581373,
49.3290687516279));
#60431=CARTESIAN_POINT('Ctrl Pts',(-6.72868405703783,-0.742763936377985,
49.3378182264852));
#60432=CARTESIAN_POINT('Ctrl Pts',(-6.70571545643628,-0.927506130400437,
49.3465677013423));
#60433=CARTESIAN_POINT('Ctrl Pts',(-6.67517739401647,-1.1109886400911,49.3553171761995));
#60434=CARTESIAN_POINT('Ctrl Pts',(-6.64463945804475,-1.29447039004101,
49.3640666148281));
#60435=CARTESIAN_POINT('Ctrl Pts',(-6.60653217002823,-1.47669218338832,
49.3728160534566));
#60436=CARTESIAN_POINT('Ctrl Pts',(-6.56098496085594,-1.65703510627333,
49.3815654920851));
#60437=CARTESIAN_POINT('Ctrl Pts',(-6.5154379364968,-1.83737729739571,49.3903148952117));
#60438=CARTESIAN_POINT('Ctrl Pts',(-6.46245112157029,-2.01584035544528,
49.3990642983384));
#60439=CARTESIAN_POINT('Ctrl Pts',(-6.40220448361858,-2.19181813796997,
49.407813701465));
#60440=CARTESIAN_POINT('Ctrl Pts',(-6.34195808512122,-2.36779522105905,
49.4165630698165));
#60441=CARTESIAN_POINT('Ctrl Pts',(-6.2744520141651,-2.54128677725359,49.4253124381681));
#60442=CARTESIAN_POINT('Ctrl Pts',(-6.19991555052887,-2.71170355428286,
49.4340618065196));
#60443=CARTESIAN_POINT('Ctrl Pts',(-6.12537937695291,-2.88211966813154,
49.4428111408228));
#60444=CARTESIAN_POINT('Ctrl Pts',(-6.04381298028529,-3.04946076419516,
49.451560475126));
#60445=CARTESIAN_POINT('Ctrl Pts',(-5.95549339309064,-3.21315848424159,
49.4603098094291));
#60446=CARTESIAN_POINT('Ctrl Pts',(-5.86717414225886,-3.37685558084949,
49.4690591104107));
#60447=CARTESIAN_POINT('Ctrl Pts',(-5.77210188844137,-3.53690907699886,
49.4778084113923));
#60448=CARTESIAN_POINT('Ctrl Pts',(-5.67059953311434,-3.69277537023896,
49.4865577123738));
#60449=CARTESIAN_POINT('Ctrl Pts',(-5.5690975559276,-3.84864108280951,49.4953069807604));
#60450=CARTESIAN_POINT('Ctrl Pts',(-5.46116568155008,-4.00031938354772,
49.5040562491471));
#60451=CARTESIAN_POINT('Ctrl Pts',(-5.34717048488407,-4.14729511918126,
49.5128055175337));
#60452=CARTESIAN_POINT('Ctrl Pts',(-5.23317570343322,-4.29427031947159,
49.5215547540521));
#60453=CARTESIAN_POINT('Ctrl Pts',(-5.11311781951551,-4.43654276249552,
49.5303039905704));
#60454=CARTESIAN_POINT('Ctrl Pts',(-4.98740458929233,-4.57362924412395,
49.5390532270888));
#60455=CARTESIAN_POINT('Ctrl Pts',(-4.86169180652717,-4.71071523781292,
49.5478024324655));
#60456=CARTESIAN_POINT('Ctrl Pts',(-4.73032391141537,-4.84261509584525,
49.5565516378422));
#60457=CARTESIAN_POINT('Ctrl Pts',(-4.59374706947278,-4.96888084599644,
49.565300843219));
#60458=CARTESIAN_POINT('Ctrl Pts',(-4.45717070231484,-5.09514615720762,
49.5740500181807));
#60459=CARTESIAN_POINT('Ctrl Pts',(-4.31538563497366,-5.21577720520579,
49.5827991931423));
#60460=CARTESIAN_POINT('Ctrl Pts',(-4.16887340952073,-5.33036429293449,
49.591548368104));
#60461=CARTESIAN_POINT('Ctrl Pts',(-4.02236168122547,-5.4449509918366,49.6002975133773));
#60462=CARTESIAN_POINT('Ctrl Pts',(-3.87112305263238,-5.55349359497889,
49.6090466586506));
#60463=CARTESIAN_POINT('Ctrl Pts',(-3.71567116929046,-5.65562346357178,
49.6177958039238));
#60464=CARTESIAN_POINT('Ctrl Pts',(-3.5602198005338,-5.75775299408884,49.6265449202352));
#60465=CARTESIAN_POINT('Ctrl Pts',(-3.4005554444217,-5.85346967519828,49.6352940365465));
#60466=CARTESIAN_POINT('Ctrl Pts',(-3.23722035886948,-5.94244843041326,
49.6440431528579));
#60467=CARTESIAN_POINT('Ctrl Pts',(-3.07388580043611,-6.03142689847388,
49.6527922409339));
#60468=CARTESIAN_POINT('Ctrl Pts',(-2.90688078789361,-6.11366734707835,
49.6615413290099));
#60469=CARTESIAN_POINT('Ctrl Pts',(-2.73677250610548,-6.1888904700136,49.6702904170859));
#60470=CARTESIAN_POINT('Ctrl Pts',(-2.56666475917063,-6.26411335643282,
49.6790394776531));
#60471=CARTESIAN_POINT('Ctrl Pts',(-2.39345402457194,-6.33231884545219,
49.6877885382203));
#60472=CARTESIAN_POINT('Ctrl Pts',(-2.21772855944137,-6.39327529804858,
49.6965375987875));
#60473=CARTESIAN_POINT('Ctrl Pts',(-2.04200363223679,-6.45423156404674,
49.7052866325723));
#60474=CARTESIAN_POINT('Ctrl Pts',(-1.86376426061139,-6.50793874412422,
49.7140356663571));
#60475=CARTESIAN_POINT('Ctrl Pts',(-1.6836157762181,-6.55421443943281,49.7227847001419));
#60476=CARTESIAN_POINT('Ctrl Pts',(-1.50346782833343,-6.60048999692559,
49.7315337078708));
#60477=CARTESIAN_POINT('Ctrl Pts',(-1.3214110565752,-6.63933404265135,49.7402827155996));
#60478=CARTESIAN_POINT('Ctrl Pts',(-1.13806375346673,-6.67061465631506,
49.7490317233285));
#60479=CARTESIAN_POINT('Ctrl Pts',(-0.954716981171458,-6.7018951794175,
49.757780705728));
#60480=CARTESIAN_POINT('Ctrl Pts',(-0.770079967443803,-6.72561226608986,
49.7665296881274));
#60481=CARTESIAN_POINT('Ctrl Pts',(-0.584779764074661,-6.74168536995971,
49.7752786705268));
#60482=CARTESIAN_POINT('Ctrl Pts',(-0.391489587594497,-6.75845153117864,
49.7844049009424));
#60483=CARTESIAN_POINT('Ctrl Pts',(-0.197478091806726,-6.7668998514639,
49.7935311313581));
#60484=CARTESIAN_POINT('Ctrl Pts',(-0.00346214753246707,-6.76699911434415,
49.8026573617737));
#60485=CARTESIAN_POINT('Ctrl Pts',(0.184490798483177,-6.76709527525939,
49.8114983974888));
#60486=CARTESIAN_POINT('Ctrl Pts',(0.372447602153291,-6.75935633790771,
49.8203394332039));
#60487=CARTESIAN_POINT('Ctrl Pts',(0.559756448192704,-6.74380914014526,
49.829180468919));
#60488=CARTESIAN_POINT('Ctrl Pts',(0.745136131041834,-6.72842206873171,
49.8379304475324));
#60489=CARTESIAN_POINT('Ctrl Pts',(0.929880851943513,-6.70538686355745,
49.8466804261457));
#60490=CARTESIAN_POINT('Ctrl Pts',(1.11336305057309,-6.67478177303338,49.855430404759));
#60491=CARTESIAN_POINT('Ctrl Pts',(1.29684337089978,-6.64417699581289,49.864180293799));
#60492=CARTESIAN_POINT('Ctrl Pts',(1.47906091205053,-6.60600253548091,49.8729301828389));
#60493=CARTESIAN_POINT('Ctrl Pts',(1.65939671095094,-6.56038806441244,49.8816800718789));
#60494=CARTESIAN_POINT('Ctrl Pts',(1.83973072369034,-6.51477404513885,49.8904298742544));
#60495=CARTESIAN_POINT('Ctrl Pts',(2.01818275356911,-6.461720232887,49.8991796766299));
#60496=CARTESIAN_POINT('Ctrl Pts',(2.19414664033203,-6.4014068391815,49.9079294790054));
#60497=CARTESIAN_POINT('Ctrl Pts',(2.37010884271141,-6.34109402281542,49.9166791976249));
#60498=CARTESIAN_POINT('Ctrl Pts',(2.54358267847693,-6.27352185699838,49.9254289162445));
#60499=CARTESIAN_POINT('Ctrl Pts',(2.71397890841633,-6.19891986435309,49.934178634864));
#60500=CARTESIAN_POINT('Ctrl Pts',(2.88437356388832,-6.12431856103295,49.9429282726358));
#60501=CARTESIAN_POINT('Ctrl Pts',(3.05169040787062,-6.04268767582613,49.9516779104077));
#60502=CARTESIAN_POINT('Ctrl Pts',(3.21536112511943,-5.95430447954005,49.9604275481795));
#60503=CARTESIAN_POINT('Ctrl Pts',(3.37903038442726,-5.8659220705511,49.9691771080115));
#60504=CARTESIAN_POINT('Ctrl Pts',(3.5390533297985,-5.77078760703452,49.9779266678436));
#60505=CARTESIAN_POINT('Ctrl Pts',(3.69488643041764,-5.66922422085382,49.9866762276757));
#60506=CARTESIAN_POINT('Ctrl Pts',(3.8507181946862,-5.56766170563243,49.9954257124757));
#60507=CARTESIAN_POINT('Ctrl Pts',(4.00235994599108,-5.45967053456337,50.0041751972757));
#60508=CARTESIAN_POINT('Ctrl Pts',(4.1492966297419,-5.3456175020677,50.0129246820756));
#60509=CARTESIAN_POINT('Ctrl Pts',(4.29623210224934,-5.23156540974556,50.021674094751));
#60510=CARTESIAN_POINT('Ctrl Pts',(4.43846235842008,-5.11145173172281,50.0304235074264));
#60511=CARTESIAN_POINT('Ctrl Pts',(4.5755043179732,-4.98568443006661,50.0391729201017));
#60512=CARTESIAN_POINT('Ctrl Pts',(4.7125451933739,-4.85991812336791,50.0479222635596));
#60513=CARTESIAN_POINT('Ctrl Pts',(4.84439764314884,-4.72849847631203,50.0566716070175));
#60514=CARTESIAN_POINT('Ctrl Pts',(4.97061384196591,-4.59187184425447,50.0654209504754));
#60515=CARTESIAN_POINT('Ctrl Pts',(5.09682908420106,-4.45524624767861,50.0741702276228));
#60516=CARTESIAN_POINT('Ctrl Pts',(5.21740796650067,-4.31341395557017,50.0829195047701));
#60517=CARTESIAN_POINT('Ctrl Pts',(5.33194095942145,-4.16685668162992,50.0916687819175));
#60518=CARTESIAN_POINT('Ctrl Pts',(5.44647312235028,-4.02030046975357,50.100417995661));
#60519=CARTESIAN_POINT('Ctrl Pts',(5.55495930712184,-3.86901957035696,50.1091672094046));
#60520=CARTESIAN_POINT('Ctrl Pts',(5.65703106079693,-3.7135277805853,50.1179164231481));
#60521=CARTESIAN_POINT('Ctrl Pts',(5.75910210868636,-3.55803706597764,50.1266655763943));
#60522=CARTESIAN_POINT('Ctrl Pts',(5.85475865698452,-3.39833575881067,50.1354147296405));
#60523=CARTESIAN_POINT('Ctrl Pts',(5.94367583068968,-3.23496624706894,50.1441638828867));
#60524=CARTESIAN_POINT('Ctrl Pts',(6.03259241909992,-3.07159781070267,50.1529129785418));
#60525=CARTESIAN_POINT('Ctrl Pts',(6.11476958470892,-2.90456146975993,50.1616620741969));
#60526=CARTESIAN_POINT('Ctrl Pts',(6.18992823574319,-2.73442451648409,50.1704111698521));
#60527=CARTESIAN_POINT('Ctrl Pts',(6.26508641700875,-2.56428862662563,50.1791602108222));
#60528=CARTESIAN_POINT('Ctrl Pts',(6.33322605570243,-2.3910524253142,50.1879092517923));
#60529=CARTESIAN_POINT('Ctrl Pts',(6.39411573747719,-2.21530425353867,50.1966582927624));
#60530=CARTESIAN_POINT('Ctrl Pts',(6.45500505889075,-2.03955712188719,50.2054072819534));
#60531=CARTESIAN_POINT('Ctrl Pts',(6.50864441544878,-1.8612983202575,50.2141562711444));
#60532=CARTESIAN_POINT('Ctrl Pts',(6.55485164049856,-1.68113324012507,50.2229052603354));
#60533=CARTESIAN_POINT('Ctrl Pts',(6.60199852639068,-1.49730435913086,50.2318321672123));
#60534=CARTESIAN_POINT('Ctrl Pts',(6.64140767440975,-1.31149113173827,50.2407590740892));
#60535=CARTESIAN_POINT('Ctrl Pts',(6.67293975269575,-1.12435050446596,50.249685980966));
#60536=CARTESIAN_POINT('Ctrl Pts',(6.70384664831483,-0.94092029156542,50.25843589515));
#60537=CARTESIAN_POINT('Ctrl Pts',(6.72718585889647,-0.756215114279639,
50.267185809334));
#60538=CARTESIAN_POINT('Ctrl Pts',(6.7428781045185,-0.570862389376862,50.275935723518));
#60539=CARTESIAN_POINT('Ctrl Pts',(6.75857004154113,-0.385513309569948,
50.2846854656286));
#60540=CARTESIAN_POINT('Ctrl Pts',(6.7666152903555,-0.199516993261185,50.2934352077392));
#60541=CARTESIAN_POINT('Ctrl Pts',(6.76698652348896,-0.0135052182071509,
50.3021849498498));
#60542=CARTESIAN_POINT('Ctrl Pts',(6.76735774981529,0.172503146035686,50.3109345315204));
#60543=CARTESIAN_POINT('Ctrl Pts',(6.76005524147496,0.358526681830155,50.3196841131911));
#60544=CARTESIAN_POINT('Ctrl Pts',(6.74510380214909,0.543933542111445,50.3284336948617));
#60545=CARTESIAN_POINT('Ctrl Pts',(6.73015261711016,0.729337249081364,50.3371831277236));
#60546=CARTESIAN_POINT('Ctrl Pts',(6.7075527844465,0.914124015851373,50.3459325605855));
#60547=CARTESIAN_POINT('Ctrl Pts',(6.67738106408342,1.09766621749064,50.3546819934475));
#60548=CARTESIAN_POINT('Ctrl Pts',(6.64720981677314,1.28120554143013,50.3634312891298));
#60549=CARTESIAN_POINT('Ctrl Pts',(6.60946696581589,1.46350005650325,50.3721805848122));
#60550=CARTESIAN_POINT('Ctrl Pts',(6.56428070011065,1.64393062206252,50.3809298804945));
#60551=CARTESIAN_POINT('Ctrl Pts',(6.5190950828282,1.82435859844368,50.3896790506245));
#60552=CARTESIAN_POINT('Ctrl Pts',(6.4664663341575,2.00292240086278,50.3984282207545));
#60553=CARTESIAN_POINT('Ctrl Pts',(6.4065731959729,2.17901557696168,50.4071773908845));
#60554=CARTESIAN_POINT('Ctrl Pts',(6.34668083768402,2.35510646007145,50.4159264470876));
#60555=CARTESIAN_POINT('Ctrl Pts',(6.27952437144002,2.52872650996239,50.4246755032906));
#60556=CARTESIAN_POINT('Ctrl Pts',(6.20533187335263,2.69928607997632,50.4334245594937));
#60557=CARTESIAN_POINT('Ctrl Pts',(6.12831449784381,2.87633970115123,50.4425067357826));
#60558=CARTESIAN_POINT('Ctrl Pts',(6.04371489463282,3.05009490562094,50.4515889120714));
#60559=CARTESIAN_POINT('Ctrl Pts',(5.95184265120618,3.21991584599395,50.4606710883603));
#60560=CARTESIAN_POINT('Ctrl Pts',(5.86333281335626,3.3835215590507,50.4694208687147));
#60561=CARTESIAN_POINT('Ctrl Pts',(5.76807337235824,3.54347560903599,50.4781706490691));
#60562=CARTESIAN_POINT('Ctrl Pts',(5.66638790086499,3.69923467178427,50.4869204294235));
#60563=CARTESIAN_POINT('Ctrl Pts',(5.56470608502893,3.85498813489548,50.4956698952178));
#60564=CARTESIAN_POINT('Ctrl Pts',(5.45659885767108,4.00654667256049,50.5044193610121));
#60565=CARTESIAN_POINT('Ctrl Pts',(5.34243340580669,4.15339551506003,50.5131688268063));
#60566=CARTESIAN_POINT('Ctrl Pts',(5.22827145140762,4.30023985883666,50.5219180245602));
#60567=CARTESIAN_POINT('Ctrl Pts',(5.10805181978264,4.44237456992841,50.5306672223141));
#60568=CARTESIAN_POINT('Ctrl Pts',(4.98218281282733,4.57931691626251,50.5394164200679));
#60569=CARTESIAN_POINT('Ctrl Pts',(4.8563169929641,4.71625579511976,50.5481653962859));
#60570=CARTESIAN_POINT('Ctrl Pts',(4.72480227792017,4.84800236135595,50.5569143725039));
#60571=CARTESIAN_POINT('Ctrl Pts',(4.5880853084829,4.97410918678746,50.5656633487219));
#60572=CARTESIAN_POINT('Ctrl Pts',(4.45135945057145,5.10022421088856,50.5744128937431));
#60573=CARTESIAN_POINT('Ctrl Pts',(4.30943087208213,5.22069856611844,50.5831624387643));
#60574=CARTESIAN_POINT('Ctrl Pts',(4.16278164322637,5.33512305301551,50.5919119837856));
#60575=CARTESIAN_POINT('Ctrl Pts',(4.01614103534579,5.44954081331287,50.6006610144528));
#60576=CARTESIAN_POINT('Ctrl Pts',(3.86478055833622,5.55790924068192,50.6094100451201));
#60577=CARTESIAN_POINT('Ctrl Pts',(3.70921425812181,5.65986029751141,50.6181590757873));
#60578=CARTESIAN_POINT('Ctrl Pts',(3.55364584530355,5.76181273884508,50.6269082252672));
#60579=CARTESIAN_POINT('Ctrl Pts',(3.39387173464586,5.85734747817923,50.635657374747));
#60580=CARTESIAN_POINT('Ctrl Pts',(3.23043456092652,5.94614005448673,50.6444065242269));
#60581=CARTESIAN_POINT('Ctrl Pts',(3.18690768806561,5.96978744811192,50.6467366129599));
#60582=CARTESIAN_POINT('Ctrl Pts',(3.14312114982971,5.99295688499254,50.649066701693));
#60583=CARTESIAN_POINT('Ctrl Pts',(3.09908550384729,6.01564277861008,50.6513967904261));
#60584=CARTESIAN_POINT('Origin',(0.,0.,-63.6971797838103));
#60585=CARTESIAN_POINT('',(3.09908550384738,6.01564277861003,53.0457619208681));
#60586=CARTESIAN_POINT('',(3.09908550384726,6.0156427786101,52.6512695067322));
#60587=CARTESIAN_POINT('',(3.09908550384721,6.01564277861012,-63.6971797838103));
#60588=CARTESIAN_POINT('',(-6.76699958286891,-0.00237601598699733,51.6971797837748));
#60589=CARTESIAN_POINT('Ctrl Pts',(-6.76699958286865,-0.00237601672971834,
51.6971797838098));
#60590=CARTESIAN_POINT('Ctrl Pts',(-6.76692339209237,-0.219370680476571,
51.7073982192068));
#60591=CARTESIAN_POINT('Ctrl Pts',(-6.75640560764649,-0.436117771244051,
51.7176166546039));
#60592=CARTESIAN_POINT('Ctrl Pts',(-6.73554224636009,-0.651735872496242,
51.7278350900009));
#60593=CARTESIAN_POINT('Ctrl Pts',(-6.72434858357413,-0.767419835537226,
51.733317510521));
#60594=CARTESIAN_POINT('Ctrl Pts',(-6.71017775251439,-0.882779033068135,
51.7387999310411));
#60595=CARTESIAN_POINT('Ctrl Pts',(-6.69305057914311,-0.997678778481391,
51.7442823515612));
#60596=CARTESIAN_POINT('Ctrl Pts',(-6.66706730317644,-1.17199077549657,
51.7525996168945));
#60597=CARTESIAN_POINT('Ctrl Pts',(-6.63424504598464,-1.34545547933586,
51.7609168822278));
#60598=CARTESIAN_POINT('Ctrl Pts',(-6.59465426282857,-1.51750589908473,
51.7692341475611));
#60599=CARTESIAN_POINT('Ctrl Pts',(-6.55509687145169,-1.68941120754333,
51.7775443979211));
#60600=CARTESIAN_POINT('Ctrl Pts',(-6.5087824056808,-1.85990427123355,51.7858546482811));
#60601=CARTESIAN_POINT('Ctrl Pts',(-6.45583272896794,-2.02842618194166,
51.7941648986411));
#60602=CARTESIAN_POINT('Ctrl Pts',(-6.40291801411033,-2.19683682023008,
51.8024696618709));
#60603=CARTESIAN_POINT('Ctrl Pts',(-6.34337692216246,-2.36327856825245,
51.8107744251008));
#60604=CARTESIAN_POINT('Ctrl Pts',(-6.27738176702665,-2.52720540340538,
51.8190791883306));
#60605=CARTESIAN_POINT('Ctrl Pts',(-6.21141810664073,-2.69105400804786,
51.8273799882931));
#60606=CARTESIAN_POINT('Ctrl Pts',(-6.13900665096635,-2.85238976968202,
51.8356807882556));
#60607=CARTESIAN_POINT('Ctrl Pts',(-6.06036875139973,-3.01068424067648,
51.8439815882181));
#60608=CARTESIAN_POINT('Ctrl Pts',(-5.98175398977785,-3.16893213605354,
51.8522799458029));
#60609=CARTESIAN_POINT('Ctrl Pts',(-5.89691659061609,-3.32414021335686,
51.8605783033877));
#60610=CARTESIAN_POINT('Ctrl Pts',(-5.80612508777875,-3.47580213261144,
51.8688766609725));
#60611=CARTESIAN_POINT('Ctrl Pts',(-5.71532434711396,-3.62747948311891,
51.8771758628962));
#60612=CARTESIAN_POINT('Ctrl Pts',(-5.61856846448963,-3.77560965235233,
51.8854750648199));
#60613=CARTESIAN_POINT('Ctrl Pts',(-5.51617108132283,-3.91971243863344,
51.8937742667436));
#60614=CARTESIAN_POINT('Ctrl Pts',(-5.41376331700229,-4.06382983420566,
51.9020743100491));
#60615=CARTESIAN_POINT('Ctrl Pts',(-5.30571311328846,-4.20391874899488,
51.9103743533545));
#60616=CARTESIAN_POINT('Ctrl Pts',(-5.19237639804994,-4.33952950686753,
51.91867439666));
#60617=CARTESIAN_POINT('Ctrl Pts',(-5.07900937847468,-4.47517652478232,
51.9269766592578));
#60618=CARTESIAN_POINT('Ctrl Pts',(-4.96035325320555,-4.60634273229985,
51.9352789218557));
#60619=CARTESIAN_POINT('Ctrl Pts',(-4.83680315784621,-4.73261283143349,
51.9435811844535));
#60620=CARTESIAN_POINT('Ctrl Pts',(-4.71319951521926,-4.85893765669883,
51.951887045296));
#60621=CARTESIAN_POINT('Ctrl Pts',(-4.58469791833195,-4.98036189589384,
51.9601929061386));
#60622=CARTESIAN_POINT('Ctrl Pts',(-4.45172927328002,-5.09650816514815,
51.9684987669812));
#60623=CARTESIAN_POINT('Ctrl Pts',(-4.31860344990854,-5.21279172748697,
51.9768144459372));
#60624=CARTESIAN_POINT('Ctrl Pts',(-4.18100029065957,-5.32378462558094,
51.9851301248932));
#60625=CARTESIAN_POINT('Ctrl Pts',(-4.03938352653386,-5.42915000028245,
51.9934458038493));
#60626=CARTESIAN_POINT('Ctrl Pts',(-3.8976771909327,-5.5345820177443,52.001766742406));
#60627=CARTESIAN_POINT('Ctrl Pts',(-3.75195247451745,-5.63437921724193,
52.0100876809628));
#60628=CARTESIAN_POINT('Ctrl Pts',(-3.60270092702286,-5.72824886247347,
52.0184086195196));
#60629=CARTESIAN_POINT('Ctrl Pts',(-3.45322754549838,-5.82225802707373,
52.0267419255684));
#60630=CARTESIAN_POINT('Ctrl Pts',(-3.30021715839903,-5.91032185718474,
52.0350752316172));
#60631=CARTESIAN_POINT('Ctrl Pts',(-3.14418586534891,-5.99219360869958,
52.0434085376661));
#60632=CARTESIAN_POINT('Ctrl Pts',(-3.02933762153226,-6.05245605154592,
52.0495423429188));
#60633=CARTESIAN_POINT('Ctrl Pts',(-2.91285318970383,-6.1093647091172,52.0556761481715));
#60634=CARTESIAN_POINT('Ctrl Pts',(-2.79494455544713,-6.16283813936213,
52.0618099534242));
#60635=CARTESIAN_POINT('Ctrl Pts',(-2.6397897579363,-6.23320329365438,52.0698813666668));
#60636=CARTESIAN_POINT('Ctrl Pts',(-2.48169049578681,-6.297834770252,52.0779527799093));
#60637=CARTESIAN_POINT('Ctrl Pts',(-2.32111802262275,-6.35646915551833,
52.0860241931519));
#60638=CARTESIAN_POINT('Ctrl Pts',(-2.16074713489885,-6.41502993017053,
52.0940854734037));
#60639=CARTESIAN_POINT('Ctrl Pts',(-1.99790956002941,-6.46760846766957,
52.1021467536555));
#60640=CARTESIAN_POINT('Ctrl Pts',(-1.83310086105797,-6.51398727609968,
52.1102080339073));
#60641=CARTESIAN_POINT('Ctrl Pts',(-1.66846292244738,-6.56031803086446,
52.1182609617655));
#60642=CARTESIAN_POINT('Ctrl Pts',(-1.50185827995957,-6.60046173957115,
52.1263138896236));
#60643=CARTESIAN_POINT('Ctrl Pts',(-1.33380208825379,-6.63424909009074,
52.1343668174818));
#60644=CARTESIAN_POINT('Ctrl Pts',(-1.16588322122824,-6.66800883176677,
52.1424131650067));
#60645=CARTESIAN_POINT('Ctrl Pts',(-0.996515529540075,-6.69542247996154,
52.1504595125317));
#60646=CARTESIAN_POINT('Ctrl Pts',(-0.826228832144859,-6.71637066554047,
52.1585058600566));
#60647=CARTESIAN_POINT('Ctrl Pts',(-0.65604403212678,-6.73730631599365,
52.1665473927504));
#60648=CARTESIAN_POINT('Ctrl Pts',(-0.484941690377815,-6.75178416017236,
52.174588925444));
#60649=CARTESIAN_POINT('Ctrl Pts',(-0.313461205972948,-6.75973602090718,
52.1826304581378));
#60650=CARTESIAN_POINT('Ctrl Pts',(-0.138684054289472,-6.76784075407631,
52.1908265871856));
#60651=CARTESIAN_POINT('Ctrl Pts',(0.0364855390093745,-6.76916595288036,
52.1990227162336));
#60652=CARTESIAN_POINT('Ctrl Pts',(0.21147113835977,-6.76369491902472,52.2072188452814));
#60653=CARTESIAN_POINT('Ctrl Pts',(0.383096874713335,-6.75832893338033,
52.2152576021181));
#60654=CARTESIAN_POINT('Ctrl Pts',(0.554545232689751,-6.74642537015907,
52.2232963589547));
#60655=CARTESIAN_POINT('Ctrl Pts',(0.725273008550923,-6.72802111048022,
52.2313351157914));
#60656=CARTESIAN_POINT('Ctrl Pts',(0.896017309056241,-6.70961506946357,
52.2393746506947));
#60657=CARTESIAN_POINT('Ctrl Pts',(1.06604051722078,-6.68470711906572,52.2474141855981));
#60658=CARTESIAN_POINT('Ctrl Pts',(1.23480554568945,-6.65338592480059,52.2554537205014));
#60659=CARTESIAN_POINT('Ctrl Pts',(1.40362032436361,-6.62205549736752,52.2634956253775));
#60660=CARTESIAN_POINT('Ctrl Pts',(1.5711758180773,-6.58430813107191,52.2715375302536));
#60661=CARTESIAN_POINT('Ctrl Pts',(1.73694625459791,-6.54028338137105,52.2795794351296));
#60662=CARTESIAN_POINT('Ctrl Pts',(1.90830850624375,-6.49477357639478,52.2878926118094));
#60663=CARTESIAN_POINT('Ctrl Pts',(2.07776274408362,-6.44255559117958,52.2962057884892));
#60664=CARTESIAN_POINT('Ctrl Pts',(2.24474748498567,-6.38383879250178,52.304518965169));
#60665=CARTESIAN_POINT('Ctrl Pts',(2.40656372173722,-6.32693939352188,52.3125748327801));
#60666=CARTESIAN_POINT('Ctrl Pts',(2.56606073966611,-6.26393769263172,52.3206307003911));
#60667=CARTESIAN_POINT('Ctrl Pts',(2.72275047413203,-6.19507214289017,52.3286865680022));
#60668=CARTESIAN_POINT('Ctrl Pts',(2.88694734965355,-6.12290718494205,52.3371283992164));
#60669=CARTESIAN_POINT('Ctrl Pts',(3.04806088839697,-6.04430288375702,52.3455702304305));
#60670=CARTESIAN_POINT('Ctrl Pts',(3.20556180836742,-5.95958576519679,52.3540120616447));
#60671=CARTESIAN_POINT('Ctrl Pts',(3.36306272833788,-5.87486864663656,52.3624538928589));
#60672=CARTESIAN_POINT('Ctrl Pts',(3.51695067594288,-5.78403901878042,52.370895724073));
#60673=CARTESIAN_POINT('Ctrl Pts',(3.66673498003363,-5.68747251300591,52.3793375552872));
#60674=CARTESIAN_POINT('Ctrl Pts',(3.81276883251153,-5.59332393753143,52.3875680113531));
#60675=CARTESIAN_POINT('Ctrl Pts',(3.95538799712883,-5.49340951628428,52.3957984674189));
#60676=CARTESIAN_POINT('Ctrl Pts',(4.09410662674354,-5.388003334154,52.4040289234848));
#60677=CARTESIAN_POINT('Ctrl Pts',(4.23266058917079,-5.28272227537306,52.4122496095143));
#60678=CARTESIAN_POINT('Ctrl Pts',(4.3673229536294,-5.17196265135855,52.4204702955438));
#60679=CARTESIAN_POINT('Ctrl Pts',(4.4976345674635,-5.05604314633068,52.4286909815733));
#60680=CARTESIAN_POINT('Ctrl Pts',(4.62781763827388,-4.94023798754752,52.436903558488));
#60681=CARTESIAN_POINT('Ctrl Pts',(4.75365823930553,-4.81928332078326,52.4451161354027));
#60682=CARTESIAN_POINT('Ctrl Pts',(4.87472812724708,-4.69353967549292,52.4533287123174));
#60683=CARTESIAN_POINT('Ctrl Pts',(4.99570287010013,-4.56789484825274,52.4615348352213));
#60684=CARTESIAN_POINT('Ctrl Pts',(5.11191411979888,-4.43746879566858,52.4697409581252));
#60685=CARTESIAN_POINT('Ctrl Pts',(5.2229684656058,-4.3026607357875,52.4779470810292));
#60686=CARTESIAN_POINT('Ctrl Pts',(5.33395780444062,-4.16793158739542,52.4861484003822));
#60687=CARTESIAN_POINT('Ctrl Pts',(5.43979602554531,-4.02882581757971,52.4943497197353));
#60688=CARTESIAN_POINT('Ctrl Pts',(5.54012814395647,-3.88577780483412,52.5025510390883));
#60689=CARTESIAN_POINT('Ctrl Pts',(5.64043147946015,-3.74277082917397,52.5107500056772));
#60690=CARTESIAN_POINT('Ctrl Pts',(5.73523164973299,-3.59582415415112,52.518948972266));
#60691=CARTESIAN_POINT('Ctrl Pts',(5.82421523360115,-3.44540359213377,52.5271479388549));
#60692=CARTESIAN_POINT('Ctrl Pts',(5.9131870667851,-3.29500289383112,52.5353458227331));
#60693=CARTESIAN_POINT('Ctrl Pts',(5.99634366011715,-3.14112953031877,52.5435437066114));
#60694=CARTESIAN_POINT('Ctrl Pts',(6.07341605438554,-2.98427653382389,52.5517415904897));
#60695=CARTESIAN_POINT('Ctrl Pts',(6.15049227131832,-2.82741575767759,52.5599398809695));
#60696=CARTESIAN_POINT('Ctrl Pts',(6.22148352979553,-2.66757537598841,52.5681381714494));
#60697=CARTESIAN_POINT('Ctrl Pts',(6.28616777047431,-2.50527119519027,52.5763364619293));
#60698=CARTESIAN_POINT('Ctrl Pts',(6.35086696943216,-2.34292948142884,52.58453664827));
#60699=CARTESIAN_POINT('Ctrl Pts',(6.40925611294659,-2.17812316683632,52.5927368346107));
#60700=CARTESIAN_POINT('Ctrl Pts',(6.46116202352605,-2.01138616524645,52.6009370209514));
#60701=CARTESIAN_POINT('Ctrl Pts',(6.51311700707134,-1.84449152690403,52.6091449599248));
#60702=CARTESIAN_POINT('Ctrl Pts',(6.55857640511746,-1.67566289763885,52.6173528988982));
#60703=CARTESIAN_POINT('Ctrl Pts',(6.59741724550374,-1.5054483347926,52.6255608378717));
#60704=CARTESIAN_POINT('Ctrl Pts',(6.63627692875847,-1.33515119570491,52.6337727587651));
#60705=CARTESIAN_POINT('Ctrl Pts',(6.66851158650499,-1.16346713474569,52.6419846796584));
#60706=CARTESIAN_POINT('Ctrl Pts',(6.6940497798853,-0.990952342152505,52.6501966005517));
#60707=CARTESIAN_POINT('Ctrl Pts',(6.71962299485218,-0.818200972850359,
52.6584197827937));
#60708=CARTESIAN_POINT('Ctrl Pts',(6.73848135445139,-0.644616951801082,
52.6666429650357));
#60709=CARTESIAN_POINT('Ctrl Pts',(6.7506054051546,-0.470760728924464,52.6748661472776));
#60710=CARTESIAN_POINT('Ctrl Pts',(6.76141699865814,-0.315724853884322,
52.6821991505685));
#60711=CARTESIAN_POINT('Ctrl Pts',(6.76687410868896,-0.160472716684156,
52.6895321538594));
#60712=CARTESIAN_POINT('Ctrl Pts',(6.76699784576786,-0.00539957157468165,
52.6968651571503));
#60713=CARTESIAN_POINT('Ctrl Pts',(6.76714861808691,0.183555412008736,52.7058003439324));
#60714=CARTESIAN_POINT('Ctrl Pts',(6.75938087136423,0.372636727960242,52.7147355307145));
#60715=CARTESIAN_POINT('Ctrl Pts',(6.7436899197528,0.561190935622188,52.7236707174967));
#60716=CARTESIAN_POINT('Ctrl Pts',(6.72802246833288,0.749462747410466,52.7325925221331));
#60717=CARTESIAN_POINT('Ctrl Pts',(6.70445551119342,0.937208769276504,52.7415143267696));
#60718=CARTESIAN_POINT('Ctrl Pts',(6.67303631072846,1.12377728919014,52.750436131406));
#60719=CARTESIAN_POINT('Ctrl Pts',(6.64169374914481,1.3098907242371,52.7593361736451));
#60720=CARTESIAN_POINT('Ctrl Pts',(6.6025372141473,1.49483213548823,52.7682362158841));
#60721=CARTESIAN_POINT('Ctrl Pts',(6.55566537160227,1.67795725081864,52.7771362581231));
#60722=CARTESIAN_POINT('Ctrl Pts',(6.50886568894818,1.86080044234077,52.7860225986163));
#60723=CARTESIAN_POINT('Ctrl Pts',(6.45437445567373,2.04183266664652,52.7949089391094));
#60724=CARTESIAN_POINT('Ctrl Pts',(6.39234132796682,2.22041918266967,52.8037952796025));
#60725=CARTESIAN_POINT('Ctrl Pts',(6.33046680813958,2.39854908414358,52.8126588992741));
#60726=CARTESIAN_POINT('Ctrl Pts',(6.26108895703377,2.57424551200998,52.8215225189456));
#60727=CARTESIAN_POINT('Ctrl Pts',(6.184407005314,2.74688896619852,52.8303861386172));
#60728=CARTESIAN_POINT('Ctrl Pts',(6.11161249114023,2.91078015690351,52.838800411772));
#60729=CARTESIAN_POINT('Ctrl Pts',(6.0322360834037,3.07191996059379,52.8472146849269));
#60730=CARTESIAN_POINT('Ctrl Pts',(5.94649005211601,3.22979025016879,52.8556289580817));
#60731=CARTESIAN_POINT('Ctrl Pts',(5.86282314627675,3.38383258255816,52.86383920629));
#60732=CARTESIAN_POINT('Ctrl Pts',(5.77317128137702,3.53461350358046,52.8720494544983));
#60733=CARTESIAN_POINT('Ctrl Pts',(5.67782841486083,3.68165091927507,52.8802597027066));
#60734=CARTESIAN_POINT('Ctrl Pts',(5.58246288344398,3.82872328869556,52.8884719026546));
#60735=CARTESIAN_POINT('Ctrl Pts',(5.48140384877693,3.97205008117772,52.8966841026027));
#60736=CARTESIAN_POINT('Ctrl Pts',(5.3749883397868,4.11117858371002,52.9048963025507));
#60737=CARTESIAN_POINT('Ctrl Pts',(5.2685285840888,4.2503649347483,52.9131119170651));
#60738=CARTESIAN_POINT('Ctrl Pts',(5.15670813311193,4.38534923569393,52.9213275315794));
#60739=CARTESIAN_POINT('Ctrl Pts',(5.03990403583711,4.51571215973215,52.9295431460938));
#60740=CARTESIAN_POINT('Ctrl Pts',(4.92296877268048,4.64622147562037,52.9377679863831));
#60741=CARTESIAN_POINT('Ctrl Pts',(4.80103892298979,4.77209878408107,52.9459928266725));
#60742=CARTESIAN_POINT('Ctrl Pts',(4.67452878860127,4.89296123063917,52.9542176669618));
#60743=CARTESIAN_POINT('Ctrl Pts',(4.5479376200735,5.01390109379612,52.9624477755473));
#60744=CARTESIAN_POINT('Ctrl Pts',(4.4167605844359,5.12981945661114,52.9706778841329));
#60745=CARTESIAN_POINT('Ctrl Pts',(4.28144468026112,5.24037407537513,52.9789079927184));
#60746=CARTESIAN_POINT('Ctrl Pts',(4.14594325590463,5.35108026621845,52.9871493849091));
#60747=CARTESIAN_POINT('Ctrl Pts',(4.00629191223432,5.45640781091807,52.9953907770998));
#60748=CARTESIAN_POINT('Ctrl Pts',(3.86296701449437,5.5560574911468,53.0036321692905));
#60749=CARTESIAN_POINT('Ctrl Pts',(3.80058837805495,5.59942756342531,53.0072190325314));
#60750=CARTESIAN_POINT('Ctrl Pts',(3.73751421717592,5.64172271250377,53.0108058957724));
#60751=CARTESIAN_POINT('Ctrl Pts',(3.67378519826734,5.68292101977424,53.0143927590134));
#60752=CARTESIAN_POINT('Ctrl Pts',(3.52366072521857,5.77997059429149,53.0228422214901));
#60753=CARTESIAN_POINT('Ctrl Pts',(3.36955833612814,5.87115183969503,53.0312916839669));
#60754=CARTESIAN_POINT('Ctrl Pts',(3.21196465222055,5.95613734503208,53.0397411464436));
#60755=CARTESIAN_POINT('Ctrl Pts',(3.17453284224266,5.97632318755934,53.0417480712518));
#60756=CARTESIAN_POINT('Ctrl Pts',(3.13690420305201,5.9961596765056,53.04375499606));
#60757=CARTESIAN_POINT('Ctrl Pts',(3.09908550384738,6.01564277861003,53.0457619208681));
#60758=CARTESIAN_POINT('Ctrl Pts',(3.0990855038473,6.01564277861008,51.0457613895064));
#60759=CARTESIAN_POINT('Ctrl Pts',(2.93977103845707,6.09771699219197,51.0541945390125));
#60760=CARTESIAN_POINT('Ctrl Pts',(2.77726086164494,6.17342423470136,51.0626276885186));
#60761=CARTESIAN_POINT('Ctrl Pts',(2.61209614700951,6.2425349593557,51.0710608380246));
#60762=CARTESIAN_POINT('Ctrl Pts',(2.44678085035074,6.31170869282385,51.0795016761022));
#60763=CARTESIAN_POINT('Ctrl Pts',(2.27880649072714,6.37427377006968,51.0879425141797));
#60764=CARTESIAN_POINT('Ctrl Pts',(2.10873242976109,6.43004949745132,51.0963833522573));
#60765=CARTESIAN_POINT('Ctrl Pts',(2.02246941290357,6.45833942293456,51.1006646174499));
#60766=CARTESIAN_POINT('Ctrl Pts',(1.93566646209994,6.48488351458044,51.1049458826424));
#60767=CARTESIAN_POINT('Ctrl Pts',(1.84839780253877,6.50966316821154,51.109227147835));
#60768=CARTESIAN_POINT('Ctrl Pts',(1.68244540946173,6.55678481348922,51.117368515053));
#60769=CARTESIAN_POINT('Ctrl Pts',(1.51447841508181,6.59761636710254,51.1255098822709));
#60770=CARTESIAN_POINT('Ctrl Pts',(1.34501910234251,6.63198406318454,51.1336512494888));
#60771=CARTESIAN_POINT('Ctrl Pts',(1.17570771469497,6.6663217588817,51.1417855099124));
#60772=CARTESIAN_POINT('Ctrl Pts',(1.00490695799231,6.69420675616965,51.149919770336));
#60773=CARTESIAN_POINT('Ctrl Pts',(0.833154105077299,6.71551511331729,51.1580540307596));
#60774=CARTESIAN_POINT('Ctrl Pts',(0.661518415754918,6.73680893467332,51.1661827422845));
#60775=CARTESIAN_POINT('Ctrl Pts',(0.488932285107155,6.751535003179,51.1743114538094));
#60776=CARTESIAN_POINT('Ctrl Pts',(0.315942968594335,6.75962048051485,51.1824401653343));
#60777=CARTESIAN_POINT('Ctrl Pts',(0.143036147489403,6.767702102036,51.190565000427));
#60778=CARTESIAN_POINT('Ctrl Pts',(-0.0302731117240618,6.7691494214961,
51.1986898355196));
#60779=CARTESIAN_POINT('Ctrl Pts',(-0.203432659633227,6.7639414658167,51.2068146706122));
#60780=CARTESIAN_POINT('Ctrl Pts',(-0.376543731041455,6.75873496811909,
51.2149372311345));
#60781=CARTESIAN_POINT('Ctrl Pts',(-0.549504809086361,6.74687691816608,
51.2230597916567));
#60782=CARTESIAN_POINT('Ctrl Pts',(-0.721764004372139,6.72839845148849,
51.231182352179));
#60783=CARTESIAN_POINT('Ctrl Pts',(-0.894032354787369,6.70991900272832,
51.2393053443943));
#60784=CARTESIAN_POINT('Ctrl Pts',(-1.06559838353237,6.68481846948204,51.2474283366096));
#60785=CARTESIAN_POINT('Ctrl Pts',(-1.23591539037973,6.65317985235801,51.2555513288248));
#60786=CARTESIAN_POINT('Ctrl Pts',(-1.32285703202534,6.63702930249175,51.2596978688055));
#60787=CARTESIAN_POINT('Ctrl Pts',(-1.40947332344334,6.61917589421818,51.263844408786));
#60788=CARTESIAN_POINT('Ctrl Pts',(-1.49569253948153,6.59963581020493,51.2679909487667));
#60789=CARTESIAN_POINT('Ctrl Pts',(-1.68249021710502,6.55730136920716,51.2769746077947));
#60790=CARTESIAN_POINT('Ctrl Pts',(-1.86733093762222,6.50706793785618,51.2859582668227));
#60791=CARTESIAN_POINT('Ctrl Pts',(-2.04957887020492,6.44914842865394,51.2949419258508));
#60792=CARTESIAN_POINT('Ctrl Pts',(-2.23213990280502,6.3911294143485,51.3039410187098));
#60793=CARTESIAN_POINT('Ctrl Pts',(-2.41209901646806,6.32539800234898,51.3129401115689));
#60794=CARTESIAN_POINT('Ctrl Pts',(-2.58883872890599,6.25221585005799,51.321939204428));
#60795=CARTESIAN_POINT('Ctrl Pts',(-2.76599284657973,6.17886210607062,51.330959397645));
#60796=CARTESIAN_POINT('Ctrl Pts',(-2.93991223778385,6.09802275946844,51.3399795908621));
#60797=CARTESIAN_POINT('Ctrl Pts',(-3.10999997975497,6.01000741479776,51.3489997840791));
#60798=CARTESIAN_POINT('Ctrl Pts',(-3.28025997815563,5.92190293255114,51.3580291125004));
#60799=CARTESIAN_POINT('Ctrl Pts',(-3.4466803656029,5.82660804874572,51.3670584409218));
#60800=CARTESIAN_POINT('Ctrl Pts',(-3.60869038939335,5.72447750222674,51.3760877693431));
#60801=CARTESIAN_POINT('Ctrl Pts',(-3.77092881466131,5.62220297222342,51.3851298272976));
#60802=CARTESIAN_POINT('Ctrl Pts',(-3.92874424145666,5.51307363799984,51.394171885252));
#60803=CARTESIAN_POINT('Ctrl Pts',(-4.08159446284338,5.39748790094858,51.4032139432064));
#60804=CARTESIAN_POINT('Ctrl Pts',(-4.2142419015127,5.29717956100994,51.4110608787036));
#60805=CARTESIAN_POINT('Ctrl Pts',(-4.34315034565717,5.19200947772809,51.4189078142008));
#60806=CARTESIAN_POINT('Ctrl Pts',(-4.46798590640216,5.08226238403643,51.426754749698));
#60807=CARTESIAN_POINT('Ctrl Pts',(-4.60565239656515,4.96123519351512,51.4354082139992));
#60808=CARTESIAN_POINT('Ctrl Pts',(-4.73848618965122,4.8345340811254,51.4440616783005));
#60809=CARTESIAN_POINT('Ctrl Pts',(-4.86602383026489,4.70256324607062,51.4527151426017));
#60810=CARTESIAN_POINT('Ctrl Pts',(-4.99344398262479,4.57071398314846,51.4613606352924));
#60811=CARTESIAN_POINT('Ctrl Pts',(-5.11557750295289,4.43360489781744,51.470006127983));
#60812=CARTESIAN_POINT('Ctrl Pts',(-5.23199650576142,4.29167817569075,51.4786516206737));
#60813=CARTESIAN_POINT('Ctrl Pts',(-5.35191777441042,4.14548183177755,51.48755719817));
#60814=CARTESIAN_POINT('Ctrl Pts',(-5.46577508277386,3.99417367043613,51.4964627756663));
#60815=CARTESIAN_POINT('Ctrl Pts',(-5.57314262826314,3.83827698909761,51.5053683531627));
#60816=CARTESIAN_POINT('Ctrl Pts',(-5.67717675938209,3.68722039454225,51.5139974413356));
#60817=CARTESIAN_POINT('Ctrl Pts',(-5.77511785628655,3.53185619126521,51.5226265295086));
#60818=CARTESIAN_POINT('Ctrl Pts',(-5.86661983604594,3.37269338946076,51.5312556176816));
#60819=CARTESIAN_POINT('Ctrl Pts',(-5.96251961310948,3.20588085436599,51.5402994398396));
#60820=CARTESIAN_POINT('Ctrl Pts',(-6.05134583987484,3.03489584060695,51.5493432619976));
#60821=CARTESIAN_POINT('Ctrl Pts',(-6.13275139796263,2.86035824518319,51.5583870841557));
#60822=CARTESIAN_POINT('Ctrl Pts',(-6.21415695605036,2.68582064975955,51.5674309063137));
#60823=CARTESIAN_POINT('Ctrl Pts',(-6.28814165119957,2.50773080723462,51.5764747284717));
#60824=CARTESIAN_POINT('Ctrl Pts',(-6.35441396599907,2.32673852177592,51.5855185506297));
#60825=CARTESIAN_POINT('Ctrl Pts',(-6.41379649453772,2.16456251224549,51.5936221611497));
#60826=CARTESIAN_POINT('Ctrl Pts',(-6.46697760690456,2.00008111175776,51.6017257716698));
#60827=CARTESIAN_POINT('Ctrl Pts',(-6.51378575904546,1.83381680798725,51.6098293821898));
#60828=CARTESIAN_POINT('Ctrl Pts',(-6.56060798484162,1.66750251406791,51.6179354291961));
#60829=CARTESIAN_POINT('Ctrl Pts',(-6.60105331856789,1.499404599782,51.6260414762025));
#60830=CARTESIAN_POINT('Ctrl Pts',(-6.63500037413545,1.33005978633387,51.6341475232088));
#60831=CARTESIAN_POINT('Ctrl Pts',(-6.6689527451573,1.16068845675348,51.6422548394658));
#60832=CARTESIAN_POINT('Ctrl Pts',(-6.69640474652884,0.990070201969377,
51.6503621557227));
#60833=CARTESIAN_POINT('Ctrl Pts',(-6.71728642054541,0.818750355331961,
51.6584694719797));
#60834=CARTESIAN_POINT('Ctrl Pts',(-6.7381836852255,0.647302597968643,51.6665828413165));
#60835=CARTESIAN_POINT('Ctrl Pts',(-6.75250078859449,0.475152569323373,
51.6746962106534));
#60836=CARTESIAN_POINT('Ctrl Pts',(-6.76021974971399,0.302849691393129,
51.6828095799902));
#60837=CARTESIAN_POINT('Ctrl Pts',(-6.76477696220644,0.201123459633057,
51.6875996479184));
#60838=CARTESIAN_POINT('Ctrl Pts',(-6.76703529859893,0.0993439772433435,
51.6923897158466));
#60839=CARTESIAN_POINT('Ctrl Pts',(-6.76699958286891,-0.00237601598698748,
51.6971797837748));
#60840=CARTESIAN_POINT('',(-6.767,5.55191004660612E-12,51.3028202161897));
#60841=CARTESIAN_POINT('Ctrl Pts',(3.09908550384729,6.01564277861008,50.6513967904261));
#60842=CARTESIAN_POINT('Ctrl Pts',(2.9337323201834,6.10082796552475,50.6601462383254));
#60843=CARTESIAN_POINT('Ctrl Pts',(2.76486502144439,6.17919158180185,50.6688956862247));
#60844=CARTESIAN_POINT('Ctrl Pts',(2.59305716434367,6.25046746591373,50.677645134124));
#60845=CARTESIAN_POINT('Ctrl Pts',(2.42125069459293,6.32174277447221,50.6863945113714));
#60846=CARTESIAN_POINT('Ctrl Pts',(2.24650397871065,6.38593035557824,50.6951438886188));
#60847=CARTESIAN_POINT('Ctrl Pts',(2.06941053323773,6.44281220003538,50.7038932658662));
#60848=CARTESIAN_POINT('Ctrl Pts',(1.89231845896681,6.49969360406686,50.7126425753688));
#60849=CARTESIAN_POINT('Ctrl Pts',(1.71287996431499,6.54926929700882,50.7213918848714));
#60850=CARTESIAN_POINT('Ctrl Pts',(1.53170449173495,6.59137090065481,50.730141194374));
#60851=CARTESIAN_POINT('Ctrl Pts',(1.35053036178145,6.63347219230089,50.7388904390386));
#60852=CARTESIAN_POINT('Ctrl Pts',(1.16761955878803,6.66809944062462,50.7476396837032));
#60853=CARTESIAN_POINT('Ctrl Pts',(0.98359330930991,6.695135039854,50.7563889283678));
#60854=CARTESIAN_POINT('Ctrl Pts',(0.799568362459444,6.72217044771221,50.765138111101));
#60855=CARTESIAN_POINT('Ctrl Pts',(0.614428268438097,6.74161427235981,50.7738872938341));
#60856=CARTESIAN_POINT('Ctrl Pts',(0.428801816329812,6.75340047696805,50.7826364765673));
#60857=CARTESIAN_POINT('Ctrl Pts',(0.243176616522342,6.76518660206243,50.7913856002755));
#60858=CARTESIAN_POINT('Ctrl Pts',(0.057065351165034,6.76931519233997,50.8001347239836));
#60859=CARTESIAN_POINT('Ctrl Pts',(-0.128899900800441,6.76577222610794,
50.8088838476917));
#60860=CARTESIAN_POINT('Ctrl Pts',(-0.31486395994235,6.76222928260131,50.817632915281));
#60861=CARTESIAN_POINT('Ctrl Pts',(-0.500681721080927,6.75101488651275,
50.8263819828702));
#60862=CARTESIAN_POINT('Ctrl Pts',(-0.685722110173463,6.73216712415989,
50.8351310504595));
#60863=CARTESIAN_POINT('Ctrl Pts',(-0.870761373827964,6.71331947644141,
50.8438800648359));
#60864=CARTESIAN_POINT('Ctrl Pts',(-1.05502298984397,6.68683858439988,50.8526290792122));
#60865=CARTESIAN_POINT('Ctrl Pts',(-1.23788117676131,6.65281438131413,50.8613780935886));
#60866=CARTESIAN_POINT('Ctrl Pts',(-1.43009641451859,6.61704912302363,50.8705748044761));
#60867=CARTESIAN_POINT('Ctrl Pts',(-1.62076048992755,6.5729483708315,50.8797715153637));
#60868=CARTESIAN_POINT('Ctrl Pts',(-1.80915798961185,6.52067760042034,50.8889682262512));
#60869=CARTESIAN_POINT('Ctrl Pts',(-1.98840443003071,6.47094578577391,50.8977182239577));
#60870=CARTESIAN_POINT('Ctrl Pts',(-2.16559895952256,6.41381888474454,50.9064682216642));
#60871=CARTESIAN_POINT('Ctrl Pts',(-2.34013966242391,6.34949095285209,50.9152182193707));
#60872=CARTESIAN_POINT('Ctrl Pts',(-2.51467682554086,6.28516432556656,50.9239680396223));
#60873=CARTESIAN_POINT('Ctrl Pts',(-2.68656000078916,6.21363705879629,50.9327178598739));
#60874=CARTESIAN_POINT('Ctrl Pts',(-2.85520533840965,6.13515211510823,50.9414676801255));
#60875=CARTESIAN_POINT('Ctrl Pts',(-3.02384747998402,6.05666865881084,50.9502173345567));
#60876=CARTESIAN_POINT('Ctrl Pts',(-3.18925164684609,5.97122791039805,50.958966988988));
#60877=CARTESIAN_POINT('Ctrl Pts',(-3.35085601829228,5.87912008251868,50.9677166434192));
#60878=CARTESIAN_POINT('Ctrl Pts',(-3.51245754191484,5.78701387778134,50.9764661436624));
#60879=CARTESIAN_POINT('Ctrl Pts',(-3.67025915510997,5.68824097060943,50.9852156439055));
#60880=CARTESIAN_POINT('Ctrl Pts',(-3.82372487928891,5.58313684656816,50.9939651441487));
#60881=CARTESIAN_POINT('Ctrl Pts',(-3.97718810300834,5.47803443501746,51.0027145018338));
#60882=CARTESIAN_POINT('Ctrl Pts',(-4.12631534263042,5.36660117496362,51.0114638595189));
#60883=CARTESIAN_POINT('Ctrl Pts',(-4.27060009886224,5.24921554097352,51.020213217204));
#60884=CARTESIAN_POINT('Ctrl Pts',(-4.41488269594234,5.13183166360274,51.0289624439592));
#60885=CARTESIAN_POINT('Ctrl Pts',(-4.5543227323513,5.00849577139434,51.0377116707144));
#60886=CARTESIAN_POINT('Ctrl Pts',(-4.68844662480268,4.87962675277284,51.0464608974696));
#60887=CARTESIAN_POINT('Ctrl Pts',(-4.8225686883521,4.75075949139828,51.055210004921));
#60888=CARTESIAN_POINT('Ctrl Pts',(-4.95137454637907,4.61635945312477,51.0639591123725));
#60889=CARTESIAN_POINT('Ctrl Pts',(-5.07442674461115,4.47688309134549,51.072708219824));
#60890=CARTESIAN_POINT('Ctrl Pts',(-5.19747742838558,4.33740844616327,51.0814572195964));
#60891=CARTESIAN_POINT('Ctrl Pts',(-5.31477440450931,4.19285781736023,51.0902062193687));
#60892=CARTESIAN_POINT('Ctrl Pts',(-5.42591931531142,4.04372211999421,51.0989552191411));
#60893=CARTESIAN_POINT('Ctrl Pts',(-5.53707636462976,3.89457013500809,51.1077051744217));
#60894=CARTESIAN_POINT('Ctrl Pts',(-5.6420798327347,3.74083230916422,51.1164551297023));
#60895=CARTESIAN_POINT('Ctrl Pts',(-5.74057303468751,3.58303087251822,51.1252050849829));
#60896=CARTESIAN_POINT('Ctrl Pts',(-5.83906243363768,3.42523552887426,51.1339547024117));
#60897=CARTESIAN_POINT('Ctrl Pts',(-5.93104191768428,3.26337713156988,51.1427043198405));
#60898=CARTESIAN_POINT('Ctrl Pts',(-6.01619906699658,3.09800545291152,51.1514539372693));
#60899=CARTESIAN_POINT('Ctrl Pts',(-6.10135338095388,2.93263928039585,51.1602032633747));
#60900=CARTESIAN_POINT('Ctrl Pts',(-6.17968568352847,2.76376031540206,51.1689525894801));
#60901=CARTESIAN_POINT('Ctrl Pts',(-6.25092992694897,2.59194213831516,51.1777019155855));
#60902=CARTESIAN_POINT('Ctrl Pts',(-6.32217217691108,2.42012876880806,51.1864509968793));
#60903=CARTESIAN_POINT('Ctrl Pts',(-6.3863266548385,2.24537661647669,51.195200078173));
#60904=CARTESIAN_POINT('Ctrl Pts',(-6.44317547869346,2.06827917621469,51.2039491594668));
#60905=CARTESIAN_POINT('Ctrl Pts',(-6.50002944235934,1.89116572423432,51.2126990317818));
#60906=CARTESIAN_POINT('Ctrl Pts',(-6.54957634250397,1.71170683289203,51.2214489040967));
#60907=CARTESIAN_POINT('Ctrl Pts',(-6.59164787708395,1.53051209225365,51.2301987764117));
#60908=CARTESIAN_POINT('Ctrl Pts',(-6.63371649075014,1.34932993148009,51.2389480412465));
#60909=CARTESIAN_POINT('Ctrl Pts',(-6.66831071257132,1.16641244173961,51.2476973060813));
#60910=CARTESIAN_POINT('Ctrl Pts',(-6.69531304840342,0.982380875159358,
51.2564465709161));
#60911=CARTESIAN_POINT('Ctrl Pts',(-6.72231677033052,0.798339861795154,
51.2651962848718));
#60912=CARTESIAN_POINT('Ctrl Pts',(-6.74172778477897,0.61318494072943,51.2739459988274));
#60913=CARTESIAN_POINT('Ctrl Pts',(-6.75348015835523,0.427545027689796,
51.2826957127831));
#60914=CARTESIAN_POINT('Ctrl Pts',(-6.76249038365211,0.28521995354819,51.2894038805853));
#60915=CARTESIAN_POINT('Ctrl Pts',(-6.76699999999988,0.142609995760808,
51.2961120483875));
#60916=CARTESIAN_POINT('Ctrl Pts',(-6.767,5.55191001589178E-12,51.3028202161897));
#60917=CARTESIAN_POINT('Ctrl Pts',(-6.76699999999988,1.30184050356826E-6,
51.3028480745936));
#60918=CARTESIAN_POINT('Ctrl Pts',(-6.7670000339791,-0.176623542518988,
51.3111183913113));
#60919=CARTESIAN_POINT('Ctrl Pts',(-6.76008062728606,-0.353204966336715,
51.319388708029));
#60920=CARTESIAN_POINT('Ctrl Pts',(-6.74627795308297,-0.529171786612536,
51.3276590247467));
#60921=CARTESIAN_POINT('Ctrl Pts',(-6.73246948759393,-0.705212438535618,
51.3359328114998));
#60922=CARTESIAN_POINT('Ctrl Pts',(-6.71177202596096,-0.880637625385335,
51.3442065982531));
#60923=CARTESIAN_POINT('Ctrl Pts',(-6.68427351682208,-1.05488224570849,
51.3524803850062));
#60924=CARTESIAN_POINT('Ctrl Pts',(-6.65665801029845,-1.22986822130954,
51.3607893740828));
#60925=CARTESIAN_POINT('Ctrl Pts',(-6.62218351491507,-1.40366321268522,
51.3690983631594));
#60926=CARTESIAN_POINT('Ctrl Pts',(-6.58099054131082,-1.57570698265177,
51.3774073522359));
#60927=CARTESIAN_POINT('Ctrl Pts',(-6.53989629136811,-1.74733843009267,
51.3856964278721));
#60928=CARTESIAN_POINT('Ctrl Pts',(-6.49211587419647,-1.91722671861169,
51.3939855035082));
#60929=CARTESIAN_POINT('Ctrl Pts',(-6.43783827923141,-2.0848326768503,51.4022745791444));
#60930=CARTESIAN_POINT('Ctrl Pts',(-6.38336509183233,-2.25304261279556,
51.4105935249411));
#60931=CARTESIAN_POINT('Ctrl Pts',(-6.32234795000335,-2.41895341249869,
51.4189124707379));
#60932=CARTESIAN_POINT('Ctrl Pts',(-6.25502576616589,-2.58204215004341,
51.4272314165347));
#60933=CARTESIAN_POINT('Ctrl Pts',(-6.18770358232849,-2.74513088758802,
51.4355503623314));
#60934=CARTESIAN_POINT('Ctrl Pts',(-6.11407655201758,-2.90539726828797,
51.4438693081282));
#60935=CARTESIAN_POINT('Ctrl Pts',(-6.0344288562706,-3.06234507830334,51.452188253925));
#60936=CARTESIAN_POINT('Ctrl Pts',(-5.95354082525634,-3.22173700050624,
51.4606367487534));
#60937=CARTESIAN_POINT('Ctrl Pts',(-5.86626371181114,-3.37806009651829,
51.4690852435818));
#60938=CARTESIAN_POINT('Ctrl Pts',(-5.77285319420822,-3.53078673925798,
51.4775337384102));
#60939=CARTESIAN_POINT('Ctrl Pts',(-5.679528001687,-3.68337387508126,51.4859745160294));
#60940=CARTESIAN_POINT('Ctrl Pts',(-5.5800807456535,-3.8323708228384,51.4944152936486));
#60941=CARTESIAN_POINT('Ctrl Pts',(-5.4748131506473,-3.9772741878703,51.5028560712677));
#60942=CARTESIAN_POINT('Ctrl Pts',(-5.3696255235808,-4.12206747511848,51.511290436737));
#60943=CARTESIAN_POINT('Ctrl Pts',(-5.25862656714004,-4.26277311012421,
51.5197248022063));
#60944=CARTESIAN_POINT('Ctrl Pts',(-5.14216168741832,-4.39891602334566,
51.5281591676756));
#60945=CARTESIAN_POINT('Ctrl Pts',(-5.02576739655974,-4.53497642093242,
51.5365884211122));
#60946=CARTESIAN_POINT('Ctrl Pts',(-4.90391400364841,-4.66647935755995,
51.5450176745489));
#60947=CARTESIAN_POINT('Ctrl Pts',(-4.77698786484249,-4.79298194646585,
51.5534469279855));
#60948=CARTESIAN_POINT('Ctrl Pts',(-4.65011918532413,-4.91942726782465,
51.5618723655108));
#60949=CARTESIAN_POINT('Ctrl Pts',(-4.51818257479515,-5.04087652022402,
51.570297803036));
#60950=CARTESIAN_POINT('Ctrl Pts',(-4.38160226463412,-5.15692258954439,
51.5787232405613));
#60951=CARTESIAN_POINT('Ctrl Pts',(-4.24505195749479,-5.27294316666362,
51.5871468272445));
#60952=CARTESIAN_POINT('Ctrl Pts',(-4.10386023675893,-5.38356270951558,
51.5955704139276));
#60953=CARTESIAN_POINT('Ctrl Pts',(-3.9584859282339,-5.48841308175453,51.6039940006108));
#60954=CARTESIAN_POINT('Ctrl Pts',(-3.81312788633164,-5.59325172178666,
51.6124166447388));
#60955=CARTESIAN_POINT('Ctrl Pts',(-3.6635884600021,-5.69232228314028,51.6208392888668));
#60956=CARTESIAN_POINT('Ctrl Pts',(-3.51035733890251,-5.78529863993323,
51.6292619329948));
#60957=CARTESIAN_POINT('Ctrl Pts',(-3.35712199610203,-5.87827755833616,
51.6376848091767));
#60958=CARTESIAN_POINT('Ctrl Pts',(-3.20019504098331,-5.96516176480793,
51.6461076853586));
#60959=CARTESIAN_POINT('Ctrl Pts',(-3.04009307362458,-6.04566978123184,
51.6545305615406));
#60960=CARTESIAN_POINT('Ctrl Pts',(-2.87996436834894,-6.12619124294121,
51.6629548443895));
#60961=CARTESIAN_POINT('Ctrl Pts',(-2.71665989177677,-6.20033424236853,
51.6713791272386));
#60962=CARTESIAN_POINT('Ctrl Pts',(-2.55071897302026,-6.26786420726187,
51.6798034100875));
#60963=CARTESIAN_POINT('Ctrl Pts',(-2.38466598390274,-6.33543977939665,
51.6882333823857));
#60964=CARTESIAN_POINT('Ctrl Pts',(-2.21597330377069,-6.39639326673437,
51.6966633546838));
#60965=CARTESIAN_POINT('Ctrl Pts',(-2.0451992380346,-6.45053866562652,51.705093326982));
#60966=CARTESIAN_POINT('Ctrl Pts',(-1.87436412332623,-6.50470342062488,
51.7135263128592));
#60967=CARTESIAN_POINT('Ctrl Pts',(-1.70144645902587,-6.55205513943922,
51.7219592987364));
#60968=CARTESIAN_POINT('Ctrl Pts',(-1.52701824724029,-6.59245813582424,
51.7303922846136));
#60969=CARTESIAN_POINT('Ctrl Pts',(-1.3524295625626,-6.63289830271977,51.7388330287864));
#60970=CARTESIAN_POINT('Ctrl Pts',(-1.17632788015482,-6.66637690539049,
51.7472737729592));
#60971=CARTESIAN_POINT('Ctrl Pts',(-0.99929498448611,-6.69280946493929,
51.755714517132));
#60972=CARTESIAN_POINT('Ctrl Pts',(-0.901408768343539,-6.70742473306458,
51.7603816300173));
#60973=CARTESIAN_POINT('Ctrl Pts',(-0.803237970703355,-6.71988674641108,
51.7650487429027));
#60974=CARTESIAN_POINT('Ctrl Pts',(-0.704881448882504,-6.73018804663149,
51.769715855788));
#60975=CARTESIAN_POINT('Ctrl Pts',(-0.53330716257365,-6.74815775723785,
51.777857223006));
#60976=CARTESIAN_POINT('Ctrl Pts',(-0.360826604970594,-6.75958510253059,
51.7859985902239));
#60977=CARTESIAN_POINT('Ctrl Pts',(-0.187984118427604,-6.76438844029665,
51.7941399574419));
#60978=CARTESIAN_POINT('Ctrl Pts',(-0.0152925102300434,-6.76918758511416,
51.8022742178654));
#60979=CARTESIAN_POINT('Ctrl Pts',(0.157760034616686,-6.76737422195983,
51.810408478289));
#60980=CARTESIAN_POINT('Ctrl Pts',(0.330622948664547,-6.75891836508005,
51.8185427387125));
#60981=CARTESIAN_POINT('Ctrl Pts',(0.503367941876163,-6.75046827648041,
51.8266714502374));
#60982=CARTESIAN_POINT('Ctrl Pts',(0.675923197719367,-6.73538473358101,
51.8348001617624));
#60983=CARTESIAN_POINT('Ctrl Pts',(0.847737076126017,-6.71368980887271,
51.8429288732873));
#60984=CARTESIAN_POINT('Ctrl Pts',(1.01946901967,-6.69200523007299,51.8510537083799));
#60985=CARTESIAN_POINT('Ctrl Pts',(1.19045992742188,-6.66371559364873,51.8591785434725));
#60986=CARTESIAN_POINT('Ctrl Pts',(1.36016223062419,-6.6288949083828,51.8673033785652));
#60987=CARTESIAN_POINT('Ctrl Pts',(1.52981702519052,-6.59408397126542,51.8754259390874));
#60988=CARTESIAN_POINT('Ctrl Pts',(1.69818357564917,-6.55274570142064,51.8835484996097));
#60989=CARTESIAN_POINT('Ctrl Pts',(1.86472350392635,-6.50500539999043,51.8916710601319));
#60990=CARTESIAN_POINT('Ctrl Pts',(2.03127228336902,-6.45726256128695,51.8997940523472));
#60991=CARTESIAN_POINT('Ctrl Pts',(2.19599389372482,-6.40311710838076,51.9079170445625));
#60992=CARTESIAN_POINT('Ctrl Pts',(2.35836396200425,-6.34274454969768,51.9160400367778));
#60993=CARTESIAN_POINT('Ctrl Pts',(2.44124893369111,-6.31192619832211,51.9201865767584));
#60994=CARTESIAN_POINT('Ctrl Pts',(2.52352140191928,-6.2794859902824,51.924333116739));
#60995=CARTESIAN_POINT('Ctrl Pts',(2.60511347837492,-6.24545216656003,51.9284796567196));
#60996=CARTESIAN_POINT('Ctrl Pts',(2.78188625705105,-6.17171640875458,51.9374633157477));
#60997=CARTESIAN_POINT('Ctrl Pts',(2.95537670176367,-6.0905341743684,51.9464469747757));
#60998=CARTESIAN_POINT('Ctrl Pts',(3.12499490347401,-6.00222424216736,51.9554306338037));
#60999=CARTESIAN_POINT('Ctrl Pts',(3.29490450745654,-5.91376259443909,51.9644297266627));
#61000=CARTESIAN_POINT('Ctrl Pts',(3.46092835986613,-5.81814888441678,51.9734288195217));
#61001=CARTESIAN_POINT('Ctrl Pts',(3.62250298626108,-5.7157467678799,51.9824279123807));
#61002=CARTESIAN_POINT('Ctrl Pts',(3.78445646000414,-5.61310454699523,51.9914481055977));
#61003=CARTESIAN_POINT('Ctrl Pts',(3.94193963195968,-5.50364220120201,52.0004682988147));
#61004=CARTESIAN_POINT('Ctrl Pts',(4.09441750374241,-5.3877670982558,52.0094884920317));
#61005=CARTESIAN_POINT('Ctrl Pts',(4.24704979755183,-5.27177464275194,52.0185178204531));
#61006=CARTESIAN_POINT('Ctrl Pts',(4.39466647775626,-5.14935660501642,52.0275471488744));
#61007=CARTESIAN_POINT('Ctrl Pts',(4.53676606718758,-5.02096033161141,52.0365764772958));
#61008=CARTESIAN_POINT('Ctrl Pts',(4.67906598839709,-4.89238304534164,52.0456185352502));
#61009=CARTESIAN_POINT('Ctrl Pts',(4.81583308913101,-4.75781083171856,52.0546605932046));
#61010=CARTESIAN_POINT('Ctrl Pts',(4.9466015016186,-4.61772915881655,52.063702651159));
#61011=CARTESIAN_POINT('Ctrl Pts',(5.06008576626844,-4.49616260204803,52.0715495866563));
#61012=CARTESIAN_POINT('Ctrl Pts',(5.16905281435452,-4.37044738490407,52.0793965221536));
#61013=CARTESIAN_POINT('Ctrl Pts',(5.27322252168006,-4.24092127218205,52.087243457651));
#61014=CARTESIAN_POINT('Ctrl Pts',(5.38809906729759,-4.09808212269426,52.0958969219522));
#61015=CARTESIAN_POINT('Ctrl Pts',(5.49724163451786,-3.9504816874404,52.1045503862535));
#61016=CARTESIAN_POINT('Ctrl Pts',(5.60026293498195,-3.79859764374531,52.1132038505548));
#61017=CARTESIAN_POINT('Ctrl Pts',(5.70318933175574,-3.6468535163217,52.1218493432454));
#61018=CARTESIAN_POINT('Ctrl Pts',(5.80000553872059,-3.49083390173163,52.130494835936));
#61019=CARTESIAN_POINT('Ctrl Pts',(5.8903658238081,-3.33104780237593,52.1391403286267));
#61020=CARTESIAN_POINT('Ctrl Pts',(5.98344444294921,-3.16645481252903,52.148045906123));
#61021=CARTESIAN_POINT('Ctrl Pts',(6.06967243221642,-2.99786542904594,52.1569514836193));
#61022=CARTESIAN_POINT('Ctrl Pts',(6.14872001898878,-2.82586820784103,52.1658570611157));
#61023=CARTESIAN_POINT('Ctrl Pts',(6.22531343434019,-2.65921094300921,52.1744861492886));
#61024=CARTESIAN_POINT('Ctrl Pts',(6.29516546568033,-2.48935456885595,52.1831152374617));
#61025=CARTESIAN_POINT('Ctrl Pts',(6.35802242980817,-2.31685989694159,52.1917443256347));
#61026=CARTESIAN_POINT('Ctrl Pts',(6.42390044537226,-2.13607473114859,52.2007881477927));
#61027=CARTESIAN_POINT('Ctrl Pts',(6.48209425047706,-1.95239170379207,52.2098319699507));
#61028=CARTESIAN_POINT('Ctrl Pts',(6.53236815440517,-1.76648104867085,52.2188757921087));
#61029=CARTESIAN_POINT('Ctrl Pts',(6.58264205833331,-1.58057039354951,52.2279196142667));
#61030=CARTESIAN_POINT('Ctrl Pts',(6.62499592706467,-1.3924324735803,52.2369634364247));
#61031=CARTESIAN_POINT('Ctrl Pts',(6.65925397533326,-1.20275745352427,52.2460072585827));
#61032=CARTESIAN_POINT('Ctrl Pts',(6.6911709138044,-1.02604435249828,52.2544330484321));
#61033=CARTESIAN_POINT('Ctrl Pts',(6.71604695694967,-0.848074481819348,
52.2628588382814));
#61034=CARTESIAN_POINT('Ctrl Pts',(6.73380635353076,-0.669433337344986,
52.2712846281308));
#61035=CARTESIAN_POINT('Ctrl Pts',(6.75156987088937,-0.490750742114677,
52.2797123730469));
#61036=CARTESIAN_POINT('Ctrl Pts',(6.76221341643423,-0.311396892409265,
52.288140117963));
#61037=CARTESIAN_POINT('Ctrl Pts',(6.76571320457185,-0.131961484843546,
52.2965678628792));
#61038=CARTESIAN_POINT('Ctrl Pts',(6.76921427870605,0.0475398562333889,
52.3049987045688));
#61039=CARTESIAN_POINT('Ctrl Pts',(6.76556635501422,0.227122483642489,52.3134295462584));
#61040=CARTESIAN_POINT('Ctrl Pts',(6.75479776247298,0.406197228067859,52.321860387948));
#61041=CARTESIAN_POINT('Ctrl Pts',(6.74401927496982,0.585436519324339,52.3302989765049));
#61042=CARTESIAN_POINT('Ctrl Pts',(6.72610706626208,0.764166664077337,52.3387375650618));
#61043=CARTESIAN_POINT('Ctrl Pts',(6.70114140146456,0.941803014211341,52.3471761536188));
#61044=CARTESIAN_POINT('Ctrl Pts',(6.67616264577572,1.11953250899722,52.3556191669986));
#61045=CARTESIAN_POINT('Ctrl Pts',(6.64412311152221,1.29616673850666,52.3640621803784));
#61046=CARTESIAN_POINT('Ctrl Pts',(6.60515420132416,1.47113118950344,52.3725051937583));
#61047=CARTESIAN_POINT('Ctrl Pts',(6.56614435156976,1.64627945285122,52.3809570771121));
#61048=CARTESIAN_POINT('Ctrl Pts',(6.52019066354873,1.81975411200359,52.389408960466));
#61049=CARTESIAN_POINT('Ctrl Pts',(6.46747470330079,1.99099471675952,52.3978608438199));
#61050=CARTESIAN_POINT('Ctrl Pts',(6.453107938696,2.03766319150115,52.4001642490512));
#61051=CARTESIAN_POINT('Ctrl Pts',(6.43823919613608,2.08416584121069,52.4024676542827));
#61052=CARTESIAN_POINT('Ctrl Pts',(6.4228727731184,2.13049157246264,52.404771059514));
#61053=CARTESIAN_POINT('Ctrl Pts',(6.36738086532369,2.29778510617565,52.4130892185655));
#61054=CARTESIAN_POINT('Ctrl Pts',(6.3052951123939,2.46307085402694,52.421407377617));
#61055=CARTESIAN_POINT('Ctrl Pts',(6.23678219864711,2.62580212632988,52.4297255366685));
#61056=CARTESIAN_POINT('Ctrl Pts',(6.16832901318762,2.78839153252826,52.4380364441033));
#61057=CARTESIAN_POINT('Ctrl Pts',(6.09345996602735,2.94843058148975,52.446347351538));
#61058=CARTESIAN_POINT('Ctrl Pts',(6.0123910045044,3.10538941341575,52.4546582589727));
#61059=CARTESIAN_POINT('Ctrl Pts',(5.93138455436805,3.26222721610888,52.4629627579579));
#61060=CARTESIAN_POINT('Ctrl Pts',(5.84418788003804,3.41598922888365,52.4712672569432));
#61061=CARTESIAN_POINT('Ctrl Pts',(5.75106434729964,3.56616711235171,52.4795717559284));
#61062=CARTESIAN_POINT('Ctrl Pts',(5.65798147319061,3.71627942671255,52.4878726290895));
#61063=CARTESIAN_POINT('Ctrl Pts',(5.55897707888453,3.86281043432944,52.4961735022507));
#61064=CARTESIAN_POINT('Ctrl Pts',(5.45435986044519,4.00527745765064,52.5044743754119));
#61065=CARTESIAN_POINT('Ctrl Pts',(5.34977095072652,4.14770593034672,52.5127730024122));
#61066=CARTESIAN_POINT('Ctrl Pts',(5.2395724489538,4.28607232998326,52.5210716294125));
#61067=CARTESIAN_POINT('Ctrl Pts',(5.12411577081687,4.41992381916994,52.5293702564128));
#61068=CARTESIAN_POINT('Ctrl Pts',(5.00867116985319,4.55376130702166,52.5376680153476));
#61069=CARTESIAN_POINT('Ctrl Pts',(4.8879697163121,4.68308456287043,52.5459657742825));
#61070=CARTESIAN_POINT('Ctrl Pts',(4.76240254220935,4.8074744956118,52.5542635332173));
#61071=CARTESIAN_POINT('Ctrl Pts',(4.6367879929511,4.93191135934806,52.5625644228081));
#61072=CARTESIAN_POINT('Ctrl Pts',(4.50630429949227,5.05141093309213,52.5708653123988));
#61073=CARTESIAN_POINT('Ctrl Pts',(4.37137935344313,5.16559111315357,52.5791662019896));
#61074=CARTESIAN_POINT('Ctrl Pts',(4.23643146787009,5.27979070577766,52.5874685028721));
#61075=CARTESIAN_POINT('Ctrl Pts',(4.09704109408353,5.38866888184995,52.5957708037545));
#61076=CARTESIAN_POINT('Ctrl Pts',(3.95366873319091,5.49188424388102,52.604073104637));
#61077=CARTESIAN_POINT('Ctrl Pts',(3.81017955451864,5.59518370433485,52.6123821701172));
#61078=CARTESIAN_POINT('Ctrl Pts',(3.66270219075019,5.69281093105934,52.6206912355975));
#61079=CARTESIAN_POINT('Ctrl Pts',(3.51172644757303,5.78446768142204,52.6290003010777));
#61080=CARTESIAN_POINT('Ctrl Pts',(3.37684927108676,5.86635105841143,52.6364233696292));
#61081=CARTESIAN_POINT('Ctrl Pts',(3.23918053584598,5.94346986229731,52.6438464381807));
#61082=CARTESIAN_POINT('Ctrl Pts',(3.09908550384727,6.01564277861009,52.6512695067322));
#61083=CARTESIAN_POINT('Origin',(0.,0.,-63.6971797838103));
#61084=CARTESIAN_POINT('',(3.09908550384712,6.01564277861017,55.0459286315074));
#61085=CARTESIAN_POINT('',(3.09908550384732,6.01564277861007,54.6514561368909));
#61086=CARTESIAN_POINT('',(3.09908550384721,6.01564277861012,-63.6971797838103));
#61087=CARTESIAN_POINT('',(-6.76699920371004,0.00328283226919929,53.6971797837668));
#61088=CARTESIAN_POINT('Ctrl Pts',(-6.76699920371048,0.00328283135813808,
53.6971797838098));
#61089=CARTESIAN_POINT('Ctrl Pts',(-6.76708603743267,-0.175710136846427,
53.7056136196247));
#61090=CARTESIAN_POINT('Ctrl Pts',(-6.76006682462507,-0.35484151860626,
53.7140474554396));
#61091=CARTESIAN_POINT('Ctrl Pts',(-6.7459351913362,-0.533523564889031,
53.7224812912544));
#61092=CARTESIAN_POINT('Ctrl Pts',(-6.73181716702949,-0.712033537588325,
53.7309070051545));
#61093=CARTESIAN_POINT('Ctrl Pts',(-6.71060041001333,-0.890094707423162,
53.7393327190547));
#61094=CARTESIAN_POINT('Ctrl Pts',(-6.68233058255984,-1.06712088602251,
53.7477584329548));
#61095=CARTESIAN_POINT('Ctrl Pts',(-6.65407696605256,-1.24404555137908,
53.7561793152444));
#61096=CARTESIAN_POINT('Ctrl Pts',(-6.61877839217973,-1.41993608078952,
53.764600197534));
#61097=CARTESIAN_POINT('Ctrl Pts',(-6.57653226760037,-1.59421213557394,
53.7730210798236));
#61098=CARTESIAN_POINT('Ctrl Pts',(-6.53430748982804,-1.76840012932673,
53.7814377070733));
#61099=CARTESIAN_POINT('Ctrl Pts',(-6.4851422404297,-1.94097495261594,53.7898543343229));
#61100=CARTESIAN_POINT('Ctrl Pts',(-6.42918491865352,-2.1113669225784,53.7982709615725));
#61101=CARTESIAN_POINT('Ctrl Pts',(-6.40715469026425,-2.17844972595102,
53.801584562272));
#61102=CARTESIAN_POINT('Ctrl Pts',(-6.38407226218484,-2.24519432628294,
53.8048981629714));
#61103=CARTESIAN_POINT('Ctrl Pts',(-6.35994882873542,-2.3115665458444,53.8082117636709));
#61104=CARTESIAN_POINT('Ctrl Pts',(-6.29860800963492,-2.48033714485365,
53.8166375535363));
#61105=CARTESIAN_POINT('Ctrl Pts',(-6.23055026012783,-2.64665081014075,
53.8250633434016));
#61106=CARTESIAN_POINT('Ctrl Pts',(-6.15600474122764,-2.80996345634296,
53.833489133267));
#61107=CARTESIAN_POINT('Ctrl Pts',(-6.08144192525173,-2.97331399658961,
53.8419168781999));
#61108=CARTESIAN_POINT('Ctrl Pts',(-6.00038847602705,-3.13366182778156,
53.8503446231329));
#61109=CARTESIAN_POINT('Ctrl Pts',(-5.9131205754788,-3.29048538362492,53.8587723680658));
#61110=CARTESIAN_POINT('Ctrl Pts',(-5.82582060834682,-3.44736656427252,
53.867203209773));
#61111=CARTESIAN_POINT('Ctrl Pts',(-5.73230179791808,-3.60072059793408,
53.8756340514802));
#61112=CARTESIAN_POINT('Ctrl Pts',(-5.63288509655736,-3.75005259816206,
53.8840648931874));
#61113=CARTESIAN_POINT('Ctrl Pts',(-5.53337704392559,-3.89952181545561,
53.892503481763));
#61114=CARTESIAN_POINT('Ctrl Pts',(-5.42796045673013,-4.04496133944536,
53.9009420703386));
#61115=CARTESIAN_POINT('Ctrl Pts',(-5.31699889383973,-4.18590632514717,
53.9093806589143));
#61116=CARTESIAN_POINT('Ctrl Pts',(-5.20597914760166,-4.32692521618063,
53.9178236723134));
#61117=CARTESIAN_POINT('Ctrl Pts',(-5.08940883785281,-4.46344461334333,
53.9262666857126));
#61118=CARTESIAN_POINT('Ctrl Pts',(-4.96769061499627,-4.59503416240598,
53.9347096991117));
#61119=CARTESIAN_POINT('Ctrl Pts',(-4.84584451865206,-4.72676195547338,
53.9431615824857));
#61120=CARTESIAN_POINT('Ctrl Pts',(-4.71883993640617,-4.85354931693117,
53.9516134658596));
#61121=CARTESIAN_POINT('Ctrl Pts',(-4.58711579176472,-4.97500328773185,
53.9600653492335));
#61122=CARTESIAN_POINT('Ctrl Pts',(-4.55121680260995,-5.00810333019139,
53.9623687543565));
#61123=CARTESIAN_POINT('Ctrl Pts',(-4.51496746341224,-5.0408074754383,53.9646721594794));
#61124=CARTESIAN_POINT('Ctrl Pts',(-4.47837707016986,-5.07310829939366,
53.9669755646023));
#61125=CARTESIAN_POINT('Ctrl Pts',(-4.34625441333081,-5.18974193737625,
53.9752928298091));
#61126=CARTESIAN_POINT('Ctrl Pts',(-4.20944489272645,-5.30132355843371,
53.9836100950158));
#61127=CARTESIAN_POINT('Ctrl Pts',(-4.06836751014018,-5.4074647296525,53.9919273602225));
#61128=CARTESIAN_POINT('Ctrl Pts',(-3.92740911549309,-5.51351637894372,
54.0002376104548));
#61129=CARTESIAN_POINT('Ctrl Pts',(-3.78219030721473,-5.61413651256725,
54.008547860687));
#61130=CARTESIAN_POINT('Ctrl Pts',(-3.63316421449497,-5.70897598440501,
54.0168581109192));
#61131=CARTESIAN_POINT('Ctrl Pts',(-3.48423652142652,-5.80375283518905,
54.0251628740202));
#61132=CARTESIAN_POINT('Ctrl Pts',(-3.33150684562223,-5.8927564436729,54.0334676371213));
#61133=CARTESIAN_POINT('Ctrl Pts',(-3.17545861822658,-5.97568000849532,
54.0417724002223));
#61134=CARTESIAN_POINT('Ctrl Pts',(-3.01948486146417,-6.05856399984429,
54.0500732000551));
#61135=CARTESIAN_POINT('Ctrl Pts',(-2.86019601580814,-6.13537356719643,
54.058373999888));
#61136=CARTESIAN_POINT('Ctrl Pts',(-2.69810171373961,-6.2058469319115,54.0666747997209));
#61137=CARTESIAN_POINT('Ctrl Pts',(-2.53605510534114,-6.27629956095998,
54.0749731571754));
#61138=CARTESIAN_POINT('Ctrl Pts',(-2.37120500452698,-6.34041956500934,
54.0832715146299));
#61139=CARTESIAN_POINT('Ctrl Pts',(-2.20408290716049,-6.39799246157441,
54.0915698720845));
#61140=CARTESIAN_POINT('Ctrl Pts',(-2.03694380551152,-6.45557121604703,
54.0998690738775));
#61141=CARTESIAN_POINT('Ctrl Pts',(-1.86753257180285,-6.50660141160177,
54.1081682756705));
#61142=CARTESIAN_POINT('Ctrl Pts',(-1.69639838236628,-6.55091760964104,
54.1164674774635));
#61143=CARTESIAN_POINT('Ctrl Pts',(-1.52524684317089,-6.5952383005017,54.124767520638));
#61144=CARTESIAN_POINT('Ctrl Pts',(-1.35237233685554,-6.63284354936003,
54.1330675638126));
#61145=CARTESIAN_POINT('Ctrl Pts',(-1.17833673677863,-6.6636185015919,54.1413676069872));
#61146=CARTESIAN_POINT('Ctrl Pts',(-1.00425460250013,-6.69440168253003,
54.1496698694541));
#61147=CARTESIAN_POINT('Ctrl Pts',(-0.829011098310984,-6.71835086624514,
54.1579721319211));
#61148=CARTESIAN_POINT('Ctrl Pts',(-0.653175958323883,-6.73540274723551,
54.166274394388));
#61149=CARTESIAN_POINT('Ctrl Pts',(-0.477264610449473,-6.75246201860204,
54.1745802550998));
#61150=CARTESIAN_POINT('Ctrl Pts',(-0.300761461791976,-6.76261799591101,
54.1828861158115));
#61151=CARTESIAN_POINT('Ctrl Pts',(-0.12423920052669,-6.76585941481587,
54.1911919765233));
#61152=CARTESIAN_POINT('Ctrl Pts',(0.0524917225304711,-6.76910466530701,
54.1995076553496));
#61153=CARTESIAN_POINT('Ctrl Pts',(0.229241455126148,-6.76541902060758,
54.2078233341759));
#61154=CARTESIAN_POINT('Ctrl Pts',(0.405438289691852,-6.75484335815804,
54.2161390130022));
#61155=CARTESIAN_POINT('Ctrl Pts',(0.581746567362717,-6.74426100668559,
54.2244599514297));
#61156=CARTESIAN_POINT('Ctrl Pts',(0.757500903913943,-6.72677998111688,
54.2327808898571));
#61157=CARTESIAN_POINT('Ctrl Pts',(0.932136719472763,-6.70249283000068,
54.2411018282845));
#61158=CARTESIAN_POINT('Ctrl Pts',(1.10703209799069,-6.6781695806489,54.2494351342059));
#61159=CARTESIAN_POINT('Ctrl Pts',(1.28080529089778,-6.6470200506663,54.2577684401274));
#61160=CARTESIAN_POINT('Ctrl Pts',(1.45290255069757,-6.60918778505926,54.2661017460488));
#61161=CARTESIAN_POINT('Ctrl Pts',(1.57957632858622,-6.58134099646945,54.2722355528544));
#61162=CARTESIAN_POINT('Ctrl Pts',(1.7053423704799,-6.54987467526457,54.2783693596598));
#61163=CARTESIAN_POINT('Ctrl Pts',(1.82998604543604,-6.51486301264343,54.2845031664653));
#61164=CARTESIAN_POINT('Ctrl Pts',(1.99400337844069,-6.46879152502724,54.2925745799066));
#61165=CARTESIAN_POINT('Ctrl Pts',(2.15658146711973,-6.41643724252702,54.3006459933478));
#61166=CARTESIAN_POINT('Ctrl Pts',(2.31719014143117,-6.35790207918101,54.308717406789));
#61167=CARTESIAN_POINT('Ctrl Pts',(2.47759718485303,-6.29944040188491,54.3167786872391));
#61168=CARTESIAN_POINT('Ctrl Pts',(2.63603938745271,-6.23481340941637,54.3248399676892));
#61169=CARTESIAN_POINT('Ctrl Pts',(2.79199755016757,-6.16417380350833,54.3329012481394));
#61170=CARTESIAN_POINT('Ctrl Pts',(2.94779412266858,-6.09360738818438,54.3409541761954));
#61171=CARTESIAN_POINT('Ctrl Pts',(3.10111144025382,-6.01704090937111,54.3490071042514));
#61172=CARTESIAN_POINT('Ctrl Pts',(3.25144633841069,-5.93467654623533,54.3570600323075));
#61173=CARTESIAN_POINT('Ctrl Pts',(3.40165839257871,-5.85237948594827,54.3651063800298));
#61174=CARTESIAN_POINT('Ctrl Pts',(3.54889255243549,-5.76429414918577,54.3731527277521));
#61175=CARTESIAN_POINT('Ctrl Pts',(3.69266659323872,-5.67067036876406,54.3811990754744));
#61176=CARTESIAN_POINT('Ctrl Pts',(3.83635460148843,-5.57710261161927,54.3892406083648));
#61177=CARTESIAN_POINT('Ctrl Pts',(3.97658630068248,-5.47800321130974,54.3972821412551));
#61178=CARTESIAN_POINT('Ctrl Pts',(4.11290509995189,-5.3736673360741,54.4053236741455));
#61179=CARTESIAN_POINT('Ctrl Pts',(4.25184458684422,-5.26732563524198,54.4135198030698));
#61180=CARTESIAN_POINT('Ctrl Pts',(4.38671884754325,-5.15554426260775,54.4217159319941));
#61181=CARTESIAN_POINT('Ctrl Pts',(4.51707610318979,-5.03868162101871,54.4299120609184));
#61182=CARTESIAN_POINT('Ctrl Pts',(4.64493040063383,-4.92406283080473,54.4379508179494));
#61183=CARTESIAN_POINT('Ctrl Pts',(4.7684393074851,-4.80455640640591,54.4459895749804));
#61184=CARTESIAN_POINT('Ctrl Pts',(4.88721097112896,-4.68054034526749,54.4540283320115));
#61185=CARTESIAN_POINT('Ctrl Pts',(5.00599413059985,-4.55651228070045,54.4620678671082));
#61186=CARTESIAN_POINT('Ctrl Pts',(5.12003887546847,-4.42797397994076,54.470107402205));
#61187=CARTESIAN_POINT('Ctrl Pts',(5.22899137774639,-4.29533912182192,54.4781469373018));
#61188=CARTESIAN_POINT('Ctrl Pts',(5.33797599809285,-4.16266516432148,54.4861888423701));
#61189=CARTESIAN_POINT('Ctrl Pts',(5.44186515093747,-4.02589253415222,54.4942307474385));
#61190=CARTESIAN_POINT('Ctrl Pts',(5.54034643447907,-3.88546655962383,54.5022726525069));
#61191=CARTESIAN_POINT('Ctrl Pts',(5.64214970959698,-3.74030370629267,54.5105858288254));
#61192=CARTESIAN_POINT('Ctrl Pts',(5.73817364412583,-3.59123708396416,54.5188990051438));
#61193=CARTESIAN_POINT('Ctrl Pts',(5.8281234671109,-3.43878842793669,54.5272121814623));
#61194=CARTESIAN_POINT('Ctrl Pts',(5.91528917306922,-3.29105834594156,54.5352680492618));
#61195=CARTESIAN_POINT('Ctrl Pts',(5.99675106521978,-3.14015283067604,54.5433239170613));
#61196=CARTESIAN_POINT('Ctrl Pts',(6.07228927373558,-2.98656859557516,54.5513797848608));
#61197=CARTESIAN_POINT('Ctrl Pts',(6.15144657550925,-2.82562602247965,54.5598216154387));
#61198=CARTESIAN_POINT('Ctrl Pts',(6.22409841601709,-2.66174218003829,54.5682634460166));
#61199=CARTESIAN_POINT('Ctrl Pts',(6.29005010226811,-2.4955077060504,54.5767052765946));
#61200=CARTESIAN_POINT('Ctrl Pts',(6.35600178851914,-2.32927323206251,54.5851471071725));
#61201=CARTESIAN_POINT('Ctrl Pts',(6.41525324836093,-2.1606885899224,54.5935889377505));
#61202=CARTESIAN_POINT('Ctrl Pts',(6.46767094968941,-1.99035712537818,54.6020307683284));
#61203=CARTESIAN_POINT('Ctrl Pts',(6.51877616789689,-1.82429057834318,54.6102612245068));
#61204=CARTESIAN_POINT('Ctrl Pts',(6.5635560881325,-1.6560114131142,54.6184916806853));
#61205=CARTESIAN_POINT('Ctrl Pts',(6.60181548125312,-1.48604217688688,54.6267221368637));
#61206=CARTESIAN_POINT('Ctrl Pts',(6.64002945822782,-1.31627470412216,54.6349428230074));
#61207=CARTESIAN_POINT('Ctrl Pts',(6.67173824269077,-1.14482150151238,54.643163509151));
#61208=CARTESIAN_POINT('Ctrl Pts',(6.69679574766902,-0.972222049740749,
54.6513841952947));
#61209=CARTESIAN_POINT('Ctrl Pts',(6.72182853522794,-0.799792854865408,
54.6595967723251));
#61210=CARTESIAN_POINT('Ctrl Pts',(6.74022305831992,-0.626220014951361,
54.6678093493556));
#61211=CARTESIAN_POINT('Ctrl Pts',(6.75188382348002,-0.452055122998117,
54.676021926386));
#61212=CARTESIAN_POINT('Ctrl Pts',(6.76353542480675,-0.278027101827061,
54.684228049407));
#61213=CARTESIAN_POINT('Ctrl Pts',(6.7684637845503,-0.103408311454082,54.692434172428));
#61214=CARTESIAN_POINT('Ctrl Pts',(6.76662497176018,0.0712424841759877,
54.7006402954491));
#61215=CARTESIAN_POINT('Ctrl Pts',(6.76478723534056,0.245791045927125,54.7088416149204));
#61216=CARTESIAN_POINT('Ctrl Pts',(6.75619022140809,0.420371218071724,54.7170429343917));
#61217=CARTESIAN_POINT('Ctrl Pts',(6.74084203881244,0.594422078811799,54.725244253863));
#61218=CARTESIAN_POINT('Ctrl Pts',(6.72549825924385,0.768423008516526,54.7334432205716));
#61219=CARTESIAN_POINT('Ctrl Pts',(6.70340719629511,0.941894572244566,54.7416421872802));
#61220=CARTESIAN_POINT('Ctrl Pts',(6.67462899987217,1.11427856214928,54.7498411539888));
#61221=CARTESIAN_POINT('Ctrl Pts',(6.64585460373696,1.28663978798802,54.7580390379876));
#61222=CARTESIAN_POINT('Ctrl Pts',(6.61039489109573,1.45791337229763,54.7662369219865));
#61223=CARTESIAN_POINT('Ctrl Pts',(6.56836155679014,1.62754891148666,54.7744348059854));
#61224=CARTESIAN_POINT('Ctrl Pts',(6.52632613769632,1.7971928643355,54.7826330965866));
#61225=CARTESIAN_POINT('Ctrl Pts',(6.47771653360083,1.96519826208167,54.7908313871879));
#61226=CARTESIAN_POINT('Ctrl Pts',(6.42269498685902,2.13102747654177,54.7990296777891));
#61227=CARTESIAN_POINT('Ctrl Pts',(6.36766071633917,2.29689503914444,54.8072298642518));
#61228=CARTESIAN_POINT('Ctrl Pts',(6.30621166284734,2.46058507585072,54.8154300507144));
#61229=CARTESIAN_POINT('Ctrl Pts',(6.23855912760033,2.62157758066295,54.8236302371771));
#61230=CARTESIAN_POINT('Ctrl Pts',(6.17084263218773,2.78272229126066,54.8318381762729));
#61231=CARTESIAN_POINT('Ctrl Pts',(6.09691107670023,2.94116404370452,54.8400461153687));
#61232=CARTESIAN_POINT('Ctrl Pts',(6.01702328136955,3.09640433914191,54.8482540544645));
#61233=CARTESIAN_POINT('Ctrl Pts',(5.9370967300461,3.25171994635556,54.8564659754805));
#61234=CARTESIAN_POINT('Ctrl Pts',(5.85120835399626,3.40383068791653,54.8646778964966));
#61235=CARTESIAN_POINT('Ctrl Pts',(5.75966163813225,3.55226502589936,54.8728898175126));
#61236=CARTESIAN_POINT('Ctrl Pts',(5.66798938045788,3.70090291804941,54.8811129998766));
#61237=CARTESIAN_POINT('Ctrl Pts',(5.57064347575273,3.84585403334481,54.8893361822407));
#61238=CARTESIAN_POINT('Ctrl Pts',(5.46796992541074,3.98667704922328,54.8975593646048));
#61239=CARTESIAN_POINT('Ctrl Pts',(5.37641104923287,4.1122556138182,54.904892366467));
#61240=CARTESIAN_POINT('Ctrl Pts',(5.28061624399103,4.23455177911574,54.9122253683293));
#61241=CARTESIAN_POINT('Ctrl Pts',(5.18085617329314,4.35327673272104,54.9195583701915));
#61242=CARTESIAN_POINT('Ctrl Pts',(5.05927297191148,4.4979735021022,54.9284955114336));
#61243=CARTESIAN_POINT('Ctrl Pts',(4.93154733487648,4.63766584221061,54.9374326526757));
#61244=CARTESIAN_POINT('Ctrl Pts',(4.79809671928477,4.7718504662645,54.9463697939178));
#61245=CARTESIAN_POINT('Ctrl Pts',(4.66494098883499,4.90573858324173,54.9552871868047));
#61246=CARTESIAN_POINT('Ctrl Pts',(4.52608571207779,5.03414309339944,54.9642045796915));
#61247=CARTESIAN_POINT('Ctrl Pts',(4.38198602301382,5.15659650293791,54.9731219725784));
#61248=CARTESIAN_POINT('Ctrl Pts',(4.23809251033577,5.27887470736952,54.9820266065492));
#61249=CARTESIAN_POINT('Ctrl Pts',(4.08896975004594,5.39521863024622,54.99093124052));
#61250=CARTESIAN_POINT('Ctrl Pts',(3.93510884940687,5.50519821108376,54.9998358744908));
#61251=CARTESIAN_POINT('Ctrl Pts',(3.78160036162273,5.61492588764992,55.008720112718));
#61252=CARTESIAN_POINT('Ctrl Pts',(3.6233756001165,5.71831816228657,55.0176043509451));
#61253=CARTESIAN_POINT('Ctrl Pts',(3.46095742154545,5.81498604695226,55.0264885891723));
#61254=CARTESIAN_POINT('Ctrl Pts',(3.34249233064842,5.88549397805022,55.032968603284));
#61255=CARTESIAN_POINT('Ctrl Pts',(3.22179708303814,5.95242531536962,55.0394486173957));
#61256=CARTESIAN_POINT('Ctrl Pts',(3.09908550384712,6.01564277861017,55.0459286315074));
#61257=CARTESIAN_POINT('Ctrl Pts',(3.09908550384738,6.01564277861003,53.0457619208681));
#61258=CARTESIAN_POINT('Ctrl Pts',(2.94005757428153,6.09756937720674,53.0542010555753));
#61259=CARTESIAN_POINT('Ctrl Pts',(2.77766693021921,6.17324381468496,53.0626401902825));
#61260=CARTESIAN_POINT('Ctrl Pts',(2.61243358892099,6.24239375107638,53.0710793249896));
#61261=CARTESIAN_POINT('Ctrl Pts',(2.44731973230398,6.31149368328559,53.0795123571311));
#61262=CARTESIAN_POINT('Ctrl Pts',(2.27936758307977,6.37407839180963,53.0879453892726));
#61263=CARTESIAN_POINT('Ctrl Pts',(2.10911964718684,6.42992249672191,53.096378421414));
#61264=CARTESIAN_POINT('Ctrl Pts',(1.93896868511028,6.48573479263782,53.1048066500711));
#61265=CARTESIAN_POINT('Ctrl Pts',(1.7665248597525,6.53481403638633,53.1132348787281));
#61266=CARTESIAN_POINT('Ctrl Pts',(1.59234882218039,6.57698367251286,53.1216631073851));
#61267=CARTESIAN_POINT('Ctrl Pts',(1.41130160981969,6.62081688386268,53.1304238262806));
#61268=CARTESIAN_POINT('Ctrl Pts',(1.22838308135514,6.65718409709552,53.1391845451761));
#61269=CARTESIAN_POINT('Ctrl Pts',(1.04423928235286,6.68594445992421,53.1479452640715));
#61270=CARTESIAN_POINT('Ctrl Pts',(0.867189729917508,6.71359681310844,53.1563684711947));
#61271=CARTESIAN_POINT('Ctrl Pts',(0.689007907804055,6.73421742414931,53.164791678318));
#61272=CARTESIAN_POINT('Ctrl Pts',(0.510277575700802,6.74773338208742,53.1732148854412));
#61273=CARTESIAN_POINT('Ctrl Pts',(0.331560321883366,6.76124835101846,53.1816374762107));
#61274=CARTESIAN_POINT('Ctrl Pts',(0.152294970515892,6.7676596782313,53.1900600669802));
#61275=CARTESIAN_POINT('Ctrl Pts',(-0.0269305010389215,6.76694641238674,
53.1984826577496));
#61276=CARTESIAN_POINT('Ctrl Pts',(-0.206167850202632,6.76623309927272,
53.2069058067));
#61277=CARTESIAN_POINT('Ctrl Pts',(-0.385364980889819,6.75839425355299,
53.2153289556504));
#61278=CARTESIAN_POINT('Ctrl Pts',(-0.563934447482844,6.74346105045045,
53.2237521046008));
#61279=CARTESIAN_POINT('Ctrl Pts',(-0.742540651901937,6.72852477507901,
53.2321769864801));
#61280=CARTESIAN_POINT('Ctrl Pts',(-0.920518602661822,6.70649126080709,
53.2406018683593));
#61281=CARTESIAN_POINT('Ctrl Pts',(-1.09728612991938,6.67744353394969,53.2490267502386));
#61282=CARTESIAN_POINT('Ctrl Pts',(-1.27417574263058,6.64837574512183,53.2574574508083));
#61283=CARTESIAN_POINT('Ctrl Pts',(-1.44985293240845,6.61228411930036,53.265888151378));
#61284=CARTESIAN_POINT('Ctrl Pts',(-1.62374491164964,6.56930296621277,53.2743188519477));
#61285=CARTESIAN_POINT('Ctrl Pts',(-1.79770522804939,6.52630492212258,53.2827528656669));
#61286=CARTESIAN_POINT('Ctrl Pts',(-1.96987861305709,6.47641203825159,53.2911868793861));
#61287=CARTESIAN_POINT('Ctrl Pts',(-2.13970703579232,6.41980862650756,53.2996208931053));
#61288=CARTESIAN_POINT('Ctrl Pts',(-2.30968337277309,6.36315591529523,53.3080622525371));
#61289=CARTESIAN_POINT('Ctrl Pts',(-2.47731035402599,6.29978111381898,53.3165036119689));
#61290=CARTESIAN_POINT('Ctrl Pts',(-2.64204863773189,6.22991717407696,53.3249449714006));
#61291=CARTESIAN_POINT('Ctrl Pts',(-2.68742496602256,6.2106735046997,53.3272701012258));
#61292=CARTESIAN_POINT('Ctrl Pts',(-2.73258226158266,6.19093777935084,53.329595231051));
#61293=CARTESIAN_POINT('Ctrl Pts',(-2.77750956863203,6.17071548494642,53.3319203608762));
#61294=CARTESIAN_POINT('Ctrl Pts',(-2.93482108857445,6.09990777181137,53.34006172814));
#61295=CARTESIAN_POINT('Ctrl Pts',(-3.08962364653538,6.02299031381432,53.3482030954038));
#61296=CARTESIAN_POINT('Ctrl Pts',(-3.24140575636373,5.94016647263459,53.3563444626677));
#61297=CARTESIAN_POINT('Ctrl Pts',(-3.39305537194837,5.85741493037211,53.3644787231368));
#61298=CARTESIAN_POINT('Ctrl Pts',(-3.54168946849646,5.76876744180524,53.3726129836059));
#61299=CARTESIAN_POINT('Ctrl Pts',(-3.68681717397462,5.67447514098756,53.380747244075));
#61300=CARTESIAN_POINT('Ctrl Pts',(-3.83184587856846,5.58024716297534,53.3888759556451));
#61301=CARTESIAN_POINT('Ctrl Pts',(-3.97337264865834,5.48038223792717,53.3970046672151));
#61302=CARTESIAN_POINT('Ctrl Pts',(-4.1109318811139,5.37517702674445,53.4051333787852));
#61303=CARTESIAN_POINT('Ctrl Pts',(-4.24842551410248,5.27002198599127,53.4132582139224));
#61304=CARTESIAN_POINT('Ctrl Pts',(-4.38195508703994,5.15953195235009,53.4213830490595));
#61305=CARTESIAN_POINT('Ctrl Pts',(-4.51108464955587,5.0440464197449,53.4295078841966));
#61306=CARTESIAN_POINT('Ctrl Pts',(-4.64017806188347,4.92859321764308,53.437630444763));
#61307=CARTESIAN_POINT('Ctrl Pts',(-4.76487364522968,4.80814754655193,53.4457530053294));
#61308=CARTESIAN_POINT('Ctrl Pts',(-4.88476920195721,4.68308860087126,53.4538755658958));
#61309=CARTESIAN_POINT('Ctrl Pts',(-5.00467113081215,4.55802300864289,53.4619985581546));
#61310=CARTESIAN_POINT('Ctrl Pts',(-5.11977226725638,4.42834391355026,53.4701215504132));
#61311=CARTESIAN_POINT('Ctrl Pts',(-5.2297077808273,4.29446685016364,53.4782445426719));
#61312=CARTESIAN_POINT('Ctrl Pts',(-5.28582650632384,4.22612669395352,53.4823910823839));
#61313=CARTESIAN_POINT('Ctrl Pts',(-5.34059980372301,4.15669319334044,53.4865376220959));
#61314=CARTESIAN_POINT('Ctrl Pts',(-5.39398321700727,4.08622491483814,53.4906841618079));
#61315=CARTESIAN_POINT('Ctrl Pts',(-5.50964070727787,3.93355231985311,53.4996678207178));
#61316=CARTESIAN_POINT('Ctrl Pts',(-5.61871462356346,3.77609639131443,53.5086514796278));
#61317=CARTESIAN_POINT('Ctrl Pts',(-5.72085559517629,3.61442945139896,53.5176351385377));
#61318=CARTESIAN_POINT('Ctrl Pts',(-5.82317204386379,3.45248476944483,53.5266342312756));
#61319=CARTESIAN_POINT('Ctrl Pts',(-5.9185316139385,3.28631481864143,53.5356333240135));
#61320=CARTESIAN_POINT('Ctrl Pts',(-6.00663036087874,3.11651740052414,53.5446324167514));
#61321=CARTESIAN_POINT('Ctrl Pts',(-6.09493567474315,2.94632185494635,53.5536526098451));
#61322=CARTESIAN_POINT('Ctrl Pts',(-6.17594599168649,2.77248203739202,53.5626728029389));
#61323=CARTESIAN_POINT('Ctrl Pts',(-6.2494039712688,2.59561919469897,53.5716929960326));
#61324=CARTESIAN_POINT('Ctrl Pts',(-6.3229363454474,2.41857723409586,53.5807223243302));
#61325=CARTESIAN_POINT('Ctrl Pts',(-6.3889010161122,2.23850635506613,53.5897516526279));
#61326=CARTESIAN_POINT('Ctrl Pts',(-6.44708972823528,2.05604548492565,53.5987809809255));
#61327=CARTESIAN_POINT('Ctrl Pts',(-6.50536047472599,1.8733273816973,53.607823038758));
#61328=CARTESIAN_POINT('Ctrl Pts',(-6.55583327026295,1.68821277814971,53.6168650965905));
#61329=CARTESIAN_POINT('Ctrl Pts',(-6.59834981517535,1.50135562628429,53.6259071544229));
#61330=CARTESIAN_POINT('Ctrl Pts',(-6.63524679344428,1.33919606496578,53.6337540905284));
#61331=CARTESIAN_POINT('Ctrl Pts',(-6.66615251845092,1.17572443489703,53.6416010266338));
#61332=CARTESIAN_POINT('Ctrl Pts',(-6.69099487965077,1.01137358107042,53.6494479627392));
#61333=CARTESIAN_POINT('Ctrl Pts',(-6.72167052148441,0.80843120025239,53.6591374523785));
#61334=CARTESIAN_POINT('Ctrl Pts',(-6.74311813259488,0.604030993469634,
53.6688269420178));
#61335=CARTESIAN_POINT('Ctrl Pts',(-6.7552299124238,0.398945898957237,53.6785164316571));
#61336=CARTESIAN_POINT('Ctrl Pts',(-6.76300625634691,0.267271425761757,
53.6847375490271));
#61337=CARTESIAN_POINT('Ctrl Pts',(-6.76693515184334,0.13531483858658,53.690958666397));
#61338=CARTESIAN_POINT('Ctrl Pts',(-6.76699920371004,0.00328283226939312,
53.6971797837669));
#61339=CARTESIAN_POINT('',(-6.76699774277413,-0.00552714119481092,53.3028202162163));
#61340=CARTESIAN_POINT('Ctrl Pts',(3.09908550384727,6.01564277861009,52.6512695067322));
#61341=CARTESIAN_POINT('Ctrl Pts',(2.94205676261785,6.09653945308715,52.6595898239773));
#61342=CARTESIAN_POINT('Ctrl Pts',(2.78197968006646,6.17122140541269,52.6679101412225));
#61343=CARTESIAN_POINT('Ctrl Pts',(2.61938682177641,6.23947927938735,52.6762304584677));
#61344=CARTESIAN_POINT('Ctrl Pts',(2.45654726276985,6.30784072043497,52.6845634000571));
#61345=CARTESIAN_POINT('Ctrl Pts',(2.2911846245389,6.36975847955866,52.6928963416466));
#61346=CARTESIAN_POINT('Ctrl Pts',(2.12384835750788,6.42507254078202,52.7012292832361));
#61347=CARTESIAN_POINT('Ctrl Pts',(1.98281488415703,6.47169204722784,52.7082524092831));
#61348=CARTESIAN_POINT('Ctrl Pts',(1.84037982600834,6.51362155783438,52.7152755353301));
#61349=CARTESIAN_POINT('Ctrl Pts',(1.6968774011468,6.55079354624135,52.7222986613771));
#61350=CARTESIAN_POINT('Ctrl Pts',(1.53195548964767,6.59351390715661,52.7303700746197));
#61351=CARTESIAN_POINT('Ctrl Pts',(1.3651158112376,6.63008064296225,52.7384414878622));
#61352=CARTESIAN_POINT('Ctrl Pts',(1.19686780559995,6.66031504179182,52.7465129011048));
#61353=CARTESIAN_POINT('Ctrl Pts',(1.02883102139834,6.6905114838378,52.7545741813566));
#61354=CARTESIAN_POINT('Ctrl Pts',(0.859389790336993,6.71439134169229,52.7626354616083));
#61355=CARTESIAN_POINT('Ctrl Pts',(0.68906962780824,6.73182531324397,52.7706967418601));
#61356=CARTESIAN_POINT('Ctrl Pts',(0.51892593613637,6.74924122123902,52.7787496697183));
#61357=CARTESIAN_POINT('Ctrl Pts',(0.347905493140503,6.7602244960111,52.7868025975764));
#61358=CARTESIAN_POINT('Ctrl Pts',(0.176544854816426,6.7646966609182,52.7948555254346));
#61359=CARTESIAN_POINT('Ctrl Pts',(0.00532424135297324,6.76916517146061,
52.8029018729596));
#61360=CARTESIAN_POINT('Ctrl Pts',(-0.166235643212382,6.7671331519865,52.8109482204846));
#61361=CARTESIAN_POINT('Ctrl Pts',(-0.337592358950583,6.75857384358403,
52.8189945680095));
#61362=CARTESIAN_POINT('Ctrl Pts',(-0.508846537024973,6.75001965696207,
52.8270361007032));
#61363=CARTESIAN_POINT('Ctrl Pts',(-0.679897416728472,6.73494597538439,
52.8350776333968));
#61364=CARTESIAN_POINT('Ctrl Pts',(-0.850201897232936,6.71337811641364,
52.8431191660905));
#61365=CARTESIAN_POINT('Ctrl Pts',(-1.02378043665129,6.69139562101812,52.8513152951384));
#61366=CARTESIAN_POINT('Ctrl Pts',(-1.19658319035935,6.66266670040916,52.8595114241863));
#61367=CARTESIAN_POINT('Ctrl Pts',(-1.36803939605063,6.62727373894073,52.8677075532342));
#61368=CARTESIAN_POINT('Ctrl Pts',(-1.53620350591642,6.59256035054598,52.8757463100708));
#61369=CARTESIAN_POINT('Ctrl Pts',(-1.70307193424474,6.55143661169157,52.8837850669075));
#61370=CARTESIAN_POINT('Ctrl Pts',(-1.86811584513093,6.50403199478376,52.8918238237441));
#61371=CARTESIAN_POINT('Ctrl Pts',(-2.03317573052384,6.45662278960991,52.8998633586475));
#61372=CARTESIAN_POINT('Ctrl Pts',(-2.19641038783759,6.40293159890401,52.9079028935508));
#61373=CARTESIAN_POINT('Ctrl Pts',(-2.35730588590162,6.34313786388831,52.9159424284542));
#61374=CARTESIAN_POINT('Ctrl Pts',(-2.51824881431329,6.28332650229093,52.9239843333303));
#61375=CARTESIAN_POINT('Ctrl Pts',(-2.67685086103619,6.21740914561525,52.9320262382063));
#61376=CARTESIAN_POINT('Ctrl Pts',(-2.83261796802381,6.14561343132064,52.9400681430824));
#61377=CARTESIAN_POINT('Ctrl Pts',(-2.99363945500359,6.0713958837391,52.9483813197622));
#61378=CARTESIAN_POINT('Ctrl Pts',(-3.15163100226007,5.99089664338606,52.956694496442));
#61379=CARTESIAN_POINT('Ctrl Pts',(-3.30607533949969,5.9044182481894,52.9650076731218));
#61380=CARTESIAN_POINT('Ctrl Pts',(-3.45573932259533,5.82061652837128,52.9730635407329));
#61381=CARTESIAN_POINT('Ctrl Pts',(-3.60207213402685,5.73120052677407,52.9811194083439));
#61382=CARTESIAN_POINT('Ctrl Pts',(-3.74463382187001,5.63648884857473,52.9891752759549));
#61383=CARTESIAN_POINT('Ctrl Pts',(-3.89402576380447,5.53723945174072,52.9976171071691));
#61384=CARTESIAN_POINT('Ctrl Pts',(-4.03927594287096,5.43217473828971,53.0060589383833));
#61385=CARTESIAN_POINT('Ctrl Pts',(-4.17991890109239,5.32170714905383,53.0145007695975));
#61386=CARTESIAN_POINT('Ctrl Pts',(-4.32056185931392,5.21123955981787,53.0229426008117));
#61387=CARTESIAN_POINT('Ctrl Pts',(-4.45659730115733,5.09536945894082,53.0313844320259));
#61388=CARTESIAN_POINT('Ctrl Pts',(-4.58760622731821,4.97455104537798,53.0398262632401));
#61389=CARTESIAN_POINT('Ctrl Pts',(-4.71430015623976,4.85771198754503,53.0479900486795));
#61390=CARTESIAN_POINT('Ctrl Pts',(-4.83672775852154,4.73584515673678,53.0561538341188));
#61391=CARTESIAN_POINT('Ctrl Pts',(-4.95446066932031,4.60929587639567,53.0643176195582));
#61392=CARTESIAN_POINT('Ctrl Pts',(-5.07205172863916,4.4828990700109,53.0724715687925));
#61393=CARTESIAN_POINT('Ctrl Pts',(-5.1849591110035,4.35183131024003,53.0806255180269));
#61394=CARTESIAN_POINT('Ctrl Pts',(-5.29278811920486,4.2164775494723,53.0887794672613));
#61395=CARTESIAN_POINT('Ctrl Pts',(-5.40050982819502,4.08125847743077,53.0969253026093));
#61396=CARTESIAN_POINT('Ctrl Pts',(-5.50316299893138,3.94176218007957,53.1050711379572));
#61397=CARTESIAN_POINT('Ctrl Pts',(-5.6003903684417,3.79840976213276,53.1132169733052));
#61398=CARTESIAN_POINT('Ctrl Pts',(-5.6975313295111,3.65518474513282,53.1213555692417));
#61399=CARTESIAN_POINT('Ctrl Pts',(-5.78925589283027,3.50811073656579,53.1294941651782));
#61400=CARTESIAN_POINT('Ctrl Pts',(-5.87524772452096,3.35764101349614,53.1376327611147));
#61401=CARTESIAN_POINT('Ctrl Pts',(-5.96119691033611,3.20724591278252,53.1457673208825));
#61402=CARTESIAN_POINT('Ctrl Pts',(-6.04141884315825,3.05345876605319,53.1539018806502));
#61403=CARTESIAN_POINT('Ctrl Pts',(-6.11564093687291,2.89676111048948,53.1620364404179));
#61404=CARTESIAN_POINT('Ctrl Pts',(-6.18984030787155,2.74011142711506,53.1701685098316));
#61405=CARTESIAN_POINT('Ctrl Pts',(-6.25804334094355,2.58055333878037,53.1783005792453));
#61406=CARTESIAN_POINT('Ctrl Pts',(-6.32002379943877,2.41859218855257,53.1864326486589));
#61407=CARTESIAN_POINT('Ctrl Pts',(-6.3819970455106,2.25664988510999,53.1945637717755));
#61408=CARTESIAN_POINT('Ctrl Pts',(-6.43774902943269,2.09230541801023,53.202694894892));
#61409=CARTESIAN_POINT('Ctrl Pts',(-6.48710199961309,1.92608323979413,53.2108260180086));
#61410=CARTESIAN_POINT('Ctrl Pts',(-6.53647515653617,1.75979307206641,53.2189604669815));
#61411=CARTESIAN_POINT('Ctrl Pts',(-6.57944396316227,1.59162400828446,53.2270949159545));
#61412=CARTESIAN_POINT('Ctrl Pts',(-6.61588067992854,1.42211526570397,53.2352293649274));
#61413=CARTESIAN_POINT('Ctrl Pts',(-6.65232474112214,1.25257235581225,53.243365453534));
#61414=CARTESIAN_POINT('Ctrl Pts',(-6.68223402057906,1.08168958800622,53.2515015421407));
#61415=CARTESIAN_POINT('Ctrl Pts',(-6.70553213345339,0.910015278566287,
53.2596376307474));
#61416=CARTESIAN_POINT('Ctrl Pts',(-6.72885072143747,0.738190096377742,
53.267780869603));
#61417=CARTESIAN_POINT('Ctrl Pts',(-6.74554649480596,0.565572346076884,
53.2759241084586));
#61418=CARTESIAN_POINT('Ctrl Pts',(-6.75559500211094,0.392715122517212,
53.2840673473142));
#61419=CARTESIAN_POINT('Ctrl Pts',(-6.76330849069643,0.260025541828338,
53.2903183036061));
#61420=CARTESIAN_POINT('Ctrl Pts',(-6.76710614738299,0.127194964573707,
53.2965692598979));
#61421=CARTESIAN_POINT('Ctrl Pts',(-6.7669977427746,-0.00552714063103698,
53.3028202161897));
#61422=CARTESIAN_POINT('Ctrl Pts',(-6.76699774277413,-0.00552714119462325,
53.3028202162162));
#61423=CARTESIAN_POINT('Ctrl Pts',(-6.76680339762221,-0.243468087172391,
53.3140267778591));
#61424=CARTESIAN_POINT('Ctrl Pts',(-6.75405577165269,-0.480929767539937,
53.325233339502));
#61425=CARTESIAN_POINT('Ctrl Pts',(-6.72892737728901,-0.716816120891868,
53.3364399011449));
#61426=CARTESIAN_POINT('Ctrl Pts',(-6.71329563251903,-0.863555113322262,
53.3434112224644));
#61427=CARTESIAN_POINT('Ctrl Pts',(-6.69287375263082,-1.00968507150458,
53.3503825437838));
#61428=CARTESIAN_POINT('Ctrl Pts',(-6.66771230148202,-1.1549466068461,53.3573538651032));
#61429=CARTESIAN_POINT('Ctrl Pts',(-6.63546270984458,-1.34112923867007,
53.3662890518854));
#61430=CARTESIAN_POINT('Ctrl Pts',(-6.59539020231709,-1.52607862653588,
53.3752242386676));
#61431=CARTESIAN_POINT('Ctrl Pts',(-6.54760220106742,-1.70915020304744,
53.3841594254498));
#61432=CARTESIAN_POINT('Ctrl Pts',(-6.49988577146036,-1.89194759497073,
53.3930812300862));
#61433=CARTESIAN_POINT('Ctrl Pts',(-6.44447697029663,-2.07287253783184,
53.4020030347227));
#61434=CARTESIAN_POINT('Ctrl Pts',(-6.38153410230253,-2.2512910742838,53.4109248393592));
#61435=CARTESIAN_POINT('Ctrl Pts',(-6.318744766891,-2.4292744056116,53.4198248815983));
#61436=CARTESIAN_POINT('Ctrl Pts',(-6.24845812854586,-2.60476328930247,
53.4287249238373));
#61437=CARTESIAN_POINT('Ctrl Pts',(-6.17088185859762,-2.77713991135318,
53.4376249660764));
#61438=CARTESIAN_POINT('Ctrl Pts',(-6.09342501845778,-2.94925115705933,
53.4465113065696));
#61439=CARTESIAN_POINT('Ctrl Pts',(-6.00870103817247,-3.11825946426911,
53.4553976470627));
#61440=CARTESIAN_POINT('Ctrl Pts',(-5.91696619009577,-3.2835651516703,53.4642839875559));
#61441=CARTESIAN_POINT('Ctrl Pts',(-5.82546589201355,-3.44844818128242,
53.4731476072275));
#61442=CARTESIAN_POINT('Ctrl Pts',(-5.72699062046693,-3.6096472565997,53.4820112268992));
#61443=CARTESIAN_POINT('Ctrl Pts',(-5.62184287493263,-3.76658621162045,
53.4908748465708));
#61444=CARTESIAN_POINT('Ctrl Pts',(-5.52202565744206,-3.91556905216016,
53.4992891197254));
#61445=CARTESIAN_POINT('Ctrl Pts',(-5.41619576806538,-4.06071272219559,
53.5077033928799));
#61446=CARTESIAN_POINT('Ctrl Pts',(-5.30465117116774,-4.20154316319953,
53.5161176660345));
#61447=CARTESIAN_POINT('Ctrl Pts',(-5.19581125000061,-4.33895882046231,
53.5243279142428));
#61448=CARTESIAN_POINT('Ctrl Pts',(-5.08163420007673,-4.4721351858391,53.5325381624511));
#61449=CARTESIAN_POINT('Ctrl Pts',(-4.96249228527308,-4.60064770642191,
53.5407484106594));
#61450=CARTESIAN_POINT('Ctrl Pts',(-4.84332204806029,-4.72919077699372,
53.5489606106075));
#61451=CARTESIAN_POINT('Ctrl Pts',(-4.71918483657764,-4.85306753291011,
53.5571728105555));
#61452=CARTESIAN_POINT('Ctrl Pts',(-4.59049031070317,-4.9718897521305,53.5653850105035));
#61453=CARTESIAN_POINT('Ctrl Pts',(-4.46174227468526,-5.09076137666904,
53.5736006250179));
#61454=CARTESIAN_POINT('Ctrl Pts',(-4.32843341053945,-5.20457403632901,
53.5818162395323));
#61455=CARTESIAN_POINT('Ctrl Pts',(-4.19100708116593,-5.31297926267523,
53.5900318540467));
#61456=CARTESIAN_POINT('Ctrl Pts',(-4.05342642804842,-5.42150622333884,
53.598256694336));
#61457=CARTESIAN_POINT('Ctrl Pts',(-3.91171935418317,-5.52461340178658,
53.6064815346254));
#61458=CARTESIAN_POINT('Ctrl Pts',(-3.76635967012437,-5.62199464916685,
53.6147063749148));
#61459=CARTESIAN_POINT('Ctrl Pts',(-3.62090687813434,-5.71943827262164,
53.6229364835003));
#61460=CARTESIAN_POINT('Ctrl Pts',(-3.47179711443141,-5.81114846771948,
53.6311665920858));
#61461=CARTESIAN_POINT('Ctrl Pts',(-3.3195294390031,-5.89686470114346,53.6393967006713));
#61462=CARTESIAN_POINT('Ctrl Pts',(-3.1670530022546,-5.98269845283914,53.6476380928621));
#61463=CARTESIAN_POINT('Ctrl Pts',(-3.01141032175888,-6.06252166669002,
53.6558794850528));
#61464=CARTESIAN_POINT('Ctrl Pts',(-2.85312201217741,-6.1361212328008,53.6641208772435));
#61465=CARTESIAN_POINT('Ctrl Pts',(-2.78423091878326,-6.16815363365284,
53.6677077404844));
#61466=CARTESIAN_POINT('Ctrl Pts',(-2.71483890667416,-6.19900777537673,
53.6712946037254));
#61467=CARTESIAN_POINT('Ctrl Pts',(-2.64498979819209,-6.2286690365968,53.6748814669663));
#61468=CARTESIAN_POINT('Ctrl Pts',(-2.48046726377903,-6.29853314761931,
53.6833299617834));
#61469=CARTESIAN_POINT('Ctrl Pts',(-2.31303257010345,-6.36193526230486,
53.6917784566006));
#61470=CARTESIAN_POINT('Ctrl Pts',(-2.14322108452927,-6.41863633358591,
53.7002269514177));
#61471=CARTESIAN_POINT('Ctrl Pts',(-1.97356471188428,-6.47528561173162,
53.7086677290255));
#61472=CARTESIAN_POINT('Ctrl Pts',(-1.80153618968942,-6.52524594240804,
53.7171085066334));
#61473=CARTESIAN_POINT('Ctrl Pts',(-1.62769051121065,-6.56832646872206,
53.7255492842412));
#61474=CARTESIAN_POINT('Ctrl Pts',(-1.45397689693279,-6.61137426833656,
53.7339836496991));
#61475=CARTESIAN_POINT('Ctrl Pts',(-1.27844920078841,-6.64755260242074,
53.742418015157));
#61476=CARTESIAN_POINT('Ctrl Pts',(-1.10167759735194,-6.67672041285936,
53.7508523806149));
#61477=CARTESIAN_POINT('Ctrl Pts',(-0.925013134425863,-6.70587054481322,
53.7592816340401));
#61478=CARTESIAN_POINT('Ctrl Pts',(-0.747106595525708,-6.72801857046729,
53.7677108874653));
#61479=CARTESIAN_POINT('Ctrl Pts',(-0.568538762665382,-6.74307442309122,
53.7761401408905));
#61480=CARTESIAN_POINT('Ctrl Pts',(-0.390051767215453,-6.75812345995153,
53.7845655784043));
#61481=CARTESIAN_POINT('Ctrl Pts',(-0.21090440645474,-6.76608669783246,
53.7929910159183));
#61482=CARTESIAN_POINT('Ctrl Pts',(-0.0316834057099282,-6.76692582801102,
53.8014164534321));
#61483=CARTESIAN_POINT('Ctrl Pts',(0.147498225001867,-6.76776477385525,
53.809840040104));
#61484=CARTESIAN_POINT('Ctrl Pts',(0.326753130332813,-6.76148272806156,
53.8182636267758));
#61485=CARTESIAN_POINT('Ctrl Pts',(0.505493215601638,-6.74809347956745,
53.8266872134477));
#61486=CARTESIAN_POINT('Ctrl Pts',(0.684213300793744,-6.73470572925991,
53.8351098575645));
#61487=CARTESIAN_POINT('Ctrl Pts',(0.862418348359472,-6.71421238655197,
53.8435325016813));
#61488=CARTESIAN_POINT('Ctrl Pts',(1.03952370131174,-6.68667925613388,53.851955145798));
#61489=CARTESIAN_POINT('Ctrl Pts',(1.21663393373037,-6.6591453671448,53.8603780219688));
#61490=CARTESIAN_POINT('Ctrl Pts',(1.39264408174607,-6.62457135535248,53.8688008981396));
#61491=CARTESIAN_POINT('Ctrl Pts',(1.56697764901718,-6.58307451328637,53.8772237743104));
#61492=CARTESIAN_POINT('Ctrl Pts',(1.74134033096391,-6.54157074101678,53.8856480571484));
#61493=CARTESIAN_POINT('Ctrl Pts',(1.91402554977653,-6.49314191123189,53.8940723399863));
#61494=CARTESIAN_POINT('Ctrl Pts',(2.08446962294295,-6.43795583947483,53.9024966228243));
#61495=CARTESIAN_POINT('Ctrl Pts',(2.25502880773952,-6.38273249708369,53.9109265951117));
#61496=CARTESIAN_POINT('Ctrl Pts',(2.42334350489641,-6.32074289644361,53.919356567399));
#61497=CARTESIAN_POINT('Ctrl Pts',(2.5888667875922,-6.25220423179714,53.9277865396864));
#61498=CARTESIAN_POINT('Ctrl Pts',(2.75444924219275,-6.18364106568314,53.936219525553));
#61499=CARTESIAN_POINT('Ctrl Pts',(2.9172379869409,-6.10852430056944,53.9446525114195));
#61500=CARTESIAN_POINT('Ctrl Pts',(3.07670801617771,-6.0271184477483,53.953085497286));
#61501=CARTESIAN_POINT('Ctrl Pts',(3.2363247568757,-5.94563770203553,53.9615262414485));
#61502=CARTESIAN_POINT('Ctrl Pts',(3.39261638763213,-5.85785646569089,53.969966985611));
#61503=CARTESIAN_POINT('Ctrl Pts',(3.54508339183175,-5.76408472742713,53.9784077297735));
#61504=CARTESIAN_POINT('Ctrl Pts',(3.62938647299413,-5.71223582737767,53.983074842792));
#61505=CARTESIAN_POINT('Ctrl Pts',(3.71252076059832,-5.65855624031891,53.9877419558105));
#61506=CARTESIAN_POINT('Ctrl Pts',(3.7944058170641,-5.60310391617272,53.9924090688291));
#61507=CARTESIAN_POINT('Ctrl Pts',(3.93724708005844,-5.50637222471541,54.0005504360929));
#61508=CARTESIAN_POINT('Ctrl Pts',(4.07656896193991,-5.40405145202004,54.0086918033567));
#61509=CARTESIAN_POINT('Ctrl Pts',(4.21190241936764,-5.29642964738748,54.0168331706206));
#61510=CARTESIAN_POINT('Ctrl Pts',(4.3471177409749,-5.18890178840909,54.0249674310897));
#61511=CARTESIAN_POINT('Ctrl Pts',(4.47835128373244,-5.07608233467336,54.0331016915588));
#61512=CARTESIAN_POINT('Ctrl Pts',(4.60516250417448,-4.95830286591546,54.0412359520279));
#61513=CARTESIAN_POINT('Ctrl Pts',(4.73188721857703,-4.8406037420619,54.049364663598));
#61514=CARTESIAN_POINT('Ctrl Pts',(4.85419534979951,-4.71795158780571,54.0574933751681));
#61515=CARTESIAN_POINT('Ctrl Pts',(4.97167905508774,-4.59071850293633,54.0656220867382));
#61516=CARTESIAN_POINT('Ctrl Pts',(5.08910673455894,-4.46354609318366,54.0737469218753));
#61517=CARTESIAN_POINT('Ctrl Pts',(5.20171432175762,-4.33179737141275,54.0818717570124));
#61518=CARTESIAN_POINT('Ctrl Pts',(5.30913053169631,-4.19588155188037,54.0899965921495));
#61519=CARTESIAN_POINT('Ctrl Pts',(5.41651667016116,-4.0600037823687,54.0981191527159));
#61520=CARTESIAN_POINT('Ctrl Pts',(5.51871410001962,-3.91996152617119,54.1062417132823));
#61521=CARTESIAN_POINT('Ctrl Pts',(5.61539159620327,-3.77619732287519,54.1143642738487));
#61522=CARTESIAN_POINT('Ctrl Pts',(5.71207423053681,-3.63242547889697,54.1224872661074));
#61523=CARTESIAN_POINT('Ctrl Pts',(5.80323613760412,-3.48493159422831,54.1306102583661));
#61524=CARTESIAN_POINT('Ctrl Pts',(5.88858913701548,-3.33418760351353,54.1387332506248));
#61525=CARTESIAN_POINT('Ctrl Pts',(5.93215923905719,-3.25723739551951,54.1428797903368));
#61526=CARTESIAN_POINT('Ctrl Pts',(5.97421637291487,-3.17944072073768,54.1470263300488));
#61527=CARTESIAN_POINT('Ctrl Pts',(6.01472678269927,-3.10086290078748,54.1511728697608));
#61528=CARTESIAN_POINT('Ctrl Pts',(6.10249435013694,-2.93062063100326,54.1601565286708));
#61529=CARTESIAN_POINT('Ctrl Pts',(6.18295569056279,-2.75679467971065,54.1691401875807));
#61530=CARTESIAN_POINT('Ctrl Pts',(6.2558647371488,-2.58000879659319,54.1781238464906));
#61531=CARTESIAN_POINT('Ctrl Pts',(6.3288990406813,-2.40291919725752,54.1871229392285));
#61532=CARTESIAN_POINT('Ctrl Pts',(6.39435502628826,-2.22285972346298,54.1961220319664));
#61533=CARTESIAN_POINT('Ctrl Pts',(6.45203574927775,-2.04047143818332,54.2051211247044));
#61534=CARTESIAN_POINT('Ctrl Pts',(6.50985171743181,-1.85765550338093,54.2141413177981));
#61535=CARTESIAN_POINT('Ctrl Pts',(6.55985587393634,-1.67250006070934,54.2231615108918));
#61536=CARTESIAN_POINT('Ctrl Pts',(6.60190120794937,-1.48566128053357,54.2321817039855));
#61537=CARTESIAN_POINT('Ctrl Pts',(6.64398912339014,-1.29863327931332,54.2412110322832));
#61538=CARTESIAN_POINT('Ctrl Pts',(6.67810206728113,-1.10991876924692,54.2502403605809));
#61539=CARTESIAN_POINT('Ctrl Pts',(6.70414441878094,-0.920182923188831,
54.2592696888785));
#61540=CARTESIAN_POINT('Ctrl Pts',(6.73022348475264,-0.730179587791919,
54.268311746711));
#61541=CARTESIAN_POINT('Ctrl Pts',(6.74820917553739,-0.539152274397078,
54.2773538045435));
#61542=CARTESIAN_POINT('Ctrl Pts',(6.75805766199569,-0.347772392724564,
54.2863958623759));
#61543=CARTESIAN_POINT('Ctrl Pts',(6.76660443811736,-0.181687887275826,
54.2942427984813));
#61544=CARTESIAN_POINT('Ctrl Pts',(6.76902371777479,-0.0153380007074978,
54.3020897345867));
#61545=CARTESIAN_POINT('Ctrl Pts',(6.76531867369218,0.150838467878465,54.3099366706921));
#61546=CARTESIAN_POINT('Ctrl Pts',(6.7612328156501,0.334094981279396,54.3185901350712));
#61547=CARTESIAN_POINT('Ctrl Pts',(6.74969404463363,0.517302093070697,54.3272435994503));
#61548=CARTESIAN_POINT('Ctrl Pts',(6.73071363539664,0.699844953033015,54.3358970638295));
#61549=CARTESIAN_POINT('Ctrl Pts',(6.71175071100041,0.882219653668543,54.3445425565972));
#61550=CARTESIAN_POINT('Ctrl Pts',(6.68535985272872,1.06393102162104,54.3531880493649));
#61551=CARTESIAN_POINT('Ctrl Pts',(6.65160430059668,1.24436699903353,54.3618335421326));
#61552=CARTESIAN_POINT('Ctrl Pts',(6.61683327108885,1.4302310806028,54.3707391195902));
#61553=CARTESIAN_POINT('Ctrl Pts',(6.57424751678385,1.61474151269027,54.3796446970478));
#61554=CARTESIAN_POINT('Ctrl Pts',(6.52397371427464,1.79723564828142,54.3885502745054));
#61555=CARTESIAN_POINT('Ctrl Pts',(6.47526074979517,1.97406393460679,54.3971793627523));
#61556=CARTESIAN_POINT('Ctrl Pts',(6.4193300311417,2.14899892080663,54.4058084509993));
#61557=CARTESIAN_POINT('Ctrl Pts',(6.35634858520071,2.32144818236741,54.4144375392462));
#61558=CARTESIAN_POINT('Ctrl Pts',(6.29034010619849,2.50218575183112,54.4234813613091));
#61559=CARTESIAN_POINT('Ctrl Pts',(6.21658650343977,2.68019243368415,54.4325251833721));
#61560=CARTESIAN_POINT('Ctrl Pts',(6.13533902892131,2.85480367104201,54.4415690054351));
#61561=CARTESIAN_POINT('Ctrl Pts',(6.0540915544029,3.02941490839975,54.450612827498));
#61562=CARTESIAN_POINT('Ctrl Pts',(5.96535033927651,3.20063033729916,54.4596566495609));
#61563=CARTESIAN_POINT('Ctrl Pts',(5.86942530269928,3.36780872616506,54.4687004716238));
#61564=CARTESIAN_POINT('Ctrl Pts',(5.78005554338682,3.52356256174645,54.4771262614892));
#61565=CARTESIAN_POINT('Ctrl Pts',(5.68448958826155,3.67574416625311,54.4855520513545));
#61566=CARTESIAN_POINT('Ctrl Pts',(5.5830464933457,3.82385680343031,54.4939778412199));
#61567=CARTESIAN_POINT('Ctrl Pts',(5.48157986020914,3.97200380773666,54.5024055861528));
#61568=CARTESIAN_POINT('Ctrl Pts',(5.37423355559814,4.11607968873494,54.5108333310857));
#61569=CARTESIAN_POINT('Ctrl Pts',(5.26136909901297,4.25561795794118,54.5192610760187));
#61570=CARTESIAN_POINT('Ctrl Pts',(5.14846317039171,4.39520750047395,54.5276919177258));
#61571=CARTESIAN_POINT('Ctrl Pts',(5.03003525523271,4.53025584905723,54.536122759433));
#61572=CARTESIAN_POINT('Ctrl Pts',(4.90648640596404,4.66033047627419,54.5445536011402));
#61573=CARTESIAN_POINT('Ctrl Pts',(4.78282403105726,4.79052462548707,54.5529921897158));
#61574=CARTESIAN_POINT('Ctrl Pts',(4.65403154938654,4.9157356819451,54.5614307782914));
#61575=CARTESIAN_POINT('Ctrl Pts',(4.5205468380363,5.03556802010657,54.569869366867));
#61576=CARTESIAN_POINT('Ctrl Pts',(4.38699213319283,5.15546319305912,54.5783123802662));
#61577=CARTESIAN_POINT('Ctrl Pts',(4.24874054328489,5.26997380743445,54.5867553936653));
#61578=CARTESIAN_POINT('Ctrl Pts',(4.10626254426284,5.37874492029359,54.5951984070645));
#61579=CARTESIAN_POINT('Ctrl Pts',(3.96363486215945,5.48763030479778,54.6036502904385));
#61580=CARTESIAN_POINT('Ctrl Pts',(3.81677216936223,5.59076394819946,54.6121021738124));
#61581=CARTESIAN_POINT('Ctrl Pts',(3.66617426600214,5.68783396833133,54.6205540571864));
#61582=CARTESIAN_POINT('Ctrl Pts',(3.62513158157831,5.71428861420884,54.6228574623093));
#61583=CARTESIAN_POINT('Ctrl Pts',(3.58381161573429,5.74029315479914,54.6251608674323));
#61584=CARTESIAN_POINT('Ctrl Pts',(3.54222479973447,5.76584186985267,54.6274642725552));
#61585=CARTESIAN_POINT('Ctrl Pts',(3.39783780246129,5.85454551696003,54.6354615606671));
#61586=CARTESIAN_POINT('Ctrl Pts',(3.24998281800364,5.93790483836299,54.643458848779));
#61587=CARTESIAN_POINT('Ctrl Pts',(3.09908550384732,6.01564277861007,54.6514561368909));
#61588=CARTESIAN_POINT('Origin',(0.,0.,-63.6971797838103));
#61589=CARTESIAN_POINT('',(3.09908550384732,6.01564277861007,57.0457563580462));
#61590=CARTESIAN_POINT('',(3.09908550384733,6.01564277861006,56.6515377972971));
#61591=CARTESIAN_POINT('',(3.09908550384721,6.01564277861012,-63.6971797838103));
#61592=CARTESIAN_POINT('',(-6.767,6.12423652101343E-12,55.6971797838098));
#61593=CARTESIAN_POINT('Ctrl Pts',(-6.767,6.12423655037739E-12,55.6971797838098));
#61594=CARTESIAN_POINT('Ctrl Pts',(-6.76700000000017,-0.186007249553793,
55.7059292956226));
#61595=CARTESIAN_POINT('Ctrl Pts',(-6.75932637294281,-0.372014355809892,
55.7146788074353));
#61596=CARTESIAN_POINT('Ctrl Pts',(-6.74400518263414,-0.55738953758019,
55.723428319248));
#61597=CARTESIAN_POINT('Ctrl Pts',(-6.72868405703796,-0.742763936376777,
55.7321777941052));
#61598=CARTESIAN_POINT('Ctrl Pts',(-6.70571545643644,-0.927506130399208,
55.7409272689624));
#61599=CARTESIAN_POINT('Ctrl Pts',(-6.67517739401668,-1.11098864008985,
55.7496767438196));
#61600=CARTESIAN_POINT('Ctrl Pts',(-6.64463945804495,-1.29447039003999,
55.7584261824482));
#61601=CARTESIAN_POINT('Ctrl Pts',(-6.60653217002842,-1.47669218338753,
55.7671756210767));
#61602=CARTESIAN_POINT('Ctrl Pts',(-6.56098496085608,-1.65703510627276,
55.7759250597052));
#61603=CARTESIAN_POINT('Ctrl Pts',(-6.51543793649696,-1.83737729739512,
55.7846744628319));
#61604=CARTESIAN_POINT('Ctrl Pts',(-6.46245112157048,-2.01584035544466,
55.7934238659585));
#61605=CARTESIAN_POINT('Ctrl Pts',(-6.4022044836188,-2.19181813796934,55.8021732690851));
#61606=CARTESIAN_POINT('Ctrl Pts',(-6.3419580851215,-2.36779522105827,55.8109226374366));
#61607=CARTESIAN_POINT('Ctrl Pts',(-6.27445201416547,-2.54128677725268,
55.8196720057881));
#61608=CARTESIAN_POINT('Ctrl Pts',(-6.19991555052933,-2.71170355428182,
55.8284213741397));
#61609=CARTESIAN_POINT('Ctrl Pts',(-6.12537937695335,-2.8821196681306,55.8371707084429));
#61610=CARTESIAN_POINT('Ctrl Pts',(-6.04381298028571,-3.04946076419433,
55.8459200427461));
#61611=CARTESIAN_POINT('Ctrl Pts',(-5.95549339309104,-3.21315848424085,
55.8546693770492));
#61612=CARTESIAN_POINT('Ctrl Pts',(-5.86717414225929,-3.37685558084874,
55.8634186780308));
#61613=CARTESIAN_POINT('Ctrl Pts',(-5.77210188844183,-3.5369090769981,55.8721679790124));
#61614=CARTESIAN_POINT('Ctrl Pts',(-5.67059953311484,-3.69277537023819,
55.8809172799939));
#61615=CARTESIAN_POINT('Ctrl Pts',(-5.56909755592814,-3.84864108280873,
55.8896665483806));
#61616=CARTESIAN_POINT('Ctrl Pts',(-5.46116568155066,-4.00031938354693,
55.8984158167672));
#61617=CARTESIAN_POINT('Ctrl Pts',(-5.34717048488469,-4.14729511918046,
55.9071650851538));
#61618=CARTESIAN_POINT('Ctrl Pts',(-5.23317570343388,-4.29427031947079,
55.9159143216722));
#61619=CARTESIAN_POINT('Ctrl Pts',(-5.1131178195162,-4.43654276249472,55.9246635581905));
#61620=CARTESIAN_POINT('Ctrl Pts',(-4.98740458929306,-4.57362924412315,
55.9334127947089));
#61621=CARTESIAN_POINT('Ctrl Pts',(-4.86169180652812,-4.71071523781193,
55.9421620000856));
#61622=CARTESIAN_POINT('Ctrl Pts',(-4.73032391141655,-4.84261509584409,
55.9509112054623));
#61623=CARTESIAN_POINT('Ctrl Pts',(-4.5937470694742,-4.96888084599512,55.959660410839));
#61624=CARTESIAN_POINT('Ctrl Pts',(-4.45717070231623,-5.09514615720641,
55.9684095858007));
#61625=CARTESIAN_POINT('Ctrl Pts',(-4.31538563497501,-5.21577720520468,
55.9771587607624));
#61626=CARTESIAN_POINT('Ctrl Pts',(-4.16887340952202,-5.33036429293348,
55.9859079357241));
#61627=CARTESIAN_POINT('Ctrl Pts',(-4.02236168122661,-5.44495099183577,
55.9946570809974));
#61628=CARTESIAN_POINT('Ctrl Pts',(-3.87112305263335,-5.55349359497822,
56.0034062262706));
#61629=CARTESIAN_POINT('Ctrl Pts',(-3.71567116929126,-5.65562346357126,
56.0121553715439));
#61630=CARTESIAN_POINT('Ctrl Pts',(-3.56021980053452,-5.7577529940884,56.0209044878553));
#61631=CARTESIAN_POINT('Ctrl Pts',(-3.40055544442236,-5.85346967519791,
56.0296536041666));
#61632=CARTESIAN_POINT('Ctrl Pts',(-3.23722035887006,-5.94244843041294,
56.038402720478));
#61633=CARTESIAN_POINT('Ctrl Pts',(-3.07388580043661,-6.03142689847363,
56.047151808554));
#61634=CARTESIAN_POINT('Ctrl Pts',(-2.90688078789402,-6.11366734707816,
56.05590089663));
#61635=CARTESIAN_POINT('Ctrl Pts',(-2.73677250610581,-6.18889047001346,
56.064649984706));
#61636=CARTESIAN_POINT('Ctrl Pts',(-2.56666475917122,-6.26411335643257,
56.0733990452732));
#61637=CARTESIAN_POINT('Ctrl Pts',(-2.39345402457279,-6.33231884545185,
56.0821481058404));
#61638=CARTESIAN_POINT('Ctrl Pts',(-2.21772855944251,-6.39327529804818,
56.0908971664076));
#61639=CARTESIAN_POINT('Ctrl Pts',(-2.0420036322376,-6.4542315640465,56.0996462001924));
#61640=CARTESIAN_POINT('Ctrl Pts',(-1.86376426061186,-6.5079387441241,56.1083952339772));
#61641=CARTESIAN_POINT('Ctrl Pts',(-1.68361577621823,-6.55421443943278,
56.117144267762));
#61642=CARTESIAN_POINT('Ctrl Pts',(-1.50346782833358,-6.60048999692555,
56.1258932754909));
#61643=CARTESIAN_POINT('Ctrl Pts',(-1.32141105657539,-6.63933404265132,
56.1346422832198));
#61644=CARTESIAN_POINT('Ctrl Pts',(-1.13806375346695,-6.67061465631502,
56.1433912909487));
#61645=CARTESIAN_POINT('Ctrl Pts',(-0.954716981171704,-6.70189517941747,
56.1521402733481));
#61646=CARTESIAN_POINT('Ctrl Pts',(-0.770079967444078,-6.72561226608983,
56.1608892557475));
#61647=CARTESIAN_POINT('Ctrl Pts',(-0.584779764074965,-6.74168536995968,
56.1696382381469));
#61648=CARTESIAN_POINT('Ctrl Pts',(-0.391489587594831,-6.75845153117862,
56.1787644685625));
#61649=CARTESIAN_POINT('Ctrl Pts',(-0.197478091807088,-6.76689985146389,
56.1878906989782));
#61650=CARTESIAN_POINT('Ctrl Pts',(-0.00346214753285774,-6.76699911434415,
56.1970169293938));
#61651=CARTESIAN_POINT('Ctrl Pts',(0.184490798482887,-6.7670952752594,56.2058579651089));
#61652=CARTESIAN_POINT('Ctrl Pts',(0.372447602153101,-6.75935633790773,
56.2146990008241));
#61653=CARTESIAN_POINT('Ctrl Pts',(0.559756448192614,-6.74380914014526,
56.2235400365392));
#61654=CARTESIAN_POINT('Ctrl Pts',(0.745136131041716,-6.72842206873173,
56.2322900151525));
#61655=CARTESIAN_POINT('Ctrl Pts',(0.929880851943366,-6.70538686355747,
56.2410399937658));
#61656=CARTESIAN_POINT('Ctrl Pts',(1.11336305057292,-6.67478177303341,56.2497899723791));
#61657=CARTESIAN_POINT('Ctrl Pts',(1.29684337089958,-6.64417699581293,56.2585398614191));
#61658=CARTESIAN_POINT('Ctrl Pts',(1.47906091205031,-6.60600253548095,56.2672897504591));
#61659=CARTESIAN_POINT('Ctrl Pts',(1.65939671095068,-6.56038806441251,56.2760396394991));
#61660=CARTESIAN_POINT('Ctrl Pts',(1.83973072369019,-6.5147740451389,56.2847894418746));
#61661=CARTESIAN_POINT('Ctrl Pts',(2.01818275356906,-6.46172023288702,56.29353924425));
#61662=CARTESIAN_POINT('Ctrl Pts',(2.19414664033207,-6.40140683918149,56.3022890466255));
#61663=CARTESIAN_POINT('Ctrl Pts',(2.37010884271142,-6.34109402281541,56.3110387652451));
#61664=CARTESIAN_POINT('Ctrl Pts',(2.54358267847691,-6.27352185699838,56.3197884838646));
#61665=CARTESIAN_POINT('Ctrl Pts',(2.71397890841629,-6.19891986435311,56.3285382024841));
#61666=CARTESIAN_POINT('Ctrl Pts',(2.88437356388838,-6.12431856103292,56.337287840256));
#61667=CARTESIAN_POINT('Ctrl Pts',(3.05169040787076,-6.04268767582606,56.3460374780278));
#61668=CARTESIAN_POINT('Ctrl Pts',(3.21536112511966,-5.95430447953993,56.3547871157996));
#61669=CARTESIAN_POINT('Ctrl Pts',(3.37903038442757,-5.86592207055092,56.3635366756317));
#61670=CARTESIAN_POINT('Ctrl Pts',(3.5390533297989,-5.77078760703428,56.3722862354637));
#61671=CARTESIAN_POINT('Ctrl Pts',(3.69488643041811,-5.66922422085351,56.3810357952958));
#61672=CARTESIAN_POINT('Ctrl Pts',(3.85071819468664,-5.56766170563212,56.3897852800958));
#61673=CARTESIAN_POINT('Ctrl Pts',(4.00235994599149,-5.45967053456307,56.3985347648958));
#61674=CARTESIAN_POINT('Ctrl Pts',(4.14929662974228,-5.34561750206741,56.4072842496958));
#61675=CARTESIAN_POINT('Ctrl Pts',(4.29623210224969,-5.23156540974528,56.4160336623712));
#61676=CARTESIAN_POINT('Ctrl Pts',(4.43846235842039,-5.11145173172254,56.4247830750465));
#61677=CARTESIAN_POINT('Ctrl Pts',(4.57550431797349,-4.98568443006635,56.4335324877219));
#61678=CARTESIAN_POINT('Ctrl Pts',(4.71254519337425,-4.85991812336756,56.4422818311798));
#61679=CARTESIAN_POINT('Ctrl Pts',(4.84439764314925,-4.72849847631161,56.4510311746377));
#61680=CARTESIAN_POINT('Ctrl Pts',(4.97061384196638,-4.59187184425396,56.4597805180956));
#61681=CARTESIAN_POINT('Ctrl Pts',(5.09682908420159,-4.45524624767801,56.4685297952429));
#61682=CARTESIAN_POINT('Ctrl Pts',(5.21740796650125,-4.31341395556948,56.4772790723903));
#61683=CARTESIAN_POINT('Ctrl Pts',(5.33194095942206,-4.16685668162913,56.4860283495377));
#61684=CARTESIAN_POINT('Ctrl Pts',(5.44647312235093,-4.02030046975269,56.4947775632812));
#61685=CARTESIAN_POINT('Ctrl Pts',(5.55495930712253,-3.86901957035598,56.5035267770247));
#61686=CARTESIAN_POINT('Ctrl Pts',(5.65703106079764,-3.71352778058422,56.5122759907683));
#61687=CARTESIAN_POINT('Ctrl Pts',(5.75910210868695,-3.55803706597667,56.5210251440145));
#61688=CARTESIAN_POINT('Ctrl Pts',(5.85475865698501,-3.39833575880982,56.5297742972607));
#61689=CARTESIAN_POINT('Ctrl Pts',(5.94367583069008,-3.23496624706822,56.5385234505069));
#61690=CARTESIAN_POINT('Ctrl Pts',(6.03259241910023,-3.07159781070207,56.547272546162));
#61691=CARTESIAN_POINT('Ctrl Pts',(6.11476958470914,-2.90456146975947,56.5560216418171));
#61692=CARTESIAN_POINT('Ctrl Pts',(6.18992823574333,-2.73442451648376,56.5647707374722));
#61693=CARTESIAN_POINT('Ctrl Pts',(6.26508641700898,-2.56428862662509,56.5735197784423));
#61694=CARTESIAN_POINT('Ctrl Pts',(6.33322605570272,-2.39105242531344,56.5822688194125));
#61695=CARTESIAN_POINT('Ctrl Pts',(6.39411573747753,-2.21530425353768,56.5910178603826));
#61696=CARTESIAN_POINT('Ctrl Pts',(6.45500505889114,-2.03955712188598,56.5997668495736));
#61697=CARTESIAN_POINT('Ctrl Pts',(6.5086444154492,-1.86129832025606,56.6085158387646));
#61698=CARTESIAN_POINT('Ctrl Pts',(6.55485164049898,-1.6811332401234,56.6172648279556));
#61699=CARTESIAN_POINT('Ctrl Pts',(6.60199852639105,-1.4973043591292,56.6261917348325));
#61700=CARTESIAN_POINT('Ctrl Pts',(6.64140767441008,-1.31149113173663,56.6351186417094));
#61701=CARTESIAN_POINT('Ctrl Pts',(6.67293975269602,-1.12435050446434,56.6440455485863));
#61702=CARTESIAN_POINT('Ctrl Pts',(6.70384664831506,-0.94092029156382,56.6527954627703));
#61703=CARTESIAN_POINT('Ctrl Pts',(6.72718585889664,-0.756215114278064,
56.6615453769543));
#61704=CARTESIAN_POINT('Ctrl Pts',(6.74287810451863,-0.570862389375311,
56.6702952911382));
#61705=CARTESIAN_POINT('Ctrl Pts',(6.75857004154122,-0.385513309568294,
56.6790450332488));
#61706=CARTESIAN_POINT('Ctrl Pts',(6.76661529035555,-0.199516993259425,
56.6877947753594));
#61707=CARTESIAN_POINT('Ctrl Pts',(6.76698652348896,-0.0135052182052907,
56.69654451747));
#61708=CARTESIAN_POINT('Ctrl Pts',(6.76735774981525,0.172503146037646,56.7052940991406));
#61709=CARTESIAN_POINT('Ctrl Pts',(6.76005524147486,0.358526681832213,56.7140436808113));
#61710=CARTESIAN_POINT('Ctrl Pts',(6.74510380214892,0.543933542113598,56.7227932624819));
#61711=CARTESIAN_POINT('Ctrl Pts',(6.73015261710994,0.729337249083357,56.7315426953438));
#61712=CARTESIAN_POINT('Ctrl Pts',(6.70755278444625,0.914124015853203,56.7402921282058));
#61713=CARTESIAN_POINT('Ctrl Pts',(6.67738106408314,1.0976662174923,56.7490415610677));
#61714=CARTESIAN_POINT('Ctrl Pts',(6.64720981677284,1.28120554143164,56.75779085675));
#61715=CARTESIAN_POINT('Ctrl Pts',(6.60946696581558,1.46350005650459,56.7665401524324));
#61716=CARTESIAN_POINT('Ctrl Pts',(6.56428070011035,1.64393062206371,56.7752894481147));
#61717=CARTESIAN_POINT('Ctrl Pts',(6.51909508282788,1.82435859844484,56.7840386182447));
#61718=CARTESIAN_POINT('Ctrl Pts',(6.46646633415715,2.00292240086389,56.7927877883747));
#61719=CARTESIAN_POINT('Ctrl Pts',(6.40657319597253,2.17901557696276,56.8015369585047));
#61720=CARTESIAN_POINT('Ctrl Pts',(6.34668083768359,2.35510646007261,56.8102860147078));
#61721=CARTESIAN_POINT('Ctrl Pts',(6.27952437143953,2.52872650996363,56.8190350709108));
#61722=CARTESIAN_POINT('Ctrl Pts',(6.20533187335206,2.69928607997764,56.8277841271139));
#61723=CARTESIAN_POINT('Ctrl Pts',(6.12831449784326,2.87633970115239,56.8368663034028));
#61724=CARTESIAN_POINT('Ctrl Pts',(6.04371489463231,3.05009490562194,56.8459484796916));
#61725=CARTESIAN_POINT('Ctrl Pts',(5.95184265120572,3.21991584599481,56.8550306559805));
#61726=CARTESIAN_POINT('Ctrl Pts',(5.86333281335579,3.38352155905151,56.8637804363349));
#61727=CARTESIAN_POINT('Ctrl Pts',(5.76807337235776,3.54347560903676,56.8725302166893));
#61728=CARTESIAN_POINT('Ctrl Pts',(5.66638790086451,3.69923467178501,56.8812799970437));
#61729=CARTESIAN_POINT('Ctrl Pts',(5.56470608502837,3.85498813489629,56.890029462838));
#61730=CARTESIAN_POINT('Ctrl Pts',(5.45659885767044,4.00654667256137,56.8987789286322));
#61731=CARTESIAN_POINT('Ctrl Pts',(5.34243340580596,4.15339551506096,56.9075283944265));
#61732=CARTESIAN_POINT('Ctrl Pts',(5.2282714514068,4.30023985883765,56.9162775921804));
#61733=CARTESIAN_POINT('Ctrl Pts',(5.10805181978173,4.44237456992946,56.9250267899343));
#61734=CARTESIAN_POINT('Ctrl Pts',(4.98218281282632,4.5793169162636,56.9337759876881));
#61735=CARTESIAN_POINT('Ctrl Pts',(4.856316992963,4.7162557951209,56.9425249639061));
#61736=CARTESIAN_POINT('Ctrl Pts',(4.72480227791897,4.84800236135713,56.9512739401242));
#61737=CARTESIAN_POINT('Ctrl Pts',(4.58808530848159,4.97410918678867,56.9600229163422));
#61738=CARTESIAN_POINT('Ctrl Pts',(4.45135945057013,5.10022421088972,56.9687724613634));
#61739=CARTESIAN_POINT('Ctrl Pts',(4.30943087208079,5.22069856611954,56.9775220063846));
#61740=CARTESIAN_POINT('Ctrl Pts',(4.16278164322503,5.33512305301656,56.9862715514058));
#61741=CARTESIAN_POINT('Ctrl Pts',(4.01614103534424,5.44954081331402,56.995020582073));
#61742=CARTESIAN_POINT('Ctrl Pts',(3.86478055833445,5.55790924068316,57.0037696127403));
#61743=CARTESIAN_POINT('Ctrl Pts',(3.70921425811981,5.65986029751272,57.0125186434076));
#61744=CARTESIAN_POINT('Ctrl Pts',(3.55364584530154,5.76181273884632,57.0212677928874));
#61745=CARTESIAN_POINT('Ctrl Pts',(3.39387173464384,5.8573474781804,57.0300169423673));
#61746=CARTESIAN_POINT('Ctrl Pts',(3.2304345609245,5.94614005448783,57.0387660918471));
#61747=CARTESIAN_POINT('Ctrl Pts',(3.18690768806426,5.96978744811264,57.0410961805802));
#61748=CARTESIAN_POINT('Ctrl Pts',(3.14312114982904,5.99295688499288,57.0434262693132));
#61749=CARTESIAN_POINT('Ctrl Pts',(3.09908550384732,6.01564277861007,57.0457563580462));
#61750=CARTESIAN_POINT('Ctrl Pts',(3.09908550384712,6.01564277861017,55.0459286315074));
#61751=CARTESIAN_POINT('Ctrl Pts',(2.93138389954939,6.10203780404269,55.0547844279169));
#61752=CARTESIAN_POINT('Ctrl Pts',(2.75991540541463,6.18149472625787,55.0636402243264));
#61753=CARTESIAN_POINT('Ctrl Pts',(2.58525146459081,6.25370001397821,55.0724960207359));
#61754=CARTESIAN_POINT('Ctrl Pts',(2.54694817563464,6.26953442139322,55.0744380708649));
#61755=CARTESIAN_POINT('Ctrl Pts',(2.50849132126405,6.28502025628159,55.0763801209939));
#61756=CARTESIAN_POINT('Ctrl Pts',(2.4698871053878,6.30015449704522,55.0783221711229));
#61757=CARTESIAN_POINT('Ctrl Pts',(2.3066830922166,6.36413633873944,55.0865324240095));
#61758=CARTESIAN_POINT('Ctrl Pts',(2.14100011934271,6.42176905429941,55.0947426768961));
#61759=CARTESIAN_POINT('Ctrl Pts',(1.97337352215316,6.47287308249319,55.1029529297827));
#61760=CARTESIAN_POINT('Ctrl Pts',(1.80570707583378,6.52398925942164,55.1111651344564));
#61761=CARTESIAN_POINT('Ctrl Pts',(1.63609642514703,6.56857355308037,55.1193773391301));
#61762=CARTESIAN_POINT('Ctrl Pts',(1.46509094013261,6.60649661599409,55.1275895438039));
#61763=CARTESIAN_POINT('Ctrl Pts',(1.29401435157499,6.64443544719818,55.1358051630865));
#61764=CARTESIAN_POINT('Ctrl Pts',(1.121542120486,6.67570745276881,55.1440207823692));
#61765=CARTESIAN_POINT('Ctrl Pts',(0.948232737877954,6.70023459849105,55.1522364016518));
#61766=CARTESIAN_POINT('Ctrl Pts',(0.774728735607956,6.72478928723916,55.1604612467537));
#61767=CARTESIAN_POINT('Ctrl Pts',(0.600386056726659,6.74258393808573,55.1686860918556));
#61768=CARTESIAN_POINT('Ctrl Pts',(0.425768208834028,6.75359240940303,55.1769109369575));
#61769=CARTESIAN_POINT('Ctrl Pts',(0.251038511608425,6.76460793206239,55.1851410503837));
#61770=CARTESIAN_POINT('Ctrl Pts',(0.0760336489349973,6.76882860149252,
55.1933711638098));
#61771=CARTESIAN_POINT('Ctrl Pts',(-0.0986840056641186,6.76628040115292,
55.201601277236));
#61772=CARTESIAN_POINT('Ctrl Pts',(-0.273641201045822,6.76372870718867,
55.2098426742832));
#61773=CARTESIAN_POINT('Ctrl Pts',(-0.448310047454821,6.75438962611889,
55.2180840713304));
#61774=CARTESIAN_POINT('Ctrl Pts',(-0.622133408069195,6.7383409695981,55.2263254683777));
#61775=CARTESIAN_POINT('Ctrl Pts',(-0.697785100789709,6.73135624655859,
55.2299123029366));
#61776=CARTESIAN_POINT('Ctrl Pts',(-0.773276771492053,6.72310126585528,
55.2334991374956));
#61777=CARTESIAN_POINT('Ctrl Pts',(-0.848563193888382,6.71358544341084,
55.2370859720545));
#61778=CARTESIAN_POINT('Ctrl Pts',(-1.02589409518704,6.69117171571653,55.2455344622989));
#61779=CARTESIAN_POINT('Ctrl Pts',(-1.20248990432317,6.66170833558372,55.2539829525433));
#61780=CARTESIAN_POINT('Ctrl Pts',(-1.37776768511531,6.62525812371503,55.2624314427876));
#61781=CARTESIAN_POINT('Ctrl Pts',(-1.55288535925302,6.58884120711885,55.2708722157988));
#61782=CARTESIAN_POINT('Ctrl Pts',(-1.72668707997948,6.54545024778862,55.2793129888099));
#61783=CARTESIAN_POINT('Ctrl Pts',(-1.89859720039446,6.49519958666817,55.2877537618211));
#61784=CARTESIAN_POINT('Ctrl Pts',(-2.0703767266301,6.44498709923891,55.2961881226686));
#61785=CARTESIAN_POINT('Ctrl Pts',(-2.2402671982649,6.38792539158564,55.3046224835162));
#61786=CARTESIAN_POINT('Ctrl Pts',(-2.40770490801787,6.32417947847044,55.3130568443637));
#61787=CARTESIAN_POINT('Ctrl Pts',(-2.57504113436593,6.26047220152819,55.3214860931749));
#61788=CARTESIAN_POINT('Ctrl Pts',(-2.73992725189055,6.19008891465632,55.3299153419861));
#61789=CARTESIAN_POINT('Ctrl Pts',(-2.90181604565359,6.11324403546819,55.3383445907973));
#61790=CARTESIAN_POINT('Ctrl Pts',(-3.06363155267199,6.03643394380863,55.3467700237038));
#61791=CARTESIAN_POINT('Ctrl Pts',(-3.22245214084822,5.95316823537392,55.3551954566103));
#61792=CARTESIAN_POINT('Ctrl Pts',(-3.3777515039518,5.86370904612016,55.3636208895168));
#61793=CARTESIAN_POINT('Ctrl Pts',(-3.53301675259904,5.77426950827735,55.3720444716168));
#61794=CARTESIAN_POINT('Ctrl Pts',(-3.68476202841597,5.67863936622023,55.3804680537169));
#61795=CARTESIAN_POINT('Ctrl Pts',(-3.83248605746805,5.57712646613944,55.388891635817));
#61796=CARTESIAN_POINT('Ctrl Pts',(-3.98019355747117,5.47562492447954,55.3973142753906));
#61797=CARTESIAN_POINT('Ctrl Pts',(-4.12388043297538,5.36824212580545,55.4057369149642));
#61798=CARTESIAN_POINT('Ctrl Pts',(-4.26307455523596,5.25532913683812,55.4141595545379));
#61799=CARTESIAN_POINT('Ctrl Pts',(-4.40227251308705,5.14241303647513,55.4225824262032));
#61800=CARTESIAN_POINT('Ctrl Pts',(-4.53697721219067,5.02396665233598,55.4310052978685));
#61801=CARTESIAN_POINT('Ctrl Pts',(-4.66674948477618,4.90038143886181,55.4394281695338));
#61802=CARTESIAN_POINT('Ctrl Pts',(-4.7965434307853,4.77677558527221,55.447852447913));
#61803=CARTESIAN_POINT('Ctrl Pts',(-4.92140306693598,4.64802942159968,55.4562767262923));
#61804=CARTESIAN_POINT('Ctrl Pts',(-5.04092572206951,4.51457161473578,55.4647010046716));
#61805=CARTESIAN_POINT('Ctrl Pts',(-5.16052909986028,4.3810236737564,55.4731309726009));
#61806=CARTESIAN_POINT('Ctrl Pts',(-5.27478807145375,4.24275797959035,55.4815609405303));
#61807=CARTESIAN_POINT('Ctrl Pts',(-5.38333929291249,4.10023743914721,55.4899909084597));
#61808=CARTESIAN_POINT('Ctrl Pts',(-5.491929320432,3.95766594892497,55.4984238900248));
#61809=CARTESIAN_POINT('Ctrl Pts',(-5.59480733211847,3.81083684841703,55.50685687159));
#61810=CARTESIAN_POINT('Ctrl Pts',(-5.69165273767726,3.660242903646,55.5152898531552));
#61811=CARTESIAN_POINT('Ctrl Pts',(-5.78858724190164,3.50951041105802,55.5237305931411));
#61812=CARTESIAN_POINT('Ctrl Pts',(-5.87947787598317,3.35500643774,55.532171333127));
#61813=CARTESIAN_POINT('Ctrl Pts',(-5.96404896081116,3.19725022371527,55.540612073113));
#61814=CARTESIAN_POINT('Ctrl Pts',(-6.01081113704409,3.11002154624153,55.5452792400479));
#61815=CARTESIAN_POINT('Ctrl Pts',(-6.05564202835132,3.0217989628261,55.5499464069828));
#61816=CARTESIAN_POINT('Ctrl Pts',(-6.09850128228028,2.93267303155769,55.5546135739177));
#61817=CARTESIAN_POINT('Ctrl Pts',(-6.17399149377114,2.77569093821738,55.5628340954312));
#61818=CARTESIAN_POINT('Ctrl Pts',(-6.24350787023843,2.6156021268131,55.5710546169448));
#61819=CARTESIAN_POINT('Ctrl Pts',(-6.30678734622761,2.45290080709826,55.5792751384584));
#61820=CARTESIAN_POINT('Ctrl Pts',(-6.37000755867763,2.29035186310843,55.5874879611535));
#61821=CARTESIAN_POINT('Ctrl Pts',(-6.42700237321618,2.12519561424854,55.5957007838486));
#61822=CARTESIAN_POINT('Ctrl Pts',(-6.47755534204111,1.9579493841248,55.6039136065437));
#61823=CARTESIAN_POINT('Ctrl Pts',(-6.52806387776402,1.7908501536527,55.6121192106482));
#61824=CARTESIAN_POINT('Ctrl Pts',(-6.5721417481635,1.62166494372084,55.6203248147527));
#61825=CARTESIAN_POINT('Ctrl Pts',(-6.60962124146166,1.45092937265011,55.6285304188571));
#61826=CARTESIAN_POINT('Ctrl Pts',(-6.6470813752321,1.28028199274019,55.6367317844672));
#61827=CARTESIAN_POINT('Ctrl Pts',(-6.67794984266258,1.10808619492482,55.6449331500773));
#61828=CARTESIAN_POINT('Ctrl Pts',(-6.70210915377087,0.934891379220476,
55.6531345156874));
#61829=CARTESIAN_POINT('Ctrl Pts',(-6.72626158895542,0.761745856078312,
55.6613335471265));
#61830=CARTESIAN_POINT('Ctrl Pts',(-6.74370861889685,0.587602234875273,
55.6695325785656));
#61831=CARTESIAN_POINT('Ctrl Pts',(-6.75438408941495,0.413018852666844,
55.6777316100046));
#61832=CARTESIAN_POINT('Ctrl Pts',(-6.76279155916818,0.275525661819018,
55.6841887594776));
#61833=CARTESIAN_POINT('Ctrl Pts',(-6.76700007299065,0.137759960526222,
55.6906459089506));
#61834=CARTESIAN_POINT('Ctrl Pts',(-6.76699999999905,-3.5853761194E-6,55.6971030584236));
#61835=CARTESIAN_POINT('',(-6.76699931626774,0.0030419782871798,55.3028202162181));
#61836=CARTESIAN_POINT('Ctrl Pts',(3.09908550384732,6.01564277861007,54.6514561368909));
#61837=CARTESIAN_POINT('Ctrl Pts',(2.94227848457418,6.09642522833577,54.6597666288178));
#61838=CARTESIAN_POINT('Ctrl Pts',(2.78218626615245,6.17113690883049,54.6680771207447));
#61839=CARTESIAN_POINT('Ctrl Pts',(2.61931417507843,6.23950977659569,54.6763876126716));
#61840=CARTESIAN_POINT('Ctrl Pts',(2.45655077372096,6.30783701697582,54.6846925587435));
#61841=CARTESIAN_POINT('Ctrl Pts',(2.29101151582971,6.36983373938531,54.6929975048154));
#61842=CARTESIAN_POINT('Ctrl Pts',(2.1232244900123,6.42527873053084,54.7013024508872));
#61843=CARTESIAN_POINT('Ctrl Pts',(1.95551871884651,6.48069687118887,54.7096033751016));
#61844=CARTESIAN_POINT('Ctrl Pts',(1.78556767865217,6.52956949477253,54.717904299316));
#61845=CARTESIAN_POINT('Ctrl Pts',(1.61391772826252,6.57172416998766,54.7262052235304));
#61846=CARTESIAN_POINT('Ctrl Pts',(1.44231949193471,6.61386614499824,54.7345036468731));
#61847=CARTESIAN_POINT('Ctrl Pts',(1.2690237030364,6.64929412309598,54.7428020702157));
#61848=CARTESIAN_POINT('Ctrl Pts',(1.09459033265363,6.67788596815349,54.7511004935584));
#61849=CARTESIAN_POINT('Ctrl Pts',(0.920140701170592,6.70648047861188,54.7593996905001));
#61850=CARTESIAN_POINT('Ctrl Pts',(0.744553618279898,6.72823751880162,54.7676988874419));
#61851=CARTESIAN_POINT('Ctrl Pts',(0.568398247883257,6.74308626904649,54.7759980843837));
#61852=CARTESIAN_POINT('Ctrl Pts',(0.39222614389965,6.75793642982373,54.7842980696939));
#61853=CARTESIAN_POINT('Ctrl Pts',(0.215485991550797,6.76587696282492,54.792598055004));
#61854=CARTESIAN_POINT('Ctrl Pts',(0.0387509799454699,6.76688904605013,
54.8008980403142));
#61855=CARTESIAN_POINT('Ctrl Pts',(-0.138030158621772,6.76790139342405,
54.8092001918794));
#61856=CARTESIAN_POINT('Ctrl Pts',(-0.314805805832689,6.76198168490955,
54.8175023434447));
#61857=CARTESIAN_POINT('Ctrl Pts',(-0.491003677021281,6.74916323622059,
54.8258044950099));
#61858=CARTESIAN_POINT('Ctrl Pts',(-0.667276787544288,6.73633931384718,
54.8341101917278));
#61859=CARTESIAN_POINT('Ctrl Pts',(-0.842971283549303,6.7166108053603,54.8424158884456));
#61860=CARTESIAN_POINT('Ctrl Pts',(-1.01752070452666,6.69006282600243,54.8507215851635));
#61861=CARTESIAN_POINT('Ctrl Pts',(-1.19227617906004,6.6634835070645,54.8590370866595));
#61862=CARTESIAN_POINT('Ctrl Pts',(-1.36588353342741,6.6300686850292,54.8673525881556));
#61863=CARTESIAN_POINT('Ctrl Pts',(-1.5377860191125,6.58995471603729,54.8756680896516));
#61864=CARTESIAN_POINT('Ctrl Pts',(-1.70979624110599,6.54981560644944,54.8839888027153));
#61865=CARTESIAN_POINT('Ctrl Pts',(-1.88009912856106,6.50296906899714,54.892309515779));
#61866=CARTESIAN_POINT('Ctrl Pts',(-2.04815363330913,6.44960120428873,54.9006302288426));
#61867=CARTESIAN_POINT('Ctrl Pts',(-2.21645978561914,6.3961534256675,54.908963401478));
#61868=CARTESIAN_POINT('Ctrl Pts',(-2.3825104995194,6.33616492192162,54.9172965741135));
#61869=CARTESIAN_POINT('Ctrl Pts',(-2.54578394029261,6.26987026415605,54.9256297467489));
#61870=CARTESIAN_POINT('Ctrl Pts',(-2.6722392270364,6.21852504892921,54.9320837893053));
#61871=CARTESIAN_POINT('Ctrl Pts',(-2.79702896078766,6.16339806925064,54.9385378318618));
#61872=CARTESIAN_POINT('Ctrl Pts',(-2.91992138371005,6.10461695055085,54.9449918744183));
#61873=CARTESIAN_POINT('Ctrl Pts',(-3.07361041589699,6.03110539443531,54.9530632878595));
#61874=CARTESIAN_POINT('Ctrl Pts',(-3.22480427228096,5.95165085645071,54.9611347013008));
#61875=CARTESIAN_POINT('Ctrl Pts',(-3.37299810815277,5.86644464410923,54.969206114742));
#61876=CARTESIAN_POINT('Ctrl Pts',(-3.52100589893652,5.78134540111087,54.9772673951921));
#61877=CARTESIAN_POINT('Ctrl Pts',(-3.66602084390755,5.69050903474158,54.9853286756422));
#61878=CARTESIAN_POINT('Ctrl Pts',(-3.80755761490248,5.59417500702276,54.9933899560923));
#61879=CARTESIAN_POINT('Ctrl Pts',(-3.9489477378689,5.49794079220164,55.0014428841483));
#61880=CARTESIAN_POINT('Ctrl Pts',(-4.08686655277689,5.39622045970253,55.0094958122044));
#61881=CARTESIAN_POINT('Ctrl Pts',(-4.22085301193727,5.28929946700128,55.0175487402604));
#61882=CARTESIAN_POINT('Ctrl Pts',(-4.35472998599872,5.18246584324418,55.0255950879826));
#61883=CARTESIAN_POINT('Ctrl Pts',(-4.48468070977489,5.07044024897661,55.0336414357049));
#61884=CARTESIAN_POINT('Ctrl Pts',(-4.61027293592524,4.95355149930585,55.0416877834271));
#61885=CARTESIAN_POINT('Ctrl Pts',(-4.73579000928887,4.83673269437247,55.0497293163175));
#61886=CARTESIAN_POINT('Ctrl Pts',(-4.85695350461245,4.71505678056249,55.0577708492078));
#61887=CARTESIAN_POINT('Ctrl Pts',(-4.97336420201081,4.58889284186909,55.0658123820982));
#61888=CARTESIAN_POINT('Ctrl Pts',(-5.09201285980435,4.46030343967101,55.0740085110225));
#61889=CARTESIAN_POINT('Ctrl Pts',(-5.20572380913926,4.32705194261169,55.0822046399468));
#61890=CARTESIAN_POINT('Ctrl Pts',(-5.31411341305573,4.18956890779722,55.0904007688711));
#61891=CARTESIAN_POINT('Ctrl Pts',(-5.42042185434818,4.05472565155148,55.0984395259021));
#61892=CARTESIAN_POINT('Ctrl Pts',(-5.52161122379691,3.91581219988204,55.1064782829332));
#61893=CARTESIAN_POINT('Ctrl Pts',(-5.61736028292918,3.77326813939453,55.1145170399642));
#61894=CARTESIAN_POINT('Ctrl Pts',(-5.71311860954653,3.63071028216618,55.122556575061));
#61895=CARTESIAN_POINT('Ctrl Pts',(-5.80343536901764,3.48452142639071,55.1305961101577));
#61896=CARTESIAN_POINT('Ctrl Pts',(-5.88803290230934,3.33516979197801,55.1386356452545));
#61897=CARTESIAN_POINT('Ctrl Pts',(-5.9726553740777,3.18577413025029,55.1466775503229));
#61898=CARTESIAN_POINT('Ctrl Pts',(-6.05155507982264,3.03321415884263,55.1547194553913));
#61899=CARTESIAN_POINT('Ctrl Pts',(-6.12450059982879,2.87798217553494,55.1627613604598));
#61900=CARTESIAN_POINT('Ctrl Pts',(-6.19990673361083,2.71751387399201,55.1710745367782));
#61901=CARTESIAN_POINT('Ctrl Pts',(-6.26894977373616,2.55419053669711,55.1793877130967));
#61902=CARTESIAN_POINT('Ctrl Pts',(-6.33142877094932,2.38857671394394,55.1877008894152));
#61903=CARTESIAN_POINT('Ctrl Pts',(-6.39197392511329,2.22808895201547,55.1957567572147));
#61904=CARTESIAN_POINT('Ctrl Pts',(-6.44635527403393,2.06545075447282,55.2038126250141));
#61905=CARTESIAN_POINT('Ctrl Pts',(-6.49444137014837,1.90118917777936,55.2118684928136));
#61906=CARTESIAN_POINT('Ctrl Pts',(-6.54483130785059,1.72905770350139,55.2203103233916));
#61907=CARTESIAN_POINT('Ctrl Pts',(-6.58830781395067,1.55514393992903,55.2287521539696));
#61908=CARTESIAN_POINT('Ctrl Pts',(-6.62478034910879,1.38006316017131,55.2371939845475));
#61909=CARTESIAN_POINT('Ctrl Pts',(-6.66125288426691,1.20498238041358,55.2456358151255));
#61910=CARTESIAN_POINT('Ctrl Pts',(-6.69072145685252,1.02873505337369,55.2540776457034));
#61911=CARTESIAN_POINT('Ctrl Pts',(-6.71315796159003,0.85193848530306,55.2625194762814));
#61912=CARTESIAN_POINT('Ctrl Pts',(-6.74886142398984,0.570600117568218,
55.2759530562508));
#61913=CARTESIAN_POINT('Ctrl Pts',(-6.76687162267472,0.287101299100329,
55.2893866362202));
#61914=CARTESIAN_POINT('Ctrl Pts',(-6.76699931626747,0.00304197888748282,
55.3028202161897));
#61915=CARTESIAN_POINT('Ctrl Pts',(-6.76699931626774,0.0030419782871798,
55.3028202162181));
#61916=CARTESIAN_POINT('Ctrl Pts',(-6.76707603531081,-0.167622524530384,
55.3108911897205));
#61917=CARTESIAN_POINT('Ctrl Pts',(-6.76069231177937,-0.338562701080097,
55.3189621632228));
#61918=CARTESIAN_POINT('Ctrl Pts',(-6.74781185599331,-0.509238800678179,
55.3270331367252));
#61919=CARTESIAN_POINT('Ctrl Pts',(-6.7349453089077,-0.679730599131792,
55.3350953949496));
#61920=CARTESIAN_POINT('Ctrl Pts',(-6.71559601838924,-0.849958519438639,
55.3431576531739));
#61921=CARTESIAN_POINT('Ctrl Pts',(-6.68977966328148,-1.01938072217672,
55.3512199113983));
#61922=CARTESIAN_POINT('Ctrl Pts',(-6.66398552832,-1.18865710316302,55.3592752304341));
#61923=CARTESIAN_POINT('Ctrl Pts',(-6.63173546357944,-1.35712878009417,
55.3673305494698));
#61924=CARTESIAN_POINT('Ctrl Pts',(-6.59309710352087,-1.52425705953581,
55.3753858685056));
#61925=CARTESIAN_POINT('Ctrl Pts',(-6.55448354241268,-1.69127807236716,
55.3834360174602));
#61926=CARTESIAN_POINT('Ctrl Pts',(-6.50948993230037,-1.85695704176339,
55.3914861664149));
#61927=CARTESIAN_POINT('Ctrl Pts',(-6.45823531313495,-2.02076362798245,
55.3995363153695));
#61928=CARTESIAN_POINT('Ctrl Pts',(-6.4069980401316,-2.18451477694257,55.4075837399026));
#61929=CARTESIAN_POINT('Ctrl Pts',(-6.34950408402667,-2.34639444737347,
55.4156311644356));
#61930=CARTESIAN_POINT('Ctrl Pts',(-6.28592285366406,-2.50588564738774,
55.4236785889687));
#61931=CARTESIAN_POINT('Ctrl Pts',(-6.22235112075414,-2.66535302338795,
55.4317248114169));
#61932=CARTESIAN_POINT('Ctrl Pts',(-6.15269406092773,-2.82243229206626,
55.4397710338652));
#61933=CARTESIAN_POINT('Ctrl Pts',(-6.0771698586151,-2.97662485199936,55.4478172563134));
#61934=CARTESIAN_POINT('Ctrl Pts',(-6.00164198210172,-3.13082491329496,
55.4558638702049));
#61935=CARTESIAN_POINT('Ctrl Pts',(-5.9202465595136,-3.2821376510774,55.4639104840963));
#61936=CARTESIAN_POINT('Ctrl Pts',(-5.83324844597768,-3.4300876909343,55.4719570979878));
#61937=CARTESIAN_POINT('Ctrl Pts',(-5.74622886969504,-3.57807423059681,
55.4800056970077));
#61938=CARTESIAN_POINT('Ctrl Pts',(-5.65360404128081,-3.72269609982622,
55.4880542960277));
#61939=CARTESIAN_POINT('Ctrl Pts',(-5.55568289035785,-3.86350574242942,
55.4961028950476));
#61940=CARTESIAN_POINT('Ctrl Pts',(-5.45767045548426,-4.00444665044709,
55.504158997124));
#61941=CARTESIAN_POINT('Ctrl Pts',(-5.35435205319902,-4.14156792933665,
55.5122150992003));
#61942=CARTESIAN_POINT('Ctrl Pts',(-5.24607815011016,-4.27445353734682,
55.5202712012767));
#61943=CARTESIAN_POINT('Ctrl Pts',(-5.13774703862206,-4.40740935777846,
55.5283315599346));
#61944=CARTESIAN_POINT('Ctrl Pts',(-5.0244554574765,-4.53612477036807,55.5363919185925));
#61945=CARTESIAN_POINT('Ctrl Pts',(-4.90659133798229,-4.66021999931732,
55.5444522772505));
#61946=CARTESIAN_POINT('Ctrl Pts',(-4.78857774209641,-4.78447260701023,
55.5525228581315));
#61947=CARTESIAN_POINT('Ctrl Pts',(-4.6659802964762,-4.90409307297317,55.5605934390126));
#61948=CARTESIAN_POINT('Ctrl Pts',(-4.53922117807697,-5.01874088756309,
55.5686640198936));
#61949=CARTESIAN_POINT('Ctrl Pts',(-4.47962586311644,-5.07264211933486,
55.5724583726439));
#61950=CARTESIAN_POINT('Ctrl Pts',(-4.4191111051235,-5.12544481452318,55.5762527253942));
#61951=CARTESIAN_POINT('Ctrl Pts',(-4.3577229824208,-5.17711690117981,55.5800470781445));
#61952=CARTESIAN_POINT('Ctrl Pts',(-4.21316232017549,-5.29879762275609,
55.5889822617309));
#61953=CARTESIAN_POINT('Ctrl Pts',(-4.06341051789947,-5.41449746818261,
55.5979174453173));
#61954=CARTESIAN_POINT('Ctrl Pts',(-3.90896481314798,-5.52379245533094,
55.6068526289037));
#61955=CARTESIAN_POINT('Ctrl Pts',(-3.75475041987423,-5.6329237526892,55.6157744303729));
#61956=CARTESIAN_POINT('Ctrl Pts',(-3.5958563617981,-5.73566918320373,55.6246962318421));
#61957=CARTESIAN_POINT('Ctrl Pts',(-3.43281197432303,-5.8316456467231,55.6336180333113));
#61958=CARTESIAN_POINT('Ctrl Pts',(-3.27016528922406,-5.92738800180008,
55.6425180724758));
#61959=CARTESIAN_POINT('Ctrl Pts',(-3.10338870192026,-6.01639421231828,
55.6514181116403));
#61960=CARTESIAN_POINT('Ctrl Pts',(-2.93303892282319,-6.09832531742971,
55.6603181508048));
#61961=CARTESIAN_POINT('Ctrl Pts',(-2.76295139848448,-6.18013028899235,
55.6692044882925));
#61962=CARTESIAN_POINT('Ctrl Pts',(-2.58930188697861,-6.25488177080588,
55.6780908257801));
#61963=CARTESIAN_POINT('Ctrl Pts',(-2.41267260699273,-6.32228597039607,
55.6869771632678));
#61964=CARTESIAN_POINT('Ctrl Pts',(-2.23649493445352,-6.38951783027862,
55.695840780082));
#61965=CARTESIAN_POINT('Ctrl Pts',(-2.05735293670873,-6.44943980161332,
55.7047043968963));
#61966=CARTESIAN_POINT('Ctrl Pts',(-1.87584905849836,-6.50180584989515,
55.7135680137106));
#61967=CARTESIAN_POINT('Ctrl Pts',(-1.7035462594288,-6.55151727636238,55.7219823021657));
#61968=CARTESIAN_POINT('Ctrl Pts',(-1.52911532216133,-6.59441967566255,
55.7303965906208));
#61969=CARTESIAN_POINT('Ctrl Pts',(-1.35308947604772,-6.63034221362736,
55.7388108790758));
#61970=CARTESIAN_POINT('Ctrl Pts',(-1.18133202812021,-6.66539367669451,
55.7470211319624));
#61971=CARTESIAN_POINT('Ctrl Pts',(-1.00822094912745,-6.69376499554051,
55.755231384849));
#61972=CARTESIAN_POINT('Ctrl Pts',(-0.834314434246282,-6.71537105637569,
55.7634416377356));
#61973=CARTESIAN_POINT('Ctrl Pts',(-0.660366577337444,-6.73698225352428,
55.7716538424094));
#61974=CARTESIAN_POINT('Ctrl Pts',(-0.485623261046444,-6.75182494463065,
55.7798660470832));
#61975=CARTESIAN_POINT('Ctrl Pts',(-0.310647897739216,-6.75986589242939,
55.7880782517569));
#61976=CARTESIAN_POINT('Ctrl Pts',(-0.13559978022844,-6.76791018362884,
55.7962938710394));
#61977=CARTESIAN_POINT('Ctrl Pts',(0.0396802212367957,-6.76914708091198,
55.804509490322));
#61978=CARTESIAN_POINT('Ctrl Pts',(0.214628506536059,-6.76359546426175,
55.8127251096046));
#61979=CARTESIAN_POINT('Ctrl Pts',(0.389773251922865,-6.75803761336297,
55.8209499547065));
#61980=CARTESIAN_POINT('Ctrl Pts',(0.564585181229354,-6.74567603375523,
55.8291747998084));
#61981=CARTESIAN_POINT('Ctrl Pts',(0.738504649515448,-6.72658158968165,
55.8373996449103));
#61982=CARTESIAN_POINT('Ctrl Pts',(0.91253551979508,-6.70747491489488,55.8456297583364));
#61983=CARTESIAN_POINT('Ctrl Pts',(1.08567243835513,-6.68162683100076,55.8538598717626));
#61984=CARTESIAN_POINT('Ctrl Pts',(1.25736581488153,-6.64915936096942,55.8620899851887));
#61985=CARTESIAN_POINT('Ctrl Pts',(1.42929458585647,-6.61664737750164,55.8703313822359));
#61986=CARTESIAN_POINT('Ctrl Pts',(1.59977551582118,-6.57749796039881,55.8785727792831));
#61987=CARTESIAN_POINT('Ctrl Pts',(1.76827306004991,-6.53188329542879,55.8868141763304));
#61988=CARTESIAN_POINT('Ctrl Pts',(1.8416068420885,-6.51203080491336,55.8904010108894));
#61989=CARTESIAN_POINT('Ctrl Pts',(1.91456517407644,-6.49095430506856,55.8939878454485));
#61990=CARTESIAN_POINT('Ctrl Pts',(1.98710511392414,-6.4686708268559,55.8975746800075));
#61991=CARTESIAN_POINT('Ctrl Pts',(2.15796690418466,-6.4161839487493,55.9060231702519));
#61992=CARTESIAN_POINT('Ctrl Pts',(2.32689575810249,-6.35687785389252,55.9144716604962));
#61993=CARTESIAN_POINT('Ctrl Pts',(2.49332814330936,-6.29091438264594,55.9229201507406));
#61994=CARTESIAN_POINT('Ctrl Pts',(2.65960850164581,-6.22501116541832,55.9313609237517));
#61995=CARTESIAN_POINT('Ctrl Pts',(2.82339662827288,-6.15246281564555,55.9398016967628));
#61996=CARTESIAN_POINT('Ctrl Pts',(2.98414500579366,-6.07348068115778,55.948242469774));
#61997=CARTESIAN_POINT('Ctrl Pts',(3.14477126832602,-5.99455854666869,55.9566768306215));
#61998=CARTESIAN_POINT('Ctrl Pts',(3.30236208692806,-5.90921251732464,55.965111191469));
#61999=CARTESIAN_POINT('Ctrl Pts',(3.45639039551898,-5.81770181719243,55.9735455523165));
#62000=CARTESIAN_POINT('Ctrl Pts',(3.61032534809626,-5.72624658137226,55.9819748011277));
#62001=CARTESIAN_POINT('Ctrl Pts',(3.76070180963412,-5.62863429403779,55.9904040499389));
#62002=CARTESIAN_POINT('Ctrl Pts',(3.9070174327515,-5.5251700227392,55.99883329875));
#62003=CARTESIAN_POINT('Ctrl Pts',(4.05326681906635,-5.42175258951819,56.0072587316564));
#62004=CARTESIAN_POINT('Ctrl Pts',(4.19545876082964,-5.31248864703721,56.0156841645628));
#62005=CARTESIAN_POINT('Ctrl Pts',(4.33311969149858,-5.19772668953911,56.0241095974692));
#62006=CARTESIAN_POINT('Ctrl Pts',(4.47075038233014,-5.08298994168413,56.0325331795693));
#62007=CARTESIAN_POINT('Ctrl Pts',(4.60385178898657,-4.96275779810857,56.0409567616693));
#62008=CARTESIAN_POINT('Ctrl Pts',(4.73198284397695,-4.83741949434901,56.0493803437694));
#62009=CARTESIAN_POINT('Ctrl Pts',(4.86009956220309,-4.71209521486881,56.057802983343));
#62010=CARTESIAN_POINT('Ctrl Pts',(4.98324679917651,-4.58166614729252,56.0662256229166));
#62011=CARTESIAN_POINT('Ctrl Pts',(5.10101961156118,-4.44655911042103,56.0746482624902));
#62012=CARTESIAN_POINT('Ctrl Pts',(5.2187956692579,-4.31144835058083,56.0830711341555));
#62013=CARTESIAN_POINT('Ctrl Pts',(5.33119678831939,-4.17165961602029,56.0914940058208));
#62014=CARTESIAN_POINT('Ctrl Pts',(5.43785742312932,-4.02765386369253,56.0999168774861));
#62015=CARTESIAN_POINT('Ctrl Pts',(5.54453587145941,-3.88362406079188,56.1083411558653));
#62016=CARTESIAN_POINT('Ctrl Pts',(5.64547172619947,-3.73537610422097,56.1167654342445));
#62017=CARTESIAN_POINT('Ctrl Pts',(5.74034177830179,-3.58340135461869,56.1251897126237));
#62018=CARTESIAN_POINT('Ctrl Pts',(5.83527590330132,-3.4313239650126,56.1336196805531));
#62019=CARTESIAN_POINT('Ctrl Pts',(5.92413586282424,-3.27551503597956,56.1420496484824));
#62020=CARTESIAN_POINT('Ctrl Pts',(6.00664306343095,-3.1164929180951,56.1504796164117));
#62021=CARTESIAN_POINT('Ctrl Pts',(6.08917975960071,-2.95741395127055,56.1589125979769));
#62022=CARTESIAN_POINT('Ctrl Pts',(6.16535902041043,-2.79511980391235,56.167345579542));
#62023=CARTESIAN_POINT('Ctrl Pts',(6.23494949256094,-2.6301509130113,56.1757785611072));
#62024=CARTESIAN_POINT('Ctrl Pts',(6.30460398858736,-2.46503024920979,56.1842193010931));
#62025=CARTESIAN_POINT('Ctrl Pts',(6.36765746086084,-2.29723023499947,56.192660041079));
#62026=CARTESIAN_POINT('Ctrl Pts',(6.42392734140331,-2.12730968887255,56.2011007810649));
#62027=CARTESIAN_POINT('Ctrl Pts',(6.45504083694441,-2.03335494606355,56.2057679480001));
#62028=CARTESIAN_POINT('Ctrl Pts',(6.48408123300088,-1.93875215309201,56.2104351149353));
#62029=CARTESIAN_POINT('Ctrl Pts',(6.51102430173953,-1.84359744579918,56.2151022818705));
#62030=CARTESIAN_POINT('Ctrl Pts',(6.55802361925107,-1.67761018042295,56.2232436581478));
#62031=CARTESIAN_POINT('Ctrl Pts',(6.59873134817497,-1.50961294844202,56.2313850344251));
#62032=CARTESIAN_POINT('Ctrl Pts',(6.63297410745331,-1.34012816172708,56.2395264107024));
#62033=CARTESIAN_POINT('Ctrl Pts',(6.66718697503581,-1.17079132417862,56.2476606800892));
#62034=CARTESIAN_POINT('Ctrl Pts',(6.69494603443017,-0.999969873007824,
56.2557949494759));
#62035=CARTESIAN_POINT('Ctrl Pts',(6.71612773974867,-0.82820117325347,56.2639292188626));
#62036=CARTESIAN_POINT('Ctrl Pts',(6.73729499542218,-0.656549649934848,
56.2720579392483));
#62037=CARTESIAN_POINT('Ctrl Pts',(6.75189378570168,-0.483952526390221,
56.280186659634));
#62038=CARTESIAN_POINT('Ctrl Pts',(6.7598516754522,-0.310957112615279,56.2883153800197));
#62039=CARTESIAN_POINT('Ctrl Pts',(6.7678057700652,-0.138044200785899,56.2964402237983));
#62040=CARTESIAN_POINT('Ctrl Pts',(6.76912525409912,0.0352662581381283,
56.3045650675769));
#62041=CARTESIAN_POINT('Ctrl Pts',(6.76378956125084,0.208422098430536,56.3126899113555));
#62042=CARTESIAN_POINT('Ctrl Pts',(6.758455362207,0.381529461239114,56.3208124804665));
#62043=CARTESIAN_POINT('Ctrl Pts',(6.74646970953452,0.554481926106745,56.3289350495774));
#62044=CARTESIAN_POINT('Ctrl Pts',(6.72786414533262,0.726727625694658,56.3370576186884));
#62045=CARTESIAN_POINT('Ctrl Pts',(6.70925759269357,0.898982475988572,56.3451806193181));
#62046=CARTESIAN_POINT('Ctrl Pts',(6.68403046137004,1.07053012163054,56.3533036199478));
#62047=CARTESIAN_POINT('Ctrl Pts',(6.65226615470249,1.24082392264162,56.3614266205775));
#62048=CARTESIAN_POINT('Ctrl Pts',(6.63605166653127,1.32775252621626,56.3655731079856));
#62049=CARTESIAN_POINT('Ctrl Pts',(6.61813460331876,1.41435453243038,56.3697195953938));
#62050=CARTESIAN_POINT('Ctrl Pts',(6.59853119987784,1.50055823087234,56.3738660828019));
#62051=CARTESIAN_POINT('Ctrl Pts',(6.55605905001241,1.68732459571376,56.3828497388871));
#62052=CARTESIAN_POINT('Ctrl Pts',(6.50568935920778,1.87212817942224,56.3918333949723));
#62053=CARTESIAN_POINT('Ctrl Pts',(6.44763550895984,2.05433330878904,56.4008170510576));
#62054=CARTESIAN_POINT('Ctrl Pts',(6.38948192194162,2.23685146737018,56.4098161411035));
#62055=CARTESIAN_POINT('Ctrl Pts',(6.3236178621624,2.41676202112508,56.4188152311494));
#62056=CARTESIAN_POINT('Ctrl Pts',(6.25030544246359,2.59344768135199,56.4278143211954));
#62057=CARTESIAN_POINT('Ctrl Pts',(6.17682112349692,2.7705476252127,56.4368345118542));
#62058=CARTESIAN_POINT('Ctrl Pts',(6.09585359318461,2.94440732441414,56.4458547025131));
#62059=CARTESIAN_POINT('Ctrl Pts',(6.00771289633479,3.11443008513799,56.4548748931719));
#62060=CARTESIAN_POINT('Ctrl Pts',(5.91948293339877,3.28462503949042,56.4639042191921));
#62061=CARTESIAN_POINT('Ctrl Pts',(5.82406540606469,3.45097508289248,56.4729335452124));
#62062=CARTESIAN_POINT('Ctrl Pts',(5.72181547411105,3.61290972489259,56.4819628712326));
#62063=CARTESIAN_POINT('Ctrl Pts',(5.61942138691336,3.77507266756136,56.4910049270871));
#62064=CARTESIAN_POINT('Ctrl Pts',(5.51017576246176,3.93280755960706,56.5000469829417));
#62065=CARTESIAN_POINT('Ctrl Pts',(5.39447740201476,4.08557248854456,56.5090890387963));
#62066=CARTESIAN_POINT('Ctrl Pts',(5.29407113723749,4.21814615548606,56.5169359871087));
#62067=CARTESIAN_POINT('Ctrl Pts',(5.18880587225101,4.34697723133431,56.5247829354212));
#62068=CARTESIAN_POINT('Ctrl Pts',(5.07896658780163,4.47173203579941,56.5326298837336));
#62069=CARTESIAN_POINT('Ctrl Pts',(4.95782024282555,4.6093293322031,56.541284611521));
#62070=CARTESIAN_POINT('Ctrl Pts',(4.83100187746522,4.74208834403588,56.5499393393084));
#62071=CARTESIAN_POINT('Ctrl Pts',(4.69891621343056,4.86954570973098,56.5585940670958));
#62072=CARTESIAN_POINT('Ctrl Pts',(4.56699455858291,4.99684481314169,56.5672380484114));
#62073=CARTESIAN_POINT('Ctrl Pts',(4.42981887556032,5.11885519753723,56.5758820297269));
#62074=CARTESIAN_POINT('Ctrl Pts',(4.28783143721378,5.23514952661729,56.5845260110424));
#62075=CARTESIAN_POINT('Ctrl Pts',(4.14595390111223,5.3513538406369,56.5931633016749));
#62076=CARTESIAN_POINT('Ctrl Pts',(3.99927227098851,5.46185073004917,56.6018005923074));
#62077=CARTESIAN_POINT('Ctrl Pts',(3.84826372117765,5.5662514614656,56.6104378829399));
#62078=CARTESIAN_POINT('Ctrl Pts',(3.69739703195112,5.67055411665535,56.6190670595212));
#62079=CARTESIAN_POINT('Ctrl Pts',(3.5422117836102,5.76877186920301,56.6276962361025));
#62080=CARTESIAN_POINT('Ctrl Pts',(3.38321630546358,5.86055768937098,56.6363254126838));
#62081=CARTESIAN_POINT('Ctrl Pts',(3.28978520604009,5.91449412951221,56.6413962075549));
#62082=CARTESIAN_POINT('Ctrl Pts',(3.19503897899121,5.96621031813891,56.646467002426));
#62083=CARTESIAN_POINT('Ctrl Pts',(3.09908550384732,6.01564277861007,56.6515377972971));
#62084=CARTESIAN_POINT('Origin',(0.,0.,-63.6971797838103));
#62085=CARTESIAN_POINT('',(3.0990855038472,6.01564277861012,59.0457563580462));
#62086=CARTESIAN_POINT('',(3.09908550384712,6.01564277861017,58.6513967904261));
#62087=CARTESIAN_POINT('',(3.09908550384721,6.01564277861012,-63.6971797838103));
#62088=CARTESIAN_POINT('',(-6.767,-6.2375472749954E-10,57.6971797838394));
#62089=CARTESIAN_POINT('Ctrl Pts',(-6.767,-6.23560221358631E-10,57.6971797838395));
#62090=CARTESIAN_POINT('Ctrl Pts',(-6.76699999998286,-0.186007250183476,
57.7059292956522));
#62091=CARTESIAN_POINT('Ctrl Pts',(-6.75932637290819,-0.372014356438861,
57.7146788074649));
#62092=CARTESIAN_POINT('Ctrl Pts',(-6.74400518258228,-0.557389538207732,
57.7234283192776));
#62093=CARTESIAN_POINT('Ctrl Pts',(-6.72868405696884,-0.742763937002891,
57.7321777941348));
#62094=CARTESIAN_POINT('Ctrl Pts',(-6.70571545635014,-0.927506131023182,
57.7409272689921));
#62095=CARTESIAN_POINT('Ctrl Pts',(-6.6751773939133,-1.11098864071098,57.7496767438493));
#62096=CARTESIAN_POINT('Ctrl Pts',(-6.64463945792454,-1.29447039065802,
57.7584261824778));
#62097=CARTESIAN_POINT('Ctrl Pts',(-6.60653216989111,-1.47669218400177,
57.7671756211063));
#62098=CARTESIAN_POINT('Ctrl Pts',(-6.56098496070208,-1.65703510688252,
57.7759250597348));
#62099=CARTESIAN_POINT('Ctrl Pts',(-6.5154379363262,-1.83737729800064,57.7846744628614));
#62100=CARTESIAN_POINT('Ctrl Pts',(-6.46245112138313,-2.01584035604526,
57.7934238659881));
#62101=CARTESIAN_POINT('Ctrl Pts',(-6.4022044834151,-2.19181813856434,57.8021732691147));
#62102=CARTESIAN_POINT('Ctrl Pts',(-6.34195808490141,-2.36779522164779,
57.8109226374662));
#62103=CARTESIAN_POINT('Ctrl Pts',(-6.2744520139292,-2.54128677783604,57.8196720058178));
#62104=CARTESIAN_POINT('Ctrl Pts',(-6.19991555027716,-2.71170355485836,
57.8284213741693));
#62105=CARTESIAN_POINT('Ctrl Pts',(-6.12537937668529,-2.88211966870033,
57.8371707084725));
#62106=CARTESIAN_POINT('Ctrl Pts',(-6.04381298000202,-3.04946076475658,
57.8459200427757));
#62107=CARTESIAN_POINT('Ctrl Pts',(-5.95549339279206,-3.213158484795,57.8546693770788));
#62108=CARTESIAN_POINT('Ctrl Pts',(-5.86717414194521,-3.37685558139444,
57.8634186780604));
#62109=CARTESIAN_POINT('Ctrl Pts',(-5.772101888113,-3.53690907753474,57.872167979042));
#62110=CARTESIAN_POINT('Ctrl Pts',(-5.67059953277166,-3.69277537076518,
57.8809172800235));
#62111=CARTESIAN_POINT('Ctrl Pts',(-5.56909755557055,-3.84864108332618,
57.8896665484101));
#62112=CARTESIAN_POINT('Ctrl Pts',(-5.46116568117904,-4.00031938405425,
57.8984158167967));
#62113=CARTESIAN_POINT('Ctrl Pts',(-5.3471704844995,-4.14729511967709,57.9071650851834));
#62114=CARTESIAN_POINT('Ctrl Pts',(-5.2331757030352,-4.29427031995662,57.9159143217017));
#62115=CARTESIAN_POINT('Ctrl Pts',(-5.11311781910449,-4.43654276296921,
57.9246635582201));
#62116=CARTESIAN_POINT('Ctrl Pts',(-4.9874045888688,-4.57362924458579,57.9334127947384));
#62117=CARTESIAN_POINT('Ctrl Pts',(-4.86169180609106,-4.710715238263,57.9421620001151));
#62118=CARTESIAN_POINT('Ctrl Pts',(-4.73032391096716,-4.84261509628306,
57.9509112054918));
#62119=CARTESIAN_POINT('Ctrl Pts',(-4.59374706901301,-4.9688808464215,57.9596604108686));
#62120=CARTESIAN_POINT('Ctrl Pts',(-4.45717070184369,-5.09514615761976,
57.9684095858302));
#62121=CARTESIAN_POINT('Ctrl Pts',(-4.31538563449167,-5.21577720560456,
57.9771587607919));
#62122=CARTESIAN_POINT('Ctrl Pts',(-4.16887340902849,-5.33036429331947,
57.9859079357536));
#62123=CARTESIAN_POINT('Ctrl Pts',(-4.02236168072287,-5.44495099220788,
57.9946570810268));
#62124=CARTESIAN_POINT('Ctrl Pts',(-3.87112305211999,-5.55349359533604,
58.0034062263001));
#62125=CARTESIAN_POINT('Ctrl Pts',(-3.7156711687689,-5.65562346391444,58.0121553715733));
#62126=CARTESIAN_POINT('Ctrl Pts',(-3.56021980000273,-5.75775299441722,
58.0209044878847));
#62127=CARTESIAN_POINT('Ctrl Pts',(-3.40055544388173,-5.85346967551198,
58.029653604196));
#62128=CARTESIAN_POINT('Ctrl Pts',(-3.23722035832121,-5.94244843071194,
58.0384027205074));
#62129=CARTESIAN_POINT('Ctrl Pts',(-3.07388579987965,-6.03142689875748,
58.0471518085834));
#62130=CARTESIAN_POINT('Ctrl Pts',(-2.90688078732959,-6.11366734734653,
58.0559008966594));
#62131=CARTESIAN_POINT('Ctrl Pts',(-2.73677250553455,-6.18889047026607,
58.0646499847354));
#62132=CARTESIAN_POINT('Ctrl Pts',(-2.56666475859314,-6.26411335666943,
58.0733990453026));
#62133=CARTESIAN_POINT('Ctrl Pts',(-2.39345402398854,-6.33231884567268,
58.0821481058697));
#62134=CARTESIAN_POINT('Ctrl Pts',(-2.21772855885275,-6.39327529825276,
58.0908971664369));
#62135=CARTESIAN_POINT('Ctrl Pts',(-2.04200363164235,-6.45423156423482,
58.0996462002217));
#62136=CARTESIAN_POINT('Ctrl Pts',(-1.86376426001178,-6.50793874429595,
58.1083952340065));
#62137=CARTESIAN_POINT('Ctrl Pts',(-1.68361577561401,-6.55421443958799,
58.1171442677913));
#62138=CARTESIAN_POINT('Ctrl Pts',(-1.50346782772448,-6.60048999706431,
58.1258932755203));
#62139=CARTESIAN_POINT('Ctrl Pts',(-1.32141105596206,-6.6393340427734,58.1346422832492));
#62140=CARTESIAN_POINT('Ctrl Pts',(-1.1380637528501,-6.67061465642026,58.1433912909781));
#62141=CARTESIAN_POINT('Ctrl Pts',(-0.954716980551841,-6.70189517950577,
58.1521402733775));
#62142=CARTESIAN_POINT('Ctrl Pts',(-0.7700799668219,-6.72561226616107,58.160889255777));
#62143=CARTESIAN_POINT('Ctrl Pts',(-0.584779763451173,-6.74168537001379,
58.1696382381764));
#62144=CARTESIAN_POINT('Ctrl Pts',(-0.391489586975877,-6.75845153121429,
58.1787644685917));
#62145=CARTESIAN_POINT('Ctrl Pts',(-0.197478091193787,-6.7668998514816,
58.187890699007));
#62146=CARTESIAN_POINT('Ctrl Pts',(-0.00346214692596143,-6.76699911434446,
58.1970169294223));
#62147=CARTESIAN_POINT('Ctrl Pts',(0.184490799083379,-6.76709527524285,
58.2058579651372));
#62148=CARTESIAN_POINT('Ctrl Pts',(0.372447602746487,-6.75935633787485,
58.214699000852));
#62149=CARTESIAN_POINT('Ctrl Pts',(0.559756448778259,-6.74380914009665,
58.2235400365668));
#62150=CARTESIAN_POINT('Ctrl Pts',(0.745136131626023,-6.72842206866702,
58.2322900151801));
#62151=CARTESIAN_POINT('Ctrl Pts',(0.929880852525672,-6.70538686347671,
58.2410399937934));
#62152=CARTESIAN_POINT('Ctrl Pts',(1.11336305115256,-6.67478177293672,58.2497899724067));
#62153=CARTESIAN_POINT('Ctrl Pts',(1.29684337147669,-6.64417699570029,58.2585398614467));
#62154=CARTESIAN_POINT('Ctrl Pts',(1.47906091262423,-6.60600253535246,58.2672897504867));
#62155=CARTESIAN_POINT('Ctrl Pts',(1.65939671152076,-6.56038806426831,58.2760396395267));
#62156=CARTESIAN_POINT('Ctrl Pts',(1.8397307242563,-6.51477404497903,58.2847894419022));
#62157=CARTESIAN_POINT('Ctrl Pts',(2.01818275413056,-6.46172023271164,58.2935392442777));
#62158=CARTESIAN_POINT('Ctrl Pts',(2.19414664088833,-6.40140683899082,58.3022890466532));
#62159=CARTESIAN_POINT('Ctrl Pts',(2.37010884326244,-6.34109402260946,58.3110387652728));
#62160=CARTESIAN_POINT('Ctrl Pts',(2.54358267902205,-6.27352185677736,58.3197884838923));
#62161=CARTESIAN_POINT('Ctrl Pts',(2.71397890895495,-6.19891986411727,58.3285382025118));
#62162=CARTESIAN_POINT('Ctrl Pts',(2.88437356442055,-6.12431856078229,58.3372878402836));
#62163=CARTESIAN_POINT('Ctrl Pts',(3.05169040839584,-6.04268767556088,58.3460374780555));
#62164=CARTESIAN_POINT('Ctrl Pts',(3.21536112563705,-5.95430447926053,58.3547871158273));
#62165=CARTESIAN_POINT('Ctrl Pts',(3.37903038493717,-5.86592207025736,58.3635366756594));
#62166=CARTESIAN_POINT('Ctrl Pts',(3.53905333030013,-5.77078760672689,58.3722862354914));
#62167=CARTESIAN_POINT('Ctrl Pts',(3.69488643091041,-5.66922422053266,58.3810357953235));
#62168=CARTESIAN_POINT('Ctrl Pts',(3.85071819517023,-5.56766170529767,58.3897852801235));
#62169=CARTESIAN_POINT('Ctrl Pts',(4.0023599464658,-5.45967053421537,58.3985347649235));
#62170=CARTESIAN_POINT('Ctrl Pts',(4.14929663020678,-5.34561750170686,58.4072842497235));
#62171=CARTESIAN_POINT('Ctrl Pts',(4.29623210270428,-5.23156540937196,58.4160336623988));
#62172=CARTESIAN_POINT('Ctrl Pts',(4.43846235886454,-5.11145173133687,58.4247830750742));
#62173=CARTESIAN_POINT('Ctrl Pts',(4.57550431840671,-4.98568442966877,58.4335324877495));
#62174=CARTESIAN_POINT('Ctrl Pts',(4.71254519379645,-4.85991812295817,58.4422818312074));
#62175=CARTESIAN_POINT('Ctrl Pts',(4.84439764355994,-4.72849847589085,58.4510311746653));
#62176=CARTESIAN_POINT('Ctrl Pts',(4.97061384236511,-4.59187184382234,58.4597805181232));
#62177=CARTESIAN_POINT('Ctrl Pts',(5.09682908458846,-4.45524624723543,58.4685297952706));
#62178=CARTESIAN_POINT('Ctrl Pts',(5.2174079668758,-4.31341395511643,58.4772790724179));
#62179=CARTESIAN_POINT('Ctrl Pts',(5.33194095978389,-4.16685668116614,58.4860283495653));
#62180=CARTESIAN_POINT('Ctrl Pts',(5.44647312270003,-4.02030046927975,58.4947775633088));
#62181=CARTESIAN_POINT('Ctrl Pts',(5.55495930745849,-3.86901956987362,58.5035267770524));
#62182=CARTESIAN_POINT('Ctrl Pts',(5.6570310611201,-3.713527780093,58.5122759907959));
#62183=CARTESIAN_POINT('Ctrl Pts',(5.75910210899612,-3.55803706547627,58.5210251440421));
#62184=CARTESIAN_POINT('Ctrl Pts',(5.85475865728049,-3.39833575830077,58.5297742972883));
#62185=CARTESIAN_POINT('Ctrl Pts',(5.94367583097153,-3.2349662465511,58.5385234505345));
#62186=CARTESIAN_POINT('Ctrl Pts',(6.03259241936753,-3.0715978101771,58.5472725461897));
#62187=CARTESIAN_POINT('Ctrl Pts',(6.11476958496196,-2.90456146922724,58.5560216418448));
#62188=CARTESIAN_POINT('Ctrl Pts',(6.18992823598139,-2.73442451594487,58.5647707374999));
#62189=CARTESIAN_POINT('Ctrl Pts',(6.26508641723222,-2.56428862607966,58.5735197784701));
#62190=CARTESIAN_POINT('Ctrl Pts',(6.33322605591089,-2.39105242476208,58.5822688194402));
#62191=CARTESIAN_POINT('Ctrl Pts',(6.3941157376704,-2.21530425298102,58.5910178604103));
#62192=CARTESIAN_POINT('Ctrl Pts',(6.45500505906866,-2.03955712132414,58.5997668496013));
#62193=CARTESIAN_POINT('Ctrl Pts',(6.50864441561116,-1.86129831968967,58.6085158387923));
#62194=CARTESIAN_POINT('Ctrl Pts',(6.55485164064525,-1.68113323955312,58.6172648279833));
#62195=CARTESIAN_POINT('Ctrl Pts',(6.60199852651826,-1.49730435856674,58.6261917348596));
#62196=CARTESIAN_POINT('Ctrl Pts',(6.64140767451907,-1.31149113118293,58.6351186417359));
#62197=CARTESIAN_POINT('Ctrl Pts',(6.6729397527877,-1.12435050392021,58.6440455486122));
#62198=CARTESIAN_POINT('Ctrl Pts',(6.70384664839178,-0.940920291017168,
58.6527954627962));
#62199=CARTESIAN_POINT('Ctrl Pts',(6.72718585895831,-0.756215113729511,
58.6615453769802));
#62200=CARTESIAN_POINT('Ctrl Pts',(6.74287810456518,-0.57086238882548,58.6702952911642));
#62201=CARTESIAN_POINT('Ctrl Pts',(6.75857004157265,-0.385513309017313,
58.6790450332748));
#62202=CARTESIAN_POINT('Ctrl Pts',(6.76661529037181,-0.199516992707917,
58.6877947753854));
#62203=CARTESIAN_POINT('Ctrl Pts',(6.76698652349006,-0.0135052176538825,
58.6965445174959));
#62204=CARTESIAN_POINT('Ctrl Pts',(6.76735774980119,0.172503146589083,58.7052940991666));
#62205=CARTESIAN_POINT('Ctrl Pts',(6.76005524144565,0.358526682383054,58.7140436808372));
#62206=CARTESIAN_POINT('Ctrl Pts',(6.74510380210459,0.543933542663219,58.7227932625079));
#62207=CARTESIAN_POINT('Ctrl Pts',(6.7301526170505,0.729337249631886,58.7315426953698));
#62208=CARTESIAN_POINT('Ctrl Pts',(6.70755278437173,0.914124016400014,58.7402921282317));
#62209=CARTESIAN_POINT('Ctrl Pts',(6.67738106399364,1.09766621803678,58.7490415610936));
#62210=CARTESIAN_POINT('Ctrl Pts',(6.64720981666837,1.28120554197365,58.757790856776));
#62211=CARTESIAN_POINT('Ctrl Pts',(6.60946696569625,1.46350005704353,58.7665401524583));
#62212=CARTESIAN_POINT('Ctrl Pts',(6.56428069997631,1.64393062259896,58.7752894481407));
#62213=CARTESIAN_POINT('Ctrl Pts',(6.51909508267909,1.82435859897652,58.7840386182707));
#62214=CARTESIAN_POINT('Ctrl Pts',(6.46646633399376,2.00292240139141,58.7927877884007));
#62215=CARTESIAN_POINT('Ctrl Pts',(6.40657319579473,2.1790155774855,58.8015369585307));
#62216=CARTESIAN_POINT('Ctrl Pts',(6.34668083749142,2.35510646059047,58.8102860147337));
#62217=CARTESIAN_POINT('Ctrl Pts',(6.27952437123319,2.52872651047601,58.8190350709368));
#62218=CARTESIAN_POINT('Ctrl Pts',(6.20533187313181,2.69928608048396,58.8277841271399));
#62219=CARTESIAN_POINT('Ctrl Pts',(6.12831449761773,2.87633970163138,58.8368663034277));
#62220=CARTESIAN_POINT('Ctrl Pts',(6.04371489440355,3.05009490607377,58.8459484797154));
#62221=CARTESIAN_POINT('Ctrl Pts',(5.95184265097576,3.21991584641988,58.8550306560032));
#62222=CARTESIAN_POINT('Ctrl Pts',(5.86333281311414,3.38352155947026,58.8637804363576));
#62223=CARTESIAN_POINT('Ctrl Pts',(5.76807337210469,3.54347560944871,58.872530216712));
#62224=CARTESIAN_POINT('Ctrl Pts',(5.66638790060032,3.69923467218969,58.8812799970664));
#62225=CARTESIAN_POINT('Ctrl Pts',(5.56470608475312,3.8549881352936,58.8900294628607));
#62226=CARTESIAN_POINT('Ctrl Pts',(5.45659885738445,4.00654667295086,58.898778928655));
#62227=CARTESIAN_POINT('Ctrl Pts',(5.34243340550957,4.15339551544221,58.9075283944492));
#62228=CARTESIAN_POINT('Ctrl Pts',(5.22827145109994,4.30023985921074,58.9162775922031));
#62229=CARTESIAN_POINT('Ctrl Pts',(5.10805181946473,4.44237457029397,58.925026789957));
#62230=CARTESIAN_POINT('Ctrl Pts',(4.98218281249954,4.57931691661913,58.9337759877109));
#62231=CARTESIAN_POINT('Ctrl Pts',(4.85631699262644,4.71625579546744,58.9425249639289));
#62232=CARTESIAN_POINT('Ctrl Pts',(4.72480227757301,4.84800236169429,58.9512739401469));
#62233=CARTESIAN_POINT('Ctrl Pts',(4.58808530812664,4.97410918711607,58.9600229163649));
#62234=CARTESIAN_POINT('Ctrl Pts',(4.45135945020618,5.10022421120736,58.9687724613861));
#62235=CARTESIAN_POINT('Ctrl Pts',(4.30943087170825,5.22069856642706,58.9775220064073));
#62236=CARTESIAN_POINT('Ctrl Pts',(4.16278164284432,5.33512305331361,58.9862715514285));
#62237=CARTESIAN_POINT('Ctrl Pts',(4.01614103495537,5.44954081360061,58.9950205820958));
#62238=CARTESIAN_POINT('Ctrl Pts',(3.86478055793785,5.55790924095894,59.003769612763));
#62239=CARTESIAN_POINT('Ctrl Pts',(3.70921425771593,5.6598602977774,59.0125186434303));
#62240=CARTESIAN_POINT('Ctrl Pts',(3.55364584489039,5.7618127390999,59.0212677929101));
#62241=CARTESIAN_POINT('Ctrl Pts',(3.39387173422587,5.85734747842258,59.03001694239));
#62242=CARTESIAN_POINT('Ctrl Pts',(3.2304345605002,5.94614005471835,59.0387660918698));
#62243=CARTESIAN_POINT('Ctrl Pts',(3.18690768777967,5.96978744826323,59.0410961805953));
#62244=CARTESIAN_POINT('Ctrl Pts',(3.14312114968588,5.99295688506664,59.0434262693208));
#62245=CARTESIAN_POINT('Ctrl Pts',(3.0990855038472,6.01564277861012,59.0457563580462));
#62246=CARTESIAN_POINT('Ctrl Pts',(3.09908550384732,6.01564277861007,57.0457563580462));
#62247=CARTESIAN_POINT('Ctrl Pts',(2.93373232018333,6.10082796552478,57.0545058059455));
#62248=CARTESIAN_POINT('Ctrl Pts',(2.76486502144423,6.17919158180192,57.0632552538448));
#62249=CARTESIAN_POINT('Ctrl Pts',(2.59305716434342,6.25046746591383,57.0720047017441));
#62250=CARTESIAN_POINT('Ctrl Pts',(2.4212506945927,6.32174277447229,57.0807540789915));
#62251=CARTESIAN_POINT('Ctrl Pts',(2.24650397871044,6.38593035557831,57.089503456239));
#62252=CARTESIAN_POINT('Ctrl Pts',(2.06941053323754,6.44281220003544,57.0982528334864));
#62253=CARTESIAN_POINT('Ctrl Pts',(1.89231845896678,6.49969360406686,57.107002142989));
#62254=CARTESIAN_POINT('Ctrl Pts',(1.71287996431511,6.54926929700879,57.1157514524916));
#62255=CARTESIAN_POINT('Ctrl Pts',(1.53170449173522,6.59137090065475,57.1245007619941));
#62256=CARTESIAN_POINT('Ctrl Pts',(1.350530361782,6.63347219230077,57.1332500066587));
#62257=CARTESIAN_POINT('Ctrl Pts',(1.16761955878886,6.66809944062446,57.1419992513233));
#62258=CARTESIAN_POINT('Ctrl Pts',(0.983593309311028,6.69513503985383,57.1507484959879));
#62259=CARTESIAN_POINT('Ctrl Pts',(0.799568362460467,6.72217044771209,57.1594976787211));
#62260=CARTESIAN_POINT('Ctrl Pts',(0.614428268439024,6.74161427235973,57.1682468614543));
#62261=CARTESIAN_POINT('Ctrl Pts',(0.42880181633064,6.753400476968,57.1769960441874));
#62262=CARTESIAN_POINT('Ctrl Pts',(0.243176616523071,6.76518660206241,57.1857451678956));
#62263=CARTESIAN_POINT('Ctrl Pts',(0.0570653511656648,6.76931519233997,
57.1944942916037));
#62264=CARTESIAN_POINT('Ctrl Pts',(-0.12889990079991,6.76577222610795,57.2032434153118));
#62265=CARTESIAN_POINT('Ctrl Pts',(-0.31486395994192,6.76222928260133,57.2119924829011));
#62266=CARTESIAN_POINT('Ctrl Pts',(-0.500681721080598,6.75101488651277,
57.2207415504904));
#62267=CARTESIAN_POINT('Ctrl Pts',(-0.685722110173234,6.73216712415992,
57.2294906180796));
#62268=CARTESIAN_POINT('Ctrl Pts',(-0.87076137382758,6.71331947644146,57.238239632456));
#62269=CARTESIAN_POINT('Ctrl Pts',(-1.05502298984343,6.68683858439996,57.2469886468323));
#62270=CARTESIAN_POINT('Ctrl Pts',(-1.23788117676063,6.65281438131425,57.2557376612087));
#62271=CARTESIAN_POINT('Ctrl Pts',(-1.43009641451788,6.61704912302378,57.2649343720962));
#62272=CARTESIAN_POINT('Ctrl Pts',(-1.62076048992682,6.57294837083168,57.2741310829838));
#62273=CARTESIAN_POINT('Ctrl Pts',(-1.8091579896111,6.52067760042055,57.2833277938713));
#62274=CARTESIAN_POINT('Ctrl Pts',(-1.98840443002993,6.47094578577415,57.2920777915778));
#62275=CARTESIAN_POINT('Ctrl Pts',(-2.16559895952176,6.41381888474481,57.3008277892843));
#62276=CARTESIAN_POINT('Ctrl Pts',(-2.3401396624231,6.34949095285239,57.3095777869908));
#62277=CARTESIAN_POINT('Ctrl Pts',(-2.51467682554003,6.2851643255669,57.3183276072424));
#62278=CARTESIAN_POINT('Ctrl Pts',(-2.68656000078831,6.21363705879665,57.327077427494));
#62279=CARTESIAN_POINT('Ctrl Pts',(-2.85520533840878,6.13515211510864,57.3358272477456));
#62280=CARTESIAN_POINT('Ctrl Pts',(-3.02384747998314,6.05666865881128,57.3445769021768));
#62281=CARTESIAN_POINT('Ctrl Pts',(-3.1892516468452,5.97122791039853,57.3533265566081));
#62282=CARTESIAN_POINT('Ctrl Pts',(-3.35085601829138,5.87912008251919,57.3620762110393));
#62283=CARTESIAN_POINT('Ctrl Pts',(-3.51245754191393,5.78701387778189,57.3708257112825));
#62284=CARTESIAN_POINT('Ctrl Pts',(-3.67025915510905,5.68824097061002,57.3795752115256));
#62285=CARTESIAN_POINT('Ctrl Pts',(-3.82372487928799,5.58313684656879,57.3883247117687));
#62286=CARTESIAN_POINT('Ctrl Pts',(-3.97718810300752,5.47803443501806,57.3970740694539));
#62287=CARTESIAN_POINT('Ctrl Pts',(-4.12631534262969,5.36660117496419,57.4058234271389));
#62288=CARTESIAN_POINT('Ctrl Pts',(-4.2706000988616,5.24921554097404,57.4145727848241));
#62289=CARTESIAN_POINT('Ctrl Pts',(-4.4148826959415,5.13183166360346,57.4233220115792));
#62290=CARTESIAN_POINT('Ctrl Pts',(-4.55432273235027,5.00849577139527,57.4320712383344));
#62291=CARTESIAN_POINT('Ctrl Pts',(-4.68844662480147,4.879626752774,57.4408204650896));
#62292=CARTESIAN_POINT('Ctrl Pts',(-4.822568688351,4.75075949139941,57.4495695725411));
#62293=CARTESIAN_POINT('Ctrl Pts',(-4.95137454637806,4.61635945312585,57.4583186799926));
#62294=CARTESIAN_POINT('Ctrl Pts',(-5.07442674461024,4.47688309134652,57.4670677874441));
#62295=CARTESIAN_POINT('Ctrl Pts',(-5.19747742838485,4.33740844616415,57.4758167872165));
#62296=CARTESIAN_POINT('Ctrl Pts',(-5.31477440450874,4.19285781736096,57.4845657869888));
#62297=CARTESIAN_POINT('Ctrl Pts',(-5.42591931531101,4.04372211999476,57.4933147867612));
#62298=CARTESIAN_POINT('Ctrl Pts',(-5.53707636462927,3.89457013500878,57.5020647420418));
#62299=CARTESIAN_POINT('Ctrl Pts',(-5.64207983273414,3.74083230916505,57.5108146973224));
#62300=CARTESIAN_POINT('Ctrl Pts',(-5.74057303468689,3.5830308725192,57.5195646526029));
#62301=CARTESIAN_POINT('Ctrl Pts',(-5.83906243363715,3.42523552887517,57.5283142700317));
#62302=CARTESIAN_POINT('Ctrl Pts',(-5.93104191768382,3.26337713157073,57.5370638874605));
#62303=CARTESIAN_POINT('Ctrl Pts',(-6.01619906699618,3.09800545291229,57.5458135048894));
#62304=CARTESIAN_POINT('Ctrl Pts',(-6.10135338095344,2.93263928039676,57.5545628309947));
#62305=CARTESIAN_POINT('Ctrl Pts',(-6.17968568352799,2.76376031540312,57.5633121571001));
#62306=CARTESIAN_POINT('Ctrl Pts',(-6.25092992694846,2.59194213831638,57.5720614832055));
#62307=CARTESIAN_POINT('Ctrl Pts',(-6.32217217691075,2.42012876880897,57.5808105644993));
#62308=CARTESIAN_POINT('Ctrl Pts',(-6.38632665483831,2.24537661647728,57.5895596457931));
#62309=CARTESIAN_POINT('Ctrl Pts',(-6.44317547869338,2.06827917621493,57.5983087270869));
#62310=CARTESIAN_POINT('Ctrl Pts',(-6.50002944235922,1.89116572423472,57.6070585994019));
#62311=CARTESIAN_POINT('Ctrl Pts',(-6.54957634250382,1.71170683289258,57.6158084717169));
#62312=CARTESIAN_POINT('Ctrl Pts',(-6.59164787708379,1.53051209225436,57.6245583440318));
#62313=CARTESIAN_POINT('Ctrl Pts',(-6.63371649074999,1.34932993148083,57.6333076088666));
#62314=CARTESIAN_POINT('Ctrl Pts',(-6.66831071257119,1.16641244174038,57.6420568737014));
#62315=CARTESIAN_POINT('Ctrl Pts',(-6.69531304840331,0.982380875160158,
57.6508061385362));
#62316=CARTESIAN_POINT('Ctrl Pts',(-6.72231677033042,0.798339861795985,
57.6595558524919));
#62317=CARTESIAN_POINT('Ctrl Pts',(-6.74172778477889,0.613184940730294,
57.6683055664475));
#62318=CARTESIAN_POINT('Ctrl Pts',(-6.75348015835517,0.42754502769069,57.6770552804032));
#62319=CARTESIAN_POINT('Ctrl Pts',(-6.76249038365208,0.285219953548979,
57.6837634482054));
#62320=CARTESIAN_POINT('Ctrl Pts',(-6.76699999999987,0.142609995761489,
57.6904716160076));
#62321=CARTESIAN_POINT('Ctrl Pts',(-6.767,6.12589398735536E-12,57.6971797838098));
#62322=CARTESIAN_POINT('',(-6.76724680008539,0.000596459099932123,57.3032472956769));
#62323=CARTESIAN_POINT('Ctrl Pts',(3.09908550384732,6.01564277861007,56.6515377972971));
#62324=CARTESIAN_POINT('Ctrl Pts',(2.93599067927878,6.09966452411166,56.6601567701762));
#62325=CARTESIAN_POINT('Ctrl Pts',(2.76940673124068,6.17708587161028,56.6687757430553));
#62326=CARTESIAN_POINT('Ctrl Pts',(2.59988413276071,6.24763087067563,56.6773947159345));
#62327=CARTESIAN_POINT('Ctrl Pts',(2.50810438171936,6.28582402314901,56.6820610388447));
#62328=CARTESIAN_POINT('Ctrl Pts',(2.41546370318375,6.3220023997654,56.6867273617549));
#62329=CARTESIAN_POINT('Ctrl Pts',(2.3220522869404,6.35612792324973,56.691393684665));
#62330=CARTESIAN_POINT('Ctrl Pts',(2.15338129672925,6.41774764885778,56.6998195638301));
#62331=CARTESIAN_POINT('Ctrl Pts',(1.98226984749979,6.47264427983321,56.7082454429952));
#62332=CARTESIAN_POINT('Ctrl Pts',(1.80928191798352,6.52064321530153,56.7166713221602));
#62333=CARTESIAN_POINT('Ctrl Pts',(1.6362538245622,6.5686532950427,56.7250991576249));
#62334=CARTESIAN_POINT('Ctrl Pts',(1.46134870160362,6.6097623975066,56.7335269930895));
#62335=CARTESIAN_POINT('Ctrl Pts',(1.28514353867964,6.64384640739007,56.7419548285541));
#62336=CARTESIAN_POINT('Ctrl Pts',(1.10887360822069,6.677942945495,56.7503857618288));
#62337=CARTESIAN_POINT('Ctrl Pts',(0.93130301030162,6.70500917940863,56.7588166951035));
#62338=CARTESIAN_POINT('Ctrl Pts',(0.753017112247756,6.72497243330128,56.7672476283782));
#62339=CARTESIAN_POINT('Ctrl Pts',(0.574567372966716,6.74495403303087,56.7756863095144));
#62340=CARTESIAN_POINT('Ctrl Pts',(0.39540134989818,6.75781957449781,56.7841249906507));
#62341=CARTESIAN_POINT('Ctrl Pts',(0.216108822565234,6.76354832738035,56.7925636717869));
#62342=CARTESIAN_POINT('Ctrl Pts',(0.0367222718658691,6.76928008449647,
56.8010067782789));
#62343=CARTESIAN_POINT('Ctrl Pts',(-0.142790584228386,6.76786758600262,
56.8094498847708));
#62344=CARTESIAN_POINT('Ctrl Pts',(-0.321841221534579,6.75934221859799,
56.8178929912628));
#62345=CARTESIAN_POINT('Ctrl Pts',(-0.501079966452768,6.75080789458461,
56.8263449679415));
#62346=CARTESIAN_POINT('Ctrl Pts',(-0.679855192202551,6.73514579800707,
56.8347969446202));
#62347=CARTESIAN_POINT('Ctrl Pts',(-0.8575836666143,6.71243914346763,56.843248921299));
#62348=CARTESIAN_POINT('Ctrl Pts',(-0.906008180769598,6.70625240992476,
56.8455517760648));
#62349=CARTESIAN_POINT('Ctrl Pts',(-0.954355044586321,6.69954300753287,
56.8478546308306));
#62350=CARTESIAN_POINT('Ctrl Pts',(-1.00261260229868,6.6923132749231,56.8501574855964));
#62351=CARTESIAN_POINT('Ctrl Pts',(-1.17690391505033,6.66620172582829,56.8584746818914));
#62352=CARTESIAN_POINT('Ctrl Pts',(-1.35034293822587,6.63325193364448,56.8667918781864));
#62353=CARTESIAN_POINT('Ctrl Pts',(-1.52236274074635,6.59353476411456,56.8751090744814));
#62354=CARTESIAN_POINT('Ctrl Pts',(-1.69423744372123,6.55385109621159,56.8834192551806));
#62355=CARTESIAN_POINT('Ctrl Pts',(-1.8646949739395,6.50741150195246,56.8917294358798));
#62356=CARTESIAN_POINT('Ctrl Pts',(-2.03317652023222,6.45433824939292,56.900039616579));
#62357=CARTESIAN_POINT('Ctrl Pts',(-2.20154680928724,6.40130004389701,56.9083443096282));
#62358=CARTESIAN_POINT('Ctrl Pts',(-2.36794338382564,6.34163701305229,56.9166490026775));
#62359=CARTESIAN_POINT('Ctrl Pts',(-2.5318203548967,6.27552186599097,56.9249536957267));
#62360=CARTESIAN_POINT('Ctrl Pts',(-2.69561911035898,6.20943827453165,56.9332544250914));
#62361=CARTESIAN_POINT('Ctrl Pts',(-2.85690033703638,6.13690883383908,56.941555154456));
#62362=CARTESIAN_POINT('Ctrl Pts',(-3.01513575662215,6.05815527773419,56.9498558838207));
#62363=CARTESIAN_POINT('Ctrl Pts',(-3.17332461156488,5.97942489678969,56.9581541704927));
#62364=CARTESIAN_POINT('Ctrl Pts',(-3.32846913498271,5.8944742061522,56.9664524571647));
#62365=CARTESIAN_POINT('Ctrl Pts',(-3.48006319063366,5.80357210597031,56.9747507438367));
#62366=CARTESIAN_POINT('Ctrl Pts',(-3.63167266766553,5.71266075848709,56.983049874678));
#62367=CARTESIAN_POINT('Ctrl Pts',(-3.77973065308717,5.61579696418062,56.9913490055192));
#62368=CARTESIAN_POINT('Ctrl Pts',(-3.92375718192527,5.51329471163023,56.9996481363604));
#62369=CARTESIAN_POINT('Ctrl Pts',(-4.06779831126174,5.41078206804992,57.0079481085151));
#62370=CARTESIAN_POINT('Ctrl Pts',(-4.20780688556142,5.30263002828526,57.0162480806697));
#62371=CARTESIAN_POINT('Ctrl Pts',(-4.34333349638092,5.18919484498467,57.0245480528243));
#62372=CARTESIAN_POINT('Ctrl Pts',(-4.47889634541887,5.07572933045299,57.0328502442937));
#62373=CARTESIAN_POINT('Ctrl Pts',(-4.60997457558108,4.95697808015974,57.041152435763));
#62374=CARTESIAN_POINT('Ctrl Pts',(-4.73615318537281,4.83333652921903,57.0494546272324));
#62375=CARTESIAN_POINT('Ctrl Pts',(-4.86238648383141,4.70964138923021,57.0577604170595));
#62376=CARTESIAN_POINT('Ctrl Pts',(-4.98371568120406,4.58105196761277,57.0660662068867));
#62377=CARTESIAN_POINT('Ctrl Pts',(-5.09976371645401,4.44799944203449,57.0743719967138));
#62378=CARTESIAN_POINT('Ctrl Pts',(-5.21594893825968,4.31478962798792,57.0826876052569));
#62379=CARTESIAN_POINT('Ctrl Pts',(-5.32684029541498,4.17710643101975,57.0910032138001));
#62380=CARTESIAN_POINT('Ctrl Pts',(-5.43210127579277,4.03541382382657,57.0993188223432));
#62381=CARTESIAN_POINT('Ctrl Pts',(-5.5374288366751,3.89363159210926,57.1076396907406));
#62382=CARTESIAN_POINT('Ctrl Pts',(-5.63711872241454,3.74783517938533,57.1159605591379));
#62383=CARTESIAN_POINT('Ctrl Pts',(-5.73087856432538,3.59851634440583,57.1242814275352));
#62384=CARTESIAN_POINT('Ctrl Pts',(-5.82477777575151,3.4489755541283,57.132614664505));
#62385=CARTESIAN_POINT('Ctrl Pts',(-5.91272915426113,3.29590217932676,57.1409479014748));
#62386=CARTESIAN_POINT('Ctrl Pts',(-5.99448634151743,3.13981249461827,57.1492811384446));
#62387=CARTESIAN_POINT('Ctrl Pts',(-6.05467324173071,3.02490450190048,57.1554157881162));
#62388=CARTESIAN_POINT('Ctrl Pts',(-6.11150423265171,2.90836233345991,57.1615504377878));
#62389=CARTESIAN_POINT('Ctrl Pts',(-6.16489799614201,2.79039812520798,57.1676850874594));
#62390=CARTESIAN_POINT('Ctrl Pts',(-6.24111848062213,2.62200225804067,57.1764424017883));
#62391=CARTESIAN_POINT('Ctrl Pts',(-6.31054009248221,2.45025035891108,57.1851997161172));
#62392=CARTESIAN_POINT('Ctrl Pts',(-6.37287157082253,2.27569702328804,57.1939570304461));
#62393=CARTESIAN_POINT('Ctrl Pts',(-6.43744238794568,2.09487263386455,57.2030289625914));
#62394=CARTESIAN_POINT('Ctrl Pts',(-6.494403976871,1.91104198712258,57.2121008947367));
#62395=CARTESIAN_POINT('Ctrl Pts',(-6.54348336297778,1.72485201638661,57.221172826882));
#62396=CARTESIAN_POINT('Ctrl Pts',(-6.59058882189029,1.54615043284722,57.2298798943665));
#62397=CARTESIAN_POINT('Ctrl Pts',(-6.63043352000807,1.3652759072758,57.2385869618509));
#62398=CARTESIAN_POINT('Ctrl Pts',(-6.66282352986,1.18282357515561,57.2472940293354));
#62399=CARTESIAN_POINT('Ctrl Pts',(-6.69514768823904,1.00074218317589,57.2559833946573));
#62400=CARTESIAN_POINT('Ctrl Pts',(-6.72004731754403,0.817089655723656,
57.2646727599792));
#62401=CARTESIAN_POINT('Ctrl Pts',(-6.73737803352117,0.632476271038214,
57.2733621253011));
#62402=CARTESIAN_POINT('Ctrl Pts',(-6.75466194895993,0.448361423505387,
57.2820280255235));
#62403=CARTESIAN_POINT('Ctrl Pts',(-6.76441768063083,0.263291174265457,
57.290693925746));
#62404=CARTESIAN_POINT('Ctrl Pts',(-6.76655176891214,0.0778855482874975,
57.2993598259684));
#62405=CARTESIAN_POINT('Ctrl Pts',(-6.76683582396433,0.053207372962864,
57.3005132893755));
#62406=CARTESIAN_POINT('Ctrl Pts',(-6.76698492294256,0.0285232737042095,
57.3016667527825));
#62407=CARTESIAN_POINT('Ctrl Pts',(-6.76699891346671,0.00383472820380105,
57.3028202161896));
#62408=CARTESIAN_POINT('Ctrl Pts',(-6.767,5.9890047246399E-12,57.3028202161897));
#62409=CARTESIAN_POINT('Ctrl Pts',(-6.76700000000017,-0.186007249554085,
57.3115697280025));
#62410=CARTESIAN_POINT('Ctrl Pts',(-6.75932637294279,-0.37201435581034,
57.3203192398152));
#62411=CARTESIAN_POINT('Ctrl Pts',(-6.74400518263409,-0.557389537580792,
57.329068751628));
#62412=CARTESIAN_POINT('Ctrl Pts',(-6.7286840570379,-0.742763936377278,
57.3378182264852));
#62413=CARTESIAN_POINT('Ctrl Pts',(-6.70571545643639,-0.927506130399604,
57.3465677013423));
#62414=CARTESIAN_POINT('Ctrl Pts',(-6.67517739401663,-1.11098864009015,
57.3553171761995));
#62415=CARTESIAN_POINT('Ctrl Pts',(-6.64463945804491,-1.29447039004018,
57.3640666148281));
#62416=CARTESIAN_POINT('Ctrl Pts',(-6.60653217002839,-1.47669218338763,
57.3728160534566));
#62417=CARTESIAN_POINT('Ctrl Pts',(-6.56098496085608,-1.65703510627276,
57.3815654920851));
#62418=CARTESIAN_POINT('Ctrl Pts',(-6.51543793649699,-1.83737729739503,
57.3903148952117));
#62419=CARTESIAN_POINT('Ctrl Pts',(-6.46245112157053,-2.01584035544447,
57.3990642983384));
#62420=CARTESIAN_POINT('Ctrl Pts',(-6.40220448361889,-2.19181813796906,
57.407813701465));
#62421=CARTESIAN_POINT('Ctrl Pts',(-6.34195808512156,-2.36779522105814,
57.4165630698165));
#62422=CARTESIAN_POINT('Ctrl Pts',(-6.27445201416547,-2.54128677725269,
57.4253124381681));
#62423=CARTESIAN_POINT('Ctrl Pts',(-6.19991555052926,-2.71170355428198,
57.4340618065196));
#62424=CARTESIAN_POINT('Ctrl Pts',(-6.12537937695322,-2.8821196681309,57.4428111408228));
#62425=CARTESIAN_POINT('Ctrl Pts',(-6.0438129802855,-3.04946076419476,57.451560475126));
#62426=CARTESIAN_POINT('Ctrl Pts',(-5.95549339309074,-3.21315848424142,
57.4603098094292));
#62427=CARTESIAN_POINT('Ctrl Pts',(-5.86717414225902,-3.37685558084921,
57.4690591104107));
#62428=CARTESIAN_POINT('Ctrl Pts',(-5.7721018884416,-3.53690907699847,57.4778084113923));
#62429=CARTESIAN_POINT('Ctrl Pts',(-5.67059953311466,-3.69277537023847,
57.4865577123738));
#62430=CARTESIAN_POINT('Ctrl Pts',(-5.56909755592801,-3.84864108280892,
57.4953069807605));
#62431=CARTESIAN_POINT('Ctrl Pts',(-5.46116568155057,-4.00031938354704,
57.5040562491471));
#62432=CARTESIAN_POINT('Ctrl Pts',(-5.34717048488466,-4.14729511918049,
57.5128055175337));
#62433=CARTESIAN_POINT('Ctrl Pts',(-5.23317570343384,-4.29427031947084,
57.5215547540521));
#62434=CARTESIAN_POINT('Ctrl Pts',(-5.11311781951614,-4.43654276249479,
57.5303039905704));
#62435=CARTESIAN_POINT('Ctrl Pts',(-4.98740458929298,-4.57362924412324,
57.5390532270888));
#62436=CARTESIAN_POINT('Ctrl Pts',(-4.86169180652793,-4.71071523781213,
57.5478024324655));
#62437=CARTESIAN_POINT('Ctrl Pts',(-4.73032391141624,-4.84261509584439,
57.5565516378422));
#62438=CARTESIAN_POINT('Ctrl Pts',(-4.59374706947377,-4.96888084599552,
57.5653008432189));
#62439=CARTESIAN_POINT('Ctrl Pts',(-4.45717070231576,-5.09514615720682,
57.5740500181806));
#62440=CARTESIAN_POINT('Ctrl Pts',(-4.31538563497451,-5.21577720520509,
57.5827991931423));
#62441=CARTESIAN_POINT('Ctrl Pts',(-4.16887340952149,-5.33036429293389,
57.591548368104));
#62442=CARTESIAN_POINT('Ctrl Pts',(-4.02236168122615,-5.44495099183611,
57.6002975133773));
#62443=CARTESIAN_POINT('Ctrl Pts',(-3.87112305263296,-5.55349359497849,
57.6090466586505));
#62444=CARTESIAN_POINT('Ctrl Pts',(-3.71567116929095,-5.65562346357146,
57.6177958039238));
#62445=CARTESIAN_POINT('Ctrl Pts',(-3.56021980053429,-5.75775299408854,
57.6265449202352));
#62446=CARTESIAN_POINT('Ctrl Pts',(-3.4005554444222,-5.85346967519799,57.6352940365465));
#62447=CARTESIAN_POINT('Ctrl Pts',(-3.23722035886999,-5.94244843041298,
57.6440431528579));
#62448=CARTESIAN_POINT('Ctrl Pts',(-3.07388580043652,-6.03142689847368,
57.6527922409339));
#62449=CARTESIAN_POINT('Ctrl Pts',(-2.90688078789391,-6.11366734707822,
57.6615413290099));
#62450=CARTESIAN_POINT('Ctrl Pts',(-2.73677250610566,-6.18889047001352,
57.670290417086));
#62451=CARTESIAN_POINT('Ctrl Pts',(-2.56666475917128,-6.26411335643254,
57.6790394776531));
#62452=CARTESIAN_POINT('Ctrl Pts',(-2.39345402457307,-6.33231884545174,
57.6877885382203));
#62453=CARTESIAN_POINT('Ctrl Pts',(-2.21772855944301,-6.39327529804801,
57.6965375987874));
#62454=CARTESIAN_POINT('Ctrl Pts',(-2.04200363223832,-6.45423156404626,
57.7052866325722));
#62455=CARTESIAN_POINT('Ctrl Pts',(-1.86376426061281,-6.50793874412382,
57.714035666357));
#62456=CARTESIAN_POINT('Ctrl Pts',(-1.68361577621941,-6.55421443943247,
57.7227847001418));
#62457=CARTESIAN_POINT('Ctrl Pts',(-1.50346782833437,-6.60048999692538,
57.7315337078707));
#62458=CARTESIAN_POINT('Ctrl Pts',(-1.32141105657577,-6.63933404265125,
57.7402827155996));
#62459=CARTESIAN_POINT('Ctrl Pts',(-1.13806375346692,-6.67061465631502,
57.7490317233286));
#62460=CARTESIAN_POINT('Ctrl Pts',(-0.954716981171651,-6.70189517941747,
57.757780705728));
#62461=CARTESIAN_POINT('Ctrl Pts',(-0.770079967444,-6.72561226608984,57.7665296881274));
#62462=CARTESIAN_POINT('Ctrl Pts',(-0.584779764074859,-6.74168536995969,
57.7752786705269));
#62463=CARTESIAN_POINT('Ctrl Pts',(-0.391489587594695,-6.75845153117863,
57.7844049009425));
#62464=CARTESIAN_POINT('Ctrl Pts',(-0.197478091806922,-6.76689985146389,
57.7935311313581));
#62465=CARTESIAN_POINT('Ctrl Pts',(-0.00346214753266241,-6.76699911434415,
57.8026573617737));
#62466=CARTESIAN_POINT('Ctrl Pts',(0.184490798482982,-6.76709527525939,
57.8114983974888));
#62467=CARTESIAN_POINT('Ctrl Pts',(0.372447602153097,-6.75935633790772,
57.8203394332039));
#62468=CARTESIAN_POINT('Ctrl Pts',(0.559756448192511,-6.74380914014527,
57.8291804689191));
#62469=CARTESIAN_POINT('Ctrl Pts',(0.745136131041769,-6.72842206873172,
57.8379304475324));
#62470=CARTESIAN_POINT('Ctrl Pts',(0.929880851943572,-6.70538686355744,
57.8466804261457));
#62471=CARTESIAN_POINT('Ctrl Pts',(1.11336305057327,-6.67478177303335,57.855430404759));
#62472=CARTESIAN_POINT('Ctrl Pts',(1.29684337089997,-6.64417699581286,57.864180293799));
#62473=CARTESIAN_POINT('Ctrl Pts',(1.47906091205072,-6.60600253548086,57.872930182839));
#62474=CARTESIAN_POINT('Ctrl Pts',(1.65939671095112,-6.5603880644124,57.881680071879));
#62475=CARTESIAN_POINT('Ctrl Pts',(1.83973072369064,-6.51477404513877,57.8904298742545));
#62476=CARTESIAN_POINT('Ctrl Pts',(2.01818275356954,-6.46172023288687,57.89917967663));
#62477=CARTESIAN_POINT('Ctrl Pts',(2.19414664033257,-6.40140683918131,57.9079294790055));
#62478=CARTESIAN_POINT('Ctrl Pts',(2.37010884271195,-6.34109402281522,57.916679197625));
#62479=CARTESIAN_POINT('Ctrl Pts',(2.54358267847746,-6.27352185699816,57.9254289162445));
#62480=CARTESIAN_POINT('Ctrl Pts',(2.71397890841686,-6.19891986435286,57.9341786348641));
#62481=CARTESIAN_POINT('Ctrl Pts',(2.88437356388884,-6.1243185610327,57.9429282726359));
#62482=CARTESIAN_POINT('Ctrl Pts',(3.05169040787113,-6.04268767582587,57.9516779104077));
#62483=CARTESIAN_POINT('Ctrl Pts',(3.21536112511993,-5.95430447953978,57.9604275481795));
#62484=CARTESIAN_POINT('Ctrl Pts',(3.37903038442775,-5.86592207055081,57.9691771080116));
#62485=CARTESIAN_POINT('Ctrl Pts',(3.53905332979899,-5.77078760703422,57.9779266678436));
#62486=CARTESIAN_POINT('Ctrl Pts',(3.69488643041812,-5.66922422085351,57.9866762276757));
#62487=CARTESIAN_POINT('Ctrl Pts',(3.85071819468668,-5.5676617056321,57.9954257124757));
#62488=CARTESIAN_POINT('Ctrl Pts',(4.00235994599154,-5.45967053456303,58.0041751972757));
#62489=CARTESIAN_POINT('Ctrl Pts',(4.14929662974236,-5.34561750206735,58.0129246820757));
#62490=CARTESIAN_POINT('Ctrl Pts',(4.29623210224969,-5.23156540974528,58.0216740947511));
#62491=CARTESIAN_POINT('Ctrl Pts',(4.43846235842032,-5.1114517317226,58.0304235074264));
#62492=CARTESIAN_POINT('Ctrl Pts',(4.57550431797334,-4.98568443006648,58.0391729201018));
#62493=CARTESIAN_POINT('Ctrl Pts',(4.71254519337403,-4.85991812336777,58.0479222635597));
#62494=CARTESIAN_POINT('Ctrl Pts',(4.84439764314897,-4.7284984763119,58.0566716070175));
#62495=CARTESIAN_POINT('Ctrl Pts',(4.97061384196603,-4.59187184425433,58.0654209504754));
#62496=CARTESIAN_POINT('Ctrl Pts',(5.09682908420128,-4.45524624767837,58.0741702276228));
#62497=CARTESIAN_POINT('Ctrl Pts',(5.21740796650096,-4.31341395556983,58.0829195047702));
#62498=CARTESIAN_POINT('Ctrl Pts',(5.3319409594218,-4.16685668162946,58.0916687819176));
#62499=CARTESIAN_POINT('Ctrl Pts',(5.44647312235062,-4.02030046975311,58.1004179956611));
#62500=CARTESIAN_POINT('Ctrl Pts',(5.55495930712217,-3.86901957035649,58.1091672094046));
#62501=CARTESIAN_POINT('Ctrl Pts',(5.65703106079724,-3.71352778058482,58.1179164231481));
#62502=CARTESIAN_POINT('Ctrl Pts',(5.75910210868666,-3.55803706597715,58.1266655763943));
#62503=CARTESIAN_POINT('Ctrl Pts',(5.85475865698481,-3.39833575881017,58.1354147296406));
#62504=CARTESIAN_POINT('Ctrl Pts',(5.94367583068996,-3.23496624706844,58.1441638828867));
#62505=CARTESIAN_POINT('Ctrl Pts',(6.03259241910019,-3.07159781070215,58.1529129785419));
#62506=CARTESIAN_POINT('Ctrl Pts',(6.11476958470917,-2.90456146975942,58.161662074197));
#62507=CARTESIAN_POINT('Ctrl Pts',(6.18992823574342,-2.73442451648356,58.1704111698521));
#62508=CARTESIAN_POINT('Ctrl Pts',(6.26508641700891,-2.56428862662522,58.1791602108222));
#62509=CARTESIAN_POINT('Ctrl Pts',(6.33322605570254,-2.3910524253139,58.1879092517923));
#62510=CARTESIAN_POINT('Ctrl Pts',(6.39411573747726,-2.21530425353849,58.1966582927625));
#62511=CARTESIAN_POINT('Ctrl Pts',(6.45500505889081,-2.03955712188701,58.2054072819534));
#62512=CARTESIAN_POINT('Ctrl Pts',(6.50864441544883,-1.86129832025731,58.2141562711444));
#62513=CARTESIAN_POINT('Ctrl Pts',(6.5548516404986,-1.68113324012488,58.2229052603354));
#62514=CARTESIAN_POINT('Ctrl Pts',(6.60199852639072,-1.49730435913067,58.2318321672123));
#62515=CARTESIAN_POINT('Ctrl Pts',(6.64140767440979,-1.31149113173809,58.2407590740892));
#62516=CARTESIAN_POINT('Ctrl Pts',(6.67293975269578,-1.12435050446577,58.2496859809661));
#62517=CARTESIAN_POINT('Ctrl Pts',(6.70384664831486,-0.940920291565231,
58.2584358951501));
#62518=CARTESIAN_POINT('Ctrl Pts',(6.72718585889649,-0.756215114279452,
58.2671858093341));
#62519=CARTESIAN_POINT('Ctrl Pts',(6.74287810451851,-0.570862389376674,
58.2759357235181));
#62520=CARTESIAN_POINT('Ctrl Pts',(6.75857004154115,-0.385513309569632,
58.2846854656286));
#62521=CARTESIAN_POINT('Ctrl Pts',(6.76661529035551,-0.199516993260737,
58.2934352077392));
#62522=CARTESIAN_POINT('Ctrl Pts',(6.76698652348896,-0.0135052182065746,
58.3021849498498));
#62523=CARTESIAN_POINT('Ctrl Pts',(6.76735774981528,0.17250314603639,58.3109345315205));
#62524=CARTESIAN_POINT('Ctrl Pts',(6.76005524147492,0.358526681830987,58.3196841131911));
#62525=CARTESIAN_POINT('Ctrl Pts',(6.74510380214901,0.543933542112403,58.3284336948618));
#62526=CARTESIAN_POINT('Ctrl Pts',(6.73015261711005,0.72933724908232,58.3371831277237));
#62527=CARTESIAN_POINT('Ctrl Pts',(6.70755278444637,0.914124015852325,58.3459325605856));
#62528=CARTESIAN_POINT('Ctrl Pts',(6.67738106408326,1.09766621749158,58.3546819934475));
#62529=CARTESIAN_POINT('Ctrl Pts',(6.64720981677298,1.28120554143095,58.3634312891299));
#62530=CARTESIAN_POINT('Ctrl Pts',(6.60946696581573,1.46350005650393,58.3721805848122));
#62531=CARTESIAN_POINT('Ctrl Pts',(6.56428070011051,1.64393062206308,58.3809298804946));
#62532=CARTESIAN_POINT('Ctrl Pts',(6.51909508282804,1.82435859844424,58.3896790506246));
#62533=CARTESIAN_POINT('Ctrl Pts',(6.46646633415733,2.00292240086333,58.3984282207546));
#62534=CARTESIAN_POINT('Ctrl Pts',(6.40657319597271,2.17901557696222,58.4071773908846));
#62535=CARTESIAN_POINT('Ctrl Pts',(6.34668083768378,2.35510646007211,58.4159264470876));
#62536=CARTESIAN_POINT('Ctrl Pts',(6.27952437143972,2.52872650996316,58.4246755032907));
#62537=CARTESIAN_POINT('Ctrl Pts',(6.20533187335225,2.6992860799772,58.4334245594938));
#62538=CARTESIAN_POINT('Ctrl Pts',(6.12831449784346,2.87633970115199,58.4425067357826));
#62539=CARTESIAN_POINT('Ctrl Pts',(6.0437148946325,3.05009490562157,58.4515889120715));
#62540=CARTESIAN_POINT('Ctrl Pts',(5.95184265120591,3.21991584599446,58.4606710883603));
#62541=CARTESIAN_POINT('Ctrl Pts',(5.86333281335597,3.3835215590512,58.4694208687147));
#62542=CARTESIAN_POINT('Ctrl Pts',(5.76807337235793,3.54347560903648,58.4781706490692));
#62543=CARTESIAN_POINT('Ctrl Pts',(5.66638790086468,3.69923467178475,58.4869204294236));
#62544=CARTESIAN_POINT('Ctrl Pts',(5.56470608502853,3.85498813489606,58.4956698952179));
#62545=CARTESIAN_POINT('Ctrl Pts',(5.45659885767059,4.00654667256116,58.5044193610121));
#62546=CARTESIAN_POINT('Ctrl Pts',(5.3424334058061,4.15339551506079,58.5131688268064));
#62547=CARTESIAN_POINT('Ctrl Pts',(5.22827145140693,4.3002398588375,58.5219180245603));
#62548=CARTESIAN_POINT('Ctrl Pts',(5.10805181978185,4.44237456992933,58.5306672223141));
#62549=CARTESIAN_POINT('Ctrl Pts',(4.98218281282642,4.5793169162635,58.539416420068));
#62550=CARTESIAN_POINT('Ctrl Pts',(4.85631699296316,4.71625579512072,58.548165396286));
#62551=CARTESIAN_POINT('Ctrl Pts',(4.72480227791921,4.84800236135689,58.556914372504));
#62552=CARTESIAN_POINT('Ctrl Pts',(4.58808530848191,4.97410918678837,58.5656633487221));
#62553=CARTESIAN_POINT('Ctrl Pts',(4.45135945057053,5.10022421088936,58.5744128937433));
#62554=CARTESIAN_POINT('Ctrl Pts',(4.30943087208128,5.22069856611913,58.5831624387645));
#62555=CARTESIAN_POINT('Ctrl Pts',(4.16278164322561,5.3351230530161,58.5919119837856));
#62556=CARTESIAN_POINT('Ctrl Pts',(4.01614103534492,5.44954081331352,58.6006610144529));
#62557=CARTESIAN_POINT('Ctrl Pts',(3.86478055833522,5.55790924068262,58.6094100451201));
#62558=CARTESIAN_POINT('Ctrl Pts',(3.70921425812068,5.65986029751214,58.6181590757874));
#62559=CARTESIAN_POINT('Ctrl Pts',(3.55364584530241,5.76181273884579,58.6269082252672));
#62560=CARTESIAN_POINT('Ctrl Pts',(3.39387173464469,5.85734747817991,58.6356573747471));
#62561=CARTESIAN_POINT('Ctrl Pts',(3.23043456092534,5.94614005448738,58.6444065242269));
#62562=CARTESIAN_POINT('Ctrl Pts',(3.18690768806476,5.96978744811237,58.64673661296));
#62563=CARTESIAN_POINT('Ctrl Pts',(3.1431211498292,5.99295688499281,58.6490667016931));
#62564=CARTESIAN_POINT('Ctrl Pts',(3.09908550384712,6.01564277861017,58.6513967904261));
#62565=CARTESIAN_POINT('Origin',(0.,0.,0.));
#62566=CARTESIAN_POINT('',(-7.91099963985057,0.00238710789585057,-59.3576684805928));
#62567=CARTESIAN_POINT('',(3.42067962509752,7.13322310757505,-60.));
#62568=CARTESIAN_POINT('Ctrl Pts',(-7.91099962156735,0.00238334057144554,
-59.3577643889973));
#62569=CARTESIAN_POINT('Ctrl Pts',(-7.9103007141194,2.20325225569619,-59.4463198589853));
#62570=CARTESIAN_POINT('Ctrl Pts',(-6.94155688867303,4.38663744883245,-59.5348753289732));
#62571=CARTESIAN_POINT('Ctrl Pts',(-3.67820201488299,7.34180684107625,-59.7120182346939));
#62572=CARTESIAN_POINT('Ctrl Pts',(-1.40868175871762,8.08992666571332,-59.8006056704266));
#62573=CARTESIAN_POINT('Ctrl Pts',(1.69567364519639,7.78146992497721,-59.9261287374395));
#62574=CARTESIAN_POINT('Ctrl Pts',(2.5929638990806,7.53014751000292,-59.9630643687198));
#62575=CARTESIAN_POINT('Ctrl Pts',(3.42067962509752,7.13322310757505,-60.));
#62576=CARTESIAN_POINT('',(-3.4206796250969,7.13322310757535,-60.));
#62577=CARTESIAN_POINT('Origin',(0.,0.,-60.));
#62578=CARTESIAN_POINT('',(-7.91099727798874,0.000376848761340583,-57.6331939826542));
#62579=CARTESIAN_POINT('Ctrl Pts',(-3.4206796250969,7.13322310757535,-60.));
#62580=CARTESIAN_POINT('Ctrl Pts',(-3.4459264372686,7.12111620236687,-59.9988733970903));
#62581=CARTESIAN_POINT('Ctrl Pts',(-3.47110875087086,7.10887536904488,-59.9977454074563));
#62582=CARTESIAN_POINT('Ctrl Pts',(-3.53231864403775,7.07871915747642,-59.9949935134598));
#62583=CARTESIAN_POINT('Ctrl Pts',(-3.56827552297465,7.06066212837666,-59.9933683534081));
#62584=CARTESIAN_POINT('Ctrl Pts',(-3.73986127625415,6.9728487385684,-59.985573364225));
#62585=CARTESIAN_POINT('Ctrl Pts',(-3.87359132289936,6.89945445647857,-59.9793789923031));
#62586=CARTESIAN_POINT('Ctrl Pts',(-4.14154292460681,6.74214879691367,-59.9667494258034));
#62587=CARTESIAN_POINT('Ctrl Pts',(-4.27553746991937,6.65798225487813,-59.9603167584883));
#62588=CARTESIAN_POINT('Ctrl Pts',(-4.50324071723858,6.50524378023639,-59.9491914171497));
#62589=CARTESIAN_POINT('Ctrl Pts',(-4.59813091208061,6.438522027936,-59.9444936391356));
#62590=CARTESIAN_POINT('Ctrl Pts',(-4.72878633738448,6.34229003878124,-59.9379374915465));
#62591=CARTESIAN_POINT('Ctrl Pts',(-4.76581109958602,6.31451563768646,-59.936069455004));
#62592=CARTESIAN_POINT('Ctrl Pts',(-4.83839149732099,6.25906690631354,-59.9323870354179));
#62593=CARTESIAN_POINT('Ctrl Pts',(-4.87395870121748,6.23141054757177,-59.9305726128382));
#62594=CARTESIAN_POINT('Ctrl Pts',(-4.94434822953616,6.17570568186931,-59.926961558764));
#62595=CARTESIAN_POINT('Ctrl Pts',(-4.97917289452374,6.14766275790506,-59.9251649617938));
#62596=CARTESIAN_POINT('Ctrl Pts',(-5.07527846604082,6.06892041372507,-59.9201781018495));
#62597=CARTESIAN_POINT('Ctrl Pts',(-5.13603547531563,6.01758973112876,-59.9169924759526));
#62598=CARTESIAN_POINT('Ctrl Pts',(-5.3929838235426,5.79377965768501,-59.903369340895));
#62599=CARTESIAN_POINT('Ctrl Pts',(-5.581341431085,5.61255616283981,-59.8930031273601));
#62600=CARTESIAN_POINT('Ctrl Pts',(-5.887524466436,5.28728490298797,-59.8752917929499));
#62601=CARTESIAN_POINT('Ctrl Pts',(-6.00987007291324,5.1477944078182,-59.8679462273013));
#62602=CARTESIAN_POINT('Ctrl Pts',(-6.18641501837817,4.93162790625738,-59.856841896567));
#62603=CARTESIAN_POINT('Ctrl Pts',(-6.24433900024942,4.85807728042496,-59.8531092781247));
#62604=CARTESIAN_POINT('Ctrl Pts',(-6.30270618684108,4.78119485258985,-59.8492451466788));
#62605=CARTESIAN_POINT('Ctrl Pts',(-6.3044673868978,4.77887230040852,-59.8491284493683));
#62606=CARTESIAN_POINT('Ctrl Pts',(-6.30714241262381,4.77534060397661,-59.8489510506931));
#62607=CARTESIAN_POINT('Ctrl Pts',(-6.3080571753171,4.77413216930942,-59.8488903598089));
#62608=CARTESIAN_POINT('Ctrl Pts',(-6.31081668684292,4.7704845768176,-59.8487071957852));
#62609=CARTESIAN_POINT('Ctrl Pts',(-6.31266036833301,4.7680446124863,-59.8485847106565));
#62610=CARTESIAN_POINT('Ctrl Pts',(-6.32865199990914,4.74685543927622,-59.8475213487363));
#62611=CARTESIAN_POINT('Ctrl Pts',(-6.34271777491939,4.72804440770974,-59.8465795411014));
#62612=CARTESIAN_POINT('Ctrl Pts',(-6.36857658136316,4.69313876052984,-59.8448357349542));
#62613=CARTESIAN_POINT('Ctrl Pts',(-6.3803929074599,4.67706162479774,-59.8440340384655));
#62614=CARTESIAN_POINT('Ctrl Pts',(-6.40456487313833,4.64391149006302,-59.842383837772));
#62615=CARTESIAN_POINT('Ctrl Pts',(-6.41691333586168,4.62683351543582,-59.8415352287777));
#62616=CARTESIAN_POINT('Ctrl Pts',(-6.4486980556545,4.58250311890471,-59.8393362602182));
#62617=CARTESIAN_POINT('Ctrl Pts',(-6.46802978504492,4.5551764110769,-59.8379845292245));
#62618=CARTESIAN_POINT('Ctrl Pts',(-6.59223271260789,4.37722232710768,-59.8292084583593));
#62619=CARTESIAN_POINT('Ctrl Pts',(-6.69200795852055,4.2231074175154,-59.8217323044393));
#62620=CARTESIAN_POINT('Ctrl Pts',(-6.86784288495032,3.92960689993277,-59.8077962574485));
#62621=CARTESIAN_POINT('Ctrl Pts',(-6.94524387020208,3.79112968113832,-59.8013390675116));
#62622=CARTESIAN_POINT('Ctrl Pts',(-7.04996389827288,3.58979110454189,-59.7921343906334));
#62623=CARTESIAN_POINT('Ctrl Pts',(-7.08071087612344,3.52875681902811,-59.7893673585976));
#62624=CARTESIAN_POINT('Ctrl Pts',(-7.12891734355118,3.42989694827871,-59.7849231196874));
#62625=CARTESIAN_POINT('Ctrl Pts',(-7.14687554257249,3.39231861136134,-59.7832424107286));
#62626=CARTESIAN_POINT('Ctrl Pts',(-7.16957043761407,3.34384833461796,-59.7810855577106));
#62627=CARTESIAN_POINT('Ctrl Pts',(-7.17458047216048,3.33308520648557,-59.7806073077722));
#62628=CARTESIAN_POINT('Ctrl Pts',(-7.19244536492334,3.29447889065369,-59.778894344821));
#62629=CARTESIAN_POINT('Ctrl Pts',(-7.20516254188411,3.26657224622705,-59.7776607302692));
#62630=CARTESIAN_POINT('Ctrl Pts',(-7.23015905452989,3.21086354920085,-59.7752071867263));
#62631=CARTESIAN_POINT('Ctrl Pts',(-7.24244108764251,3.18306327046938,-59.7739872546977));
#62632=CARTESIAN_POINT('Ctrl Pts',(-7.27045336588329,3.11865616885249,-59.7711710868554));
#62633=CARTESIAN_POINT('Ctrl Pts',(-7.28606788640061,3.08199987253495,-59.769575836333));
#62634=CARTESIAN_POINT('Ctrl Pts',(-7.32534676476923,2.98782266210745,-59.7654960925743));
#62635=CARTESIAN_POINT('Ctrl Pts',(-7.34861093754915,2.93013768054889,-59.7630150036069));
#62636=CARTESIAN_POINT('Ctrl Pts',(-7.48787000943251,2.57274227276288,-59.7477467210624));
#62637=CARTESIAN_POINT('Ctrl Pts',(-7.58619303541677,2.26646819955346,-59.7351263362707));
#62638=CARTESIAN_POINT('Ctrl Pts',(-7.72505206006592,1.72201487909103,-59.7130348060401));
#62639=CARTESIAN_POINT('Ctrl Pts',(-7.7738297566213,1.48638218733415,-59.7035770834101));
#62640=CARTESIAN_POINT('Ctrl Pts',(-7.81636392565079,1.22033307449028,-59.6928082845712));
#62641=CARTESIAN_POINT('Ctrl Pts',(-7.82077402221008,1.19174305676959,-59.6916498278369));
#62642=CARTESIAN_POINT('Ctrl Pts',(-7.82716829164918,1.14872520855486,-59.6899043567589));
#62643=CARTESIAN_POINT('Ctrl Pts',(-7.8292696099069,1.13431496701531,-59.6893192487828));
#62644=CARTESIAN_POINT('Ctrl Pts',(-7.83325541747186,1.10644265180621,-59.688186654681));
#62645=CARTESIAN_POINT('Ctrl Pts',(-7.8351450226978,1.09298135804842,-59.6876392586051));
#62646=CARTESIAN_POINT('Ctrl Pts',(-7.83879606303384,1.0664757557661,-59.6865605662517));
#62647=CARTESIAN_POINT('Ctrl Pts',(-7.84055965627872,1.05343178731285,-59.6860293109369));
#62648=CARTESIAN_POINT('Ctrl Pts',(-7.84457499133327,1.02316465542566,-59.6847955581156));
#62649=CARTESIAN_POINT('Ctrl Pts',(-7.84680257931179,1.00593836103101,-59.6840926026132));
#62650=CARTESIAN_POINT('Ctrl Pts',(-7.85493373560022,0.941388028693867,
-59.6814552734856));
#62651=CARTESIAN_POINT('Ctrl Pts',(-7.86046602801377,0.8940185521262,-59.6795134996335));
#62652=CARTESIAN_POINT('Ctrl Pts',(-7.90202460416147,0.507908237927866,
-59.6636408433056));
#62653=CARTESIAN_POINT('Ctrl Pts',(-7.9165644024708,0.167219606303168,-59.6493630031096));
#62654=CARTESIAN_POINT('Ctrl Pts',(-7.90255536625646,-0.471997523821098,
-59.6225177961226));
#62655=CARTESIAN_POINT('Ctrl Pts',(-7.87909802108942,-0.770052694171588,
-59.6099767063755));
#62656=CARTESIAN_POINT('Ctrl Pts',(-7.81495291347873,-1.24171419120209,
-59.5901979168344));
#62657=CARTESIAN_POINT('Ctrl Pts',(-7.78516824712496,-1.41650983377954,
-59.5828810171525));
#62658=CARTESIAN_POINT('Ctrl Pts',(-7.72620181574655,-1.70387885600593,
-59.5708678846878));
#62659=CARTESIAN_POINT('Ctrl Pts',(-7.70036670579315,-1.81707202261445,
-59.5661398954469));
#62660=CARTESIAN_POINT('Ctrl Pts',(-7.66229985999402,-1.9684205752268,-59.5598181584276));
#62661=CARTESIAN_POINT('Ctrl Pts',(-7.65225635196562,-2.00711022340071,
-59.5582020923904));
#62662=CARTESIAN_POINT('Ctrl Pts',(-7.63562138922832,-2.06925114082611,
-59.5556060668173));
#62663=CARTESIAN_POINT('Ctrl Pts',(-7.62921411121102,-2.09275090087644,
-59.5546242375841));
#62664=CARTESIAN_POINT('Ctrl Pts',(-7.61564438710486,-2.1416295042748,-59.5525817573179));
#62665=CARTESIAN_POINT('Ctrl Pts',(-7.60846336906581,-2.16700289142561,
-59.5515213084641));
#62666=CARTESIAN_POINT('Ctrl Pts',(-7.59174790765712,-2.22495778262732,
-59.5490985741664));
#62667=CARTESIAN_POINT('Ctrl Pts',(-7.58213033106392,-2.25751480215078,
-59.5477371452025));
#62668=CARTESIAN_POINT('Ctrl Pts',(-7.55587237897535,-2.34434117835645,
-59.5441047338352));
#62669=CARTESIAN_POINT('Ctrl Pts',(-7.53885694212114,-2.39849515819621,
-59.5418374981111));
#62670=CARTESIAN_POINT('Ctrl Pts',(-7.43319341199761,-2.72254627372299,
-59.5282547819213));
#62671=CARTESIAN_POINT('Ctrl Pts',(-7.33064037972315,-2.98769795250401,
-59.5170527560092));
#62672=CARTESIAN_POINT('Ctrl Pts',(-6.97638573002518,-3.77482444152793,
-59.4833575876151));
#62673=CARTESIAN_POINT('Ctrl Pts',(-6.68146134200265,-4.27520317095094,
-59.4616208667055));
#62674=CARTESIAN_POINT('Ctrl Pts',(-6.11934654606272,-5.02658863221662,
-59.4266599583711));
#62675=CARTESIAN_POINT('Ctrl Pts',(-5.88479468297627,-5.29926116520742,
-59.4133255803661));
#62676=CARTESIAN_POINT('Ctrl Pts',(-5.54778736634356,-5.64097003549056,
-59.3947698599548));
#62677=CARTESIAN_POINT('Ctrl Pts',(-5.46108495315945,-5.72494866829096,
-59.3900409529335));
#62678=CARTESIAN_POINT('Ctrl Pts',(-5.36004982944706,-5.81842542396096,
-59.3845425792284));
#62679=CARTESIAN_POINT('Ctrl Pts',(-5.34756489296684,-5.82990208312555,
-59.3838633471491));
#62680=CARTESIAN_POINT('Ctrl Pts',(-5.32863549398049,-5.84719078539398,
-59.3828336706946));
#62681=CARTESIAN_POINT('Ctrl Pts',(-5.32221817112008,-5.85303255131997,
-59.3824846242076));
#62682=CARTESIAN_POINT('Ctrl Pts',(-5.31116841896764,-5.86305807480769,
-59.3818836392594));
#62683=CARTESIAN_POINT('Ctrl Pts',(-5.306540618737,-5.86724693741863,-59.3816319454594));
#62684=CARTESIAN_POINT('Ctrl Pts',(-5.29700207877371,-5.87586024924435,
-59.3811131751957));
#62685=CARTESIAN_POINT('Ctrl Pts',(-5.29209074335091,-5.88028402842771,
-59.3808460666681));
#62686=CARTESIAN_POINT('Ctrl Pts',(-5.28025946536739,-5.89091396818371,
-59.3802026027233));
#62687=CARTESIAN_POINT('Ctrl Pts',(-5.27333412678471,-5.8971140898339,-59.3798259511921));
#62688=CARTESIAN_POINT('Ctrl Pts',(-5.24797698068945,-5.91973546705514,
-59.3784467619585));
#62689=CARTESIAN_POINT('Ctrl Pts',(-5.22947938152763,-5.93608252722146,
-59.3774405161016));
#62690=CARTESIAN_POINT('Ctrl Pts',(-4.91736416025596,-6.20931998904849,
-59.3604541820488));
#62691=CARTESIAN_POINT('Ctrl Pts',(-4.60527531323464,-6.44417906201417,
-59.3431486505051));
#62692=CARTESIAN_POINT('Ctrl Pts',(-3.91638842436794,-6.88692919797293,
-59.3060294077928));
#62693=CARTESIAN_POINT('Ctrl Pts',(-3.53728693960655,-7.08911259424554,
-59.2862585949185));
#62694=CARTESIAN_POINT('Ctrl Pts',(-2.87658924348169,-7.37521922655691,
-59.2541881757267));
#62695=CARTESIAN_POINT('Ctrl Pts',(-2.60332435251557,-7.47605157714246,
-59.2415434614148));
#62696=CARTESIAN_POINT('Ctrl Pts',(-2.20581565289815,-7.59828099225087,
-59.2241381129987));
#62697=CARTESIAN_POINT('Ctrl Pts',(-2.08567057548906,-7.63213448379057,
-59.2190005874771));
#62698=CARTESIAN_POINT('Ctrl Pts',(-1.94627435684804,-7.66787465666578,
-59.2131793898532));
#62699=CARTESIAN_POINT('Ctrl Pts',(-1.92776036488935,-7.67255013697899,
-59.2124090495315));
#62700=CARTESIAN_POINT('Ctrl Pts',(-1.89966519369616,-7.67953711405647,
-59.211244277576));
#62701=CARTESIAN_POINT('Ctrl Pts',(-1.89009638579219,-7.68189779856543,
-59.2108483151821));
#62702=CARTESIAN_POINT('Ctrl Pts',(-1.87352604788985,-7.68595296887718,
-59.2101639055587));
#62703=CARTESIAN_POINT('Ctrl Pts',(-1.86652657934321,-7.68765578189194,
-59.2098751992342));
#62704=CARTESIAN_POINT('Ctrl Pts',(-1.85200667935601,-7.69116714725609,
-59.2092771149652));
#62705=CARTESIAN_POINT('Ctrl Pts',(-1.84448589963048,-7.69297423587983,
-59.2089677828621));
#62706=CARTESIAN_POINT('Ctrl Pts',(-1.8262067778567,-7.6973379867607,-59.2082170557314));
#62707=CARTESIAN_POINT('Ctrl Pts',(-1.81544568860651,-7.69988313098826,
-59.2077760199063));
#62708=CARTESIAN_POINT('Ctrl Pts',(-1.775053658752,-7.70934701301787,-59.20612403128));
#62709=CARTESIAN_POINT('Ctrl Pts',(-1.74538804702498,-7.71611738178104,
-59.2049177035166));
#62710=CARTESIAN_POINT('Ctrl Pts',(-1.27515424950573,-7.82058483957626,
-59.1859046151966));
#62711=CARTESIAN_POINT('Ctrl Pts',(-0.827043152580916,-7.88058525983827,
-59.1693598710052));
#62712=CARTESIAN_POINT('Ctrl Pts',(-0.237690842262585,-7.90864448060468,
-59.1486528950393));
#62713=CARTESIAN_POINT('Ctrl Pts',(-0.0990120393069514,-7.91159604499181,
-59.1438502081861));
#62714=CARTESIAN_POINT('Ctrl Pts',(0.476889815531139,-7.90870782026273,
-59.1240447092042));
#62715=CARTESIAN_POINT('Ctrl Pts',(0.91315294975192,-7.87027366434301,-59.1094105838292));
#62716=CARTESIAN_POINT('Ctrl Pts',(1.52876823838439,-7.76414498771538,-59.0871505562018));
#62717=CARTESIAN_POINT('Ctrl Pts',(1.71234985434018,-7.72573175310781,-59.0802962568309));
#62718=CARTESIAN_POINT('Ctrl Pts',(1.9622733308688,-7.66409118506773,-59.0704754096278));
#62719=CARTESIAN_POINT('Ctrl Pts',(2.02993596545076,-7.6464481827517,-59.0677664877448));
#62720=CARTESIAN_POINT('Ctrl Pts',(2.13413635877705,-7.61779746504728,-59.0635056615875));
#62721=CARTESIAN_POINT('Ctrl Pts',(2.17084438644799,-7.60741814130901,-59.0619874244073));
#62722=CARTESIAN_POINT('Ctrl Pts',(2.21587631772579,-7.59433273436178,-59.0601022234073));
#62723=CARTESIAN_POINT('Ctrl Pts',(2.2242732068877,-7.59187764888496,-59.0597497262076));
#62724=CARTESIAN_POINT('Ctrl Pts',(2.23743663351647,-7.58800520821032,-59.0591955829961));
#62725=CARTESIAN_POINT('Ctrl Pts',(2.24220595743785,-7.58659727236446,-59.0589944885884));
#62726=CARTESIAN_POINT('Ctrl Pts',(2.25066077169313,-7.58409268642563,-59.0586374276204));
#62727=CARTESIAN_POINT('Ctrl Pts',(2.2543467994072,-7.58299784342751,-59.0584815678906));
#62728=CARTESIAN_POINT('Ctrl Pts',(2.26219731879996,-7.58065981161029,-59.0581492040888));
#62729=CARTESIAN_POINT('Ctrl Pts',(2.26636158586512,-7.57941587792406,-59.0579726557118));
#62730=CARTESIAN_POINT('Ctrl Pts',(2.27828958108099,-7.57584208445301,-59.0574662410867));
#62731=CARTESIAN_POINT('Ctrl Pts',(2.28605073609237,-7.57350372911317,-59.0571358653761));
#62732=CARTESIAN_POINT('Ctrl Pts',(2.32033766784586,-7.56311592657507,-59.0556724538278));
#62733=CARTESIAN_POINT('Ctrl Pts',(2.34682352638379,-7.5549393563353,-59.0545315695538));
#62734=CARTESIAN_POINT('Ctrl Pts',(2.79279801382885,-7.41468909035607,-59.0351483538088));
#62735=CARTESIAN_POINT('Ctrl Pts',(3.20056175071994,-7.24801127253715,-59.0148990901773));
#62736=CARTESIAN_POINT('Ctrl Pts',(4.01246070454874,-6.83421176941562,-58.972413498533));
#62737=CARTESIAN_POINT('Ctrl Pts',(4.41264946758004,-6.58292342671961,-58.9502529872018));
#62738=CARTESIAN_POINT('Ctrl Pts',(4.98165656842049,-6.1502966555222,-58.9184213497782));
#62739=CARTESIAN_POINT('Ctrl Pts',(5.16834832232988,-5.99426737959803,-58.9079004679273));
#62740=CARTESIAN_POINT('Ctrl Pts',(5.42701160047605,-5.75700334724194,-58.8932587613058));
#62741=CARTESIAN_POINT('Ctrl Pts',(5.50495925989744,-5.68251417274034,-58.888836268167));
#62742=CARTESIAN_POINT('Ctrl Pts',(5.59326921457186,-5.59459942867227,-58.8838115436756));
#62743=CARTESIAN_POINT('Ctrl Pts',(5.60513819703576,-5.58270804100133,-58.8831359008525));
#62744=CARTESIAN_POINT('Ctrl Pts',(5.62309381999027,-5.56460353813917,-58.8821132780589));
#62745=CARTESIAN_POINT('Ctrl Pts',(5.62920820561393,-5.55841808643556,-58.8817649586013));
#62746=CARTESIAN_POINT('Ctrl Pts',(5.63978114828469,-5.54768691809375,-58.8811624909846));
#62747=CARTESIAN_POINT('Ctrl Pts',(5.64424443420745,-5.54314588558856,-58.8809081153956));
#62748=CARTESIAN_POINT('Ctrl Pts',(5.65349533536068,-5.53371108416854,-58.8803807770538));
#62749=CARTESIAN_POINT('Ctrl Pts',(5.65828209142069,-5.52881647771395,-58.880107855544));
#62750=CARTESIAN_POINT('Ctrl Pts',(5.67132284621369,-5.51544722771031,-58.8793641647569));
#62751=CARTESIAN_POINT('Ctrl Pts',(5.67956421538554,-5.50696025704371,-58.8788939994189));
#62752=CARTESIAN_POINT('Ctrl Pts',(5.7107014355378,-5.47475086950203,-58.877116951627));
#62753=CARTESIAN_POINT('Ctrl Pts',(5.73346811158974,-5.45090372496284,-58.8758162121081));
#62754=CARTESIAN_POINT('Ctrl Pts',(6.10917135080501,-5.05241213819627,-58.8543248382643));
#62755=CARTESIAN_POINT('Ctrl Pts',(6.42488629524542,-4.6443251986883,-58.8360038212009));
#62756=CARTESIAN_POINT('Ctrl Pts',(7.07990477990277,-3.60170424344757,-58.7939700944));
#62757=CARTESIAN_POINT('Ctrl Pts',(7.37681372107505,-2.94611794032011,-58.7712334759982));
#62758=CARTESIAN_POINT('Ctrl Pts',(7.59325028642241,-2.21995242192804,-58.7415007279314));
#62759=CARTESIAN_POINT('Ctrl Pts',(7.60477599339017,-2.1801423548741,-58.7398561056385));
#62760=CARTESIAN_POINT('Ctrl Pts',(7.61821263001633,-2.1323285220095,-58.7378612931551));
#62761=CARTESIAN_POINT('Ctrl Pts',(7.62042467266289,-2.12440966134322,-58.7375302794479));
#62762=CARTESIAN_POINT('Ctrl Pts',(7.62403348362295,-2.11141236667999,-58.7369859581946));
#62763=CARTESIAN_POINT('Ctrl Pts',(7.62543753704038,-2.10633594423047,-58.7367731033253));
#62764=CARTESIAN_POINT('Ctrl Pts',(7.62794608626106,-2.09723078268198,-58.7363908681864));
#62765=CARTESIAN_POINT('Ctrl Pts',(7.6290524644497,-2.09320255715398,-58.7362216035491));
#62766=CARTESIAN_POINT('Ctrl Pts',(7.63139189969614,-2.08465838628327,-58.7358622450738));
#62767=CARTESIAN_POINT('Ctrl Pts',(7.63262413951624,-2.08014222084407,-58.735672101534));
#62768=CARTESIAN_POINT('Ctrl Pts',(7.63589908407241,-2.06809744225059,-58.7351644574492));
#62769=CARTESIAN_POINT('Ctrl Pts',(7.63793465841979,-2.06056691365319,-58.7348465268661));
#62770=CARTESIAN_POINT('Ctrl Pts',(7.64739334118732,-2.02536829054338,-58.7333579710847));
#62771=CARTESIAN_POINT('Ctrl Pts',(7.65467718357615,-1.99766333537058,-58.7321790854677));
#62772=CARTESIAN_POINT('Ctrl Pts',(7.71024991795732,-1.78151862068495,-58.7229288553855));
#62773=CARTESIAN_POINT('Ctrl Pts',(7.75172079547663,-1.59140716676455,-58.7144804942424));
#62774=CARTESIAN_POINT('Ctrl Pts',(7.87261211728222,-0.919054488189767,
-58.6839708052031));
#62775=CARTESIAN_POINT('Ctrl Pts',(7.91433893120551,-0.431169202491736,
-58.660768834043));
#62776=CARTESIAN_POINT('Ctrl Pts',(7.90632283241643,0.672926640116866,-58.609447729467));
#62777=CARTESIAN_POINT('Ctrl Pts',(7.83003965222594,1.28587526484475,-58.5819068285109));
#62778=CARTESIAN_POINT('Ctrl Pts',(7.67396649017517,1.92242992753545,-58.5551605778619));
#62779=CARTESIAN_POINT('Ctrl Pts',(7.66421794379883,1.96093393288385,-58.5535491780094));
#62780=CARTESIAN_POINT('Ctrl Pts',(7.65083471628223,2.01216905891255,-58.5514132957557));
#62781=CARTESIAN_POINT('Ctrl Pts',(7.64745754802089,2.02496647650056,-58.5508804925977));
#62782=CARTESIAN_POINT('Ctrl Pts',(7.64189341264258,2.04583871632838,-58.5500126236111));
#62783=CARTESIAN_POINT('Ctrl Pts',(7.63972573204582,2.05391862621002,-58.5496769344199));
#62784=CARTESIAN_POINT('Ctrl Pts',(7.63555689422966,2.06935983041954,-58.5490359312259));
#62785=CARTESIAN_POINT('Ctrl Pts',(7.63355789866526,2.07672169558616,-58.5487305477267));
#62786=CARTESIAN_POINT('Ctrl Pts',(7.6289919149959,2.09344154966,-58.5480374874218));
#62787=CARTESIAN_POINT('Ctrl Pts',(7.62641834904931,2.1027977380295,-58.5476500239188));
#62788=CARTESIAN_POINT('Ctrl Pts',(7.61854584390188,2.13121363880509,-58.5464743408914));
#62789=CARTESIAN_POINT('Ctrl Pts',(7.61319260330413,2.15025829660143,-58.5456878787417));
#62790=CARTESIAN_POINT('Ctrl Pts',(7.56402878554174,2.32267792017561,-58.5385809194193));
#62791=CARTESIAN_POINT('Ctrl Pts',(7.51565901637437,2.47471962895778,-58.5324099532277));
#62792=CARTESIAN_POINT('Ctrl Pts',(7.3739742728133,2.87749039789218,-58.5162519161989));
#62793=CARTESIAN_POINT('Ctrl Pts',(7.27248564354219,3.12512584812754,-58.5065233425138));
#62794=CARTESIAN_POINT('Ctrl Pts',(7.07126113877967,3.5529334834802,-58.4897312974183));
#62795=CARTESIAN_POINT('Ctrl Pts',(6.97667819462898,3.73524215531146,-58.482578256606));
#62796=CARTESIAN_POINT('Ctrl Pts',(6.58220468137923,4.42821083809226,-58.4549079593774));
#62797=CARTESIAN_POINT('Ctrl Pts',(6.23245577683505,4.90825688708141,-58.4347148077986));
#62798=CARTESIAN_POINT('Ctrl Pts',(5.80177952933379,5.37822775221955,-58.4095976786779));
#62799=CARTESIAN_POINT('Ctrl Pts',(5.77083995151678,5.411412533882,-58.4077948022521));
#62800=CARTESIAN_POINT('Ctrl Pts',(5.73012878427687,5.45433178309791,-58.4054262504025));
#62801=CARTESIAN_POINT('Ctrl Pts',(5.72061443048031,5.46430980266998,-58.4048729718365));
#62802=CARTESIAN_POINT('Ctrl Pts',(5.705362606649,5.48022140535944,-58.4039865227265));
#62803=CARTESIAN_POINT('Ctrl Pts',(5.69964182742705,5.48617099292213,-58.4036541322502));
#62804=CARTESIAN_POINT('Ctrl Pts',(5.68931683244669,5.49687536577112,-58.4030544311775));
#62805=CARTESIAN_POINT('Ctrl Pts',(5.68471593614967,5.50163335126914,-58.4027872728435));
#62806=CARTESIAN_POINT('Ctrl Pts',(5.67390329032995,5.51278713030602,-58.4021595999697));
#62807=CARTESIAN_POINT('Ctrl Pts',(5.66768669515483,5.5191782012303,-58.4017988667234));
#62808=CARTESIAN_POINT('Ctrl Pts',(5.64971801805141,5.53758881622766,-58.4007566194385));
#62809=CARTESIAN_POINT('Ctrl Pts',(5.6379384449675,5.54958139568611,-58.400073890485));
#62810=CARTESIAN_POINT('Ctrl Pts',(5.55748597211704,5.63096813958138,-58.3954149885322));
#62811=CARTESIAN_POINT('Ctrl Pts',(5.48757303144064,5.69912221248253,-58.3913863832793));
#62812=CARTESIAN_POINT('Ctrl Pts',(5.24799744073205,5.924174207527,-58.3776868363816));
#62813=CARTESIAN_POINT('Ctrl Pts',(5.07272922687759,6.07492637077634,-58.3678406087008));
#62814=CARTESIAN_POINT('Ctrl Pts',(4.56671258868079,6.47297601319317,-58.3402252236996));
#62815=CARTESIAN_POINT('Ctrl Pts',(4.22282339294515,6.70239183842981,-58.3223895227089));
#62816=CARTESIAN_POINT('Ctrl Pts',(3.32694261274612,7.2036188589356,-58.2787652400962));
#62817=CARTESIAN_POINT('Ctrl Pts',(2.75820443675451,7.43996087664976,-58.2534134599075));
#62818=CARTESIAN_POINT('Ctrl Pts',(2.09783073103737,7.62812762666884,-58.2254922928406));
#62819=CARTESIAN_POINT('Ctrl Pts',(2.0275182751841,7.64711675275886,-58.2225408133375));
#62820=CARTESIAN_POINT('Ctrl Pts',(1.93007900803549,7.67199356902648,-58.2184800547628));
#62821=CARTESIAN_POINT('Ctrl Pts',(1.90316880504124,7.67871335622515,-58.2173616519004));
#62822=CARTESIAN_POINT('Ctrl Pts',(1.856840747658,7.69002350651805,-58.2154414777458));
#62823=CARTESIAN_POINT('Ctrl Pts',(1.83743987325117,7.6946821771822,-58.2146389398095));
#62824=CARTESIAN_POINT('Ctrl Pts',(1.79735988808042,7.7041462304307,-58.2129842182205));
#62825=CARTESIAN_POINT('Ctrl Pts',(1.77667863429032,7.70894186908173,-58.2121321527477));
#62826=CARTESIAN_POINT('Ctrl Pts',(1.72835992617602,7.71994140317062,-58.210145518529));
#62827=CARTESIAN_POINT('Ctrl Pts',(1.70070792937487,7.72608023836373,-58.2090117183649));
#62828=CARTESIAN_POINT('Ctrl Pts',(1.6111773099385,7.74545238850073,-58.2053506612399));
#62829=CARTESIAN_POINT('Ctrl Pts',(1.54917247353694,7.75809188923687,-58.2028304873983));
#62830=CARTESIAN_POINT('Ctrl Pts',(1.23404542944061,7.81840099921673,-58.1900959851136));
#62831=CARTESIAN_POINT('Ctrl Pts',(0.978851326724744,7.85443297248859,-58.1800297517057));
#62832=CARTESIAN_POINT('Ctrl Pts',(0.454569647660311,7.9025057080662,-58.1596538546884));
#62833=CARTESIAN_POINT('Ctrl Pts',(0.185711353493977,7.91339008240242,-58.1493665080907));
#62834=CARTESIAN_POINT('Ctrl Pts',(-0.283888863772529,7.90845223810738,
-58.1313444569159));
#62835=CARTESIAN_POINT('Ctrl Pts',(-0.48444283122238,7.89870387312902,-58.1236286385092));
#62836=CARTESIAN_POINT('Ctrl Pts',(-0.834019387507697,7.86834707379376,
-58.1099588789463));
#62837=CARTESIAN_POINT('Ctrl Pts',(-0.983229693180036,7.85109747139714,
-58.1040527964759));
#62838=CARTESIAN_POINT('Ctrl Pts',(-1.15318616015388,7.8265284259937,-58.0971844010288));
#62839=CARTESIAN_POINT('Ctrl Pts',(-1.17450432832977,7.82335766167694,-58.0963202998011));
#62840=CARTESIAN_POINT('Ctrl Pts',(-1.20926241530967,7.81804263396186,-58.0949070516125));
#62841=CARTESIAN_POINT('Ctrl Pts',(-1.22271006623472,7.81595076159331,-58.094359220368));
#62842=CARTESIAN_POINT('Ctrl Pts',(-1.2469190813266,7.81212087920173,-58.0933711333621));
#62843=CARTESIAN_POINT('Ctrl Pts',(-1.25768239115995,7.81039530553384,-58.0929311682447));
#62844=CARTESIAN_POINT('Ctrl Pts',(-1.28062793535186,7.80666801552453,-58.0919918507307));
#62845=CARTESIAN_POINT('Ctrl Pts',(-1.292809115668,7.80466001838646,-58.091492357611));
#62846=CARTESIAN_POINT('Ctrl Pts',(-1.32563273935285,7.79917028105371,-58.0901442121902));
#62847=CARTESIAN_POINT('Ctrl Pts',(-1.34626610163646,7.79563511269136,-58.0892944001892));
#62848=CARTESIAN_POINT('Ctrl Pts',(-1.44848928509931,7.77770299979589,-58.0850729666095));
#62849=CARTESIAN_POINT('Ctrl Pts',(-1.52986264908757,7.76210700315878,-58.0816770584102));
#62850=CARTESIAN_POINT('Ctrl Pts',(-1.76729348753218,7.71272243196745,-58.0716788481982));
#62851=CARTESIAN_POINT('Ctrl Pts',(-1.92258988276634,7.67548437677564,-58.0650256891158));
#62852=CARTESIAN_POINT('Ctrl Pts',(-2.45118993896757,7.53168308785487,-58.0420904965337));
#62853=CARTESIAN_POINT('Ctrl Pts',(-2.81772816400553,7.40236422159256,-58.0257073361606));
#62854=CARTESIAN_POINT('Ctrl Pts',(-3.2859207033958,7.19734424288913,-58.0044276092246));
#62855=CARTESIAN_POINT('Ctrl Pts',(-3.39738650033991,7.14540443221087,-57.9993312654881));
#62856=CARTESIAN_POINT('Ctrl Pts',(-3.5211537910845,7.0841813731803,-57.9936385347636));
#62857=CARTESIAN_POINT('Ctrl Pts',(-3.53469107360173,7.077436595536,-57.9930154147489));
#62858=CARTESIAN_POINT('Ctrl Pts',(-3.69864343101218,6.99516170256768,-57.9854629939728));
#62859=CARTESIAN_POINT('Ctrl Pts',(-3.84663221451611,6.91488775044269,-57.9785885333203));
#62860=CARTESIAN_POINT('Ctrl Pts',(-4.03382985354334,6.8054750645888,-57.969803852816));
#62861=CARTESIAN_POINT('Ctrl Pts',(-4.07548433971067,6.78061218290063,-57.967843211347));
#62862=CARTESIAN_POINT('Ctrl Pts',(-4.1418261063328,6.74018167763235,-57.9647103551485));
#62863=CARTESIAN_POINT('Ctrl Pts',(-4.16666038280748,6.72485790218505,-57.9635352862622));
#62864=CARTESIAN_POINT('Ctrl Pts',(-4.21147763075942,6.69686023987177,-57.9614102846109));
#62865=CARTESIAN_POINT('Ctrl Pts',(-4.23148958860743,6.68423344686934,-57.9604598142409));
#62866=CARTESIAN_POINT('Ctrl Pts',(-4.27881058540442,6.65407799697948,-57.9582083290824));
#62867=CARTESIAN_POINT('Ctrl Pts',(-4.30606904589383,6.63647070343678,-57.9569082432509));
#62868=CARTESIAN_POINT('Ctrl Pts',(-4.38712040982637,6.58340688865285,-57.9530325428425));
#62869=CARTESIAN_POINT('Ctrl Pts',(-4.44058948185256,6.54746033798625,-57.9504625587053));
#62870=CARTESIAN_POINT('Ctrl Pts',(-4.77512635201042,6.31657249423832,-57.9342894558847));
#62871=CARTESIAN_POINT('Ctrl Pts',(-5.04375296713457,6.10421888488895,-57.9208321884541));
#62872=CARTESIAN_POINT('Ctrl Pts',(-5.65414098254889,5.55381385463925,-57.8890405546432));
#62873=CARTESIAN_POINT('Ctrl Pts',(-5.98051846906027,5.20072847229302,-57.8711111327854));
#62874=CARTESIAN_POINT('Ctrl Pts',(-6.46536864527627,4.56976086197131,-57.8415804864115));
#62875=CARTESIAN_POINT('Ctrl Pts',(-6.6426616683718,4.3079858564548,-57.8299106187649));
#62876=CARTESIAN_POINT('Ctrl Pts',(-6.80718002875471,4.03066549121774,-57.817629579387));
#62877=CARTESIAN_POINT('Ctrl Pts',(-6.81052823181651,4.02500552164033,-57.8173789561614));
#62878=CARTESIAN_POINT('Ctrl Pts',(-6.8189644323913,4.01070388285557,-57.8167457343179));
#62879=CARTESIAN_POINT('Ctrl Pts',(-6.82404305844904,4.00205670899502,-57.8163629203958));
#62880=CARTESIAN_POINT('Ctrl Pts',(-6.83081036103721,3.99048395835019,-57.8158506319247));
#62881=CARTESIAN_POINT('Ctrl Pts',(-6.8325136322778,3.98756691166661,-57.8157215071982));
#62882=CARTESIAN_POINT('Ctrl Pts',(-6.83815734767537,3.97788717154885,-57.8152930374419));
#62883=CARTESIAN_POINT('Ctrl Pts',(-6.84208961998828,3.97111972784656,-57.8149934945661));
#62884=CARTESIAN_POINT('Ctrl Pts',(-6.85392466982884,3.9506818342451,-57.814088884912));
#62885=CARTESIAN_POINT('Ctrl Pts',(-6.86179655224738,3.93699357481537,-57.8134830495285));
#62886=CARTESIAN_POINT('Ctrl Pts',(-6.93637871859901,3.8064009464151,-57.8077026338968));
#62887=CARTESIAN_POINT('Ctrl Pts',(-7.00013441528284,3.68783865392314,-57.8024516756647));
#62888=CARTESIAN_POINT('Ctrl Pts',(-7.06821835051053,3.55309422442241,-57.7964264298944));
#62889=CARTESIAN_POINT('Ctrl Pts',(-7.07555879149618,3.53845404116284,-57.7957710216537));
#62890=CARTESIAN_POINT('Ctrl Pts',(-7.08657790562254,3.51630551763269,-57.7947782024863));
#62891=CARTESIAN_POINT('Ctrl Pts',(-7.09029024763186,3.50881391776053,-57.7944421671794));
#62892=CARTESIAN_POINT('Ctrl Pts',(-7.0967177650101,3.49579117361541,-57.7938576287531));
#62893=CARTESIAN_POINT('Ctrl Pts',(-7.09943837192253,3.49026270769964,-57.7936093520244));
#62894=CARTESIAN_POINT('Ctrl Pts',(-7.10509185007218,3.47874048026342,-57.7930916296629));
#62895=CARTESIAN_POINT('Ctrl Pts',(-7.10802360112179,3.47274617738132,-57.7928221370639));
#62896=CARTESIAN_POINT('Ctrl Pts',(-7.11492244893895,3.4585953525109,-57.7921855653948));
#62897=CARTESIAN_POINT('Ctrl Pts',(-7.11888310437012,3.4504357133911,-57.7918182106894));
#62898=CARTESIAN_POINT('Ctrl Pts',(-7.13184649088081,3.42361154990645,-57.7906095403176));
#62899=CARTESIAN_POINT('Ctrl Pts',(-7.14078987251964,3.40491855989797,-57.7897656315175));
#62900=CARTESIAN_POINT('Ctrl Pts',(-7.29862595491948,3.07166082403764,-57.7746882666538));
#62901=CARTESIAN_POINT('Ctrl Pts',(-7.42664381947607,2.74770945124755,-57.759363722193));
#62902=CARTESIAN_POINT('Ctrl Pts',(-7.78336729504308,1.63567953015698,-57.7064230228309));
#62903=CARTESIAN_POINT('Ctrl Pts',(-7.91096002178626,0.8205463410372,-57.6677770401829));
#62904=CARTESIAN_POINT('Ctrl Pts',(-7.9109999906061,0.00038552601831901,
-57.6331896426682));
#62905=CARTESIAN_POINT('',(-7.91099999999297,1.05515043374329E-5,-53.643655794299));
#62906=CARTESIAN_POINT('Ctrl Pts',(-7.91099999101477,0.000377046938387499,
-57.633189285093));
#62907=CARTESIAN_POINT('Ctrl Pts',(-7.9110051185265,-0.107205699848678,
-57.6286523644339));
#62908=CARTESIAN_POINT('Ctrl Pts',(-7.90881570339247,-0.21478056331028,
-57.6241782588173));
#62909=CARTESIAN_POINT('Ctrl Pts',(-7.90254087123815,-0.368680460629765,
-57.6178655557648));
#62910=CARTESIAN_POINT('Ctrl Pts',(-7.90024052184193,-0.415062998218047,
-57.615974464361));
#62911=CARTESIAN_POINT('Ctrl Pts',(-7.89680408507951,-0.473879665821541,
-57.613590645267));
#62912=CARTESIAN_POINT('Ctrl Pts',(-7.8960468223857,-0.486334531233799,
-57.61308666367));
#62913=CARTESIAN_POINT('Ctrl Pts',(-7.89470559684908,-0.507564659447974,
-57.6122289656369));
#62914=CARTESIAN_POINT('Ctrl Pts',(-7.89413646358415,-0.516340817067683,
-57.6118748081674));
#62915=CARTESIAN_POINT('Ctrl Pts',(-7.89304804236509,-0.532701982674763,
-57.6112153028712));
#62916=CARTESIAN_POINT('Ctrl Pts',(-7.89253245287299,-0.540287221923677,
-57.6109098452336));
#62917=CARTESIAN_POINT('Ctrl Pts',(-7.89146549924196,-0.555656521133576,
-57.610291522918));
#62918=CARTESIAN_POINT('Ctrl Pts',(-7.89091355051302,-0.563440532766269,
-57.6099786760182));
#62919=CARTESIAN_POINT('Ctrl Pts',(-7.88960282026343,-0.581545733959428,
-57.6092517320608));
#62920=CARTESIAN_POINT('Ctrl Pts',(-7.88883530071511,-0.591866286744273,
-57.6088378959365));
#62921=CARTESIAN_POINT('Ctrl Pts',(-7.88650678653762,-0.622367578713689,
-57.607616448767));
#62922=CARTESIAN_POINT('Ctrl Pts',(-7.88488858514545,-0.642543931884694,
-57.6068105443644));
#62923=CARTESIAN_POINT('Ctrl Pts',(-7.8735285938336,-0.777674638369109,
-57.6014266972127));
#62924=CARTESIAN_POINT('Ctrl Pts',(-7.8613504682385,-0.892412736649149,
-57.5969219556929));
#62925=CARTESIAN_POINT('Ctrl Pts',(-7.84088096810435,-1.0519379081305,-57.5907410310072));
#62926=CARTESIAN_POINT('Ctrl Pts',(-7.83470642121581,-1.09697907336804,
-57.5890050203785));
#62927=CARTESIAN_POINT('Ctrl Pts',(-7.6987165210187,-2.02918677873542,-57.55325203661));
#62928=CARTESIAN_POINT('Ctrl Pts',(-7.41943779744514,-2.88782805293668,
-57.5244540280875));
#62929=CARTESIAN_POINT('Ctrl Pts',(-6.96843914075548,-3.74567221643675,
-57.4893354875045));
#62930=CARTESIAN_POINT('Ctrl Pts',(-6.93373007052172,-3.80953952529224,
-57.4866744632899));
#62931=CARTESIAN_POINT('Ctrl Pts',(-6.81786359509259,-4.0159120376024,-57.4778992763193));
#62932=CARTESIAN_POINT('Ctrl Pts',(-6.73315740171557,-4.15636863900462,
-57.4716485604281));
#62933=CARTESIAN_POINT('Ctrl Pts',(-6.62867604807068,-4.31803053785839,
-57.4640187870748));
#62934=CARTESIAN_POINT('Ctrl Pts',(-6.61307112574171,-4.34189176850066,
-57.4628812498572));
#62935=CARTESIAN_POINT('Ctrl Pts',(-6.59218815915625,-4.3734498226116,-57.4613621799622));
#62936=CARTESIAN_POINT('Ctrl Pts',(-6.587024850867,-4.38122262497346,-57.4609868476811));
#62937=CARTESIAN_POINT('Ctrl Pts',(-6.5785193788084,-4.3939776712509,-57.4603690119709));
#62938=CARTESIAN_POINT('Ctrl Pts',(-6.57518526876945,-4.3989652958256,-57.4601269347862));
#62939=CARTESIAN_POINT('Ctrl Pts',(-6.56871000325737,-4.40862808787751,
-57.4596570141754));
#62940=CARTESIAN_POINT('Ctrl Pts',(-6.56556952118199,-4.41330370430207,
-57.4594292059375));
#62941=CARTESIAN_POINT('Ctrl Pts',(-6.55830187838315,-4.42409899934586,
-57.4589022584821));
#62942=CARTESIAN_POINT('Ctrl Pts',(-6.55417114469429,-4.43021625765049,
-57.4586029352165));
#62943=CARTESIAN_POINT('Ctrl Pts',(-6.54305431014482,-4.44662974765537,
-57.4577978821625));
#62944=CARTESIAN_POINT('Ctrl Pts',(-6.53605248691869,-4.45691526776444,
-57.4572913563012));
#62945=CARTESIAN_POINT('Ctrl Pts',(-6.48602297727284,-4.53003604776227,
-57.4536761143513));
#62946=CARTESIAN_POINT('Ctrl Pts',(-6.44211506546661,-4.59226236580237,
-57.4505242040204));
#62947=CARTESIAN_POINT('Ctrl Pts',(-6.04366486905114,-5.13998426307063,
-57.4221713700948));
#62948=CARTESIAN_POINT('Ctrl Pts',(-5.6357549958174,-5.58422909254062,-57.3950677438011));
#62949=CARTESIAN_POINT('Ctrl Pts',(-4.84391306934859,-6.27056353976016,
-57.3495045593447));
#62950=CARTESIAN_POINT('Ctrl Pts',(-4.48217217610062,-6.53403748987729,
-57.3306474779736));
#62951=CARTESIAN_POINT('Ctrl Pts',(-4.06413967728926,-6.78737487744593,
-57.3108251889001));
#62952=CARTESIAN_POINT('Ctrl Pts',(-4.02800625261219,-6.80888057713724,
-57.3091262498831));
#62953=CARTESIAN_POINT('Ctrl Pts',(-3.97548323797543,-6.8395765188118,-57.3066768613934));
#62954=CARTESIAN_POINT('Ctrl Pts',(-3.95922984789392,-6.84899795205211,
-57.3059216595689));
#62955=CARTESIAN_POINT('Ctrl Pts',(-3.93079907922474,-6.86534309540146,
-57.3046053919431));
#62956=CARTESIAN_POINT('Ctrl Pts',(-3.91863660382568,-6.87229251323125,
-57.3040438110042));
#62957=CARTESIAN_POINT('Ctrl Pts',(-3.89507753793784,-6.88567085941025,
-57.302958889796));
#62958=CARTESIAN_POINT('Ctrl Pts',(-3.88368333184739,-6.89210388704103,
-57.3024354699977));
#62959=CARTESIAN_POINT('Ctrl Pts',(-3.85416114729629,-6.90867528967045,
-57.3010826059953));
#62960=CARTESIAN_POINT('Ctrl Pts',(-3.83600908108455,-6.91877060913069,
-57.3002539980776));
#62961=CARTESIAN_POINT('Ctrl Pts',(-3.7988915083269,-6.93922266885189,-57.2985660615507));
#62962=CARTESIAN_POINT('Ctrl Pts',(-3.7799228919311,-6.9495734311769,-57.2977068442333));
#62963=CARTESIAN_POINT('Ctrl Pts',(-3.63391565816748,-7.02847177748308,
-57.2911186819552));
#62964=CARTESIAN_POINT('Ctrl Pts',(-3.50506274915314,-7.09360945638501,
-57.2854534601743));
#62965=CARTESIAN_POINT('Ctrl Pts',(-2.70529488909303,-7.47079245640969,
-57.2511407294273));
#62966=CARTESIAN_POINT('Ctrl Pts',(-1.9951579041801,-7.69094742817544,-57.2246725819699));
#62967=CARTESIAN_POINT('Ctrl Pts',(-1.06022670992192,-7.84237150886734,
-57.1893599941162));
#62968=CARTESIAN_POINT('Ctrl Pts',(-0.854430566780976,-7.86745285493904,
-57.1815296474756));
#62969=CARTESIAN_POINT('Ctrl Pts',(-0.555640021265778,-7.89200567687153,
-57.169859152757));
#62970=CARTESIAN_POINT('Ctrl Pts',(-0.463261210358789,-7.89796668205734,
-57.1662091802437));
#62971=CARTESIAN_POINT('Ctrl Pts',(-0.355894420758969,-7.903004673239,-57.1619016951472));
#62972=CARTESIAN_POINT('Ctrl Pts',(-0.340985666546359,-7.90366196616611,
-57.1613021037016));
#62973=CARTESIAN_POINT('Ctrl Pts',(-0.318291381785576,-7.90459817367684,
-57.1603870787388));
#62974=CARTESIAN_POINT('Ctrl Pts',(-0.31050710601753,-7.90490778109251,
-57.160072804393));
#62975=CARTESIAN_POINT('Ctrl Pts',(-0.296387815559982,-7.90544846600326,
-57.1595019973823));
#62976=CARTESIAN_POINT('Ctrl Pts',(-0.290052950382796,-7.90568342849107,
-57.159245614056));
#62977=CARTESIAN_POINT('Ctrl Pts',(-0.276441700923589,-7.90617189264842,
-57.1586941287821));
#62978=CARTESIAN_POINT('Ctrl Pts',(-0.269165239214332,-7.90642296387229,
-57.1583989325512));
#62979=CARTESIAN_POINT('Ctrl Pts',(-0.24964252644527,-7.90706960487489,
-57.1576058921898));
#62980=CARTESIAN_POINT('Ctrl Pts',(-0.237395715992339,-7.90744676865447,
-57.1571073218363));
#62981=CARTESIAN_POINT('Ctrl Pts',(-0.18179934548302,-7.90902969004254,
-57.1548388873426));
#62982=CARTESIAN_POINT('Ctrl Pts',(-0.138441766483694,-7.90990742104768,
-57.1530557623367));
#62983=CARTESIAN_POINT('Ctrl Pts',(0.626113125322077,-7.91909702702051,
-57.1213375345691));
#62984=CARTESIAN_POINT('Ctrl Pts',(1.34500692906579,-7.82910258346065,-57.0869272436465));
#62985=CARTESIAN_POINT('Ctrl Pts',(2.38437934778349,-7.55145601499462,-57.0381478117924));
#62986=CARTESIAN_POINT('Ctrl Pts',(2.72056703746041,-7.43695546067846,-57.0224810060503));
#62987=CARTESIAN_POINT('Ctrl Pts',(3.13298828165304,-7.26476396960482,-57.0036693857707));
#62988=CARTESIAN_POINT('Ctrl Pts',(3.21739169817972,-7.2277799175295,-56.999840236044));
#62989=CARTESIAN_POINT('Ctrl Pts',(3.33368829595093,-7.17437988593016,-56.994593241278));
#62990=CARTESIAN_POINT('Ctrl Pts',(3.3661432041858,-7.15920975922467,-56.993132133364));
#62991=CARTESIAN_POINT('Ctrl Pts',(3.4145312035279,-7.13619037364201,-56.9909583948226));
#62992=CARTESIAN_POINT('Ctrl Pts',(3.43054250214233,-7.12850717438436,-56.9902398871585));
#62993=CARTESIAN_POINT('Ctrl Pts',(3.45618227578814,-7.11609725338303,-56.9890905208007));
#62994=CARTESIAN_POINT('Ctrl Pts',(3.46582719975796,-7.11140477442471,-56.9886584409365));
#62995=CARTESIAN_POINT('Ctrl Pts',(3.4842097161493,-7.1024149741573,-56.9878354538307));
#62996=CARTESIAN_POINT('Ctrl Pts',(3.49294897160148,-7.09812111012051,-56.9874444236528));
#62997=CARTESIAN_POINT('Ctrl Pts',(3.50833917597229,-7.09052412528659,-56.9867561996525));
#62998=CARTESIAN_POINT('Ctrl Pts',(3.51499343397836,-7.08722775875119,-56.986458763546));
#62999=CARTESIAN_POINT('Ctrl Pts',(3.52803679441936,-7.08074348922605,-56.9858759987093));
#63000=CARTESIAN_POINT('Ctrl Pts',(3.53442624006699,-7.07755629697504,-56.9855906448145));
#63001=CARTESIAN_POINT('Ctrl Pts',(3.54967514299524,-7.06992401851332,-56.9849099112374));
#63002=CARTESIAN_POINT('Ctrl Pts',(3.55853058918476,-7.06547091814642,-56.9845148214944));
#63003=CARTESIAN_POINT('Ctrl Pts',(3.59020534688004,-7.04946811340048,-56.9831024537603));
#63004=CARTESIAN_POINT('Ctrl Pts',(3.61297710533012,-7.03782434898807,-56.9820885873691));
#63005=CARTESIAN_POINT('Ctrl Pts',(3.94273274650287,-6.8671898485744,-56.9674282094977));
#63006=CARTESIAN_POINT('Ctrl Pts',(4.23904225013443,-6.6883474456591,-56.954548142343));
#63007=CARTESIAN_POINT('Ctrl Pts',(4.80753832998855,-6.29221747680268,-56.9298604559548));
#63008=CARTESIAN_POINT('Ctrl Pts',(5.07898731727145,-6.07522230664863,-56.9180826586979));
#63009=CARTESIAN_POINT('Ctrl Pts',(5.35684074036114,-5.82142839882124,-56.9054139467907));
#63010=CARTESIAN_POINT('Ctrl Pts',(5.37826234937195,-5.80164333814783,-56.9044328531998));
#63011=CARTESIAN_POINT('Ctrl Pts',(5.4716561918071,-5.71442271826948,-56.9001343579225));
#63012=CARTESIAN_POINT('Ctrl Pts',(5.54247296549684,-5.64576317597658,-56.8968196518867));
#63013=CARTESIAN_POINT('Ctrl Pts',(5.66468067362727,-5.52276228092883,-56.8909701314387));
#63014=CARTESIAN_POINT('Ctrl Pts',(5.71661935587087,-5.4689828465595,-56.8884409583832));
#63015=CARTESIAN_POINT('Ctrl Pts',(5.85656531244334,-5.31990496306322,-56.8814846766845));
#63016=CARTESIAN_POINT('Ctrl Pts',(5.94300217255408,-5.22316667573517,-56.8770301713073));
#63017=CARTESIAN_POINT('Ctrl Pts',(6.23354336144865,-4.88144569109814,-56.8613419624065));
#63018=CARTESIAN_POINT('Ctrl Pts',(6.42517482006858,-4.62630140289441,-56.8497118356704));
#63019=CARTESIAN_POINT('Ctrl Pts',(6.60791425739633,-4.34966129566134,-56.8364408334894));
#63020=CARTESIAN_POINT('Ctrl Pts',(6.61493002516844,-4.33898432567641,-56.8359276529697));
#63021=CARTESIAN_POINT('Ctrl Pts',(6.62497859401741,-4.32361086169865,-56.8351872593192));
#63022=CARTESIAN_POINT('Ctrl Pts',(6.62803236015783,-4.3189280252128,-56.8349615348053));
#63023=CARTESIAN_POINT('Ctrl Pts',(6.63332253121521,-4.31079692040851,-56.8345692470497));
#63024=CARTESIAN_POINT('Ctrl Pts',(6.63556122114052,-4.3073501334928,-56.8344028473825));
#63025=CARTESIAN_POINT('Ctrl Pts',(6.63985916050586,-4.30072153169045,-56.834082628925));
#63026=CARTESIAN_POINT('Ctrl Pts',(6.64191881198113,-4.29753997764384,-56.8339288391609));
#63027=CARTESIAN_POINT('Ctrl Pts',(6.64677762827943,-4.29002270320983,-56.8335652463695));
#63028=CARTESIAN_POINT('Ctrl Pts',(6.64957482247711,-4.28568574601521,-56.8333553020261));
#63029=CARTESIAN_POINT('Ctrl Pts',(6.65794561255129,-4.2726791884625,-56.8327251571326));
#63030=CARTESIAN_POINT('Ctrl Pts',(6.6635064936162,-4.26400145810449,-56.8323040447077));
#63031=CARTESIAN_POINT('Ctrl Pts',(6.71662708099417,-4.18074932619382,-56.8282575888176));
#63032=CARTESIAN_POINT('Ctrl Pts',(6.7629482041704,-4.10539580112422,-56.8245459425109));
#63033=CARTESIAN_POINT('Ctrl Pts',(6.84894424862533,-3.96009442192178,-56.8173231129596));
#63034=CARTESIAN_POINT('Ctrl Pts',(6.88883580524605,-3.89028606386178,-56.8138247903952));
#63035=CARTESIAN_POINT('Ctrl Pts',(7.29229268290991,-3.15858577901082,-56.7769725311015));
#63036=CARTESIAN_POINT('Ctrl Pts',(7.56038534060125,-2.44846857765005,-56.7401392692563));
#63037=CARTESIAN_POINT('Ctrl Pts',(7.80042314666375,-1.36491530495265,-56.6905957112567));
#63038=CARTESIAN_POINT('Ctrl Pts',(7.85375165175807,-1.01401483210752,-56.6754255962818));
#63039=CARTESIAN_POINT('Ctrl Pts',(7.88548171605885,-0.635407321156414,
-56.6600425611962));
#63040=CARTESIAN_POINT('Ctrl Pts',(7.88747846062381,-0.610121224054738,
-56.6590196934819));
#63041=CARTESIAN_POINT('Ctrl Pts',(7.89012290573929,-0.574447417004055,
-56.6575829280983));
#63042=CARTESIAN_POINT('Ctrl Pts',(7.89087176130505,-0.564067505147878,
-56.6571656283729));
#63043=CARTESIAN_POINT('Ctrl Pts',(7.89210918600974,-0.546430687739474,
-56.6564578529139));
#63044=CARTESIAN_POINT('Ctrl Pts',(7.89260823240736,-0.539174545513565,
-56.6561670251689));
#63045=CARTESIAN_POINT('Ctrl Pts',(7.89359031385127,-0.524601493718695,
-56.6555836649419));
#63046=CARTESIAN_POINT('Ctrl Pts',(7.8940731839628,-0.517284580069527,-56.6552911382767));
#63047=CARTESIAN_POINT('Ctrl Pts',(7.89521799866798,-0.499562271846002,
-56.6545835010817));
#63048=CARTESIAN_POINT('Ctrl Pts',(7.89586954788158,-0.489156206056432,
-56.6541687400881));
#63049=CARTESIAN_POINT('Ctrl Pts',(7.89801118497569,-0.453831968181256,
-56.6527633120335));
#63050=CARTESIAN_POINT('Ctrl Pts',(7.89940391076771,-0.428907919491899,
-56.6517759133521));
#63051=CARTESIAN_POINT('Ctrl Pts',(7.91930405803316,-0.0397163090076934,
-56.6364227282477));
#63052=CARTESIAN_POINT('Ctrl Pts',(7.91271751605975,0.325410780283869,-56.6229414459906));
#63053=CARTESIAN_POINT('Ctrl Pts',(7.85146309809681,1.02624491709948,-56.5980335107253));
#63054=CARTESIAN_POINT('Ctrl Pts',(7.80032930329605,1.36144088503841,-56.5865491425165));
#63055=CARTESIAN_POINT('Ctrl Pts',(7.69618567560514,1.83700340995465,-56.5699926984763));
#63056=CARTESIAN_POINT('Ctrl Pts',(7.66044716840923,1.98075840516805,-56.5649492416154));
#63057=CARTESIAN_POINT('Ctrl Pts',(7.60708458895948,2.17226983230576,-56.5580904832827));
#63058=CARTESIAN_POINT('Ctrl Pts',(7.59300496777793,2.22098349031854,-56.5563334928583));
#63059=CARTESIAN_POINT('Ctrl Pts',(7.56179233023832,2.32520803729195,-56.5525417239012));
#63060=CARTESIAN_POINT('Ctrl Pts',(7.54451425593942,2.38067221164975,-56.5505038807333));
#63061=CARTESIAN_POINT('Ctrl Pts',(7.50500781911477,2.50274014158415,-56.5459649438605));
#63062=CARTESIAN_POINT('Ctrl Pts',(7.48250056748997,2.5692480515603,-56.5434561195527));
#63063=CARTESIAN_POINT('Ctrl Pts',(7.39331424795949,2.82167233063979,-56.5337667190644));
#63064=CARTESIAN_POINT('Ctrl Pts',(7.32057019925716,3.00535724369664,-56.5263675322659));
#63065=CARTESIAN_POINT('Ctrl Pts',(7.22960523936015,3.21209192340681,-56.5174247353167));
#63066=CARTESIAN_POINT('Ctrl Pts',(7.21803562468271,3.23800681462385,-56.5162924232389));
#63067=CARTESIAN_POINT('Ctrl Pts',(7.20314389236692,3.27088651415949,-56.514840675133));
#63068=CARTESIAN_POINT('Ctrl Pts',(7.19995059173247,3.27790969955461,-56.5145296989864));
#63069=CARTESIAN_POINT('Ctrl Pts',(7.19479183269735,3.28921170732236,-56.5140278597299));
#63070=CARTESIAN_POINT('Ctrl Pts',(7.19283281192515,3.29349348123548,-56.513837412748));
#63071=CARTESIAN_POINT('Ctrl Pts',(7.18909710861266,3.30163926711951,-56.5134744853762));
#63072=CARTESIAN_POINT('Ctrl Pts',(7.18732112983918,3.30550360212758,-56.5133020501257));
#63073=CARTESIAN_POINT('Ctrl Pts',(7.18326960438862,3.31430057474595,-56.5129089121036));
#63074=CARTESIAN_POINT('Ctrl Pts',(7.18099209357794,3.31923229991244,-56.5126880843669));
#63075=CARTESIAN_POINT('Ctrl Pts',(7.17405082234038,3.33422235602046,-56.5120155810414));
#63076=CARTESIAN_POINT('Ctrl Pts',(7.16937101244632,3.34427319524262,-56.5115628939466));
#63077=CARTESIAN_POINT('Ctrl Pts',(7.13615175745839,3.41522808951705,-56.5083547350272));
#63078=CARTESIAN_POINT('Ctrl Pts',(7.10685850729854,3.4757742252649,-56.505552719706));
#63079=CARTESIAN_POINT('Ctrl Pts',(7.03544522710466,3.61870019447284,-56.4987970935544));
#63080=CARTESIAN_POINT('Ctrl Pts',(6.9926454563373,3.70072817718354,-56.4948067819572));
#63081=CARTESIAN_POINT('Ctrl Pts',(6.5567874690899,4.50150463892688,-56.4548638828426));
#63082=CARTESIAN_POINT('Ctrl Pts',(6.05577003958546,5.15586211913936,-56.4148574635399));
#63083=CARTESIAN_POINT('Ctrl Pts',(5.20512774356921,5.96806930877752,-56.3625204805348));
#63084=CARTESIAN_POINT('Ctrl Pts',(4.9307030587227,6.19672632500656,-56.3472819637384));
#63085=CARTESIAN_POINT('Ctrl Pts',(4.62149012044424,6.42077690857281,-56.331790401979));
#63086=CARTESIAN_POINT('Ctrl Pts',(4.60115931459744,6.43536168522438,-56.3307790203603));
#63087=CARTESIAN_POINT('Ctrl Pts',(4.57188407152779,6.45615330858379,-56.3293328946496));
#63088=CARTESIAN_POINT('Ctrl Pts',(4.56299558458341,6.46243845647448,-56.328895166889));
#63089=CARTESIAN_POINT('Ctrl Pts',(4.54756781872209,6.47329990326894,-56.3281377157034));
#63090=CARTESIAN_POINT('Ctrl Pts',(4.54103454635026,6.47788468196677,-56.3278176706827));
#63091=CARTESIAN_POINT('Ctrl Pts',(4.52847384345462,6.48667092050229,-56.3272037311762));
#63092=CARTESIAN_POINT('Ctrl Pts',(4.52244747898099,6.49087388430473,-56.3269097799735));
#63093=CARTESIAN_POINT('Ctrl Pts',(4.50825990519403,6.50073936535008,-56.3262191609981));
#63094=CARTESIAN_POINT('Ctrl Pts',(4.50009385970311,6.50639492528747,-56.3258227556818));
#63095=CARTESIAN_POINT('Ctrl Pts',(4.47193977447099,6.52581524730864,-56.3244598342721));
#63096=CARTESIAN_POINT('Ctrl Pts',(4.45189896872856,6.53950346539863,-56.3234961918986));
#63097=CARTESIAN_POINT('Ctrl Pts',(4.22529034305106,6.69275660719473,-56.3126724593198));
#63098=CARTESIAN_POINT('Ctrl Pts',(4.01229163140428,6.8225799858531,-56.3031817128721));
#63099=CARTESIAN_POINT('Ctrl Pts',(3.2785275325376,7.2235428165947,-56.2723276062744));
#63100=CARTESIAN_POINT('Ctrl Pts',(2.73385687563266,7.44676709726335,-56.2525093989169));
#63101=CARTESIAN_POINT('Ctrl Pts',(1.97458675983539,7.66328985610069,-56.2248462048486));
#63102=CARTESIAN_POINT('Ctrl Pts',(1.77760884480998,7.7113621407906,-56.217650084488));
#63103=CARTESIAN_POINT('Ctrl Pts',(1.50081568757249,7.76774363707935,-56.2072838855619));
#63104=CARTESIAN_POINT('Ctrl Pts',(1.42238700787742,7.78248698319818,-56.2043184519667));
#63105=CARTESIAN_POINT('Ctrl Pts',(1.21810433766294,7.81769779065375,-56.196494326728));
#63106=CARTESIAN_POINT('Ctrl Pts',(1.09196857937718,7.83631153413647,-56.1915551115205));
#63107=CARTESIAN_POINT('Ctrl Pts',(0.936864840197922,7.85538247680505,-56.185348728966));
#63108=CARTESIAN_POINT('Ctrl Pts',(0.90827608838852,7.85873934591705,-56.1841996811346));
#63109=CARTESIAN_POINT('Ctrl Pts',(0.868683368133643,7.86316936231992,-56.1826018014735));
#63110=CARTESIAN_POINT('Ctrl Pts',(0.857694321414441,7.86437560548892,-56.1821576079923));
#63111=CARTESIAN_POINT('Ctrl Pts',(0.839123165517238,7.86637473235932,-56.1814057870647));
#63112=CARTESIAN_POINT('Ctrl Pts',(0.831542355979256,7.86717969964912,-56.181098568313));
#63113=CARTESIAN_POINT('Ctrl Pts',(0.816524872956141,7.86875238048455,-56.1804893449923));
#63114=CARTESIAN_POINT('Ctrl Pts',(0.809088250119467,7.86952051249878,-56.1801873545846));
#63115=CARTESIAN_POINT('Ctrl Pts',(0.792671221820548,7.87119271770173,-56.179520024034));
#63116=CARTESIAN_POINT('Ctrl Pts',(0.783690341102463,7.8720919655227,-56.179154528005));
#63117=CARTESIAN_POINT('Ctrl Pts',(0.752205463862471,7.87519010599056,-56.1778716949695));
#63118=CARTESIAN_POINT('Ctrl Pts',(0.729693694627155,7.87730787557035,-56.1769518006395));
#63119=CARTESIAN_POINT('Ctrl Pts',(0.425234455430575,7.90463322720225,-56.1644768483184));
#63120=CARTESIAN_POINT('Ctrl Pts',(0.142149800189738,7.91478569305607,-56.1524939345744));
#63121=CARTESIAN_POINT('Ctrl Pts',(-0.805552406661437,7.89790900730645,
-56.1119425953446));
#63122=CARTESIAN_POINT('Ctrl Pts',(-1.46616141161784,7.80232894986433,-56.0832399781104));
#63123=CARTESIAN_POINT('Ctrl Pts',(-2.52509117634157,7.50972519142205,-56.0374179087135));
#63124=CARTESIAN_POINT('Ctrl Pts',(-2.93297883909377,7.36000750917241,-56.0195951352827));
#63125=CARTESIAN_POINT('Ctrl Pts',(-3.37482375808801,7.15523014124652,-55.9998551342719));
#63126=CARTESIAN_POINT('Ctrl Pts',(-3.4228865459982,7.1323629683599,-55.9977030306103));
#63127=CARTESIAN_POINT('Ctrl Pts',(-3.49491425616442,7.0971980752756,-55.9944704460744));
#63128=CARTESIAN_POINT('Ctrl Pts',(-3.51905297469963,7.08526021718412,-55.9933858396881));
#63129=CARTESIAN_POINT('Ctrl Pts',(-3.56249510414999,7.06349904247396,-55.9914315588432));
#63130=CARTESIAN_POINT('Ctrl Pts',(-3.58182000477595,7.05371927048796,-55.9905613745348));
#63131=CARTESIAN_POINT('Ctrl Pts',(-3.62310889075006,7.03261073208286,-55.9887003417512));
#63132=CARTESIAN_POINT('Ctrl Pts',(-3.64506045766456,7.02125814994953,-55.9877097947332));
#63133=CARTESIAN_POINT('Ctrl Pts',(-3.70374260459236,6.99056042531679,-55.9850587419356));
#63134=CARTESIAN_POINT('Ctrl Pts',(-3.74037478836277,6.97102867643353,-55.9834005936722));
#63135=CARTESIAN_POINT('Ctrl Pts',(-3.91354769005435,6.87693737207559,-55.9755457166084));
#63136=CARTESIAN_POINT('Ctrl Pts',(-4.04802464174732,6.79864845775353,-55.9693985470876));
#63137=CARTESIAN_POINT('Ctrl Pts',(-4.60927648801326,6.44934265914479,-55.9434725910887));
#63138=CARTESIAN_POINT('Ctrl Pts',(-5.01185322770294,6.14172432425867,-55.9242689433172));
#63139=CARTESIAN_POINT('Ctrl Pts',(-5.50689407882182,5.68215893836712,-55.8981743734901));
#63140=CARTESIAN_POINT('Ctrl Pts',(-5.6277040006146,5.56253165607085,-55.8915697760371));
#63141=CARTESIAN_POINT('Ctrl Pts',(-5.80217058828601,5.37826715126918,-55.88156464109));
#63142=CARTESIAN_POINT('Ctrl Pts',(-5.85880565161739,5.31651549999864,-55.8782380314659));
#63143=CARTESIAN_POINT('Ctrl Pts',(-5.92742763606071,5.23926565129193,-55.8740973684555));
#63144=CARTESIAN_POINT('Ctrl Pts',(-5.9403525706433,5.22460661469507,-55.8733125167763));
#63145=CARTESIAN_POINT('Ctrl Pts',(-5.96112482600534,5.20087067428051,-55.872043027975));
#63146=CARTESIAN_POINT('Ctrl Pts',(-5.96900597782746,5.19182362925176,-55.871559480729));
#63147=CARTESIAN_POINT('Ctrl Pts',(-5.9841083484137,5.17440725741117,-55.8706292606443));
#63148=CARTESIAN_POINT('Ctrl Pts',(-5.99133267064603,5.16604065216632,-55.8701826819754));
#63149=CARTESIAN_POINT('Ctrl Pts',(-6.00780430702971,5.14688355761278,-55.8691608313342));
#63150=CARTESIAN_POINT('Ctrl Pts',(-6.01704012174154,5.13608324685826,-55.8685852306889));
#63151=CARTESIAN_POINT('Ctrl Pts',(-6.04143956876111,5.10739452820873,-55.8670576484932));
#63152=CARTESIAN_POINT('Ctrl Pts',(-6.05655281452251,5.08946352051693,-55.8661042927006));
#63153=CARTESIAN_POINT('Ctrl Pts',(-6.16290819730177,4.96213428201292,-55.8593452467601));
#63154=CARTESIAN_POINT('Ctrl Pts',(-6.25125914364643,4.85035791077833,-55.8534682487453));
#63155=CARTESIAN_POINT('Ctrl Pts',(-6.4782697424781,4.54664516700848,-55.8377106137285));
#63156=CARTESIAN_POINT('Ctrl Pts',(-6.61141355276991,4.35076661848367,-55.8277645734934));
#63157=CARTESIAN_POINT('Ctrl Pts',(-6.94189623509074,3.81428204311281,-55.8012958665957));
#63158=CARTESIAN_POINT('Ctrl Pts',(-7.1229553825257,3.46441789577465,-55.7848325679527));
#63159=CARTESIAN_POINT('Ctrl Pts',(-7.31693430575079,3.00942491103916,-55.7645080043756));
#63160=CARTESIAN_POINT('Ctrl Pts',(-7.3548393813469,2.91556237010038,-55.7603686120139));
#63161=CARTESIAN_POINT('Ctrl Pts',(-7.4181337538715,2.74973292056485,-55.7531447938877));
#63162=CARTESIAN_POINT('Ctrl Pts',(-7.44430232529682,2.6780781459825,-55.7500520799141));
#63163=CARTESIAN_POINT('Ctrl Pts',(-7.48087684049921,2.57324891858899,-55.7455669322779));
#63164=CARTESIAN_POINT('Ctrl Pts',(-7.49210676994035,2.54036699329138,-55.7441656539896));
#63165=CARTESIAN_POINT('Ctrl Pts',(-7.5114890668149,2.48236787288347,-55.7417035004907));
#63166=CARTESIAN_POINT('Ctrl Pts',(-7.51973297341991,2.45728188681206,-55.7406416730075));
#63167=CARTESIAN_POINT('Ctrl Pts',(-7.53558576116841,2.40821534948107,-55.7385707138626));
#63168=CARTESIAN_POINT('Ctrl Pts',(-7.54320615177066,2.38423884919182,-55.7375614745711));
#63169=CARTESIAN_POINT('Ctrl Pts',(-7.5635162237632,2.31926393497324,-55.7348336912542));
#63170=CARTESIAN_POINT('Ctrl Pts',(-7.5759868893089,2.27819787168256,-55.7331173816548));
#63171=CARTESIAN_POINT('Ctrl Pts',(-7.62387371744798,2.11576340791,-55.7263573899878));
#63172=CARTESIAN_POINT('Ctrl Pts',(-7.65671267005228,1.9936541386152,-55.721338967626));
#63173=CARTESIAN_POINT('Ctrl Pts',(-7.68845622645815,1.86322911090229,-55.7160318767724));
#63174=CARTESIAN_POINT('Ctrl Pts',(-7.69028996399285,1.85564601569213,-55.7157235032714));
#63175=CARTESIAN_POINT('Ctrl Pts',(-7.83752454740121,1.2428169714209,-55.6908171746891));
#63176=CARTESIAN_POINT('Ctrl Pts',(-7.91100180423729,0.622499836634585,
-55.666937553817));
#63177=CARTESIAN_POINT('Ctrl Pts',(-7.91099845657851,-0.532535813923126,
-55.6238481307725));
#63178=CARTESIAN_POINT('Ctrl Pts',(-7.85723020891476,-1.0636513855998,-55.6045015296109));
#63179=CARTESIAN_POINT('Ctrl Pts',(-7.74990284520874,-1.58837550848826,
-55.5836168389627));
#63180=CARTESIAN_POINT('Ctrl Pts',(-7.74927157453051,-1.59145245932399,
-55.583494305611));
#63181=CARTESIAN_POINT('Ctrl Pts',(-7.74423889981475,-1.61590881988658,
-55.5825198447304));
#63182=CARTESIAN_POINT('Ctrl Pts',(-7.73975088130106,-1.63727020923664,
-55.5816654479737));
#63183=CARTESIAN_POINT('Ctrl Pts',(-7.72278761683751,-1.71638079086475,
-55.5784884040048));
#63184=CARTESIAN_POINT('Ctrl Pts',(-7.70975412148755,-1.77400754719334,
-55.5761487545977));
#63185=CARTESIAN_POINT('Ctrl Pts',(-7.69311887990501,-1.84391054982302,
-55.573274621882));
#63186=CARTESIAN_POINT('Ctrl Pts',(-7.69013109713555,-1.85633184605752,
-55.5727625167274));
#63187=CARTESIAN_POINT('Ctrl Pts',(-7.68516576318915,-1.87675681998095,
-55.5719180743792));
#63188=CARTESIAN_POINT('Ctrl Pts',(-7.68320575973477,-1.88476476568983,
-55.5715863988233));
#63189=CARTESIAN_POINT('Ctrl Pts',(-7.67965620408566,-1.89916956417051,
-55.5709886785668));
#63190=CARTESIAN_POINT('Ctrl Pts',(-7.67807116664546,-1.90556752859101,
-55.570722807939));
#63191=CARTESIAN_POINT('Ctrl Pts',(-7.67467881183064,-1.91918773508362,
-55.5701559694763));
#63192=CARTESIAN_POINT('Ctrl Pts',(-7.67286929246645,-1.9264094184512,-55.5698549155698));
#63193=CARTESIAN_POINT('Ctrl Pts',(-7.66798139670256,-1.94580057366551,
-55.5690451643568));
#63194=CARTESIAN_POINT('Ctrl Pts',(-7.66488425276642,-1.9579652606602,-55.5685357180314));
#63195=CARTESIAN_POINT('Ctrl Pts',(-7.64982344735919,-2.01653636490782,
-55.5660755527685));
#63196=CARTESIAN_POINT('Ctrl Pts',(-7.6374673909556,-2.06284012801415,-55.5641086825192));
#63197=CARTESIAN_POINT('Ctrl Pts',(-7.603799098474,-2.18455987054575,-55.5588740026004));
#63198=CARTESIAN_POINT('Ctrl Pts',(-7.58178686316967,-2.25977193784916,
-55.5555716405067));
#63199=CARTESIAN_POINT('Ctrl Pts',(-7.52667515768994,-2.43820220542041,
-55.547588302883));
#63200=CARTESIAN_POINT('Ctrl Pts',(-7.49256449695593,-2.54109124659927,
-55.5428659183496));
#63201=CARTESIAN_POINT('Ctrl Pts',(-7.38780807938719,-2.83659965150273,
-55.5290125342096));
#63202=CARTESIAN_POINT('Ctrl Pts',(-7.31177130844375,-3.02720999963955,
-55.5197159469372));
#63203=CARTESIAN_POINT('Ctrl Pts',(-6.97343703411647,-3.78798538396104,
-55.4816120433421));
#63204=CARTESIAN_POINT('Ctrl Pts',(-6.65111500182147,-4.32902682033968,
-55.452365440589));
#63205=CARTESIAN_POINT('Ctrl Pts',(-6.11280593547542,-5.02816363891197,
-55.4141211414029));
#63206=CARTESIAN_POINT('Ctrl Pts',(-5.94771284151276,-5.22240873526371,
-55.4034081083382));
#63207=CARTESIAN_POINT('Ctrl Pts',(-5.75635002591773,-5.42669202613192,
-55.3920414765225));
#63208=CARTESIAN_POINT('Ctrl Pts',(-5.73909005137082,-5.44494236554374,
-55.3910250113978));
#63209=CARTESIAN_POINT('Ctrl Pts',(-5.71462805941281,-5.47056243033573,
-55.3895966239102));
#63210=CARTESIAN_POINT('Ctrl Pts',(-5.70749820542755,-5.47800067521219,
-55.3891817466346));
#63211=CARTESIAN_POINT('Ctrl Pts',(-5.69506360702925,-5.49092248358392,
-55.3884607057034));
#63212=CARTESIAN_POINT('Ctrl Pts',(-5.68976543106216,-5.49641233430998,
-55.3881542721157));
#63213=CARTESIAN_POINT('Ctrl Pts',(-5.67868946254114,-5.5078558274845,-55.3875153086717));
#63214=CARTESIAN_POINT('Ctrl Pts',(-5.67291022777081,-5.51380806489604,
-55.3871828390426));
#63215=CARTESIAN_POINT('Ctrl Pts',(-5.65921619352339,-5.52786771264241,
-55.3863972355055));
#63216=CARTESIAN_POINT('Ctrl Pts',(-5.65129330984199,-5.53596724168018,
-55.3859444378222));
#63217=CARTESIAN_POINT('Ctrl Pts',(-5.62505673278056,-5.56267376012855,
-55.3844506707206));
#63218=CARTESIAN_POINT('Ctrl Pts',(-5.60666824705465,-5.58120719844518,
-55.3834128217441));
#63219=CARTESIAN_POINT('Ctrl Pts',(-5.31472250470243,-5.87255539814665,
-55.3670771640219));
#63220=CARTESIAN_POINT('Ctrl Pts',(-5.0216222160986,-6.1250740224363,-55.3526667189258));
#63221=CARTESIAN_POINT('Ctrl Pts',(-4.49814111733228,-6.51314057549209,
-55.3293109718319));
#63222=CARTESIAN_POINT('Ctrl Pts',(-4.27725093900374,-6.66028553317942,
-55.3200747146529));
#63223=CARTESIAN_POINT('Ctrl Pts',(-3.82922638058848,-6.92723778879926,
-55.3020266643066));
#63224=CARTESIAN_POINT('Ctrl Pts',(-3.60282775155223,-7.04763984001828,
-55.2932204435217));
#63225=CARTESIAN_POINT('Ctrl Pts',(-3.02509029888152,-7.31976361230073,
-55.2707988941708));
#63226=CARTESIAN_POINT('Ctrl Pts',(-2.66785583847887,-7.45738689122056,
-55.2569781168214));
#63227=CARTESIAN_POINT('Ctrl Pts',(-2.2795820804605,-7.57548549945729,-55.2408490092121));
#63228=CARTESIAN_POINT('Ctrl Pts',(-2.25703293581027,-7.5822343225758,-55.2399085715611));
#63229=CARTESIAN_POINT('Ctrl Pts',(-2.22586865214535,-7.59141026722428,
-55.2386040125424));
#63230=CARTESIAN_POINT('Ctrl Pts',(-2.21727884871055,-7.59392359772011,
-55.2382439332683));
#63231=CARTESIAN_POINT('Ctrl Pts',(-2.20357551004866,-7.59790788858827,
-55.2376687151734));
#63232=CARTESIAN_POINT('Ctrl Pts',(-2.19846470673627,-7.5993882809737,-55.2374540081885));
#63233=CARTESIAN_POINT('Ctrl Pts',(-2.18850769401081,-7.60226153845866,
-55.2370353776009));
#63234=CARTESIAN_POINT('Ctrl Pts',(-2.18366163803773,-7.60365492879917,
-55.2368314778365));
#63235=CARTESIAN_POINT('Ctrl Pts',(-2.17204936964131,-7.60698179673731,
-55.2363425255854));
#63236=CARTESIAN_POINT('Ctrl Pts',(-2.16528190982576,-7.60891087939554,
-55.2360572776687));
#63237=CARTESIAN_POINT('Ctrl Pts',(-2.14492160107624,-7.61468527763998,
-55.235198227941));
#63238=CARTESIAN_POINT('Ctrl Pts',(-2.13132106284457,-7.61850320441981,
-55.2346232313804));
#63239=CARTESIAN_POINT('Ctrl Pts',(-2.00895972791461,-7.65249903204976,
-55.2294401519018));
#63240=CARTESIAN_POINT('Ctrl Pts',(-1.89957795843188,-7.68038167387948,
-55.2247364600537));
#63241=CARTESIAN_POINT('Ctrl Pts',(-1.6009105569652,-7.74974494082192,-55.2117685234611));
#63242=CARTESIAN_POINT('Ctrl Pts',(-1.41063882166443,-7.78662667780105,
-55.2033741580621));
#63243=CARTESIAN_POINT('Ctrl Pts',(-0.762131857371492,-7.88778048372765,
-55.1746688886916));
#63244=CARTESIAN_POINT('Ctrl Pts',(-0.2996540427684,-7.91884865599477,-55.1541084505469));
#63245=CARTESIAN_POINT('Ctrl Pts',(0.520687287788129,-7.90195422711492,
-55.1188307209384));
#63246=CARTESIAN_POINT('Ctrl Pts',(0.877588525604872,-7.87031519222064,
-55.1038662783691));
#63247=CARTESIAN_POINT('Ctrl Pts',(1.26992637823986,-7.80850495511669,-55.0877714276107));
#63248=CARTESIAN_POINT('Ctrl Pts',(1.30866590547101,-7.80210588377465,-55.0861857423325));
#63249=CARTESIAN_POINT('Ctrl Pts',(1.36516216870489,-7.79234109685443,-55.0838778715657));
#63250=CARTESIAN_POINT('Ctrl Pts',(1.38295738154021,-7.78920255228993,-55.083151609686));
#63251=CARTESIAN_POINT('Ctrl Pts',(1.4144628695433,-7.7835345540384,-55.0818669245178));
#63252=CARTESIAN_POINT('Ctrl Pts',(1.42817748632771,-7.78102977967554,-55.081308067353));
#63253=CARTESIAN_POINT('Ctrl Pts',(1.4566565951586,-7.77575065496306,-55.0801483179159));
#63254=CARTESIAN_POINT('Ctrl Pts',(1.47141995361585,-7.77297047506448,-55.0795475297301));
#63255=CARTESIAN_POINT('Ctrl Pts',(1.50954510166274,-7.76567838066628,-55.0779970600195));
#63256=CARTESIAN_POINT('Ctrl Pts',(1.53289465464886,-7.76110308592623,-55.0770484699124));
#63257=CARTESIAN_POINT('Ctrl Pts',(1.62735465395755,-7.74215094015142,-55.0732145595764));
#63258=CARTESIAN_POINT('Ctrl Pts',(1.69828723292825,-7.72690138648523,-55.0703436068045));
#63259=CARTESIAN_POINT('Ctrl Pts',(2.14578345272487,-7.62423583244075,-55.0522776679822));
#63260=CARTESIAN_POINT('Ctrl Pts',(2.51573295400785,-7.5102908542568,-55.0375832247385));
#63261=CARTESIAN_POINT('Ctrl Pts',(3.38700965856274,-7.17029422832482,-55.0027578942878));
#63262=CARTESIAN_POINT('Ctrl Pts',(3.87597666938707,-6.9182161861047,-54.9830738033588));
#63263=CARTESIAN_POINT('Ctrl Pts',(4.33965173363069,-6.61448229573179,-54.962016916029));
#63264=CARTESIAN_POINT('Ctrl Pts',(4.3443958525004,-6.6113673235132,-54.9618011901168));
#63265=CARTESIAN_POINT('Ctrl Pts',(4.3974363263187,-6.57645938835733,-54.9593861362115));
#63266=CARTESIAN_POINT('Ctrl Pts',(4.4453856116793,-6.54414325641568,-54.9571733577931));
#63267=CARTESIAN_POINT('Ctrl Pts',(4.59519688106566,-6.4407694412966,-54.9501555438857));
#63268=CARTESIAN_POINT('Ctrl Pts',(4.69573992322429,-6.36783873595535,-54.9452917982395));
#63269=CARTESIAN_POINT('Ctrl Pts',(4.80844199040373,-6.28196727989032,-54.9396215895873));
#63270=CARTESIAN_POINT('Ctrl Pts',(4.82232724922656,-6.27131462901099,-54.9389191316937));
#63271=CARTESIAN_POINT('Ctrl Pts',(4.84268646293899,-6.25558762068886,-54.9378833047485));
#63272=CARTESIAN_POINT('Ctrl Pts',(4.84918808710363,-6.25054906017829,-54.9375516365831));
#63273=CARTESIAN_POINT('Ctrl Pts',(4.86073761865742,-6.24156965948325,-54.9369608707167));
#63274=CARTESIAN_POINT('Ctrl Pts',(4.86578862728181,-6.23763280787818,-54.9367019664899));
#63275=CARTESIAN_POINT('Ctrl Pts',(4.87631014924028,-6.22941157822333,-54.9361615137879));
#63276=CARTESIAN_POINT('Ctrl Pts',(4.88177980762432,-6.22512611855818,-54.9358799120873));
#63277=CARTESIAN_POINT('Ctrl Pts',(4.89595552391453,-6.21398931800964,-54.935148393218));
#63278=CARTESIAN_POINT('Ctrl Pts',(4.904652830353,-6.20712689966362,-54.9346979211494));
#63279=CARTESIAN_POINT('Ctrl Pts',(4.94160509759953,-6.17784437039839,-54.9327768172258));
#63280=CARTESIAN_POINT('Ctrl Pts',(4.9697206627543,-6.15524966826104,-54.9312972045296));
#63281=CARTESIAN_POINT('Ctrl Pts',(5.25984438735853,-5.91881196421239,-54.9158329396264));
#63282=CARTESIAN_POINT('Ctrl Pts',(5.50798872129549,-5.68860916505424,-54.9008070963306));
#63283=CARTESIAN_POINT('Ctrl Pts',(6.03214537722044,-5.13582259156433,-54.8661360406876));
#63284=CARTESIAN_POINT('Ctrl Pts',(6.2985253196356,-4.80541867519549,-54.8463934387766));
#63285=CARTESIAN_POINT('Ctrl Pts',(6.78842564247443,-4.0865946783684,-54.8071227023162));
#63286=CARTESIAN_POINT('Ctrl Pts',(7.00807421978223,-3.69729074594163,-54.787744617808));
#63287=CARTESIAN_POINT('Ctrl Pts',(7.20589821174535,-3.26493570680751,-54.7684269573946));
#63288=CARTESIAN_POINT('Ctrl Pts',(7.21790426194962,-3.23830701100864,-54.7672453917297));
#63289=CARTESIAN_POINT('Ctrl Pts',(7.23402020937555,-3.20202788821996,-54.7656466811127));
#63290=CARTESIAN_POINT('Ctrl Pts',(7.2382587250096,-3.19243506081349,-54.7652250009554));
#63291=CARTESIAN_POINT('Ctrl Pts',(7.24541350942567,-3.17615448412737,-54.7645111103161));
#63292=CARTESIAN_POINT('Ctrl Pts',(7.24833961969394,-3.16947108956614,-54.7642185529997));
#63293=CARTESIAN_POINT('Ctrl Pts',(7.25396054134746,-3.15658410481679,-54.7636554106787));
#63294=CARTESIAN_POINT('Ctrl Pts',(7.256656650154,-3.15038108937497,-54.7633847801005));
#63295=CARTESIAN_POINT('Ctrl Pts',(7.26300349355916,-3.13572734702164,-54.762746471548));
#63296=CARTESIAN_POINT('Ctrl Pts',(7.26664744309853,-3.12727368178568,-54.7623790328226));
#63297=CARTESIAN_POINT('Ctrl Pts',(7.27724324812621,-3.10257376629456,-54.7613077724458));
#63298=CARTESIAN_POINT('Ctrl Pts',(7.28415545578017,-3.08631051080405,-54.7606053470367));
#63299=CARTESIAN_POINT('Ctrl Pts',(7.33372162733152,-2.96859560391608,-54.7555421433691));
#63300=CARTESIAN_POINT('Ctrl Pts',(7.37430993498511,-2.86628452979121,-54.7512543531303));
#63301=CARTESIAN_POINT('Ctrl Pts',(7.49720447543486,-2.53659401286478,-54.7377762512702));
#63302=CARTESIAN_POINT('Ctrl Pts',(7.57122921646478,-2.3062704185657,-54.7288726969598));
#63303=CARTESIAN_POINT('Ctrl Pts',(7.78021302806817,-1.53657481876719,-54.7004080150176));
#63304=CARTESIAN_POINT('Ctrl Pts',(7.86891080164407,-0.98641532140443,-54.6822068182024));
#63305=CARTESIAN_POINT('Ctrl Pts',(7.91985465720725,-0.0538123649053755,
-54.6504379347047));
#63306=CARTESIAN_POINT('Ctrl Pts',(7.91337000618335,0.324836871746122,-54.6372436818979));
#63307=CARTESIAN_POINT('Ctrl Pts',(7.87327200216501,0.775231485755742,-54.619811775851));
#63308=CARTESIAN_POINT('Ctrl Pts',(7.86567703515646,0.84883449291347,-54.6169067280316));
#63309=CARTESIAN_POINT('Ctrl Pts',(7.85576524074399,0.933271187966665,-54.6134988001413));
#63310=CARTESIAN_POINT('Ctrl Pts',(7.85445656603355,0.944221731294924,-54.6130553700091));
#63311=CARTESIAN_POINT('Ctrl Pts',(7.85249638782133,0.960337745646011,-54.612400578634));
#63312=CARTESIAN_POINT('Ctrl Pts',(7.85186267142784,0.965505409223002,-54.6121902853711));
#63313=CARTESIAN_POINT('Ctrl Pts',(7.85072544155476,0.974703822634847,-54.6118153680675));
#63314=CARTESIAN_POINT('Ctrl Pts',(7.85022392345908,0.978734822084512,-54.611650864954));
#63315=CARTESIAN_POINT('Ctrl Pts',(7.84917084580588,0.987146151749603,-54.6113071738757));
#63316=CARTESIAN_POINT('Ctrl Pts',(7.84861872384529,0.991526408678677,-54.6111279516508));
#63317=CARTESIAN_POINT('Ctrl Pts',(7.84716333717579,1.00299532640415,-54.6106580495513));
#63318=CARTESIAN_POINT('Ctrl Pts',(7.84625413587649,1.01008321421707,-54.610367004847));
#63319=CARTESIAN_POINT('Ctrl Pts',(7.84215581171683,1.04169320323664,-54.6090662002666));
#63320=CARTESIAN_POINT('Ctrl Pts',(7.83886135644933,1.06620125290702,-54.6080500618417));
#63321=CARTESIAN_POINT('Ctrl Pts',(7.81369071433686,1.2470251224477,-54.6004990826753));
#63322=CARTESIAN_POINT('Ctrl Pts',(7.78725676529886,1.40266187281416,-54.5937034431917));
#63323=CARTESIAN_POINT('Ctrl Pts',(7.70506796774039,1.81198142835418,-54.5752509547224));
#63324=CARTESIAN_POINT('Ctrl Pts',(7.64144676829595,2.06388651160993,-54.5633017912286));
#63325=CARTESIAN_POINT('Ctrl Pts',(7.47887793826145,2.59581610504982,-54.5374347302143));
#63326=CARTESIAN_POINT('Ctrl Pts',(7.37631452000722,2.8743461955747,-54.5235027177867));
#63327=CARTESIAN_POINT('Ctrl Pts',(7.04605136604026,3.63620759033023,-54.4851950114512));
#63328=CARTESIAN_POINT('Ctrl Pts',(6.78470450018962,4.10326537204607,-54.4615825201537));
#63329=CARTESIAN_POINT('Ctrl Pts',(6.45876003852165,4.56831410171105,-54.4384992005601));
#63330=CARTESIAN_POINT('Ctrl Pts',(6.43908386116293,4.59600631378975,-54.4371257891758));
#63331=CARTESIAN_POINT('Ctrl Pts',(6.41215176109188,4.63339804657379,-54.4352727123481));
#63332=CARTESIAN_POINT('Ctrl Pts',(6.40505119591575,4.64320867986584,-54.4347866427965));
#63333=CARTESIAN_POINT('Ctrl Pts',(6.39381803244136,4.65865439789752,-54.4340215785352));
#63334=CARTESIAN_POINT('Ctrl Pts',(6.38970046314842,4.66430035724578,-54.4337419618911));
#63335=CARTESIAN_POINT('Ctrl Pts',(6.3817465600791,4.6751763510422,-54.4332034051865));
#63336=CARTESIAN_POINT('Ctrl Pts',(6.37791126535237,4.68040713635017,-54.4329444223479));
#63337=CARTESIAN_POINT('Ctrl Pts',(6.36883352970287,4.69275597282373,-54.4323330957064));
#63338=CARTESIAN_POINT('Ctrl Pts',(6.36358557674847,4.6998699724186,-54.4319809815307));
#63339=CARTESIAN_POINT('Ctrl Pts',(6.34820472643205,4.72064689436233,-54.430952784423));
#63340=CARTESIAN_POINT('Ctrl Pts',(6.33803964259337,4.73428599091872,-54.430278043914));
#63341=CARTESIAN_POINT('Ctrl Pts',(6.26353355945322,4.83358518469697,-54.4253670949496));
#63342=CARTESIAN_POINT('Ctrl Pts',(6.19750097002333,4.91796515815086,-54.4212023316967));
#63343=CARTESIAN_POINT('Ctrl Pts',(5.97891491343344,5.1858892174626,-54.4079836331619));
#63344=CARTESIAN_POINT('Ctrl Pts',(5.8197617867117,5.36388418691865,-54.3992147139541));
#63345=CARTESIAN_POINT('Ctrl Pts',(5.33027516492885,5.86384052010145,-54.3742520668002));
#63346=CARTESIAN_POINT('Ctrl Pts',(4.97956829569996,6.16444331915136,-54.3588510296888));
#63347=CARTESIAN_POINT('Ctrl Pts',(4.37634108328926,6.59624298780893,-54.3334674905199));
#63348=CARTESIAN_POINT('Ctrl Pts',(4.13945996405782,6.74741715699987,-54.3237195428597));
#63349=CARTESIAN_POINT('Ctrl Pts',(3.82726271215184,6.92401964554158,-54.3105162097722));
#63350=CARTESIAN_POINT('Ctrl Pts',(3.7589064297778,6.96136551161078,-54.307604097445));
#63351=CARTESIAN_POINT('Ctrl Pts',(3.60447522246403,7.04279988979407,-54.3009525199181));
#63352=CARTESIAN_POINT('Ctrl Pts',(3.51812227366375,7.08633093732711,-54.2971837011257));
#63353=CARTESIAN_POINT('Ctrl Pts',(3.42133577018634,7.13291647927615,-54.2928806013251));
#63354=CARTESIAN_POINT('Ctrl Pts',(3.4116657194556,7.13754670530057,-54.2924498027213));
#63355=CARTESIAN_POINT('Ctrl Pts',(3.3970822320114,7.14449318102415,-54.2917987827865));
#63356=CARTESIAN_POINT('Ctrl Pts',(3.39217591269258,7.14682398564675,-54.2915795360823));
#63357=CARTESIAN_POINT('Ctrl Pts',(3.38365866963553,7.15085945548636,-54.2911985456685));
#63358=CARTESIAN_POINT('Ctrl Pts',(3.38004884333335,7.15256644577872,-54.2910369526625));
#63359=CARTESIAN_POINT('Ctrl Pts',(3.37253689852509,7.15611168679145,-54.2907004361862));
#63360=CARTESIAN_POINT('Ctrl Pts',(3.36863456654996,7.15794948030829,-54.2905254834173));
#63361=CARTESIAN_POINT('Ctrl Pts',(3.3594473907408,7.16226698102246,-54.2901132747033));
#63362=CARTESIAN_POINT('Ctrl Pts',(3.35416130734875,7.16474402910058,-54.2898758496834));
#63363=CARTESIAN_POINT('Ctrl Pts',(3.33690059896053,7.17280907387874,-54.2890997796702));
#63364=CARTESIAN_POINT('Ctrl Pts',(3.32491476919125,7.17837289302026,-54.2885596162353));
#63365=CARTESIAN_POINT('Ctrl Pts',(3.2967952988251,7.19134040826854,-54.2872895073843));
#63366=CARTESIAN_POINT('Ctrl Pts',(3.28065061923264,7.19871985945701,-54.2865580848041));
#63367=CARTESIAN_POINT('Ctrl Pts',(3.22445435503362,7.22417788266252,-54.2840048889515));
#63368=CARTESIAN_POINT('Ctrl Pts',(3.18427766640323,7.24197677251273,-54.282166727798));
#63369=CARTESIAN_POINT('Ctrl Pts',(3.0010058660068,7.32134906706468,-54.273730655506));
#63370=CARTESIAN_POINT('Ctrl Pts',(2.85626581382342,7.37901951401763,-54.2669279512671));
#63371=CARTESIAN_POINT('Ctrl Pts',(2.36597498690947,7.55778490999441,-54.2436384530356));
#63372=CARTESIAN_POINT('Ctrl Pts',(2.01374597081392,7.65916174261451,-54.2265237130789));
#63373=CARTESIAN_POINT('Ctrl Pts',(0.954777347137354,7.88582517094258,-54.1760220124996));
#63374=CARTESIAN_POINT('Ctrl Pts',(0.236505269843306,7.93991533835738,-54.143326706896));
#63375=CARTESIAN_POINT('Ctrl Pts',(-0.527536777721723,7.89353919428657,
-54.1119875467441));
#63376=CARTESIAN_POINT('Ctrl Pts',(-0.575743200093329,7.89016957608742,
-54.1100229434521));
#63377=CARTESIAN_POINT('Ctrl Pts',(-0.638558583107613,7.88520004022847,
-54.1074791035554));
#63378=CARTESIAN_POINT('Ctrl Pts',(-0.653197666611395,7.88400085932392,
-54.1068874066684));
#63379=CARTESIAN_POINT('Ctrl Pts',(-0.676593578275714,7.88201874025823,
-54.1059435772616));
#63380=CARTESIAN_POINT('Ctrl Pts',(-0.685352554448037,7.88126196549125,
-54.1055906314457));
#63381=CARTESIAN_POINT('Ctrl Pts',(-0.701132244824671,7.87987209705478,
-54.104955509869));
#63382=CARTESIAN_POINT('Ctrl Pts',(-0.70815340196265,7.87924421821569,-54.1046731723242));
#63383=CARTESIAN_POINT('Ctrl Pts',(-0.724622764837934,7.87774922606578,
-54.1040115045075));
#63384=CARTESIAN_POINT('Ctrl Pts',(-0.734070277839707,7.87687449741978,
-54.1036324113009));
#63385=CARTESIAN_POINT('Ctrl Pts',(-0.761298783026993,7.87430404548855,
-54.102541169781));
#63386=CARTESIAN_POINT('Ctrl Pts',(-0.779075686902149,7.87256509132898,
-54.101830364832));
#63387=CARTESIAN_POINT('Ctrl Pts',(-0.898106115901136,7.86051429523538,
-54.0970818016465));
#63388=CARTESIAN_POINT('Ctrl Pts',(-0.999160426027807,7.84830930590992,
-54.0931030971454));
#63389=CARTESIAN_POINT('Ctrl Pts',(-1.28813586429848,7.80773576039618,-54.0818599010228));
#63390=CARTESIAN_POINT('Ctrl Pts',(-1.47531081369862,7.7745414531394,-54.0747426720493));
#63391=CARTESIAN_POINT('Ctrl Pts',(-1.83166968149462,7.69800867037327,-54.0613989607363));
#63392=CARTESIAN_POINT('Ctrl Pts',(-2.00096880400117,7.65574802760517,-54.0551507118788));
#63393=CARTESIAN_POINT('Ctrl Pts',(-2.28597915186834,7.57450217896144,-54.0446809017212));
#63394=CARTESIAN_POINT('Ctrl Pts',(-2.40243493916674,7.53837454788521,-54.0404167511492));
#63395=CARTESIAN_POINT('Ctrl Pts',(-2.81028230597749,7.40143817982617,-54.0254402659087));
#63396=CARTESIAN_POINT('Ctrl Pts',(-3.09656329809623,7.2863066337836,-54.0148577191107));
#63397=CARTESIAN_POINT('Ctrl Pts',(-3.40956978446522,7.13864014658615,-54.0026343744809));
#63398=CARTESIAN_POINT('Ctrl Pts',(-3.44363326145886,7.12227064854316,-54.0012950392811));
#63399=CARTESIAN_POINT('Ctrl Pts',(-3.76574166829126,6.96462766408025,-53.9885334794922));
#63400=CARTESIAN_POINT('Ctrl Pts',(-4.04505660463857,6.80620108412178,-53.9766925878763));
#63401=CARTESIAN_POINT('Ctrl Pts',(-4.33844329437361,6.61533686096317,-53.9627985377571));
#63402=CARTESIAN_POINT('Ctrl Pts',(-4.36280775354252,6.59929393807605,-53.9616345004365));
#63403=CARTESIAN_POINT('Ctrl Pts',(-4.39663083261573,6.57675375666423,-53.9600048083122));
#63404=CARTESIAN_POINT('Ctrl Pts',(-4.40616505888879,6.57037001441782,-53.9595438886546));
#63405=CARTESIAN_POINT('Ctrl Pts',(-4.4214421071285,6.56009289807269,-53.9588029098848));
#63406=CARTESIAN_POINT('Ctrl Pts',(-4.42719377251512,6.55621265963195,-53.9585233838279));
#63407=CARTESIAN_POINT('Ctrl Pts',(-4.43906753975161,6.54817952596347,-53.9579451917989));
#63408=CARTESIAN_POINT('Ctrl Pts',(-4.4451889342762,6.54402560087327,-53.9576464848813));
#63409=CARTESIAN_POINT('Ctrl Pts',(-4.45732492998902,6.53576533437485,-53.9570530497392));
#63410=CARTESIAN_POINT('Ctrl Pts',(-4.46333970672917,6.53165926082139,-53.9567583321149));
#63411=CARTESIAN_POINT('Ctrl Pts',(-4.47726592047649,6.52212411282612,-53.9560745773543));
#63412=CARTESIAN_POINT('Ctrl Pts',(-4.48517315990093,6.51668894382885,-53.9556853060677));
#63413=CARTESIAN_POINT('Ctrl Pts',(-4.50566675118284,6.50254737353732,-53.9546737452906));
#63414=CARTESIAN_POINT('Ctrl Pts',(-4.51823773553338,6.49381882867644,-53.9540506256486));
#63415=CARTESIAN_POINT('Ctrl Pts',(-4.55523033899245,6.46797394418664,-53.9522093826615));
#63416=CARTESIAN_POINT('Ctrl Pts',(-4.57958047769725,6.45075600290295,-53.9509876024828));
#63417=CARTESIAN_POINT('Ctrl Pts',(-4.66479673544995,6.38977404577522,-53.9466785186104));
#63418=CARTESIAN_POINT('Ctrl Pts',(-4.7251369363859,6.34528341028031,-53.943567207087));
#63419=CARTESIAN_POINT('Ctrl Pts',(-4.97783665199664,6.15335683717133,-53.9303023267239));
#63420=CARTESIAN_POINT('Ctrl Pts',(-5.1639967069711,5.99798225554863,-53.919948609754));
#63421=CARTESIAN_POINT('Ctrl Pts',(-5.56753592953707,5.62844433692675,-53.8964533828573));
#63422=CARTESIAN_POINT('Ctrl Pts',(-5.7802616289256,5.40975237373494,-53.8833066262118));
#63423=CARTESIAN_POINT('Ctrl Pts',(-6.24458390832893,4.87366548593838,-53.853022640944));
#63424=CARTESIAN_POINT('Ctrl Pts',(-6.48551043081799,4.54814423017104,-53.8360489401067));
#63425=CARTESIAN_POINT('Ctrl Pts',(-6.70282136106142,4.20191931343049,-53.8191356191575));
#63426=CARTESIAN_POINT('Ctrl Pts',(-6.70514255138793,4.19821432045426,-53.8189547476318));
#63427=CARTESIAN_POINT('Ctrl Pts',(-6.87885152113025,3.92043531800506,-53.8054029773147));
#63428=CARTESIAN_POINT('Ctrl Pts',(-7.0332886609483,3.6361065271504,-53.7921346187607));
#63429=CARTESIAN_POINT('Ctrl Pts',(-7.18961545053255,3.30083744898722,-53.7771431321115));
#63430=CARTESIAN_POINT('Ctrl Pts',(-7.20895930240743,3.25837444117939,-53.7752562593331));
#63431=CARTESIAN_POINT('Ctrl Pts',(-7.23934303553309,3.19008185295821,-53.7722404787148));
#63432=CARTESIAN_POINT('Ctrl Pts',(-7.25062294358469,3.16436040169295,-53.7711088712501));
#63433=CARTESIAN_POINT('Ctrl Pts',(-7.27043170174463,3.11852865971118,-53.7691000058417));
#63434=CARTESIAN_POINT('Ctrl Pts',(-7.27901467459513,3.09844210880646,-53.7682221276886));
#63435=CARTESIAN_POINT('Ctrl Pts',(-7.29677053647698,3.05640746370622,-53.7663902825494));
#63436=CARTESIAN_POINT('Ctrl Pts',(-7.30592784959485,3.03445301614396,-53.7654365069312));
#63437=CARTESIAN_POINT('Ctrl Pts',(-7.32425095668012,2.98996001677971,-53.7635095607009));
#63438=CARTESIAN_POINT('Ctrl Pts',(-7.33341207479184,2.9674198092773,-53.7625364546635));
#63439=CARTESIAN_POINT('Ctrl Pts',(-7.35570370444462,2.91183929149015,-53.7601444383015));
#63440=CARTESIAN_POINT('Ctrl Pts',(-7.36871576535513,2.87875199201673,-53.7587269627814));
#63441=CARTESIAN_POINT('Ctrl Pts',(-7.47764032933658,2.59619880073618,-53.7466764401149));
#63442=CARTESIAN_POINT('Ctrl Pts',(-7.56107837369439,2.34210426292137,-53.7362052059926));
#63443=CARTESIAN_POINT('Ctrl Pts',(-7.78632216112692,1.51738015987966,-53.7030462575338));
#63444=CARTESIAN_POINT('Ctrl Pts',(-7.87749459837603,0.935029773221766,
-53.6809717783752));
#63445=CARTESIAN_POINT('Ctrl Pts',(-7.90556123071894,0.297601721963366,
-53.6556410791621));
#63446=CARTESIAN_POINT('Ctrl Pts',(-7.90729799371476,0.247191245373527,
-53.6536290007675));
#63447=CARTESIAN_POINT('Ctrl Pts',(-7.9089784646963,0.179649317186588,-53.6509186451043));
#63448=CARTESIAN_POINT('Ctrl Pts',(-7.90934879906975,0.162529388289797,
-53.6502303822926));
#63449=CARTESIAN_POINT('Ctrl Pts',(-7.90985409391974,0.13504327102425,-53.6491233474437));
#63450=CARTESIAN_POINT('Ctrl Pts',(-7.91002426783803,0.124677799078725,
-53.6487054081451));
#63451=CARTESIAN_POINT('Ctrl Pts',(-7.91032660525457,0.10375662961902,-53.6478609566455));
#63452=CARTESIAN_POINT('Ctrl Pts',(-7.91045801604645,0.0932009418190795,
-53.6474344283171));
#63453=CARTESIAN_POINT('Ctrl Pts',(-7.9106823020334,0.0717328708784928,
-53.6465660377603));
#63454=CARTESIAN_POINT('Ctrl Pts',(-7.91077372669421,0.0608204953856951,
-53.6461241447665));
#63455=CARTESIAN_POINT('Ctrl Pts',(-7.91094750178523,0.0332756570924339,
-53.6450075353264));
#63456=CARTESIAN_POINT('Ctrl Pts',(-7.91099997780887,0.016643096219158,
-53.644332190979));
#63457=CARTESIAN_POINT('Ctrl Pts',(-7.91099999999297,1.05515043374329E-5,
-53.643655794299));
#63458=CARTESIAN_POINT('',(-7.89680882399629,-0.000256294892049957,-49.6423315082368));
#63459=CARTESIAN_POINT('Ctrl Pts',(-7.91099999999197,1.12721192983993E-5,
-53.6436558236043));
#63460=CARTESIAN_POINT('Ctrl Pts',(-7.91100002702492,-0.0189609985400898,
-53.6428842771856));
#63461=CARTESIAN_POINT('Ctrl Pts',(-7.91093180470916,-0.0379331745797025,
-53.6421113645619));
#63462=CARTESIAN_POINT('Ctrl Pts',(-7.91048557968446,-0.0999664205042712,
-53.6395798981015));
#63463=CARTESIAN_POINT('Ctrl Pts',(-7.90982423016865,-0.143024459786413,
-53.6378160390351));
#63464=CARTESIAN_POINT('Ctrl Pts',(-7.90073970735434,-0.529147779870896,
-53.6219444644952));
#63465=CARTESIAN_POINT('Ctrl Pts',(-7.87035369665328,-0.871327190126642,
-53.6075096709314));
#63466=CARTESIAN_POINT('Ctrl Pts',(-7.76213187703278,-1.5702950088947,-53.5778013395704));
#63467=CARTESIAN_POINT('Ctrl Pts',(-7.68163567755936,-1.92587693057893,
-53.5625699733064));
#63468=CARTESIAN_POINT('Ctrl Pts',(-7.54580730289272,-2.37832499210327,
-53.5431354014342));
#63469=CARTESIAN_POINT('Ctrl Pts',(-7.51255932009513,-2.48134852123084,
-53.5387046220139));
#63470=CARTESIAN_POINT('Ctrl Pts',(-7.45924604033683,-2.63563923007961,
-53.5320571036591));
#63471=CARTESIAN_POINT('Ctrl Pts',(-7.44074298114661,-2.68743178207014,
-53.5298235762763));
#63472=CARTESIAN_POINT('Ctrl Pts',(-7.40980630311237,-2.77125817332328,
-53.5262043965742));
#63473=CARTESIAN_POINT('Ctrl Pts',(-7.39770146552207,-2.80341119935944,
-53.5248151816664));
#63474=CARTESIAN_POINT('Ctrl Pts',(-7.37607954411903,-2.85972830219121,
-53.5223798726228));
#63475=CARTESIAN_POINT('Ctrl Pts',(-7.3666522171318,-2.88392623359077,-53.5213328164106));
#63476=CARTESIAN_POINT('Ctrl Pts',(-7.34733957858663,-2.93278501879802,
-53.5192171699519));
#63477=CARTESIAN_POINT('Ctrl Pts',(-7.33744884296905,-2.9574433776601,-53.5181486530537));
#63478=CARTESIAN_POINT('Ctrl Pts',(-7.3180684927669,-3.00506436558251,-53.5160834273292));
#63479=CARTESIAN_POINT('Ctrl Pts',(-7.30859454848868,-3.02803303094017,
-53.5150865653112));
#63480=CARTESIAN_POINT('Ctrl Pts',(-7.28572123517774,-3.08275442350778,
-53.5127096164695));
#63481=CARTESIAN_POINT('Ctrl Pts',(-7.27222225325317,-3.11446500435225,
-53.5113305899829));
#63482=CARTESIAN_POINT('Ctrl Pts',(-7.22195588171039,-3.23043743296493,
-53.5062805077389));
#63483=CARTESIAN_POINT('Ctrl Pts',(-7.18392752531771,-3.31414517998115,
-53.5026224676579));
#63484=CARTESIAN_POINT('Ctrl Pts',(-6.87478793413653,-3.96428365237463,
-53.4740724235326));
#63485=CARTESIAN_POINT('Ctrl Pts',(-6.53854507107019,-4.49730640849635,
-53.4498176057152));
#63486=CARTESIAN_POINT('Ctrl Pts',(-5.97557082726451,-5.19104145605043,
-53.4163758555366));
#63487=CARTESIAN_POINT('Ctrl Pts',(-5.79807018158413,-5.38857501834833,
-53.4065603048889));
#63488=CARTESIAN_POINT('Ctrl Pts',(-5.36046472943528,-5.82886124220214,
-53.3834768605279));
#63489=CARTESIAN_POINT('Ctrl Pts',(-5.09326571789599,-6.06373013307058,
-53.3702017227878));
#63490=CARTESIAN_POINT('Ctrl Pts',(-4.77484522693447,-6.30768355747168,
-53.3543740885788));
#63491=CARTESIAN_POINT('Ctrl Pts',(-4.73824652610216,-6.33522206106347,
-53.3525544075141));
#63492=CARTESIAN_POINT('Ctrl Pts',(-4.69406355250205,-6.36787027438284,
-53.3503546979899));
#63493=CARTESIAN_POINT('Ctrl Pts',(-4.68670652980634,-6.37328693602695,
-53.3499883215119));
#63494=CARTESIAN_POINT('Ctrl Pts',(-4.67390153620025,-6.38268054396916,
-53.3493504422283));
#63495=CARTESIAN_POINT('Ctrl Pts',(-4.66845782315042,-6.38666329546004,
-53.3490792028215));
#63496=CARTESIAN_POINT('Ctrl Pts',(-4.65753742873333,-6.39463149664297,
-53.3485349453204));
#63497=CARTESIAN_POINT('Ctrl Pts',(-4.65206070892645,-6.39861688476756,
-53.3482619247411));
#63498=CARTESIAN_POINT('Ctrl Pts',(-4.64161709505353,-6.40619616692135,
-53.3477411563492));
#63499=CARTESIAN_POINT('Ctrl Pts',(-4.63665112701863,-6.40979133140875,
-53.347493468229));
#63500=CARTESIAN_POINT('Ctrl Pts',(-4.62508553787768,-6.4181438870735,-53.3469164562783));
#63501=CARTESIAN_POINT('Ctrl Pts',(-4.61848275423037,-6.42289687260343,
-53.3465869244099));
#63502=CARTESIAN_POINT('Ctrl Pts',(-4.59531119625548,-6.4395226140326,-53.345430030395));
#63503=CARTESIAN_POINT('Ctrl Pts',(-4.57870396493736,-6.45134144794868,
-53.3446000755267));
#63504=CARTESIAN_POINT('Ctrl Pts',(-4.36692899180706,-6.60082527398464,
-53.3340040559917));
#63505=CARTESIAN_POINT('Ctrl Pts',(-4.16570619869486,-6.72962258959657,
-53.3237352679951));
#63506=CARTESIAN_POINT('Ctrl Pts',(-3.89865460003981,-6.88398652516736,
-53.310048830646));
#63507=CARTESIAN_POINT('Ctrl Pts',(-3.83785873621647,-6.91806462862786,
-53.3069307604148));
#63508=CARTESIAN_POINT('Ctrl Pts',(-3.72617696676273,-6.97874071467036,
-53.3012076582846));
#63509=CARTESIAN_POINT('Ctrl Pts',(-3.67543608525703,-7.0055967775992,-53.2986092187451));
#63510=CARTESIAN_POINT('Ctrl Pts',(-3.46542712837245,-7.11384040233811,
-53.2878726130681));
#63511=CARTESIAN_POINT('Ctrl Pts',(-3.3037151895838,-7.19036680263977,-53.2796482495858));
#63512=CARTESIAN_POINT('Ctrl Pts',(-2.79942460730235,-7.40840436506582,
-53.2543485302309));
#63513=CARTESIAN_POINT('Ctrl Pts',(-2.4493707651624,-7.5313902550396,-53.237286030588));
#63514=CARTESIAN_POINT('Ctrl Pts',(-1.82198656211996,-7.70341873800769,
-53.2082899639828));
#63515=CARTESIAN_POINT('Ctrl Pts',(-1.54824521200786,-7.76306968124812,
-53.1961371237463));
#63516=CARTESIAN_POINT('Ctrl Pts',(-1.1502316833176,-7.82790419135908,-53.179251288626));
#63517=CARTESIAN_POINT('Ctrl Pts',(-1.02811373373937,-7.84487736208303,
-53.174173430987));
#63518=CARTESIAN_POINT('Ctrl Pts',(-0.886452852558304,-7.86120191727009,
-53.168398556748));
#63519=CARTESIAN_POINT('Ctrl Pts',(-0.867252224354421,-7.86334329848461,
-53.1676182726197));
#63520=CARTESIAN_POINT('Ctrl Pts',(-0.838082974517854,-7.86648830803632,
-53.1664365500466));
#63521=CARTESIAN_POINT('Ctrl Pts',(-0.828120036341239,-7.86754336365334,
-53.1660335751573));
#63522=CARTESIAN_POINT('Ctrl Pts',(-0.810852193222569,-7.86933883053438,
-53.1653362562627));
#63523=CARTESIAN_POINT('Ctrl Pts',(-0.803548222908068,-7.87008800222871,
-53.1650416507617));
#63524=CARTESIAN_POINT('Ctrl Pts',(-0.788380924656921,-7.87162238460148,
-53.1644305961292));
#63525=CARTESIAN_POINT('Ctrl Pts',(-0.78051743965155,-7.87240598387672,
-53.1641141954394));
#63526=CARTESIAN_POINT('Ctrl Pts',(-0.761377482731788,-7.87428432846523,
-53.1633450373065));
#63527=CARTESIAN_POINT('Ctrl Pts',(-0.75009979337468,-7.87536663641831,
-53.1628926517963));
#63528=CARTESIAN_POINT('Ctrl Pts',(-0.707584451377801,-7.87935463568644,
-53.1611902893438));
#63529=CARTESIAN_POINT('Ctrl Pts',(-0.676331749001465,-7.88209874484733,
-53.1599451391207));
#63530=CARTESIAN_POINT('Ctrl Pts',(-0.139654209866519,-7.92600566489746,
-53.138668157586));
#63531=CARTESIAN_POINT('Ctrl Pts',(0.368573939751416,-7.91866740911749,
-53.1202152915526));
#63532=CARTESIAN_POINT('Ctrl Pts',(1.15287861987413,-7.83162110008994,-53.0925550642215));
#63533=CARTESIAN_POINT('Ctrl Pts',(1.43124899721987,-7.78556006609077,-53.0828787207781));
#63534=CARTESIAN_POINT('Ctrl Pts',(2.02037120439611,-7.65540997558865,-53.0619686508084));
#63535=CARTESIAN_POINT('Ctrl Pts',(2.32964800912201,-7.56702867024691,-53.0507245832274));
#63536=CARTESIAN_POINT('Ctrl Pts',(2.75242743429345,-7.41782924016103,-53.0341127852327));
#63537=CARTESIAN_POINT('Ctrl Pts',(2.87113992820904,-7.37269290110939,-53.029305586341));
#63538=CARTESIAN_POINT('Ctrl Pts',(3.04632359976529,-7.30121260201027,-53.0219365156387));
#63539=CARTESIAN_POINT('Ctrl Pts',(3.10365348030273,-7.27702740358645,-53.0194792903216));
#63540=CARTESIAN_POINT('Ctrl Pts',(3.1711544788704,-7.24760860241437,-53.0165299997432));
#63541=CARTESIAN_POINT('Ctrl Pts',(3.18160411427374,-7.24302743614106,-53.0160718703603));
#63542=CARTESIAN_POINT('Ctrl Pts',(3.19707522586062,-7.23620489199369,-53.0153913197354));
#63543=CARTESIAN_POINT('Ctrl Pts',(3.20210436562234,-7.23398084529981,-53.015169739179));
#63544=CARTESIAN_POINT('Ctrl Pts',(3.21227539615853,-7.22947020512913,-53.0147208950278));
#63545=CARTESIAN_POINT('Ctrl Pts',(3.21741717395064,-7.22718336533366,-53.014493619703));
#63546=CARTESIAN_POINT('Ctrl Pts',(3.22737650677894,-7.2227411512545,-53.0140526883302));
#63547=CARTESIAN_POINT('Ctrl Pts',(3.23219435455598,-7.22058643800766,-53.013839063575));
#63548=CARTESIAN_POINT('Ctrl Pts',(3.2436599360143,-7.21544484653496,-53.0133299125973));
#63549=CARTESIAN_POINT('Ctrl Pts',(3.25030569732191,-7.21245360382402,-53.013034182912));
#63550=CARTESIAN_POINT('Ctrl Pts',(3.2738930285119,-7.2017977756235,-53.0119824201069));
#63551=CARTESIAN_POINT('Ctrl Pts',(3.29081161635932,-7.19408268375149,-53.0112240736656));
#63552=CARTESIAN_POINT('Ctrl Pts',(3.59139985970576,-7.05572839257941,-52.9976824491142));
#63553=CARTESIAN_POINT('Ctrl Pts',(3.86710227865614,-6.90846984218416,-52.9841908795885));
#63554=CARTESIAN_POINT('Ctrl Pts',(4.54289989184964,-6.49435763903491,-52.9494867387107));
#63555=CARTESIAN_POINT('Ctrl Pts',(4.92875672625827,-6.20661073241221,-52.928156868474));
#63556=CARTESIAN_POINT('Ctrl Pts',(5.45361778779953,-5.73521180589861,-52.8979547851229));
#63557=CARTESIAN_POINT('Ctrl Pts',(5.61461250349194,-5.57769975749903,-52.8884824431236));
#63558=CARTESIAN_POINT('Ctrl Pts',(5.8226450180353,-5.35601961679021,-52.8759407528129));
#63559=CARTESIAN_POINT('Ctrl Pts',(5.87575217778226,-5.29770495360397,-52.8727098871846));
#63560=CARTESIAN_POINT('Ctrl Pts',(5.95270327768995,-5.21062747916333,-52.8679818155184));
#63561=CARTESIAN_POINT('Ctrl Pts',(5.9772291981772,-5.18247490884502,-52.8664676575379));
#63562=CARTESIAN_POINT('Ctrl Pts',(6.01567415556181,-5.13770912892152,-52.8640822325936));
#63563=CARTESIAN_POINT('Ctrl Pts',(6.02972570971153,-5.12121064891564,-52.8632077962738));
#63564=CARTESIAN_POINT('Ctrl Pts',(6.05346525922978,-5.09310396029484,-52.861725985687));
#63565=CARTESIAN_POINT('Ctrl Pts',(6.06318806952148,-5.08152536454749,-52.8611178006525));
#63566=CARTESIAN_POINT('Ctrl Pts',(6.08242592134681,-5.05848177713828,-52.8599118088436));
#63567=CARTESIAN_POINT('Ctrl Pts',(6.09194188579058,-5.04701763819135,-52.8593139825223));
#63568=CARTESIAN_POINT('Ctrl Pts',(6.11032991156404,-5.02473731370604,-52.8581562391133));
#63569=CARTESIAN_POINT('Ctrl Pts',(6.11920577843296,-5.01392434551207,-52.8575962382175));
#63570=CARTESIAN_POINT('Ctrl Pts',(6.13967113511034,-4.98885726848925,-52.8563022898844));
#63571=CARTESIAN_POINT('Ctrl Pts',(6.15123975863613,-4.97458620666899,-52.8555688017202));
#63572=CARTESIAN_POINT('Ctrl Pts',(6.18224014556943,-4.93607061970106,-52.8535976201832));
#63573=CARTESIAN_POINT('Ctrl Pts',(6.20157901639117,-4.91175163219555,-52.8523618919502));
#63574=CARTESIAN_POINT('Ctrl Pts',(6.32577904400391,-4.75366490269811,-52.8443850291563));
#63575=CARTESIAN_POINT('Ctrl Pts',(6.42645115662078,-4.61665879369899,-52.8377319897511));
#63576=CARTESIAN_POINT('Ctrl Pts',(6.54444612974146,-4.44473078544374,-52.829676839139));
#63577=CARTESIAN_POINT('Ctrl Pts',(6.56602602861521,-4.41278926735364,-52.8281922947841));
#63578=CARTESIAN_POINT('Ctrl Pts',(6.65530053349824,-4.27854461822577,-52.8220017005931));
#63579=CARTESIAN_POINT('Ctrl Pts',(6.72084506145249,-4.17483073539156,-52.8173366316686));
#63580=CARTESIAN_POINT('Ctrl Pts',(7.08487275782888,-3.5680078834272,-52.7906434222177));
#63581=CARTESIAN_POINT('Ctrl Pts',(7.32921812444578,-3.03457336670946,-52.7696645232624));
#63582=CARTESIAN_POINT('Ctrl Pts',(7.58610694931989,-2.2561117262073,-52.7389391062643));
#63583=CARTESIAN_POINT('Ctrl Pts',(7.64972400461407,-2.02996842347896,-52.7299800208232));
#63584=CARTESIAN_POINT('Ctrl Pts',(7.70869948872653,-1.77776807519418,-52.7197024752829));
#63585=CARTESIAN_POINT('Ctrl Pts',(7.71410390660696,-1.75416876033622,-52.7187380155588));
#63586=CARTESIAN_POINT('Ctrl Pts',(7.72334957399867,-1.71292684116246,-52.7170472764588));
#63587=CARTESIAN_POINT('Ctrl Pts',(7.72723892429009,-1.69529513823244,-52.7163227795032));
#63588=CARTESIAN_POINT('Ctrl Pts',(7.73275670556999,-1.66986770567176,-52.7152753825));
#63589=CARTESIAN_POINT('Ctrl Pts',(7.73443379454953,-1.66208251874812,-52.7149543515154));
#63590=CARTESIAN_POINT('Ctrl Pts',(7.73745670238156,-1.64794627520262,-52.7143707814436));
#63591=CARTESIAN_POINT('Ctrl Pts',(7.7388064657309,-1.64159606262795,-52.7141083965554));
#63592=CARTESIAN_POINT('Ctrl Pts',(7.74137834962042,-1.62942249069487,-52.7136049329361));
#63593=CARTESIAN_POINT('Ctrl Pts',(7.74260172054804,-1.62359939698613,-52.7133639038175));
#63594=CARTESIAN_POINT('Ctrl Pts',(7.74545563358543,-1.60993854460412,-52.7127979697225));
#63595=CARTESIAN_POINT('Ctrl Pts',(7.7470808484334,-1.60209968991191,-52.712472851856));
#63596=CARTESIAN_POINT('Ctrl Pts',(7.75180614388307,-1.57913298061151,-52.7115191795198));
#63597=CARTESIAN_POINT('Ctrl Pts',(7.75487382108652,-1.56399855408818,-52.7108893083089));
#63598=CARTESIAN_POINT('Ctrl Pts',(7.782224164587,-1.4270063188038,-52.7051743687861));
#63599=CARTESIAN_POINT('Ctrl Pts',(7.80367416563023,-1.30461766666458,-52.6999637659348));
#63600=CARTESIAN_POINT('Ctrl Pts',(7.84117742111788,-1.05637987885594,-52.68917316117));
#63601=CARTESIAN_POINT('Ctrl Pts',(7.85710242186937,-0.930559546041092,
-52.6835999825171));
#63602=CARTESIAN_POINT('Ctrl Pts',(7.93065946988354,-0.210914545287183,
-52.6513330725044));
#63603=CARTESIAN_POINT('Ctrl Pts',(7.92399604971076,0.387550362873824,-52.6231564290536));
#63604=CARTESIAN_POINT('Ctrl Pts',(7.8011078152088,1.37232105446176,-52.5787878422552));
#63605=CARTESIAN_POINT('Ctrl Pts',(7.72269823713091,1.76083492376877,-52.5617773198753));
#63606=CARTESIAN_POINT('Ctrl Pts',(7.60931988864801,2.16395408861853,-52.5448129476295));
#63607=CARTESIAN_POINT('Ctrl Pts',(7.60301760707755,2.18599399444951,-52.5438875203673));
#63608=CARTESIAN_POINT('Ctrl Pts',(7.59376218832772,2.21783715296122,-52.5425534351542));
#63609=CARTESIAN_POINT('Ctrl Pts',(7.59088570658172,2.2276624521231,-52.542142208943));
#63610=CARTESIAN_POINT('Ctrl Pts',(7.58583759785336,2.24478214135517,-52.5414263949472));
#63611=CARTESIAN_POINT('Ctrl Pts',(7.58367450555498,2.25207902112035,-52.5411215207078));
#63612=CARTESIAN_POINT('Ctrl Pts',(7.57947874693681,2.26615821510045,-52.5405337043885));
#63613=CARTESIAN_POINT('Ctrl Pts',(7.57744749947612,2.27294094163086,-52.5402507149134));
#63614=CARTESIAN_POINT('Ctrl Pts',(7.57261570315503,2.28899677709366,-52.5395812897497));
#63615=CARTESIAN_POINT('Ctrl Pts',(7.56980721958029,2.29826749803552,-52.5391951221967));
#63616=CARTESIAN_POINT('Ctrl Pts',(7.55990958804265,2.33072432308706,-52.5378444077641));
#63617=CARTESIAN_POINT('Ctrl Pts',(7.55273084925143,2.35388308592757,-52.5368828931832));
#63618=CARTESIAN_POINT('Ctrl Pts',(7.46232250866173,2.64087036090666,-52.5249950893046));
#63619=CARTESIAN_POINT('Ctrl Pts',(7.36541257242053,2.9002015642793,-52.5145512182811));
#63620=CARTESIAN_POINT('Ctrl Pts',(7.12674886395633,3.4492071834908,-52.4928082906876));
#63621=CARTESIAN_POINT('Ctrl Pts',(6.98048116937463,3.73637221448944,-52.4816734275056));
#63622=CARTESIAN_POINT('Ctrl Pts',(6.60216276518799,4.37890997598966,-52.4563792469477));
#63623=CARTESIAN_POINT('Ctrl Pts',(6.35824027697082,4.72611508094225,-52.4424273341736));
#63624=CARTESIAN_POINT('Ctrl Pts',(5.96980495537363,5.19417289012871,-52.4211834513752));
#63625=CARTESIAN_POINT('Ctrl Pts',(5.84697543773632,5.33206108968397,-52.4145758744677));
#63626=CARTESIAN_POINT('Ctrl Pts',(5.65238512565059,5.53569182749666,-52.4040603209864));
#63627=CARTESIAN_POINT('Ctrl Pts',(5.58404534539639,5.60462112066307,-52.4003588169086));
#63628=CARTESIAN_POINT('Ctrl Pts',(5.48002523511382,5.70574714492927,-52.394681705838));
#63629=CARTESIAN_POINT('Ctrl Pts',(5.44528995727355,5.73890618090714,-52.3927790298638));
#63630=CARTESIAN_POINT('Ctrl Pts',(5.40369271140936,5.77789814714745,-52.3904893711769));
#63631=CARTESIAN_POINT('Ctrl Pts',(5.39711930433196,5.7840388252189,-52.390127222238));
#63632=CARTESIAN_POINT('Ctrl Pts',(5.38698938303814,5.79346958743522,-52.3895686089832));
#63633=CARTESIAN_POINT('Ctrl Pts',(5.38344027707442,5.79676765589825,-52.3893727951164));
#63634=CARTESIAN_POINT('Ctrl Pts',(5.37722856001985,5.80252937712869,-52.3890299005343));
#63635=CARTESIAN_POINT('Ctrl Pts',(5.37456727662865,5.80499446580583,-52.3888829375943));
#63636=CARTESIAN_POINT('Ctrl Pts',(5.36898273534355,5.81016017218064,-52.3885744236157));
#63637=CARTESIAN_POINT('Ctrl Pts',(5.36605913386094,5.8128604155447,-52.3884128418346));
#63638=CARTESIAN_POINT('Ctrl Pts',(5.35785377439249,5.82042743402754,-52.3879591487498));
#63639=CARTESIAN_POINT('Ctrl Pts',(5.3525674371411,5.82528921279591,-52.3876666244402));
#63640=CARTESIAN_POINT('Ctrl Pts',(5.3307643088617,5.84528654331986,-52.3864592112173));
#63641=CARTESIAN_POINT('Ctrl Pts',(5.3141900322955,5.86035896257719,-52.3855391976666));
#63642=CARTESIAN_POINT('Ctrl Pts',(5.04434088963895,6.10366996801012,-52.3705290887467));
#63643=CARTESIAN_POINT('Ctrl Pts',(4.77665722413495,6.31535139484789,-52.3552083962517));
#63644=CARTESIAN_POINT('Ctrl Pts',(4.04824236441221,6.81850800380864,-52.3144007927183));
#63645=CARTESIAN_POINT('Ctrl Pts',(3.5695024999634,7.08089340082615,-52.2885144927858));
#63646=CARTESIAN_POINT('Ctrl Pts',(2.71618024454574,7.43986843705048,-52.2469874924611));
#63647=CARTESIAN_POINT('Ctrl Pts',(2.35450097964251,7.56212006460558,-52.2306214389443));
#63648=CARTESIAN_POINT('Ctrl Pts',(1.96347746520389,7.66349717170413,-52.2142862625562));
#63649=CARTESIAN_POINT('Ctrl Pts',(1.94155716979059,7.66908002470962,-52.2133748159648));
#63650=CARTESIAN_POINT('Ctrl Pts',(1.90997785344604,7.67697884884465,-52.212067853168));
#63651=CARTESIAN_POINT('Ctrl Pts',(1.90033805074685,7.67937073855313,-52.2116697109006));
#63652=CARTESIAN_POINT('Ctrl Pts',(1.88358904636068,7.68349314042776,-52.2109793575367));
#63653=CARTESIAN_POINT('Ctrl Pts',(1.8764819128227,7.68523195263545,-52.2106868599002));
#63654=CARTESIAN_POINT('Ctrl Pts',(1.86280423899916,7.68855819115315,-52.2101247941411));
#63655=CARTESIAN_POINT('Ctrl Pts',(1.85623405910754,7.69014706034183,-52.2098551764426));
#63656=CARTESIAN_POINT('Ctrl Pts',(1.84074085060018,7.69387277690071,-52.2092202693648));
#63657=CARTESIAN_POINT('Ctrl Pts',(1.83181611497211,7.69600252780231,-52.2088552248557));
#63658=CARTESIAN_POINT('Ctrl Pts',(1.80089854231039,7.7033237030865,-52.2075929896733));
#63659=CARTESIAN_POINT('Ctrl Pts',(1.77888708044802,7.70843644332623,-52.2066985082712));
#63660=CARTESIAN_POINT('Ctrl Pts',(1.52487292395613,7.76629193975539,-52.1964233911832));
#63661=CARTESIAN_POINT('Ctrl Pts',(1.2906175486389,7.80863919253579,-52.1874074763967));
#63662=CARTESIAN_POINT('Ctrl Pts',(0.905913718999365,7.86039491587526,-52.1731863518083));
#63663=CARTESIAN_POINT('Ctrl Pts',(0.756488696690766,7.87618022622692,-52.1678032308911));
#63664=CARTESIAN_POINT('Ctrl Pts',(0.0764748867062996,7.92848507510148,
-52.1437663093828));
#63665=CARTESIAN_POINT('Ctrl Pts',(-0.456480890272077,7.91570058333451,
-52.126304291775));
#63666=CARTESIAN_POINT('Ctrl Pts',(-1.31263247889229,7.80836343996087,-52.0961333439424));
#63667=CARTESIAN_POINT('Ctrl Pts',(-1.6382144281175,7.74659630279577,-52.0841136890893));
#63668=CARTESIAN_POINT('Ctrl Pts',(-1.97184319933447,7.66132710062903,-52.0703347168536));
#63669=CARTESIAN_POINT('Ctrl Pts',(-1.98474433396213,7.65799506876364,-52.0697995648192));
#63670=CARTESIAN_POINT('Ctrl Pts',(-2.00328121652762,7.65315747865286,-52.0690272416492));
#63671=CARTESIAN_POINT('Ctrl Pts',(-2.00892368045347,7.65167829115342,-52.0687917033403));
#63672=CARTESIAN_POINT('Ctrl Pts',(-2.01873496751384,7.64909463465776,-52.0683813656391));
#63673=CARTESIAN_POINT('Ctrl Pts',(-2.02290453985602,7.64799299303434,-52.0682067373896));
#63674=CARTESIAN_POINT('Ctrl Pts',(-2.03093525397468,7.64586417337647,-52.0678699308539));
#63675=CARTESIAN_POINT('Ctrl Pts',(-2.03479652357463,7.64483747839677,-52.0677077816061));
#63676=CARTESIAN_POINT('Ctrl Pts',(-2.04391325595666,7.64240598211994,-52.0673244462228));
#63677=CARTESIAN_POINT('Ctrl Pts',(-2.04916804469141,7.64099868588791,-52.0671031114254));
#63678=CARTESIAN_POINT('Ctrl Pts',(-2.06743480624309,7.63608642685687,-52.0663323780964));
#63679=CARTESIAN_POINT('Ctrl Pts',(-2.08043920847536,7.63255365471261,-52.0657813388633));
#63680=CARTESIAN_POINT('Ctrl Pts',(-2.23229172628981,7.59088452323878,-52.0593199823909));
#63681=CARTESIAN_POINT('Ctrl Pts',(-2.37007545257036,7.54899940413262,-52.0531947498979));
#63682=CARTESIAN_POINT('Ctrl Pts',(-2.60168303749548,7.47162696093144,-52.0425393809127));
#63683=CARTESIAN_POINT('Ctrl Pts',(-2.69611990071184,7.4380710128333,-52.0380911567544));
#63684=CARTESIAN_POINT('Ctrl Pts',(-3.45070691149286,7.15368739651151,-52.0018452066305));
#63685=CARTESIAN_POINT('Ctrl Pts',(-4.07522237928604,6.81728234884755,-51.9678085769398));
#63686=CARTESIAN_POINT('Ctrl Pts',(-4.86606314810196,6.24329487968668,-51.9241099679494));
#63687=CARTESIAN_POINT('Ctrl Pts',(-5.07698861820723,6.07301462714687,-51.9123412604108));
#63688=CARTESIAN_POINT('Ctrl Pts',(-5.36790319137211,5.81238811973075,-51.8959905922589));
#63689=CARTESIAN_POINT('Ctrl Pts',(-5.45520950872661,5.73052625856688,-51.8910653468149));
#63690=CARTESIAN_POINT('Ctrl Pts',(-5.55393232665606,5.63365814943078,-51.8854702522365));
#63691=CARTESIAN_POINT('Ctrl Pts',(-5.56719075829702,5.62055651164667,-51.8847182716075));
#63692=CARTESIAN_POINT('Ctrl Pts',(-5.58724444294296,5.60059940547699,-51.8835799927851));
#63693=CARTESIAN_POINT('Ctrl Pts',(-5.59407361410657,5.59377820141565,-51.8831922002885));
#63694=CARTESIAN_POINT('Ctrl Pts',(-5.60635820195487,5.58146294950753,-51.8824943321489));
#63695=CARTESIAN_POINT('Ctrl Pts',(-5.61181806386953,5.57597336469755,-51.8821840617384));
#63696=CARTESIAN_POINT('Ctrl Pts',(-5.62354035283546,5.56415260406781,-51.8815176846796));
#63697=CARTESIAN_POINT('Ctrl Pts',(-5.62980016955799,5.55781884850796,-51.8811616920667));
#63698=CARTESIAN_POINT('Ctrl Pts',(-5.64671302372387,5.54064833293842,-51.8801994769993));
#63699=CARTESIAN_POINT('Ctrl Pts',(-5.65734557731959,5.52979140145784,-51.8795941442827));
#63700=CARTESIAN_POINT('Ctrl Pts',(-5.70475215607721,5.48110456544492,-51.8768932397982));
#63701=CARTESIAN_POINT('Ctrl Pts',(-5.74117887027941,5.44293760141292,-51.8748126271556));
#63702=CARTESIAN_POINT('Ctrl Pts',(-6.33560021263209,4.80751123021564,-51.8407604969326));
#63703=CARTESIAN_POINT('Ctrl Pts',(-6.79806115087063,4.12775191221742,-51.8134309984279));
#63704=CARTESIAN_POINT('Ctrl Pts',(-7.23260456860779,3.21125255831868,-51.777802732156));
#63705=CARTESIAN_POINT('Ctrl Pts',(-7.31030530489373,3.03020515981736,-51.7707841542783));
#63706=CARTESIAN_POINT('Ctrl Pts',(-7.44795201078235,2.67327214306416,-51.7566918276523));
#63707=CARTESIAN_POINT('Ctrl Pts',(-7.50861251308763,2.49782109226252,-51.7496330668647));
#63708=CARTESIAN_POINT('Ctrl Pts',(-7.57372968107876,2.28557750604726,-51.7408475337281));
#63709=CARTESIAN_POINT('Ctrl Pts',(-7.58416520886395,2.25070741097705,-51.7393975943091));
#63710=CARTESIAN_POINT('Ctrl Pts',(-7.59775409898043,2.20413260282507,-51.7374531962301));
#63711=CARTESIAN_POINT('Ctrl Pts',(-7.60112182798788,2.19249055497184,-51.7369665211825));
#63712=CARTESIAN_POINT('Ctrl Pts',(-7.60662724639801,2.17329348730776,-51.7361630022699));
#63713=CARTESIAN_POINT('Ctrl Pts',(-7.60878047072409,2.16574291998235,-51.7358467036186));
#63714=CARTESIAN_POINT('Ctrl Pts',(-7.61294566986035,2.15105421337129,-51.7352308919514));
#63715=CARTESIAN_POINT('Ctrl Pts',(-7.61495885539926,2.1439164235754,-51.734931420812));
#63716=CARTESIAN_POINT('Ctrl Pts',(-7.61960567029669,2.12735192858325,-51.7342359362108));
#63717=CARTESIAN_POINT('Ctrl Pts',(-7.62223184562949,2.11792315474802,-51.7338396731333));
#63718=CARTESIAN_POINT('Ctrl Pts',(-7.62928334386571,2.09242312355431,-51.7327669858963));
#63719=CARTESIAN_POINT('Ctrl Pts',(-7.63367536873292,2.07634275334951,-51.7320894775174));
#63720=CARTESIAN_POINT('Ctrl Pts',(-7.66635511477985,1.95518823359428,-51.7269773494542));
#63721=CARTESIAN_POINT('Ctrl Pts',(-7.69252247064552,1.84955637934844,-51.7224775718625));
#63722=CARTESIAN_POINT('Ctrl Pts',(-7.84562356914092,1.17192027586025,-51.6934449805958));
#63723=CARTESIAN_POINT('Ctrl Pts',(-7.91085769820133,0.587841411826712,
-51.6678539456649));
#63724=CARTESIAN_POINT('Ctrl Pts',(-7.91115880092942,-0.653968790779282,
-51.6149583235055));
#63725=CARTESIAN_POINT('Ctrl Pts',(-7.82975041299619,-1.30734903275606,
-51.5878788503464));
#63726=CARTESIAN_POINT('Ctrl Pts',(-7.6496804303836,-2.01798571026065,-51.5580644153787));
#63727=CARTESIAN_POINT('Ctrl Pts',(-7.62963011481745,-2.09251558247885,
-51.5549362491295));
#63728=CARTESIAN_POINT('Ctrl Pts',(-7.6005735868381,-2.19454735098087,-51.550652001369));
#63729=CARTESIAN_POINT('Ctrl Pts',(-7.59250239519923,-2.22231057938892,
-51.5494860538214));
#63730=CARTESIAN_POINT('Ctrl Pts',(-7.57839448709955,-2.2698647724461,-51.5474886053196));
#63731=CARTESIAN_POINT('Ctrl Pts',(-7.5724320021874,-2.28967741449144,-51.5466562954138));
#63732=CARTESIAN_POINT('Ctrl Pts',(-7.55999145597246,-2.33043576655436,
-51.5449438326371));
#63733=CARTESIAN_POINT('Ctrl Pts',(-7.55350390798825,-2.35137840253406,
-51.5440637943952));
#63734=CARTESIAN_POINT('Ctrl Pts',(-7.5382003007495,-2.40006345208207,-51.5420176321078));
#63735=CARTESIAN_POINT('Ctrl Pts',(-7.52931800349152,-2.42778474308957,
-51.5408522814545));
#63736=CARTESIAN_POINT('Ctrl Pts',(-7.50026087280275,-2.51677750164869,
-51.5371101786234));
#63737=CARTESIAN_POINT('Ctrl Pts',(-7.47948948210573,-2.57785168889583,
-51.5345405042055));
#63738=CARTESIAN_POINT('Ctrl Pts',(-7.37101298124165,-2.88445171254307,
-51.5216288181685));
#63739=CARTESIAN_POINT('Ctrl Pts',(-7.27195434326239,-3.12579253703037,
-51.5114336306219));
#63740=CARTESIAN_POINT('Ctrl Pts',(-7.01490772950438,-3.6733409917938,-51.4879998169136));
#63741=CARTESIAN_POINT('Ctrl Pts',(-6.84848470130402,-3.97499954234526,
-51.4748631892665));
#63742=CARTESIAN_POINT('Ctrl Pts',(-6.52197142381995,-4.48510793736571,
-51.4514962852165));
#63743=CARTESIAN_POINT('Ctrl Pts',(-6.37016410401951,-4.69822368477,-51.4413349417497));
#63744=CARTESIAN_POINT('Ctrl Pts',(-6.19175974097778,-4.92409649654297,
-51.4298292383923));
#63745=CARTESIAN_POINT('Ctrl Pts',(-6.1753281031961,-4.94468783739816,-51.4287732418327));
#63746=CARTESIAN_POINT('Ctrl Pts',(-6.15047299402803,-4.97551793445031,
-51.4271810477261));
#63747=CARTESIAN_POINT('Ctrl Pts',(-6.14212613181137,-4.98581822227533,
-51.4266472283091));
#63748=CARTESIAN_POINT('Ctrl Pts',(-6.12684693887751,-5.00457662380944,
-51.4256716831409));
#63749=CARTESIAN_POINT('Ctrl Pts',(-6.11992287945425,-5.01304144653195,
-51.4252302012787));
#63750=CARTESIAN_POINT('Ctrl Pts',(-6.10489343052953,-5.03133775023564,
-51.4242732490831));
#63751=CARTESIAN_POINT('Ctrl Pts',(-6.0967817992794,-5.04116405661127,-51.4237576010309));
#63752=CARTESIAN_POINT('Ctrl Pts',(-6.07426441811411,-5.06830742799209,
-51.4223285501622));
#63753=CARTESIAN_POINT('Ctrl Pts',(-6.0598084250752,-5.08558258707628,-51.4214137625465));
#63754=CARTESIAN_POINT('Ctrl Pts',(-5.97859906784162,-5.18179126208211,
-51.41629010409));
#63755=CARTESIAN_POINT('Ctrl Pts',(-5.91037810030055,-5.25947123228704,
-51.41204351051));
#63756=CARTESIAN_POINT('Ctrl Pts',(-5.59255185305285,-5.60736972679043,
-51.3925595134165));
#63757=CARTESIAN_POINT('Ctrl Pts',(-5.32581065192357,-5.86131114711035,
-51.3770407265267));
#63758=CARTESIAN_POINT('Ctrl Pts',(-4.70553156696177,-6.3744013776366,-51.3432766963854));
#63759=CARTESIAN_POINT('Ctrl Pts',(-4.34616362434512,-6.62464381515314,
-51.3251420144015));
#63760=CARTESIAN_POINT('Ctrl Pts',(-3.92260981431283,-6.87021111458166,
-51.3052716912954));
#63761=CARTESIAN_POINT('Ctrl Pts',(-3.87700297907093,-6.8960507872474,-51.3031498256281));
#63762=CARTESIAN_POINT('Ctrl Pts',(-3.80216552578969,-6.93747470193981,
-51.2996959001553));
#63763=CARTESIAN_POINT('Ctrl Pts',(-3.77308801813951,-6.95333191672927,
-51.2983606902068));
#63764=CARTESIAN_POINT('Ctrl Pts',(-3.72082538975083,-6.98140861285222,
-51.2959726885243));
#63765=CARTESIAN_POINT('Ctrl Pts',(-3.69767753350805,-6.99369635202022,
-51.2949191349702));
#63766=CARTESIAN_POINT('Ctrl Pts',(-3.64832019010333,-7.01958350917208,
-51.2926812591103));
#63767=CARTESIAN_POINT('Ctrl Pts',(-3.62209474538898,-7.0331516772173,-51.2914972974356));
#63768=CARTESIAN_POINT('Ctrl Pts',(-3.55097434433926,-7.06944368949022,
-51.2882999583313));
#63769=CARTESIAN_POINT('Ctrl Pts',(-3.50593745475715,-7.09188659467569,
-51.2862896332745));
#63770=CARTESIAN_POINT('Ctrl Pts',(-3.26474904857026,-7.2092172209269,-51.2755962495039));
#63771=CARTESIAN_POINT('Ctrl Pts',(-3.06495174181175,-7.29640128959952,
-51.2669867264147));
#63772=CARTESIAN_POINT('Ctrl Pts',(-2.59334614902039,-7.47939846638989,
-51.2471211487817));
#63773=CARTESIAN_POINT('Ctrl Pts',(-2.31938973368994,-7.56883640588344,
-51.2359588529723));
#63774=CARTESIAN_POINT('Ctrl Pts',(-1.28385742608788,-7.84538349478491,
-51.1950867690578));
#63775=CARTESIAN_POINT('Ctrl Pts',(-0.50079728503031,-7.9339326311962,-51.1673286297828));
#63776=CARTESIAN_POINT('Ctrl Pts',(0.350595666864294,-7.90352210794903,
-51.1339748743647));
#63777=CARTESIAN_POINT('Ctrl Pts',(0.418766487416467,-7.90020337423685,
-51.1312774087229));
#63778=CARTESIAN_POINT('Ctrl Pts',(0.50028633030346,-7.89517668427529,-51.1280118677253));
#63779=CARTESIAN_POINT('Ctrl Pts',(0.513685846673798,-7.89431619182426,
-51.1274738154278));
#63780=CARTESIAN_POINT('Ctrl Pts',(0.535509064584842,-7.89285894691583,
-51.1265953265743));
#63781=CARTESIAN_POINT('Ctrl Pts',(0.543934145133511,-7.89228281039404,
-51.1262556458331));
#63782=CARTESIAN_POINT('Ctrl Pts',(0.558954867062194,-7.89123147454816,
-51.1256490738963));
#63783=CARTESIAN_POINT('Ctrl Pts',(0.565550873262386,-7.89076149289352,
-51.1253823782969));
#63784=CARTESIAN_POINT('Ctrl Pts',(0.579452283226118,-7.88975346319276,
-51.1248195884137));
#63785=CARTESIAN_POINT('Ctrl Pts',(0.586757541634805,-7.88921353782308,
-51.1245234228963));
#63786=CARTESIAN_POINT('Ctrl Pts',(0.606045453088392,-7.88776104643983,
-51.1237403412208));
#63787=CARTESIAN_POINT('Ctrl Pts',(0.618026767350007,-7.8868313237754,-51.1232527603647));
#63788=CARTESIAN_POINT('Ctrl Pts',(0.672205628635941,-7.88250295136452,
-51.1210426027769));
#63789=CARTESIAN_POINT('Ctrl Pts',(0.714377071824375,-7.87879295867929,
-51.1193076118357));
#63790=CARTESIAN_POINT('Ctrl Pts',(1.02485158869387,-7.84896609050352,-51.1064140820309));
#63791=CARTESIAN_POINT('Ctrl Pts',(1.29165694320329,-7.80949245402892,-51.0946222498107));
#63792=CARTESIAN_POINT('Ctrl Pts',(1.80780471731166,-7.70595724358861,-51.0709642130253));
#63793=CARTESIAN_POINT('Ctrl Pts',(2.05710147070141,-7.64318405877536,-51.0591459303334));
#63794=CARTESIAN_POINT('Ctrl Pts',(2.62007621950843,-7.47188328610893,-51.0320449107439));
#63795=CARTESIAN_POINT('Ctrl Pts',(2.93088805981931,-7.35552511223655,-51.0167873922339));
#63796=CARTESIAN_POINT('Ctrl Pts',(3.61514140498033,-7.04908125357026,-50.983205550084));
#63797=CARTESIAN_POINT('Ctrl Pts',(3.98266857793027,-6.84815377889291,-50.9651943943171));
#63798=CARTESIAN_POINT('Ctrl Pts',(4.35605752954808,-6.603746543205,-50.9470512397213));
#63799=CARTESIAN_POINT('Ctrl Pts',(4.37941254673051,-6.5882813671881,-50.9459168771084));
#63800=CARTESIAN_POINT('Ctrl Pts',(4.41165501386604,-6.56668391198242,-50.9443514196605));
#63801=CARTESIAN_POINT('Ctrl Pts',(4.42061265601532,-6.56065707897303,-50.943916563782));
#63802=CARTESIAN_POINT('Ctrl Pts',(4.43598542116435,-6.55026827868145,-50.943170379889));
#63803=CARTESIAN_POINT('Ctrl Pts',(4.44240650607878,-6.54591518541474,-50.9428587345088));
#63804=CARTESIAN_POINT('Ctrl Pts',(4.45561412152811,-6.53693286536937,-50.9422177654212));
#63805=CARTESIAN_POINT('Ctrl Pts',(4.46239986687624,-6.53230249719979,-50.9418884832708));
#63806=CARTESIAN_POINT('Ctrl Pts',(4.47812364828313,-6.52153717433555,-50.9411255475665));
#63807=CARTESIAN_POINT('Ctrl Pts',(4.48705631977775,-6.51539439403655,-50.940692176628));
#63808=CARTESIAN_POINT('Ctrl Pts',(4.51526295771662,-6.49591185710497,-50.9393238758649));
#63809=CARTESIAN_POINT('Ctrl Pts',(4.53449035493805,-6.48250473698929,-50.9383913821458));
#63810=CARTESIAN_POINT('Ctrl Pts',(4.8412070250609,-6.26660117227177,-50.9235190035972));
#63811=CARTESIAN_POINT('Ctrl Pts',(5.11495265432941,-6.0452349940009,-50.9103086314897));
#63812=CARTESIAN_POINT('Ctrl Pts',(6.00115951643161,-5.22515986270115,-50.8666751865921));
#63813=CARTESIAN_POINT('Ctrl Pts',(6.53068747688535,-4.5459855468661,-50.8394422880699));
#63814=CARTESIAN_POINT('Ctrl Pts',(6.9901067209013,-3.70577236652726,-50.8028310642281));
#63815=CARTESIAN_POINT('Ctrl Pts',(7.03733979483702,-3.6152716995536,-50.7988462732997));
#63816=CARTESIAN_POINT('Ctrl Pts',(7.08923850508311,-3.51095809404536,-50.7941875172756));
#63817=CARTESIAN_POINT('Ctrl Pts',(7.09563227369168,-3.49801828933242,-50.7936085765508));
#63818=CARTESIAN_POINT('Ctrl Pts',(7.10511799575358,-3.47868792290354,-50.7927422542781));
#63819=CARTESIAN_POINT('Ctrl Pts',(7.10823684082791,-3.47231052942442,-50.7924562042512));
#63820=CARTESIAN_POINT('Ctrl Pts',(7.11378826614767,-3.46092018855829,-50.7919448941995));
#63821=CARTESIAN_POINT('Ctrl Pts',(7.11622414549413,-3.45590884688926,-50.7917197945082));
#63822=CARTESIAN_POINT('Ctrl Pts',(7.1213525220973,-3.44532981075189,-50.7912443127918));
#63823=CARTESIAN_POINT('Ctrl Pts',(7.12404378802492,-3.43976152586636,-50.7909938721382));
#63824=CARTESIAN_POINT('Ctrl Pts',(7.13114405624069,-3.42502684826846,-50.7903307220744));
#63825=CARTESIAN_POINT('Ctrl Pts',(7.13554190529191,-3.41585511675836,-50.7899174893364));
#63826=CARTESIAN_POINT('Ctrl Pts',(7.15544462876395,-3.37414174649278,-50.7880361381745));
#63827=CARTESIAN_POINT('Ctrl Pts',(7.17074451252823,-3.34150317067397,-50.78655868445));
#63828=CARTESIAN_POINT('Ctrl Pts',(7.29108978723452,-3.08014267467658,-50.7746912762179));
#63829=CARTESIAN_POINT('Ctrl Pts',(7.38538420009903,-2.84663972505008,-50.7638726948913));
#63830=CARTESIAN_POINT('Ctrl Pts',(7.62286631188374,-2.1668498815343,-50.7324654800523));
#63831=CARTESIAN_POINT('Ctrl Pts',(7.73777630141721,-1.71177553406259,-50.7116101036829));
#63832=CARTESIAN_POINT('Ctrl Pts',(7.87134101354573,-0.8765501012583,-50.6751467221012));
#63833=CARTESIAN_POINT('Ctrl Pts',(7.90419477168064,-0.500086066636779,
-50.6593350359073));
#63834=CARTESIAN_POINT('Ctrl Pts',(7.91065019298988,-0.0839022222059317,
-50.6424664431928));
#63835=CARTESIAN_POINT('Ctrl Pts',(7.91096652669874,-0.0451076997346217,
-50.6408994828876));
#63836=CARTESIAN_POINT('Ctrl Pts',(7.91101205126465,0.0119475677737271,
-50.6386024496337));
#63837=CARTESIAN_POINT('Ctrl Pts',(7.91096340131129,0.0302073834516963,
-50.637868442496));
#63838=CARTESIAN_POINT('Ctrl Pts',(7.91076565430058,0.0624839856616776,
-50.6365729156257));
#63839=CARTESIAN_POINT('Ctrl Pts',(7.91064252193986,0.0765008317092797,
-50.6360109458787));
#63840=CARTESIAN_POINT('Ctrl Pts',(7.91031238700873,0.105351961879948,-50.6348555163186));
#63841=CARTESIAN_POINT('Ctrl Pts',(7.91010090888753,0.120186142443491,-50.6342621355591));
#63842=CARTESIAN_POINT('Ctrl Pts',(7.90945614677868,0.157958195428076,-50.6327529375033));
#63843=CARTESIAN_POINT('Ctrl Pts',(7.90896480859124,0.180894974566873,-50.6318381032264));
#63844=CARTESIAN_POINT('Ctrl Pts',(7.90666199048649,0.270241996525144,-50.6282804268825));
#63845=CARTESIAN_POINT('Ctrl Pts',(7.90411374765819,0.336631249599331,-50.6256494706157));
#63846=CARTESIAN_POINT('Ctrl Pts',(7.88373632351083,0.736145225041601,-50.6098890953637));
#63847=CARTESIAN_POINT('Ctrl Pts',(7.84568628200952,1.06790943464732,-50.5971220975674));
#63848=CARTESIAN_POINT('Ctrl Pts',(7.65787819692602,2.11527191240606,-50.5572287282404));
#63849=CARTESIAN_POINT('Ctrl Pts',(7.43001352765958,2.81286287181111,-50.5315422631011));
#63850=CARTESIAN_POINT('Ctrl Pts',(7.0783016175668,3.53365356080735,-50.5001301446837));
#63851=CARTESIAN_POINT('Ctrl Pts',(7.04598689262584,3.59765612791403,-50.497292467389));
#63852=CARTESIAN_POINT('Ctrl Pts',(7.00663198479293,3.67303788120783,-50.4938843704703));
#63853=CARTESIAN_POINT('Ctrl Pts',(7.00042675450575,3.68485064815832,-50.4933483627922));
#63854=CARTESIAN_POINT('Ctrl Pts',(6.9903300437204,3.70395399206473,-50.4924783275316));
#63855=CARTESIAN_POINT('Ctrl Pts',(6.98645695910169,3.71125429651992,-50.4921450825857));
#63856=CARTESIAN_POINT('Ctrl Pts',(6.97956877002564,3.72418871952677,-50.4915532785027));
#63857=CARTESIAN_POINT('Ctrl Pts',(6.97655826112576,3.72982528585153,-50.4912949188243));
#63858=CARTESIAN_POINT('Ctrl Pts',(6.97023740806948,3.74162537175719,-50.4907530647431));
#63859=CARTESIAN_POINT('Ctrl Pts',(6.96692571159675,3.74778815784844,-50.4904695109031));
#63860=CARTESIAN_POINT('Ctrl Pts',(6.95824751850061,3.76388628704237,-50.4897273390218));
#63861=CARTESIAN_POINT('Ctrl Pts',(6.95286792860482,3.77381452592923,-50.4892681351879));
#63862=CARTESIAN_POINT('Ctrl Pts',(6.92929962532464,3.81708927362661,-50.4872599839791));
#63863=CARTESIAN_POINT('Ctrl Pts',(6.91089233878381,3.85031567933861,-50.4857010032407));
#63864=CARTESIAN_POINT('Ctrl Pts',(6.62758785284108,4.35312262233801,-50.4618323809549));
#63865=CARTESIAN_POINT('Ctrl Pts',(6.31565441203594,4.79446475130553,-50.4369048889312));
#63866=CARTESIAN_POINT('Ctrl Pts',(5.53213177991521,5.69260531977242,-50.3820704303982));
#63867=CARTESIAN_POINT('Ctrl Pts',(5.04357587745989,6.1296689204548,-50.352628476872));
#63868=CARTESIAN_POINT('Ctrl Pts',(4.47382734249726,6.52459952005059,-50.324341785341));
#63869=CARTESIAN_POINT('Ctrl Pts',(4.44068703382505,6.54720006711995,-50.3227148465226));
#63870=CARTESIAN_POINT('Ctrl Pts',(4.39634303016149,6.57694955673791,-50.3205621157626));
#63871=CARTESIAN_POINT('Ctrl Pts',(4.38529146731117,6.58432352332115,-50.3200275904864));
#63872=CARTESIAN_POINT('Ctrl Pts',(4.3680389154279,6.59577228893435,-50.3191962263211));
#63873=CARTESIAN_POINT('Ctrl Pts',(4.36185070641929,6.59986624633198,-50.3188986451421));
#63874=CARTESIAN_POINT('Ctrl Pts',(4.34948272019712,6.60802359008308,-50.3183051143201));
#63875=CARTESIAN_POINT('Ctrl Pts',(4.34330298615006,6.61208702841166,-50.3180091628021));
#63876=CARTESIAN_POINT('Ctrl Pts',(4.32952667154837,6.62111789528892,-50.3173507599687));
#63877=CARTESIAN_POINT('Ctrl Pts',(4.32192721663954,6.62608093202653,-50.3169884786351));
#63878=CARTESIAN_POINT('Ctrl Pts',(4.29982316844608,6.64046239420716,-50.3159373826134));
#63879=CARTESIAN_POINT('Ctrl Pts',(4.28529616837165,6.64984637741067,-50.3152498977376));
#63880=CARTESIAN_POINT('Ctrl Pts',(4.25246038938186,6.67090497130716,-50.3137033619748));
#63881=CARTESIAN_POINT('Ctrl Pts',(4.23413404784577,6.6825520105902,-50.3128453725298));
#63882=CARTESIAN_POINT('Ctrl Pts',(4.17605096460324,6.7191310088871,-50.3101422526924));
#63883=CARTESIAN_POINT('Ctrl Pts',(4.13611989101968,6.74378495497205,-50.3083077447178));
#63884=CARTESIAN_POINT('Ctrl Pts',(3.96935566372673,6.84470888815572,-50.3007429622345));
#63885=CARTESIAN_POINT('Ctrl Pts',(3.84061113646125,6.91776937268805,-50.2951338091314));
#63886=CARTESIAN_POINT('Ctrl Pts',(3.4628219752736,7.11835902720264,-50.2792727371081));
#63887=CARTESIAN_POINT('Ctrl Pts',(3.20896340045187,7.23634842036956,-50.2693503883374));
#63888=CARTESIAN_POINT('Ctrl Pts',(2.18649523964833,7.64716282654438,-50.2313021393824));
#63889=CARTESIAN_POINT('Ctrl Pts',(1.3806450503099,7.83282971056397,-50.2058365755785));
#63890=CARTESIAN_POINT('Ctrl Pts',(0.515590293249944,7.89431093915223,-50.1718655069737));
#63891=CARTESIAN_POINT('Ctrl Pts',(0.470318198440033,7.89713740469457,-50.1700676385573));
#63892=CARTESIAN_POINT('Ctrl Pts',(0.416543549603061,7.9000306719362,-50.1679058752051));
#63893=CARTESIAN_POINT('Ctrl Pts',(0.408061223877586,7.90047335181657,-50.1675641075957));
#63894=CARTESIAN_POINT('Ctrl Pts',(0.394386074585608,7.90116495535142,-50.1670118414062));
#63895=CARTESIAN_POINT('Ctrl Pts',(0.389193672276127,7.90142242337732,-50.1668018527531));
#63896=CARTESIAN_POINT('Ctrl Pts',(0.379944842484468,7.90187189267213,-50.1664272844804));
#63897=CARTESIAN_POINT('Ctrl Pts',(0.375888509097299,7.90206588938216,-50.1662628249936));
#63898=CARTESIAN_POINT('Ctrl Pts',(0.367418333469839,7.90246444421802,-50.1659190279133));
#63899=CARTESIAN_POINT('Ctrl Pts',(0.363004467074932,7.90266842785537,-50.1657396555847));
#63900=CARTESIAN_POINT('Ctrl Pts',(0.351434551364988,7.90319340952089,-50.1652688984083));
#63901=CARTESIAN_POINT('Ctrl Pts',(0.344278247815564,7.90350838549429,-50.1649771462506));
#63902=CARTESIAN_POINT('Ctrl Pts',(0.312250244393492,7.9048744766831,-50.1636688665219));
#63903=CARTESIAN_POINT('Ctrl Pts',(0.287374350005182,7.90581789962738,-50.1626458703736));
#63904=CARTESIAN_POINT('Ctrl Pts',(0.103012979485181,7.91193856015273,-50.1550156939559));
#63905=CARTESIAN_POINT('Ctrl Pts',(-0.0565832717197611,7.91240643719036,
-50.1481420524796));
#63906=CARTESIAN_POINT('Ctrl Pts',(-0.474797623077827,7.90097943838766,
-50.1296390512189));
#63907=CARTESIAN_POINT('Ctrl Pts',(-0.733007093242634,7.8812179796775,-50.117726170947));
#63908=CARTESIAN_POINT('Ctrl Pts',(-1.06788231419738,7.83898890330095,-50.1020280120369));
#63909=CARTESIAN_POINT('Ctrl Pts',(-1.14584356729661,7.82797305084484,-50.0983551795533));
#63910=CARTESIAN_POINT('Ctrl Pts',(-1.46745850095647,7.77762158786638,-50.0831574566117));
#63911=CARTESIAN_POINT('Ctrl Pts',(-1.7093753562552,7.72805751626557,-50.0716215927051));
#63912=CARTESIAN_POINT('Ctrl Pts',(-2.12067099191058,7.62352953502085,-50.0521205553961));
#63913=CARTESIAN_POINT('Ctrl Pts',(-2.29124305111174,7.57401199007608,-50.0440656354579));
#63914=CARTESIAN_POINT('Ctrl Pts',(-2.78182531772033,7.41350256084451,-50.0211054739684));
#63915=CARTESIAN_POINT('Ctrl Pts',(-3.09656993286252,7.28765168696647,-50.0066540517767));
#63916=CARTESIAN_POINT('Ctrl Pts',(-3.42453938820976,7.13141340801815,-49.9919468024326));
#63917=CARTESIAN_POINT('Ctrl Pts',(-3.44671809519011,7.12072058187303,-49.9909538876192));
#63918=CARTESIAN_POINT('Ctrl Pts',(-3.4781623918426,7.10537928727822,-49.9895484531765));
#63919=CARTESIAN_POINT('Ctrl Pts',(-3.4874692029791,7.10081593899745,-49.9891327620558));
#63920=CARTESIAN_POINT('Ctrl Pts',(-3.50333300515518,7.0929988323063,-49.9884246834869));
#63921=CARTESIAN_POINT('Ctrl Pts',(-3.50989448543127,7.08975424691479,-49.9881319538266));
#63922=CARTESIAN_POINT('Ctrl Pts',(-3.52247300259231,7.08351255614379,-49.9875710520813));
#63923=CARTESIAN_POINT('Ctrl Pts',(-3.52849073919045,7.08051688019976,-49.9873028268835));
#63924=CARTESIAN_POINT('Ctrl Pts',(-3.54099465700996,7.07427243353015,-49.9867457398022));
#63925=CARTESIAN_POINT('Ctrl Pts',(-3.54748020415842,7.0710224031796,-49.9864569254204));
#63926=CARTESIAN_POINT('Ctrl Pts',(-3.5700381493954,7.05967934330331,-49.9854528442587));
#63927=CARTESIAN_POINT('Ctrl Pts',(-3.58608745660496,7.05154036915597,-49.9847393006769));
#63928=CARTESIAN_POINT('Ctrl Pts',(-3.72265105237299,6.98169900387593,-49.9786746377811));
#63929=CARTESIAN_POINT('Ctrl Pts',(-3.84159406186037,6.91696532092125,-49.9734388779074));
#63930=CARTESIAN_POINT('Ctrl Pts',(-4.2567869070942,6.67698514880334,-49.9552771346581));
#63931=CARTESIAN_POINT('Ctrl Pts',(-4.54320870177555,6.48549493197682,-49.9429811493431));
#63932=CARTESIAN_POINT('Ctrl Pts',(-5.3770783347942,5.84556995998697,-49.9065470307282));
#63933=CARTESIAN_POINT('Ctrl Pts',(-5.87758571081711,5.34203741898331,-49.8839677383611));
#63934=CARTESIAN_POINT('Ctrl Pts',(-6.35051900834556,4.71811755601942,-49.8538224746301));
#63935=CARTESIAN_POINT('Ctrl Pts',(-6.39565875514631,4.6567449269159,-49.8508337888967));
#63936=CARTESIAN_POINT('Ctrl Pts',(-6.44637085893052,4.58566764327877,-49.8473335936902));
#63937=CARTESIAN_POINT('Ctrl Pts',(-6.45281876227475,4.57658988809689,-49.8468858344942));
#63938=CARTESIAN_POINT('Ctrl Pts',(-6.46238351516107,4.56306364247085,-49.8462175727975));
#63939=CARTESIAN_POINT('Ctrl Pts',(-6.46551492957519,4.55862558206055,-49.8459981402066));
#63940=CARTESIAN_POINT('Ctrl Pts',(-6.471090095203,4.5507067657032,-49.8456063078174));
#63941=CARTESIAN_POINT('Ctrl Pts',(-6.47353561785015,4.54722725316642,-49.845434034498));
#63942=CARTESIAN_POINT('Ctrl Pts',(-6.478683128316,4.53989075859541,-49.8450705852104));
#63943=CARTESIAN_POINT('Ctrl Pts',(-6.48138447942148,4.5360333339643,-49.8448793643845));
#63944=CARTESIAN_POINT('Ctrl Pts',(-6.48850361921426,4.5258481350072,-49.8443741392364));
#63945=CARTESIAN_POINT('Ctrl Pts',(-6.49291558631341,4.51951631769417,-49.8440597282011));
#63946=CARTESIAN_POINT('Ctrl Pts',(-6.51273126346036,4.49098902297851,-49.8426417448845));
#63947=CARTESIAN_POINT('Ctrl Pts',(-6.52803031447734,4.46872141601819,-49.8415309910108));
#63948=CARTESIAN_POINT('Ctrl Pts',(-6.64140116739109,4.30188671240078,-49.8331824512981));
#63949=CARTESIAN_POINT('Ctrl Pts',(-6.73476871017237,4.15419325531452,-49.8256444414951));
#63950=CARTESIAN_POINT('Ctrl Pts',(-7.30785402088005,3.17749382740418,-49.7754643099273));
#63951=CARTESIAN_POINT('Ctrl Pts',(-7.63858723699549,2.27022401886193,-49.7284877914644));
#63952=CARTESIAN_POINT('Ctrl Pts',(-7.80633479458858,1.28331654043723,-49.6857447098148));
#63953=CARTESIAN_POINT('Ctrl Pts',(-7.813184502083,1.24093202099951,-49.6839219044292));
#63954=CARTESIAN_POINT('Ctrl Pts',(-7.84171190431721,1.05480215838642,-49.6759735533229));
#63955=CARTESIAN_POINT('Ctrl Pts',(-7.8597708115176,0.91052674374437,-49.6699605067032));
#63956=CARTESIAN_POINT('Ctrl Pts',(-7.8757113327133,0.746635079015344,-49.6632905931188));
#63957=CARTESIAN_POINT('Ctrl Pts',(-7.87750810772939,0.727433128841045,
-49.6625116059943));
#63958=CARTESIAN_POINT('Ctrl Pts',(-7.88012320654811,0.698339287697318,
-49.6613350352185));
#63959=CARTESIAN_POINT('Ctrl Pts',(-7.88099315503344,0.688452178677763,
-49.6609358439442));
#63960=CARTESIAN_POINT('Ctrl Pts',(-7.88247453774052,0.671245197680348,
-49.6602422357563));
#63961=CARTESIAN_POINT('Ctrl Pts',(-7.88309438760575,0.663926072716579,
-49.6599475572496));
#63962=CARTESIAN_POINT('Ctrl Pts',(-7.88432197881017,0.649186693958512,
-49.659354836624));
#63963=CARTESIAN_POINT('Ctrl Pts',(-7.88492944083915,0.641766423669323,
-49.6590568034539));
#63964=CARTESIAN_POINT('Ctrl Pts',(-7.88614962268587,0.626598381449461,
-49.658448317774));
#63965=CARTESIAN_POINT('Ctrl Pts',(-7.88676140196441,0.61885054087986,-49.658137894759));
#63966=CARTESIAN_POINT('Ctrl Pts',(-7.88815103450292,0.600914847350158,
-49.6574201896538));
#63967=CARTESIAN_POINT('Ctrl Pts',(-7.88892057080252,0.590726354119546,
-49.6570131656898));
#63968=CARTESIAN_POINT('Ctrl Pts',(-7.89085908622961,0.564381324933235,
-49.655962426544));
#63969=CARTESIAN_POINT('Ctrl Pts',(-7.89199818678615,0.548222602932063,
-49.6553196358621));
#63970=CARTESIAN_POINT('Ctrl Pts',(-7.90502435428461,0.354980115724583,
-49.647652334971));
#63971=CARTESIAN_POINT('Ctrl Pts',(-7.91099882920443,0.177544359459989,
-49.6408130228063));
#63972=CARTESIAN_POINT('Ctrl Pts',(-7.91099999982794,5.21758335036288E-5,
-49.6341351303446));
#63973=CARTESIAN_POINT('',(-7.92228552985236,-0.00797182984248199,-47.642334701651));
#63974=CARTESIAN_POINT('Ctrl Pts',(-7.89680882399629,-0.000256294892049957,
-49.6423315082368));
#63975=CARTESIAN_POINT('Ctrl Pts',(-7.90103566610738,-1.00262630581715,
-49.6020840516645));
#63976=CARTESIAN_POINT('Ctrl Pts',(-7.49007435790851,-3.32159447341453,
-49.508915328115));
#63977=CARTESIAN_POINT('Ctrl Pts',(-5.25514852513718,-6.34001891784867,
-49.3628253375884));
#63978=CARTESIAN_POINT('Ctrl Pts',(-1.58860116256843,-8.09809403774528,
-49.2040615366568));
#63979=CARTESIAN_POINT('Ctrl Pts',(2.4623766104365,-7.85805627968503,-49.0452977357255));
#63980=CARTESIAN_POINT('Ctrl Pts',(7.12803414838975,-5.02805760499318,-48.8336126678165));
#63981=CARTESIAN_POINT('Ctrl Pts',(8.69862114564058,0.679830947526981,-48.621927599908));
#63982=CARTESIAN_POINT('Ctrl Pts',(6.13163661536245,5.48447080059073,-48.4102425319994));
#63983=CARTESIAN_POINT('Ctrl Pts',(1.66597412306723,8.5573936163116,-48.1985574640906));
#63984=CARTESIAN_POINT('Ctrl Pts',(-5.44962191887428,7.46990471586691,-47.9425881873078));
#63985=CARTESIAN_POINT('Ctrl Pts',(-7.90759395183775,2.39848959991299,-47.7395401775023));
#63986=CARTESIAN_POINT('Ctrl Pts',(-7.92228552985236,-0.007971829842482,
-47.642334701651));
#63987=CARTESIAN_POINT('',(-7.91099978972198,-0.00182401173648303,-43.6333998034544));
#63988=CARTESIAN_POINT('Ctrl Pts',(-7.91099573933849,-0.00821049135054118,
-47.6488343437815));
#63989=CARTESIAN_POINT('Ctrl Pts',(-7.91081080808585,-0.186395972497414,
-47.6423568197832));
#63990=CARTESIAN_POINT('Ctrl Pts',(-7.90460580372303,-0.364516329474105,
-47.635666846442));
#63991=CARTESIAN_POINT('Ctrl Pts',(-7.8903646074285,-0.571789395021273,
-47.6274730261266));
#63992=CARTESIAN_POINT('Ctrl Pts',(-7.88817050756462,-0.601300880753049,
-47.6262966852719));
#63993=CARTESIAN_POINT('Ctrl Pts',(-7.8851863919924,-0.638606221840542,
-47.6247965949078));
#63994=CARTESIAN_POINT('Ctrl Pts',(-7.8845502874544,-0.646412490263166,
-47.624481969626));
#63995=CARTESIAN_POINT('Ctrl Pts',(-7.88347754936708,-0.659339931389938,
-47.6239597245305));
#63996=CARTESIAN_POINT('Ctrl Pts',(-7.88304751993685,-0.66446159759016,
-47.6237525038514));
#63997=CARTESIAN_POINT('Ctrl Pts',(-7.88226742940965,-0.673645153490175,
-47.6233803807103));
#63998=CARTESIAN_POINT('Ctrl Pts',(-7.88191921859132,-0.67770720302512,
-47.623215587559));
#63999=CARTESIAN_POINT('Ctrl Pts',(-7.88120989304127,-0.685907337785932,
-47.6228825223307));
#64000=CARTESIAN_POINT('Ctrl Pts',(-7.88084865890561,-0.690045411185815,
-47.6227142432993));
#64001=CARTESIAN_POINT('Ctrl Pts',(-7.88011861584145,-0.698332982660445,
-47.6223768171713));
#64002=CARTESIAN_POINT('Ctrl Pts',(-7.87974978808002,-0.702482477736017,
-47.6222076690253));
#64003=CARTESIAN_POINT('Ctrl Pts',(-7.87872074563448,-0.713956933812933,
-47.6217393726878));
#64004=CARTESIAN_POINT('Ctrl Pts',(-7.87805359497069,-0.721281252424524,
-47.6214398244835));
#64005=CARTESIAN_POINT('Ctrl Pts',(-7.8753969433784,-0.750003887355095,
-47.620262699611));
#64006=CARTESIAN_POINT('Ctrl Pts',(-7.87333048123411,-0.771394816526295,
-47.6193807477432));
#64007=CARTESIAN_POINT('Ctrl Pts',(-7.86512809104895,-0.852833197753838,
-47.6160035217687));
#64008=CARTESIAN_POINT('Ctrl Pts',(-7.85839228578871,-0.912816892416241,
-47.6134755989487));
#64009=CARTESIAN_POINT('Ctrl Pts',(-7.83628256849354,-1.09126848847356,
-47.6058461731687));
#64010=CARTESIAN_POINT('Ctrl Pts',(-7.81891140243297,-1.20946830906336,
-47.6006494970985));
#64011=CARTESIAN_POINT('Ctrl Pts',(-7.79426482707434,-1.3542934530718,-47.5941418230878));
#64012=CARTESIAN_POINT('Ctrl Pts',(-7.78951731860821,-1.38133807281919,
-47.5929205191432));
#64013=CARTESIAN_POINT('Ctrl Pts',(-7.63534153071512,-2.23353758484971,
-47.5542556795445));
#64014=CARTESIAN_POINT('Ctrl Pts',(-7.35580726828862,-3.02978797298011,
-47.5134615717166));
#64015=CARTESIAN_POINT('Ctrl Pts',(-6.86664322150951,-3.93301634601935,
-47.4685807219584));
#64016=CARTESIAN_POINT('Ctrl Pts',(-6.77104338455511,-4.09541018667361,
-47.4605383077332));
#64017=CARTESIAN_POINT('Ctrl Pts',(-6.61702076499226,-4.33688426368195,
-47.4486262081206));
#64018=CARTESIAN_POINT('Ctrl Pts',(-6.56277672367486,-4.41853952181064,
-47.4446061716372));
#64019=CARTESIAN_POINT('Ctrl Pts',(-6.49697339058278,-4.51370915209901,
-47.4399277741486));
#64020=CARTESIAN_POINT('Ctrl Pts',(-6.48687016831328,-4.52821697496735,
-47.4392147809419));
#64021=CARTESIAN_POINT('Ctrl Pts',(-6.47129255251722,-4.55042668129623,
-47.4381235369378));
#64022=CARTESIAN_POINT('Ctrl Pts',(-6.46585288223967,-4.55815278244807,
-47.4377439741418));
#64023=CARTESIAN_POINT('Ctrl Pts',(-6.45633306360225,-4.57162268894201,
-47.4370823130549));
#64024=CARTESIAN_POINT('Ctrl Pts',(-6.45225906547943,-4.57737081636275,
-47.4367999821844));
#64025=CARTESIAN_POINT('Ctrl Pts',(-6.44306803429431,-4.59030206919125,
-47.4361648916574));
#64026=CARTESIAN_POINT('Ctrl Pts',(-6.43794665357822,-4.59748210081245,
-47.4358122975664));
#64027=CARTESIAN_POINT('Ctrl Pts',(-6.42419174187811,-4.61669804771272,
-47.4348687419172));
#64028=CARTESIAN_POINT('Ctrl Pts',(-6.41553637799922,-4.62871833078726,
-47.4342786114712));
#64029=CARTESIAN_POINT('Ctrl Pts',(-6.37787985757637,-4.68070592600241,
-47.4317266687814));
#64030=CARTESIAN_POINT('Ctrl Pts',(-6.34853831978792,-4.72042590827255,
-47.4297778602427));
#64031=CARTESIAN_POINT('Ctrl Pts',(-5.78363054813279,-5.47035288388846,
-47.3929902536307));
#64032=CARTESIAN_POINT('Ctrl Pts',(-5.13253035028886,-6.08540461357812,
-47.3638063292011));
#64033=CARTESIAN_POINT('Ctrl Pts',(-4.12004779212685,-6.76141255821326,
-47.3205103034668));
#64034=CARTESIAN_POINT('Ctrl Pts',(-3.83621882830373,-6.92639346719417,
-47.3084042144463));
#64035=CARTESIAN_POINT('Ctrl Pts',(-3.5191600522768,-7.08520584512437,-47.29430595933));
#64036=CARTESIAN_POINT('Ctrl Pts',(-3.49530382824877,-7.09700503516655,
-47.2932428822244));
#64037=CARTESIAN_POINT('Ctrl Pts',(-3.46176248589624,-7.11338430371735,
-47.2917453936115));
#64038=CARTESIAN_POINT('Ctrl Pts',(-3.45212676686707,-7.11806550583347,
-47.2913148711693));
#64039=CARTESIAN_POINT('Ctrl Pts',(-3.4363443899559,-7.12569327834722,-47.2906092133009));
#64040=CARTESIAN_POINT('Ctrl Pts',(-3.43020336326552,-7.12865150991296,
-47.2903345126682));
#64041=CARTESIAN_POINT('Ctrl Pts',(-3.41744693800903,-7.13477618540431,
-47.2897636427108));
#64042=CARTESIAN_POINT('Ctrl Pts',(-3.41083094528969,-7.13794137354602,
-47.2894674278895));
#64043=CARTESIAN_POINT('Ctrl Pts',(-3.39516850316283,-7.14540776819984,
-47.2887658653787));
#64044=CARTESIAN_POINT('Ctrl Pts',(-3.38611827691685,-7.14970099741707,
-47.2883602333194));
#64045=CARTESIAN_POINT('Ctrl Pts',(-3.35692769239853,-7.16348051522755,
-47.2870511537397));
#64046=CARTESIAN_POINT('Ctrl Pts',(-3.33675551858699,-7.17289894135313,
-47.2861453579588));
#64047=CARTESIAN_POINT('Ctrl Pts',(-3.03983713260541,-7.31000713769421,
-47.2727980296533));
#64048=CARTESIAN_POINT('Ctrl Pts',(-2.7559863766488,-7.42168037881745,-47.2598626832925));
#64049=CARTESIAN_POINT('Ctrl Pts',(-2.16861771682077,-7.61441065150595,
-47.2333759346065));
#64050=CARTESIAN_POINT('Ctrl Pts',(-1.86527609733113,-7.69434205688113,
-47.2198429762008));
#64051=CARTESIAN_POINT('Ctrl Pts',(-0.923671471035601,-7.88348589578352,
-47.1787512640205));
#64052=CARTESIAN_POINT('Ctrl Pts',(-0.276099562582266,-7.93261210645452,
-47.1519016549248));
#64053=CARTESIAN_POINT('Ctrl Pts',(0.464415530699387,-7.89791944996969,
-47.1215697064018));
#64054=CARTESIAN_POINT('Ctrl Pts',(0.558525976136821,-7.89182250038105,
-47.1177241621843));
#64055=CARTESIAN_POINT('Ctrl Pts',(0.7198357008134,-7.87847205841443,-47.1111503518853));
#64056=CARTESIAN_POINT('Ctrl Pts',(0.787092112245193,-7.87203731649334,
-47.1084147241325));
#64057=CARTESIAN_POINT('Ctrl Pts',(0.883689393133947,-7.86154504356056,
-47.104493167488));
#64058=CARTESIAN_POINT('Ctrl Pts',(0.913102494607912,-7.85818307614163,
-47.1033000828654));
#64059=CARTESIAN_POINT('Ctrl Pts',(0.964340771219736,-7.8520348914912,-47.1012234006919));
#64060=CARTESIAN_POINT('Ctrl Pts',(0.986174450426143,-7.84932258332225,
-47.1003390218964));
#64061=CARTESIAN_POINT('Ctrl Pts',(1.0283692298457,-7.8439020660569,-47.0986309237827));
#64062=CARTESIAN_POINT('Ctrl Pts',(1.04873165403313,-7.84120557156168,-47.0978070835589));
#64063=CARTESIAN_POINT('Ctrl Pts',(1.10269476887119,-7.83384554274431,-47.0956249690934));
#64064=CARTESIAN_POINT('Ctrl Pts',(1.13627641701961,-7.82904513066987,-47.094268229384));
#64065=CARTESIAN_POINT('Ctrl Pts',(1.25648721952042,-7.81107155794474,-47.0894155843942));
#64066=CARTESIAN_POINT('Ctrl Pts',(1.34292752780436,-7.79667524624111,-47.0859337405068));
#64067=CARTESIAN_POINT('Ctrl Pts',(2.16096770243014,-7.64642543890663,-47.0530341839737));
#64068=CARTESIAN_POINT('Ctrl Pts',(2.87016735658576,-7.40943125419746,-47.0252880528389));
#64069=CARTESIAN_POINT('Ctrl Pts',(3.62380988329656,-7.03289481278728,-46.9921599443215));
#64070=CARTESIAN_POINT('Ctrl Pts',(3.71102301907194,-6.98726807143252,-46.9882599576255));
#64071=CARTESIAN_POINT('Ctrl Pts',(3.8153274110473,-6.93019604263933,-46.9834971434339));
#64072=CARTESIAN_POINT('Ctrl Pts',(3.83325561713376,-6.92029564493929,-46.9826749058896));
#64073=CARTESIAN_POINT('Ctrl Pts',(3.86178547296399,-6.9043958705667,-46.9813605919302));
#64074=CARTESIAN_POINT('Ctrl Pts',(3.87241194497495,-6.89844149818201,-46.9808697612837));
#64075=CARTESIAN_POINT('Ctrl Pts',(3.89261357290445,-6.88706045449287,-46.9799342336741));
#64076=CARTESIAN_POINT('Ctrl Pts',(3.9021912446441,-6.88163829484771,-46.9794896545158));
#64077=CARTESIAN_POINT('Ctrl Pts',(3.92357562209219,-6.86947306601572,-46.9784947249004));
#64078=CARTESIAN_POINT('Ctrl Pts',(3.93537631378454,-6.86271951446659,-46.9779441114432));
#64079=CARTESIAN_POINT('Ctrl Pts',(3.97028834699748,-6.842619651787,-46.9763105342148));
#64080=CARTESIAN_POINT('Ctrl Pts',(3.99334955875609,-6.82918681448292,-46.9752254787562));
#64081=CARTESIAN_POINT('Ctrl Pts',(4.16325696793383,-6.72906319468068,-46.967188022899));
#64082=CARTESIAN_POINT('Ctrl Pts',(4.3073314793589,-6.63776268406193,-46.9601343609143));
#64083=CARTESIAN_POINT('Ctrl Pts',(4.92806501999091,-6.21567699823795,-46.9288527910563));
#64084=CARTESIAN_POINT('Ctrl Pts',(5.37047476700102,-5.83767934230883,-46.9042852855195));
#64085=CARTESIAN_POINT('Ctrl Pts',(5.84435346736302,-5.33292045592954,-46.8757833709088));
#64086=CARTESIAN_POINT('Ctrl Pts',(5.91939567274526,-5.24950124830275,-46.8711886540498));
#64087=CARTESIAN_POINT('Ctrl Pts',(6.04659681284652,-5.1019035124837,-46.8632516007834));
#64088=CARTESIAN_POINT('Ctrl Pts',(6.09957053243825,-5.03845134620229,-46.8598984971033));
#64089=CARTESIAN_POINT('Ctrl Pts',(6.17409083206231,-4.94629251480734,-46.8551093434953));
#64090=CARTESIAN_POINT('Ctrl Pts',(6.19645126950599,-4.91825161247471,-46.8536626455808));
#64091=CARTESIAN_POINT('Ctrl Pts',(6.23504857306082,-4.86916796154105,-46.8511481318721));
#64092=CARTESIAN_POINT('Ctrl Pts',(6.25137148204905,-4.84819367860421,-46.8500792305038));
#64093=CARTESIAN_POINT('Ctrl Pts',(6.28273945739343,-4.80746528436973,-46.8480142252346));
#64094=CARTESIAN_POINT('Ctrl Pts',(6.29779782106404,-4.78772181308015,-46.8470179657835));
#64095=CARTESIAN_POINT('Ctrl Pts',(6.33349818969855,-4.74045412693079,-46.8446439943562));
#64096=CARTESIAN_POINT('Ctrl Pts',(6.35405410991627,-4.71286547954811,-46.8432673366394));
#64097=CARTESIAN_POINT('Ctrl Pts',(6.42853642956144,-4.61152764706807,-46.8382424324697));
#64098=CARTESIAN_POINT('Ctrl Pts',(6.48136439604962,-4.53697957074589,-46.8346070219429));
#64099=CARTESIAN_POINT('Ctrl Pts',(6.87038007757268,-3.96735549623886,-46.8072495586798));
#64100=CARTESIAN_POINT('Ctrl Pts',(7.15072881016182,-3.43644921757755,-46.7840798838598));
#64101=CARTESIAN_POINT('Ctrl Pts',(7.53228906133853,-2.45988228830297,-46.744736981882));
#64102=CARTESIAN_POINT('Ctrl Pts',(7.65998412699178,-2.02756667580617,-46.728284660055));
#64103=CARTESIAN_POINT('Ctrl Pts',(7.78362586869896,-1.42365861976096,-46.7050306428745));
#64104=CARTESIAN_POINT('Ctrl Pts',(7.81185973333916,-1.25955550757048,-46.6986766141416));
#64105=CARTESIAN_POINT('Ctrl Pts',(7.84550096603101,-1.0187788924089,-46.6891790795465));
#64106=CARTESIAN_POINT('Ctrl Pts',(7.85500315086523,-0.942719952492079,
-46.686153475079));
#64107=CARTESIAN_POINT('Ctrl Pts',(7.8649920554046,-0.852075482128857,-46.6825066092279));
#64108=CARTESIAN_POINT('Ctrl Pts',(7.86654573419024,-0.837610212058618,
-46.6819233907563));
#64109=CARTESIAN_POINT('Ctrl Pts',(7.86886823925142,-0.815410355033859,
-46.6810263205606));
#64110=CARTESIAN_POINT('Ctrl Pts',(7.86966558769957,-0.807678742472628,
-46.6807135223358));
#64111=CARTESIAN_POINT('Ctrl Pts',(7.87110179489947,-0.793548289435133,
-46.6801411466819));
#64112=CARTESIAN_POINT('Ctrl Pts',(7.87174424893307,-0.78714981573849,-46.6798817048132));
#64113=CARTESIAN_POINT('Ctrl Pts',(7.87311112089516,-0.773367521752226,
-46.6793222917062));
#64114=CARTESIAN_POINT('Ctrl Pts',(7.87383295423602,-0.765983455415304,
-46.6790222219281));
#64115=CARTESIAN_POINT('Ctrl Pts',(7.87574848486042,-0.746099507689448,
-46.6782132068987));
#64116=CARTESIAN_POINT('Ctrl Pts',(7.87692280772485,-0.733597812768984,
-46.6777035081889));
#64117=CARTESIAN_POINT('Ctrl Pts',(7.88212990727205,-0.676709371332206,
-46.6753792036738));
#64118=CARTESIAN_POINT('Ctrl Pts',(7.88581724566145,-0.632292416603385,
-46.6735507708098));
#64119=CARTESIAN_POINT('Ctrl Pts',(7.94899980271243,0.21564088930325,-46.6383480578211));
#64120=CARTESIAN_POINT('Ctrl Pts',(7.88577226059548,1.02348818189203,-46.5996498958108));
#64121=CARTESIAN_POINT('Ctrl Pts',(7.66032504632049,1.98395773844054,-46.5551195563703));
#64122=CARTESIAN_POINT('Ctrl Pts',(7.61293865587728,2.15866566095496,-46.5470608666512));
#64123=CARTESIAN_POINT('Ctrl Pts',(7.50084403057775,2.52210296041095,-46.530443748767));
#64124=CARTESIAN_POINT('Ctrl Pts',(7.43490532711301,2.71032365760512,-46.5219241720325));
#64125=CARTESIAN_POINT('Ctrl Pts',(7.32417347436791,2.99182865848988,-46.5093293312852));
#64126=CARTESIAN_POINT('Ctrl Pts',(7.28455027390585,3.08705103926472,-46.5050948076135));
#64127=CARTESIAN_POINT('Ctrl Pts',(7.23566449572441,3.19834643441602,-46.5001740420391));
#64128=CARTESIAN_POINT('Ctrl Pts',(7.22819436232519,3.21519313189428,-46.4994299632057));
#64129=CARTESIAN_POINT('Ctrl Pts',(7.21664936332346,3.24098589887956,-46.4982919185032));
#64130=CARTESIAN_POINT('Ctrl Pts',(7.21261659934645,3.24995067986846,-46.4978965844961));
#64131=CARTESIAN_POINT('Ctrl Pts',(7.2055511563716,3.26557914219114,-46.4972077632018));
#64132=CARTESIAN_POINT('Ctrl Pts',(7.20252592075397,3.27224616467548,-46.4969140337519));
#64133=CARTESIAN_POINT('Ctrl Pts',(7.19569727936826,3.28723979374393,-46.4962537217343));
#64134=CARTESIAN_POINT('Ctrl Pts',(7.19188866460989,3.29556402371873,-46.4958873097886));
#64135=CARTESIAN_POINT('Ctrl Pts',(7.18165521225326,3.31782835847886,-46.4949077723015));
#64136=CARTESIAN_POINT('Ctrl Pts',(7.1752042238846,3.33175643659699,-46.4942955032666));
#64137=CARTESIAN_POINT('Ctrl Pts',(7.14715713228492,3.39185256104063,-46.4916558585567));
#64138=CARTESIAN_POINT('Ctrl Pts',(7.12515545689423,3.4378305224918,-46.4896418166548));
#64139=CARTESIAN_POINT('Ctrl Pts',(6.66393456249095,4.37821547257291,-46.4485501715703));
#64140=CARTESIAN_POINT('Ctrl Pts',(6.06019181408714,5.18175372986905,-46.4166301706448));
#64141=CARTESIAN_POINT('Ctrl Pts',(5.13946478140763,6.01926165108473,-46.3717855922758));
#64142=CARTESIAN_POINT('Ctrl Pts',(4.94797626957656,6.1776309287007,-46.3625450263026));
#64143=CARTESIAN_POINT('Ctrl Pts',(4.7208296306728,6.34814636189649,-46.35133239936));
#64144=CARTESIAN_POINT('Ctrl Pts',(4.69214489657217,6.36937758141047,-46.3499118253417));
#64145=CARTESIAN_POINT('Ctrl Pts',(4.65513844145907,6.39638254203304,-46.3480740719181));
#64146=CARTESIAN_POINT('Ctrl Pts',(4.64694745986555,6.40233573291896,-46.3476669938368));
#64147=CARTESIAN_POINT('Ctrl Pts',(4.63374358944189,6.41189359471545,-46.3470103137547));
#64148=CARTESIAN_POINT('Ctrl Pts',(4.62873785281334,6.41550816477266,-46.3467612505415));
#64149=CARTESIAN_POINT('Ctrl Pts',(4.61920492860361,6.42237478654887,-46.3462867366303));
#64150=CARTESIAN_POINT('Ctrl Pts',(4.6146785233206,6.42562792242978,-46.3460613440979));
#64151=CARTESIAN_POINT('Ctrl Pts',(4.60436453730023,6.43302408424657,-46.3455475730646));
#64152=CARTESIAN_POINT('Ctrl Pts',(4.5985748008839,6.43716408529797,-46.3452590358056));
#64153=CARTESIAN_POINT('Ctrl Pts',(4.58134054206066,6.44945247375808,-46.3443997738154));
#64154=CARTESIAN_POINT('Ctrl Pts',(4.56987992981583,6.45757816810056,-46.343827881491));
#64155=CARTESIAN_POINT('Ctrl Pts',(4.48993862549141,6.51393800106107,-46.3398356821975));
#64156=CARTESIAN_POINT('Ctrl Pts',(4.42071877357429,6.56111133929279,-46.3363632941156));
#64157=CARTESIAN_POINT('Ctrl Pts',(4.02135508916013,6.82408867567449,-46.3162983662107));
#64158=CARTESIAN_POINT('Ctrl Pts',(3.67619450692529,7.01605725040587,-46.2988732920287));
#64159=CARTESIAN_POINT('Ctrl Pts',(2.98172504576119,7.33693393827933,-46.2651941957141));
#64160=CARTESIAN_POINT('Ctrl Pts',(2.63475557387146,7.46855871800295,-46.2489737479029));
#64161=CARTESIAN_POINT('Ctrl Pts',(2.03455713219143,7.64918971749609,-46.2223375073545));
#64162=CARTESIAN_POINT('Ctrl Pts',(1.78584145007397,7.71105092273632,-46.2116837921155));
#64163=CARTESIAN_POINT('Ctrl Pts',(1.48087482201751,7.77135282386084,-46.1990382743033));
#64164=CARTESIAN_POINT('Ctrl Pts',(1.42708803839516,7.78140956215893,-46.196823183032));
#64165=CARTESIAN_POINT('Ctrl Pts',(1.35263810591344,7.79453187276956,-46.1937768138725));
#64166=CARTESIAN_POINT('Ctrl Pts',(1.33206106015131,7.7980747815172,-46.1929369040217));
#64167=CARTESIAN_POINT('Ctrl Pts',(1.29727163054062,7.80392302704917,-46.1915202710039));
#64168=CARTESIAN_POINT('Ctrl Pts',(1.28306657425787,7.80627109848949,-46.1909427928282));
#64169=CARTESIAN_POINT('Ctrl Pts',(1.25489896044459,7.81084819450168,-46.1897995461573));
#64170=CARTESIAN_POINT('Ctrl Pts',(1.24093668106705,7.81307859128018,-46.1892337557156));
#64171=CARTESIAN_POINT('Ctrl Pts',(1.21005885675839,7.81792629448048,-46.1879844455336));
#64172=CARTESIAN_POINT('Ctrl Pts',(1.19314063463265,7.82052615949026,-46.1873012269771));
#64173=CARTESIAN_POINT('Ctrl Pts',(1.13390901955557,7.82943174889413,-46.1849136198153));
#64174=CARTESIAN_POINT('Ctrl Pts',(1.0915527382616,7.83544917886948,-46.1832139959015));
#64175=CARTESIAN_POINT('Ctrl Pts',(0.66942373535693,7.89193043690149,-46.1663490122429));
#64176=CARTESIAN_POINT('Ctrl Pts',(0.286498496674969,7.91508913926764,-46.1516800474058));
#64177=CARTESIAN_POINT('Ctrl Pts',(-0.491860302685967,7.90558271175945,
-46.1225543993435));
#64178=CARTESIAN_POINT('Ctrl Pts',(-0.886187022359869,7.87113954983068,
-46.1081597352916));
#64179=CARTESIAN_POINT('Ctrl Pts',(-1.55499311477938,7.76180846047775,-46.0831269836869));
#64180=CARTESIAN_POINT('Ctrl Pts',(-1.83105045775446,7.70135808951158,-46.0725983276471));
#64181=CARTESIAN_POINT('Ctrl Pts',(-2.20519709555398,7.59817120309017,-46.0575479044527));
#64182=CARTESIAN_POINT('Ctrl Pts',(-2.30654569286578,7.56802125350935,-46.0533895694548));
#64183=CARTESIAN_POINT('Ctrl Pts',(-2.42195202978884,7.53115577779498,-46.0485357448582));
#64184=CARTESIAN_POINT('Ctrl Pts',(-2.4366333785046,7.52641858779002,-46.0479160475372));
#64185=CARTESIAN_POINT('Ctrl Pts',(-2.45880955982573,7.51919137406076,-46.0469765296921));
#64186=CARTESIAN_POINT('Ctrl Pts',(-2.46631472108787,7.5167330049173,-46.0466579642458));
#64187=CARTESIAN_POINT('Ctrl Pts',(-2.47979216542416,7.5122960138325,-46.0460848009101));
#64188=CARTESIAN_POINT('Ctrl Pts',(-2.48576579941761,7.51032149600094,-46.0458303688146));
#64189=CARTESIAN_POINT('Ctrl Pts',(-2.49856054540299,7.50607539854739,-46.0452845671158));
#64190=CARTESIAN_POINT('Ctrl Pts',(-2.50538092557005,7.50380164350481,-46.0449931086137));
#64191=CARTESIAN_POINT('Ctrl Pts',(-2.52372411924307,7.49765865563016,-46.0442078407993));
#64192=CARTESIAN_POINT('Ctrl Pts',(-2.5352411020684,7.49377216751113,-46.0437133140088));
#64193=CARTESIAN_POINT('Ctrl Pts',(-2.58572074934318,7.4766077602358,-46.0415390939463));
#64194=CARTESIAN_POINT('Ctrl Pts',(-2.62458791699199,7.46305256368384,-46.0398475636577));
#64195=CARTESIAN_POINT('Ctrl Pts',(-3.43318739480252,7.17395004562452,-46.0042635044944));
#64196=CARTESIAN_POINT('Ctrl Pts',(-4.15562220808074,6.78107312963025,-45.9647341281851));
#64197=CARTESIAN_POINT('Ctrl Pts',(-5.11796982472318,6.04528758692267,-45.9105894038012));
#64198=CARTESIAN_POINT('Ctrl Pts',(-5.41263985942702,5.78294955417933,-45.8936601956213));
#64199=CARTESIAN_POINT('Ctrl Pts',(-5.70263496842228,5.48310220251716,-45.8767599997803));
#64200=CARTESIAN_POINT('Ctrl Pts',(-5.71863232259236,5.46641561880391,-45.8758267317313));
#64201=CARTESIAN_POINT('Ctrl Pts',(-5.74163308798811,5.44221241912649,-45.8744834321203));
#64202=CARTESIAN_POINT('Ctrl Pts',(-5.74869528104079,5.43475198134925,-45.8740707825273));
#64203=CARTESIAN_POINT('Ctrl Pts',(-5.76096829275034,5.42173619272754,-45.8733533060573));
#64204=CARTESIAN_POINT('Ctrl Pts',(-5.76618564892686,5.4161870422041,-45.8730481888646));
#64205=CARTESIAN_POINT('Ctrl Pts',(-5.77623138959779,5.40547148161288,-45.8724604832198));
#64206=CARTESIAN_POINT('Ctrl Pts',(-5.78106087508253,5.40030611758432,-45.8721778460438));
#64207=CARTESIAN_POINT('Ctrl Pts',(-5.79246602286586,5.38807493810376,-45.8715101455475));
#64208=CARTESIAN_POINT('Ctrl Pts',(-5.79903569988085,5.38100354182154,-45.871125347038));
#64209=CARTESIAN_POINT('Ctrl Pts',(-5.82192938116851,5.35627087370684,-45.8697837650972));
#64210=CARTESIAN_POINT('Ctrl Pts',(-5.83818585476969,5.33854711794419,-45.8688299599811));
#64211=CARTESIAN_POINT('Ctrl Pts',(-6.03442265878631,5.12262994648761,-45.8573015188262));
#64212=CARTESIAN_POINT('Ctrl Pts',(-6.20431871039024,4.915489818738,-45.8471776854424));
#64213=CARTESIAN_POINT('Ctrl Pts',(-6.70320704563663,4.24005511599285,-45.8165993517304));
#64214=CARTESIAN_POINT('Ctrl Pts',(-6.99213411407292,3.7444796510817,-45.7976890116023));
#64215=CARTESIAN_POINT('Ctrl Pts',(-7.4197574403165,2.78559736458829,-45.7622219736168));
#64216=CARTESIAN_POINT('Ctrl Pts',(-7.57444341709705,2.33239309061962,-45.7457952744723));
#64217=CARTESIAN_POINT('Ctrl Pts',(-7.69588628559903,1.83264405283303,-45.725533234582));
#64218=CARTESIAN_POINT('Ctrl Pts',(-7.70424944171213,1.79716176283651,-45.7240831241887));
#64219=CARTESIAN_POINT('Ctrl Pts',(-7.71420897086044,1.7535590614912,-45.7222857213359));
#64220=CARTESIAN_POINT('Ctrl Pts',(-7.7160383554138,1.745491771679,-45.7219525229698));
#64221=CARTESIAN_POINT('Ctrl Pts',(-7.71888447954771,1.73284891466236,-45.7214293107346));
#64222=CARTESIAN_POINT('Ctrl Pts',(-7.7199098161388,1.728275267469,-45.7212398234076));
#64223=CARTESIAN_POINT('Ctrl Pts',(-7.72171924607018,1.72017033160128,-45.7209036553157));
#64224=CARTESIAN_POINT('Ctrl Pts',(-7.72250498409914,1.7166394074838,-45.7207570760731));
#64225=CARTESIAN_POINT('Ctrl Pts',(-7.72430599307227,1.70851983071402,-45.7204197131408));
#64226=CARTESIAN_POINT('Ctrl Pts',(-7.72531959673453,1.70393081281934,-45.7202288258396));
#64227=CARTESIAN_POINT('Ctrl Pts',(-7.72810193807077,1.69128044639467,-45.7197020124517));
#64228=CARTESIAN_POINT('Ctrl Pts',(-7.72986214199745,1.68321727006244,-45.7193655572016));
#64229=CARTESIAN_POINT('Ctrl Pts',(-7.73866554974908,1.6425854122323,-45.7176667741155));
#64230=CARTESIAN_POINT('Ctrl Pts',(-7.74551545103198,1.60997567013182,-45.7162926430861));
#64231=CARTESIAN_POINT('Ctrl Pts',(-7.85712288276098,1.06145267070195,-45.6930111743576));
#64232=CARTESIAN_POINT('Ctrl Pts',(-7.91032359295643,0.536430839407822,
-45.6683285380629));
#64233=CARTESIAN_POINT('Ctrl Pts',(-7.91131182240876,-0.239937634875093,
-45.6320774332878));
#64234=CARTESIAN_POINT('Ctrl Pts',(-7.89977858925934,-0.489826479416971,
-45.620431413072));
#64235=CARTESIAN_POINT('Ctrl Pts',(-7.85216932097601,-0.997424927092319,
-45.5971534571454));
#64236=CARTESIAN_POINT('Ctrl Pts',(-7.81517914549196,-1.25475508284187,
-45.5855548581645));
#64237=CARTESIAN_POINT('Ctrl Pts',(-7.72747818539019,-1.70583678516334,
-45.5657374871808));
#64238=CARTESIAN_POINT('Ctrl Pts',(-7.68195679462964,-1.90035426354798,
-45.5573629996407));
#64239=CARTESIAN_POINT('Ctrl Pts',(-7.61990714418702,-2.12653445498801,
-45.5478264935644));
#64240=CARTESIAN_POINT('Ctrl Pts',(-7.61047244758596,-2.16005621277204,
-45.5464182765945));
#64241=CARTESIAN_POINT('Ctrl Pts',(-7.59742428039041,-2.20526982254841,
-45.5445257369249));
#64242=CARTESIAN_POINT('Ctrl Pts',(-7.59400465629136,-2.21701690760492,
-45.5440346561769));
#64243=CARTESIAN_POINT('Ctrl Pts',(-7.58858210884531,-2.2354846801254,-45.5432635960282));
#64244=CARTESIAN_POINT('Ctrl Pts',(-7.58659748428991,-2.24221069248022,
-45.5429829776822));
#64245=CARTESIAN_POINT('Ctrl Pts',(-7.58276179317837,-2.2551466865685,-45.5424436604605));
#64246=CARTESIAN_POINT('Ctrl Pts',(-7.58091203544779,-2.26135704856781,
-45.5421849160937));
#64247=CARTESIAN_POINT('Ctrl Pts',(-7.57653585646197,-2.27598388290856,
-45.5415759191349));
#64248=CARTESIAN_POINT('Ctrl Pts',(-7.57400303562984,-2.28439844083197,
-45.5412258907679));
#64249=CARTESIAN_POINT('Ctrl Pts',(-7.56659878752784,-2.30884921084181,
-45.54020970256));
#64250=CARTESIAN_POINT('Ctrl Pts',(-7.56169039969263,-2.32487423181379,
-45.5395448373039));
#64251=CARTESIAN_POINT('Ctrl Pts',(-7.52679158624773,-2.43753295128165,
-45.5348786373005));
#64252=CARTESIAN_POINT('Ctrl Pts',(-7.4949999812168,-2.5336011430177,-45.5309408457111));
#64253=CARTESIAN_POINT('Ctrl Pts',(-7.39020687791995,-2.83101076822703,
-45.5188618106794));
#64254=CARTESIAN_POINT('Ctrl Pts',(-7.31086629345214,-3.03002004204275,
-45.5109436891407));
#64255=CARTESIAN_POINT('Ctrl Pts',(-6.91431833129005,-3.91807343023484,
-45.4759700650823));
#64256=CARTESIAN_POINT('Ctrl Pts',(-6.50718026558615,-4.56239587239376,
-45.4520390599114));
#64257=CARTESIAN_POINT('Ctrl Pts',(-5.89333776720512,-5.28084843272612,
-45.4174652914252));
#64258=CARTESIAN_POINT('Ctrl Pts',(-5.7670575190648,-5.41847106450267,-45.4103879356583));
#64259=CARTESIAN_POINT('Ctrl Pts',(-5.62634023128691,-5.56133145084387,
-45.4023690535234));
#64260=CARTESIAN_POINT('Ctrl Pts',(-5.6166186990233,-5.57114945892926,-45.4018144041505));
#64261=CARTESIAN_POINT('Ctrl Pts',(-5.60301223786957,-5.584819136508,-45.401037129599));
#64262=CARTESIAN_POINT('Ctrl Pts',(-5.59914904886678,-5.58869223105992,
-45.4008163367014));
#64263=CARTESIAN_POINT('Ctrl Pts',(-5.59245198137082,-5.59539255640104,
-45.4004333996879));
#64264=CARTESIAN_POINT('Ctrl Pts',(-5.58961996430724,-5.59822165322737,
-45.4002714100843));
#64265=CARTESIAN_POINT('Ctrl Pts',(-5.58373667952937,-5.60408995651756,
-45.3999347773274));
#64266=CARTESIAN_POINT('Ctrl Pts',(-5.5806850754036,-5.60712882285447,-45.399760106395));
#64267=CARTESIAN_POINT('Ctrl Pts',(-5.57351947741971,-5.61425286645683,
-45.3993498107253));
#64268=CARTESIAN_POINT('Ctrl Pts',(-5.56940347570227,-5.61833601150611,
-45.3991140213328));
#64269=CARTESIAN_POINT('Ctrl Pts',(-5.55604753505774,-5.6315562370619,-45.3983485650238));
#64270=CARTESIAN_POINT('Ctrl Pts',(-5.54678961246672,-5.6406750353316,-45.3978174365163));
#64271=CARTESIAN_POINT('Ctrl Pts',(-5.31587719976169,-5.86699919123651,
-45.3845575846435));
#64272=CARTESIAN_POINT('Ctrl Pts',(-5.08167441891715,-6.0709783650749,-45.3708316321397));
#64273=CARTESIAN_POINT('Ctrl Pts',(-4.65342953800843,-6.40178167051542,
-45.3461622491373));
#64274=CARTESIAN_POINT('Ctrl Pts',(-4.46464806289698,-6.53483956533783,
-45.3354166971247));
#64275=CARTESIAN_POINT('Ctrl Pts',(-3.95845565660522,-6.85943179932433,
-45.3073755364382));
#64276=CARTESIAN_POINT('Ctrl Pts',(-3.63290975909653,-7.03726989980414,
-45.2901021890545));
#64277=CARTESIAN_POINT('Ctrl Pts',(-2.91856779895789,-7.36466851416871,
-45.2546967839063));
#64278=CARTESIAN_POINT('Ctrl Pts',(-2.52798116618026,-7.50771337743377,
-45.2367807096817));
#64279=CARTESIAN_POINT('Ctrl Pts',(-2.10121423891686,-7.62689902997033,
-45.2187800556535));
#64280=CARTESIAN_POINT('Ctrl Pts',(-2.07446461545123,-7.63421814404193,
-45.217657983075));
#64281=CARTESIAN_POINT('Ctrl Pts',(-2.03751758159717,-7.64411889804656,
-45.216116602081));
#64282=CARTESIAN_POINT('Ctrl Pts',(-2.02735284147749,-7.64682104406813,
-45.2156934219346));
#64283=CARTESIAN_POINT('Ctrl Pts',(-2.00993027837801,-7.65141539399573,
-45.2149695809295));
#64284=CARTESIAN_POINT('Ctrl Pts',(-2.00267510957927,-7.65331755915798,
-45.2146686007973));
#64285=CARTESIAN_POINT('Ctrl Pts',(-1.98854536880815,-7.65700063649053,
-45.2140832912774));
#64286=CARTESIAN_POINT('Ctrl Pts',(-1.98167108286418,-7.65878261545047,
-45.2137989279234));
#64287=CARTESIAN_POINT('Ctrl Pts',(-1.96520804139635,-7.66302657957349,
-45.2131188595991));
#64288=CARTESIAN_POINT('Ctrl Pts',(-1.95561703554585,-7.66547982949513,
-45.2127234342194));
#64289=CARTESIAN_POINT('Ctrl Pts',(-1.92679183894951,-7.67279530569442,
-45.2115372988393));
#64290=CARTESIAN_POINT('Ctrl Pts',(-1.90754387333352,-7.67760320492577,
-45.2107483223068));
#64291=CARTESIAN_POINT('Ctrl Pts',(-1.73649819091085,-7.71964532282843,
-45.2037639917618));
#64292=CARTESIAN_POINT('Ctrl Pts',(-1.58364181847314,-7.75244682354744,
-45.1977109030058));
#64293=CARTESIAN_POINT('Ctrl Pts',(-1.18553483729385,-7.82560946630156,
-45.1823687021595));
#64294=CARTESIAN_POINT('Ctrl Pts',(-0.939173244481577,-7.85898336470746,
-45.1732880575031));
#64295=CARTESIAN_POINT('Ctrl Pts',(0.129995793870823,-7.95281751627099,
-45.1349809229434));
#64296=CARTESIAN_POINT('Ctrl Pts',(0.957828023675432,-7.89599430028632,
-45.1084586478026));
#64297=CARTESIAN_POINT('Ctrl Pts',(1.80848824980824,-7.70166066423514,-45.0741234542654));
#64298=CARTESIAN_POINT('Ctrl Pts',(1.85499876553423,-7.6905907571515,-45.0722250975418));
#64299=CARTESIAN_POINT('Ctrl Pts',(1.91501472248869,-7.67573033532885,-45.0697502989462));
#64300=CARTESIAN_POINT('Ctrl Pts',(1.92861497835151,-7.67232440857544,-45.0691878026162));
#64301=CARTESIAN_POINT('Ctrl Pts',(1.95022814899501,-7.6668506995021,-45.0682912864331));
#64302=CARTESIAN_POINT('Ctrl Pts',(1.95824703068331,-7.66480645860213,-45.0679580899528));
#64303=CARTESIAN_POINT('Ctrl Pts',(1.97326850842459,-7.66095194522913,-45.0673328667234));
#64304=CARTESIAN_POINT('Ctrl Pts',(1.98027186255802,-7.65914464306761,-45.0670409418176));
#64305=CARTESIAN_POINT('Ctrl Pts',(1.99605121294747,-7.65504949740419,-45.0663822406648));
#64306=CARTESIAN_POINT('Ctrl Pts',(2.00482576667705,-7.65275616343229,-45.0660152804689));
#64307=CARTESIAN_POINT('Ctrl Pts',(2.03070576644008,-7.6459445526041,-45.0649310045302));
#64308=CARTESIAN_POINT('Ctrl Pts',(2.04779996948997,-7.64138399055018,-45.0642123053483));
#64309=CARTESIAN_POINT('Ctrl Pts',(2.18268437504961,-7.6049130649026,-45.0585220147928));
#64310=CARTESIAN_POINT('Ctrl Pts',(2.29973467972043,-7.57033901535893,-45.0534680757386));
#64311=CARTESIAN_POINT('Ctrl Pts',(2.74374870694774,-7.42793905649057,-45.0339382037399));
#64312=CARTESIAN_POINT('Ctrl Pts',(3.06434465874631,-7.30152173758252,-45.019104241431));
#64313=CARTESIAN_POINT('Ctrl Pts',(3.88083126550361,-6.91628902789055,-44.9802681980221));
#64314=CARTESIAN_POINT('Ctrl Pts',(4.35934292189458,-6.6251100900236,-44.9565246107859));
#64315=CARTESIAN_POINT('Ctrl Pts',(4.85946314109944,-6.24296029957444,-44.9304128801675));
#64316=CARTESIAN_POINT('Ctrl Pts',(4.91514953653958,-6.19921288828366,-44.9274828472938));
#64317=CARTESIAN_POINT('Ctrl Pts',(4.98261429184455,-6.14473178792635,-44.9239020125934));
#64318=CARTESIAN_POINT('Ctrl Pts',(4.99495713294828,-6.13470269594719,-44.9232455948541));
#64319=CARTESIAN_POINT('Ctrl Pts',(5.22818074404094,-5.94402794789168,-44.9108170763868));
#64320=CARTESIAN_POINT('Ctrl Pts',(5.4391645057724,-5.75159438011302,-44.8991153935043));
#64321=CARTESIAN_POINT('Ctrl Pts',(5.66981237664644,-5.51715892151711,-44.8857945654762));
#64322=CARTESIAN_POINT('Ctrl Pts',(5.70007731670018,-5.48588493873102,-44.8840354158309));
#64323=CARTESIAN_POINT('Ctrl Pts',(5.74901493522847,-5.43447350553338,-44.881172386596));
#64324=CARTESIAN_POINT('Ctrl Pts',(5.76784347151739,-5.41448582070249,-44.8800662851112));
#64325=CARTESIAN_POINT('Ctrl Pts',(5.80137060070719,-5.37852130513472,-44.8780884452025));
#64326=CARTESIAN_POINT('Ctrl Pts',(5.81610820099359,-5.36258125106156,-44.8772161437571));
#64327=CARTESIAN_POINT('Ctrl Pts',(5.84725222962449,-5.32861674363766,-44.8753665552628));
#64328=CARTESIAN_POINT('Ctrl Pts',(5.86364135858383,-5.31057671634118,-44.8743895303016));
#64329=CARTESIAN_POINT('Ctrl Pts',(5.90739974449084,-5.26196096360556,-44.871770847484));
#64330=CARTESIAN_POINT('Ctrl Pts',(5.93461496046871,-5.23124748199467,-44.8701314969858));
#64331=CARTESIAN_POINT('Ctrl Pts',(6.07004079832293,-5.07599688568197,-44.8619190020448));
#64332=CARTESIAN_POINT('Ctrl Pts',(6.17457707950895,-4.94830668042966,-44.8554023219878));
#64333=CARTESIAN_POINT('Ctrl Pts',(6.46776497958753,-4.56640932576637,-44.8365342983207));
#64334=CARTESIAN_POINT('Ctrl Pts',(6.64524879998031,-4.30403894886653,-44.8243466543364));
#64335=CARTESIAN_POINT('Ctrl Pts',(6.94804926018985,-3.79283938164235,-44.8015130314557));
#64336=CARTESIAN_POINT('Ctrl Pts',(7.07688024818179,-3.54665771125622,-44.7908739850804));
#64337=CARTESIAN_POINT('Ctrl Pts',(7.25457570584618,-3.15868255042331,-44.7742298738312));
#64338=CARTESIAN_POINT('Ctrl Pts',(7.31280706914215,-3.02142269764379,-44.7683624429864));
#64339=CARTESIAN_POINT('Ctrl Pts',(7.3758477494229,-2.86030839469314,-44.7614416826826));
#64340=CARTESIAN_POINT('Ctrl Pts',(7.38446980394693,-2.83797460285967,-44.7604815638511));
#64341=CARTESIAN_POINT('Ctrl Pts',(7.39760687681806,-2.80348029150055,-44.7589972114741));
#64342=CARTESIAN_POINT('Ctrl Pts',(7.40219357857654,-2.79134725043559,-44.7584748396518));
#64343=CARTESIAN_POINT('Ctrl Pts',(7.41020457897124,-2.76999743172974,-44.7575552228572));
#64344=CARTESIAN_POINT('Ctrl Pts',(7.41364157835485,-2.76078543552947,-44.7571582875394));
#64345=CARTESIAN_POINT('Ctrl Pts',(7.42143726232586,-2.7397715677649,-44.7562525233606));
#64346=CARTESIAN_POINT('Ctrl Pts',(7.42578498214266,-2.7279656669084,-44.7557434374359));
#64347=CARTESIAN_POINT('Ctrl Pts',(7.43758749551783,-2.69567955421509,-44.7543506841743));
#64348=CARTESIAN_POINT('Ctrl Pts',(7.44498582980727,-2.67517887250671,-44.7534657433738));
#64349=CARTESIAN_POINT('Ctrl Pts',(7.4834511116676,-2.56719664687747,-44.7488019662596));
#64350=CARTESIAN_POINT('Ctrl Pts',(7.51306077962544,-2.47920480516808,-44.7449927779498));
#64351=CARTESIAN_POINT('Ctrl Pts',(7.59866283024998,-2.20918713104892,-44.7332981265431));
#64352=CARTESIAN_POINT('Ctrl Pts',(7.64963710808998,-2.0256443056373,-44.7253422308271));
#64353=CARTESIAN_POINT('Ctrl Pts',(7.82265265429128,-1.30235638319295,-44.6941556173193));
#64354=CARTESIAN_POINT('Ctrl Pts',(7.8945690814699,-0.752226771582995,-44.6708898658725));
#64355=CARTESIAN_POINT('Ctrl Pts',(7.91122720184627,-0.0905400669992552,
-44.6438350874794));
#64356=CARTESIAN_POINT('Ctrl Pts',(7.91172468266514,0.0180637388576222,
-44.6394200639881));
#64357=CARTESIAN_POINT('Ctrl Pts',(7.90934834411637,0.166485818170939,-44.6334161883937));
#64358=CARTESIAN_POINT('Ctrl Pts',(7.90840944598711,0.206322104156794,-44.6318076789081));
#64359=CARTESIAN_POINT('Ctrl Pts',(7.90640499519587,0.270711909233743,-44.6292120722264));
#64360=CARTESIAN_POINT('Ctrl Pts',(7.90552593140272,0.295270449449205,-44.6282231139418));
#64361=CARTESIAN_POINT('Ctrl Pts',(7.90345141816608,0.3465424911911,-44.6261604067414));
#64362=CARTESIAN_POINT('Ctrl Pts',(7.90223492731764,0.37325484149204,-44.6250868794899));
#64363=CARTESIAN_POINT('Ctrl Pts',(7.89901986948427,0.43676559278134,-44.6225369504241));
#64364=CARTESIAN_POINT('Ctrl Pts',(7.89689955789119,0.47355724942195,-44.6210617538831));
#64365=CARTESIAN_POINT('Ctrl Pts',(7.88873349368569,0.59988103282007,-44.6160025734615));
#64366=CARTESIAN_POINT('Ctrl Pts',(7.88142150774053,0.689324735200001,-44.6124306478669));
#64367=CARTESIAN_POINT('Ctrl Pts',(7.80137745721727,1.49864091254664,-44.5801643225063));
#64368=CARTESIAN_POINT('Ctrl Pts',(7.63172077361449,2.20552977340986,-44.5524402960951));
#64369=CARTESIAN_POINT('Ctrl Pts',(7.18194481785759,3.35646032186492,-44.5064496494739));
#64370=CARTESIAN_POINT('Ctrl Pts',(6.94969292536717,3.81416528856029,-44.4877776552294));
#64371=CARTESIAN_POINT('Ctrl Pts',(6.67321101181492,4.24878633463581,-44.4675680141162));
#64372=CARTESIAN_POINT('Ctrl Pts',(6.6715529056615,4.25138946140321,-44.4674468714398));
#64373=CARTESIAN_POINT('Ctrl Pts',(6.63819046336895,4.3036989038502,-44.4650105307815));
#64374=CARTESIAN_POINT('Ctrl Pts',(6.60593341904417,4.35304954538979,-44.4626757536));
#64375=CARTESIAN_POINT('Ctrl Pts',(6.56602459655137,4.4126414960672,-44.4598069651511));
#64376=CARTESIAN_POINT('Ctrl Pts',(6.55889528270141,4.4232314707251,-44.4592952354856));
#64377=CARTESIAN_POINT('Ctrl Pts',(6.54712137839123,4.44062952499507,-44.4584512847815));
#64378=CARTESIAN_POINT('Ctrl Pts',(6.54249171277528,4.44744770731264,-44.4581197240461));
#64379=CARTESIAN_POINT('Ctrl Pts',(6.53414027003356,4.4597057498507,-44.4575221266501));
#64380=CARTESIAN_POINT('Ctrl Pts',(6.53042232892211,4.46514822254661,-44.4572562637464));
#64381=CARTESIAN_POINT('Ctrl Pts',(6.52248924768152,4.47672988586845,-44.4566893513785));
#64382=CARTESIAN_POINT('Ctrl Pts',(6.51827223386542,4.48286778099488,-44.4563882156077));
#64383=CARTESIAN_POINT('Ctrl Pts',(6.50691866336469,4.49934309663846,-44.4555780258122));
#64384=CARTESIAN_POINT('Ctrl Pts',(6.49976615902982,4.50966946332464,-44.4550682213655));
#64385=CARTESIAN_POINT('Ctrl Pts',(6.46515267481044,4.55938897426312,-44.4526037666466));
#64386=CARTESIAN_POINT('Ctrl Pts',(6.43735839255185,4.59854799986632,-44.4506328965492));
#64387=CARTESIAN_POINT('Ctrl Pts',(6.10443628261212,5.05866449098989,-44.4270913703434));
#64388=CARTESIAN_POINT('Ctrl Pts',(5.75892180876415,5.44875254975246,-44.4031993467315));
#64389=CARTESIAN_POINT('Ctrl Pts',(5.17862629303202,5.98660453099862,-44.3667604549579));
#64390=CARTESIAN_POINT('Ctrl Pts',(4.9701723592034,6.16076274054971,-44.3542610464885));
#64391=CARTESIAN_POINT('Ctrl Pts',(4.37230274434813,6.61013656869777,-44.3204537852897));
#64392=CARTESIAN_POINT('Ctrl Pts',(3.96631509282608,6.86144133614805,-44.2997475536641));
#64393=CARTESIAN_POINT('Ctrl Pts',(3.51378452998848,7.08788454175108,-44.279163188166));
#64394=CARTESIAN_POINT('Ctrl Pts',(3.48736358200873,7.10092136772575,-44.2779696203012));
#64395=CARTESIAN_POINT('Ctrl Pts',(3.45095111220224,7.11863604192004,-44.2763358981831));
#64396=CARTESIAN_POINT('Ctrl Pts',(3.44102187503583,7.1234409615633,-44.2758915424382));
#64397=CARTESIAN_POINT('Ctrl Pts',(3.4240358399727,7.13161697850625,-44.2751333191468));
#64398=CARTESIAN_POINT('Ctrl Pts',(3.4169840464456,7.13499840142198,-44.2748191109533));
#64399=CARTESIAN_POINT('Ctrl Pts',(3.40268787822359,7.14182753716762,-44.2741832646201));
#64400=CARTESIAN_POINT('Ctrl Pts',(3.39544324884939,7.14527469811882,-44.2738616449055));
#64401=CARTESIAN_POINT('Ctrl Pts',(3.37884540730548,7.15314138877483,-44.2731261594983));
#64402=CARTESIAN_POINT('Ctrl Pts',(3.36948873674098,7.1575536091772,-44.2727125347048));
#64403=CARTESIAN_POINT('Ctrl Pts',(3.34986867032473,7.16675862566739,-44.2718472640278));
#64404=CARTESIAN_POINT('Ctrl Pts',(3.3396035769206,7.17154775883957,-44.2713957389301));
#64405=CARTESIAN_POINT('Ctrl Pts',(3.31252508512835,7.18411036074909,-44.2702077416731));
#64406=CARTESIAN_POINT('Ctrl Pts',(3.29569456757509,7.19184687253205,-44.2694724794255));
#64407=CARTESIAN_POINT('Ctrl Pts',(3.24532174250652,7.21478787188485,-44.2672811480845));
#64408=CARTESIAN_POINT('Ctrl Pts',(3.21170008565048,7.22981741486764,-44.2658307732497));
#64409=CARTESIAN_POINT('Ctrl Pts',(3.09291135834524,7.28192614760107,-44.2607486440928));
#64410=CARTESIAN_POINT('Ctrl Pts',(3.00719617425933,7.31774015175861,-44.2571575654721));
#64411=CARTESIAN_POINT('Ctrl Pts',(2.60008434714947,7.47948037006064,-44.240435744412));
#64412=CARTESIAN_POINT('Ctrl Pts',(2.27129058719802,7.58579774742386,-44.2279221395332));
#64413=CARTESIAN_POINT('Ctrl Pts',(1.16965892285502,7.8639361655957,-44.1878651200387));
#64414=CARTESIAN_POINT('Ctrl Pts',(0.378133496479003,7.94142856352877,-44.162259375322));
#64415=CARTESIAN_POINT('Ctrl Pts',(-0.454598790872861,7.89804507163571,
-44.1294837668276));
#64416=CARTESIAN_POINT('Ctrl Pts',(-0.497589125549506,7.89545317889029,
-44.127774030864));
#64417=CARTESIAN_POINT('Ctrl Pts',(-0.551678184800923,7.8917486311373,-44.1256011868434));
#64418=CARTESIAN_POINT('Ctrl Pts',(-0.562798408572342,7.89096339023692,
-44.1251533324544));
#64419=CARTESIAN_POINT('Ctrl Pts',(-0.580369493145021,7.88968529839876,
-44.124443919229));
#64420=CARTESIAN_POINT('Ctrl Pts',(-0.586821501426138,7.88920803258754,
-44.1241830518139));
#64421=CARTESIAN_POINT('Ctrl Pts',(-0.598243105009983,7.88834906871723,
-44.1237205991244));
#64422=CARTESIAN_POINT('Ctrl Pts',(-0.603212944556086,7.88797058729222,
-44.123519154298));
#64423=CARTESIAN_POINT('Ctrl Pts',(-0.614626382982608,7.88709053966962,
-44.1230560289645));
#64424=CARTESIAN_POINT('Ctrl Pts',(-0.621069725854733,7.8865857737598,-44.1227942107449));
#64425=CARTESIAN_POINT('Ctrl Pts',(-0.638898405614348,7.88516710594123,
-44.1220687637841));
#64426=CARTESIAN_POINT('Ctrl Pts',(-0.650282365318184,7.88423644399116,
-44.1216044253024));
#64427=CARTESIAN_POINT('Ctrl Pts',(-0.712264357565476,7.8790341346586,-44.1190702607237));
#64428=CARTESIAN_POINT('Ctrl Pts',(-0.762821681273152,7.87430011727032,
-44.1169814588417));
#64429=CARTESIAN_POINT('Ctrl Pts',(-1.49646675410485,7.79847232987358,-44.0863874625686));
#64430=CARTESIAN_POINT('Ctrl Pts',(-2.16750913615516,7.63921219173083,-44.0551920006656));
#64431=CARTESIAN_POINT('Ctrl Pts',(-3.17779515468966,7.25539122150705,-44.0085019889685));
#64432=CARTESIAN_POINT('Ctrl Pts',(-3.53507699169281,7.08818386040135,-43.9919710119758));
#64433=CARTESIAN_POINT('Ctrl Pts',(-3.8988190290467,6.88358032139274,-43.9750565924681));
#64434=CARTESIAN_POINT('Ctrl Pts',(-3.91915006175604,6.87202522280835,-43.9741107245761));
#64435=CARTESIAN_POINT('Ctrl Pts',(-3.95993679039919,6.84860429791978,-43.9722121322862));
#64436=CARTESIAN_POINT('Ctrl Pts',(-3.98039111488974,6.83673656017006,-43.9712594598489));
#64437=CARTESIAN_POINT('Ctrl Pts',(-4.01435675634706,6.81682536582943,-43.9696764541024));
#64438=CARTESIAN_POINT('Ctrl Pts',(-4.02789781762661,6.80883304306072,-43.9690450823159));
#64439=CARTESIAN_POINT('Ctrl Pts',(-4.05205855090279,6.79447538747914,-43.9679180127365));
#64440=CARTESIAN_POINT('Ctrl Pts',(-4.06268726649798,6.78812540151049,-43.9674220080568));
#64441=CARTESIAN_POINT('Ctrl Pts',(-4.08700758415542,6.77351796708618,-43.9662866037054));
#64442=CARTESIAN_POINT('Ctrl Pts',(-4.10068915796714,6.76524390360077,-43.9656475377697));
#64443=CARTESIAN_POINT('Ctrl Pts',(-4.13839705812951,6.74228327368155,-43.9638851918284));
#64444=CARTESIAN_POINT('Ctrl Pts',(-4.16237024968604,6.72750978214497,-43.9627636250008));
#64445=CARTESIAN_POINT('Ctrl Pts',(-4.28124024249631,6.65337747075567,-43.9571958515007));
#64446=CARTESIAN_POINT('Ctrl Pts',(-4.37494977807241,6.59213659655248,-43.9527859324027));
#64447=CARTESIAN_POINT('Ctrl Pts',(-5.12198473007164,6.08098808972116,-43.9174365848067));
#64448=CARTESIAN_POINT('Ctrl Pts',(-5.70551537586047,5.53716423219042,-43.8891417510623));
#64449=CARTESIAN_POINT('Ctrl Pts',(-6.29481586633187,4.79408964371179,-43.8537172574395));
#64450=CARTESIAN_POINT('Ctrl Pts',(-6.38764087108726,4.66969423305072,-43.8478580062982));
#64451=CARTESIAN_POINT('Ctrl Pts',(-6.49955185713226,4.5101357136543,-43.8403503720539));
#64452=CARTESIAN_POINT('Ctrl Pts',(-6.52211318770562,4.47744771221047,-43.838812688951));
#64453=CARTESIAN_POINT('Ctrl Pts',(-6.59520684119632,4.36982115103825,-43.8337473460104));
#64454=CARTESIAN_POINT('Ctrl Pts',(-6.64470025680236,4.2941876933423,-43.830183890962));
#64455=CARTESIAN_POINT('Ctrl Pts',(-6.70054731093767,4.20556693466053,-43.8259884268985));
#64456=CARTESIAN_POINT('Ctrl Pts',(-6.70817566551772,4.19338845627804,-43.825411441167));
#64457=CARTESIAN_POINT('Ctrl Pts',(-6.72025219105539,4.17399130127671,-43.8244916739843));
#64458=CARTESIAN_POINT('Ctrl Pts',(-6.72472203198342,4.16678610998573,-43.8241498506543));
#64459=CARTESIAN_POINT('Ctrl Pts',(-6.73256880097563,4.15409194320933,-43.8235473040035));
#64460=CARTESIAN_POINT('Ctrl Pts',(-6.73595062620695,4.14860599400494,-43.8232868008956));
#64461=CARTESIAN_POINT('Ctrl Pts',(-6.74290816332254,4.1372886401684,-43.8227491644229));
#64462=CARTESIAN_POINT('Ctrl Pts',(-6.74648302207489,4.13145671931096,-43.8224719926551));
#64463=CARTESIAN_POINT('Ctrl Pts',(-6.75557372088396,4.1165831556833,-43.8217647719074));
#64464=CARTESIAN_POINT('Ctrl Pts',(-6.76107896502204,4.10753507632421,-43.8213342361609));
#64465=CARTESIAN_POINT('Ctrl Pts',(-6.78315011483523,4.0710957042091,-43.8195990017079));
#64466=CARTESIAN_POINT('Ctrl Pts',(-6.79956771423268,4.04361528467046,-43.818287360785));
#64467=CARTESIAN_POINT('Ctrl Pts',(-6.96435157946995,3.76395226766393,-43.8049021163545));
#64468=CARTESIAN_POINT('Ctrl Pts',(-7.09875764317999,3.50387054291138,-43.7920500307316));
#64469=CARTESIAN_POINT('Ctrl Pts',(-7.55182419316041,2.49353953357784,-43.7420414547854));
#64470=CARTESIAN_POINT('Ctrl Pts',(-7.76843741877283,1.70283027448166,-43.7035157770758));
#64471=CARTESIAN_POINT('Ctrl Pts',(-7.8652569248955,0.850573682097738,-43.6675723436489));
#64472=CARTESIAN_POINT('Ctrl Pts',(-7.8697307651614,0.808133555404825,-43.6657947051532));
#64473=CARTESIAN_POINT('Ctrl Pts',(-7.88183650337382,0.68364090430447,-43.6606161618421));
#64474=CARTESIAN_POINT('Ctrl Pts',(-7.88853013505056,0.601501798532957,
-43.6572451382015));
#64475=CARTESIAN_POINT('Ctrl Pts',(-7.89496600620694,0.503663980293447,
-43.6532834618211));
#64476=CARTESIAN_POINT('Ctrl Pts',(-7.89594639005154,0.488053535393955,
-43.6526529784477));
#64477=CARTESIAN_POINT('Ctrl Pts',(-7.89745491676051,0.462838376977011,
-43.6516371759946));
#64478=CARTESIAN_POINT('Ctrl Pts',(-7.89801184716472,0.453235466824881,
-43.6512509281057));
#64479=CARTESIAN_POINT('Ctrl Pts',(-7.89896170445024,0.436323918044981,
-43.6505717811464));
#64480=CARTESIAN_POINT('Ctrl Pts',(-7.89936200502844,0.429015715012015,
-43.6502786440621));
#64481=CARTESIAN_POINT('Ctrl Pts',(-7.90012531107592,0.414716855233308,
-43.6497057922665));
#64482=CARTESIAN_POINT('Ctrl Pts',(-7.90048918131097,0.407726252577871,
-43.649426049842));
#64483=CARTESIAN_POINT('Ctrl Pts',(-7.90124949256747,0.392736052081179,
-43.6488268731163));
#64484=CARTESIAN_POINT('Ctrl Pts',(-7.90164306460424,0.384736312941631,
-43.6485075319314));
#64485=CARTESIAN_POINT('Ctrl Pts',(-7.90256087074338,0.365485359797262,
-43.6477400568437));
#64486=CARTESIAN_POINT('Ctrl Pts',(-7.90307322721607,0.354233582099445,
-43.6472923078335));
#64487=CARTESIAN_POINT('Ctrl Pts',(-7.90522771154322,0.304586186118256,
-43.6453202741824));
#64488=CARTESIAN_POINT('Ctrl Pts',(-7.90661408876186,0.266179680381141,
-43.6438042818066));
#64489=CARTESIAN_POINT('Ctrl Pts',(-7.90992443894157,0.151248008270138,
-43.6392956068646));
#64490=CARTESIAN_POINT('Ctrl Pts',(-7.91101765627593,0.0747029496055771,
-43.6363298934422));
#64491=CARTESIAN_POINT('Ctrl Pts',(-7.91099978439819,-0.00184695744787657,
-43.6333989249003));
#64492=CARTESIAN_POINT('',(-7.91099765047707,0.00609706046871071,-39.6423315082368));
#64493=CARTESIAN_POINT('Ctrl Pts',(-7.91099978972198,-0.00182401173648303,
-43.6333998034544));
#64494=CARTESIAN_POINT('Ctrl Pts',(-7.91081183821771,-0.816996568458522,
-43.6021881287131));
#64495=CARTESIAN_POINT('Ctrl Pts',(-7.78464881683108,-1.62722230157388,
-43.5757980757572));
#64496=CARTESIAN_POINT('Ctrl Pts',(-7.4589866112574,-2.64824243785534,-43.5392415117727));
#64497=CARTESIAN_POINT('Ctrl Pts',(-7.36924138152087,-2.88858752493205,
-43.5303177158346));
#64498=CARTESIAN_POINT('Ctrl Pts',(-7.21990949736473,-3.23599310220964,
-43.5164155290938));
#64499=CARTESIAN_POINT('Ctrl Pts',(-7.16925451213632,-3.34671956534006,
-43.5118274409518));
#64500=CARTESIAN_POINT('Ctrl Pts',(-7.09058732957546,-3.50868829766092,
-43.5048216944913));
#64501=CARTESIAN_POINT('Ctrl Pts',(-7.0645291626779,-3.56086360696497,-43.5025187266709));
#64502=CARTESIAN_POINT('Ctrl Pts',(-7.03356423302713,-3.62118560723126,
-43.4997969921473));
#64503=CARTESIAN_POINT('Ctrl Pts',(-7.02921615105167,-3.62961861941296,
-43.4994151389089));
#64504=CARTESIAN_POINT('Ctrl Pts',(-7.02257664445033,-3.64243912420972,
-43.4988325238346));
#64505=CARTESIAN_POINT('Ctrl Pts',(-7.02029624195143,-3.64683234818561,
-43.4986325034782));
#64506=CARTESIAN_POINT('Ctrl Pts',(-7.01615416623397,-3.65479382646461,
-43.4982693384759));
#64507=CARTESIAN_POINT('Ctrl Pts',(-7.01429388855268,-3.65836280912893,
-43.4981062886103));
#64508=CARTESIAN_POINT('Ctrl Pts',(-7.01029267735949,-3.66602494745113,
-43.4977557021633));
#64509=CARTESIAN_POINT('Ctrl Pts',(-7.00815087970693,-3.67011765272518,
-43.4975681063131));
#64510=CARTESIAN_POINT('Ctrl Pts',(-7.0023394284181,-3.68119896719949,-43.4970592732793));
#64511=CARTESIAN_POINT('Ctrl Pts',(-6.99866291404689,-3.68818393271218,
-43.4967375646631));
#64512=CARTESIAN_POINT('Ctrl Pts',(-6.981177638206,-3.72128371001466,-43.4952085127401));
#64513=CARTESIAN_POINT('Ctrl Pts',(-6.96723329617623,-3.74732622232824,
-43.493991978368));
#64514=CARTESIAN_POINT('Ctrl Pts',(-6.73296683984179,-4.17901539971919,
-43.473610134267));
#64515=CARTESIAN_POINT('Ctrl Pts',(-6.47771879030042,-4.56465715665231,
-43.4522658669892));
#64516=CARTESIAN_POINT('Ctrl Pts',(-5.93245091127666,-5.24990418329373,
-43.4114177311384));
#64517=CARTESIAN_POINT('Ctrl Pts',(-5.6494882618426,-5.55326838040774,-43.3920152701908));
#64518=CARTESIAN_POINT('Ctrl Pts',(-5.06392859816913,-6.08973639356223,
-43.3563853763366));
#64519=CARTESIAN_POINT('Ctrl Pts',(-4.76565274706613,-6.3258890846241,-43.3400695787678));
#64520=CARTESIAN_POINT('Ctrl Pts',(-4.43157774077439,-6.55329092311202,
-43.3237161081398));
#64521=CARTESIAN_POINT('Ctrl Pts',(-4.41156933500068,-6.56677692725913,
-43.3227434237852));
#64522=CARTESIAN_POINT('Ctrl Pts',(-4.38301731790371,-6.5858320796829,-43.3213649246844));
#64523=CARTESIAN_POINT('Ctrl Pts',(-4.37452425973476,-6.59147650325015,
-43.32095606936));
#64524=CARTESIAN_POINT('Ctrl Pts',(-4.36038332664269,-6.60083509393963,
-43.3202772989397));
#64525=CARTESIAN_POINT('Ctrl Pts',(-4.35474157537353,-6.60455846402135,
-43.3200070133658));
#64526=CARTESIAN_POINT('Ctrl Pts',(-4.34300117598336,-6.61228515758575,
-43.3194456326554));
#64527=CARTESIAN_POINT('Ctrl Pts',(-4.33690174709132,-6.61628728640856,
-43.3191545856371));
#64528=CARTESIAN_POINT('Ctrl Pts',(-4.32221702288224,-6.62589360923801,
-43.3184553217672));
#64529=CARTESIAN_POINT('Ctrl Pts',(-4.31362634143258,-6.631489568824,-43.3180474350915));
#64530=CARTESIAN_POINT('Ctrl Pts',(-4.28488911204101,-6.65012949677434,
-43.3166869384512));
#64531=CARTESIAN_POINT('Ctrl Pts',(-4.2646939914463,-6.66309854343295,-43.3157373204382));
#64532=CARTESIAN_POINT('Ctrl Pts',(-3.98718274791531,-6.83953415534704,
-43.3027757474687));
#64533=CARTESIAN_POINT('Ctrl Pts',(-3.72067635320959,-6.98809303667278,
-43.2913722855702));
#64534=CARTESIAN_POINT('Ctrl Pts',(-3.23102945415126,-7.22506283259982,
-43.2718174197311));
#64535=CARTESIAN_POINT('Ctrl Pts',(-3.01120352961416,-7.31940869168366,
-43.263501616798));
#64536=CARTESIAN_POINT('Ctrl Pts',(-2.41495038670087,-7.54389477985291,
-43.2416564017362));
#64537=CARTESIAN_POINT('Ctrl Pts',(-2.03242620888376,-7.65581860908378,
-43.2283866911835));
#64538=CARTESIAN_POINT('Ctrl Pts',(-1.49660847698611,-7.76958923368827,
-43.2091146435396));
#64539=CARTESIAN_POINT('Ctrl Pts',(-1.34924972032207,-7.79652973624795,
-43.2037411783932));
#64540=CARTESIAN_POINT('Ctrl Pts',(-1.09477686865112,-7.83562264838259,
-43.194203054522));
#64541=CARTESIAN_POINT('Ctrl Pts',(-0.988014039631855,-7.84979905750442,
-43.1901237789848));
#64542=CARTESIAN_POINT('Ctrl Pts',(-0.826025131388013,-7.86795167644452,
-43.1837717059559));
#64543=CARTESIAN_POINT('Ctrl Pts',(-0.770989221291343,-7.8735351930206,
-43.1815852750323));
#64544=CARTESIAN_POINT('Ctrl Pts',(-0.706519088023917,-7.87939341050408,
-43.1789861136164));
#64545=CARTESIAN_POINT('Ctrl Pts',(-0.697136198361799,-7.88022911196833,
-43.178606891156));
#64546=CARTESIAN_POINT('Ctrl Pts',(-0.682687991573719,-7.88148995713126,
-43.1780215073568));
#64547=CARTESIAN_POINT('Ctrl Pts',(-0.677623694750723,-7.88192698305918,
-43.177816050527));
#64548=CARTESIAN_POINT('Ctrl Pts',(-0.668388570352403,-7.88271496618133,
-43.1774408935832));
#64549=CARTESIAN_POINT('Ctrl Pts',(-0.664217874932868,-7.8830674951776,
-43.1772712855331));
#64550=CARTESIAN_POINT('Ctrl Pts',(-0.655125647587734,-7.88382875096019,
-43.1769011403839));
#64551=CARTESIAN_POINT('Ctrl Pts',(-0.650204011696049,-7.88423617933624,
-43.1767005279892));
#64552=CARTESIAN_POINT('Ctrl Pts',(-0.636794170269173,-7.88533364612062,
-43.1761532437376));
#64553=CARTESIAN_POINT('Ctrl Pts',(-0.628305247794709,-7.88601458535544,
-43.1758060490336));
#64554=CARTESIAN_POINT('Ctrl Pts',(-0.587711649431648,-7.88920484114297,
-43.1741422796069));
#64555=CARTESIAN_POINT('Ctrl Pts',(-0.555593357254782,-7.89153178874744,
-43.1728154082782));
#64556=CARTESIAN_POINT('Ctrl Pts',(-0.0109578040255894,-7.92764887924346,
-43.1501482014188));
#64557=CARTESIAN_POINT('Ctrl Pts',(0.503595250355316,-7.91163922487543,
-43.1262839227008));
#64558=CARTESIAN_POINT('Ctrl Pts',(1.41864730434796,-7.79350558893383,-43.083260556332));
#64559=CARTESIAN_POINT('Ctrl Pts',(1.81973671019622,-7.70972666276991,-43.0641908228352));
#64560=CARTESIAN_POINT('Ctrl Pts',(2.5778771201574,-7.48887516573073,-43.0288557539893));
#64561=CARTESIAN_POINT('Ctrl Pts',(2.93506507778931,-7.35623188741114,-43.0125304885158));
#64562=CARTESIAN_POINT('Ctrl Pts',(3.29836029107813,-7.19062512753387,-42.9963160462383));
#64563=CARTESIAN_POINT('Ctrl Pts',(3.31533969185014,-7.18281233698664,-42.9955590681318));
#64564=CARTESIAN_POINT('Ctrl Pts',(3.34250680367161,-7.17019498570641,-42.9943492132727));
#64565=CARTESIAN_POINT('Ctrl Pts',(3.35271216854238,-7.16542873678227,-42.9938950275704));
#64566=CARTESIAN_POINT('Ctrl Pts',(3.37215287073074,-7.1562986487085,-42.9930303859468));
#64567=CARTESIAN_POINT('Ctrl Pts',(3.38138999860773,-7.15193868901353,-42.992619798255));
#64568=CARTESIAN_POINT('Ctrl Pts',(3.39771488630759,-7.14419458296152,-42.9918945818404));
#64569=CARTESIAN_POINT('Ctrl Pts',(3.40480608941857,-7.14081775301371,-42.9915797029703));
#64570=CARTESIAN_POINT('Ctrl Pts',(3.41862015561495,-7.13421424121544,-42.9909665715115));
#64571=CARTESIAN_POINT('Ctrl Pts',(3.42534350623976,-7.13098860415294,-42.9906682835995));
#64572=CARTESIAN_POINT('Ctrl Pts',(3.44139280883428,-7.12326075460672,-42.9899565359143));
#64573=CARTESIAN_POINT('Ctrl Pts',(3.45071451247693,-7.11874972149438,-42.9895433793226));
#64574=CARTESIAN_POINT('Ctrl Pts',(3.48407754469506,-7.10252348758256,-42.9880655004954));
#64575=CARTESIAN_POINT('Ctrl Pts',(3.50806841229001,-7.09070463786781,-42.9870043410509));
#64576=CARTESIAN_POINT('Ctrl Pts',(3.87878355785397,-6.90573371863429,-42.9706298022709));
#64577=CARTESIAN_POINT('Ctrl Pts',(4.21239776005106,-6.70744840797596,-42.9562404715785));
#64578=CARTESIAN_POINT('Ctrl Pts',(4.69710314179151,-6.36887835826286,-42.9351127020209));
#64579=CARTESIAN_POINT('Ctrl Pts',(4.85948458113003,-6.24586276344972,-42.927985190256));
#64580=CARTESIAN_POINT('Ctrl Pts',(5.36167160179725,-5.83396819690105,-42.9054037916875));
#64581=CARTESIAN_POINT('Ctrl Pts',(5.68186560095015,-5.52259660427665,-42.8901979887975));
#64582=CARTESIAN_POINT('Ctrl Pts',(6.02580563033462,-5.12638333944188,-42.8709312177263));
#64583=CARTESIAN_POINT('Ctrl Pts',(6.0766057020977,-5.06606378741388,-42.8679990555525));
#64584=CARTESIAN_POINT('Ctrl Pts',(6.2065704002251,-4.9069771477098,-42.8602421887724));
#64585=CARTESIAN_POINT('Ctrl Pts',(6.28427293798439,-4.80706265987731,-42.8553375129544));
#64586=CARTESIAN_POINT('Ctrl Pts',(6.37659033729413,-4.68228979851745,-42.8491728299081));
#64587=CARTESIAN_POINT('Ctrl Pts',(6.39350819288933,-4.65916248363337,-42.8480289505576));
#64588=CARTESIAN_POINT('Ctrl Pts',(6.4167667466558,-4.62700197731813,-42.8464370736674));
#64589=CARTESIAN_POINT('Ctrl Pts',(6.42321486648299,-4.61804650871885,-42.8459936672717));
#64590=CARTESIAN_POINT('Ctrl Pts',(6.43408355269712,-4.60288473636843,-42.8452427854875));
#64591=CARTESIAN_POINT('Ctrl Pts',(6.43851393899757,-4.59668547066967,-42.8449357163325));
#64592=CARTESIAN_POINT('Ctrl Pts',(6.44727587630592,-4.58438771579683,-42.8443264780818));
#64593=CARTESIAN_POINT('Ctrl Pts',(6.45160774841539,-4.57828946377511,-42.8440243224111));
#64594=CARTESIAN_POINT('Ctrl Pts',(6.46115570408235,-4.56480773865446,-42.843356245642));
#64595=CARTESIAN_POINT('Ctrl Pts',(6.46636779077903,-4.55742145482825,-42.8429901674711));
#64596=CARTESIAN_POINT('Ctrl Pts',(6.48462145688415,-4.53145900544274,-42.8417032575424));
#64597=CARTESIAN_POINT('Ctrl Pts',(6.49759568525072,-4.51283574453198,-42.8407798473039));
#64598=CARTESIAN_POINT('Ctrl Pts',(6.7058668329626,-4.21112240394115,-42.8258176819473));
#64599=CARTESIAN_POINT('Ctrl Pts',(6.88257305811105,-3.91565741047275,-42.8111555985502));
#64600=CARTESIAN_POINT('Ctrl Pts',(7.32939738187478,-3.04426657739399,-42.7691109407579));
#64601=CARTESIAN_POINT('Ctrl Pts',(7.55015820567726,-2.44597837343103,-42.7418377464457));
#64602=CARTESIAN_POINT('Ctrl Pts',(7.79036741386173,-1.43440792637692,-42.6985816283015));
#64603=CARTESIAN_POINT('Ctrl Pts',(7.85348377275889,-1.03448450679828,-42.6819747236043));
#64604=CARTESIAN_POINT('Ctrl Pts',(7.88989833998355,-0.579757523518488,
-42.6634871925656));
#64605=CARTESIAN_POINT('Ctrl Pts',(7.89353203978945,-0.527983505120561,
-42.6613889208779));
#64606=CARTESIAN_POINT('Ctrl Pts',(7.89826098626518,-0.449561317177088,
-42.658220666819));
#64607=CARTESIAN_POINT('Ctrl Pts',(7.89973138660155,-0.422937360300898,
-42.6571468006313));
#64608=CARTESIAN_POINT('Ctrl Pts',(7.90204711831214,-0.376769166245137,
-42.6552876078282));
#64609=CARTESIAN_POINT('Ctrl Pts',(7.90295461202745,-0.357228312644079,
-42.654501623179));
#64610=CARTESIAN_POINT('Ctrl Pts',(7.90469252431315,-0.316550985936338,
-42.6528673768239));
#64611=CARTESIAN_POINT('Ctrl Pts',(7.90551066800371,-0.295414136178893,
-42.6520192547414));
#64612=CARTESIAN_POINT('Ctrl Pts',(7.9075301542098,-0.237200314182017,-42.6496863048612));
#64613=CARTESIAN_POINT('Ctrl Pts',(7.90855549702967,-0.200117706100361,
-42.6482034356713));
#64614=CARTESIAN_POINT('Ctrl Pts',(7.9115948087887,-0.0526662218354875,
-42.6423195051316));
#64615=CARTESIAN_POINT('Ctrl Pts',(7.91155948451444,0.0577331483655337,
-42.6379419032013));
#64616=CARTESIAN_POINT('Ctrl Pts',(7.89391523870753,0.8879231308623,-42.6051961937961));
#64617=CARTESIAN_POINT('Ctrl Pts',(7.78042415335899,1.6022601279125,-42.5783315359479));
#64618=CARTESIAN_POINT('Ctrl Pts',(7.54482416140158,2.38081669756805,-42.5463174223513));
#64619=CARTESIAN_POINT('Ctrl Pts',(7.5161647671828,2.46980292231212,-42.5426107179413));
#64620=CARTESIAN_POINT('Ctrl Pts',(7.47940883772384,2.57735752075816,-42.5380571001372));
#64621=CARTESIAN_POINT('Ctrl Pts',(7.47280907061646,2.59643080831596,-42.5372467271813));
#64622=CARTESIAN_POINT('Ctrl Pts',(7.46212823934856,2.62692027162976,-42.5359466306197));
#64623=CARTESIAN_POINT('Ctrl Pts',(7.45809383883152,2.63835256626456,-42.5354581025129));
#64624=CARTESIAN_POINT('Ctrl Pts',(7.450342210185,2.66015852559232,-42.5345243193796));
#64625=CARTESIAN_POINT('Ctrl Pts',(7.44662955301984,2.67053379108492,-42.5340791748039));
#64626=CARTESIAN_POINT('Ctrl Pts',(7.43808535272337,2.6942547646898,-42.533059521074));
#64627=CARTESIAN_POINT('Ctrl Pts',(7.43323955134159,2.70759528400082,-42.5324846816955));
#64628=CARTESIAN_POINT('Ctrl Pts',(7.41854954427258,2.74770029378803,-42.5307524527797));
#64629=CARTESIAN_POINT('Ctrl Pts',(7.40859652532278,2.77442458105489,-42.5295926432102));
#64630=CARTESIAN_POINT('Ctrl Pts',(7.31017698971493,3.03437900319004,-42.5182589680592));
#64631=CARTESIAN_POINT('Ctrl Pts',(7.21087222326577,3.26335103575648,-42.5078715040871));
#64632=CARTESIAN_POINT('Ctrl Pts',(6.90618907627086,3.88376392751844,-42.4789133209328));
#64633=CARTESIAN_POINT('Ctrl Pts',(6.67858280134164,4.26328689410199,-42.4602908977703));
#64634=CARTESIAN_POINT('Ctrl Pts',(6.29175713444509,4.80065246838734,-42.4329001559247));
#64635=CARTESIAN_POINT('Ctrl Pts',(6.15560975979426,4.97402691950493,-42.4238745544273));
#64636=CARTESIAN_POINT('Ctrl Pts',(5.97962108093384,5.17982591499766,-42.4128993836702));
#64637=CARTESIAN_POINT('Ctrl Pts',(5.94647597165847,5.21784326520502,-42.4108602468522));
#64638=CARTESIAN_POINT('Ctrl Pts',(5.89331773442231,5.27765119372362,-42.4076328801001));
#64639=CARTESIAN_POINT('Ctrl Pts',(5.87354212186838,5.29965083680797,-42.406441476891));
#64640=CARTESIAN_POINT('Ctrl Pts',(5.83602086554149,5.34092386999577,-42.4041980422957));
#64641=CARTESIAN_POINT('Ctrl Pts',(5.8183019764274,5.36022102572518,-42.4031456696459));
#64642=CARTESIAN_POINT('Ctrl Pts',(5.77801988167561,5.403656072691,-42.400768891833));
#64643=CARTESIAN_POINT('Ctrl Pts',(5.75540063243217,5.4277413604217,-42.3994452552681));
#64644=CARTESIAN_POINT('Ctrl Pts',(5.69641596879597,5.48976573660764,-42.396021350378));
#64645=CARTESIAN_POINT('Ctrl Pts',(5.65982214910994,5.52748550538911,-42.3939241179831));
#64646=CARTESIAN_POINT('Ctrl Pts',(5.45356060024357,5.73589746656889,-42.3822472723453));
#64647=CARTESIAN_POINT('Ctrl Pts',(5.27654490396205,5.89914566053216,-42.3727492807683));
#64648=CARTESIAN_POINT('Ctrl Pts',(4.45861384018537,6.58714590047324,-42.3309024817012));
#64649=CARTESIAN_POINT('Ctrl Pts',(3.74512058442697,7.01738825772705,-42.3007233616847));
#64650=CARTESIAN_POINT('Ctrl Pts',(2.80078388928725,7.40108732751654,-42.2624410359698));
#64651=CARTESIAN_POINT('Ctrl Pts',(2.6210871998957,7.46661782343709,-42.2551794897459));
#64652=CARTESIAN_POINT('Ctrl Pts',(2.35926653111254,7.55147951529407,-42.2444507851027));
#64653=CARTESIAN_POINT('Ctrl Pts',(2.27892776614147,7.57611174093569,-42.2411387322165));
#64654=CARTESIAN_POINT('Ctrl Pts',(2.18387550933831,7.60360648255676,-42.2371825647751));
#64655=CARTESIAN_POINT('Ctrl Pts',(2.169525771373,7.60771330332445,-42.2365843118217));
#64656=CARTESIAN_POINT('Ctrl Pts',(2.14750082524071,7.61394934621418,-42.2356644294713));
#64657=CARTESIAN_POINT('Ctrl Pts',(2.13983383837818,7.61610764004155,-42.2353439092076));
#64658=CARTESIAN_POINT('Ctrl Pts',(2.12644992670361,7.61985347055614,-42.2347838411365));
#64659=CARTESIAN_POINT('Ctrl Pts',(2.12073444404472,7.62144616336766,-42.2345444940052));
#64660=CARTESIAN_POINT('Ctrl Pts',(2.10786264490656,7.62501745558707,-42.2340050582863));
#64661=CARTESIAN_POINT('Ctrl Pts',(2.10070532950367,7.62699241155473,-42.2337048263829));
#64662=CARTESIAN_POINT('Ctrl Pts',(2.08152709347011,7.63225532018683,-42.2328995713882));
#64663=CARTESIAN_POINT('Ctrl Pts',(2.0695011953893,7.63552494025853,-42.2323938138036));
#64664=CARTESIAN_POINT('Ctrl Pts',(2.01741481335839,7.64955417551561,-42.2301995818011));
#64665=CARTESIAN_POINT('Ctrl Pts',(1.97727826212934,7.66002690558088,-42.2284992895499));
#64666=CARTESIAN_POINT('Ctrl Pts',(1.31687324853165,7.82680848588956,-42.2003422356022));
#64667=CARTESIAN_POINT('Ctrl Pts',(0.680064371117668,7.90761519724527,-42.1703841306729));
#64668=CARTESIAN_POINT('Ctrl Pts',(-0.324571243112215,7.91276924241778,
-42.124250103043));
#64669=CARTESIAN_POINT('Ctrl Pts',(-0.68943928843699,7.88935795499171,-42.1077049519506));
#64670=CARTESIAN_POINT('Ctrl Pts',(-1.24063437403823,7.81544619761173,-42.0834857769178));
#64671=CARTESIAN_POINT('Ctrl Pts',(-1.42889093076588,7.78322875417702,-42.0753489547174));
#64672=CARTESIAN_POINT('Ctrl Pts',(-1.71081449990175,7.72440640722361,-42.0633790781107));
#64673=CARTESIAN_POINT('Ctrl Pts',(-1.8054522319059,7.70283607999391,-42.0593977226977));
#64674=CARTESIAN_POINT('Ctrl Pts',(-1.91725887444196,7.67517867280289,-42.0547359906525));
#64675=CARTESIAN_POINT('Ctrl Pts',(-1.9348315368889,7.67076763957507,-42.054004537019));
#64676=CARTESIAN_POINT('Ctrl Pts',(-1.96185039238002,7.66388670078803,-42.0528817605837));
#64677=CARTESIAN_POINT('Ctrl Pts',(-1.97130737246376,7.6614596239034,-42.0524891262482));
#64678=CARTESIAN_POINT('Ctrl Pts',(-1.98784179670236,7.65718352265487,-42.0518032641221));
#64679=CARTESIAN_POINT('Ctrl Pts',(-1.99492120546629,7.65534217998639,-42.051509801001));
#64680=CARTESIAN_POINT('Ctrl Pts',(-2.01090158223136,7.65116203745574,-42.0508478073153));
#64681=CARTESIAN_POINT('Ctrl Pts',(-2.01980105009127,7.64881751747142,-42.0504794529638));
#64682=CARTESIAN_POINT('Ctrl Pts',(-2.04374421603517,7.64246510979039,-42.0494892578281));
#64683=CARTESIAN_POINT('Ctrl Pts',(-2.05878024103004,7.63842832639485,-42.048868306663));
#64684=CARTESIAN_POINT('Ctrl Pts',(-2.1248173697459,7.62048991217921,-42.0461449430197));
#64685=CARTESIAN_POINT('Ctrl Pts',(-2.17569082962811,7.60612154126863,-42.0440569366472));
#64686=CARTESIAN_POINT('Ctrl Pts',(-3.11149686375139,7.3316613245939,-42.0058219162382));
#64687=CARTESIAN_POINT('Ctrl Pts',(-3.9442575466547,6.91934799402131,-41.9756397270761));
#64688=CARTESIAN_POINT('Ctrl Pts',(-4.96486456524271,6.16869655541085,-41.9307579717741));
#64689=CARTESIAN_POINT('Ctrl Pts',(-5.22884871016925,5.94658088533544,-41.9181276287174));
#64690=CARTESIAN_POINT('Ctrl Pts',(-5.48938088826067,5.69656823412778,-41.9037092138061));
#64691=CARTESIAN_POINT('Ctrl Pts',(-5.50122696005389,5.68512920787922,-41.9030492676399));
#64692=CARTESIAN_POINT('Ctrl Pts',(-5.51841110818064,5.66843152801336,-41.9020856935766));
#64693=CARTESIAN_POINT('Ctrl Pts',(-5.52377762029411,5.66320209313052,-41.9017838837749));
#64694=CARTESIAN_POINT('Ctrl Pts',(-5.5331612756938,5.65403209777566,-41.9012546028455));
#64695=CARTESIAN_POINT('Ctrl Pts',(-5.53718166541381,5.65009485491111,-41.9010273348866));
#64696=CARTESIAN_POINT('Ctrl Pts',(-5.54496484835306,5.64245635238092,-41.9005863974892));
#64697=CARTESIAN_POINT('Ctrl Pts',(-5.54872814585027,5.63875560928773,-41.9003727592979));
#64698=CARTESIAN_POINT('Ctrl Pts',(-5.5576798519271,5.62993506139776,-41.8998635440783));
#64699=CARTESIAN_POINT('Ctrl Pts',(-5.56286488711169,5.62481185278913,-41.8995677634699));
#64700=CARTESIAN_POINT('Ctrl Pts',(-5.58125707950899,5.60658866436246,-41.8985156473082));
#64701=CARTESIAN_POINT('Ctrl Pts',(-5.59442504002702,5.59344933849766,-41.897756996418));
#64702=CARTESIAN_POINT('Ctrl Pts',(-5.82952261943001,5.35720233424159,-41.8841174553474));
#64703=CARTESIAN_POINT('Ctrl Pts',(-6.0379808617838,5.12110506706688,-41.8705177038608));
#64704=CARTESIAN_POINT('Ctrl Pts',(-6.68964401530127,4.28776942123393,-41.8241878296159));
#64705=CARTESIAN_POINT('Ctrl Pts',(-7.06276121718457,3.64059938964207,-41.7913266625748));
#64706=CARTESIAN_POINT('Ctrl Pts',(-7.37253253740109,2.87006393643871,-41.7573027399143));
#64707=CARTESIAN_POINT('Ctrl Pts',(-7.40367628172029,2.78874181438626,-41.7537629951243));
#64708=CARTESIAN_POINT('Ctrl Pts',(-7.4419800249354,2.68355596750651,-41.7492455813139));
#64709=CARTESIAN_POINT('Ctrl Pts',(-7.45037831651982,2.66015079861557,-41.7482442416188));
#64710=CARTESIAN_POINT('Ctrl Pts',(-7.46375304019118,2.62231662760657,-41.7466316218151));
#64711=CARTESIAN_POINT('Ctrl Pts',(-7.4687982924261,2.60791219356127,-41.7460190623004));
#64712=CARTESIAN_POINT('Ctrl Pts',(-7.47834891983583,2.58038966288955,-41.7448512812874));
#64713=CARTESIAN_POINT('Ctrl Pts',(-7.48286154058232,2.56727414683741,-41.7442959290753));
#64714=CARTESIAN_POINT('Ctrl Pts',(-7.49310971916191,2.53723217992936,-41.7430264194268));
#64715=CARTESIAN_POINT('Ctrl Pts',(-7.49882246338263,2.52029801091779,-41.7423126743188));
#64716=CARTESIAN_POINT('Ctrl Pts',(-7.51580419970742,2.46939049161486,-41.7401724560626));
#64717=CARTESIAN_POINT('Ctrl Pts',(-7.5269001007057,2.43535973984098,-41.738748997024));
#64718=CARTESIAN_POINT('Ctrl Pts',(-7.59778237742529,2.2128536026966,-41.729487243481));
#64719=CARTESIAN_POINT('Ctrl Pts',(-7.65071676690429,2.0222647615266,-41.7217693942327));
#64720=CARTESIAN_POINT('Ctrl Pts',(-7.7264090630307,1.70390519075901,-41.7091885546783));
#64721=CARTESIAN_POINT('Ctrl Pts',(-7.75326496031128,1.57720425805516,-41.7042609205742));
#64722=CARTESIAN_POINT('Ctrl Pts',(-7.86645885154126,0.970052656448543,
-41.6809599169124));
#64723=CARTESIAN_POINT('Ctrl Pts',(-7.91131610941931,0.482963186128997,
-41.6632635675703));
#64724=CARTESIAN_POINT('Ctrl Pts',(-7.91076872629169,-0.357807502292524,
-41.6321363169891));
#64725=CARTESIAN_POINT('Ctrl Pts',(-7.88695811714254,-0.710034828332207,
-41.6188952219463));
#64726=CARTESIAN_POINT('Ctrl Pts',(-7.83695990569885,-1.08000448836327,
-41.6039823309859));
#64727=CARTESIAN_POINT('Ctrl Pts',(-7.83410456311462,-1.10052530308577,
-41.6031518246918));
#64728=CARTESIAN_POINT('Ctrl Pts',(-7.8300008310785,-1.12919258889206,-41.6019867093645));
#64729=CARTESIAN_POINT('Ctrl Pts',(-7.82882025987236,-1.13734878356024,
-41.6016546636447));
#64730=CARTESIAN_POINT('Ctrl Pts',(-7.82675654894313,-1.15145084866713,
-41.6010795763058));
#64731=CARTESIAN_POINT('Ctrl Pts',(-7.82587937179862,-1.15739759423216,
-41.6008367642765));
#64732=CARTESIAN_POINT('Ctrl Pts',(-7.82404689701327,-1.16972336815349,
-41.6003328558814));
#64733=CARTESIAN_POINT('Ctrl Pts',(-7.82309057415665,-1.17610223742525,
-41.6000717197172));
#64734=CARTESIAN_POINT('Ctrl Pts',(-7.82083181453331,-1.19104397397079,
-41.5994592027343));
#64735=CARTESIAN_POINT('Ctrl Pts',(-7.81952311595772,-1.19960587584501,
-41.5991075745614));
#64736=CARTESIAN_POINT('Ctrl Pts',(-7.81524751667815,-1.22727384797813,
-41.5979691581138));
#64737=CARTESIAN_POINT('Ctrl Pts',(-7.81222464552318,-1.24637110190474,
-41.5971801164791));
#64738=CARTESIAN_POINT('Ctrl Pts',(-7.76506238628768,-1.53740928744274,
-41.5851032634546));
#64739=CARTESIAN_POINT('Ctrl Pts',(-7.70682706740391,-1.8068159369177,-41.5731273577745));
#64740=CARTESIAN_POINT('Ctrl Pts',(-7.39067179809481,-2.97141330746483,
-41.518976943685));
#64741=CARTESIAN_POINT('Ctrl Pts',(-6.98973801243016,-3.82043105359153,
-41.4746626591274));
#64742=CARTESIAN_POINT('Ctrl Pts',(-6.42203612067811,-4.61992987645502,
-41.4345250705146));
#64743=CARTESIAN_POINT('Ctrl Pts',(-6.39342979444065,-4.65943725968026,
-41.4325429584003));
#64744=CARTESIAN_POINT('Ctrl Pts',(-6.355932258651,-4.71022847118526,-41.4299961854272));
#64745=CARTESIAN_POINT('Ctrl Pts',(-6.34737349090102,-4.7217557007161,-41.429418284439));
#64746=CARTESIAN_POINT('Ctrl Pts',(-6.33370728516738,-4.74005748947649,
-41.4285008955895));
#64747=CARTESIAN_POINT('Ctrl Pts',(-6.32862026800039,-4.74684721491845,
-41.4281605881106));
#64748=CARTESIAN_POINT('Ctrl Pts',(-6.31947145713717,-4.75901743533498,
-41.4275506596682));
#64749=CARTESIAN_POINT('Ctrl Pts',(-6.31541369367337,-4.76440094087907,
-41.4272808766064));
#64750=CARTESIAN_POINT('Ctrl Pts',(-6.30592566202864,-4.7769554588536,-41.4266517763668));
#64751=CARTESIAN_POINT('Ctrl Pts',(-6.30049002975001,-4.78412241656116,
-41.4262926767733));
#64752=CARTESIAN_POINT('Ctrl Pts',(-6.28493897714689,-4.80455422807314,
-41.4252690313776));
#64753=CARTESIAN_POINT('Ctrl Pts',(-6.27479377954778,-4.81779641595894,
-41.4246056966922));
#64754=CARTESIAN_POINT('Ctrl Pts',(-6.21024598295809,-4.9014987590468,-41.420413421678));
#64755=CARTESIAN_POINT('Ctrl Pts',(-6.15469823776888,-4.97106985728453,
-41.4169316677854));
#64756=CARTESIAN_POINT('Ctrl Pts',(-5.98783674302622,-5.17297100070451,
-41.4068269341414));
#64757=CARTESIAN_POINT('Ctrl Pts',(-5.87334332640912,-5.30260882812959,
-41.4003394388996));
#64758=CARTESIAN_POINT('Ctrl Pts',(-5.51311335384148,-5.68449171454556,
-41.3811231561032));
#64759=CARTESIAN_POINT('Ctrl Pts',(-5.25470414713677,-5.9241851063745,-41.368931342189));
#64760=CARTESIAN_POINT('Ctrl Pts',(-4.8717255247844,-6.23458583329594,-41.3522139742931));
#64761=CARTESIAN_POINT('Ctrl Pts',(-4.75992306688475,-6.3203562264405,-41.347476428427));
#64762=CARTESIAN_POINT('Ctrl Pts',(-4.5212483824416,-6.49353125105699,-41.3375591025633));
#64763=CARTESIAN_POINT('Ctrl Pts',(-4.39399410028985,-6.58030775967649,
-41.3323813808221));
#64764=CARTESIAN_POINT('Ctrl Pts',(-3.902524625278,-6.89483113864197,-41.3125343122149));
#64765=CARTESIAN_POINT('Ctrl Pts',(-3.52254227305133,-7.09647878512309,
-41.2975081062685));
#64766=CARTESIAN_POINT('Ctrl Pts',(-3.10239720792502,-7.27735097823584,
-41.279398939432));
#64767=CARTESIAN_POINT('Ctrl Pts',(-3.07660938110214,-7.28829063457542,
-41.2782816083009));
#64768=CARTESIAN_POINT('Ctrl Pts',(-3.04353794050842,-7.30211333435504,
-41.27684063205));
#64769=CARTESIAN_POINT('Ctrl Pts',(-3.03630711301348,-7.30512295979145,
-41.2765250817361));
#64770=CARTESIAN_POINT('Ctrl Pts',(-3.02479018188331,-7.30989649979695,
-41.2760216886902));
#64771=CARTESIAN_POINT('Ctrl Pts',(-3.02050696036158,-7.31166740110527,
-41.2758342978797));
#64772=CARTESIAN_POINT('Ctrl Pts',(-3.0125027957268,-7.31496849567399,-41.2754837837171));
#64773=CARTESIAN_POINT('Ctrl Pts',(-3.00878223459501,-7.31649961741468,
-41.2753207209106));
#64774=CARTESIAN_POINT('Ctrl Pts',(-3.00049607188368,-7.31990223089548,
-41.2749572579134));
#64775=CARTESIAN_POINT('Ctrl Pts',(-2.99592991523275,-7.3217722779518,-41.2747567646821));
#64776=CARTESIAN_POINT('Ctrl Pts',(-2.98245821438458,-7.32727483465932,
-41.2741646376998));
#64777=CARTESIAN_POINT('Ctrl Pts',(-2.9735478616077,-7.33089534888164,-41.2737722220114));
#64778=CARTESIAN_POINT('Ctrl Pts',(-2.90402533921412,-7.35899660110856,
-41.2707045235178));
#64779=CARTESIAN_POINT('Ctrl Pts',(-2.84312010567347,-7.38274080015654,
-41.2679821594313));
#64780=CARTESIAN_POINT('Ctrl Pts',(-2.6336961820862,-7.46140999598996,-41.2585219952544));
#64781=CARTESIAN_POINT('Ctrl Pts',(-2.48383209146895,-7.51262719897673,
-41.2515833670681));
#64782=CARTESIAN_POINT('Ctrl Pts',(-1.82795972718848,-7.71500666962809,
-41.2208278000417));
#64783=CARTESIAN_POINT('Ctrl Pts',(-1.30906271879428,-7.81979113584119,
-41.1956137530407));
#64784=CARTESIAN_POINT('Ctrl Pts',(-0.268294000585628,-7.92338943159521,
-41.1474663403125));
#64785=CARTESIAN_POINT('Ctrl Pts',(0.250847845163416,-7.92396995462643,
-41.1246286101601));
#64786=CARTESIAN_POINT('Ctrl Pts',(0.799336731662875,-7.87058304382767,
-41.1022369240626));
#64787=CARTESIAN_POINT('Ctrl Pts',(0.832261621015753,-7.86716958581137,
-41.1008989568986));
#64788=CARTESIAN_POINT('Ctrl Pts',(0.877073872558543,-7.86223924683237,
-41.0990861907204));
#64789=CARTESIAN_POINT('Ctrl Pts',(0.888980385718612,-7.86090188387578,
-41.098605338419));
#64790=CARTESIAN_POINT('Ctrl Pts',(0.907800778729958,-7.8587446337576,-41.0978465136171));
#64791=CARTESIAN_POINT('Ctrl Pts',(0.914716668260801,-7.85794266265786,
-41.0975679367006));
#64792=CARTESIAN_POINT('Ctrl Pts',(0.928080612388626,-7.85637508907095,
-41.0970301409965));
#64793=CARTESIAN_POINT('Ctrl Pts',(0.934528799367214,-7.85561067560656,
-41.096770882297));
#64794=CARTESIAN_POINT('Ctrl Pts',(0.949810635946557,-7.85377997692017,
-41.0961569993789));
#64795=CARTESIAN_POINT('Ctrl Pts',(0.958643451263589,-7.85270672469646,
-41.0958026106864));
#64796=CARTESIAN_POINT('Ctrl Pts',(0.98463001658667,-7.84950466668104,-41.0947612461403));
#64797=CARTESIAN_POINT('Ctrl Pts',(1.00177867503754,-7.84733453302721,-41.0940756661462));
#64798=CARTESIAN_POINT('Ctrl Pts',(1.1321533298797,-7.83040151431789,-41.0888756386054));
#64799=CARTESIAN_POINT('Ctrl Pts',(1.24505756276356,-7.81324466076694,-41.084442602824));
#64800=CARTESIAN_POINT('Ctrl Pts',(1.66026340928925,-7.74092110546754,-41.0683689060161));
#64801=CARTESIAN_POINT('Ctrl Pts',(1.95965581483859,-7.6705999017265,-41.057242764371));
#64802=CARTESIAN_POINT('Ctrl Pts',(2.67903312191313,-7.45675001650187,-41.0309321763449));
#64803=CARTESIAN_POINT('Ctrl Pts',(3.09247466664108,-7.2949935885172,-41.0162025780311));
#64804=CARTESIAN_POINT('Ctrl Pts',(3.83095984203199,-6.9319444573193,-40.9878090161078));
#64805=CARTESIAN_POINT('Ctrl Pts',(4.15919029753097,-6.74011754176666,-40.9743090227546));
#64806=CARTESIAN_POINT('Ctrl Pts',(4.49273176996395,-6.51152004123016,-40.9582659505304));
#64807=CARTESIAN_POINT('Ctrl Pts',(4.51305539053108,-6.49745050214394,-40.9572786453223));
#64808=CARTESIAN_POINT('Ctrl Pts',(4.53958882484194,-6.47889751051672,-40.9559763704938));
#64809=CARTESIAN_POINT('Ctrl Pts',(4.54585866408004,-6.4744998768867,-40.9556676672064));
#64810=CARTESIAN_POINT('Ctrl Pts',(4.55557823238001,-6.46766154234924,-40.955187608314));
#64811=CARTESIAN_POINT('Ctrl Pts',(4.55903242330815,-6.46522715925784,-40.955016707087));
#64812=CARTESIAN_POINT('Ctrl Pts',(4.56594159770817,-6.46034954415488,-40.9546742766365));
#64813=CARTESIAN_POINT('Ctrl Pts',(4.56939657487203,-6.45790630527874,-40.9545027469217));
#64814=CARTESIAN_POINT('Ctrl Pts',(4.57709992751761,-6.4524494871278,-40.9541196417457));
#64815=CARTESIAN_POINT('Ctrl Pts',(4.58134728702753,-6.44943448418638,-40.9539079652952));
#64816=CARTESIAN_POINT('Ctrl Pts',(4.59373884826159,-6.44061987371016,-40.9532891102286));
#64817=CARTESIAN_POINT('Ctrl Pts',(4.6018750108861,-6.43480903726657,-40.9528811419198));
#64818=CARTESIAN_POINT('Ctrl Pts',(4.66030443647288,-6.39291132725107,-40.9499396960017));
#64819=CARTESIAN_POINT('Ctrl Pts',(4.71018239314291,-6.35625157687396,-40.9473666070419));
#64820=CARTESIAN_POINT('Ctrl Pts',(4.86560163578552,-6.23918625096984,-40.9391652586494));
#64821=CARTESIAN_POINT('Ctrl Pts',(4.96954997766387,-6.15671131102497,-40.9334093786302));
#64822=CARTESIAN_POINT('Ctrl Pts',(5.41790949455732,-5.78221816854286,-40.9075463089138));
#64823=CARTESIAN_POINT('Ctrl Pts',(5.73901990692258,-5.46364479344847,-40.8862852593344));
#64824=CARTESIAN_POINT('Ctrl Pts',(6.13601470784765,-4.99594659755881,-40.8577281434779));
#64825=CARTESIAN_POINT('Ctrl Pts',(6.23702158898411,-4.86926302251088,-40.8502202551786));
#64826=CARTESIAN_POINT('Ctrl Pts',(6.64362247519964,-4.32587183079825,-40.8191037278331));
#64827=CARTESIAN_POINT('Ctrl Pts',(6.91193388103915,-3.88280672604363,-40.7964197138117));
#64828=CARTESIAN_POINT('Ctrl Pts',(7.14932570246748,-3.38705502601568,-40.7740441729964));
#64829=CARTESIAN_POINT('Ctrl Pts',(7.16332630974431,-3.35734358730521,-40.7727135281773));
#64830=CARTESIAN_POINT('Ctrl Pts',(7.1824213615432,-3.3161577080871,-40.7708831225569));
#64831=CARTESIAN_POINT('Ctrl Pts',(7.18767403781135,-3.30475725094974,-40.7703779455581));
#64832=CARTESIAN_POINT('Ctrl Pts',(7.19601572168429,-3.28653841659955,-40.7695729943519));
#64833=CARTESIAN_POINT('Ctrl Pts',(7.19912221367841,-3.27972809595844,-40.7692726237954));
#64834=CARTESIAN_POINT('Ctrl Pts',(7.20548636568614,-3.26572344271429,-40.7686560216634));
#64835=CARTESIAN_POINT('Ctrl Pts',(7.20874292863689,-3.25852861882229,-40.7683398276544));
#64836=CARTESIAN_POINT('Ctrl Pts',(7.21625171008556,-3.24187289174032,-40.767609193049));
#64837=CARTESIAN_POINT('Ctrl Pts',(7.22049611052776,-3.23240846868263,-40.7671950182692));
#64838=CARTESIAN_POINT('Ctrl Pts',(7.23378083681923,-3.2026286462558,-40.7658949421695));
#64839=CARTESIAN_POINT('Ctrl Pts',(7.24275416643337,-3.18228338394865,-40.7650113090593));
#64840=CARTESIAN_POINT('Ctrl Pts',(7.37195678710983,-2.88596440786888,-40.7522071293867));
#64841=CARTESIAN_POINT('Ctrl Pts',(7.47642934830995,-2.60337517850799,-40.7408337454558));
#64842=CARTESIAN_POINT('Ctrl Pts',(7.78609698742599,-1.59171639857824,-40.7022504797429));
#64843=CARTESIAN_POINT('Ctrl Pts',(7.90260401769231,-0.839968278326332,
-40.6776529256632));
#64844=CARTESIAN_POINT('Ctrl Pts',(7.91270903614201,0.120915433268998,-40.6422210643717));
#64845=CARTESIAN_POINT('Ctrl Pts',(7.90695646312843,0.324992131708635,-40.6344159645815));
#64846=CARTESIAN_POINT('Ctrl Pts',(7.89192805825546,0.549385791618619,-40.6254484076656));
#64847=CARTESIAN_POINT('Ctrl Pts',(7.89045703498724,0.570123665650544,-40.6246164632991));
#64848=CARTESIAN_POINT('Ctrl Pts',(7.8881886719457,0.600410093513533,-40.6233969909907));
#64849=CARTESIAN_POINT('Ctrl Pts',(7.88745569659465,0.609963472639379,-40.6230116778194));
#64850=CARTESIAN_POINT('Ctrl Pts',(7.88612724313967,0.626875271386329,-40.6223284515789));
#64851=CARTESIAN_POINT('Ctrl Pts',(7.88553881639428,0.634234243475945,-40.6220307752064));
#64852=CARTESIAN_POINT('Ctrl Pts',(7.88430985428062,0.649337747093043,-40.6214190609975));
#64853=CARTESIAN_POINT('Ctrl Pts',(7.88366820695913,0.657082179199908,-40.6211049869075));
#64854=CARTESIAN_POINT('Ctrl Pts',(7.88200451251843,0.676809048514088,-40.6203039311986));
#64855=CARTESIAN_POINT('Ctrl Pts',(7.88096655331049,0.688790104042845,-40.6198164383797));
#64856=CARTESIAN_POINT('Ctrl Pts',(7.87864554482095,0.714889040092531,-40.6187524379704));
#64857=CARTESIAN_POINT('Ctrl Pts',(7.87735185983723,0.729005921937583,-40.6181756008765));
#64858=CARTESIAN_POINT('Ctrl Pts',(7.87350191834591,0.769809896595038,-40.6165045820007));
#64859=CARTESIAN_POINT('Ctrl Pts',(7.87084794943553,0.796487460580511,-40.6154074865756));
#64860=CARTESIAN_POINT('Ctrl Pts',(7.84072195577667,1.08444570913927,-40.6035186264793));
#64861=CARTESIAN_POINT('Ctrl Pts',(7.8003869403428,1.34420903164681,-40.592384305761));
#64862=CARTESIAN_POINT('Ctrl Pts',(7.67259103952429,1.96242783110019,-40.5653703836025));
#64863=CARTESIAN_POINT('Ctrl Pts',(7.57284101488135,2.31772737091015,-40.5494361751091));
#64864=CARTESIAN_POINT('Ctrl Pts',(7.35996956682926,2.91275300041657,-40.5224569150024));
#64865=CARTESIAN_POINT('Ctrl Pts',(7.25892752640277,3.15614614831353,-40.5113238892242));
#64866=CARTESIAN_POINT('Ctrl Pts',(7.12238311253849,3.44363072547556,-40.4980176937047));
#64867=CARTESIAN_POINT('Ctrl Pts',(7.09831877946582,3.49296497644646,-40.4957281640083));
#64868=CARTESIAN_POINT('Ctrl Pts',(6.89577504042249,3.89746078041413,-40.4768988231518));
#64869=CARTESIAN_POINT('Ctrl Pts',(6.69126657616328,4.2389714793584,-40.4605660371429));
#64870=CARTESIAN_POINT('Ctrl Pts',(6.43079143386363,4.60779355556764,-40.4422461420249));
#64871=CARTESIAN_POINT('Ctrl Pts',(6.39917319302399,4.65160428353957,-40.4400594651048));
#64872=CARTESIAN_POINT('Ctrl Pts',(6.35081871105179,4.71717882508442,-40.4367704530723));
#64873=CARTESIAN_POINT('Ctrl Pts',(6.33441400633733,4.73918490580629,-40.4356639256815));
#64874=CARTESIAN_POINT('Ctrl Pts',(6.30566793187097,4.77733039389061,-40.4337409891041));
#64875=CARTESIAN_POINT('Ctrl Pts',(6.29337831452153,4.79350843876057,-40.432923903403));
#64876=CARTESIAN_POINT('Ctrl Pts',(6.26754589871677,4.82724362936544,-40.4312168245302));
#64877=CARTESIAN_POINT('Ctrl Pts',(6.25399132618685,4.84479154818442,-40.4303269999983));
#64878=CARTESIAN_POINT('Ctrl Pts',(6.2215582331757,4.88641691385109,-40.4282117681163));
#64879=CARTESIAN_POINT('Ctrl Pts',(6.20261343387411,4.91044231248741,-40.4269872982482));
#64880=CARTESIAN_POINT('Ctrl Pts',(6.13793702241006,4.99149208024213,-40.4228440958205));
#64881=CARTESIAN_POINT('Ctrl Pts',(6.09155440947989,5.04799257975371,-40.4199348036114));
#64882=CARTESIAN_POINT('Ctrl Pts',(5.86635486834498,5.31469262296304,-40.406094940282));
#64883=CARTESIAN_POINT('Ctrl Pts',(5.67740130990779,5.51608529848486,-40.3953281644438));
#64884=CARTESIAN_POINT('Ctrl Pts',(5.14107604971754,6.03090110012436,-40.3665812496767));
#64885=CARTESIAN_POINT('Ctrl Pts',(4.77582654299774,6.32407255768823,-40.3488710249984));
#64886=CARTESIAN_POINT('Ctrl Pts',(4.28974959174131,6.64797588203683,-40.3259797207577));
#64887=CARTESIAN_POINT('Ctrl Pts',(4.1912355399102,6.71051999702798,-40.3213688298057));
#64888=CARTESIAN_POINT('Ctrl Pts',(4.07230449253366,6.78238554303078,-40.315807063516));
#64889=CARTESIAN_POINT('Ctrl Pts',(4.05318435206589,6.79382912205043,-40.3149130437107));
#64890=CARTESIAN_POINT('Ctrl Pts',(4.02331900479149,6.81153285413725,-40.3135165805301));
#64891=CARTESIAN_POINT('Ctrl Pts',(4.01260699002138,6.81784869145547,-40.3130157093874));
#64892=CARTESIAN_POINT('Ctrl Pts',(3.99326407303528,6.82919195878064,-40.3121113234708));
#64893=CARTESIAN_POINT('Ctrl Pts',(3.98463844732899,6.83422835514391,-40.3117080459762));
#64894=CARTESIAN_POINT('Ctrl Pts',(3.96493868402577,6.84568083059403,-40.3107870752994));
#64895=CARTESIAN_POINT('Ctrl Pts',(3.95385847661961,6.85208639378673,-40.3102691153952));
#64896=CARTESIAN_POINT('Ctrl Pts',(3.92300963252268,6.86982063524985,-40.3088272184641));
#64897=CARTESIAN_POINT('Ctrl Pts',(3.9032075719456,6.8810908132513,-40.3079018562612));
#64898=CARTESIAN_POINT('Ctrl Pts',(3.78974949869452,6.94501719558232,-40.3026016574966));
#64899=CARTESIAN_POINT('Ctrl Pts',(3.69507828950515,6.99584597562974,-40.2981860487181));
#64900=CARTESIAN_POINT('Ctrl Pts',(3.27083592900838,7.21260645710959,-40.278476415239));
#64901=CARTESIAN_POINT('Ctrl Pts',(2.93092971118178,7.35728937334601,-40.2629078050704));
#64902=CARTESIAN_POINT('Ctrl Pts',(2.17418842772657,7.61860388962891,-40.2293344260413));
#64903=CARTESIAN_POINT('Ctrl Pts',(1.7553462493612,7.72586583785553,-40.211434790284));
#64904=CARTESIAN_POINT('Ctrl Pts',(1.27823873834105,7.80722528306463,-40.1917919286573));
#64905=CARTESIAN_POINT('Ctrl Pts',(1.22655334363743,7.81551200072618,-40.1896730286218));
#64906=CARTESIAN_POINT('Ctrl Pts',(1.14205828081036,7.82820026321815,-40.1862229450668));
#64907=CARTESIAN_POINT('Ctrl Pts',(1.10929665281381,7.83290989512358,-40.1848886233092));
#64908=CARTESIAN_POINT('Ctrl Pts',(1.05054536920667,7.84097966552636,-40.1825015977743));
#64909=CARTESIAN_POINT('Ctrl Pts',(1.0245667795969,7.84441652435373,-40.1814481347195));
#64910=CARTESIAN_POINT('Ctrl Pts',(0.969267068633086,7.85145305060143,-40.1792098067353));
#64911=CARTESIAN_POINT('Ctrl Pts',(0.939941876738519,7.85501769139072,-40.1780253041434));
#64912=CARTESIAN_POINT('Ctrl Pts',(0.860551000913941,7.86421714103228,-40.174824892798));
#64913=CARTESIAN_POINT('Ctrl Pts',(0.810450232133061,7.86953808830135,-40.1728120465091));
#64914=CARTESIAN_POINT('Ctrl Pts',(0.557865441654368,7.89392612766439,-40.1626950192012));
#64915=CARTESIAN_POINT('Ctrl Pts',(0.354748409626442,7.90565863400223,-40.1546558608531));
#64916=CARTESIAN_POINT('Ctrl Pts',(-0.206941258283457,7.91641049302499,
-40.1325703480023));
#64917=CARTESIAN_POINT('Ctrl Pts',(-0.565346974519267,7.89890987858248,
-40.1187109082741));
#64918=CARTESIAN_POINT('Ctrl Pts',(-1.54237812293619,7.78434214235141,-40.081426527625));
#64919=CARTESIAN_POINT('Ctrl Pts',(-2.15255149708795,7.63815174885554,-40.0588693548574));
#64920=CARTESIAN_POINT('Ctrl Pts',(-2.77206934745137,7.40950650078815,-40.0336424348689));
#64921=CARTESIAN_POINT('Ctrl Pts',(-2.80494398026005,7.39712405551427,-40.0322957283807));
#64922=CARTESIAN_POINT('Ctrl Pts',(-2.8490165421248,7.38018778990801,-40.0304783840893));
#64923=CARTESIAN_POINT('Ctrl Pts',(-2.86028825044234,7.37582661094145,-40.0300125397745));
#64924=CARTESIAN_POINT('Ctrl Pts',(-2.87959047288601,7.36830741555266,-40.0292129428926));
#64925=CARTESIAN_POINT('Ctrl Pts',(-2.88762590664674,7.36516205418619,-40.0288795196797));
#64926=CARTESIAN_POINT('Ctrl Pts',(-2.9206916710006,7.35215647986442,-40.0275051503301));
#64927=CARTESIAN_POINT('Ctrl Pts',(-2.94567665703891,7.34218181187786,-40.0264611422381));
#64928=CARTESIAN_POINT('Ctrl Pts',(-3.04979054553636,7.29999981500444,-40.0220860566482));
#64929=CARTESIAN_POINT('Ctrl Pts',(-3.12844458258924,7.26663977228303,-40.0187212650157));
#64930=CARTESIAN_POINT('Ctrl Pts',(-3.219745101746,7.22615880643598,-40.0147306421476));
#64931=CARTESIAN_POINT('Ctrl Pts',(-3.23293287610872,7.22026832128495,-40.0141521318089));
#64932=CARTESIAN_POINT('Ctrl Pts',(-3.25399979638979,7.21078922747734,-40.013224537516));
#64933=CARTESIAN_POINT('Ctrl Pts',(-3.26188934387766,7.20722372800899,-40.0128763784793));
#64934=CARTESIAN_POINT('Ctrl Pts',(-3.27583979412024,7.20089154427038,-40.0122593593607));
#64935=CARTESIAN_POINT('Ctrl Pts',(-3.28190309245019,7.19813013778664,-40.0119907156508));
#64936=CARTESIAN_POINT('Ctrl Pts',(-3.29354234473155,7.19281151248553,-40.0114741092385));
#64937=CARTESIAN_POINT('Ctrl Pts',(-3.29911882860543,7.19025546035431,-40.0112261953097));
#64938=CARTESIAN_POINT('Ctrl Pts',(-3.31390259975156,7.18345831201984,-40.0105678713862));
#64939=CARTESIAN_POINT('Ctrl Pts',(-3.32310470007956,7.17920600848224,-40.0101569864204));
#64940=CARTESIAN_POINT('Ctrl Pts',(-3.35665045919183,7.16362615040749,-40.0086549789998));
#64941=CARTESIAN_POINT('Ctrl Pts',(-3.38094440406278,7.15219244988336,-40.0075592371313));
#64942=CARTESIAN_POINT('Ctrl Pts',(-3.43941617011596,7.12430881686727,-40.0049016447652));
#64943=CARTESIAN_POINT('Ctrl Pts',(-3.47353457567281,7.10773643192132,-40.003334092941));
#64944=CARTESIAN_POINT('Ctrl Pts',(-3.59947340678139,7.04544063514227,-39.9974808815868));
#64945=CARTESIAN_POINT('Ctrl Pts',(-3.69051730429007,6.9981799515626,-39.9931152838472));
#64946=CARTESIAN_POINT('Ctrl Pts',(-3.93059416943244,6.86756892209665,-39.9812867750648));
#64947=CARTESIAN_POINT('Ctrl Pts',(-4.07788928558076,6.78114206576112,-39.9736973323876));
#64948=CARTESIAN_POINT('Ctrl Pts',(-4.87654415300198,6.27708782578244,-39.9310801982133));
#64949=CARTESIAN_POINT('Ctrl Pts',(-5.46683546790264,5.77031334956111,-39.8944765460214));
#64950=CARTESIAN_POINT('Ctrl Pts',(-6.11642704986206,5.02198739181439,-39.8519133279298));
#64951=CARTESIAN_POINT('Ctrl Pts',(-6.2519177081555,4.85227488285968,-39.8428363942572));
#64952=CARTESIAN_POINT('Ctrl Pts',(-6.39335673692499,4.65933482988213,-39.8331259105448));
#64953=CARTESIAN_POINT('Ctrl Pts',(-6.40637475313049,4.64141939011161,-39.8322297800548));
#64954=CARTESIAN_POINT('Ctrl Pts',(-6.42565581552434,4.61464906162792,-39.8308989065396));
#64955=CARTESIAN_POINT('Ctrl Pts',(-6.43197610640599,4.60583564506453,-39.8304620645509));
#64956=CARTESIAN_POINT('Ctrl Pts',(-6.44279370922174,4.59068519973505,-39.8297133673501));
#64957=CARTESIAN_POINT('Ctrl Pts',(-6.44729983684922,4.58435450165353,-39.8294011899437));
#64958=CARTESIAN_POINT('Ctrl Pts',(-6.45654686876411,4.57132266553615,-39.8287599411487));
#64959=CARTESIAN_POINT('Ctrl Pts',(-6.46128668659713,4.56462076574895,-39.8284309095784));
#64960=CARTESIAN_POINT('Ctrl Pts',(-6.47223760445543,4.5490854024422,-39.827669914031));
#64961=CARTESIAN_POINT('Ctrl Pts',(-6.47844107243326,4.54024656592385,-39.8272382280842));
#64962=CARTESIAN_POINT('Ctrl Pts',(-6.4979249363231,4.51236429612383,-39.8258804857053));
#64963=CARTESIAN_POINT('Ctrl Pts',(-6.51113966176919,4.49327501218704,-39.8249568118256));
#64964=CARTESIAN_POINT('Ctrl Pts',(-6.70826564474867,4.20582162245222,-39.8111352178431));
#64965=CARTESIAN_POINT('Ctrl Pts',(-6.8755430524976,3.9264101354522,-39.7988574987771));
#64966=CARTESIAN_POINT('Ctrl Pts',(-7.38248377374669,2.9473413829766,-39.7587748485092));
#64967=CARTESIAN_POINT('Ctrl Pts',(-7.63614189350831,2.20840374459733,-39.7336235632478));
#64968=CARTESIAN_POINT('Ctrl Pts',(-7.78395816519833,1.41243584266472,-39.7038423927743));
#64969=CARTESIAN_POINT('Ctrl Pts',(-7.78970164853697,1.38040860688653,-39.702639100945));
#64970=CARTESIAN_POINT('Ctrl Pts',(-7.7990957047587,1.32609841331165,-39.7005890243852));
#64971=CARTESIAN_POINT('Ctrl Pts',(-7.80284877796693,1.30383348262326,-39.6997458532954));
#64972=CARTESIAN_POINT('Ctrl Pts',(-7.8073949721912,1.27614059995982,-39.698693459307));
#64973=CARTESIAN_POINT('Ctrl Pts',(-7.80827785336296,1.27072736931404,-39.6984875699799));
#64974=CARTESIAN_POINT('Ctrl Pts',(-7.81070562765827,1.25574383358761,-39.6979171888144));
#64975=CARTESIAN_POINT('Ctrl Pts',(-7.81223855733062,1.24617161735705,-39.6975522479067));
#64976=CARTESIAN_POINT('Ctrl Pts',(-7.83484572431392,1.10332241804954,-39.6920975951547));
#64977=CARTESIAN_POINT('Ctrl Pts',(-7.85252411320311,0.969532303097608,
-39.6868765365133));
#64978=CARTESIAN_POINT('Ctrl Pts',(-7.86840140557257,0.820011204379038,
-39.6808683304173));
#64979=CARTESIAN_POINT('Ctrl Pts',(-7.86998571960172,0.804663794838905,
-39.6802497281055));
#64980=CARTESIAN_POINT('Ctrl Pts',(-7.87224516436768,0.782131161641253,
-39.6793388277476));
#64981=CARTESIAN_POINT('Ctrl Pts',(-7.87295538323075,0.774949427428805,
-39.6790480999309));
#64982=CARTESIAN_POINT('Ctrl Pts',(-7.87419962718364,0.762189368993637,
-39.6785308539216));
#64983=CARTESIAN_POINT('Ctrl Pts',(-7.87473755481492,0.756611423056453,
-39.6783045072469));
#64984=CARTESIAN_POINT('Ctrl Pts',(-7.87576392313471,0.745849009109519,
-39.6778673293359));
#64985=CARTESIAN_POINT('Ctrl Pts',(-7.87625317258029,0.740664619496111,
-39.6776565332134));
#64986=CARTESIAN_POINT('Ctrl Pts',(-7.87729241098965,0.729534730686895,
-39.6772035661759));
#64987=CARTESIAN_POINT('Ctrl Pts',(-7.87784078822961,0.723589086806906,
-39.6769613265918));
#64988=CARTESIAN_POINT('Ctrl Pts',(-7.87914725952928,0.709246464024163,
-39.676376350878));
#64989=CARTESIAN_POINT('Ctrl Pts',(-7.87989866121983,0.7008488939964,-39.6760333338132));
#64990=CARTESIAN_POINT('Ctrl Pts',(-7.88189437793506,0.678136041678968,
-39.6751042134066));
#64991=CARTESIAN_POINT('Ctrl Pts',(-7.88311311339261,0.663818584941344,
-39.6745170602974));
#64992=CARTESIAN_POINT('Ctrl Pts',(-7.90192929177044,0.435407918223026,
-39.6651274982165));
#64993=CARTESIAN_POINT('Ctrl Pts',(-7.91083737108919,0.220699508074797,
-39.6559883201535));
#64994=CARTESIAN_POINT('Ctrl Pts',(-7.91099779352309,0.00590854236546028,
-39.6466906819873));
#64995=CARTESIAN_POINT('',(-7.91099999260968,0.000341949715757575,-37.6423315082368));
#64996=CARTESIAN_POINT('Ctrl Pts',(-7.91099765047707,0.00609706046871071,
-39.6423315082368));
#64997=CARTESIAN_POINT('Ctrl Pts',(-7.91114330160451,-0.182886751144705,
-39.6347110559693));
#64998=CARTESIAN_POINT('Ctrl Pts',(-7.90451297234196,-0.372147225623654,
-39.6270906037017));
#64999=CARTESIAN_POINT('Ctrl Pts',(-7.89107380823835,-0.561137374387657,
-39.6194701514342));
#65000=CARTESIAN_POINT('Ctrl Pts',(-7.87764520868798,-0.749978957625515,
-39.6118556896191));
#65001=CARTESIAN_POINT('Ctrl Pts',(-7.85741844921442,-0.938550270991757,
-39.6042412278041));
#65002=CARTESIAN_POINT('Ctrl Pts',(-7.83041270643092,-1.12630273326724,
-39.596626765989));
#65003=CARTESIAN_POINT('Ctrl Pts',(-7.80342401238723,-1.3139366673132,-39.5890171111878));
#65004=CARTESIAN_POINT('Ctrl Pts',(-7.76966490711269,-1.50075241408661,
-39.5814074563865));
#65005=CARTESIAN_POINT('Ctrl Pts',(-7.72920651725325,-1.68620509240422,
-39.5737978015853));
#65006=CARTESIAN_POINT('Ctrl Pts',(-7.68876294287454,-1.87158985970036,
-39.5661909333678));
#65007=CARTESIAN_POINT('Ctrl Pts',(-7.64162504534338,-2.05561219066511,
-39.5585840651504));
#65008=CARTESIAN_POINT('Ctrl Pts',(-7.58791530460303,-2.2377359831247,-39.5509771969329));
#65009=CARTESIAN_POINT('Ctrl Pts',(-7.53421063202268,-2.4198425900141,-39.543371046515));
#65010=CARTESIAN_POINT('Ctrl Pts',(-7.47393545193249,-2.60005065878146,
-39.535764896097));
#65011=CARTESIAN_POINT('Ctrl Pts',(-7.40726250799875,-2.77783785300656,
-39.5281587456791));
#65012=CARTESIAN_POINT('Ctrl Pts',(-7.38187403647389,-2.84553765523149,
-39.5252623903975));
#65013=CARTESIAN_POINT('Ctrl Pts',(-7.35555838855058,-2.91288659458526,
-39.522366035116));
#65014=CARTESIAN_POINT('Ctrl Pts',(-7.32832696856371,-2.97985651362978,
-39.5194696798344));
#65015=CARTESIAN_POINT('Ctrl Pts',(-7.24822733924639,-3.17684461390011,
-39.5109502201611));
#65016=CARTESIAN_POINT('Ctrl Pts',(-7.1602564859085,-3.37041596226114,-39.5024307604878));
#65017=CARTESIAN_POINT('Ctrl Pts',(-7.06473739458507,-3.55997282932768,
-39.4939113008145));
#65018=CARTESIAN_POINT('Ctrl Pts',(-6.96904628063741,-3.74987107390593,
-39.4853764982418));
#65019=CARTESIAN_POINT('Ctrl Pts',(-6.86577987219144,-3.93574016488276,
-39.4768416956691));
#65020=CARTESIAN_POINT('Ctrl Pts',(-6.75530589298582,-4.11700902260257,
-39.4683068930964));
#65021=CARTESIAN_POINT('Ctrl Pts',(-6.63924079654431,-4.30745194503894,
-39.4593401419136));
#65022=CARTESIAN_POINT('Ctrl Pts',(-6.51521994139232,-4.49281668990722,
-39.4503733907308));
#65023=CARTESIAN_POINT('Ctrl Pts',(-6.3837177659858,-4.67247990731231,-39.441406639548));
#65024=CARTESIAN_POINT('Ctrl Pts',(-6.25802762523127,-4.84420250440433,
-39.4328361941178));
#65025=CARTESIAN_POINT('Ctrl Pts',(-6.125503364898,-5.01071652534564,-39.4242657486876));
#65026=CARTESIAN_POINT('Ctrl Pts',(-5.9865983332433,-5.17151442001359,-39.4156953032573));
#65027=CARTESIAN_POINT('Ctrl Pts',(-5.84751972121477,-5.33251325310929,
-39.4071141479118));
#65028=CARTESIAN_POINT('Ctrl Pts',(-5.70204457486867,-5.4877815046477,-39.3985329925663));
#65029=CARTESIAN_POINT('Ctrl Pts',(-5.55066330241482,-5.63684822424956,
-39.3899518372208));
#65030=CARTESIAN_POINT('Ctrl Pts',(-5.39903015939884,-5.78616296342381,
-39.3813564044129));
#65031=CARTESIAN_POINT('Ctrl Pts',(-5.2414714220748,-5.9292553673493,-39.3727609716051));
#65032=CARTESIAN_POINT('Ctrl Pts',(-5.07851243344497,-6.06569307361862,
-39.3641655387972));
#65033=CARTESIAN_POINT('Ctrl Pts',(-5.05664878058053,-6.08399845629541,
-39.3630123188324));
#65034=CARTESIAN_POINT('Ctrl Pts',(-5.03468796465651,-6.10218411204924,
-39.3618590988676));
#65035=CARTESIAN_POINT('Ctrl Pts',(-5.01263129570722,-6.12024905484218,
-39.3607058789028));
#65036=CARTESIAN_POINT('Ctrl Pts',(-4.86136202219078,-6.24414223103694,
-39.3527968538963));
#65037=CARTESIAN_POINT('Ctrl Pts',(-4.70530392627715,-6.36258181591704,
-39.3448878288898));
#65038=CARTESIAN_POINT('Ctrl Pts',(-4.54488693057181,-6.4751775101782,-39.3369788038834));
#65039=CARTESIAN_POINT('Ctrl Pts',(-4.3846334554305,-6.58765843036975,-39.3290778409169));
#65040=CARTESIAN_POINT('Ctrl Pts',(-4.22003021091666,-6.69430712920731,
-39.3211768779504));
#65041=CARTESIAN_POINT('Ctrl Pts',(-4.05154106789086,-6.79477269488787,
-39.3132759149839));
#65042=CARTESIAN_POINT('Ctrl Pts',(-3.88319241760989,-6.89515448850556,
-39.305381540145));
#65043=CARTESIAN_POINT('Ctrl Pts',(-3.71096461826943,-6.98936324436329,
-39.297487165306));
#65044=CARTESIAN_POINT('Ctrl Pts',(-3.53535170331116,-7.07709045681168,
-39.2895927904671));
#65045=CARTESIAN_POINT('Ctrl Pts',(-3.35985265248481,-7.1647607885751,-39.2817035341933));
#65046=CARTESIAN_POINT('Ctrl Pts',(-3.18097316639855,-7.24595779649179,
-39.2738142779195));
#65047=CARTESIAN_POINT('Ctrl Pts',(-2.99923338572382,-7.32041802754185,
-39.2659250216457));
#65048=CARTESIAN_POINT('Ctrl Pts',(-2.81757774346421,-7.39484378641522,
-39.2580394177892));
#65049=CARTESIAN_POINT('Ctrl Pts',(-2.63306476376436,-7.46253885294553,
-39.2501538139328));
#65050=CARTESIAN_POINT('Ctrl Pts',(-2.44623640628078,-7.52328707710841,
-39.2422682100763));
#65051=CARTESIAN_POINT('Ctrl Pts',(-2.24969869307562,-7.58719234940788,
-39.2339727961997));
#65052=CARTESIAN_POINT('Ctrl Pts',(-2.0505989028863,-7.6434093441205,-39.2256773823232));
#65053=CARTESIAN_POINT('Ctrl Pts',(-1.84958913357896,-7.69174499297439,
-39.2173819684467));
#65054=CARTESIAN_POINT('Ctrl Pts',(-1.65854121144815,-7.7376851744402,-39.2094976671524));
#65055=CARTESIAN_POINT('Ctrl Pts',(-1.46576840672236,-7.77650619550339,
-39.201613365858));
#65056=CARTESIAN_POINT('Ctrl Pts',(-1.27184360280945,-7.8080941880841,-39.1937290645637));
#65057=CARTESIAN_POINT('Ctrl Pts',(-1.0778935148621,-7.83968629912659,-39.1858437353093));
#65058=CARTESIAN_POINT('Ctrl Pts',(-0.882791468855304,-7.8640434464469,
-39.177958406055));
#65059=CARTESIAN_POINT('Ctrl Pts',(-0.687118104711814,-7.88110333076386,
-39.1700730768006));
#65060=CARTESIAN_POINT('Ctrl Pts',(-0.49138635318538,-7.89816830561526,
-39.1621853946264));
#65061=CARTESIAN_POINT('Ctrl Pts',(-0.295083287350566,-7.90793164841032,
-39.1542977124522));
#65062=CARTESIAN_POINT('Ctrl Pts',(-0.0987924503084548,-7.9103831166235,
-39.1464100302781));
#65063=CARTESIAN_POINT('Ctrl Pts',(0.0975899382150019,-7.91283572821937,
-39.1385186692312));
#65064=CARTESIAN_POINT('Ctrl Pts',(0.293959742127451,-7.90796966517475,
-39.1306273081844));
#65065=CARTESIAN_POINT('Ctrl Pts',(0.4897353923057,-7.89582676136725,-39.1227359471376));
#65066=CARTESIAN_POINT('Ctrl Pts',(0.685736641728731,-7.88366986485981,
-39.1148354925948));
#65067=CARTESIAN_POINT('Ctrl Pts',(0.881142025725839,-7.86421940045347,
-39.106935038052));
#65068=CARTESIAN_POINT('Ctrl Pts',(1.07537591434748,-7.8375689880754,-39.0990345835091));
#65069=CARTESIAN_POINT('Ctrl Pts',(1.26973970529285,-7.81090075208004,-39.0911288451952));
#65070=CARTESIAN_POINT('Ctrl Pts',(1.46293010048366,-7.77702302808523,-39.0832231068814));
#65071=CARTESIAN_POINT('Ctrl Pts',(1.6543833391645,-7.73608019394156,-39.0753173685675));
#65072=CARTESIAN_POINT('Ctrl Pts',(1.84609467093527,-7.69508216583697,-39.0674009727351));
#65073=CARTESIAN_POINT('Ctrl Pts',(2.03606383617461,-7.64700008975067,-39.0594845769027));
#65074=CARTESIAN_POINT('Ctrl Pts',(2.22374278064302,-7.59202799293694,-39.0515681810703));
#65075=CARTESIAN_POINT('Ctrl Pts',(2.2900443470788,-7.57260793418003,-39.0487715463935));
#65076=CARTESIAN_POINT('Ctrl Pts',(2.35606027923801,-7.55232843405329,-39.0459749117166));
#65077=CARTESIAN_POINT('Ctrl Pts',(2.42176706436186,-7.53119945865014,-39.0431782770398));
#65078=CARTESIAN_POINT('Ctrl Pts',(2.60412977562313,-7.47255806821491,-39.0354164929088));
#65079=CARTESIAN_POINT('Ctrl Pts',(2.78468143073056,-7.40718596574286,-39.0276547087777));
#65080=CARTESIAN_POINT('Ctrl Pts',(2.96287496700522,-7.3352091265276,-39.0198929246467));
#65081=CARTESIAN_POINT('Ctrl Pts',(3.1408545273114,-7.26331871757352,-39.012140460917));
#65082=CARTESIAN_POINT('Ctrl Pts',(3.31648127664525,-7.18483949068495,-39.0043879971873));
#65083=CARTESIAN_POINT('Ctrl Pts',(3.48922086645204,-7.09994779875991,-38.9966355334577));
#65084=CARTESIAN_POINT('Ctrl Pts',(3.66178806420543,-7.01514082773239,-38.9888908065945));
#65085=CARTESIAN_POINT('Ctrl Pts',(3.83147351918181,-6.92393428806278,-38.9811460797312));
#65086=CARTESIAN_POINT('Ctrl Pts',(3.99776042318241,-6.82655349344282,-38.973401352868));
#65087=CARTESIAN_POINT('Ctrl Pts',(4.16391505251984,-6.72925016139807,-38.9656627866291));
#65088=CARTESIAN_POINT('Ctrl Pts',(4.32667620541288,-6.62578253307438,-38.9579242203902));
#65089=CARTESIAN_POINT('Ctrl Pts',(4.48554927957113,-6.51642299582669,-38.9501856541512));
#65090=CARTESIAN_POINT('Ctrl Pts',(4.64432811995388,-6.40712832395746,-38.9424516779558));
#65091=CARTESIAN_POINT('Ctrl Pts',(4.79922317918888,-6.29194890493478,-38.9347177017603));
#65092=CARTESIAN_POINT('Ctrl Pts',(4.94976651931873,-6.17120186059663,-38.9269837255648));
#65093=CARTESIAN_POINT('Ctrl Pts',(5.10025100350101,-6.0505020231406,-38.9192527730202));
#65094=CARTESIAN_POINT('Ctrl Pts',(5.24638687758578,-5.92423911990399,-38.9115218204755));
#65095=CARTESIAN_POINT('Ctrl Pts',(5.38773707494352,-5.79277223885758,-38.9037908679309));
#65096=CARTESIAN_POINT('Ctrl Pts',(5.52908747092009,-5.66130517307991,-38.8960599045231));
#65097=CARTESIAN_POINT('Ctrl Pts',(5.66565190623245,-5.52463435097297,-38.8883289411152));
#65098=CARTESIAN_POINT('Ctrl Pts',(5.79702787322901,-5.38315788705903,-38.8805979777074));
#65099=CARTESIAN_POINT('Ctrl Pts',(5.92841064115388,-5.24167409934526,-38.8728666140915));
#65100=CARTESIAN_POINT('Ctrl Pts',(6.05460416074512,-5.09538443698233,-38.8651352504756));
#65101=CARTESIAN_POINT('Ctrl Pts',(6.17524428003438,-4.94472234629031,-38.8574038868596));
#65102=CARTESIAN_POINT('Ctrl Pts',(6.29591273538659,-4.79402486794689,-38.8496707072938));
#65103=CARTESIAN_POINT('Ctrl Pts',(6.41102496835412,-4.63895319635809,-38.8419375277281));
#65104=CARTESIAN_POINT('Ctrl Pts',(6.52025842974105,-4.47997221078332,-38.8342043481623));
#65105=CARTESIAN_POINT('Ctrl Pts',(6.62953755649719,-4.3209247627408,-38.8264679357181));
#65106=CARTESIAN_POINT('Ctrl Pts',(6.73293281469685,-4.15796504196802,-38.8187315232739));
#65107=CARTESIAN_POINT('Ctrl Pts',(6.83016609837389,-3.99158515738095,-38.8109951108297));
#65108=CARTESIAN_POINT('Ctrl Pts',(6.92751508747393,-3.82500728446936,-38.8032494922285));
#65109=CARTESIAN_POINT('Ctrl Pts',(7.01868727693405,-3.65500142969943,-38.7955038736273));
#65110=CARTESIAN_POINT('Ctrl Pts',(7.10345101489146,-3.48208338197659,-38.7877582550261));
#65111=CARTESIAN_POINT('Ctrl Pts',(7.18826986520101,-3.30905290504087,-38.7800076003178));
#65112=CARTESIAN_POINT('Ctrl Pts',(7.26667181868098,-3.13310679001022,-38.7722569456096));
#65113=CARTESIAN_POINT('Ctrl Pts',(7.3384742033577,-2.95477873395853,-38.7645062909013));
#65114=CARTESIAN_POINT('Ctrl Pts',(7.41038566743114,-2.7761797688436,-38.7567438616992));
#65115=CARTESIAN_POINT('Ctrl Pts',(7.47567741825765,-2.59519197199196,-38.748981432497));
#65116=CARTESIAN_POINT('Ctrl Pts',(7.53421693182173,-2.4123632032202,-38.7412190032949));
#65117=CARTESIAN_POINT('Ctrl Pts',(7.57335254823366,-2.29013607613814,-38.7360295605888));
#65118=CARTESIAN_POINT('Ctrl Pts',(7.60947139783775,-2.16708638633235,-38.7308401178828));
#65119=CARTESIAN_POINT('Ctrl Pts',(7.64254676158435,-2.04337955284782,-38.7256506751768));
#65120=CARTESIAN_POINT('Ctrl Pts',(7.69362905697515,-1.85232408756769,-38.7176359894652));
#65121=CARTESIAN_POINT('Ctrl Pts',(7.7376057576374,-1.65911698728575,-38.7096213037537));
#65122=CARTESIAN_POINT('Ctrl Pts',(7.77429613102985,-1.46432259664815,-38.7016066180422));
#65123=CARTESIAN_POINT('Ctrl Pts',(7.81094479234527,-1.26974966133722,-38.6936010439628));
#65124=CARTESIAN_POINT('Ctrl Pts',(7.84032357099007,-1.07359335731651,-38.6855954698835));
#65125=CARTESIAN_POINT('Ctrl Pts',(7.86230162724109,-0.876432611375287,
-38.6775898958042));
#65126=CARTESIAN_POINT('Ctrl Pts',(7.88425842429107,-0.679462577473684,
-38.6695920654537));
#65127=CARTESIAN_POINT('Ctrl Pts',(7.89882872813028,-0.481490368201534,
-38.6615942351033));
#65128=CARTESIAN_POINT('Ctrl Pts',(7.90593274707188,-0.283104925383739,
-38.6535964047528));
#65129=CARTESIAN_POINT('Ctrl Pts',(7.9130310982357,-0.084877759818765,-38.645604955287));
#65130=CARTESIAN_POINT('Ctrl Pts',(7.91267502487342,0.113761649406268,-38.6376135058211));
#65131=CARTESIAN_POINT('Ctrl Pts',(7.90483651293712,0.312218999639936,-38.6296220563553));
#65132=CARTESIAN_POINT('Ctrl Pts',(7.89700292713308,0.510551628859768,-38.6216356291356));
#65133=CARTESIAN_POINT('Ctrl Pts',(7.88169628922905,0.708702093908644,-38.613649201916));
#65134=CARTESIAN_POINT('Ctrl Pts',(7.85894066079851,0.906075432868546,-38.6056627746964));
#65135=CARTESIAN_POINT('Ctrl Pts',(7.83548868449896,1.10948861838344,-38.5974319538054));
#65136=CARTESIAN_POINT('Ctrl Pts',(7.80412457699479,1.31207599825623,-38.5892011329145));
#65137=CARTESIAN_POINT('Ctrl Pts',(7.76493252859522,1.51318995052302,-38.5809703120236));
#65138=CARTESIAN_POINT('Ctrl Pts',(7.72692975904522,1.70820111971135,-38.5729892545821));
#65139=CARTESIAN_POINT('Ctrl Pts',(7.68156724094024,1.9018266242896,-38.5650081971406));
#65140=CARTESIAN_POINT('Ctrl Pts',(7.62897396363313,2.0934844786164,-38.5570271396992));
#65141=CARTESIAN_POINT('Ctrl Pts',(7.57638479645517,2.28512735501116,-38.5490467059719));
#65142=CARTESIAN_POINT('Ctrl Pts',(7.51656608476441,2.47480256510407,-38.5410662722447));
#65143=CARTESIAN_POINT('Ctrl Pts',(7.44969719269671,2.66194153525707,-38.5330858385175));
#65144=CARTESIAN_POINT('Ctrl Pts',(7.38282326122531,2.84909460866182,-38.5251048033652));
#65145=CARTESIAN_POINT('Ctrl Pts',(7.30889820321929,3.0337107462913,-38.5171237682129));
#65146=CARTESIAN_POINT('Ctrl Pts',(7.22815033052729,3.21523930669214,-38.5091427330607));
#65147=CARTESIAN_POINT('Ctrl Pts',(7.14738397653984,3.39680941472572,-38.5011598712365));
#65148=CARTESIAN_POINT('Ctrl Pts',(7.05979183164243,3.57529023167102,-38.4931770094123));
#65149=CARTESIAN_POINT('Ctrl Pts',(6.96564931355491,3.75015341560475,-38.4851941475882));
#65150=CARTESIAN_POINT('Ctrl Pts',(6.87143693663302,3.92514635746778,-38.4772053620493));
#65151=CARTESIAN_POINT('Ctrl Pts',(6.77066463560454,4.09651600926776,-38.4692165765104));
#65152=CARTESIAN_POINT('Ctrl Pts',(6.66365304698806,4.26375996854499,-38.4612277909715));
#65153=CARTESIAN_POINT('Ctrl Pts',(6.55659426377389,4.43107768629526,-38.4532354821925));
#65154=CARTESIAN_POINT('Ctrl Pts',(6.44329089350447,4.59426580675474,-38.4452431734135));
#65155=CARTESIAN_POINT('Ctrl Pts',(6.32410577346231,4.75285252938282,-38.4372508646345));
#65156=CARTESIAN_POINT('Ctrl Pts',(6.20480913217169,4.91158764125019,-38.4292510774702));
#65157=CARTESIAN_POINT('Ctrl Pts',(6.07961995739964,5.06571249501295,-38.4212512903059));
#65158=CARTESIAN_POINT('Ctrl Pts',(5.94894069895238,5.21478911945133,-38.4132515031416));
#65159=CARTESIAN_POINT('Ctrl Pts',(5.92101581407187,5.24664534227721,-38.4115420265323));
#65160=CARTESIAN_POINT('Ctrl Pts',(5.8928403652959,5.27827118024825,-38.409832549923));
#65161=CARTESIAN_POINT('Ctrl Pts',(5.86441849184323,5.30966258367961,-38.4081230733138));
#65162=CARTESIAN_POINT('Ctrl Pts',(5.72929214138113,5.45890699533412,-38.3999956943851));
#65163=CARTESIAN_POINT('Ctrl Pts',(5.58835543949867,5.6031116452127,-38.3918683154565));
#65164=CARTESIAN_POINT('Ctrl Pts',(5.44201034328428,5.74181542925118,-38.3837409365279));
#65165=CARTESIAN_POINT('Ctrl Pts',(5.2957895315639,5.8804014182281,-38.375620459827));
#65166=CARTESIAN_POINT('Ctrl Pts',(5.14416971282125,6.01349563669138,-38.3674999831261));
#65167=CARTESIAN_POINT('Ctrl Pts',(4.9875910098358,6.14067235069623,-38.3593795064252));
#65168=CARTESIAN_POINT('Ctrl Pts',(4.83112559544692,6.2677570491768,-38.3512649050917));
#65169=CARTESIAN_POINT('Ctrl Pts',(4.66970869721374,6.38893257959597,-38.3431503037582));
#65170=CARTESIAN_POINT('Ctrl Pts',(4.50381539255678,6.50381179845855,-38.3350357024247));
#65171=CARTESIAN_POINT('Ctrl Pts',(4.33803961153578,6.61860963354542,-38.3269268497105));
#65172=CARTESIAN_POINT('Ctrl Pts',(4.16779401220337,6.72711987488408,-38.3188179969963));
#65173=CARTESIAN_POINT('Ctrl Pts',(3.99358497150644,6.82899700361319,-38.3107091442821));
#65174=CARTESIAN_POINT('Ctrl Pts',(3.81945053928184,6.93083050144399,-38.3026037643447));
#65175=CARTESIAN_POINT('Ctrl Pts',(3.64135632485281,7.02603639028042,-38.2944983844073));
#65176=CARTESIAN_POINT('Ctrl Pts',(3.45983650205037,7.11431320501704,-38.2863930044699));
#65177=CARTESIAN_POINT('Ctrl Pts',(3.27837328238472,7.20256249248671,-38.2782901520247));
#65178=CARTESIAN_POINT('Ctrl Pts',(3.09348687109394,7.28388687586475,-38.2701872995794));
#65179=CARTESIAN_POINT('Ctrl Pts',(2.90573528503304,7.35803122127883,-38.2620844471342));
#65180=CARTESIAN_POINT('Ctrl Pts',(2.80745007174017,7.39684470326517,-38.2578427222169));
#65181=CARTESIAN_POINT('Ctrl Pts',(2.70838007268159,7.43369136736052,-38.2536009972996));
#65182=CARTESIAN_POINT('Ctrl Pts',(2.60860759688772,7.46853984427075,-38.2493592723822));
#65183=CARTESIAN_POINT('Ctrl Pts',(2.41363851383687,7.53663854117933,-38.2410703609254));
#65184=CARTESIAN_POINT('Ctrl Pts',(2.21606962171687,7.59707469984934,-38.2327814494686));
#65185=CARTESIAN_POINT('Ctrl Pts',(2.01651896469399,7.64967791903878,-38.2244925380117));
#65186=CARTESIAN_POINT('Ctrl Pts',(1.81685357638307,7.70231138235361,-38.2161988608603));
#65187=CARTESIAN_POINT('Ctrl Pts',(1.61520443171274,7.74710284233969,-38.2079051837089));
#65188=CARTESIAN_POINT('Ctrl Pts',(1.41220107318992,7.78393275464795,-38.1996115065575));
#65189=CARTESIAN_POINT('Ctrl Pts',(1.2090687712019,7.82078606054216,-38.1913125614367));
#65190=CARTESIAN_POINT('Ctrl Pts',(1.00458082601934,7.84966767223038,-38.1830136163159));
#65191=CARTESIAN_POINT('Ctrl Pts',(0.799374070348638,7.8705096465003,-38.1747146711952));
#65192=CARTESIAN_POINT('Ctrl Pts',(0.593929230478708,7.8913758019661,-38.1664060975039));
#65193=CARTESIAN_POINT('Ctrl Pts',(0.387764204450145,7.90418364551509,-38.1580975238127));
#65194=CARTESIAN_POINT('Ctrl Pts',(0.181519753465613,7.90891721913321,-38.1497889501215));
#65195=CARTESIAN_POINT('Ctrl Pts',(-0.0248516342685485,7.91365370611189,
-38.1414752627734));
#65196=CARTESIAN_POINT('Ctrl Pts',(-0.231302252182532,7.91030600339276,
-38.1331615754254));
#65197=CARTESIAN_POINT('Ctrl Pts',(-0.43719284541712,7.89891026762022,-38.1248478880774));
#65198=CARTESIAN_POINT('Ctrl Pts',(-0.643307520746114,7.88750212923957,
-38.1165251524847));
#65199=CARTESIAN_POINT('Ctrl Pts',(-0.848860661520386,7.86802847371838,
-38.1082024168919));
#65200=CARTESIAN_POINT('Ctrl Pts',(-1.05321799701201,7.84057732891973,-38.0998796812992));
#65201=CARTESIAN_POINT('Ctrl Pts',(-1.12920648924262,7.83036986023144,-38.096784944683));
#65202=CARTESIAN_POINT('Ctrl Pts',(-1.20502973461416,7.81905988640283,-38.0936902080669));
#65203=CARTESIAN_POINT('Ctrl Pts',(-1.28065549613145,7.80665373256867,-38.0905954714507));
#65204=CARTESIAN_POINT('Ctrl Pts',(-1.49318710159551,7.77178863185289,-38.0818983115369));
#65205=CARTESIAN_POINT('Ctrl Pts',(-1.70434647359446,7.72823160532294,-38.0732011516231));
#65206=CARTESIAN_POINT('Ctrl Pts',(-1.91344654627575,7.67610860492121,-38.0645039917092));
#65207=CARTESIAN_POINT('Ctrl Pts',(-2.12236348806853,7.62403125410368,-38.0558144488115));
#65208=CARTESIAN_POINT('Ctrl Pts',(-2.32922450981592,7.56340296467206,-38.0471249059138));
#65209=CARTESIAN_POINT('Ctrl Pts',(-2.53335406831927,7.4944004539743,-38.0384353630161));
#65210=CARTESIAN_POINT('Ctrl Pts',(-2.74204326463621,7.42385663559275,-38.0295517219747));
#65211=CARTESIAN_POINT('Ctrl Pts',(-2.94787731222795,7.34456015467706,-38.0206680809332));
#65212=CARTESIAN_POINT('Ctrl Pts',(-3.1501485870133,7.25675443154432,-38.0117844398918));
#65213=CARTESIAN_POINT('Ctrl Pts',(-3.34742030639273,7.17111900954913,-38.0031203765222));
#65214=CARTESIAN_POINT('Ctrl Pts',(-3.54130303678552,7.07739006003169,-37.9944563131526));
#65215=CARTESIAN_POINT('Ctrl Pts',(-3.73115693726987,6.97584324002933,-37.9857922497831));
#65216=CARTESIAN_POINT('Ctrl Pts',(-3.92822818064668,6.87043609259769,-37.9767988199057));
#65217=CARTESIAN_POINT('Ctrl Pts',(-4.12095806562072,6.75660511920194,-37.9678053900284));
#65218=CARTESIAN_POINT('Ctrl Pts',(-4.30865354453088,6.63471368132804,-37.9588119601511));
#65219=CARTESIAN_POINT('Ctrl Pts',(-4.49634902344105,6.51282224345414,-37.9498185302738));
#65220=CARTESIAN_POINT('Ctrl Pts',(-4.67900982833887,6.38287043622605,-37.9408251003964));
#65221=CARTESIAN_POINT('Ctrl Pts',(-4.85596988937692,6.24527640969274,-37.9318316705191));
#65222=CARTESIAN_POINT('Ctrl Pts',(-5.00968481138059,6.12575647433179,-37.9240196005863));
#65223=CARTESIAN_POINT('Ctrl Pts',(-5.15903177185281,6.00052123967778,-37.9162075306536));
#65224=CARTESIAN_POINT('Ctrl Pts',(-5.30356492179082,5.86993357035239,-37.9083954607208));
#65225=CARTESIAN_POINT('Ctrl Pts',(-5.44808776416868,5.73935521404797,-37.9005839479154));
#65226=CARTESIAN_POINT('Ctrl Pts',(-5.58779721865798,5.60342541942066,-37.8927724351101));
#65227=CARTESIAN_POINT('Ctrl Pts',(-5.72228207817539,5.46254600143493,-37.8849609223047));
#65228=CARTESIAN_POINT('Ctrl Pts',(-5.85678106193276,5.32165178762229,-37.8771485890971));
#65229=CARTESIAN_POINT('Ctrl Pts',(-5.98605411528906,5.17580717022823,-37.8693362558895));
#65230=CARTESIAN_POINT('Ctrl Pts',(-6.10972822563091,5.02544943352622,-37.8615239226819));
#65231=CARTESIAN_POINT('Ctrl Pts',(-6.23348995220829,4.87498517672201,-37.8537060548703));
#65232=CARTESIAN_POINT('Ctrl Pts',(-6.35164458732493,4.72000168508857,-37.8458881870587));
#65233=CARTESIAN_POINT('Ctrl Pts',(-6.46386009101385,4.56096850721406,-37.8380703192471));
#65234=CARTESIAN_POINT('Ctrl Pts',(-6.57611711920151,4.40187648031443,-37.8302495584926));
#65235=CARTESIAN_POINT('Ctrl Pts',(-6.68243044177497,4.23873207404659,-37.8224287977381));
#65236=CARTESIAN_POINT('Ctrl Pts',(-6.78251236144226,4.07203230179758,-37.8146080369836));
#65237=CARTESIAN_POINT('Ctrl Pts',(-6.8827051411969,3.90514787730196,-37.8067786132236));
#65238=CARTESIAN_POINT('Ctrl Pts',(-6.97665255602243,3.73470052589074,-37.7989491894636));
#65239=CARTESIAN_POINT('Ctrl Pts',(-7.06411322178446,3.56121122510446,-37.7911197657037));
#65240=CARTESIAN_POINT('Ctrl Pts',(-7.13133106143543,3.42787613212517,-37.7851024669983));
#65241=CARTESIAN_POINT('Ctrl Pts',(-7.19471832935731,3.29274475070456,-37.779085168293));
#65242=CARTESIAN_POINT('Ctrl Pts',(-7.25418513020149,3.15606069282002,-37.7730678695876));
#65243=CARTESIAN_POINT('Ctrl Pts',(-7.34246840311898,2.95314215988416,-37.7641347032446));
#65244=CARTESIAN_POINT('Ctrl Pts',(-7.4222494179899,2.74648092902733,-37.7552015369015));
#65245=CARTESIAN_POINT('Ctrl Pts',(-7.49324770286426,2.53676168835771,-37.7462683705585));
#65246=CARTESIAN_POINT('Ctrl Pts',(-7.56410161708253,2.32746889889639,-37.7373533692611));
#65247=CARTESIAN_POINT('Ctrl Pts',(-7.62620841446035,2.11513068903211,-37.7284383679637));
#65248=CARTESIAN_POINT('Ctrl Pts',(-7.67933726836815,1.9004473469823,-37.7195233666663));
#65249=CARTESIAN_POINT('Ctrl Pts',(-7.7323797293992,1.68611310170654,-37.7106228620605));
#65250=CARTESIAN_POINT('Ctrl Pts',(-7.776473349148,1.46944151070523,-37.7017223574547));
#65251=CARTESIAN_POINT('Ctrl Pts',(-7.81143731559288,1.25114669985702,-37.6928218528488));
#65252=CARTESIAN_POINT('Ctrl Pts',(-7.84628292098092,1.03359086708085,-37.6839514784954));
#65253=CARTESIAN_POINT('Ctrl Pts',(-7.87206052311267,0.814422958168712,
-37.6750811041419));
#65254=CARTESIAN_POINT('Ctrl Pts',(-7.8886406852852,0.594364482841163,-37.6662107297884));
#65255=CARTESIAN_POINT('Ctrl Pts',(-7.90351872575645,0.396897240488833,
-37.6582509892712));
#65256=CARTESIAN_POINT('Ctrl Pts',(-7.91099141809527,0.198713173039897,
-37.650291248754));
#65257=CARTESIAN_POINT('Ctrl Pts',(-7.91099999260968,0.000341949715757575,
-37.6423315082368));
#65258=CARTESIAN_POINT('',(-7.91099999400094,-0.000308086119090196,-33.6436736902287));
#65259=CARTESIAN_POINT('Ctrl Pts',(-7.91099999086604,0.000380154568757167,
-37.6333945227008));
#65260=CARTESIAN_POINT('Ctrl Pts',(-7.91100804081377,-0.167138906403437,
-37.6262687265125));
#65261=CARTESIAN_POINT('Ctrl Pts',(-7.90569518377744,-0.334622696508921,
-37.619293165992));
#65262=CARTESIAN_POINT('Ctrl Pts',(-7.89373004197606,-0.522868907718592,
-37.6116167499129));
#65263=CARTESIAN_POINT('Ctrl Pts',(-7.89230793117402,-0.543913043018763,
-37.6107608910436));
#65264=CARTESIAN_POINT('Ctrl Pts',(-7.88991667126631,-0.577312304649131,
-37.6094061542906));
#65265=CARTESIAN_POINT('Ctrl Pts',(-7.88900262693277,-0.589671205509749,
-37.6089056373613));
#65266=CARTESIAN_POINT('Ctrl Pts',(-7.88739293238899,-0.610762197319669,
-37.6080528118984));
#65267=CARTESIAN_POINT('Ctrl Pts',(-7.88671181393218,-0.619495356050412,
-37.6077000707848));
#65268=CARTESIAN_POINT('Ctrl Pts',(-7.88541266715558,-0.635803292941461,
-37.6070420991516));
#65269=CARTESIAN_POINT('Ctrl Pts',(-7.88479822618885,-0.643378342299304,
-37.6067367620263));
#65270=CARTESIAN_POINT('Ctrl Pts',(-7.88349958502888,-0.659107157046066,
-37.6061033626495));
#65271=CARTESIAN_POINT('Ctrl Pts',(-7.88281364832599,-0.667260772022794,
-37.6057753525923));
#65272=CARTESIAN_POINT('Ctrl Pts',(-7.88122373420322,-0.685815167712521,
-37.6050296924272));
#65273=CARTESIAN_POINT('Ctrl Pts',(-7.88031181509016,-0.696215261832065,
-37.6046122798259));
#65274=CARTESIAN_POINT('Ctrl Pts',(-7.87741867844866,-0.728476348754434,
-37.603319142472));
#65275=CARTESIAN_POINT('Ctrl Pts',(-7.87536705312983,-0.750331003093177,
-37.6024455206183));
#65276=CARTESIAN_POINT('Ctrl Pts',(-7.85913350215745,-0.915850566986409,
-37.5958468159735));
#65277=CARTESIAN_POINT('Ctrl Pts',(-7.84111208802052,-1.05911539898391,
-37.5902376764449));
#65278=CARTESIAN_POINT('Ctrl Pts',(-7.81233038629602,-1.24637379925773,
-37.583019522908));
#65279=CARTESIAN_POINT('Ctrl Pts',(-7.80510025786298,-1.29087712353991,
-37.5813124795044));
#65280=CARTESIAN_POINT('Ctrl Pts',(-7.63798994468429,-2.2667063709624,-37.5440523205259));
#65281=CARTESIAN_POINT('Ctrl Pts',(-7.31295421319051,-3.16182939678263,
-37.514238819932));
#65282=CARTESIAN_POINT('Ctrl Pts',(-6.75782772920575,-4.11594486905787,
-37.4732333980651));
#65283=CARTESIAN_POINT('Ctrl Pts',(-6.67368286036299,-4.2510223224782,-37.4671598010197));
#65284=CARTESIAN_POINT('Ctrl Pts',(-6.57000435691224,-4.40678436757921,
-37.4597409285784));
#65285=CARTESIAN_POINT('Ctrl Pts',(-6.55435898328399,-4.43002076738572,
-37.4586230902748));
#65286=CARTESIAN_POINT('Ctrl Pts',(-6.53337496386369,-4.46083158546764,
-37.4571265807389));
#65287=CARTESIAN_POINT('Ctrl Pts',(-6.52814580939585,-4.46848063020689,
-37.4567538807208));
#65288=CARTESIAN_POINT('Ctrl Pts',(-6.51951821717661,-4.48105333685371,
-37.456139356301));
#65289=CARTESIAN_POINT('Ctrl Pts',(-6.51612760101633,-4.4859823761148,-37.4558979497426));
#65290=CARTESIAN_POINT('Ctrl Pts',(-6.5095325528281,-4.49554654035601,-37.455428593167));
#65291=CARTESIAN_POINT('Ctrl Pts',(-6.50632875235116,-4.5001820984187,-37.4552006764631));
#65292=CARTESIAN_POINT('Ctrl Pts',(-6.49889977635036,-4.51090651902743,
-37.4546724018062));
#65293=CARTESIAN_POINT('Ctrl Pts',(-6.49467099596951,-4.51699286915906,
-37.4543718563921));
#65294=CARTESIAN_POINT('Ctrl Pts',(-6.48137044706001,-4.53607863800801,
-37.45342710173));
#65295=CARTESIAN_POINT('Ctrl Pts',(-6.47226819047899,-4.54905668767551,
-37.4527813341078));
#65296=CARTESIAN_POINT('Ctrl Pts',(-6.38907048960195,-4.66692526682044,
-37.4468864828682));
#65297=CARTESIAN_POINT('Ctrl Pts',(-6.31247247337594,-4.7700211987608,-37.4415147426215));
#65298=CARTESIAN_POINT('Ctrl Pts',(-6.20032993199196,-4.9135236342309,-37.4337763864183));
#65299=CARTESIAN_POINT('Ctrl Pts',(-6.16682813959291,-4.95550565985593,
-37.431479624319));
#65300=CARTESIAN_POINT('Ctrl Pts',(-6.05584973477682,-5.0917074226508,-37.4239275409087));
#65301=CARTESIAN_POINT('Ctrl Pts',(-5.97662192680819,-5.1844758551655,-37.4186238673784));
#65302=CARTESIAN_POINT('Ctrl Pts',(-5.41167651355209,-5.81580794641059,
-37.3815700789123));
#65303=CARTESIAN_POINT('Ctrl Pts',(-4.85596822372214,-6.28726235977595,
-37.3494025827222));
#65304=CARTESIAN_POINT('Ctrl Pts',(-4.14664146554219,-6.73814053072876,
-37.3147690013578));
#65305=CARTESIAN_POINT('Ctrl Pts',(-4.04815094056536,-6.7977678762687,-37.3100743517993));
#65306=CARTESIAN_POINT('Ctrl Pts',(-3.92472106725473,-6.86885956807116,
-37.3043217318996));
#65307=CARTESIAN_POINT('Ctrl Pts',(-3.90097910332909,-6.88237090457642,
-37.3032210636053));
#65308=CARTESIAN_POINT('Ctrl Pts',(-3.86338953558672,-6.90350578632141,
-37.3014874484482));
#65309=CARTESIAN_POINT('Ctrl Pts',(-3.84958831295894,-6.91121123018868,
-37.3008528496209));
#65310=CARTESIAN_POINT('Ctrl Pts',(-3.82371107118499,-6.92555734715423,
-37.2996664951357));
#65311=CARTESIAN_POINT('Ctrl Pts',(-3.8116406208102,-6.9322079241595,-37.2991145450163));
#65312=CARTESIAN_POINT('Ctrl Pts',(-3.78508059651708,-6.94675162389639,
-37.2979031119846));
#65313=CARTESIAN_POINT('Ctrl Pts',(-3.77058357404085,-6.95463102973133,
-37.2972438975247));
#65314=CARTESIAN_POINT('Ctrl Pts',(-3.7381551863088,-6.9721252696882,-37.2957737112228));
#65315=CARTESIAN_POINT('Ctrl Pts',(-3.72021115136542,-6.98171640548203,
-37.2949631914853));
#65316=CARTESIAN_POINT('Ctrl Pts',(-3.68402110957613,-7.00088094596724,
-37.293334403295));
#65317=CARTESIAN_POINT('Ctrl Pts',(-3.66577427122168,-7.01045252125632,
-37.2925161635183));
#65318=CARTESIAN_POINT('Ctrl Pts',(-3.45082124719638,-7.12213974821639,
-37.2829118562996));
#65319=CARTESIAN_POINT('Ctrl Pts',(-3.24994064461362,-7.21601918148237,
-37.2742819592309));
#65320=CARTESIAN_POINT('Ctrl Pts',(-2.50450852996305,-7.52693767661634,
-37.2433532648222));
#65321=CARTESIAN_POINT('Ctrl Pts',(-1.94025833784646,-7.69173280875099,
-37.2221441794592));
#65322=CARTESIAN_POINT('Ctrl Pts',(-1.10226686597287,-7.83830236860144,
-37.1906657194633));
#65323=CARTESIAN_POINT('Ctrl Pts',(-0.839429810923603,-7.87078926402653,
-37.1807676890986));
#65324=CARTESIAN_POINT('Ctrl Pts',(-0.473095344020291,-7.89750835825004,
-37.1665114592575));
#65325=CARTESIAN_POINT('Ctrl Pts',(-0.370586791446918,-7.9029818334549,
-37.1624719415133));
#65326=CARTESIAN_POINT('Ctrl Pts',(-0.252694815885022,-7.90697799124675,
-37.1577457021912));
#65327=CARTESIAN_POINT('Ctrl Pts',(-0.237384756964401,-7.90745244039719,
-37.1571303679746));
#65328=CARTESIAN_POINT('Ctrl Pts',(-0.214201750141736,-7.90810347828646,
-37.1561961438979));
#65329=CARTESIAN_POINT('Ctrl Pts',(-0.206329709239931,-7.90831278235552,
-37.1558784878495));
#65330=CARTESIAN_POINT('Ctrl Pts',(-0.192169871288246,-7.90866811152913,
-37.1553063136895));
#65331=CARTESIAN_POINT('Ctrl Pts',(-0.185882181307633,-7.90881839291601,
-37.1550519589696));
#65332=CARTESIAN_POINT('Ctrl Pts',(-0.17239137538223,-7.90912473811163,
-37.15450560673));
#65333=CARTESIAN_POINT('Ctrl Pts',(-0.165188215741935,-7.90927846027977,
-37.1542135184852));
#65334=CARTESIAN_POINT('Ctrl Pts',(-0.145763289389005,-7.90966645884243,
-37.1534248102971));
#65335=CARTESIAN_POINT('Ctrl Pts',(-0.133541203498214,-7.9098822476309,
-37.1529274618868));
#65336=CARTESIAN_POINT('Ctrl Pts',(-0.0795569260902536,-7.91071021796403,
-37.1507257067991));
#65337=CARTESIAN_POINT('Ctrl Pts',(-0.0377912921008751,-7.91101998350292,
-37.1490090899123));
#65338=CARTESIAN_POINT('Ctrl Pts',(0.746279780841901,-7.91062608934885,
-37.1165090588486));
#65339=CARTESIAN_POINT('Ctrl Pts',(1.48473784213369,-7.80578374461432,-37.0809906747664));
#65340=CARTESIAN_POINT('Ctrl Pts',(2.5239952840951,-7.50524873336213,-37.0320630245931));
#65341=CARTESIAN_POINT('Ctrl Pts',(2.84391900448066,-7.38995735815767,-37.0171048249811));
#65342=CARTESIAN_POINT('Ctrl Pts',(3.23762109589815,-7.2187088494996,-36.9990528123513));
#65343=CARTESIAN_POINT('Ctrl Pts',(3.31916674298965,-7.18157925903927,-36.9953324063199));
#65344=CARTESIAN_POINT('Ctrl Pts',(3.43174352031694,-7.1279932824626,-36.9902223764811));
#65345=CARTESIAN_POINT('Ctrl Pts',(3.46332068548813,-7.11270424636407,-36.9887919284498));
#65346=CARTESIAN_POINT('Ctrl Pts',(3.51048351028922,-7.08948039837846,-36.9866597050816));
#65347=CARTESIAN_POINT('Ctrl Pts',(3.52614605002107,-7.08170324386752,-36.985952311779));
#65348=CARTESIAN_POINT('Ctrl Pts',(3.55127170556941,-7.06912320485884,-36.9848186428435));
#65349=CARTESIAN_POINT('Ctrl Pts',(3.56075112431946,-7.06435312283342,-36.9843911894188));
#65350=CARTESIAN_POINT('Ctrl Pts',(3.5788350411953,-7.05520757517427,-36.9835762229094));
#65351=CARTESIAN_POINT('Ctrl Pts',(3.58744118064361,-7.05083540845978,-36.9831885917368));
#65352=CARTESIAN_POINT('Ctrl Pts',(3.60264165218483,-7.04307809622997,-36.9825043142645));
#65353=CARTESIAN_POINT('Ctrl Pts',(3.60923926056099,-7.03969941858782,-36.9822074343742));
#65354=CARTESIAN_POINT('Ctrl Pts',(3.62220456835119,-7.03303678339793,-36.9816242614886));
#65355=CARTESIAN_POINT('Ctrl Pts',(3.62857257285298,-7.02975343916738,-36.9813379466937));
#65356=CARTESIAN_POINT('Ctrl Pts',(3.64382363085682,-7.02186374646099,-36.9806525097189));
#65357=CARTESIAN_POINT('Ctrl Pts',(3.65270243345464,-7.01724918043411,-36.9802536869128));
#65358=CARTESIAN_POINT('Ctrl Pts',(3.68475668997787,-7.00051235156845,-36.9788146502941));
#65359=CARTESIAN_POINT('Ctrl Pts',(3.70788087016787,-6.98829196004266,-36.9777780210405));
#65360=CARTESIAN_POINT('Ctrl Pts',(4.06829471452783,-6.7955321817756,-36.9616437329532));
#65361=CARTESIAN_POINT('Ctrl Pts',(4.39212799681132,-6.59086745187698,-36.947494031072));
#65362=CARTESIAN_POINT('Ctrl Pts',(4.96383337233385,-6.16862482498478,-36.9224100057049));
#65363=CARTESIAN_POINT('Ctrl Pts',(5.21538206816902,-5.95746365722914,-36.9113207047966));
#65364=CARTESIAN_POINT('Ctrl Pts',(5.51660244329462,-5.67086438129691,-36.8973326211622));
#65365=CARTESIAN_POINT('Ctrl Pts',(5.5791010802608,-5.60938824274689,-36.8943869132303));
#65366=CARTESIAN_POINT('Ctrl Pts',(5.67104567810395,-5.51589083465691,-36.8899694860655));
#65367=CARTESIAN_POINT('Ctrl Pts',(5.70127024313005,-5.48464478187801,-36.8885033308486));
#65368=CARTESIAN_POINT('Ctrl Pts',(5.7972634321957,-5.38375640324336,-36.8837965646248));
#65369=CARTESIAN_POINT('Ctrl Pts',(5.86202486353776,-5.31316859436954,-36.880544399188));
#65370=CARTESIAN_POINT('Ctrl Pts',(6.03182102473429,-5.12121210985923,-36.8717621143674));
#65371=CARTESIAN_POINT('Ctrl Pts',(6.13446865397284,-4.99779650251522,-36.866179614706));
#65372=CARTESIAN_POINT('Ctrl Pts',(6.37046340959012,-4.69582190531446,-36.8524616648609));
#65373=CARTESIAN_POINT('Ctrl Pts',(6.50015349295495,-4.51459167351524,-36.8441825525713));
#65374=CARTESIAN_POINT('Ctrl Pts',(6.63864638757703,-4.3026990672836,-36.8341724311));
#65375=CARTESIAN_POINT('Ctrl Pts',(6.65513100642762,-4.27715750953957,-36.8329605374057));
#65376=CARTESIAN_POINT('Ctrl Pts',(6.67565321503586,-4.24495415826991,-36.8314251639933));
#65377=CARTESIAN_POINT('Ctrl Pts',(6.67982892877,-4.23838024895617,-36.8311113520266));
#65378=CARTESIAN_POINT('Ctrl Pts',(6.68644465939088,-4.22793091116827,-36.8306119153894));
#65379=CARTESIAN_POINT('Ctrl Pts',(6.6888910398079,-4.22405949651634,-36.830426740755));
#65380=CARTESIAN_POINT('Ctrl Pts',(6.69348320607412,-4.21677836749901,-36.8300782147641));
#65381=CARTESIAN_POINT('Ctrl Pts',(6.69562975276506,-4.21336913222301,-36.8299149176486));
#65382=CARTESIAN_POINT('Ctrl Pts',(6.70044078416009,-4.20571508971917,-36.8295480571607));
#65383=CARTESIAN_POINT('Ctrl Pts',(6.70310382214755,-4.2014694176372,-36.8293443923453));
#65384=CARTESIAN_POINT('Ctrl Pts',(6.70991397592451,-4.19058905797614,-36.828822028534));
#65385=CARTESIAN_POINT('Ctrl Pts',(6.71405525497882,-4.18395079432018,-36.8285029167931));
#65386=CARTESIAN_POINT('Ctrl Pts',(6.73781892124601,-4.1457326868581,-36.8266634130837));
#65387=CARTESIAN_POINT('Ctrl Pts',(6.75722802785665,-4.11402146489108,-36.8251280794695));
#65388=CARTESIAN_POINT('Ctrl Pts',(7.09368322141513,-3.55550569434129,-36.7979480552711));
#65389=CARTESIAN_POINT('Ctrl Pts',(7.34845571558426,-2.99367510098595,-36.7686212590121));
#65390=CARTESIAN_POINT('Ctrl Pts',(7.64558335139573,-2.06386546927526,-36.7232170676629));
#65391=CARTESIAN_POINT('Ctrl Pts',(7.7318685613809,-1.7125218871774,-36.7066763668442));
#65392=CARTESIAN_POINT('Ctrl Pts',(7.8362881398365,-1.1125678924626,-36.6800292468911));
#65393=CARTESIAN_POINT('Ctrl Pts',(7.86726945297144,-0.866779205352294,
-36.6695441449394));
#65394=CARTESIAN_POINT('Ctrl Pts',(7.88996304109896,-0.578071526730317,
-36.6577391462557));
#65395=CARTESIAN_POINT('Ctrl Pts',(7.89291966738994,-0.536192764212517,
-36.6560390689986));
#65396=CARTESIAN_POINT('Ctrl Pts',(7.89633415811472,-0.481651605205528,
-36.6538407098114));
#65397=CARTESIAN_POINT('Ctrl Pts',(7.89709514194546,-0.469009303260957,
-36.6533322439661));
#65398=CARTESIAN_POINT('Ctrl Pts',(7.89819957195826,-0.449896110454877,
-36.6525651753496));
#65399=CARTESIAN_POINT('Ctrl Pts',(7.89856543108893,-0.44342656637629,-36.6523058196505));
#65400=CARTESIAN_POINT('Ctrl Pts',(7.89928004152794,-0.430508456265079,
-36.6517885185563));
#65401=CARTESIAN_POINT('Ctrl Pts',(7.89962884623889,-0.424059898294344,
-36.6515305715585));
#65402=CARTESIAN_POINT('Ctrl Pts',(7.90039931244321,-0.409484944508133,
-36.6509482005867));
#65403=CARTESIAN_POINT('Ctrl Pts',(7.9008163329911,-0.401358304658727,-36.6506239326938));
#65404=CARTESIAN_POINT('Ctrl Pts',(7.90191173921254,-0.379348224021622,
-36.6497468975114));
#65405=CARTESIAN_POINT('Ctrl Pts',(7.90256607569152,-0.365463584242073,
-36.6491949375829));
#65406=CARTESIAN_POINT('Ctrl Pts',(7.90543006229951,-0.301083385969035,
-36.6466415937777));
#65407=CARTESIAN_POINT('Ctrl Pts',(7.90719237138449,-0.250568562800633,
-36.6446552198575));
#65408=CARTESIAN_POINT('Ctrl Pts',(7.92934324276393,0.625155307034691,-36.6105043400619));
#65409=CARTESIAN_POINT('Ctrl Pts',(7.82095457630954,1.44841150599309,-36.5835525351485));
#65410=CARTESIAN_POINT('Ctrl Pts',(7.57291219708224,2.28855420027638,-36.5533025338191));
#65411=CARTESIAN_POINT('Ctrl Pts',(7.55812497264545,2.33692667961003,-36.5515480011804));
#65412=CARTESIAN_POINT('Ctrl Pts',(7.44040459893448,2.70920879317726,-36.5379238560629));
#65413=CARTESIAN_POINT('Ctrl Pts',(7.31716695785351,3.0262938873901,-36.5256191386117));
#65414=CARTESIAN_POINT('Ctrl Pts',(7.16830818070849,3.34655905283701,-36.5114878601219));
#65415=CARTESIAN_POINT('Ctrl Pts',(7.16264357224805,3.3586659142455,-36.5109510316382));
#65416=CARTESIAN_POINT('Ctrl Pts',(7.15445974513855,3.37604218953926,-36.5101767287743));
#65417=CARTESIAN_POINT('Ctrl Pts',(7.15196539131631,3.38132313620158,-36.509940899095));
#65418=CARTESIAN_POINT('Ctrl Pts',(7.14761846766423,3.3904999410864,-36.509530219597));
#65419=CARTESIAN_POINT('Ctrl Pts',(7.14576855196236,3.39439706154809,-36.5093555417459));
#65420=CARTESIAN_POINT('Ctrl Pts',(7.14219990844338,3.40189908981225,-36.5090187580625));
#65421=CARTESIAN_POINT('Ctrl Pts',(7.14048163620965,3.40550421410387,-36.5088566815429));
#65422=CARTESIAN_POINT('Ctrl Pts',(7.13641934464273,3.41401075801059,-36.5084737007591));
#65423=CARTESIAN_POINT('Ctrl Pts',(7.13407300721182,3.4189110614175,-36.5082526484939));
#65424=CARTESIAN_POINT('Ctrl Pts',(7.12710460103978,3.43342610416973,-36.5075966059898));
#65425=CARTESIAN_POINT('Ctrl Pts',(7.12246814567264,3.44303388288791,-36.5071607058831));
#65426=CARTESIAN_POINT('Ctrl Pts',(7.08120074850047,3.52810914404482,-36.5032864100088));
#65427=CARTESIAN_POINT('Ctrl Pts',(7.04339221447428,3.60299643762418,-36.4997750132669));
#65428=CARTESIAN_POINT('Ctrl Pts',(6.90609219613828,3.86452348037295,-36.487190749631));
#65429=CARTESIAN_POINT('Ctrl Pts',(6.80031893456534,4.04775278822696,-36.4777901259391));
#65430=CARTESIAN_POINT('Ctrl Pts',(6.30128577960179,4.83734099834449,-36.4353460759295));
#65431=CARTESIAN_POINT('Ctrl Pts',(5.83327964164717,5.3925075386169,-36.4006266502012));
#65432=CARTESIAN_POINT('Ctrl Pts',(5.05880547240706,6.09054410989927,-36.3546380653008));
#65433=CARTESIAN_POINT('Ctrl Pts',(4.80841510011181,6.29010462281645,-36.3410639428603));
#65434=CARTESIAN_POINT('Ctrl Pts',(4.52824817609912,6.48686308355301,-36.327190282024));
#65435=CARTESIAN_POINT('Ctrl Pts',(4.50983582460034,6.49967730391375,-36.3262842061157));
#65436=CARTESIAN_POINT('Ctrl Pts',(4.48279948697111,6.5183232604816,-36.3249619908701));
#65437=CARTESIAN_POINT('Ctrl Pts',(4.47421817744401,6.52421651006624,-36.3245435306302));
#65438=CARTESIAN_POINT('Ctrl Pts',(4.45910166665309,6.5345539851972,-36.3238085045496));
#65439=CARTESIAN_POINT('Ctrl Pts',(4.45257140086587,6.53900538152787,-36.3234916693953));
#65440=CARTESIAN_POINT('Ctrl Pts',(4.43985255456151,6.54764737542861,-36.3228759198539));
#65441=CARTESIAN_POINT('Ctrl Pts',(4.43366468533356,6.55183900272528,-36.3225769670415));
#65442=CARTESIAN_POINT('Ctrl Pts',(4.41711828319405,6.56301326588214,-36.3217792063909));
#65443=CARTESIAN_POINT('Ctrl Pts',(4.40674911648145,6.56998015842378,-36.321280986726));
#65444=CARTESIAN_POINT('Ctrl Pts',(4.36936609337057,6.59496895178782,-36.3194909316489));
#65445=CARTESIAN_POINT('Ctrl Pts',(4.34225766850095,6.6128491518278,-36.3182043610287));
#65446=CARTESIAN_POINT('Ctrl Pts',(3.8958964077793,6.90333230344256,-36.2972050167528));
#65447=CARTESIAN_POINT('Ctrl Pts',(3.45181104172885,7.13576009545579,-36.2790748099056));
#65448=CARTESIAN_POINT('Ctrl Pts',(2.8020593427605,7.4008803862583,-36.2544801072376));
#65449=CARTESIAN_POINT('Ctrl Pts',(2.61254753033994,7.46988375050931,-36.2475078331805));
#65450=CARTESIAN_POINT('Ctrl Pts',(1.92434919993394,7.6910669604578,-36.2224343342477));
#65451=CARTESIAN_POINT('Ctrl Pts',(1.41352853388726,7.80112780467744,-36.2042562882558));
#65452=CARTESIAN_POINT('Ctrl Pts',(0.85807071809913,7.86441746461932,-36.1821469324375));
#65453=CARTESIAN_POINT('Ctrl Pts',(0.820515854500712,7.86842430783968,-36.1806429552084));
#65454=CARTESIAN_POINT('Ctrl Pts',(0.770703364800185,7.87337846131501,-36.1786370144707));
#65455=CARTESIAN_POINT('Ctrl Pts',(0.758469807700295,7.87456637666376,-36.1781434864491));
#65456=CARTESIAN_POINT('Ctrl Pts',(0.738379286970201,7.87646997532498,-36.177331582769));
#65457=CARTESIAN_POINT('Ctrl Pts',(0.730523909257359,7.87720242605999,-36.1770137756065));
#65458=CARTESIAN_POINT('Ctrl Pts',(0.715298655577549,7.87859908801104,-36.1763971318763));
#65459=CARTESIAN_POINT('Ctrl Pts',(0.707928915023725,7.87926471234134,-36.1760983424647));
#65460=CARTESIAN_POINT('Ctrl Pts',(0.69090621322045,7.88077810263616,-36.1754075049309));
#65461=CARTESIAN_POINT('Ctrl Pts',(0.681252615580431,7.8816184741035,-36.1750152172217));
#65462=CARTESIAN_POINT('Ctrl Pts',(0.65532220320219,7.88382778977752,-36.1739601548447));
#65463=CARTESIAN_POINT('Ctrl Pts',(0.639042691671107,7.8851640593566,-36.1732963497333));
#65464=CARTESIAN_POINT('Ctrl Pts',(0.521523476562182,7.89444404921093,-36.1684946251035));
#65465=CARTESIAN_POINT('Ctrl Pts',(0.420145120151339,7.90048801185732,-36.1642999520708));
#65466=CARTESIAN_POINT('Ctrl Pts',(-0.209180713104586,7.92585989448046,
-36.1380188316244));
#65467=CARTESIAN_POINT('Ctrl Pts',(-0.737844362038266,7.89421311080287,
-36.1150069505851));
#65468=CARTESIAN_POINT('Ctrl Pts',(-1.98910054495842,7.69244483530152,-36.0607932867541));
#65469=CARTESIAN_POINT('Ctrl Pts',(-2.698737292223,7.47309241050851,-36.0302256528162));
#65470=CARTESIAN_POINT('Ctrl Pts',(-3.4276097422322,7.13020419761666,-35.9975164125075));
#65471=CARTESIAN_POINT('Ctrl Pts',(-3.48727116714997,7.10121541291687,-35.9948309746968));
#65472=CARTESIAN_POINT('Ctrl Pts',(-3.57283208578464,7.05830402001027,-35.9909680213152));
#65473=CARTESIAN_POINT('Ctrl Pts',(-3.5990293312361,7.04498208891827,-35.9897836408525));
#65474=CARTESIAN_POINT('Ctrl Pts',(-3.6446765389618,7.02144831705688,-35.9877170574925));
#65475=CARTESIAN_POINT('Ctrl Pts',(-3.66415930814574,7.01130088576769,-35.9868340954848));
#65476=CARTESIAN_POINT('Ctrl Pts',(-3.70182855099322,6.99148129251876,-35.9851251051604));
#65477=CARTESIAN_POINT('Ctrl Pts',(-3.7200200097285,6.98181899039991,-35.9842989639616));
#65478=CARTESIAN_POINT('Ctrl Pts',(-3.76334164696845,6.95859153668349,-35.9823295588024));
#65479=CARTESIAN_POINT('Ctrl Pts',(-3.78843654579443,6.94496112822049,-35.9811871208501));
#65480=CARTESIAN_POINT('Ctrl Pts',(-3.87867729703123,6.89531179174015,-35.9770728889689));
#65481=CARTESIAN_POINT('Ctrl Pts',(-3.94338810630175,6.85850950723549,-35.9741112202626));
#65482=CARTESIAN_POINT('Ctrl Pts',(-4.42325726081035,6.57656170287584,-35.9520535054794));
#65483=CARTESIAN_POINT('Ctrl Pts',(-4.81574937525418,6.29483448008435,-35.9335449453065));
#65484=CARTESIAN_POINT('Ctrl Pts',(-5.4563141483298,5.73986644266791,-35.9009740292749));
#65485=CARTESIAN_POINT('Ctrl Pts',(-5.71555839624837,5.48177019544208,-35.8869375065442));
#65486=CARTESIAN_POINT('Ctrl Pts',(-5.97447397431258,5.18559228683308,-35.8712206481904));
#65487=CARTESIAN_POINT('Ctrl Pts',(-5.99280928880847,5.16439187650242,-35.8700975367698));
#65488=CARTESIAN_POINT('Ctrl Pts',(-6.01983591005004,5.13280430392408,-35.8684264615334));
#65489=CARTESIAN_POINT('Ctrl Pts',(-6.02861386087113,5.12249151498152,-35.8678812548076));
#65490=CARTESIAN_POINT('Ctrl Pts',(-6.04377031616883,5.10459201189912,-35.8669356417218));
#65491=CARTESIAN_POINT('Ctrl Pts',(-6.05016113397797,5.0970157440192,-35.8665356050787));
#65492=CARTESIAN_POINT('Ctrl Pts',(-6.0633977480039,5.08126386393095,-35.8657043403288));
#65493=CARTESIAN_POINT('Ctrl Pts',(-6.07024128559197,5.07308638200377,-35.8652730479767));
#65494=CARTESIAN_POINT('Ctrl Pts',(-6.08687056059915,5.05313389785313,-35.8642213681008));
#65495=CARTESIAN_POINT('Ctrl Pts',(-6.09663867715392,5.04134428987303,-35.8636004906358));
#65496=CARTESIAN_POINT('Ctrl Pts',(-6.13359387258776,4.99647680748224,-35.8612398147393));
#65497=CARTESIAN_POINT('Ctrl Pts',(-6.16054633187781,4.96320693986651,-35.8594938339987));
#65498=CARTESIAN_POINT('Ctrl Pts',(-6.44783167812667,4.60263886266071,-35.840627145596));
#65499=CARTESIAN_POINT('Ctrl Pts',(-6.6820859261543,4.25541250915445,-35.8229797949973));
#65500=CARTESIAN_POINT('Ctrl Pts',(-7.03994298738624,3.62198927814194,-35.7924469388437));
#65501=CARTESIAN_POINT('Ctrl Pts',(-7.17617196042905,3.34397466834248,-35.779536768843));
#65502=CARTESIAN_POINT('Ctrl Pts',(-7.33892386593008,2.95576942802021,-35.7622094778198));
#65503=CARTESIAN_POINT('Ctrl Pts',(-7.37989169441482,2.85194239758499,-35.7576391863045));
#65504=CARTESIAN_POINT('Ctrl Pts',(-7.4472357576786,2.67008923898223,-35.7497401651053));
#65505=CARTESIAN_POINT('Ctrl Pts',(-7.47461565903563,2.59245403093063,-35.7464008099209));
#65506=CARTESIAN_POINT('Ctrl Pts',(-7.51215983333576,2.48045515221475,-35.7416276414148));
#65507=CARTESIAN_POINT('Ctrl Pts',(-7.52330993310817,2.44642816948199,-35.7401832793307));
#65508=CARTESIAN_POINT('Ctrl Pts',(-7.54233007878435,2.38702405365369,-35.7376714786114));
#65509=CARTESIAN_POINT('Ctrl Pts',(-7.55030399794099,2.36168084093396,-35.7366029613231));
#65510=CARTESIAN_POINT('Ctrl Pts',(-7.565487595315,2.31256043178719,-35.7345377356777));
#65511=CARTESIAN_POINT('Ctrl Pts',(-7.5727132213212,2.28878849562426,-35.7335408741272));
#65512=CARTESIAN_POINT('Ctrl Pts',(-7.58969399611725,2.23196187114615,-35.7311639277338));
#65513=CARTESIAN_POINT('Ctrl Pts',(-7.59934537785147,2.19887666519629,-35.7297849032229));
#65514=CARTESIAN_POINT('Ctrl Pts',(-7.63394801414356,2.07730844877326,-35.724734842826));
#65515=CARTESIAN_POINT('Ctrl Pts',(-7.657572681896,1.98845505174388,-35.7210768224582));
#65516=CARTESIAN_POINT('Ctrl Pts',(-7.83053002696736,1.28908477186011,-35.6925051429103));
#65517=CARTESIAN_POINT('Ctrl Pts',(-7.90817944247995,0.663114381764724,
-35.6682303155321));
#65518=CARTESIAN_POINT('Ctrl Pts',(-7.91097491555085,0.0230183952757,-35.6442717049117));
#65519=CARTESIAN_POINT('Ctrl Pts',(-7.91100006308073,0.0114875306561859,
-35.6438403068342));
#65520=CARTESIAN_POINT('Ctrl Pts',(-7.91099762551218,-0.433264208104541,
-35.6272082196128));
#65521=CARTESIAN_POINT('Ctrl Pts',(-7.87540975307761,-0.86573933378559,
-35.6113586004474));
#65522=CARTESIAN_POINT('Ctrl Pts',(-7.77046872412384,-1.49911219422672,
-35.5870431545332));
#65523=CARTESIAN_POINT('Ctrl Pts',(-7.72819625901884,-1.70367164050496,
-35.5790038503414));
#65524=CARTESIAN_POINT('Ctrl Pts',(-7.67303583723596,-1.92583666242136,
-35.5698763507552));
#65525=CARTESIAN_POINT('Ctrl Pts',(-7.66811310799267,-1.94534499873562,
-35.5690714532635));
#65526=CARTESIAN_POINT('Ctrl Pts',(-7.6611046790867,-1.97267880785223,-35.567938657577));
#65527=CARTESIAN_POINT('Ctrl Pts',(-7.65908127959233,-1.98052026873652,
-35.5676131025769));
#65528=CARTESIAN_POINT('Ctrl Pts',(-7.65535334490466,-1.99487631444721,
-35.5670159954335));
#65529=CARTESIAN_POINT('Ctrl Pts',(-7.65365252415963,-2.00139186177033,
-35.5667445861702));
#65530=CARTESIAN_POINT('Ctrl Pts',(-7.6501940923712,-2.0145716294404,-35.5661947319215));
#65531=CARTESIAN_POINT('Ctrl Pts',(-7.64843608753133,-2.02123573975508,
-35.5659162717187));
#65532=CARTESIAN_POINT('Ctrl Pts',(-7.64409570543554,-2.03760218153334,
-35.5652313095971));
#65533=CARTESIAN_POINT('Ctrl Pts',(-7.64150356627544,-2.0473018950403,-35.5648244194402));
#65534=CARTESIAN_POINT('Ctrl Pts',(-7.63203110653457,-2.08247896122746,
-35.5633452922324));
#65535=CARTESIAN_POINT('Ctrl Pts',(-7.62504182683714,-2.10792659997468,
-35.5622686092578));
#65536=CARTESIAN_POINT('Ctrl Pts',(-7.52536283990521,-2.46386967251659,
-35.5471098150298));
#65537=CARTESIAN_POINT('Ctrl Pts',(-7.41140481046643,-2.78796166301723,
-35.5319719820265));
#65538=CARTESIAN_POINT('Ctrl Pts',(-7.00452647881092,-3.74194919107196,
-35.4849380674929));
#65539=CARTESIAN_POINT('Ctrl Pts',(-6.64938958715585,-4.3418175869482,-35.4522725299542));
#65540=CARTESIAN_POINT('Ctrl Pts',(-6.05762591733933,-5.09495916674867,
-35.4106724477684));
#65541=CARTESIAN_POINT('Ctrl Pts',(-5.8844549938626,-5.2940199062029,-35.399570596877));
#65542=CARTESIAN_POINT('Ctrl Pts',(-5.68409276339649,-5.50233152688531,
-35.3878326825618));
#65543=CARTESIAN_POINT('Ctrl Pts',(-5.66644350084613,-5.52050548783489,
-35.3868074887323));
#65544=CARTESIAN_POINT('Ctrl Pts',(-5.64146717168599,-5.5459783708589,-35.3853689022681));
#65545=CARTESIAN_POINT('Ctrl Pts',(-5.63421271468866,-5.55334809154366,
-35.3849524982774));
#65546=CARTESIAN_POINT('Ctrl Pts',(-5.62157429834714,-5.56613705925956,
-35.3842295461687));
#65547=CARTESIAN_POINT('Ctrl Pts',(-5.61619690874079,-5.57156276434006,
-35.3839227245571));
#65548=CARTESIAN_POINT('Ctrl Pts',(-5.60496829158744,-5.58285949632484,
-35.3832836658961));
#65549=CARTESIAN_POINT('Ctrl Pts',(-5.59911567676641,-5.58872913497522,
-35.3829514875609));
#65550=CARTESIAN_POINT('Ctrl Pts',(-5.58527084741467,-5.60257065879835,
-35.3821678434919));
#65551=CARTESIAN_POINT('Ctrl Pts',(-5.57727076473569,-5.61053466649369,
-35.3817167093311));
#65552=CARTESIAN_POINT('Ctrl Pts',(-5.55087901208505,-5.63669518040547,
-35.380233968605));
#65553=CARTESIAN_POINT('Ctrl Pts',(-5.53241503937061,-5.65481867182481,
-35.3792054187525));
#65554=CARTESIAN_POINT('Ctrl Pts',(-5.25445701072294,-5.92498656794431,
-35.3638516409251));
#65555=CARTESIAN_POINT('Ctrl Pts',(-4.97805269959303,-6.15904285466105,
-35.3502992519259));
#65556=CARTESIAN_POINT('Ctrl Pts',(-4.46722501297464,-6.53467320750191,
-35.3274539326845));
#65557=CARTESIAN_POINT('Ctrl Pts',(-4.23968781674317,-6.68454238024796,
-35.3179451525401));
#65558=CARTESIAN_POINT('Ctrl Pts',(-3.78392362052155,-6.95208484434698,
-35.2996388159202));
#65559=CARTESIAN_POINT('Ctrl Pts',(-3.5568070146853,-7.07097469710224,-35.2908416258373));
#65560=CARTESIAN_POINT('Ctrl Pts',(-3.21658183206928,-7.22852823133639,
-35.2777148970113));
#65561=CARTESIAN_POINT('Ctrl Pts',(-3.10773045924041,-7.27598994043385,
-35.2735217812319));
#65562=CARTESIAN_POINT('Ctrl Pts',(-2.72981047278163,-7.43074360231403,
-35.2588788098745));
#65563=CARTESIAN_POINT('Ctrl Pts',(-2.45594898219325,-7.52569735684425,
-35.248120713389));
#65564=CARTESIAN_POINT('Ctrl Pts',(-2.16049365823181,-7.61028917634762,
-35.2358616796864));
#65565=CARTESIAN_POINT('Ctrl Pts',(-2.14346375334845,-7.61510323799295,
-35.2351529788124));
#65566=CARTESIAN_POINT('Ctrl Pts',(-2.11954711484406,-7.62177747724523,
-35.2341548896942));
#65567=CARTESIAN_POINT('Ctrl Pts',(-2.11267371174344,-7.62368557011198,
-35.2338677253339));
#65568=CARTESIAN_POINT('Ctrl Pts',(-2.10074969967808,-7.62697837452272,
-35.2333690018159));
#65569=CARTESIAN_POINT('Ctrl Pts',(-2.09570027221066,-7.62836737414888,
-35.233157638081));
#65570=CARTESIAN_POINT('Ctrl Pts',(-2.08519915329935,-7.63124481507142,
-35.2327177228191));
#65571=CARTESIAN_POINT('Ctrl Pts',(-2.07974723900186,-7.63273243066278,
-35.2324891343224));
#65572=CARTESIAN_POINT('Ctrl Pts',(-2.0669228801507,-7.63621693956748,-35.2319509807382));
#65573=CARTESIAN_POINT('Ctrl Pts',(-2.0595491359283,-7.63820899797494,-35.2316412021114));
#65574=CARTESIAN_POINT('Ctrl Pts',(-2.03550566598467,-7.64466712877018,
-35.2306299923322));
#65575=CARTESIAN_POINT('Ctrl Pts',(-2.01882428102815,-7.64908931453851,
-35.2299266625003));
#65576=CARTESIAN_POINT('Ctrl Pts',(-1.97958629193512,-7.65935389218984,
-35.2282683895571));
#65577=CARTESIAN_POINT('Ctrl Pts',(-1.95701814457604,-7.66515126397186,
-35.2273115945122));
#65578=CARTESIAN_POINT('Ctrl Pts',(-1.70082120016819,-7.72975868291033,
-35.2164181869762));
#65579=CARTESIAN_POINT('Ctrl Pts',(-1.46465799305012,-7.77796428603496,
-35.2060823536449));
#65580=CARTESIAN_POINT('Ctrl Pts',(-0.748549508464131,-7.89036322858865,
-35.1745103794928));
#65581=CARTESIAN_POINT('Ctrl Pts',(-0.264515694422575,-7.92137748778909,
-35.1529389995076));
#65582=CARTESIAN_POINT('Ctrl Pts',(0.592938821828755,-7.89759768850724,
-35.1159785226326));
#65583=CARTESIAN_POINT('Ctrl Pts',(0.965377247226943,-7.86076988579311,
-35.1003244704665));
#65584=CARTESIAN_POINT('Ctrl Pts',(1.37281518020253,-7.7910758681119,-35.0835727804889));
#65585=CARTESIAN_POINT('Ctrl Pts',(1.41174239337147,-7.78411640141012,-35.0819757131983));
#65586=CARTESIAN_POINT('Ctrl Pts',(1.46843066395291,-7.77354235784925,-35.0796544182308));
#65587=CARTESIAN_POINT('Ctrl Pts',(1.48623389388585,-7.77015818500329,-35.0789260459248));
#65588=CARTESIAN_POINT('Ctrl Pts',(1.51772057623712,-7.76406078314223,-35.0776389191964));
#65589=CARTESIAN_POINT('Ctrl Pts',(1.53140875673541,-7.76137248256273,-35.0770797253856));
#65590=CARTESIAN_POINT('Ctrl Pts',(1.55980095615707,-7.755718340598,-35.0759205426458));
#65591=CARTESIAN_POINT('Ctrl Pts',(1.57450379788584,-7.75274685474108,-35.0753206548458));
#65592=CARTESIAN_POINT('Ctrl Pts',(1.61240549244743,-7.7449745485653,-35.0737751858412));
#65593=CARTESIAN_POINT('Ctrl Pts',(1.63559143000825,-7.74011129834192,-35.0728306827089));
#65594=CARTESIAN_POINT('Ctrl Pts',(1.7289456021244,-7.72009205588672,-35.0690311088362));
#65595=CARTESIAN_POINT('Ctrl Pts',(1.79892871156013,-7.70408527621593,-35.0661900825253));
#65596=CARTESIAN_POINT('Ctrl Pts',(2.23770390295012,-7.59742222810576,-35.0484192294951));
#65597=CARTESIAN_POINT('Ctrl Pts',(2.59979382924729,-7.4812590359623,-35.0339707284821));
#65598=CARTESIAN_POINT('Ctrl Pts',(3.5407244301004,-7.10279194348282,-34.9961758761288));
#65599=CARTESIAN_POINT('Ctrl Pts',(4.09864149704759,-6.79613295558115,-34.9736097722637));
#65600=CARTESIAN_POINT('Ctrl Pts',(4.70396036629784,-6.36152245801653,-34.9447716993639));
#65601=CARTESIAN_POINT('Ctrl Pts',(4.79264226889207,-6.29498132670956,-34.9404187951235));
#65602=CARTESIAN_POINT('Ctrl Pts',(4.89323880580509,-6.2161420872334,-34.9353025206132));
#65603=CARTESIAN_POINT('Ctrl Pts',(4.90654975584002,-6.20564081681379,-34.9346218504229));
#65604=CARTESIAN_POINT('Ctrl Pts',(4.92625388151001,-6.18999281534984,-34.9336086418575));
#65605=CARTESIAN_POINT('Ctrl Pts',(4.93267302013859,-6.18487875668803,-34.9332776733857));
#65606=CARTESIAN_POINT('Ctrl Pts',(4.94407013503759,-6.17576976898899,-34.9326884413778));
#65607=CARTESIAN_POINT('Ctrl Pts',(4.94905126260671,-6.17177878245103,-34.9324303712347));
#65608=CARTESIAN_POINT('Ctrl Pts',(4.95950457480096,-6.16338257156014,-34.9318876325583));
#65609=CARTESIAN_POINT('Ctrl Pts',(4.96497573052723,-6.15897607932861,-34.9316029009146));
#65610=CARTESIAN_POINT('Ctrl Pts',(4.97932597885788,-6.1473867803685,-34.9308543081485));
#65611=CARTESIAN_POINT('Ctrl Pts',(4.98819537985467,-6.14019203948405,-34.9303898423009));
#65612=CARTESIAN_POINT('Ctrl Pts',(5.02742522801277,-6.10822820814862,-34.9283274319327));
#65613=CARTESIAN_POINT('Ctrl Pts',(5.05761663504678,-6.08325325465704,-34.9267187660813));
#65614=CARTESIAN_POINT('Ctrl Pts',(5.26768446062512,-5.90683600722821,-34.9153669425712));
#65615=CARTESIAN_POINT('Ctrl Pts',(5.44088726497666,-5.74768861053685,-34.90513123598));
#65616=CARTESIAN_POINT('Ctrl Pts',(5.92339599696948,-5.26296353557398,-34.8745333269023));
#65617=CARTESIAN_POINT('Ctrl Pts',(6.21241409076899,-4.91846703608904,-34.8535621020513));
#65618=CARTESIAN_POINT('Ctrl Pts',(6.76706166340391,-4.12991917886488,-34.8096257209357));
#65619=CARTESIAN_POINT('Ctrl Pts',(7.02162366245384,-3.68052795501237,-34.7869716560156));
#65620=CARTESIAN_POINT('Ctrl Pts',(7.2440879241625,-3.17933972295181,-34.7646586182065));
#65621=CARTESIAN_POINT('Ctrl Pts',(7.25729289881124,-3.14908093629346,-34.7633218557471));
#65622=CARTESIAN_POINT('Ctrl Pts',(7.27514369911938,-3.10746771609591,-34.7614975728146));
#65623=CARTESIAN_POINT('Ctrl Pts',(7.27995300924211,-3.09618404402211,-34.7610043217873));
#65624=CARTESIAN_POINT('Ctrl Pts',(7.28755002653919,-3.07824425351844,-34.7602223444753));
#65625=CARTESIAN_POINT('Ctrl Pts',(7.29035489281484,-3.07159545038098,-34.7599330169151));
#65626=CARTESIAN_POINT('Ctrl Pts',(7.29578036711737,-3.05868532317851,-34.7593721660426));
#65627=CARTESIAN_POINT('Ctrl Pts',(7.29840202156909,-3.05242444678329,-34.759100606208));
#65628=CARTESIAN_POINT('Ctrl Pts',(7.30463164796263,-3.03749332146113,-34.7584540036308));
#65629=CARTESIAN_POINT('Ctrl Pts',(7.30823224945373,-3.02881999781881,-34.7580792192978));
#65630=CARTESIAN_POINT('Ctrl Pts',(7.31890395523677,-3.0029835937782,-34.7569652302405));
#65631=CARTESIAN_POINT('Ctrl Pts',(7.32593012786765,-2.98580195899009,-34.7562275988927));
#65632=CARTESIAN_POINT('Ctrl Pts',(7.38340376055676,-2.84383309373227,-34.7501587976858));
#65633=CARTESIAN_POINT('Ctrl Pts',(7.43072081848879,-2.71779840093948,-34.744937894455));
#65634=CARTESIAN_POINT('Ctrl Pts',(7.58321345841792,-2.27780529355867,-34.7272431528378));
#65635=CARTESIAN_POINT('Ctrl Pts',(7.6718886615137,-1.95848708701791,-34.7153392914277));
#65636=CARTESIAN_POINT('Ctrl Pts',(7.835197542763,-1.18514102093041,-34.6878886196244));
#65637=CARTESIAN_POINT('Ctrl Pts',(7.89077800856185,-0.728350936736043,
-34.6727928426398));
#65638=CARTESIAN_POINT('Ctrl Pts',(7.91631565513461,0.021349773999759,-34.6472012598829));
#65639=CARTESIAN_POINT('Ctrl Pts',(7.91017943541785,0.31233066044255,-34.6370514594814));
#65640=CARTESIAN_POINT('Ctrl Pts',(7.87744582784855,0.741032525252417,-34.6210032087692));
#65641=CARTESIAN_POINT('Ctrl Pts',(7.8631943369072,0.879461643933766,-34.615650124476));
#65642=CARTESIAN_POINT('Ctrl Pts',(7.84364293976988,1.03021969383116,-34.6095669673779));
#65643=CARTESIAN_POINT('Ctrl Pts',(7.84195375766663,1.04299973295427,-34.6090492897763));
#65644=CARTESIAN_POINT('Ctrl Pts',(7.83954109214129,1.06091628860935,-34.6083206796611));
#65645=CARTESIAN_POINT('Ctrl Pts',(7.83884377448122,1.06605637085358,-34.6081113172853));
#65646=CARTESIAN_POINT('Ctrl Pts',(7.83762636236382,1.07496440499251,-34.6077479013901));
#65647=CARTESIAN_POINT('Ctrl Pts',(7.83710860417076,1.07873267974389,-34.6075939893686));
#65648=CARTESIAN_POINT('Ctrl Pts',(7.83602713009787,1.08656183669143,-34.6072738376019));
#65649=CARTESIAN_POINT('Ctrl Pts',(7.83546297490771,1.09062265578152,-34.6071075711264));
#65650=CARTESIAN_POINT('Ctrl Pts',(7.8341263851294,1.10018893314528,-34.6067153891645));
#65651=CARTESIAN_POINT('Ctrl Pts',(7.83335130932743,1.10569397704878,-34.6064893116876));
#65652=CARTESIAN_POINT('Ctrl Pts',(7.83075246659903,1.1240125980999,-34.6057357182032));
#65653=CARTESIAN_POINT('Ctrl Pts',(7.82890306802288,1.13682244054341,-34.6052066367563));
#65654=CARTESIAN_POINT('Ctrl Pts',(7.78075620307085,1.46462126881256,-34.5916148029));
#65655=CARTESIAN_POINT('Ctrl Pts',(7.71552118288662,1.77650662751726,-34.5774421260612));
#65656=CARTESIAN_POINT('Ctrl Pts',(7.53610070933983,2.43368380429925,-34.5462216207576));
#65657=CARTESIAN_POINT('Ctrl Pts',(7.41653883908029,2.77679361749781,-34.5290970696112));
#65658=CARTESIAN_POINT('Ctrl Pts',(7.04737857539898,3.64007257618154,-34.4855560537162));
#65659=CARTESIAN_POINT('Ctrl Pts',(6.76372588247223,4.14341428172199,-34.4598467180261));
#65660=CARTESIAN_POINT('Ctrl Pts',(6.40530712137303,4.64300118916018,-34.4348069840798));
#65661=CARTESIAN_POINT('Ctrl Pts',(6.38251196662498,4.67428715606589,-34.4332401587761));
#65662=CARTESIAN_POINT('Ctrl Pts',(6.35189072963362,4.71567262455864,-34.4311690087661));
#65663=CARTESIAN_POINT('Ctrl Pts',(6.34426870957117,4.72592199323101,-34.430656195847));
#65664=CARTESIAN_POINT('Ctrl Pts',(6.33235885378093,4.74185649840118,-34.4298591118876));
#65665=CARTESIAN_POINT('Ctrl Pts',(6.32808812585682,4.74755435737609,-34.4295741260206));
#65666=CARTESIAN_POINT('Ctrl Pts',(6.31953825490305,4.75892926869899,-34.4290052631051));
#65667=CARTESIAN_POINT('Ctrl Pts',(6.31525914086791,4.76460633460062,-34.4287213852677));
#65668=CARTESIAN_POINT('Ctrl Pts',(6.30562048504548,4.77735806421826,-34.4280838172497));
#65669=CARTESIAN_POINT('Ctrl Pts',(6.30025667402075,4.78442949758283,-34.4277303068892));
#65670=CARTESIAN_POINT('Ctrl Pts',(6.28447615238046,4.80516135045984,-34.4266940361215));
#65671=CARTESIAN_POINT('Ctrl Pts',(6.27402680130437,4.81879692614263,-34.42601265078));
#65672=CARTESIAN_POINT('Ctrl Pts',(6.19549273585925,4.92058917790372,-34.4209271804231));
#65673=CARTESIAN_POINT('Ctrl Pts',(6.12559579001011,5.0073351835864,-34.416600475273));
#65674=CARTESIAN_POINT('Ctrl Pts',(5.89031539433097,5.28702869742106,-34.4026481045688));
#65675=CARTESIAN_POINT('Ctrl Pts',(5.71746297837752,5.47349221975548,-34.393349472242));
#65676=CARTESIAN_POINT('Ctrl Pts',(5.21931476104331,5.96146863092521,-34.3685918498023));
#65677=CARTESIAN_POINT('Ctrl Pts',(4.8771937497999,6.24446457849056,-34.3537799423491));
#65678=CARTESIAN_POINT('Ctrl Pts',(4.2517640016512,6.67890251538361,-34.3277169275132));
#65679=CARTESIAN_POINT('Ctrl Pts',(3.9796377923198,6.84453749619405,-34.3166434870554));
#65680=CARTESIAN_POINT('Ctrl Pts',(3.66920515596642,7.008704407714,-34.3034978306381));
#65681=CARTESIAN_POINT('Ctrl Pts',(3.64001889965825,7.02390677009814,-34.3022569942088));
#65682=CARTESIAN_POINT('Ctrl Pts',(3.52018126211033,7.08537955737316,-34.2971386388032));
#65683=CARTESIAN_POINT('Ctrl Pts',(3.42873911143441,7.13007896443768,-34.293178290537));
#65684=CARTESIAN_POINT('Ctrl Pts',(3.32550939752141,7.17809544456404,-34.2886180010974));
#65685=CARTESIAN_POINT('Ctrl Pts',(3.31454345721508,7.18316564143365,-34.2881324432548));
#65686=CARTESIAN_POINT('Ctrl Pts',(3.29852262923274,7.19052851117672,-34.2874214040077));
#65687=CARTESIAN_POINT('Ctrl Pts',(3.29347702608026,7.19284094666214,-34.2871972318837));
#65688=CARTESIAN_POINT('Ctrl Pts',(3.28453421728705,7.19692811645605,-34.2867994953801));
#65689=CARTESIAN_POINT('Ctrl Pts',(3.28063799115679,7.19870500220724,-34.2866260692451));
#65690=CARTESIAN_POINT('Ctrl Pts',(3.27254782269935,7.20238661593111,-34.2862656792296));
#65691=CARTESIAN_POINT('Ctrl Pts',(3.26835365679055,7.20429084582015,-34.2860786837615));
#65692=CARTESIAN_POINT('Ctrl Pts',(3.25754784847799,7.20918550680156,-34.2855965047311));
#65693=CARTESIAN_POINT('Ctrl Pts',(3.2509337628638,7.21217050030017,-34.2853009787966));
#65694=CARTESIAN_POINT('Ctrl Pts',(3.22346149783864,7.22452349957682,-34.28407188963));
#65695=CARTESIAN_POINT('Ctrl Pts',(3.20256704343217,7.23381007047417,-34.2831332797168));
#65696=CARTESIAN_POINT('Ctrl Pts',(3.10705129585717,7.27576724201358,-34.2788262157856));
#65697=CARTESIAN_POINT('Ctrl Pts',(3.03197055622898,7.30737370099201,-34.2753952287199));
#65698=CARTESIAN_POINT('Ctrl Pts',(2.79829834041538,7.40152062994559,-34.2646073244767));
#65699=CARTESIAN_POINT('Ctrl Pts',(2.63816879594159,7.46009656462854,-34.257060766031));
#65700=CARTESIAN_POINT('Ctrl Pts',(2.16998481309971,7.61440050673667,-34.2347985550791));
#65701=CARTESIAN_POINT('Ctrl Pts',(1.85781035825427,7.69652251551661,-34.2197228795837));
#65702=CARTESIAN_POINT('Ctrl Pts',(0.841785984186737,7.89837001423378,-34.1714190552531));
#65703=CARTESIAN_POINT('Ctrl Pts',(0.126352228757221,7.94211774774373,-34.1389048366125));
#65704=CARTESIAN_POINT('Ctrl Pts',(-0.633270771559198,7.88575932885764,
-34.1077214463337));
#65705=CARTESIAN_POINT('Ctrl Pts',(-0.681179630311586,7.88176544186874,
-34.1057670684238));
#65706=CARTESIAN_POINT('Ctrl Pts',(-0.743645628450338,7.87598419538801,
-34.1032345218652));
#65707=CARTESIAN_POINT('Ctrl Pts',(-0.758237850520886,7.87459276608903,
-34.1026440288978));
#65708=CARTESIAN_POINT('Ctrl Pts',(-0.781569086497848,7.87230258171593,
-34.1017016683943));
#65709=CARTESIAN_POINT('Ctrl Pts',(-0.79031058328466,7.87142981659932,-34.1013489920002));
#65710=CARTESIAN_POINT('Ctrl Pts',(-0.806064725748986,7.8698303896959,-34.1007141010258));
#65711=CARTESIAN_POINT('Ctrl Pts',(-0.813077881343419,7.86910891167922,
-34.1004317254306));
#65712=CARTESIAN_POINT('Ctrl Pts',(-0.829536348111731,7.86739351046913,
-34.0997696399199));
#65713=CARTESIAN_POINT('Ctrl Pts',(-0.838980861862348,7.86639195029397,
-34.0993901680515));
#65714=CARTESIAN_POINT('Ctrl Pts',(-0.866226760906352,7.8634529845493,-34.0982967664704));
#65715=CARTESIAN_POINT('Ctrl Pts',(-0.884023453044639,7.86147213830416,
-34.0975841884575));
#65716=CARTESIAN_POINT('Ctrl Pts',(-1.00386127618572,7.84772160733433,-34.0927966269589));
#65717=CARTESIAN_POINT('Ctrl Pts',(-1.1056735946487,7.83402570540929,-34.0887818242651));
#65718=CARTESIAN_POINT('Ctrl Pts',(-1.38576151356889,7.79077871807958,-34.0778655749685));
#65719=CARTESIAN_POINT('Ctrl Pts',(-1.56333844745471,7.75709644901095,-34.0710903483388));
#65720=CARTESIAN_POINT('Ctrl Pts',(-1.9133987348326,7.67818745085649,-34.0579264306725));
#65721=CARTESIAN_POINT('Ctrl Pts',(-2.08581565796202,7.63315355667764,-34.0515373613274));
#65722=CARTESIAN_POINT('Ctrl Pts',(-2.30940231155686,7.56661222368156,-34.0432900876323));
#65723=CARTESIAN_POINT('Ctrl Pts',(-2.36206998616337,7.55033674883141,-34.0413500465401));
#65724=CARTESIAN_POINT('Ctrl Pts',(-2.77134181080822,7.41916116884508,-34.0262772393355));
#65725=CARTESIAN_POINT('Ctrl Pts',(-3.119539543831,7.27961221287191,-34.0134931406521));
#65726=CARTESIAN_POINT('Ctrl Pts',(-3.77475243938495,6.96134483563091,-33.9877902085086));
#65727=CARTESIAN_POINT('Ctrl Pts',(-4.08224722029417,6.78559840237176,-33.9748998792063));
#65728=CARTESIAN_POINT('Ctrl Pts',(-4.40755640575439,6.5695294518865,-33.9594533526562));
#65729=CARTESIAN_POINT('Ctrl Pts',(-4.43801695643573,6.54899046638664,-33.9579904810914));
#65730=CARTESIAN_POINT('Ctrl Pts',(-4.47875111654204,6.52110947776384,-33.9560128820582));
#65731=CARTESIAN_POINT('Ctrl Pts',(-4.48915209373867,6.5139537810832,-33.9555060415567));
#65732=CARTESIAN_POINT('Ctrl Pts',(-4.50542879572151,6.50269818609319,-33.9547099627527));
#65733=CARTESIAN_POINT('Ctrl Pts',(-4.51131617923028,6.49861513427263,-33.9544214164643));
#65734=CARTESIAN_POINT('Ctrl Pts',(-4.52259967333522,6.49076701850407,-33.9538672601218));
#65735=CARTESIAN_POINT('Ctrl Pts',(-4.52799665074761,6.48700320828363,-33.9536017007683));
#65736=CARTESIAN_POINT('Ctrl Pts',(-4.54065392646536,6.4781526307505,-33.9529777261907));
#65737=CARTESIAN_POINT('Ctrl Pts',(-4.5479103759164,6.47306038896221,-33.9526190937365));
#65738=CARTESIAN_POINT('Ctrl Pts',(-4.56289789360019,6.46250519735602,-33.951876515904));
#65739=CARTESIAN_POINT('Ctrl Pts',(-4.57062774541276,6.4570405469782,-33.9514925047066));
#65740=CARTESIAN_POINT('Ctrl Pts',(-4.60793025930997,6.43056883681158,-33.9496344524702));
#65741=CARTESIAN_POINT('Ctrl Pts',(-4.63736778742327,6.40937257463789,-33.9481532470131));
#65742=CARTESIAN_POINT('Ctrl Pts',(-4.78777251946277,6.29949620433307,-33.9405116945555));
#65743=CARTESIAN_POINT('Ctrl Pts',(-4.90634320912309,6.20759310774439,-33.9342417078726));
#65744=CARTESIAN_POINT('Ctrl Pts',(-5.31970208808019,5.86795737886039,-33.9116316095972));
#65745=CARTESIAN_POINT('Ctrl Pts',(-5.59893574946353,5.60214870551604,-33.8949676080558));
#65746=CARTESIAN_POINT('Ctrl Pts',(-5.97609805917676,5.1866369664785,-33.8708841312394));
#65747=CARTESIAN_POINT('Ctrl Pts',(-6.09010428659148,5.05228483686145,-33.8633542715402));
#65748=CARTESIAN_POINT('Ctrl Pts',(-6.58127375678991,4.43265251240791,-33.8297807581608));
#65749=CARTESIAN_POINT('Ctrl Pts',(-6.9056123193095,3.90821284940221,-33.8044384159982));
#65750=CARTESIAN_POINT('Ctrl Pts',(-7.19813126015926,3.28277149173211,-33.7763617770897));
#65751=CARTESIAN_POINT('Ctrl Pts',(-7.22929696790898,3.2135568746672,-33.7732854786019));
#65752=CARTESIAN_POINT('Ctrl Pts',(-7.27088453514792,3.11752870281932,-33.7690596351629));
#65753=CARTESIAN_POINT('Ctrl Pts',(-7.28216330227458,3.09109119615708,-33.7679005749624));
#65754=CARTESIAN_POINT('Ctrl Pts',(-7.30129562816427,3.04555896363137,-33.7659118063905));
#65755=CARTESIAN_POINT('Ctrl Pts',(-7.30921896385016,3.02649391081043,-33.7650813047093));
#65756=CARTESIAN_POINT('Ctrl Pts',(-7.32541116249065,2.98709792438398,-33.7633697208899));
#65757=CARTESIAN_POINT('Ctrl Pts',(-7.3336702352314,2.96676315094066,-33.7624887592621));
#65758=CARTESIAN_POINT('Ctrl Pts',(-7.3498307880992,2.92649417867642,-33.7607490815807));
#65759=CARTESIAN_POINT('Ctrl Pts',(-7.35773605629634,2.90656170082227,-33.7598903274552));
#65760=CARTESIAN_POINT('Ctrl Pts',(-7.37584723585191,2.86034847127394,-33.7579047188519));
#65761=CARTESIAN_POINT('Ctrl Pts',(-7.38599390619506,2.83404478597447,-33.756778577526));
#65762=CARTESIAN_POINT('Ctrl Pts',(-7.41190360055456,2.76579356387896,-33.7538668056964));
#65763=CARTESIAN_POINT('Ctrl Pts',(-7.42745124224312,2.72376524248096,-33.7520837746251));
#65764=CARTESIAN_POINT('Ctrl Pts',(-7.59669977809516,2.25402596861566,-33.7322634098724));
#65765=CARTESIAN_POINT('Ctrl Pts',(-7.71362711179566,1.81396055494999,-33.7147474440197));
#65766=CARTESIAN_POINT('Ctrl Pts',(-7.82181301429372,1.19696049024682,-33.6906766901119));
#65767=CARTESIAN_POINT('Ctrl Pts',(-7.84597545822106,1.02671407996487,-33.6840775606361));
#65768=CARTESIAN_POINT('Ctrl Pts',(-7.87486832308192,0.761201646125015,
-33.6737573560437));
#65769=CARTESIAN_POINT('Ctrl Pts',(-7.88345596015881,0.666408967094082,
-33.6700670649077));
#65770=CARTESIAN_POINT('Ctrl Pts',(-7.90097122667123,0.424580745398112,
-33.6606078799385));
#65771=CARTESIAN_POINT('Ctrl Pts',(-7.90750635809786,0.277410544480438,
-33.6548094366254));
#65772=CARTESIAN_POINT('Ctrl Pts',(-7.91031987236066,0.106413949164605,
-33.6479680406686));
#65773=CARTESIAN_POINT('Ctrl Pts',(-7.91060355106177,0.0826792966977804,
-33.6470160946721));
#65774=CARTESIAN_POINT('Ctrl Pts',(-7.91087363748045,0.0464312653507314,
-33.6455583962039));
#65775=CARTESIAN_POINT('Ctrl Pts',(-7.91093718192898,0.0339186198397731,
-33.64505451301));
#65776=CARTESIAN_POINT('Ctrl Pts',(-7.91098859675916,0.0149172626381395,
-33.6442883065941));
#65777=CARTESIAN_POINT('Ctrl Pts',(-7.91099817097294,0.0084286091475209,
-33.6440264783865));
#65778=CARTESIAN_POINT('Ctrl Pts',(-7.91099994589624,0.00119061020498363,
-33.6437342135727));
#65779=CARTESIAN_POINT('Ctrl Pts',(-7.91100002318357,0.000441261981302332,
-33.6437039530873));
#65780=CARTESIAN_POINT('Ctrl Pts',(-7.91099999400094,-0.000308086119090196,
-33.6436736902287));
#65781=CARTESIAN_POINT('',(-7.91099998316719,0.000516070481359765,-29.6338967485033));
#65782=CARTESIAN_POINT('Ctrl Pts',(-7.91099999400114,-0.000308081041544692,
-33.6436736904337));
#65783=CARTESIAN_POINT('Ctrl Pts',(-7.91099975116352,-0.00654374027287683,
-33.6434218597107));
#65784=CARTESIAN_POINT('Ctrl Pts',(-7.91099213565916,-0.012779390569126,
-33.6431698646668));
#65785=CARTESIAN_POINT('Ctrl Pts',(-7.91094622120392,-0.0318815649900821,
-33.6423974103053));
#65786=CARTESIAN_POINT('Ctrl Pts',(-7.91088390541829,-0.0447479894069168,
-33.6418764260389));
#65787=CARTESIAN_POINT('Ctrl Pts',(-7.91060669521863,-0.0828106997961559,
-33.640333213343));
#65788=CARTESIAN_POINT('Ctrl Pts',(-7.91030281151989,-0.108006104068315,
-33.6393091173118));
#65789=CARTESIAN_POINT('Ctrl Pts',(-7.90759339903516,-0.268900999890681,
-33.6327538553811));
#65790=CARTESIAN_POINT('Ctrl Pts',(-7.90181651311258,-0.404519133671654,
-33.6271582775097));
#65791=CARTESIAN_POINT('Ctrl Pts',(-7.88637549202989,-0.630236467805673,
-33.6177630874385));
#65792=CARTESIAN_POINT('Ctrl Pts',(-7.87864718876571,-0.720440611788852,
-33.6139864299638));
#65793=CARTESIAN_POINT('Ctrl Pts',(-7.84943820910063,-1.00404175163524,
-33.602059726394));
#65794=CARTESIAN_POINT('Ctrl Pts',(-7.8223700537451,-1.19679003749189,-33.5938773133038));
#65795=CARTESIAN_POINT('Ctrl Pts',(-7.70641831644982,-1.84724733058121,
-33.5661346377338));
#65796=CARTESIAN_POINT('Ctrl Pts',(-7.58421084998201,-2.29803817935784,
-33.5467353136327));
#65797=CARTESIAN_POINT('Ctrl Pts',(-7.4066564329207,-2.77985630186073,-33.5258627700985));
#65798=CARTESIAN_POINT('Ctrl Pts',(-7.38989459555859,-2.82411375031992,
-33.5239436005063));
#65799=CARTESIAN_POINT('Ctrl Pts',(-7.36143836923563,-2.89726029611382,
-33.5207679244007));
#65800=CARTESIAN_POINT('Ctrl Pts',(-7.34996862211976,-2.92623535466211,
-33.5195089751718));
#65801=CARTESIAN_POINT('Ctrl Pts',(-7.32901452298634,-2.97826942052895,
-33.5172461328413));
#65802=CARTESIAN_POINT('Ctrl Pts',(-7.31959180344659,-3.00135277085317,
-33.5162415802156));
#65803=CARTESIAN_POINT('Ctrl Pts',(-7.30016355598999,-3.04831152900338,
-33.5141964220223));
#65804=CARTESIAN_POINT('Ctrl Pts',(-7.29014964339136,-3.07218314953111,
-33.5131559206929));
#65805=CARTESIAN_POINT('Ctrl Pts',(-7.26822744566847,-3.12373151517014,
-33.5109070720977));
#65806=CARTESIAN_POINT('Ctrl Pts',(-7.25627784508661,-3.15139026839842,
-33.5096991830757));
#65807=CARTESIAN_POINT('Ctrl Pts',(-7.22337076328335,-3.22637800053255,
-33.5064206157943));
#65808=CARTESIAN_POINT('Ctrl Pts',(-7.20210627459281,-3.27357074674933,
-33.5043531868903));
#65809=CARTESIAN_POINT('Ctrl Pts',(-7.0934302443917,-3.50857242883045,-33.4940338036087));
#65810=CARTESIAN_POINT('Ctrl Pts',(-6.99912780718079,-3.69310769745149,
-33.4858478040287));
#65811=CARTESIAN_POINT('Ctrl Pts',(-6.69806615845088,-4.22918808858231,
-33.4616902344549));
#65812=CARTESIAN_POINT('Ctrl Pts',(-6.47125863300228,-4.56869292762793,
-33.4459926729266));
#65813=CARTESIAN_POINT('Ctrl Pts',(-6.11656342129852,-5.01988039722635,
-33.4243657770923));
#65814=CARTESIAN_POINT('Ctrl Pts',(-6.00974699848067,-5.14727978717806,
-33.4181558888902));
#65815=CARTESIAN_POINT('Ctrl Pts',(-5.64252241837052,-5.55823890907365,
-33.3976443985068));
#65816=CARTESIAN_POINT('Ctrl Pts',(-5.36545142205661,-5.82614743134477,
-33.3835042222331));
#65817=CARTESIAN_POINT('Ctrl Pts',(-4.95439511978196,-6.16932463678031,
-33.3631157373137));
#65818=CARTESIAN_POINT('Ctrl Pts',(-4.83606915140695,-6.26250988370454,
-33.3573027937192));
#65819=CARTESIAN_POINT('Ctrl Pts',(-4.68239720516316,-6.37657762611485,
-33.3497399113811));
#65820=CARTESIAN_POINT('Ctrl Pts',(-4.64944723928385,-6.40064263247512,
-33.3481174870228));
#65821=CARTESIAN_POINT('Ctrl Pts',(-4.60888887047265,-6.42978599599392,
-33.346117736105));
#65822=CARTESIAN_POINT('Ctrl Pts',(-4.60145557970969,-6.43510770086762,
-33.3457511238254));
#65823=CARTESIAN_POINT('Ctrl Pts',(-4.58714950908,-6.4453123632409,-33.3450453017315));
#65824=CARTESIAN_POINT('Ctrl Pts',(-4.58027811266058,-6.45019724414681,
-33.3447061789804));
#65825=CARTESIAN_POINT('Ctrl Pts',(-4.56850809678264,-6.45853626584105,
-33.3441250911654));
#65826=CARTESIAN_POINT('Ctrl Pts',(-4.56361332744736,-6.46199584686292,
-33.3438833751956));
#65827=CARTESIAN_POINT('Ctrl Pts',(-4.55357960874533,-6.46907050699592,
-33.343387752268));
#65828=CARTESIAN_POINT('Ctrl Pts',(-4.54844027635345,-6.47268503248875,
-33.3431338199898));
#65829=CARTESIAN_POINT('Ctrl Pts',(-4.53472404981306,-6.48230733988631,
-33.3424559032936));
#65830=CARTESIAN_POINT('Ctrl Pts',(-4.52613954119064,-6.48830420903565,
-33.3420314068993));
#65831=CARTESIAN_POINT('Ctrl Pts',(-4.49534808729745,-6.5097233096708,-33.3405079509229));
#65832=CARTESIAN_POINT('Ctrl Pts',(-4.47307418059586,-6.52504860857923,
-33.3394043427976));
#65833=CARTESIAN_POINT('Ctrl Pts',(-4.13933728495706,-6.7521604389403,-33.3228389091674));
#65834=CARTESIAN_POINT('Ctrl Pts',(-3.81327791381509,-6.94151182641307,
-33.3061051961278));
#65835=CARTESIAN_POINT('Ctrl Pts',(-3.22345567403898,-7.22991599444711,
-33.2761890818522));
#65836=CARTESIAN_POINT('Ctrl Pts',(-2.96551324051819,-7.33948783377742,
-33.2632259919968));
#65837=CARTESIAN_POINT('Ctrl Pts',(-2.60312049815171,-7.47119949869815,
-33.2455187866376));
#65838=CARTESIAN_POINT('Ctrl Pts',(-2.50322273719411,-7.50526046411354,
-33.2406877605261));
#65839=CARTESIAN_POINT('Ctrl Pts',(-2.26771995944067,-7.58033178706349,
-33.2294387985025));
#65840=CARTESIAN_POINT('Ctrl Pts',(-2.13163373923896,-7.61971935969843,
-33.2230457069636));
#65841=CARTESIAN_POINT('Ctrl Pts',(-1.72251794331189,-7.72631114015468,
-33.2041967822373));
#65842=CARTESIAN_POINT('Ctrl Pts',(-1.44687696458316,-7.78264209645099,
-33.1919903336011));
#65843=CARTESIAN_POINT('Ctrl Pts',(-1.04657423384607,-7.84244075222704,
-33.1750408360357));
#65844=CARTESIAN_POINT('Ctrl Pts',(-0.92392997689602,-7.8578336525633,-33.1699497776056));
#65845=CARTESIAN_POINT('Ctrl Pts',(-0.781739138214376,-7.87230453199216,
-33.1641616305432));
#65846=CARTESIAN_POINT('Ctrl Pts',(-0.762499328266004,-7.87419135566427,
-33.1633808409355));
#65847=CARTESIAN_POINT('Ctrl Pts',(-0.733275815145492,-7.87694915584677,
-33.1621985097021));
#65848=CARTESIAN_POINT('Ctrl Pts',(-0.72329711811362,-7.87787171161783,
-33.1617954292195));
#65849=CARTESIAN_POINT('Ctrl Pts',(-0.706003986697468,-7.87943737106048,
-33.1610979917474));
#65850=CARTESIAN_POINT('Ctrl Pts',(-0.698690371053566,-7.88008925580459,
-33.1608033729948));
#65851=CARTESIAN_POINT('Ctrl Pts',(-0.683504845477504,-7.88142148065165,
-33.1601923519832));
#65852=CARTESIAN_POINT('Ctrl Pts',(-0.675632800335419,-7.88210021181129,
-33.1598759980345));
#65853=CARTESIAN_POINT('Ctrl Pts',(-0.656474966494718,-7.8837230975129,
-33.1591070566646));
#65854=CARTESIAN_POINT('Ctrl Pts',(-0.645188127303895,-7.88465481435837,
-33.1586548407356));
#65855=CARTESIAN_POINT('Ctrl Pts',(-0.602655710461948,-7.88807388178188,
-33.156953762904));
#65856=CARTESIAN_POINT('Ctrl Pts',(-0.571397260350143,-7.89039977872344,
-33.1557097183328));
#65857=CARTESIAN_POINT('Ctrl Pts',(-0.0348851117538426,-7.92711596220801,
-33.1344603052237));
#65858=CARTESIAN_POINT('Ctrl Pts',(0.472522377447815,-7.91310167155002,
-33.1160293912721));
#65859=CARTESIAN_POINT('Ctrl Pts',(1.2543879991653,-7.81598410215948,-33.0884101257007));
#65860=CARTESIAN_POINT('Ctrl Pts',(1.5315762728853,-7.76642594525951,-33.0787525461689));
#65861=CARTESIAN_POINT('Ctrl Pts',(2.11624890266608,-7.62936831474116,-33.0579415421913));
#65862=CARTESIAN_POINT('Ctrl Pts',(2.42225881325035,-7.53779902730156,-33.0467791582183));
#65863=CARTESIAN_POINT('Ctrl Pts',(2.8428723242534,-7.38367125612125,-33.0302010632184));
#65864=CARTESIAN_POINT('Ctrl Pts',(2.96275347547337,-7.33638969189162,-33.0253285447979));
#65865=CARTESIAN_POINT('Ctrl Pts',(3.14015679321238,-7.26136372225862,-33.0178320876334));
#65866=CARTESIAN_POINT('Ctrl Pts',(3.19858482446452,-7.23581666043191,-33.0153148580121));
#65867=CARTESIAN_POINT('Ctrl Pts',(3.26715385952687,-7.20484269249831,-33.0123013358167));
#65868=CARTESIAN_POINT('Ctrl Pts',(3.27759672206606,-7.20009807509195,-33.0118407943475));
#65869=CARTESIAN_POINT('Ctrl Pts',(3.29303702766819,-7.19304236395944,-33.0111575439482));
#65870=CARTESIAN_POINT('Ctrl Pts',(3.29804246726797,-7.19074872312905,-33.0109356867872));
#65871=CARTESIAN_POINT('Ctrl Pts',(3.30816227481626,-7.18609873802644,-33.0104864199762));
#65872=CARTESIAN_POINT('Ctrl Pts',(3.31327652928834,-7.1837421549929,-33.0102589988858));
#65873=CARTESIAN_POINT('Ctrl Pts',(3.32317344899002,-7.17916896410884,-33.0098181820529));
#65874=CARTESIAN_POINT('Ctrl Pts',(3.32795642441959,-7.17695303205271,-33.0096048184951));
#65875=CARTESIAN_POINT('Ctrl Pts',(3.33932479184172,-7.17167230811722,-33.0090969182399));
#65876=CARTESIAN_POINT('Ctrl Pts',(3.34590817657788,-7.16860322753352,-33.0088021803645));
#65877=CARTESIAN_POINT('Ctrl Pts',(3.36919929717044,-7.15770616344069,-33.0077572852488));
#65878=CARTESIAN_POINT('Ctrl Pts',(3.38588378471459,-7.14982883814051,-33.0070048536794));
#65879=CARTESIAN_POINT('Ctrl Pts',(3.65917911901093,-7.01962548740865,-32.9946171728656));
#65880=CARTESIAN_POINT('Ctrl Pts',(3.90902888102771,-6.88361897579363,-32.9823923633244));
#65881=CARTESIAN_POINT('Ctrl Pts',(4.51993206419288,-6.50706969771793,-32.9510556570855));
#65882=CARTESIAN_POINT('Ctrl Pts',(4.86956790317307,-6.24972560429389,-32.9317859898353));
#65883=CARTESIAN_POINT('Ctrl Pts',(5.47059121383305,-5.72615240501683,-32.8973174829665));
#65884=CARTESIAN_POINT('Ctrl Pts',(5.72803002127639,-5.46862779329378,-32.8819914389672));
#65885=CARTESIAN_POINT('Ctrl Pts',(6.01100357535518,-5.14356678559633,-32.8644090147828));
#65886=CARTESIAN_POINT('Ctrl Pts',(6.05450967967861,-5.0922839641663,-32.8616817998936));
#65887=CARTESIAN_POINT('Ctrl Pts',(6.11120313294994,-5.02370277025904,-32.8580935744274));
#65888=CARTESIAN_POINT('Ctrl Pts',(6.12498018024438,-5.0068963493628,-32.8572188452947));
#65889=CARTESIAN_POINT('Ctrl Pts',(6.14816722751216,-4.97837188150031,-32.8557418632176));
#65890=CARTESIAN_POINT('Ctrl Pts',(6.1576133824918,-4.96668342876062,-32.855138793822));
#65891=CARTESIAN_POINT('Ctrl Pts',(6.17575703400108,-4.94410157320073,-32.8539777716219));
#65892=CARTESIAN_POINT('Ctrl Pts',(6.18445915477627,-4.93321196315864,-32.8534197177471));
#65893=CARTESIAN_POINT('Ctrl Pts',(6.204370724138,-4.90815964982803,-32.8521400101731));
#65894=CARTESIAN_POINT('Ctrl Pts',(6.21556055231134,-4.89398143174669,-32.8514187841809));
#65895=CARTESIAN_POINT('Ctrl Pts',(6.25071236576182,-4.84912684158986,-32.8491464516005));
#65896=CARTESIAN_POINT('Ctrl Pts',(6.27449667331526,-4.81831170944602,-32.8475990536365));
#65897=CARTESIAN_POINT('Ctrl Pts',(6.45048905139206,-4.58678159439591,-32.8360721331522));
#65898=CARTESIAN_POINT('Ctrl Pts',(6.59326381190027,-4.3790700091061,-32.8262936934251));
#65899=CARTESIAN_POINT('Ctrl Pts',(7.02530206741455,-3.68137124254638,-32.7950208390114));
#65900=CARTESIAN_POINT('Ctrl Pts',(7.27169732556693,-3.16698266687693,-32.774464149447));
#65901=CARTESIAN_POINT('Ctrl Pts',(7.54446197269405,-2.39338586603758,-32.7440686361809));
#65902=CARTESIAN_POINT('Ctrl Pts',(7.61674565110016,-2.15229622553774,-32.7346402846619));
#65903=CARTESIAN_POINT('Ctrl Pts',(7.7016896927013,-1.81053084840643,-32.7209641919364));
#65904=CARTESIAN_POINT('Ctrl Pts',(7.72409479258239,-1.71242656060331,-32.7170028856897));
#65905=CARTESIAN_POINT('Ctrl Pts',(7.74767715787882,-1.59926355688924,-32.7123714068681));
#65906=CARTESIAN_POINT('Ctrl Pts',(7.75069067405599,-1.58459437662371,-32.7117698396851));
#65907=CARTESIAN_POINT('Ctrl Pts',(7.75493763748704,-1.5636190476616,-32.7109078686173));
#65908=CARTESIAN_POINT('Ctrl Pts',(7.75620509241316,-1.55731976537862,-32.7106487714502));
#65909=CARTESIAN_POINT('Ctrl Pts',(7.75873682595479,-1.54465722897979,-32.7101274713721));
#65910=CARTESIAN_POINT('Ctrl Pts',(7.76000095447597,-1.53829394970195,-32.7098652628382));
#65911=CARTESIAN_POINT('Ctrl Pts',(7.76241052815726,-1.52608625628955,-32.7093617551096));
#65912=CARTESIAN_POINT('Ctrl Pts',(7.76355720446431,-1.52024208666437,-32.7091205046364));
#65913=CARTESIAN_POINT('Ctrl Pts',(7.76623389114372,-1.50651803231158,-32.7085534729951));
#65914=CARTESIAN_POINT('Ctrl Pts',(7.76775850793353,-1.4986371126418,-32.708227476838));
#65915=CARTESIAN_POINT('Ctrl Pts',(7.77219662212758,-1.47550726382906,-32.7072695525705));
#65916=CARTESIAN_POINT('Ctrl Pts',(7.77507721932865,-1.46025211775057,-32.7066362908509));
#65917=CARTESIAN_POINT('Ctrl Pts',(7.80109650128312,-1.32019862599851,-32.7008083616989));
#65918=CARTESIAN_POINT('Ctrl Pts',(7.82127073023713,-1.1948860339039,-32.6954821733052));
#65919=CARTESIAN_POINT('Ctrl Pts',(7.85493456737977,-0.948077779458153,
-32.6847651062696));
#65920=CARTESIAN_POINT('Ctrl Pts',(7.86863920814285,-0.826658045808646,
-32.679395370693));
#65921=CARTESIAN_POINT('Ctrl Pts',(7.93283774152335,-0.109108229877746,
-32.6472747806219));
#65922=CARTESIAN_POINT('Ctrl Pts',(7.91839076644309,0.490888276221883,-32.6190150259049));
#65923=CARTESIAN_POINT('Ctrl Pts',(7.78256157320981,1.47323180602296,-32.5746772523025));
#65924=CARTESIAN_POINT('Ctrl Pts',(7.69968531600709,1.85838127856973,-32.5577631630825));
#65925=CARTESIAN_POINT('Ctrl Pts',(7.58151361412394,2.25946469655219,-32.5408113548146));
#65926=CARTESIAN_POINT('Ctrl Pts',(7.57443194662476,2.28309222259275,-32.5398150713345));
#65927=CARTESIAN_POINT('Ctrl Pts',(7.56416393225476,2.31677713438323,-32.5383980022589));
#65928=CARTESIAN_POINT('Ctrl Pts',(7.56106782853289,2.32686174447559,-32.5379741820458));
#65929=CARTESIAN_POINT('Ctrl Pts',(7.55568716098863,2.34426348430817,-32.5372435747448));
#65930=CARTESIAN_POINT('Ctrl Pts',(7.55341212064429,2.35158352918303,-32.5369364667325));
#65931=CARTESIAN_POINT('Ctrl Pts',(7.54903676536361,2.3655895731733,-32.53634927484));
#65932=CARTESIAN_POINT('Ctrl Pts',(7.54693819921652,2.37227610767411,-32.5360691322126));
#65933=CARTESIAN_POINT('Ctrl Pts',(7.54200334777107,2.38792690515176,-32.5354138488803));
#65934=CARTESIAN_POINT('Ctrl Pts',(7.539159957983,2.39688892753199,-32.5350389492426));
#65935=CARTESIAN_POINT('Ctrl Pts',(7.52927388934537,2.42785698975545,-32.5337446302023));
#65936=CARTESIAN_POINT('Ctrl Pts',(7.52215075158326,2.4498373305024,-32.5328279448631));
#65937=CARTESIAN_POINT('Ctrl Pts',(7.44531820945634,2.68343005160304,-32.5231067942964));
#65938=CARTESIAN_POINT('Ctrl Pts',(7.36679274350922,2.89204677443386,-32.5146110853235));
#65939=CARTESIAN_POINT('Ctrl Pts',(7.13872410506814,3.42811249674343,-32.4931078208729));
#65940=CARTESIAN_POINT('Ctrl Pts',(6.97546676642291,3.74916302766533,-32.480577571531));
#65941=CARTESIAN_POINT('Ctrl Pts',(6.58503702180654,4.40253312551474,-32.454700110483));
#65942=CARTESIAN_POINT('Ctrl Pts',(6.35324246340856,4.73088854210571,-32.441464045706));
#65943=CARTESIAN_POINT('Ctrl Pts',(5.92275830655111,5.25167726547717,-32.418104336083));
#65944=CARTESIAN_POINT('Ctrl Pts',(5.73710624632675,5.45387675820919,-32.4083269804624));
#65945=CARTESIAN_POINT('Ctrl Pts',(5.47491071862247,5.71121160557892,-32.3942918116502));
#65946=CARTESIAN_POINT('Ctrl Pts',(5.40733532785586,5.7752323545567,-32.3906557489583));
#65947=CARTESIAN_POINT('Ctrl Pts',(5.33084553661318,5.8451790965201,-32.386499268072));
#65948=CARTESIAN_POINT('Ctrl Pts',(5.32302816480776,5.85229903201796,-32.3860740047682));
#65949=CARTESIAN_POINT('Ctrl Pts',(5.31136523167655,5.86287874120508,-32.3854388134704));
#65950=CARTESIAN_POINT('Ctrl Pts',(5.30753048579824,5.86635047541383,-32.3852298468624));
#65951=CARTESIAN_POINT('Ctrl Pts',(5.30096940571265,5.8722787593301,-32.3848721088648));
#65952=CARTESIAN_POINT('Ctrl Pts',(5.29824475679287,5.87473718260022,-32.384723488992));
#65953=CARTESIAN_POINT('Ctrl Pts',(5.29266672137329,5.87976315089379,-32.3844191012588));
#65954=CARTESIAN_POINT('Ctrl Pts',(5.28981317538925,5.88233051634398,-32.3842633189152));
#65955=CARTESIAN_POINT('Ctrl Pts',(5.28297311986841,5.88847558431058,-32.3838897388713));
#65956=CARTESIAN_POINT('Ctrl Pts',(5.27898486140652,5.89205130024744,-32.3836717801424));
#65957=CARTESIAN_POINT('Ctrl Pts',(5.2644324553446,5.90507178012516,-32.3828760122147));
#65958=CARTESIAN_POINT('Ctrl Pts',(5.25384662044065,5.91449215816656,-32.3822962329614));
#65959=CARTESIAN_POINT('Ctrl Pts',(5.07941270129891,6.06888379338286,-32.3727285656124));
#65960=CARTESIAN_POINT('Ctrl Pts',(4.90965746375843,6.20701477127757,-32.363216270089));
#65961=CARTESIAN_POINT('Ctrl Pts',(4.37918376024788,6.60327728527229,-32.3335285653968));
#65962=CARTESIAN_POINT('Ctrl Pts',(4.00228358519768,6.83829200804005,-32.3125315517497));
#65963=CARTESIAN_POINT('Ctrl Pts',(3.30320535949796,7.19651358568546,-32.2760486399687));
#65964=CARTESIAN_POINT('Ctrl Pts',(2.98890427546332,7.33262958075132,-32.2604263714526));
#65965=CARTESIAN_POINT('Ctrl Pts',(2.40679434784978,7.54105467722124,-32.23337234627));
#65966=CARTESIAN_POINT('Ctrl Pts',(2.14212368382098,7.62046538319659,-32.2217270911215));
#65967=CARTESIAN_POINT('Ctrl Pts',(1.85394742782154,7.69072287483236,-32.2097445658143));
#65968=CARTESIAN_POINT('Ctrl Pts',(1.83405579931766,7.69549080542412,-32.2089209132692));
#65969=CARTESIAN_POINT('Ctrl Pts',(1.804868910847,7.70236717199143,-32.2077173889253));
#65970=CARTESIAN_POINT('Ctrl Pts',(1.79558806080767,7.70453602459496,-32.2073354343768));
#65971=CARTESIAN_POINT('Ctrl Pts',(1.77923898479974,7.70832551339784,-32.2066638873008));
#65972=CARTESIAN_POINT('Ctrl Pts',(1.77217241767054,7.70995321049081,-32.2063740518554));
#65973=CARTESIAN_POINT('Ctrl Pts',(1.75840745610898,7.71310387625409,-32.2058103112632));
#65974=CARTESIAN_POINT('Ctrl Pts',(1.75170929862791,7.71462784073159,-32.2055363720951));
#65975=CARTESIAN_POINT('Ctrl Pts',(1.73565106202119,7.71825941800575,-32.2048805401445));
#65976=CARTESIAN_POINT('Ctrl Pts',(1.72628910549807,7.72035873375667,-32.2044989327082));
#65977=CARTESIAN_POINT('Ctrl Pts',(1.69244201488533,7.72788392681384,-32.2031219449185));
#65978=CARTESIAN_POINT('Ctrl Pts',(1.66793480644154,7.73321042370125,-32.2021299754383));
#65979=CARTESIAN_POINT('Ctrl Pts',(1.27838780762894,7.81593822799994,-32.1864413953011));
#65980=CARTESIAN_POINT('Ctrl Pts',(0.908332360471245,7.86753688897652,-32.1726726555434));
#65981=CARTESIAN_POINT('Ctrl Pts',(0.00835074983038954,7.92865252690538,
-32.1407982816582));
#65982=CARTESIAN_POINT('Ctrl Pts',(-0.521515106097596,7.91148496056122,
-32.1234100645256));
#65983=CARTESIAN_POINT('Ctrl Pts',(-1.21729330654373,7.81870113380843,-32.0989485180566));
#65984=CARTESIAN_POINT('Ctrl Pts',(-1.38808789987639,7.79019242940608,-32.0927999834681));
#65985=CARTESIAN_POINT('Ctrl Pts',(-1.71207660744212,7.72511975176859,-32.0806346281471));
#65986=CARTESIAN_POINT('Ctrl Pts',(-1.86538329318018,7.689539726963,-32.0746592061713));
#65987=CARTESIAN_POINT('Ctrl Pts',(-2.04150312302437,7.64308846587454,-32.0674307113828));
#65988=CARTESIAN_POINT('Ctrl Pts',(-2.06545809478339,7.63664973296589,-32.0664396455627));
#65989=CARTESIAN_POINT('Ctrl Pts',(-2.09648790095491,7.62815270934539,-32.0651451671526));
#65990=CARTESIAN_POINT('Ctrl Pts',(-2.1035907835459,7.62619702673632,-32.0648481276027));
#65991=CARTESIAN_POINT('Ctrl Pts',(-2.11515392850836,7.62299588770096,-32.0643633895021));
#65992=CARTESIAN_POINT('Ctrl Pts',(-2.11961586177037,7.62175642772344,-32.0641760564711));
#65993=CARTESIAN_POINT('Ctrl Pts',(-2.12819363664245,7.61936553204851,-32.06381537719));
#65994=CARTESIAN_POINT('Ctrl Pts',(-2.13230963998533,7.61821467701593,-32.0636420660704));
#65995=CARTESIAN_POINT('Ctrl Pts',(-2.14171656790985,7.6155762322766,-32.0632454241767));
#65996=CARTESIAN_POINT('Ctrl Pts',(-2.14700687391039,7.61408646457101,-32.0630219628334));
#65997=CARTESIAN_POINT('Ctrl Pts',(-2.16098721046364,7.61013382659959,-32.0624303966404));
#65998=CARTESIAN_POINT('Ctrl Pts',(-2.16967456145709,7.60766159070037,-32.0620617358865));
#65999=CARTESIAN_POINT('Ctrl Pts',(-2.22580841298331,7.59158311628547,-32.059672823784));
#66000=CARTESIAN_POINT('Ctrl Pts',(-2.27312998747154,7.57754822889774,-32.0576275689743));
#66001=CARTESIAN_POINT('Ctrl Pts',(-2.38671856513298,7.54269976804518,-32.0526477087665));
#66002=CARTESIAN_POINT('Ctrl Pts',(-2.45284811076,7.52145470899978,-32.049690334444));
#66003=CARTESIAN_POINT('Ctrl Pts',(-2.58698096558104,7.47640559113867,-32.0435848420577));
#66004=CARTESIAN_POINT('Ctrl Pts',(-2.65495631547724,7.45253765890907,-32.0404339980243));
#66005=CARTESIAN_POINT('Ctrl Pts',(-2.77988267086951,7.40674666808781,-32.0345499131621));
#66006=CARTESIAN_POINT('Ctrl Pts',(-2.83692500027038,7.38508633429586,-32.0318267332487));
#66007=CARTESIAN_POINT('Ctrl Pts',(-3.5587836452981,7.10138196667477,-31.996947785242));
#66008=CARTESIAN_POINT('Ctrl Pts',(-4.18539840775809,6.75108696618127,-31.9624937419401));
#66009=CARTESIAN_POINT('Ctrl Pts',(-4.93936408894463,6.18376722407008,-31.9203867231155));
#66010=CARTESIAN_POINT('Ctrl Pts',(-5.11618277903207,6.0382927677589,-31.9104217604096));
#66011=CARTESIAN_POINT('Ctrl Pts',(-5.39781378012161,5.78532053022073,-31.8944358069358));
#66012=CARTESIAN_POINT('Ctrl Pts',(-5.50631490771182,5.68214982457405,-31.8882452908753));
#66013=CARTESIAN_POINT('Ctrl Pts',(-5.62568190793324,5.56201496216017,-31.881391030868));
#66014=CARTESIAN_POINT('Ctrl Pts',(-5.63948439736159,5.54801974651152,-31.8805977673115));
#66015=CARTESIAN_POINT('Ctrl Pts',(-5.66013375588702,5.52692537804683,-31.8794099005564));
#66016=CARTESIAN_POINT('Ctrl Pts',(-5.66701969465247,5.51986467681662,-31.8790135982288));
#66017=CARTESIAN_POINT('Ctrl Pts',(-5.67883746072272,5.50770155795427,-31.8783331331016));
#66018=CARTESIAN_POINT('Ctrl Pts',(-5.68377565104897,5.50260535616149,-31.878048695048));
#66019=CARTESIAN_POINT('Ctrl Pts',(-5.69392905745856,5.49209881180137,-31.8774636577124));
#66020=CARTESIAN_POINT('Ctrl Pts',(-5.69914343532038,5.48668766870981,-31.8771630946481));
#66021=CARTESIAN_POINT('Ctrl Pts',(-5.71167409476967,5.47364702660575,-31.876440539001));
#66022=CARTESIAN_POINT('Ctrl Pts',(-5.71898281967478,5.46601026765811,-31.8760188708912));
#66023=CARTESIAN_POINT('Ctrl Pts',(-5.74135282243992,5.44254225861115,-31.8747275532989));
#66024=CARTESIAN_POINT('Ctrl Pts',(-5.75636388964646,5.4266631780618,-31.8738600463295));
#66025=CARTESIAN_POINT('Ctrl Pts',(-5.92870775218247,5.24283379469023,-31.8638881040256));
#66026=CARTESIAN_POINT('Ctrl Pts',(-6.07871146979071,5.06815139237069,-31.8550974647243));
#66027=CARTESIAN_POINT('Ctrl Pts',(-6.67321262052441,4.31140878770776,-31.8194064573866));
#66028=CARTESIAN_POINT('Ctrl Pts',(-7.04337583036219,3.67570134342679,-31.7953324453942));
#66029=CARTESIAN_POINT('Ctrl Pts',(-7.36130324978087,2.89940210962108,-31.7652216831868));
#66030=CARTESIAN_POINT('Ctrl Pts',(-7.39975851398585,2.79980197502376,-31.7613391272579));
#66031=CARTESIAN_POINT('Ctrl Pts',(-7.46945580569004,2.607807025721,-31.7537712966342));
#66032=CARTESIAN_POINT('Ctrl Pts',(-7.50102796752054,2.51555280927087,-31.750098726213));
#66033=CARTESIAN_POINT('Ctrl Pts',(-7.56108482316893,2.32887115202488,-31.7425562914119));
#66034=CARTESIAN_POINT('Ctrl Pts',(-7.58952403819407,2.23445012072022,-31.73868237867));
#66035=CARTESIAN_POINT('Ctrl Pts',(-7.62073256200793,2.12335545137803,-31.7340710950086));
#66036=CARTESIAN_POINT('Ctrl Pts',(-7.62522389075164,2.10716961003202,-31.7333979525943));
#66037=CARTESIAN_POINT('Ctrl Pts',(-7.63201120865279,2.08240361106789,-31.7323660853802));
#66038=CARTESIAN_POINT('Ctrl Pts',(-7.63434436910622,2.07383363401384,-31.7320086746811));
#66039=CARTESIAN_POINT('Ctrl Pts',(-7.6385654724808,2.0582253580658,-31.7313571213943));
#66040=CARTESIAN_POINT('Ctrl Pts',(-7.64045813435538,2.05118833819628,-31.7310631417621));
#66041=CARTESIAN_POINT('Ctrl Pts',(-7.64423883960379,2.03705363330922,-31.7304722061582));
#66042=CARTESIAN_POINT('Ctrl Pts',(-7.64612672711592,2.02995591438787,-31.7301752452873));
#66043=CARTESIAN_POINT('Ctrl Pts',(-7.65145525925875,2.00980982032354,-31.7293317362019));
#66044=CARTESIAN_POINT('Ctrl Pts',(-7.65487239786894,1.99675528502656,-31.7287844125234));
#66045=CARTESIAN_POINT('Ctrl Pts',(-7.66918248491949,1.94150965955897,-31.726465222876));
#66046=CARTESIAN_POINT('Ctrl Pts',(-7.67976005484682,1.89923805015853,-31.7246833763051));
#66047=CARTESIAN_POINT('Ctrl Pts',(-7.83664148386959,1.24953790713281,-31.6972021956544));
#66048=CARTESIAN_POINT('Ctrl Pts',(-7.91082999871584,0.626958964402656,
-31.66983724223));
#66049=CARTESIAN_POINT('Ctrl Pts',(-7.91109466759892,-0.347457805831875,
-31.6282329859476));
#66050=CARTESIAN_POINT('Ctrl Pts',(-7.88801474621749,-0.696693083483909,
-31.6135149405729));
#66051=CARTESIAN_POINT('Ctrl Pts',(-7.83562621999283,-1.09048238114358,
-31.5970167840547));
#66052=CARTESIAN_POINT('Ctrl Pts',(-7.82891799512992,-1.1376436764792,-31.5950420537283));
#66053=CARTESIAN_POINT('Ctrl Pts',(-7.81745870441516,-1.21329907349436,
-31.5918748988473));
#66054=CARTESIAN_POINT('Ctrl Pts',(-7.81297682828593,-1.24183264687565,
-31.5906805534045));
#66055=CARTESIAN_POINT('Ctrl Pts',(-7.75905559585409,-1.5732674538819,-31.5768072149549));
#66056=CARTESIAN_POINT('Ctrl Pts',(-7.69218417252294,-1.87307889726213,
-31.5642139934612));
#66057=CARTESIAN_POINT('Ctrl Pts',(-7.59567359883595,-2.21172036286853,
-31.5499472757927));
#66058=CARTESIAN_POINT('Ctrl Pts',(-7.58291171445534,-2.25508632719177,
-31.5481196431667));
#66059=CARTESIAN_POINT('Ctrl Pts',(-7.56165552687678,-2.32509537312519,
-31.5451680282555));
#66060=CARTESIAN_POINT('Ctrl Pts',(-7.55339044700967,-2.35180687203545,
-31.5440415905585));
#66061=CARTESIAN_POINT('Ctrl Pts',(-7.5384401749273,-2.399232052998,-31.5420411291327));
#66062=CARTESIAN_POINT('Ctrl Pts',(-7.53181079206163,-2.41996299787068,
-31.541166491798));
#66063=CARTESIAN_POINT('Ctrl Pts',(-7.51766472171895,-2.4635783556302,-31.5393259586859));
#66064=CARTESIAN_POINT('Ctrl Pts',(-7.51012889729581,-2.48645634048862,
-31.5383602911232));
#66065=CARTESIAN_POINT('Ctrl Pts',(-7.48988525798992,-2.54698226377594,
-31.5358048334161));
#66066=CARTESIAN_POINT('Ctrl Pts',(-7.4769980624138,-2.58456956291366,-31.534217156352));
#66067=CARTESIAN_POINT('Ctrl Pts',(-7.41440487462207,-2.76274439590827,
-31.5266870249399));
#66068=CARTESIAN_POINT('Ctrl Pts',(-7.36101321425368,-2.90200650837284,
-31.5207899802911));
#66069=CARTESIAN_POINT('Ctrl Pts',(-7.02348621961875,-3.713013987416,-31.4863027288329));
#66070=CARTESIAN_POINT('Ctrl Pts',(-6.65150756393093,-4.34432729815641,
-31.4591922932361));
#66071=CARTESIAN_POINT('Ctrl Pts',(-6.16916204865855,-4.95253163277003,
-31.4283500456975));
#66072=CARTESIAN_POINT('Ctrl Pts',(-6.13963029584588,-4.98909508004706,
-31.426474196967));
#66073=CARTESIAN_POINT('Ctrl Pts',(-6.09910413680891,-5.03836599412793,
-31.4239145313122));
#66074=CARTESIAN_POINT('Ctrl Pts',(-6.08839234084904,-5.0513049661903,-31.4232393010717));
#66075=CARTESIAN_POINT('Ctrl Pts',(-6.07103919780077,-5.07213075193236,
-31.4221475882695));
#66076=CARTESIAN_POINT('Ctrl Pts',(-6.06442350095374,-5.08003886857636,
-31.4217318913639));
#66077=CARTESIAN_POINT('Ctrl Pts',(-6.05060564939187,-5.09649066916684,
-31.4208647227296));
#66078=CARTESIAN_POINT('Ctrl Pts',(-6.04340081586462,-5.1050320707336,-31.4204131727678));
#66079=CARTESIAN_POINT('Ctrl Pts',(-6.02635166138397,-5.12515733901525,
-31.4193461025629));
#66080=CARTESIAN_POINT('Ctrl Pts',(-6.01649201046782,-5.13672813978014,
-31.4187301459302));
#66081=CARTESIAN_POINT('Ctrl Pts',(-5.98386411175924,-5.17479581898658,
-31.4166956491679));
#66082=CARTESIAN_POINT('Ctrl Pts',(-5.9609537915148,-5.20117019004048,-31.4152732298421));
#66083=CARTESIAN_POINT('Ctrl Pts',(-5.90580608055135,-5.26381326938454,
-31.4118647957323));
#66084=CARTESIAN_POINT('Ctrl Pts',(-5.87340829052887,-5.29993873438837,
-31.4098748493547));
#66085=CARTESIAN_POINT('Ctrl Pts',(-5.75200465406127,-5.43283064896739,
-31.402467223556));
#66086=CARTESIAN_POINT('Ctrl Pts',(-5.66092392741577,-5.52767092563341,
-31.3970065564033));
#66087=CARTESIAN_POINT('Ctrl Pts',(-5.26077358381815,-5.92407104147126,
-31.3734943694112));
#66088=CARTESIAN_POINT('Ctrl Pts',(-4.9296589999206,-6.20232423878793,-31.3552500741704));
#66089=CARTESIAN_POINT('Ctrl Pts',(-4.47462468353753,-6.5251485024711,-31.3320447396165));
#66090=CARTESIAN_POINT('Ctrl Pts',(-4.37002468866521,-6.59565871001531,
-31.3268231857919));
#66091=CARTESIAN_POINT('Ctrl Pts',(-4.12213687538663,-6.7542717238362,-31.3147073967786));
#66092=CARTESIAN_POINT('Ctrl Pts',(-3.97763548498383,-6.84036668589475,
-31.3078391026435));
#66093=CARTESIAN_POINT('Ctrl Pts',(-3.78809977310634,-6.94525516157924,
-31.2990624028942));
#66094=CARTESIAN_POINT('Ctrl Pts',(-3.74548646663433,-6.96832837304617,
-31.2971037585309));
#66095=CARTESIAN_POINT('Ctrl Pts',(-3.6769023527847,-7.00465273192349,-31.2939740311931));
#66096=CARTESIAN_POINT('Ctrl Pts',(-3.65106573109852,-7.01815430448605,
-31.2928001024155));
#66097=CARTESIAN_POINT('Ctrl Pts',(-3.60414440196854,-7.04234498672688,
-31.2906771447898));
#66098=CARTESIAN_POINT('Ctrl Pts',(-3.58308530723572,-7.05308297607197,
-31.2897275795047));
#66099=CARTESIAN_POINT('Ctrl Pts',(-3.53303413109263,-7.07832194988251,
-31.2874783007508));
#66100=CARTESIAN_POINT('Ctrl Pts',(-3.5040003957738,-7.09273945905055,-31.2861795145715));
#66101=CARTESIAN_POINT('Ctrl Pts',(-3.41707677125766,-7.13523980924604,
-31.2823083771361));
#66102=CARTESIAN_POINT('Ctrl Pts',(-3.35893186966483,-7.16279537351854,
-31.2797416470523));
#66103=CARTESIAN_POINT('Ctrl Pts',(-2.97726518649957,-7.33800229979876,
-31.2630312364852));
#66104=CARTESIAN_POINT('Ctrl Pts',(-2.64442345671335,-7.46441046931321,
-31.2490443105964));
#66105=CARTESIAN_POINT('Ctrl Pts',(-1.83062750384364,-7.7121845546595,-31.2161459464004));
#66106=CARTESIAN_POINT('Ctrl Pts',(-1.34455963419208,-7.81160457120767,
-31.1976698995017));
#66107=CARTESIAN_POINT('Ctrl Pts',(-0.557261029012222,-7.89692975917552,
-31.1682678806545));
#66108=CARTESIAN_POINT('Ctrl Pts',(-0.260582110359735,-7.91227705620617,
-31.1572768914029));
#66109=CARTESIAN_POINT('Ctrl Pts',(0.144575850814257,-7.91042058861035,
-31.141845536624));
#66110=CARTESIAN_POINT('Ctrl Pts',(0.252879680932102,-7.90769922577814,
-31.1376779733704));
#66111=CARTESIAN_POINT('Ctrl Pts',(0.388978521577137,-7.90148062305087,
-31.1323571733784));
#66112=CARTESIAN_POINT('Ctrl Pts',(0.416858741833247,-7.90005880338862,
-31.131262759116));
#66113=CARTESIAN_POINT('Ctrl Pts',(0.460534313892255,-7.89759961586249,
-31.1295406836525));
#66114=CARTESIAN_POINT('Ctrl Pts',(0.4763351861932,-7.89666235402076,-31.1289161085196));
#66115=CARTESIAN_POINT('Ctrl Pts',(0.53053420741295,-7.89328415998898,-31.1267680880751));
#66116=CARTESIAN_POINT('Ctrl Pts',(0.568916992292914,-7.89061054501134,
-31.1252371718538));
#66117=CARTESIAN_POINT('Ctrl Pts',(0.619321065328954,-7.8867298866248,-31.1232124536208));
#66118=CARTESIAN_POINT('Ctrl Pts',(0.631361596800325,-7.8857751311256,-31.1227277132532));
#66119=CARTESIAN_POINT('Ctrl Pts',(0.649985009579569,-7.88425545884588,
-31.1219762312868));
#66120=CARTESIAN_POINT('Ctrl Pts',(0.656569477659818,-7.8837098610813,-31.1217102054028));
#66121=CARTESIAN_POINT('Ctrl Pts',(0.669706449459131,-7.88260474208809,
-31.1211787685045));
#66122=CARTESIAN_POINT('Ctrl Pts',(0.676258953935233,-7.88204529772041,
-31.1209133606));
#66123=CARTESIAN_POINT('Ctrl Pts',(0.690825885127546,-7.88078329362997,
-31.1203225695147));
#66124=CARTESIAN_POINT('Ctrl Pts',(0.698839946687277,-7.8800766781179,-31.1199970312885));
#66125=CARTESIAN_POINT('Ctrl Pts',(0.722093744835764,-7.87799059256053,
-31.1190509237418));
#66126=CARTESIAN_POINT('Ctrl Pts',(0.737330522670652,-7.87657913365695,
-31.1184291055345));
#66127=CARTESIAN_POINT('Ctrl Pts',(0.846367068153694,-7.86615937655385,
-31.1139651887446));
#66128=CARTESIAN_POINT('Ctrl Pts',(0.939994042255055,-7.85552107058926,
-31.1100547342848));
#66129=CARTESIAN_POINT('Ctrl Pts',(1.15435315451245,-7.82727727986818,-31.100904455957));
#66130=CARTESIAN_POINT('Ctrl Pts',(1.27490171354553,-7.80854815308775,-31.095622016279));
#66131=CARTESIAN_POINT('Ctrl Pts',(1.70456875705568,-7.7315779295109,-31.0764030940466));
#66132=CARTESIAN_POINT('Ctrl Pts',(2.01057796622553,-7.65770280881923,-31.0619939145715));
#66133=CARTESIAN_POINT('Ctrl Pts',(2.85686237701296,-7.39916218104642,-31.0212642570759));
#66134=CARTESIAN_POINT('Ctrl Pts',(3.38279802794428,-7.1739853360649,-30.9950230237459));
#66135=CARTESIAN_POINT('Ctrl Pts',(4.06947196698913,-6.78753305416735,-30.9611753859278));
#66136=CARTESIAN_POINT('Ctrl Pts',(4.2545058690236,-6.67310993921001,-30.9520815792078));
#66137=CARTESIAN_POINT('Ctrl Pts',(4.452947618013,-6.538781951025,-30.9423547502225));
#66138=CARTESIAN_POINT('Ctrl Pts',(4.47124318868071,-6.52628502667661,-30.9414581880409));
#66139=CARTESIAN_POINT('Ctrl Pts',(4.49841805062522,-6.50755512618639,-30.9401267786751));
#66140=CARTESIAN_POINT('Ctrl Pts',(4.50733733985906,-6.5013805291198,-30.9396898302069));
#66141=CARTESIAN_POINT('Ctrl Pts',(4.52262443695468,-6.49075108102595,-30.9389409982033));
#66142=CARTESIAN_POINT('Ctrl Pts',(4.5289984215394,-6.48630516485975,-30.9386287922143));
#66143=CARTESIAN_POINT('Ctrl Pts',(4.5420912619051,-6.47714407312334,-30.9379875280657));
#66144=CARTESIAN_POINT('Ctrl Pts',(4.54880935265136,-6.47242781722705,-30.9376585096318));
#66145=CARTESIAN_POINT('Ctrl Pts',(4.56434665209146,-6.46148413278624,-30.9368976166995));
#66146=CARTESIAN_POINT('Ctrl Pts',(4.57316048614798,-6.45524908332551,-30.9364660199888));
#66147=CARTESIAN_POINT('Ctrl Pts',(4.60087811428871,-6.43555592387886,-30.9351088354027));
#66148=CARTESIAN_POINT('Ctrl Pts',(4.61973554799491,-6.42203261823497,-30.9341856272678));
#66149=CARTESIAN_POINT('Ctrl Pts',(4.90103247327797,-6.21842488961355,-30.9204154852491));
#66150=CARTESIAN_POINT('Ctrl Pts',(5.15162069471398,-6.01246677347793,-30.9081836514859));
#66151=CARTESIAN_POINT('Ctrl Pts',(5.94882546433572,-5.27070814939611,-30.8685838381294));
#66152=CARTESIAN_POINT('Ctrl Pts',(6.4301978690022,-4.67132585070535,-30.8437682332246));
#66153=CARTESIAN_POINT('Ctrl Pts',(6.92775375727652,-3.82582519228611,-30.8078365056906));
#66154=CARTESIAN_POINT('Ctrl Pts',(7.02976558435145,-3.63498329576021,-30.7996450988271));
#66155=CARTESIAN_POINT('Ctrl Pts',(7.13051200700972,-3.42636188930724,-30.7903979936733));
#66156=CARTESIAN_POINT('Ctrl Pts',(7.13715605391671,-3.41250065723276,-30.7897823748592));
#66157=CARTESIAN_POINT('Ctrl Pts',(7.14697082519832,-3.39187041254928,-30.7888644081967));
#66158=CARTESIAN_POINT('Ctrl Pts',(7.15017244975129,-3.38511607039545,-30.7885635932995));
#66159=CARTESIAN_POINT('Ctrl Pts',(7.15563941755037,-3.37354026274542,-30.7880475934594));
#66160=CARTESIAN_POINT('Ctrl Pts',(7.15790947587095,-3.36872102041342,-30.7878326378659));
#66161=CARTESIAN_POINT('Ctrl Pts',(7.16231772733507,-3.35933790702278,-30.7874138609325));
#66162=CARTESIAN_POINT('Ctrl Pts',(7.16445643131997,-3.35477427622103,-30.7872100641228));
#66163=CARTESIAN_POINT('Ctrl Pts',(7.16956372523411,-3.34384902061821,-30.7867219017297));
#66164=CARTESIAN_POINT('Ctrl Pts',(7.17252820822192,-3.33748548831229,-30.7864373424223));
#66165=CARTESIAN_POINT('Ctrl Pts',(7.18139747888165,-3.31838039778606,-30.7855823635895));
#66166=CARTESIAN_POINT('Ctrl Pts',(7.18727679387116,-3.30562709615756,-30.7850107658882));
#66167=CARTESIAN_POINT('Ctrl Pts',(7.23882999771045,-3.19301110735589,-30.7799561324362));
#66168=CARTESIAN_POINT('Ctrl Pts',(7.28245270813326,-3.09222586318413,-30.7753826068113));
#66169=CARTESIAN_POINT('Ctrl Pts',(7.39619358228847,-2.81367219273417,-30.7626677858631));
#66170=CARTESIAN_POINT('Ctrl Pts',(7.46199051755742,-2.6342216983436,-30.754396543991));
#66171=CARTESIAN_POINT('Ctrl Pts',(7.67189178844118,-1.99052403353636,-30.724802594924));
#66172=CARTESIAN_POINT('Ctrl Pts',(7.77967009335558,-1.51554641116677,-30.7031871408693));
#66173=CARTESIAN_POINT('Ctrl Pts',(7.88771849966673,-0.695716921782237,
-30.667719962537));
#66174=CARTESIAN_POINT('Ctrl Pts',(7.91037113883237,-0.355213942632094,
-30.6534900027122));
#66175=CARTESIAN_POINT('Ctrl Pts',(7.91105602012169,0.0238600128303358,
-30.6381300520454));
#66176=CARTESIAN_POINT('Ctrl Pts',(7.91084894626896,0.0620131744865623,
-30.6365892061203));
#66177=CARTESIAN_POINT('Ctrl Pts',(7.91013643208999,0.118283622747458,-30.6343237316644));
#66178=CARTESIAN_POINT('Ctrl Pts',(7.90984472935629,0.136402897178744,-30.6335953192977));
#66179=CARTESIAN_POINT('Ctrl Pts',(7.90921744801982,0.168511634603927,-30.6323063591118));
#66180=CARTESIAN_POINT('Ctrl Pts',(7.908907005286,0.18250149105554,-30.6317453757599));
#66181=CARTESIAN_POINT('Ctrl Pts',(7.90818961924645,0.21137561387696,-30.630588784483));
#66182=CARTESIAN_POINT('Ctrl Pts',(7.90777776946245,0.22625970608043,-30.6299932630263));
#66183=CARTESIAN_POINT('Ctrl Pts',(7.90661705563113,0.264320758550473,-30.6284720976446));
#66184=CARTESIAN_POINT('Ctrl Pts',(7.90580830189384,0.287495787338779,-30.627547467775));
#66185=CARTESIAN_POINT('Ctrl Pts',(7.90222075301944,0.378780691624412,-30.6239113195488));
#66186=CARTESIAN_POINT('Ctrl Pts',(7.89866355399836,0.446857785799987,-30.6212123650041));
#66187=CARTESIAN_POINT('Ctrl Pts',(7.87156157505004,0.862389213760703,-30.6048124122027));
#66188=CARTESIAN_POINT('Ctrl Pts',(7.8259744721659,1.20803051391749,-30.5915094442729));
#66189=CARTESIAN_POINT('Ctrl Pts',(7.62220316891117,2.22819915116485,-30.552584810201));
#66190=CARTESIAN_POINT('Ctrl Pts',(7.39819884383389,2.88606464509801,-30.5281325351967));
#66191=CARTESIAN_POINT('Ctrl Pts',(7.05113323551834,3.58799949102011,-30.4976519169709));
#66192=CARTESIAN_POINT('Ctrl Pts',(7.00934880589826,3.66895745839981,-30.494060726343));
#66193=CARTESIAN_POINT('Ctrl Pts',(6.95934964213475,3.7618587255609,-30.4898352487537));
#66194=CARTESIAN_POINT('Ctrl Pts',(6.95248809044918,3.7745248523972,-30.4892568705016));
#66195=CARTESIAN_POINT('Ctrl Pts',(6.94152802215273,3.79462538135589,-30.488335297493));
#66196=CARTESIAN_POINT('Ctrl Pts',(6.93745205013071,3.8020720822456,-30.4879930667205));
#66197=CARTESIAN_POINT('Ctrl Pts',(6.93025991427406,3.81516186753541,-30.4873900429003));
#66198=CARTESIAN_POINT('Ctrl Pts',(6.92714882041902,3.82080773846862,-30.4871294711461));
#66199=CARTESIAN_POINT('Ctrl Pts',(6.92072410762015,3.83243337371045,-30.4865919252732));
#66200=CARTESIAN_POINT('Ctrl Pts',(6.91740963189957,3.83841265653451,-30.4863149133089));
#66201=CARTESIAN_POINT('Ctrl Pts',(6.90894911680448,3.85362879670824,-30.4856085737933));
#66202=CARTESIAN_POINT('Ctrl Pts',(6.90379231165114,3.86285962954263,-30.4851787618871));
#66203=CARTESIAN_POINT('Ctrl Pts',(6.88301737254324,3.89987290053247,-30.4834499609341));
#66204=CARTESIAN_POINT('Ctrl Pts',(6.86725005879419,3.92757092605988,-30.4821440951859));
#66205=CARTESIAN_POINT('Ctrl Pts',(6.76860172730848,4.09845370468132,-30.4740082398556));
#66206=CARTESIAN_POINT('Ctrl Pts',(6.68142618216043,4.23908297715535,-30.4669420226383));
#66207=CARTESIAN_POINT('Ctrl Pts',(6.51919463786934,4.48334252897653,-30.4540841834948));
#66208=CARTESIAN_POINT('Ctrl Pts',(6.44590830374343,4.58808491743453,-30.4483753981573));
#66209=CARTESIAN_POINT('Ctrl Pts',(6.31501405763401,4.76583197783503,-30.4384047701096));
#66210=CARTESIAN_POINT('Ctrl Pts',(6.25859556829831,4.83968367395317,-30.4341739281798));
#66211=CARTESIAN_POINT('Ctrl Pts',(6.15134952572091,4.97505624425465,-30.4262752009007));
#66212=CARTESIAN_POINT('Ctrl Pts',(6.1008662976941,5.0368359017448,-30.4226127841326));
#66213=CARTESIAN_POINT('Ctrl Pts',(5.58042171337021,5.65443213686781,-30.3854804491462));
#66214=CARTESIAN_POINT('Ctrl Pts',(5.03671743501126,6.14374077407838,-30.3521828128889));
#66215=CARTESIAN_POINT('Ctrl Pts',(4.40298918985832,6.57259326334364,-30.3209082476206));
#66216=CARTESIAN_POINT('Ctrl Pts',(4.37213294565909,6.59315930091494,-30.3194010359288));
#66217=CARTESIAN_POINT('Ctrl Pts',(4.32751036219462,6.62244974296305,-30.317243554153));
#66218=CARTESIAN_POINT('Ctrl Pts',(4.31386012184477,6.63134959012074,-30.3165865302608));
#66219=CARTESIAN_POINT('Ctrl Pts',(4.29194471543767,6.64554195523146,-30.3155363983548));
#66220=CARTESIAN_POINT('Ctrl Pts',(4.28369706581746,6.65086135536977,-30.3151422572139));
#66221=CARTESIAN_POINT('Ctrl Pts',(4.26907029292369,6.66025653698573,-30.3144451502541));
#66222=CARTESIAN_POINT('Ctrl Pts',(4.26269518647914,6.66433853071539,-30.3141419461005));
#66223=CARTESIAN_POINT('Ctrl Pts',(4.24958902082864,6.67270393531837,-30.3135199015106));
#66224=CARTESIAN_POINT('Ctrl Pts',(4.24285731990081,6.67698632751498,-30.3132011003094));
#66225=CARTESIAN_POINT('Ctrl Pts',(4.22563809724778,6.68790383328617,-30.3123874092189));
#66226=CARTESIAN_POINT('Ctrl Pts',(4.21514140173554,6.69452447731995,-30.3118930737478));
#66227=CARTESIAN_POINT('Ctrl Pts',(4.19236714760905,6.70881422091352,-30.3108241647312));
#66228=CARTESIAN_POINT('Ctrl Pts',(4.18008401940079,6.71647438354288,-30.3102499332002));
#66229=CARTESIAN_POINT('Ctrl Pts',(4.14477228199984,6.73836155524108,-30.3086056181984));
#66230=CARTESIAN_POINT('Ctrl Pts',(4.12169148490385,6.75250420519344,-30.3075387458022));
#66231=CARTESIAN_POINT('Ctrl Pts',(4.04459541712736,6.79920188896021,-30.3040010904465));
#66232=CARTESIAN_POINT('Ctrl Pts',(3.99026289614521,6.83122980659411,-30.3015502208364));
#66233=CARTESIAN_POINT('Ctrl Pts',(3.78671200957979,6.94796174178403,-30.2925201123927));
#66234=CARTESIAN_POINT('Ctrl Pts',(3.63512973373935,7.02845617994655,-30.2860966644913));
#66235=CARTESIAN_POINT('Ctrl Pts',(3.19316172133092,7.24502690815435,-30.2681148696377));
#66236=CARTESIAN_POINT('Ctrl Pts',(2.89696188599029,7.36846826317054,-30.2569698250116));
#66237=CARTESIAN_POINT('Ctrl Pts',(1.90094924939149,7.71418302410957,-30.2211059987988));
#66238=CARTESIAN_POINT('Ctrl Pts',(1.17783382901439,7.85713752256069,-30.197786284806));
#66239=CARTESIAN_POINT('Ctrl Pts',(0.403260771362742,7.90082867502684,-30.1673425235347));
#66240=CARTESIAN_POINT('Ctrl Pts',(0.360978219879948,7.90287337602871,-30.1656629086913));
#66241=CARTESIAN_POINT('Ctrl Pts',(0.310393605175625,7.90491275220911,-30.1636302553017));
#66242=CARTESIAN_POINT('Ctrl Pts',(0.302104657898855,7.90523387287599,-30.1632964322839));
#66243=CARTESIAN_POINT('Ctrl Pts',(0.288624248632822,7.90573488215121,-30.1627522976938));
#66244=CARTESIAN_POINT('Ctrl Pts',(0.283433071205645,7.90592269615651,-30.1625424589822));
#66245=CARTESIAN_POINT('Ctrl Pts',(0.274195440017041,7.90624779863203,-30.1621685185534));
#66246=CARTESIAN_POINT('Ctrl Pts',(0.270149053977545,7.90638709406591,-30.1620045376311));
#66247=CARTESIAN_POINT('Ctrl Pts',(0.261640806977383,7.90667344829711,-30.1616593512281));
#66248=CARTESIAN_POINT('Ctrl Pts',(0.257178922972824,7.90681983678431,-30.1614781050564));
#66249=CARTESIAN_POINT('Ctrl Pts',(0.245342475801262,7.90719814520814,-30.1609966974662));
#66250=CARTESIAN_POINT('Ctrl Pts',(0.237967728469296,7.90742352460471,-30.1606961378068));
#66251=CARTESIAN_POINT('Ctrl Pts',(0.203564688608862,7.90842674318086,-30.1592911958015));
#66252=CARTESIAN_POINT('Ctrl Pts',(0.176533141881781,7.90907631449856,-30.1581791195421));
#66253=CARTESIAN_POINT('Ctrl Pts',(-0.0336745918107459,7.91304945149483,
-30.1494708525657));
#66254=CARTESIAN_POINT('Ctrl Pts',(-0.21690176027324,7.91014729597411,-30.1415249856171));
#66255=CARTESIAN_POINT('Ctrl Pts',(-0.648250508851609,7.88831752313143,
-30.1222683675568));
#66256=CARTESIAN_POINT('Ctrl Pts',(-0.895910941305013,7.86403939117933,
-30.1107839212929));
#66257=CARTESIAN_POINT('Ctrl Pts',(-1.21906046256736,7.81689686316326,-30.0955776740002));
#66258=CARTESIAN_POINT('Ctrl Pts',(-1.29594598064942,7.80451849415018,-30.091942651396));
#66259=CARTESIAN_POINT('Ctrl Pts',(-1.64087612471697,7.74374797855015,-30.0755881460682));
#66260=CARTESIAN_POINT('Ctrl Pts',(-1.90650453261117,7.682665953918,-30.062874757192));
#66261=CARTESIAN_POINT('Ctrl Pts',(-2.33549162529119,7.56039458835516,-30.0425012568226));
#66262=CARTESIAN_POINT('Ctrl Pts',(-2.50091650644738,7.50729701304209,-30.0346825799805));
#66263=CARTESIAN_POINT('Ctrl Pts',(-2.94934599264981,7.34689187755918,-30.0136782152457));
#66264=CARTESIAN_POINT('Ctrl Pts',(-3.22816313801968,7.22872419540384,-30.0008421042003));
#66265=CARTESIAN_POINT('Ctrl Pts',(-3.52106894085083,7.08424803693792,-29.9876237250175));
#66266=CARTESIAN_POINT('Ctrl Pts',(-3.54253976029041,7.07353580580807,-29.9866562763712));
#66267=CARTESIAN_POINT('Ctrl Pts',(-3.5731138759585,7.05810763037794,-29.9852807244915));
#66268=CARTESIAN_POINT('Ctrl Pts',(-3.58225714495782,7.05347147446315,-29.9848696286543));
#66269=CARTESIAN_POINT('Ctrl Pts',(-3.5978920740052,7.04550543627943,-29.9841671079139));
#66270=CARTESIAN_POINT('Ctrl Pts',(-3.60438817455887,7.04218432848272,-29.9838753534939));
#66271=CARTESIAN_POINT('Ctrl Pts',(-3.61738559692894,7.03551674781922,-29.9832918746423));
#66272=CARTESIAN_POINT('Ctrl Pts',(-3.62388689188834,7.03217023833397,-29.9830001520037));
#66273=CARTESIAN_POINT('Ctrl Pts',(-3.63979032738198,7.02395611220406,-29.982286863193));
#66274=CARTESIAN_POINT('Ctrl Pts',(-3.64918736676555,7.019078618801,-29.9818656700143));
#66275=CARTESIAN_POINT('Ctrl Pts',(-3.68203957603911,7.00194301349661,-29.9803941208854));
#66276=CARTESIAN_POINT('Ctrl Pts',(-3.70544312699072,6.98958601456133,-29.9793475031024));
#66277=CARTESIAN_POINT('Ctrl Pts',(-4.09654791494488,6.78056751458441,-29.9618842723436));
#66278=CARTESIAN_POINT('Ctrl Pts',(-4.44821553869818,6.55524440088101,-29.9466396627183));
#66279=CARTESIAN_POINT('Ctrl Pts',(-5.05758943008729,6.09308185077178,-29.9198776352081));
#66280=CARTESIAN_POINT('Ctrl Pts',(-5.32051739514024,5.86489168612146,-29.9081768421803));
#66281=CARTESIAN_POINT('Ctrl Pts',(-5.89495300460541,5.29582917055988,-29.8805859109353));
#66282=CARTESIAN_POINT('Ctrl Pts',(-6.19333240531306,4.94356294329962,-29.8646281384437));
#66283=CARTESIAN_POINT('Ctrl Pts',(-6.47609337262869,4.54367462723823,-29.845251765124));
#66284=CARTESIAN_POINT('Ctrl Pts',(-6.49273025527776,4.51986927669983,-29.8440937411108));
#66285=CARTESIAN_POINT('Ctrl Pts',(-6.51385249860407,4.4892886547941,-29.8425995638788));
#66286=CARTESIAN_POINT('Ctrl Pts',(-6.51845921293386,4.48259706953394,-29.8422722108618));
#66287=CARTESIAN_POINT('Ctrl Pts',(-6.52577154285505,4.47194027395814,-29.8417502584495));
#66288=CARTESIAN_POINT('Ctrl Pts',(-6.52848388508983,4.46797965587464,-29.8415561377309));
#66289=CARTESIAN_POINT('Ctrl Pts',(-6.53356081859692,4.46055171961291,-29.841191823043));
#66290=CARTESIAN_POINT('Ctrl Pts',(-6.53592626027069,4.45708498166893,-29.8410216890955));
#66291=CARTESIAN_POINT('Ctrl Pts',(-6.54125105177545,4.44926773327967,-29.8406378214743));
#66292=CARTESIAN_POINT('Ctrl Pts',(-6.54420881976992,4.44491615306122,-29.8404239775491));
#66293=CARTESIAN_POINT('Ctrl Pts',(-6.55291636980478,4.43207774489391,-29.8397926169946));
#66294=CARTESIAN_POINT('Ctrl Pts',(-6.55865398074421,4.42358271601417,-29.8393742614107));
#66295=CARTESIAN_POINT('Ctrl Pts',(-6.60249254913352,4.35840314377062,-29.8361599787696));
#66296=CARTESIAN_POINT('Ctrl Pts',(-6.63987346627582,4.3012400132315,-29.8333157024461));
#66297=CARTESIAN_POINT('Ctrl Pts',(-6.76411840035756,4.10576399663811,-29.8235235792462));
#66298=CARTESIAN_POINT('Ctrl Pts',(-6.84743431510808,3.9652532546874,-29.8163752520347));
#66299=CARTESIAN_POINT('Ctrl Pts',(-7.38896915008159,2.98393845548317,-29.7662270800584));
#66300=CARTESIAN_POINT('Ctrl Pts',(-7.69563882200766,2.06849683217669,-29.7195093910852));
#66301=CARTESIAN_POINT('Ctrl Pts',(-7.83742618279089,1.07728973648198,-29.6771439962136));
#66302=CARTESIAN_POINT('Ctrl Pts',(-7.84321500574677,1.0343020834259,-29.6753195703304));
#66303=CARTESIAN_POINT('Ctrl Pts',(-7.86283508600912,0.878954527467531,
-29.6687729210172));
#66304=CARTESIAN_POINT('Ctrl Pts',(-7.87460802587007,0.766346197070954,
-29.664115099647));
#66305=CARTESIAN_POINT('Ctrl Pts',(-7.88558033158646,0.633978207912988,
-29.6587389001528));
#66306=CARTESIAN_POINT('Ctrl Pts',(-7.88712759804527,0.614429648812501,
-29.657947441783));
#66307=CARTESIAN_POINT('Ctrl Pts',(-7.88935323263258,0.584915662421159,
-29.6567562734582));
#66308=CARTESIAN_POINT('Ctrl Pts',(-7.89008543379534,0.574954441454825,
-29.6563548897692));
#66309=CARTESIAN_POINT('Ctrl Pts',(-7.89133631516723,0.557484360391646,
-29.65565206487));
#66310=CARTESIAN_POINT('Ctrl Pts',(-7.89186314712144,0.549976107359509,
-29.655350370752));
#66311=CARTESIAN_POINT('Ctrl Pts',(-7.89288103445576,0.535166816837853,
-29.654756024068));
#66312=CARTESIAN_POINT('Ctrl Pts',(-7.89337267674014,0.527865828005366,
-29.6544633535741));
#66313=CARTESIAN_POINT('Ctrl Pts',(-7.89441055682498,0.512127375832744,
-29.6538331906477));
#66314=CARTESIAN_POINT('Ctrl Pts',(-7.89495339960037,0.503689693650676,
-29.6534958037456));
#66315=CARTESIAN_POINT('Ctrl Pts',(-7.89623313480466,0.483287666565888,
-29.6526811083181));
#66316=CARTESIAN_POINT('Ctrl Pts',(-7.89695636427905,0.471322469351202,
-29.6522042229476));
#66317=CARTESIAN_POINT('Ctrl Pts',(-7.90026880855241,0.41437196929971,-29.6499386941727));
#66318=CARTESIAN_POINT('Ctrl Pts',(-7.90250086876657,0.369366320770449,
-29.6481610895407));
#66319=CARTESIAN_POINT('Ctrl Pts',(-7.90877563734356,0.216448369893865,
-29.6421629416023));
#66320=CARTESIAN_POINT('Ctrl Pts',(-7.91099340001276,0.108472183981981,
-29.6379982978424));
#66321=CARTESIAN_POINT('Ctrl Pts',(-7.91099998529096,0.000482417337385414,
-29.6338954699259));
#66322=CARTESIAN_POINT('',(-7.91099357096916,0.0100856375418233,-25.6423315082367));
#66323=CARTESIAN_POINT('Ctrl Pts',(-7.91099998316719,0.000516070481359765,
-29.6338967485033));
#66324=CARTESIAN_POINT('Ctrl Pts',(-7.91106109109898,-0.936225837637782,
-29.5983072379579));
#66325=CARTESIAN_POINT('Ctrl Pts',(-7.74476825623127,-1.86545424022548,
-29.5686551740999));
#66326=CARTESIAN_POINT('Ctrl Pts',(-7.3896962694167,-2.82557461689186,-29.5306286759953));
#66327=CARTESIAN_POINT('Ctrl Pts',(-7.35819158792394,-2.90663012849464,
-29.5273496043355));
#66328=CARTESIAN_POINT('Ctrl Pts',(-7.2870418028981,-3.08111015846711,-29.5201117040888));
#66329=CARTESIAN_POINT('Ctrl Pts',(-7.24692385690003,-3.17432044295903,
-29.5161277416962));
#66330=CARTESIAN_POINT('Ctrl Pts',(-7.19804016399774,-3.2821372659141,-29.511397454883));
#66331=CARTESIAN_POINT('Ctrl Pts',(-7.19100455296732,-3.2975234265895,-29.5107194944065));
#66332=CARTESIAN_POINT('Ctrl Pts',(-7.18018945622697,-3.3209757176619,-29.5096817613069));
#66333=CARTESIAN_POINT('Ctrl Pts',(-7.1764455899473,-3.32905828101778,-29.5093233265068));
#66334=CARTESIAN_POINT('Ctrl Pts',(-7.16961355284964,-3.34374275697509,
-29.508670695892));
#66335=CARTESIAN_POINT('Ctrl Pts',(-7.16652989105734,-3.35034676447669,
-29.50837666581));
#66336=CARTESIAN_POINT('Ctrl Pts',(-7.16032700665847,-3.36358319003425,
-29.5077862992548));
#66337=CARTESIAN_POINT('Ctrl Pts',(-7.1572076847347,-3.37021555330357,-29.5074899593864));
#66338=CARTESIAN_POINT('Ctrl Pts',(-7.14835125920349,-3.38897850994578,
-29.5066501409211));
#66339=CARTESIAN_POINT('Ctrl Pts',(-7.14259251424448,-3.40109882816688,
-29.5061058976552));
#66340=CARTESIAN_POINT('Ctrl Pts',(-7.11826957243991,-3.45195662142256,
-29.5038150098009));
#66341=CARTESIAN_POINT('Ctrl Pts',(-7.09942101555662,-3.49055688895462,
-29.5020586794983));
#66342=CARTESIAN_POINT('Ctrl Pts',(-6.86941582636518,-3.95201785168591,
-29.4808628278932));
#66343=CARTESIAN_POINT('Ctrl Pts',(-6.62109082776764,-4.35527931618148,
-29.4603983174135));
#66344=CARTESIAN_POINT('Ctrl Pts',(-5.9972238798474,-5.19057234523664,-29.41557834769));
#66345=CARTESIAN_POINT('Ctrl Pts',(-5.60782149410329,-5.60902168805794,
-29.3914868123181));
#66346=CARTESIAN_POINT('Ctrl Pts',(-5.01148041478717,-6.12509612416234,
-29.3588857124585));
#66347=CARTESIAN_POINT('Ctrl Pts',(-4.84026346110284,-6.2612770444313,-29.3498956108031));
#66348=CARTESIAN_POINT('Ctrl Pts',(-4.5654100381966,-6.46186785145347,-29.3359968767411));
#66349=CARTESIAN_POINT('Ctrl Pts',(-4.465554858833,-6.53127286687329,-29.3310535486224));
#66350=CARTESIAN_POINT('Ctrl Pts',(-4.3334061986132,-6.61867580254186,-29.3246488857999));
#66351=CARTESIAN_POINT('Ctrl Pts',(-4.30253185217634,-6.63878741475022,
-29.3231620483453));
#66352=CARTESIAN_POINT('Ctrl Pts',(-4.25178177865611,-6.67134338200633,
-29.3207334651445));
#66353=CARTESIAN_POINT('Ctrl Pts',(-4.23198929183552,-6.68391632592351,
-29.3197901189104));
#66354=CARTESIAN_POINT('Ctrl Pts',(-4.19355002944703,-6.70809522390468,
-29.3179653390826));
#66355=CARTESIAN_POINT('Ctrl Pts',(-4.1749102459602,-6.7197118854999,-29.3170837759764));
#66356=CARTESIAN_POINT('Ctrl Pts',(-4.13167576167638,-6.74640709162962,
-29.3150465895203));
#66357=CARTESIAN_POINT('Ctrl Pts',(-4.10704645061681,-6.76142904319136,
-29.3138917046242));
#66358=CARTESIAN_POINT('Ctrl Pts',(-4.06237225842249,-6.78834264045562,
-29.3118069668739));
#66359=CARTESIAN_POINT('Ctrl Pts',(-4.04235596726764,-6.8002810536311,-29.3108765205304));
#66360=CARTESIAN_POINT('Ctrl Pts',(-3.90819160345405,-6.87949967266792,
-29.3046638981426));
#66361=CARTESIAN_POINT('Ctrl Pts',(-3.7924204022117,-6.9439920512294,-29.2994188259116));
#66362=CARTESIAN_POINT('Ctrl Pts',(-3.04085383111548,-7.33826096562028,
-29.2660433643931));
#66363=CARTESIAN_POINT('Ctrl Pts',(-2.36441270184676,-7.58329347524111,
-29.2393558037556));
#66364=CARTESIAN_POINT('Ctrl Pts',(-1.59314994728801,-7.74926383300711,
-29.2081823562558));
#66365=CARTESIAN_POINT('Ctrl Pts',(-1.5217998712111,-7.7635907683359,-29.2052885943377));
#66366=CARTESIAN_POINT('Ctrl Pts',(-1.43186558811601,-7.78036195679973,
-29.2016212186808));
#66367=CARTESIAN_POINT('Ctrl Pts',(-1.413456061651,-7.7837274617579,-29.2008694435223));
#66368=CARTESIAN_POINT('Ctrl Pts',(-1.38338428959784,-7.78911477613938,
-29.1996396418152));
#66369=CARTESIAN_POINT('Ctrl Pts',(-1.3717292212564,-7.79117577975042,-29.1991625732938));
#66370=CARTESIAN_POINT('Ctrl Pts',(-1.34912126127317,-7.79512131651534,
-29.1982363790025));
#66371=CARTESIAN_POINT('Ctrl Pts',(-1.33816893293537,-7.797008940793,-29.1977873250286));
#66372=CARTESIAN_POINT('Ctrl Pts',(-1.312831366838,-7.80132088907797,-29.1967476556345));
#66373=CARTESIAN_POINT('Ctrl Pts',(-1.29844334160651,-7.80372851262283,
-29.1961566728842));
#66374=CARTESIAN_POINT('Ctrl Pts',(-1.25963417804321,-7.81011235120941,
-29.1945610546533));
#66375=CARTESIAN_POINT('Ctrl Pts',(-1.23520096789705,-7.81401380601213,
-29.1935548471101));
#66376=CARTESIAN_POINT('Ctrl Pts',(-1.03574133942523,-7.84490430186414,
-29.1853283988042));
#66377=CARTESIAN_POINT('Ctrl Pts',(-0.859875055411986,-7.86612332505235,
-29.1779986507248));
#66378=CARTESIAN_POINT('Ctrl Pts',(-0.110163712509447,-7.93113561746692,
-29.1466205779375));
#66379=CARTESIAN_POINT('Ctrl Pts',(0.466860514342553,-7.91815149700524,
-29.1222618340021));
#66380=CARTESIAN_POINT('Ctrl Pts',(1.14734958195007,-7.82814281222514,-29.094009778787));
#66381=CARTESIAN_POINT('Ctrl Pts',(1.25702445714687,-7.81128164242897,-29.0894666302711));
#66382=CARTESIAN_POINT('Ctrl Pts',(1.44701972670491,-7.7779669172184,-29.0816099025397));
#66383=CARTESIAN_POINT('Ctrl Pts',(1.52750589023526,-7.76256152219709,-29.0782858541982));
#66384=CARTESIAN_POINT('Ctrl Pts',(1.64273535455978,-7.73864452500787,-29.0735304911287));
#66385=CARTESIAN_POINT('Ctrl Pts',(1.67768246791217,-7.73114351701248,-29.072088737585));
#66386=CARTESIAN_POINT('Ctrl Pts',(1.73850535919063,-7.71765673087432,-29.0695799641694));
#66387=CARTESIAN_POINT('Ctrl Pts',(1.76440401304015,-7.71177701856108,-29.0685118733644));
#66388=CARTESIAN_POINT('Ctrl Pts',(1.81449042903207,-7.70014049499746,-29.0664463912986));
#66389=CARTESIAN_POINT('Ctrl Pts',(1.83868162280341,-7.69439985016794,-29.065448849489));
#66390=CARTESIAN_POINT('Ctrl Pts',(1.89640527066943,-7.68041407936262,-29.0630685472436));
#66391=CARTESIAN_POINT('Ctrl Pts',(1.92991162874521,-7.6720632490916,-29.0616868539979));
#66392=CARTESIAN_POINT('Ctrl Pts',(2.05238240223913,-7.64068663105737,-29.0566357002509));
#66393=CARTESIAN_POINT('Ctrl Pts',(2.14099883181857,-7.61633047590636,-29.052979231412));
#66394=CARTESIAN_POINT('Ctrl Pts',(2.88196908750552,-7.3987211499181,-29.0223525927401));
#66395=CARTESIAN_POINT('Ctrl Pts',(3.50734879203526,-7.12358211206623,-28.9961938106266));
#66396=CARTESIAN_POINT('Ctrl Pts',(4.42913738788019,-6.56687218225373,-28.956033772302));
#66397=CARTESIAN_POINT('Ctrl Pts',(4.75257750455889,-6.33672319210183,-28.9414930046943));
#66398=CARTESIAN_POINT('Ctrl Pts',(5.14148184237209,-6.01340523476452,-28.9223269706478));
#66399=CARTESIAN_POINT('Ctrl Pts',(5.22410749502594,-5.94176557208121,-28.9181456255602));
#66400=CARTESIAN_POINT('Ctrl Pts',(5.38143778013061,-5.79953490778136,-28.9099212535867));
#66401=CARTESIAN_POINT('Ctrl Pts',(5.45630420630964,-5.72915536034199,-28.9058858701553));
#66402=CARTESIAN_POINT('Ctrl Pts',(5.54102043583112,-5.64634932799137,-28.9011515709169));
#66403=CARTESIAN_POINT('Ctrl Pts',(5.5522312829077,-5.63532572092069,-28.9005215816529));
#66404=CARTESIAN_POINT('Ctrl Pts',(5.56919149154765,-5.6185490370615,-28.8995630905561));
#66405=CARTESIAN_POINT('Ctrl Pts',(5.57496500143965,-5.61282035909817,-28.8992358472747));
#66406=CARTESIAN_POINT('Ctrl Pts',(5.58539491217175,-5.60243946868339,-28.8986429212698));
#66407=CARTESIAN_POINT('Ctrl Pts',(5.59005436567966,-5.59779032419086,-28.8983774006648));
#66408=CARTESIAN_POINT('Ctrl Pts',(5.59934070528277,-5.58850137354454,-28.8978469303617));
#66409=CARTESIAN_POINT('Ctrl Pts',(5.6039676395646,-5.58386162349275,-28.8975819836987));
#66410=CARTESIAN_POINT('Ctrl Pts',(5.61693085708274,-5.57083015908879,-28.8968378749946));
#66411=CARTESIAN_POINT('Ctrl Pts',(5.62525407090698,-5.56242550965028,-28.8963580028937));
#66412=CARTESIAN_POINT('Ctrl Pts',(5.65908202407958,-5.52811300128049,-28.8943989185358));
#66413=CARTESIAN_POINT('Ctrl Pts',(5.68442661379711,-5.50204841131561,-28.8929108079608));
#66414=CARTESIAN_POINT('Ctrl Pts',(6.05329442048727,-5.11743245042505,-28.8709374505878));
#66415=CARTESIAN_POINT('Ctrl Pts',(6.36243439207665,-4.72755175129115,-28.8482805888229));
#66416=CARTESIAN_POINT('Ctrl Pts',(6.8578893374167,-3.96530284972688,-28.8064414376334));
#66417=CARTESIAN_POINT('Ctrl Pts',(7.05540865302301,-3.60215403996331,-28.7873925065042));
#66418=CARTESIAN_POINT('Ctrl Pts',(7.33283202367148,-2.98079829469735,-28.7571474678541));
#66419=CARTESIAN_POINT('Ctrl Pts',(7.42949820963403,-2.73096262786812,-28.7455544670296));
#66420=CARTESIAN_POINT('Ctrl Pts',(7.53803121207694,-2.40171575409068,-28.7310511573295));
#66421=CARTESIAN_POINT('Ctrl Pts',(7.56162285030325,-2.32637345231992,-28.72778279189));
#66422=CARTESIAN_POINT('Ctrl Pts',(7.59336449473806,-2.2194145395362,-28.723213100953));
#66423=CARTESIAN_POINT('Ctrl Pts',(7.60245225292419,-2.18808249892832,-28.7218829133489));
#66424=CARTESIAN_POINT('Ctrl Pts',(7.6159663128838,-2.1403890647661,-28.7198707918558));
#66425=CARTESIAN_POINT('Ctrl Pts',(7.62053422254066,-2.12406835932387,-28.719184491423));
#66426=CARTESIAN_POINT('Ctrl Pts',(7.62789144284665,-2.09745247901034,-28.7180689082519));
#66427=CARTESIAN_POINT('Ctrl Pts',(7.6307124300657,-2.08716615924759,-28.7176386491493));
#66428=CARTESIAN_POINT('Ctrl Pts',(7.63610513163827,-2.06734538404361,-28.7168112742887));
#66429=CARTESIAN_POINT('Ctrl Pts',(7.63867981252932,-2.05781176031477,-28.7164140676765));
#66430=CARTESIAN_POINT('Ctrl Pts',(7.6432990665153,-2.040579288221,-28.7156974535657));
#66431=CARTESIAN_POINT('Ctrl Pts',(7.64534987336381,-2.0328821328408,-28.7153778544967));
#66432=CARTESIAN_POINT('Ctrl Pts',(7.64974410009473,-2.01628887682175,-28.7146899215454));
#66433=CARTESIAN_POINT('Ctrl Pts',(7.65208363614419,-2.00739175496107,-28.7143217075091));
#66434=CARTESIAN_POINT('Ctrl Pts',(7.6583365684027,-1.9834424335918,-28.7133322826367));
#66435=CARTESIAN_POINT('Ctrl Pts',(7.66222111400438,-1.96838270816126,-28.7127119590087));
#66436=CARTESIAN_POINT('Ctrl Pts',(7.67907910699989,-1.90222101205837,-28.7099947229937));
#66437=CARTESIAN_POINT('Ctrl Pts',(7.69158605547179,-1.85100102399073,-28.7079121367047));
#66438=CARTESIAN_POINT('Ctrl Pts',(7.93071249994053,-0.827401825605291,
-28.6666979732494));
#66439=CARTESIAN_POINT('Ctrl Pts',(7.97173027098429,0.17889522674085,-28.6347507474529));
#66440=CARTESIAN_POINT('Ctrl Pts',(7.78850526491565,1.40816144164982,-28.5899213022138));
#66441=CARTESIAN_POINT('Ctrl Pts',(7.74125526478127,1.64823677330166,-28.5808126926365));
#66442=CARTESIAN_POINT('Ctrl Pts',(7.67743914785488,1.90824182202314,-28.5702421744213));
#66443=CARTESIAN_POINT('Ctrl Pts',(7.67181285556926,1.93073721569665,-28.5693216882624));
#66444=CARTESIAN_POINT('Ctrl Pts',(7.66175835496983,1.97019983653994,-28.5676967119715));
#66445=CARTESIAN_POINT('Ctrl Pts',(7.65737247737749,1.98717770244354,-28.5669942926999));
#66446=CARTESIAN_POINT('Ctrl Pts',(7.65098246125254,2.01157835777966,-28.5659801469876));
#66447=CARTESIAN_POINT('Ctrl Pts',(7.64902387024681,2.01901311131518,-28.5656705232232));
#66448=CARTESIAN_POINT('Ctrl Pts',(7.6456046246641,2.03191608051712,-28.5651321125693));
#66449=CARTESIAN_POINT('Ctrl Pts',(7.64414893177836,2.03738561482827,-28.5649035505595));
#66450=CARTESIAN_POINT('Ctrl Pts',(7.64133741353184,2.04790401678002,-28.5644633744909));
#66451=CARTESIAN_POINT('Ctrl Pts',(7.6399824505011,2.05295311326221,-28.5642517990459));
#66452=CARTESIAN_POINT('Ctrl Pts',(7.63677681591546,2.06485137480345,-28.5637525648457));
#66453=CARTESIAN_POINT('Ctrl Pts',(7.63492193553477,2.0716993927518,-28.5634647206182));
#66454=CARTESIAN_POINT('Ctrl Pts',(7.62940803942683,2.09194811972763,-28.5626121079663));
#66455=CARTESIAN_POINT('Ctrl Pts',(7.62572294801977,2.10534165501714,-28.5620462103866));
#66456=CARTESIAN_POINT('Ctrl Pts',(7.59234938490404,2.22540128649788,-28.5569565484836));
#66457=CARTESIAN_POINT('Ctrl Pts',(7.56046072658498,2.33143994406994,-28.5523412774118));
#66458=CARTESIAN_POINT('Ctrl Pts',(7.39466084342466,2.84353948750738,-28.5295764708306));
#66459=CARTESIAN_POINT('Ctrl Pts',(7.23020692954665,3.23895386463656,-28.5105789611331));
#66460=CARTESIAN_POINT('Ctrl Pts',(6.76520642749348,4.14278865434088,-28.4659154577401));
#66461=CARTESIAN_POINT('Ctrl Pts',(6.43814927524766,4.63476772279218,-28.4406954132187));
#66462=CARTESIAN_POINT('Ctrl Pts',(6.03497240257439,5.11512300004893,-28.4152896718719));
#66463=CARTESIAN_POINT('Ctrl Pts',(6.01024534967043,5.14415455375549,-28.413749910315));
#66464=CARTESIAN_POINT('Ctrl Pts',(5.97350491776182,5.18666423408005,-28.4114884492553));
#66465=CARTESIAN_POINT('Ctrl Pts',(5.96165387577313,5.20028171816147,-28.4107629668972));
#66466=CARTESIAN_POINT('Ctrl Pts',(5.94059921516042,5.22430808909983,-28.4094810121066));
#66467=CARTESIAN_POINT('Ctrl Pts',(5.93141460311106,5.23473350347544,-28.4089241038223));
#66468=CARTESIAN_POINT('Ctrl Pts',(5.91338088808173,5.25509509943758,-28.4078351131801));
#66469=CARTESIAN_POINT('Ctrl Pts',(5.90453409040301,5.2650332580284,-28.4073029806427));
#66470=CARTESIAN_POINT('Ctrl Pts',(5.88308962672749,5.28900113208535,-28.4060181069144));
#66471=CARTESIAN_POINT('Ctrl Pts',(5.87046677827221,5.30300823494344,-28.4052659389114));
#66472=CARTESIAN_POINT('Ctrl Pts',(5.83149619490156,5.34594277144678,-28.4029563132327));
#66473=CARTESIAN_POINT('Ctrl Pts',(5.80498366035441,5.37472015288788,-28.4014024673781));
#66474=CARTESIAN_POINT('Ctrl Pts',(5.48654949583485,5.71525187515873,-28.3829433440637));
#66475=CARTESIAN_POINT('Ctrl Pts',(5.17005010600584,6.00307768269678,-28.3666699365887));
#66476=CARTESIAN_POINT('Ctrl Pts',(4.4832223527339,6.53287813057973,-28.3343738332653));
#66477=CARTESIAN_POINT('Ctrl Pts',(4.11276170905502,6.77221979058195,-28.3184282208909));
#66478=CARTESIAN_POINT('Ctrl Pts',(3.5412480899392,7.07718461818058,-28.294272434203));
#66479=CARTESIAN_POINT('Ctrl Pts',(3.35440742571648,7.16763038927264,-28.2864305837784));
#66480=CARTESIAN_POINT('Ctrl Pts',(3.08028571539536,7.28725946526883,-28.2747840884502));
#66481=CARTESIAN_POINT('Ctrl Pts',(2.99570878388925,7.32243393490419,-28.2711716650385));
#66482=CARTESIAN_POINT('Ctrl Pts',(2.89669907079718,7.36160832461066,-28.2669044114181));
#66483=CARTESIAN_POINT('Ctrl Pts',(2.8828405733456,7.36704641336545,-28.266306252031));
#66484=CARTESIAN_POINT('Ctrl Pts',(2.86171208015673,7.37526850850629,-28.2653928923228));
#66485=CARTESIAN_POINT('Ctrl Pts',(2.8544531464668,7.37808097247224,-28.2650788437346));
#66486=CARTESIAN_POINT('Ctrl Pts',(2.84127379362208,7.38316493387341,-28.264508179904));
#66487=CARTESIAN_POINT('Ctrl Pts',(2.83535476666007,7.38544003820881,-28.2642517131174));
#66488=CARTESIAN_POINT('Ctrl Pts',(2.82262482354458,7.39031550450002,-28.2636997507483));
#66489=CARTESIAN_POINT('Ctrl Pts',(2.81581303906429,7.39291357173288,-28.2634041600687));
#66490=CARTESIAN_POINT('Ctrl Pts',(2.79751208260711,7.39986473514165,-28.2626093551761));
#66491=CARTESIAN_POINT('Ctrl Pts',(2.78601637343714,7.40420047779482,-28.2621094098849));
#66492=CARTESIAN_POINT('Ctrl Pts',(2.73363453699236,7.42381764439868,-28.2598280389522));
#66493=CARTESIAN_POINT('Ctrl Pts',(2.69263301095811,7.43878710258297,-28.258033174505));
#66494=CARTESIAN_POINT('Ctrl Pts',(2.10201054853958,7.64889767341104,-28.2320248170893));
#66495=CARTESIAN_POINT('Ctrl Pts',(1.53266637623529,7.78298197922414,-28.2048051267462));
#66496=CARTESIAN_POINT('Ctrl Pts',(0.384839772036364,7.92239770949138,-28.1517071741412));
#66497=CARTESIAN_POINT('Ctrl Pts',(-0.190081851935726,7.92947210523636,
-28.1260320686397));
#66498=CARTESIAN_POINT('Ctrl Pts',(-0.824803680846273,7.86814825909378,
-28.0997994097756));
#66499=CARTESIAN_POINT('Ctrl Pts',(-0.888749302406901,7.86118204086309,
-28.0971783753605));
#66500=CARTESIAN_POINT('Ctrl Pts',(-0.967595350660919,7.85161819546899,
-28.0939731060691));
#66501=CARTESIAN_POINT('Ctrl Pts',(-0.982581611011396,7.84975683898128,
-28.0933650644133));
#66502=CARTESIAN_POINT('Ctrl Pts',(-1.00614309531457,7.84676187276624,-28.0924109481948));
#66503=CARTESIAN_POINT('Ctrl Pts',(-1.01472190801242,7.84565709588272,-28.0920639374751));
#66504=CARTESIAN_POINT('Ctrl Pts',(-1.02996385580326,7.84366882479992,-28.0914480881507));
#66505=CARTESIAN_POINT('Ctrl Pts',(-1.03662770219387,7.84279090533138,-28.0911790684092));
#66506=CARTESIAN_POINT('Ctrl Pts',(-1.05200739279171,7.84074478451052,-28.0905587241565));
#66507=CARTESIAN_POINT('Ctrl Pts',(-1.0607224318006,7.83957054012894,-28.0902075969387));
#66508=CARTESIAN_POINT('Ctrl Pts',(-1.08462705246292,7.83630909522304,-28.0892455670826));
#66509=CARTESIAN_POINT('Ctrl Pts',(-1.09981258963091,7.83419225893851,-28.0886356324339));
#66510=CARTESIAN_POINT('Ctrl Pts',(-1.17426406351798,7.82359311934316,-28.0856510866978));
#66511=CARTESIAN_POINT('Ctrl Pts',(-1.23343929830801,7.81448226635349,-28.083297088091));
#66512=CARTESIAN_POINT('Ctrl Pts',(-2.3002793955211,7.63780699895001,-28.0411720287286));
#66513=CARTESIAN_POINT('Ctrl Pts',(-3.26595261456846,7.27739366888304,-28.0097278330247));
#66514=CARTESIAN_POINT('Ctrl Pts',(-4.35604485606599,6.60871683639882,-27.9645133355323));
#66515=CARTESIAN_POINT('Ctrl Pts',(-4.56887744331886,6.4634049318769,-27.9550463736945));
#66516=CARTESIAN_POINT('Ctrl Pts',(-4.80005364149785,6.28843821469499,-27.943595730092));
#66517=CARTESIAN_POINT('Ctrl Pts',(-4.82576012368288,6.26873267185341,-27.9423054077498));
#66518=CARTESIAN_POINT('Ctrl Pts',(-4.85762993385714,6.24399037027071,-27.9406834621312));
#66519=CARTESIAN_POINT('Ctrl Pts',(-4.86390797332854,6.23910118081247,-27.940362871161));
#66520=CARTESIAN_POINT('Ctrl Pts',(-4.87381727004453,6.23136000710423,-27.9398551160989));
#66521=CARTESIAN_POINT('Ctrl Pts',(-4.87745344016932,6.22851428983845,-27.9396684282131));
#66522=CARTESIAN_POINT('Ctrl Pts',(-4.88425445886473,6.22318211045409,-27.9393185547313));
#66523=CARTESIAN_POINT('Ctrl Pts',(-4.88741990716037,6.22069641196122,-27.9391554276967));
#66524=CARTESIAN_POINT('Ctrl Pts',(-4.89448046191163,6.21514332809244,-27.9387909368037));
#66525=CARTESIAN_POINT('Ctrl Pts',(-4.89837455752306,6.21207471581865,-27.9385894773447));
#66526=CARTESIAN_POINT('Ctrl Pts',(-4.90826709324148,6.20426414720608,-27.9380765885646));
#66527=CARTESIAN_POINT('Ctrl Pts',(-4.91426150021762,6.19951718874224,-27.9377647718871));
#66528=CARTESIAN_POINT('Ctrl Pts',(-4.94756648995815,6.17306438010286,-27.9360266285208));
#66529=CARTESIAN_POINT('Ctrl Pts',(-4.97473974314961,6.15118707445163,-27.9345871883522));
#66530=CARTESIAN_POINT('Ctrl Pts',(-5.70134220793611,5.55823251873582,-27.8955449161371));
#66531=CARTESIAN_POINT('Ctrl Pts',(-6.29805806490332,4.87176805505265,-27.8505574879898));
#66532=CARTESIAN_POINT('Ctrl Pts',(-6.89489647186251,3.88666130920369,-27.799231697136));
#66533=CARTESIAN_POINT('Ctrl Pts',(-7.01363742710394,3.66805656879702,-27.7884693232043));
#66534=CARTESIAN_POINT('Ctrl Pts',(-7.16980821494936,3.34512833641964,-27.7735019123845));
#66535=CARTESIAN_POINT('Ctrl Pts',(-7.21565190241228,3.24505815590305,-27.7689861010196));
#66536=CARTESIAN_POINT('Ctrl Pts',(-7.26620104460356,3.12834408820099,-27.7638564983357));
#66537=CARTESIAN_POINT('Ctrl Pts',(-7.27295702103943,3.1126051034531,-27.7631676113766));
#66538=CARTESIAN_POINT('Ctrl Pts',(-7.28313208703254,3.08868687112371,-27.7621250088209));
#66539=CARTESIAN_POINT('Ctrl Pts',(-7.28658860773067,3.08052366447897,-27.7617699277431));
#66540=CARTESIAN_POINT('Ctrl Pts',(-7.29281758615763,3.06574364928079,-27.7611283918311));
#66541=CARTESIAN_POINT('Ctrl Pts',(-7.29559477547872,3.05912885319581,-27.7608417648784));
#66542=CARTESIAN_POINT('Ctrl Pts',(-7.30111932847793,3.04591998922036,-27.7602703887025));
#66543=CARTESIAN_POINT('Ctrl Pts',(-7.30386676632562,3.03932595973891,-27.7599856369564));
#66544=CARTESIAN_POINT('Ctrl Pts',(-7.31154502175472,3.0208271105831,-27.7591881551756));
#66545=CARTESIAN_POINT('Ctrl Pts',(-7.31645570107348,3.00891392591512,-27.7586761563171));
#66546=CARTESIAN_POINT('Ctrl Pts',(-7.33632482683317,2.96037568213916,-27.7565964779631));
#66547=CARTESIAN_POINT('Ctrl Pts',(-7.35103767066584,2.9236503501859,-27.7550376883872));
#66548=CARTESIAN_POINT('Ctrl Pts',(-7.58042512149548,2.33838702433607,-27.7304255659623));
#66549=CARTESIAN_POINT('Ctrl Pts',(-7.7334623478822,1.76763698171038,-27.7098208176552));
#66550=CARTESIAN_POINT('Ctrl Pts',(-7.8816045555661,0.789947111044109,-27.6761198933998));
#66551=CARTESIAN_POINT('Ctrl Pts',(-7.91144566130026,0.390775051233245,
-27.6627266678462));
#66552=CARTESIAN_POINT('Ctrl Pts',(-7.91072732530986,-0.246282008699786,
-27.6398530282432));
#66553=CARTESIAN_POINT('Ctrl Pts',(-7.89977706852779,-0.483493966778849,
-27.6309960325901));
#66554=CARTESIAN_POINT('Ctrl Pts',(-7.8768534656682,-0.73437988567683,-27.6209278043275));
#66555=CARTESIAN_POINT('Ctrl Pts',(-7.87548416948709,-0.748921512842783,
-27.6203417171391));
#66556=CARTESIAN_POINT('Ctrl Pts',(-7.87353437670132,-0.769031049000135,
-27.6195276570814));
#66557=CARTESIAN_POINT('Ctrl Pts',(-7.87298824237683,-0.774602136914305,
-27.6193017565361));
#66558=CARTESIAN_POINT('Ctrl Pts',(-7.87203812900076,-0.784189382962326,
-27.6189123646765));
#66559=CARTESIAN_POINT('Ctrl Pts',(-7.87163698778819,-0.788205826642706,
-27.6187490406282));
#66560=CARTESIAN_POINT('Ctrl Pts',(-7.87084645888596,-0.796060237862896,
-27.6184292734702));
#66561=CARTESIAN_POINT('Ctrl Pts',(-7.87045733739571,-0.799898232136896,
-27.6182728459499));
#66562=CARTESIAN_POINT('Ctrl Pts',(-7.86951318149984,-0.809143269415839,
-27.6178956189523));
#66563=CARTESIAN_POINT('Ctrl Pts',(-7.86895538201957,-0.814550022870949,
-27.6176746589788));
#66564=CARTESIAN_POINT('Ctrl Pts',(-7.86724125600599,-0.83099896938901,
-27.6170013855905));
#66565=CARTESIAN_POINT('Ctrl Pts',(-7.86606726008854,-0.842039265530992,
-27.6165480573806));
#66566=CARTESIAN_POINT('Ctrl Pts',(-7.85436742566049,-0.949904882813457,
-27.612105159079));
#66567=CARTESIAN_POINT('Ctrl Pts',(-7.842077979138,-1.04652684205039,-27.6080166930794));
#66568=CARTESIAN_POINT('Ctrl Pts',(-7.80343947915181,-1.31117314124377,
-27.5965645854855));
#66569=CARTESIAN_POINT('Ctrl Pts',(-7.7734518012122,-1.47860878984053,-27.5890369594463));
#66570=CARTESIAN_POINT('Ctrl Pts',(-7.59911278605078,-2.29873149330377,
-27.5511769429548));
#66571=CARTESIAN_POINT('Ctrl Pts',(-7.37783632946214,-2.93229158722346,
-27.5190703790969));
#66572=CARTESIAN_POINT('Ctrl Pts',(-7.0125323180258,-3.66480966211215,-27.4823330398026));
#66573=CARTESIAN_POINT('Ctrl Pts',(-6.94175369762942,-3.79716972271399,
-27.4756977649427));
#66574=CARTESIAN_POINT('Ctrl Pts',(-6.74349025189868,-4.14383942122636,
-27.4583573334232));
#66575=CARTESIAN_POINT('Ctrl Pts',(-6.60956466793515,-4.35427787607738,
-27.4478757255589));
#66576=CARTESIAN_POINT('Ctrl Pts',(-6.45188981432674,-4.57795056814913,
-27.4367742409427));
#66577=CARTESIAN_POINT('Ctrl Pts',(-6.43777236246147,-4.59778213963121,
-27.4357902368387));
#66578=CARTESIAN_POINT('Ctrl Pts',(-6.41775800878671,-4.62562450582225,
-27.4344090941133));
#66579=CARTESIAN_POINT('Ctrl Pts',(-6.41193726322171,-4.63368972435727,
-27.4340090530539));
#66580=CARTESIAN_POINT('Ctrl Pts',(-6.40178836865561,-4.64769628035908,
-27.4333143811981));
#66581=CARTESIAN_POINT('Ctrl Pts',(-6.39746712647089,-4.65364259453183,
-27.4330194868146));
#66582=CARTESIAN_POINT('Ctrl Pts',(-6.38843793597988,-4.66603101181621,
-27.4324051493163));
#66583=CARTESIAN_POINT('Ctrl Pts',(-6.38372851496776,-4.67247203445605,
-27.4320857631051));
#66584=CARTESIAN_POINT('Ctrl Pts',(-6.37257951266082,-4.68767208142353,
-27.4313320966869));
#66585=CARTESIAN_POINT('Ctrl Pts',(-6.36613159761376,-4.69642498835094,
-27.4308981368789));
#66586=CARTESIAN_POINT('Ctrl Pts',(-6.34483367020274,-4.72521201469312,
-27.4294710107324));
#66587=CARTESIAN_POINT('Ctrl Pts',(-6.32990690333001,-4.74518930031956,
-27.4284807972041));
#66588=CARTESIAN_POINT('Ctrl Pts',(-6.10349662599432,-5.04523679511466,
-27.4136097917576));
#66589=CARTESIAN_POINT('Ctrl Pts',(-5.87369252688523,-5.3110123469392,-27.400480560774));
#66590=CARTESIAN_POINT('Ctrl Pts',(-5.34029090143199,-5.85077487943084,
-27.3731407842722));
#66591=CARTESIAN_POINT('Ctrl Pts',(-5.03159100800513,-6.11828184522846,
-27.3591460778023));
#66592=CARTESIAN_POINT('Ctrl Pts',(-4.53299344402663,-6.48698214240671,
-27.3375890347829));
#66593=CARTESIAN_POINT('Ctrl Pts',(-4.35733761268778,-6.60625246895442,
-27.3301623126459));
#66594=CARTESIAN_POINT('Ctrl Pts',(-3.93533168088193,-6.86863420418269,
-27.3122774620414));
#66595=CARTESIAN_POINT('Ctrl Pts',(-3.68567294192124,-7.00576817613231,
-27.3016174474028));
#66596=CARTESIAN_POINT('Ctrl Pts',(-3.4098730563285,-7.1384271764568,-27.2894194862543));
#66597=CARTESIAN_POINT('Ctrl Pts',(-3.39059593829015,-7.1476035135341,-27.2885654234527));
#66598=CARTESIAN_POINT('Ctrl Pts',(-3.36318136343904,-7.16051759992009,
-27.287348933279));
#66599=CARTESIAN_POINT('Ctrl Pts',(-3.35507424959395,-7.16431978356063,
-27.286988954194));
#66600=CARTESIAN_POINT('Ctrl Pts',(-3.34020106806225,-7.17126442683742,
-27.2863281300824));
#66601=CARTESIAN_POINT('Ctrl Pts',(-3.33343697097425,-7.17441109881701,
-27.2860274413432));
#66602=CARTESIAN_POINT('Ctrl Pts',(-3.31973459647433,-7.1807619104956,-27.2854180171989));
#66603=CARTESIAN_POINT('Ctrl Pts',(-3.31279610693833,-7.18396557339068,
-27.2851092649461));
#66604=CARTESIAN_POINT('Ctrl Pts',(-3.29572717635036,-7.19181671095949,
-27.2843493522136));
#66605=CARTESIAN_POINT('Ctrl Pts',(-3.2855915491317,-7.19645283427168,-27.2838977907962));
#66606=CARTESIAN_POINT('Ctrl Pts',(-3.24869492185973,-7.21323547336111,
-27.2822528795748));
#66607=CARTESIAN_POINT('Ctrl Pts',(-3.22187623944488,-7.22525419370994,
-27.2810551659734));
#66608=CARTESIAN_POINT('Ctrl Pts',(-2.93466166876387,-7.35205155061018,
-27.2682096172954));
#66609=CARTESIAN_POINT('Ctrl Pts',(-2.6683284178278,-7.45284598382061,-27.2561439982762));
#66610=CARTESIAN_POINT('Ctrl Pts',(-2.30749208127807,-7.56757912203419,
-27.2399323268636));
#66611=CARTESIAN_POINT('Ctrl Pts',(-2.21732680717962,-7.59448715663533,
-27.2358913576763));
#66612=CARTESIAN_POINT('Ctrl Pts',(-1.62766077078796,-7.75906470670896,
-27.2095691813035));
#66613=CARTESIAN_POINT('Ctrl Pts',(-1.11611994660299,-7.84899218240182,
-27.1873421409751));
#66614=CARTESIAN_POINT('Ctrl Pts',(-0.378316581510499,-7.90506063052417,
-27.1563756614105));
#66615=CARTESIAN_POINT('Ctrl Pts',(-0.156563979800241,-7.91255946086726,
-27.1471883215448));
#66616=CARTESIAN_POINT('Ctrl Pts',(0.106246507178032,-7.9103929433845,-27.1363586662188));
#66617=CARTESIAN_POINT('Ctrl Pts',(0.147276525232371,-7.90973542359412,
-27.1346694680072));
#66618=CARTESIAN_POINT('Ctrl Pts',(0.413490338914267,-7.90339714032062,
-27.123716062221));
#66619=CARTESIAN_POINT('Ctrl Pts',(0.638352249946675,-7.88841998441327,
-27.1145014200982));
#66620=CARTESIAN_POINT('Ctrl Pts',(0.906774129406987,-7.85898759493737,
-27.1035692865867));
#66621=CARTESIAN_POINT('Ctrl Pts',(0.951235169787291,-7.85373013408749,
-27.101760606931));
#66622=CARTESIAN_POINT('Ctrl Pts',(1.02088757557395,-7.84489367540608,-27.098930367042));
#66623=CARTESIAN_POINT('Ctrl Pts',(1.04611027056555,-7.84157009326246,-27.097906137784));
#66624=CARTESIAN_POINT('Ctrl Pts',(1.09252587231078,-7.83522599912955,-27.0960225079175));
#66625=CARTESIAN_POINT('Ctrl Pts',(1.11372338158077,-7.83224102487008,-27.0951627317109));
#66626=CARTESIAN_POINT('Ctrl Pts',(1.16057433521738,-7.82544955813506,-27.0932634247007));
#66627=CARTESIAN_POINT('Ctrl Pts',(1.18622172353228,-7.82160287939206,-27.0922243468334));
#66628=CARTESIAN_POINT('Ctrl Pts',(1.25955441885894,-7.81023521302536,-27.0892551142748));
#66629=CARTESIAN_POINT('Ctrl Pts',(1.30719054922633,-7.80240375285811,-27.0873284794851));
#66630=CARTESIAN_POINT('Ctrl Pts',(1.6616643946366,-7.74079022980866,-27.0730057420437));
#66631=CARTESIAN_POINT('Ctrl Pts',(1.96516251488765,-7.66936153525198,-27.0608332113915));
#66632=CARTESIAN_POINT('Ctrl Pts',(2.71257581264168,-7.44616323458239,-27.0306660500482));
#66633=CARTESIAN_POINT('Ctrl Pts',(3.14868098258042,-7.27249644154382,-27.0129172598648));
#66634=CARTESIAN_POINT('Ctrl Pts',(3.67215897578549,-7.00807327084671,-26.9899381938502));
#66635=CARTESIAN_POINT('Ctrl Pts',(3.77627004924275,-6.95252659780564,-26.9852762741621));
#66636=CARTESIAN_POINT('Ctrl Pts',(3.89867396298879,-6.88365940884823,-26.9796550380944));
#66637=CARTESIAN_POINT('Ctrl Pts',(3.91820291888899,-6.87256221581759,-26.9787538582107));
#66638=CARTESIAN_POINT('Ctrl Pts',(3.94868570221931,-6.85506842531772,-26.9773401786166));
#66639=CARTESIAN_POINT('Ctrl Pts',(3.95967181975755,-6.84872841986575,-26.9768292598422));
#66640=CARTESIAN_POINT('Ctrl Pts',(3.97915354067233,-6.83742312047786,-26.9759207501858));
#66641=CARTESIAN_POINT('Ctrl Pts',(3.98765522765118,-6.83246833973081,-26.975523435941));
#66642=CARTESIAN_POINT('Ctrl Pts',(4.00724743973372,-6.82100098006514,-26.9746058865539));
#66643=CARTESIAN_POINT('Ctrl Pts',(4.01833136270747,-6.81447719721559,-26.9740853657956));
#66644=CARTESIAN_POINT('Ctrl Pts',(4.049254555275,-6.79617472407491,-26.9726291996323));
#66645=CARTESIAN_POINT('Ctrl Pts',(4.06905822980302,-6.78433625701872,-26.9716920835983));
#66646=CARTESIAN_POINT('Ctrl Pts',(4.18485767054794,-6.71442291928582,-26.9661862466527));
#66647=CARTESIAN_POINT('Ctrl Pts',(4.27965980737125,-6.65439855179556,-26.9615730474371));
#66648=CARTESIAN_POINT('Ctrl Pts',(4.69914266024798,-6.37612842531886,-26.9407341068016));
#66649=CARTESIAN_POINT('Ctrl Pts',(5.00864224736656,-6.13599670245876,-26.9242110735848));
#66650=CARTESIAN_POINT('Ctrl Pts',(5.59883376851369,-5.60356429078551,-26.8909114857512));
#66651=CARTESIAN_POINT('Ctrl Pts',(5.87743511898193,-5.31061650709209,-26.8741964441616));
#66652=CARTESIAN_POINT('Ctrl Pts',(6.16568376860829,-4.9569173531308,-26.8556776178277));
#66653=CARTESIAN_POINT('Ctrl Pts',(6.19849540174365,-4.91582554419991,-26.8535489712848));
#66654=CARTESIAN_POINT('Ctrl Pts',(6.25133283012902,-4.8482841381268,-26.8500862628274));
#66655=CARTESIAN_POINT('Ctrl Pts',(6.27160615106713,-4.82203043688913,-26.8487490234751));
#66656=CARTESIAN_POINT('Ctrl Pts',(6.30760343923941,-4.77480333779046,-26.846358788992));
#66657=CARTESIAN_POINT('Ctrl Pts',(6.32338939578482,-4.75387785034587,-26.8453050262313));
#66658=CARTESIAN_POINT('Ctrl Pts',(6.35671767139323,-4.70923894865541,-26.8430681714588));
#66659=CARTESIAN_POINT('Ctrl Pts',(6.3742319633911,-4.68550508630174,-26.8418854362024));
#66660=CARTESIAN_POINT('Ctrl Pts',(6.42059623210256,-4.6219351147287,-26.8387346512104));
#66661=CARTESIAN_POINT('Ctrl Pts',(6.4492081826016,-4.58192689062148,-26.8367694508401));
#66662=CARTESIAN_POINT('Ctrl Pts',(6.58125215208702,-4.39360177240497,-26.8275984501725));
#66663=CARTESIAN_POINT('Ctrl Pts',(6.67995334818959,-4.24203260762008,-26.8204453044737));
#66664=CARTESIAN_POINT('Ctrl Pts',(7.27298807521295,-3.25924910162444,-26.7752464398691));
#66665=CARTESIAN_POINT('Ctrl Pts',(7.61654083547722,-2.34673663413072,-26.7403197360597));
#66666=CARTESIAN_POINT('Ctrl Pts',(7.82309166324541,-1.19371577026954,-26.6959217822952));
#66667=CARTESIAN_POINT('Ctrl Pts',(7.85132630488589,-0.991155424814066,
-26.6880442400835));
#66668=CARTESIAN_POINT('Ctrl Pts',(7.8736786850477,-0.767793432446921,-26.679093163955));
#66669=CARTESIAN_POINT('Ctrl Pts',(7.87559881607283,-0.747840938898423,
-26.6782912538544));
#66670=CARTESIAN_POINT('Ctrl Pts',(7.8781870613395,-0.719829847060135,-26.6771619599563));
#66671=CARTESIAN_POINT('Ctrl Pts',(7.87891869080055,-0.711777103689533,
-26.6768369000944));
#66672=CARTESIAN_POINT('Ctrl Pts',(7.88023669811501,-0.697019284945764,
-26.6762404169343));
#66673=CARTESIAN_POINT('Ctrl Pts',(7.8808268679918,-0.690314550255293,-26.6759691354154));
#66674=CARTESIAN_POINT('Ctrl Pts',(7.88200438442451,-0.67673882661333,-26.675419247869));
#66675=CARTESIAN_POINT('Ctrl Pts',(7.88259130464137,-0.669867807214394,
-26.6751406259219));
#66676=CARTESIAN_POINT('Ctrl Pts',(7.88399544173782,-0.653172307322653,
-26.6744628486587));
#66677=CARTESIAN_POINT('Ctrl Pts',(7.88480327856925,-0.64334706458688,-26.674063331828));
#66678=CARTESIAN_POINT('Ctrl Pts',(7.88756996709961,-0.608909372998559,
-26.6726606769803));
#66679=CARTESIAN_POINT('Ctrl Pts',(7.8894319462005,-0.584289446869026,-26.6716537153327));
#66680=CARTESIAN_POINT('Ctrl Pts',(7.91552171488661,-0.216425906159299,
-26.6565406554417));
#66681=CARTESIAN_POINT('Ctrl Pts',(7.91744021781857,0.127963835146736,-26.6413724820697));
#66682=CARTESIAN_POINT('Ctrl Pts',(7.87716927232321,0.802702023358791,-26.6107232663353));
#66683=CARTESIAN_POINT('Ctrl Pts',(7.8365521942496,1.13250761392438,-26.5953260484416));
#66684=CARTESIAN_POINT('Ctrl Pts',(7.66339555573778,2.05543543422849,-26.5522455904789));
#66685=CARTESIAN_POINT('Ctrl Pts',(7.4831358621491,2.63729385469906,-26.5252511741441));
#66686=CARTESIAN_POINT('Ctrl Pts',(7.22214464587847,3.22894766974172,-26.4988479644866));
#66687=CARTESIAN_POINT('Ctrl Pts',(7.20595788777413,3.26491153259682,-26.4972464884926));
#66688=CARTESIAN_POINT('Ctrl Pts',(7.18372509887963,3.31333766070552,-26.495094542088));
#66689=CARTESIAN_POINT('Ctrl Pts',(7.1779144222368,3.32590698901554,-26.4945363992654));
#66690=CARTESIAN_POINT('Ctrl Pts',(7.16872151558605,3.34565626158041,-26.4936600624466));
#66691=CARTESIAN_POINT('Ctrl Pts',(7.16536144467328,3.35284645582093,-26.493341143315));
#66692=CARTESIAN_POINT('Ctrl Pts',(7.15887574415441,3.36667088709225,-26.4927282158988));
#66693=CARTESIAN_POINT('Ctrl Pts',(7.15575169932326,3.37330585631193,-26.4924341560302));
#66694=CARTESIAN_POINT('Ctrl Pts',(7.14836924454377,3.38892860021987,-26.4917420209145));
#66695=CARTESIAN_POINT('Ctrl Pts',(7.14410309863472,3.39791271675712,-26.4913442004944));
#66696=CARTESIAN_POINT('Ctrl Pts',(7.13164961859254,3.42401148652931,-26.4901891177879));
#66697=CARTESIAN_POINT('Ctrl Pts',(7.12341762162699,3.44110481332186,-26.4894333279246));
#66698=CARTESIAN_POINT('Ctrl Pts',(7.06490429357745,3.56149501496587,-26.4841151858965));
#66699=CARTESIAN_POINT('Ctrl Pts',(7.0124384777503,3.66371769069153,-26.4796257220311));
#66700=CARTESIAN_POINT('Ctrl Pts',(6.84071711559277,3.98108064032858,-26.4657467119362));
#66701=CARTESIAN_POINT('Ctrl Pts',(6.71364250442224,4.19182874658243,-26.4566217365204));
#66702=CARTESIAN_POINT('Ctrl Pts',(6.21512883228206,4.93761088599112,-26.4242200574751));
#66703=CARTESIAN_POINT('Ctrl Pts',(5.7878964285974,5.43212886115796,-26.4026878403289));
#66704=CARTESIAN_POINT('Ctrl Pts',(5.0860750568429,6.06653091872794,-26.3688364267392));
#66705=CARTESIAN_POINT('Ctrl Pts',(4.85633125435657,6.25195896130502,-26.3579071863796));
#66706=CARTESIAN_POINT('Ctrl Pts',(4.60071082779649,6.43566410238741,-26.3453675531536));
#66707=CARTESIAN_POINT('Ctrl Pts',(4.58459895571675,6.44715169390477,-26.3445758064534));
#66708=CARTESIAN_POINT('Ctrl Pts',(4.56233554730994,6.46289960783889,-26.3434800844333));
#66709=CARTESIAN_POINT('Ctrl Pts',(4.55622071651262,6.46721190074518,-26.3431789608303));
#66710=CARTESIAN_POINT('Ctrl Pts',(4.54574027695638,6.47458066094199,-26.3426625683444));
#66711=CARTESIAN_POINT('Ctrl Pts',(4.54137767391532,6.47764140897164,-26.3424475295959));
#66712=CARTESIAN_POINT('Ctrl Pts',(4.53288394578318,6.4835877048677,-26.3420287030601));
#66713=CARTESIAN_POINT('Ctrl Pts',(4.52875314793903,6.48647371978808,-26.3418249400539));
#66714=CARTESIAN_POINT('Ctrl Pts',(4.52019601326417,6.49244007154966,-26.3414026895453));
#66715=CARTESIAN_POINT('Ctrl Pts',(4.51576927890193,6.49551983297078,-26.3411841721739));
#66716=CARTESIAN_POINT('Ctrl Pts',(4.50196850370122,6.50510036236643,-26.3405026800691));
#66717=CARTESIAN_POINT('Ctrl Pts',(4.49258357488468,6.5115853640684,-26.3400388969211));
#66718=CARTESIAN_POINT('Ctrl Pts',(4.441191713205,6.54693323752778,-26.3374974612629));
#66719=CARTESIAN_POINT('Ctrl Pts',(4.39892121571435,6.57540954089305,-26.3354006894831));
#66720=CARTESIAN_POINT('Ctrl Pts',(4.27515217488365,6.65706122820978,-26.3292494495808));
#66721=CARTESIAN_POINT('Ctrl Pts',(4.1929451703833,6.70914303202189,-26.3251491593789));
#66722=CARTESIAN_POINT('Ctrl Pts',(3.89135074835776,6.8925082739511,-26.3101080508249));
#66723=CARTESIAN_POINT('Ctrl Pts',(3.6665964464434,7.01465215189373,-26.2989080781976));
#66724=CARTESIAN_POINT('Ctrl Pts',(3.13158359812893,7.27265933744835,-26.2727773009049));
#66725=CARTESIAN_POINT('Ctrl Pts',(2.81771386701074,7.39992498569645,-26.2578490749036));
#66726=CARTESIAN_POINT('Ctrl Pts',(2.12813227768752,7.62927300188556,-26.2264755996703));
#66727=CARTESIAN_POINT('Ctrl Pts',(1.7510676111502,7.72454207138937,-26.2101860683649));
#66728=CARTESIAN_POINT('Ctrl Pts',(1.32933640382543,7.79861317309115,-26.1928323147608));
#66729=CARTESIAN_POINT('Ctrl Pts',(1.29011388881635,7.80519755591137,-26.1912260214675));
#66730=CARTESIAN_POINT('Ctrl Pts',(1.23290764069069,7.81435791867093,-26.1888938527981));
#66731=CARTESIAN_POINT('Ctrl Pts',(1.21496222993433,7.8171681390782,-26.1881637770749));
#66732=CARTESIAN_POINT('Ctrl Pts',(1.18321164343683,7.82202825264009,-26.1868746771612));
#66733=CARTESIAN_POINT('Ctrl Pts',(1.16941044226136,7.82410346283992,-26.1863152091249));
#66734=CARTESIAN_POINT('Ctrl Pts',(1.14078252472775,7.82833064522088,-26.1851564699651));
#66735=CARTESIAN_POINT('Ctrl Pts',(1.12595503788139,7.83047704255814,-26.1845572976074));
#66736=CARTESIAN_POINT('Ctrl Pts',(1.08774718134297,7.83589716776827,-26.183015802612));
#66737=CARTESIAN_POINT('Ctrl Pts',(1.06435805506313,7.83910838626123,-26.182074547487));
#66738=CARTESIAN_POINT('Ctrl Pts',(0.971855249926465,7.85138696366532,-26.1783609317616));
#66739=CARTESIAN_POINT('Ctrl Pts',(0.902636607513331,7.85964548971532,-26.1756017233081));
#66740=CARTESIAN_POINT('Ctrl Pts',(0.542230824946419,7.89782177759786,-26.1613335839797));
#66741=CARTESIAN_POINT('Ctrl Pts',(0.249650306886075,7.91247677627833,-26.1500948850438));
#66742=CARTESIAN_POINT('Ctrl Pts',(-0.52348962255973,7.90826661083432,-26.1209754254826));
#66743=CARTESIAN_POINT('Ctrl Pts',(-1.00265614419949,7.86189550403551,-26.1035604943761));
#66744=CARTESIAN_POINT('Ctrl Pts',(-1.81604546017868,7.70757064101029,-26.0728947493653));
#66745=CARTESIAN_POINT('Ctrl Pts',(-2.15278183807161,7.62037843932074,-26.0598358259865));
#66746=CARTESIAN_POINT('Ctrl Pts',(-2.50234178175803,7.50484082366656,-26.0451295875244));
#66747=CARTESIAN_POINT('Ctrl Pts',(-2.52198615509201,7.49826219900052,-26.0442991553091));
#66748=CARTESIAN_POINT('Ctrl Pts',(-2.54940835484547,7.48895893649532,-26.0431341272675));
#66749=CARTESIAN_POINT('Ctrl Pts',(-2.55720820240652,7.48629916054448,-26.0428020942493));
#66750=CARTESIAN_POINT('Ctrl Pts',(-2.57069014778048,7.48167824063792,-26.0422270229247));
#66751=CARTESIAN_POINT('Ctrl Pts',(-2.57637420169948,7.47972279599352,-26.0419842141776));
#66752=CARTESIAN_POINT('Ctrl Pts',(-2.58815299057617,7.47565560353843,-26.0414803069073));
#66753=CARTESIAN_POINT('Ctrl Pts',(-2.59424738058112,7.47354287693327,-26.0412191685736));
#66754=CARTESIAN_POINT('Ctrl Pts',(-2.60630304418866,7.46934704763521,-26.0407017645673));
#66755=CARTESIAN_POINT('Ctrl Pts',(-2.61226442141986,7.46726425596696,-26.0404455119087));
#66756=CARTESIAN_POINT('Ctrl Pts',(-2.63221520770664,7.4602670163953,-26.0395865529036));
#66757=CARTESIAN_POINT('Ctrl Pts',(-2.64619323979615,7.45532039480542,-26.0389824956307));
#66758=CARTESIAN_POINT('Ctrl Pts',(-2.74828808582239,7.41886722072071,-26.0345535847021));
#66759=CARTESIAN_POINT('Ctrl Pts',(-2.83585127866618,7.38583953741168,-26.0306615230953));
#66760=CARTESIAN_POINT('Ctrl Pts',(-3.03824872475572,7.30536778226849,-26.021420159309));
#66761=CARTESIAN_POINT('Ctrl Pts',(-3.1525863116302,7.25675898372272,-26.0160203417105));
#66762=CARTESIAN_POINT('Ctrl Pts',(-3.44219095796604,7.1255019713277,-26.0019662473122));
#66763=CARTESIAN_POINT('Ctrl Pts',(-3.61565148249121,7.03907070061639,-25.9931874837726));
#66764=CARTESIAN_POINT('Ctrl Pts',(-4.32980245154933,6.64985942573321,-25.955984556967));
#66765=CARTESIAN_POINT('Ctrl Pts',(-4.83720612773704,6.29042296392473,-25.9271292698404));
#66766=CARTESIAN_POINT('Ctrl Pts',(-5.45746633986913,5.73117697321142,-25.8912031962797));
#66767=CARTESIAN_POINT('Ctrl Pts',(-5.61150767334488,5.58044082207839,-25.8821914538865));
#66768=CARTESIAN_POINT('Ctrl Pts',(-5.77349428649123,5.4084303341021,-25.8726186590545));
#66769=CARTESIAN_POINT('Ctrl Pts',(-5.78771604756971,5.3932084992706,-25.8717773162712));
#66770=CARTESIAN_POINT('Ctrl Pts',(-5.80874335375377,5.37052359202541,-25.8705320110328));
#66771=CARTESIAN_POINT('Ctrl Pts',(-5.81559494149654,5.36310343734814,-25.8701260224298));
#66772=CARTESIAN_POINT('Ctrl Pts',(-5.82729969633738,5.35037857924892,-25.8694320875033));
#66773=CARTESIAN_POINT('Ctrl Pts',(-5.83215986790318,5.34508035185919,-25.8691438337372));
#66774=CARTESIAN_POINT('Ctrl Pts',(-5.84160090492786,5.33476017001521,-25.8685836740214));
#66775=CARTESIAN_POINT('Ctrl Pts',(-5.84618253361711,5.32973892306135,-25.8683117346831));
#66776=CARTESIAN_POINT('Ctrl Pts',(-5.85712468510994,5.31771576015617,-25.8676620291693));
#66777=CARTESIAN_POINT('Ctrl Pts',(-5.86347913868678,5.31070832128241,-25.8672845285229));
#66778=CARTESIAN_POINT('Ctrl Pts',(-5.88249023109461,5.2896679285158,-25.8661545356114));
#66779=CARTESIAN_POINT('Ctrl Pts',(-5.89510921470534,5.27560095782055,-25.8654036857886));
#66780=CARTESIAN_POINT('Ctrl Pts',(-6.00456458525174,5.15270284385823,-25.858883782831));
#66781=CARTESIAN_POINT('Ctrl Pts',(-6.09843096140382,5.04125828864852,-25.8532443731781));
#66782=CARTESIAN_POINT('Ctrl Pts',(-6.3285556555196,4.75219810265208,-25.8392550774896));
#66783=CARTESIAN_POINT('Ctrl Pts',(-6.46045438448535,4.57127345663248,-25.831081856693));
#66784=CARTESIAN_POINT('Ctrl Pts',(-6.72441131354408,4.17491529904849,-25.8141719020635));
#66785=CARTESIAN_POINT('Ctrl Pts',(-6.8541820150543,3.95825980541488,-25.805507473234));
#66786=CARTESIAN_POINT('Ctrl Pts',(-7.02474077471563,3.63988589744167,-25.7932750387913));
#66787=CARTESIAN_POINT('Ctrl Pts',(-7.07412271750674,3.54295642761574,-25.7896130722676));
#66788=CARTESIAN_POINT('Ctrl Pts',(-7.1453661606639,3.39568394126348,-25.7841100684482));
#66789=CARTESIAN_POINT('Ctrl Pts',(-7.16872818457411,3.34608176999011,-25.7822667750531));
#66790=CARTESIAN_POINT('Ctrl Pts',(-7.21752977791426,3.23960890309111,-25.7783254353854));
#66791=CARTESIAN_POINT('Ctrl Pts',(-7.24281696218559,3.18267251808447,-25.7762270429855));
#66792=CARTESIAN_POINT('Ctrl Pts',(-7.45824729347857,2.68174373697036,-25.7578065782573));
#66793=CARTESIAN_POINT('Ctrl Pts',(-7.60801025880316,2.22154794257502,-25.7412040442325));
#66794=CARTESIAN_POINT('Ctrl Pts',(-7.72180834420059,1.7200524883768,-25.7208888125697));
#66795=CARTESIAN_POINT('Ctrl Pts',(-7.728566774953,1.68942600283106,-25.7196394297873));
#66796=CARTESIAN_POINT('Ctrl Pts',(-7.73685655934682,1.65076902731365,-25.7180505917615));
#66797=CARTESIAN_POINT('Ctrl Pts',(-7.7385579085848,1.6427748768277,-25.7177213866442));
#66798=CARTESIAN_POINT('Ctrl Pts',(-7.74122106205984,1.63016554171537,-25.7172010997431));
#66799=CARTESIAN_POINT('Ctrl Pts',(-7.74219113870885,1.62555208977765,-25.7170105230912));
#66800=CARTESIAN_POINT('Ctrl Pts',(-7.74397271149544,1.6170415854928,-25.7166585604414));
#66801=CARTESIAN_POINT('Ctrl Pts',(-7.74478539181711,1.61314477967048,-25.7164972473494));
#66802=CARTESIAN_POINT('Ctrl Pts',(-7.74657568696197,1.6045277692481,-25.7161401880889));
#66803=CARTESIAN_POINT('Ctrl Pts',(-7.74755192346658,1.59980731004779,-25.715944357752));
#66804=CARTESIAN_POINT('Ctrl Pts',(-7.750351001544,1.58621009696657,-25.7153796030039));
#66805=CARTESIAN_POINT('Ctrl Pts',(-7.75216289150439,1.57733117037897,-25.7150100028913));
#66806=CARTESIAN_POINT('Ctrl Pts',(-7.76425995423043,1.51752678822539,-25.712515147549));
#66807=CARTESIAN_POINT('Ctrl Pts',(-7.77405827833374,1.46650531072789,-25.7103603479874));
#66808=CARTESIAN_POINT('Ctrl Pts',(-7.86769013711608,0.951616359210873,
-25.6883791981394));
#66809=CARTESIAN_POINT('Ctrl Pts',(-7.91039868325133,0.48127547722744,-25.666431686808));
#66810=CARTESIAN_POINT('Ctrl Pts',(-7.91099369507502,0.00998781674201629,
-25.6444276219939));
#66811=CARTESIAN_POINT('',(-7.91099983344385,-0.00162334571786968,-23.6423315082368));
#66812=CARTESIAN_POINT('Ctrl Pts',(-7.91099357096916,0.0100856375418233,
-25.6423315082367));
#66813=CARTESIAN_POINT('Ctrl Pts',(-7.91123506252348,-0.179336015354617,
-25.6347047121618));
#66814=CARTESIAN_POINT('Ctrl Pts',(-7.90466927635026,-0.369027385880647,
-25.6270779160869));
#66815=CARTESIAN_POINT('Ctrl Pts',(-7.8912651987913,-0.558439398990916,
-25.619451120012));
#66816=CARTESIAN_POINT('Ctrl Pts',(-7.87787160594339,-0.747703253436783,
-25.6118302896406));
#66817=CARTESIAN_POINT('Ctrl Pts',(-7.85765039173663,-0.936687819513366,
-25.6042094592693));
#66818=CARTESIAN_POINT('Ctrl Pts',(-7.83062257872658,-1.12484266879304,
-25.5965886288979));
#66819=CARTESIAN_POINT('Ctrl Pts',(-7.80361018813151,-1.31289015451486,
-25.5889721470696));
#66820=CARTESIAN_POINT('Ctrl Pts',(-7.7697989813212,-1.5001085016849,-25.5813556652413));
#66821=CARTESIAN_POINT('Ctrl Pts',(-7.7292619224564,-1.68595110666521,-25.573739183413));
#66822=CARTESIAN_POINT('Ctrl Pts',(-7.68840281620738,-1.87327014152192,
-25.5660621923095));
#66823=CARTESIAN_POINT('Ctrl Pts',(-7.64071055259476,-2.05919110115924,
-25.558385201206));
#66824=CARTESIAN_POINT('Ctrl Pts',(-7.586312756841,-2.24316289096255,-25.5507082101025));
#66825=CARTESIAN_POINT('Ctrl Pts',(-7.53236089607785,-2.4256265413786,-25.5430941524122));
#66826=CARTESIAN_POINT('Ctrl Pts',(-7.47181315887367,-2.60617250643201,
-25.5354800947219));
#66827=CARTESIAN_POINT('Ctrl Pts',(-7.40484452833836,-2.78427701767219,
-25.5278660370316));
#66828=CARTESIAN_POINT('Ctrl Pts',(-7.33786942044865,-2.96239875557548,
-25.5202512428927));
#66829=CARTESIAN_POINT('Ctrl Pts',(-7.26447231295879,-3.13807822384796,
-25.5126364487539));
#66830=CARTESIAN_POINT('Ctrl Pts',(-7.18487676777222,-3.31081060043112,
-25.505021654615));
#66831=CARTESIAN_POINT('Ctrl Pts',(-7.10525830259229,-3.48359271629195,
-25.4974046677526));
#66832=CARTESIAN_POINT('Ctrl Pts',(-7.01943800243577,-3.65342571655013,
-25.4897876808901));
#66833=CARTESIAN_POINT('Ctrl Pts',(-6.92768585912072,-3.81982848271212,
-25.4821706940276));
#66834=CARTESIAN_POINT('Ctrl Pts',(-6.83465340084418,-3.98855324314535,
-25.4744474192694));
#66835=CARTESIAN_POINT('Ctrl Pts',(-6.73552251516363,-4.15375098330507,
-25.4667241445113));
#66836=CARTESIAN_POINT('Ctrl Pts',(-6.63062013894973,-4.31495047166873,
-25.4590008697531));
#66837=CARTESIAN_POINT('Ctrl Pts',(-6.52698990291307,-4.47419511064673,
-25.4513712543425));
#66838=CARTESIAN_POINT('Ctrl Pts',(-6.41772764119896,-4.62953766908532,
-25.4437416389319));
#66839=CARTESIAN_POINT('Ctrl Pts',(-6.30318894457212,-4.78055751236441,
-25.4361120235213));
#66840=CARTESIAN_POINT('Ctrl Pts',(-6.18654117317038,-4.93435818126271,
-25.4283419190893));
#66841=CARTESIAN_POINT('Ctrl Pts',(-6.06442103802342,-5.08367509333987,
-25.4205718146573));
#66842=CARTESIAN_POINT('Ctrl Pts',(-5.93724273672725,-5.22810383267008,
-25.4128017102253));
#66843=CARTESIAN_POINT('Ctrl Pts',(-5.81006443543108,-5.37253257200029,
-25.4050316057933));
#66844=CARTESIAN_POINT('Ctrl Pts',(-5.67782829672822,-5.51207290763824,
-25.3972615013613));
#66845=CARTESIAN_POINT('Ctrl Pts',(-5.54098276437416,-5.64636440596146,
-25.3894913969293));
#66846=CARTESIAN_POINT('Ctrl Pts',(-5.39982971521734,-5.78488302719869,
-25.3814767112178));
#66847=CARTESIAN_POINT('Ctrl Pts',(-5.25330579159423,-5.91827595657096,
-25.3734620255063));
#66848=CARTESIAN_POINT('Ctrl Pts',(-5.10181324297096,-6.04610805674578,
-25.3654473397948));
#66849=CARTESIAN_POINT('Ctrl Pts',(-4.95049292123658,-6.17379482881623,
-25.3574417657154));
#66850=CARTESIAN_POINT('Ctrl Pts',(-4.79421548356322,-6.29593315497069,
-25.3494361916361));
#66851=CARTESIAN_POINT('Ctrl Pts',(-4.63342043398249,-6.41212414742209,
-25.3414306175568));
#66852=CARTESIAN_POINT('Ctrl Pts',(-4.47278092018917,-6.52820274923991,
-25.3334327872064));
#66853=CARTESIAN_POINT('Ctrl Pts',(-4.30763277227287,-6.63834528706121,
-25.3254349568559));
#66854=CARTESIAN_POINT('Ctrl Pts',(-4.13844934218697,-6.74219237653096,
-25.3174371265055));
#66855=CARTESIAN_POINT('Ctrl Pts',(-3.96940089120078,-6.84595661399425,
-25.3094456770396));
#66856=CARTESIAN_POINT('Ctrl Pts',(-3.79632385843553,-6.94343523941891,
-25.3014542275738));
#66857=CARTESIAN_POINT('Ctrl Pts',(-3.61972175177961,-7.03431129817934,
-25.2934627781079));
#66858=CARTESIAN_POINT('Ctrl Pts',(-3.44323063115577,-7.12513024565518,
-25.2854763508883));
#66859=CARTESIAN_POINT('Ctrl Pts',(-3.26321914907742,-7.20935474495823,
-25.2774899236687));
#66860=CARTESIAN_POINT('Ctrl Pts',(-3.08021702368259,-7.28671284510485,
-25.2695034964491));
#66861=CARTESIAN_POINT('Ctrl Pts',(-2.8916148270596,-7.36643819027641,-25.2612726755581));
#66862=CARTESIAN_POINT('Ctrl Pts',(-2.69983635889162,-7.438870040111,-25.2530418546672));
#66863=CARTESIAN_POINT('Ctrl Pts',(-2.50548677509752,-7.50376285738105,
-25.2448110337762));
#66864=CARTESIAN_POINT('Ctrl Pts',(-2.31703471028687,-7.56668650850076,
-25.2368299763348));
#66865=CARTESIAN_POINT('Ctrl Pts',(-2.12616562556187,-7.62252186081628,
-25.2288489188933));
#66866=CARTESIAN_POINT('Ctrl Pts',(-1.9334495992081,-7.67109468376724,-25.2208678614518));
#66867=CARTESIAN_POINT('Ctrl Pts',(-1.74074863348217,-7.71966371078476,
-25.2128874277246));
#66868=CARTESIAN_POINT('Ctrl Pts',(-1.54620133807989,-7.76097125783855,
-25.2049069939974));
#66869=CARTESIAN_POINT('Ctrl Pts',(-1.35039091616937,-7.79489354472062,
-25.1969265602702));
#66870=CARTESIAN_POINT('Ctrl Pts',(-1.15456573750393,-7.82881838806966,
-25.1889455251179));
#66871=CARTESIAN_POINT('Ctrl Pts',(-0.957477572220607,-7.85535680512861,
-25.1809644899656));
#66872=CARTESIAN_POINT('Ctrl Pts',(-0.759718111332479,-7.87443644912532,
-25.1729834548133));
#66873=CARTESIAN_POINT('Ctrl Pts',(-0.561913387939105,-7.89352046000533,
-25.1650005929891));
#66874=CARTESIAN_POINT('Ctrl Pts',(-0.363437395565307,-7.90514226350875,
-25.1570177311649));
#66875=CARTESIAN_POINT('Ctrl Pts',(-0.164885604876271,-7.9092814931133,
-25.1490348693408));
#66876=CARTESIAN_POINT('Ctrl Pts',(0.0338135219682023,-7.91342379424984,
-25.1410460838018));
#66877=CARTESIAN_POINT('Ctrl Pts',(0.232588224897808,-7.910072423161,-25.1330572982629));
#66878=CARTESIAN_POINT('Ctrl Pts',(0.430843350893744,-7.89925914291908,
-25.125068512724));
#66879=CARTESIAN_POINT('Ctrl Pts',(0.629185912007195,-7.8884410937693,-25.117076203945));
#66880=CARTESIAN_POINT('Ctrl Pts',(0.827008106243506,-7.87015460036465,
-25.109083895166));
#66881=CARTESIAN_POINT('Ctrl Pts',(1.0237206423262,-7.84448322367224,-25.101091586387));
#66882=CARTESIAN_POINT('Ctrl Pts',(1.22061724188688,-7.81878782633034,-25.0930917992226));
#66883=CARTESIAN_POINT('Ctrl Pts',(1.41640177977645,-7.7856937973946,-25.0850920120583));
#66884=CARTESIAN_POINT('Ctrl Pts',(1.61049490985842,-7.74533583166799,-25.0770922248939));
#66885=CARTESIAN_POINT('Ctrl Pts',(1.65197072153519,-7.73671172742779,-25.0753827482847));
#66886=CARTESIAN_POINT('Ctrl Pts',(1.69336934984051,-7.72775610821929,-25.0736732716755));
#66887=CARTESIAN_POINT('Ctrl Pts',(1.7346852321027,-7.71847058331667,-25.0719637950663));
#66888=CARTESIAN_POINT('Ctrl Pts',(1.93111367640522,-7.67432433467604,-25.0638364161376));
#66889=CARTESIAN_POINT('Ctrl Pts',(2.12601574851104,-7.62263954703202,-25.0557090372089));
#66890=CARTESIAN_POINT('Ctrl Pts',(2.31879220931818,-7.56353909820035,-25.0475816582802));
#66891=CARTESIAN_POINT('Ctrl Pts',(2.51140495350226,-7.50448884079694,-25.0394611815792));
#66892=CARTESIAN_POINT('Ctrl Pts',(2.70189538193847,-7.43803557075885,-25.0313407048783));
#66893=CARTESIAN_POINT('Ctrl Pts',(2.88967625408622,-7.36435279889348,-25.0232202281773));
#66894=CARTESIAN_POINT('Ctrl Pts',(3.0773212620885,-7.29072333835168,-25.0151056268438));
#66895=CARTESIAN_POINT('Ctrl Pts',(3.26226032689824,-7.20987492145338,-25.0069910255103));
#66896=CARTESIAN_POINT('Ctrl Pts',(3.44392259038269,-7.12203048234503,-24.9988764241768));
#66897=CARTESIAN_POINT('Ctrl Pts',(3.62545615904357,-7.03424827478866,-24.9907675714625));
#66898=CARTESIAN_POINT('Ctrl Pts',(3.80371727134879,-6.93948007122018,-24.9826587187483));
#66899=CARTESIAN_POINT('Ctrl Pts',(3.97815589200227,-6.83799654130708,-24.9745498660341));
#66900=CARTESIAN_POINT('Ctrl Pts',(4.15251980586028,-6.73655647372638,-24.9664444860967));
#66901=CARTESIAN_POINT('Ctrl Pts',(4.32306421720474,-6.6284069742295,-24.9583391061593));
#66902=CARTESIAN_POINT('Ctrl Pts',(4.48926375227958,-6.5138645950364,-24.9502337262218));
#66903=CARTESIAN_POINT('Ctrl Pts',(4.65541146152757,-6.39935793347336,-24.9421308737766));
#66904=CARTESIAN_POINT('Ctrl Pts',(4.81721673446147,-6.27846254868579,-24.9340280213313));
#66905=CARTESIAN_POINT('Ctrl Pts',(4.9741827877033,-6.15153855507029,-24.925925168886));
#66906=CARTESIAN_POINT('Ctrl Pts',(5.05635222416706,-6.08509569807211,-24.9216834439689));
#66907=CARTESIAN_POINT('Ctrl Pts',(5.13719602657742,-6.01700149142288,-24.9174417190518));
#66908=CARTESIAN_POINT('Ctrl Pts',(5.21664637008845,-5.94731213654059,-24.9131999941347));
#66909=CARTESIAN_POINT('Ctrl Pts',(5.3719032232417,-5.81112959208374,-24.9049110826779));
#66910=CARTESIAN_POINT('Ctrl Pts',(5.52177023652025,-5.66891189016605,-24.8966221712211));
#66911=CARTESIAN_POINT('Ctrl Pts',(5.66579482943032,-5.52111310795212,-24.8883332597643));
#66912=CARTESIAN_POINT('Ctrl Pts',(5.80990222901842,-5.37322934909687,-24.880039582613));
#66913=CARTESIAN_POINT('Ctrl Pts',(5.94816029916871,-5.21975831446292,-24.8717459054616));
#66914=CARTESIAN_POINT('Ctrl Pts',(6.08015506622352,-5.06118912615173,-24.8634522283103));
#66915=CARTESIAN_POINT('Ctrl Pts',(6.21223367357894,-4.90251921802632,-24.8551532831896));
#66916=CARTESIAN_POINT('Ctrl Pts',(6.33804084964781,-4.73874491702806,-24.8468543380689));
#66917=CARTESIAN_POINT('Ctrl Pts',(6.45720394705447,-4.57038709368738,-24.8385553929482));
#66918=CARTESIAN_POINT('Ctrl Pts',(6.57650529941532,-4.4018339388753,-24.830246819257));
#66919=CARTESIAN_POINT('Ctrl Pts',(6.68914699549787,-4.22868687099223,-24.8219382455659));
#66920=CARTESIAN_POINT('Ctrl Pts',(6.79479970344629,-4.05149577193981,-24.8136296718748));
#66921=CARTESIAN_POINT('Ctrl Pts',(6.90051743719965,-3.87419561752983,-24.8053159845268));
#66922=CARTESIAN_POINT('Ctrl Pts',(6.9992374524674,-3.69284671806907,-24.7970022971788));
#66923=CARTESIAN_POINT('Ctrl Pts',(7.09067652112688,-3.50802329991408,-24.7886886098308));
#66924=CARTESIAN_POINT('Ctrl Pts',(7.18221510797048,-3.32299872823435,-24.7803658742382));
#66925=CARTESIAN_POINT('Ctrl Pts',(7.26645678622909,-3.13449234482788,-24.7720431386455));
#66926=CARTESIAN_POINT('Ctrl Pts',(7.34316593170256,-2.943099573491,-24.7637204030528));
#66927=CARTESIAN_POINT('Ctrl Pts',(7.37168955818027,-2.87193184131968,-24.7606256664363));
#66928=CARTESIAN_POINT('Ctrl Pts',(7.39917218120556,-2.80036519070873,-24.7575309298198));
#66929=CARTESIAN_POINT('Ctrl Pts',(7.42560343635673,-2.72843079552462,-24.7544361932033));
#66930=CARTESIAN_POINT('Ctrl Pts',(7.49988337719257,-2.52627306265205,-24.7457390332893));
#66931=CARTESIAN_POINT('Ctrl Pts',(7.56592206394861,-2.32103079898211,-24.7370418733753));
#66932=CARTESIAN_POINT('Ctrl Pts',(7.62349089207904,-2.11336405249732,-24.7283447134613));
#66933=CARTESIAN_POINT('Ctrl Pts',(7.68100930114178,-1.90587918158805,-24.7196551705635));
#66934=CARTESIAN_POINT('Ctrl Pts',(7.73007260230958,-1.69597428817814,-24.7109656276657));
#66935=CARTESIAN_POINT('Ctrl Pts',(7.77050205128734,-1.48432438197962,-24.7022760847679));
#66936=CARTESIAN_POINT('Ctrl Pts',(7.81183457204725,-1.26794685611739,-24.6933924437265));
#66937=CARTESIAN_POINT('Ctrl Pts',(7.84414294455433,-1.04974567349245,-24.6845088026852));
#66938=CARTESIAN_POINT('Ctrl Pts',(7.86729069163524,-0.830456605313957,
-24.6756251616438));
#66939=CARTESIAN_POINT('Ctrl Pts',(7.88986629398568,-0.6165877227098,-24.6669610982742));
#66940=CARTESIAN_POINT('Ctrl Pts',(7.90372867389307,-0.401684340823563,
-24.6582970349045));
#66941=CARTESIAN_POINT('Ctrl Pts',(7.9088027830959,-0.18643910023009,-24.6496329715349));
#66942=CARTESIAN_POINT('Ctrl Pts',(7.91406978581251,0.0369887413136039,
-24.6406395416577));
#66943=CARTESIAN_POINT('Ctrl Pts',(7.9098672206449,0.260784714269032,-24.6316461117805));
#66944=CARTESIAN_POINT('Ctrl Pts',(7.89617018668819,0.484166689123351,-24.6226526819033));
#66945=CARTESIAN_POINT('Ctrl Pts',(7.88247315273147,0.707548663977633,-24.6136592520261));
#66946=CARTESIAN_POINT('Ctrl Pts',(7.85928160087558,0.930516360671599,-24.6046658221489));
#66947=CARTESIAN_POINT('Ctrl Pts',(7.82663160079334,1.15228416003304,-24.5956723922717));
#66948=CARTESIAN_POINT('Ctrl Pts',(7.79827044298945,1.34492096057421,-24.587860322339));
#66949=CARTESIAN_POINT('Ctrl Pts',(7.76278420421041,1.5365693507524,-24.5800482524063));
#66950=CARTESIAN_POINT('Ctrl Pts',(7.72026924495075,1.72666261483463,-24.5722361824735));
#66951=CARTESIAN_POINT('Ctrl Pts',(7.67775731769792,1.91674232218098,-24.5644246696682));
#66952=CARTESIAN_POINT('Ctrl Pts',(7.62821774528126,2.10526678082068,-24.5566131568629));
#66953=CARTESIAN_POINT('Ctrl Pts',(7.57179784568462,2.29168025345722,-24.5488016440576));
#66954=CARTESIAN_POINT('Ctrl Pts',(7.5153720206018,2.47811330412321,-24.5409893108501));
#66955=CARTESIAN_POINT('Ctrl Pts',(7.45206453178849,2.66243459048561,-24.5331769776426));
#66956=CARTESIAN_POINT('Ctrl Pts',(7.38207237361253,2.8441041596163,-24.525364644435));
#66957=CARTESIAN_POINT('Ctrl Pts',(7.31203062988117,3.02590243154338,-24.5175467766235));
#66958=CARTESIAN_POINT('Ctrl Pts',(7.235294882239,3.20504490420628,-24.5097289088119));
#66959=CARTESIAN_POINT('Ctrl Pts',(7.15211037938772,3.3810114050465,-24.5019110410003));
#66960=CARTESIAN_POINT('Ctrl Pts',(7.06889509473996,3.55704302096018,-24.4940902802459));
#66961=CARTESIAN_POINT('Ctrl Pts',(6.97922645886915,3.72989600934564,-24.4862695194914));
#66962=CARTESIAN_POINT('Ctrl Pts',(6.88339545620493,3.89907527415121,-24.478448758737));
#66963=CARTESIAN_POINT('Ctrl Pts',(6.7874583021662,4.06844193772125,-24.470619334977));
#66964=CARTESIAN_POINT('Ctrl Pts',(6.68534532667827,4.23412644693136,-24.4627899112171));
#66965=CARTESIAN_POINT('Ctrl Pts',(6.57739117288376,4.3956622207434,-24.4549604874571));
#66966=CARTESIAN_POINT('Ctrl Pts',(6.49442307589354,4.51981043809258,-24.4489431887515));
#66967=CARTESIAN_POINT('Ctrl Pts',(6.40800567594872,4.64150870828585,-24.4429258900459));
#66968=CARTESIAN_POINT('Ctrl Pts',(6.31830676552403,4.76055885550565,-24.4369085913403));
#66969=CARTESIAN_POINT('Ctrl Pts',(6.19730100926472,4.92116006045795,-24.4287911261775));
#66970=CARTESIAN_POINT('Ctrl Pts',(6.07008248282852,5.07725910620167,-24.4206736610147));
#66971=CARTESIAN_POINT('Ctrl Pts',(5.93701302250922,5.22836469372174,-24.4125561958519));
#66972=CARTESIAN_POINT('Ctrl Pts',(5.80404066699095,5.37936001493444,-24.4044446542485));
#66973=CARTESIAN_POINT('Ctrl Pts',(5.66522610178564,5.52536890359633,-24.396333112645));
#66974=CARTESIAN_POINT('Ctrl Pts',(5.52097203150046,5.66593229992996,-24.3882215710415));
#66975=CARTESIAN_POINT('Ctrl Pts',(5.37680273946463,5.80641308702672,-24.3801147965985));
#66976=CARTESIAN_POINT('Ctrl Pts',(5.2272005460241,5.94145454023021,-24.3720080221554));
#66977=CARTESIAN_POINT('Ctrl Pts',(5.07260607365836,6.07063329657494,-24.3639012477124));
#66978=CARTESIAN_POINT('Ctrl Pts',(4.91808052315557,6.19975446198252,-24.3557980874607));
#66979=CARTESIAN_POINT('Ctrl Pts',(4.75856737795069,6.32301793776689,-24.3476949272089));
#66980=CARTESIAN_POINT('Ctrl Pts',(4.59454193338072,6.44003924075049,-24.3395917669572));
#66981=CARTESIAN_POINT('Ctrl Pts',(4.43056636294747,6.55702496183715,-24.33149107058));
#66982=CARTESIAN_POINT('Ctrl Pts',(4.26208149043596,6.66777210977236,-24.3233903742029));
#66983=CARTESIAN_POINT('Ctrl Pts',(4.08959377008074,6.77193796455024,-24.3152896778257));
#66984=CARTESIAN_POINT('Ctrl Pts',(3.91578235993709,6.87690319958538,-24.3071268158112));
#66985=CARTESIAN_POINT('Ctrl Pts',(3.73790667150301,6.97518550845407,-24.2989639537967));
#66986=CARTESIAN_POINT('Ctrl Pts',(3.55651331511241,7.06647960723217,-24.2908010917821));
#66987=CARTESIAN_POINT('Ctrl Pts',(3.37650210555571,7.15707808048081,-24.2827004276017));
#66988=CARTESIAN_POINT('Ctrl Pts',(3.1930269502046,7.24079434660195,-24.2745997634213));
#66989=CARTESIAN_POINT('Ctrl Pts',(3.00664561236294,7.31737679511303,-24.2664990992409));
#66990=CARTESIAN_POINT('Ctrl Pts',(2.82023911686269,7.39396958068423,-24.2583973416369));
#66991=CARTESIAN_POINT('Ctrl Pts',(2.63092595321616,7.46342650635095,-24.250295584033));
#66992=CARTESIAN_POINT('Ctrl Pts',(2.43928317682044,7.52554440444549,-24.242193826429));
#66993=CARTESIAN_POINT('Ctrl Pts',(2.24758980797307,7.58767870126277,-24.2340899300135));
#66994=CARTESIAN_POINT('Ctrl Pts',(2.05356590493151,7.6424700078357,-24.225986033598));
#66995=CARTESIAN_POINT('Ctrl Pts',(1.85780349400208,7.68976509248974,-24.2178821371825));
#66996=CARTESIAN_POINT('Ctrl Pts',(1.6595159340693,7.73767023877568,-24.2096737082071));
#66997=CARTESIAN_POINT('Ctrl Pts',(1.45944503542726,7.77788435778688,-24.2014652792316));
#66998=CARTESIAN_POINT('Ctrl Pts',(1.25821628523376,7.8103017086136,-24.1932568502562));
#66999=CARTESIAN_POINT('Ctrl Pts',(1.05929224513906,7.84234777752482,-24.1851424339362));
#67000=CARTESIAN_POINT('Ctrl Pts',(0.859237060204384,7.86677472953465,-24.1770280176161));
#67001=CARTESIAN_POINT('Ctrl Pts',(0.658660039973107,7.88353270759643,-24.1689136012961));
#67002=CARTESIAN_POINT('Ctrl Pts',(0.454597227748876,7.9005819195477,-24.160658165993));
#67003=CARTESIAN_POINT('Ctrl Pts',(0.249994624954955,7.90969313899543,-24.1524027306898));
#67004=CARTESIAN_POINT('Ctrl Pts',(0.0454940565222883,7.91086918681008,
-24.1441472953866));
#67005=CARTESIAN_POINT('Ctrl Pts',(-0.159006511910379,7.91204523462473,
-24.1358918600835));
#67006=CARTESIAN_POINT('Ctrl Pts',(-0.363404700568143,7.90528615647321,
-24.1276364247803));
#67007=CARTESIAN_POINT('Ctrl Pts',(-0.567063678828794,7.89065014964883,
-24.1193809894772));
#67008=CARTESIAN_POINT('Ctrl Pts',(-0.762575431271365,7.87659964538218,
-24.1114558067178));
#67009=CARTESIAN_POINT('Ctrl Pts',(-0.95782422640749,7.85525971528149,-24.1035306239584));
#67010=CARTESIAN_POINT('Ctrl Pts',(-1.15222679269407,7.82664004654602,-24.0956054411991));
#67011=CARTESIAN_POINT('Ctrl Pts',(-1.34642164499087,7.79805095716809,-24.0876887262875));
#67012=CARTESIAN_POINT('Ctrl Pts',(-1.53977173385837,7.76219767094114,-24.0797720113759));
#67013=CARTESIAN_POINT('Ctrl Pts',(-1.73169585682538,7.71914182143675,-24.0718552964643));
#67014=CARTESIAN_POINT('Ctrl Pts',(-1.92344654674741,7.67612487953276,-24.0639457355255));
#67015=CARTESIAN_POINT('Ctrl Pts',(-2.11377350589463,7.62591841449473,-24.0560361745868));
#67016=CARTESIAN_POINT('Ctrl Pts',(-2.30210242628272,7.56863563787445,-24.0481266136481));
#67017=CARTESIAN_POINT('Ctrl Pts',(-2.49026575105275,7.51140322939083,-24.0402240075023));
#67018=CARTESIAN_POINT('Ctrl Pts',(-2.67643421347492,7.44710701282308,-24.0323214013564));
#67019=CARTESIAN_POINT('Ctrl Pts',(-2.86004540557255,7.37591087785525,-24.0244187952106));
#67020=CARTESIAN_POINT('Ctrl Pts',(-3.04356234462664,7.30475128996459,-24.0165202457057));
#67021=CARTESIAN_POINT('Ctrl Pts',(-3.22452431024445,7.22669896282485,-24.0086216962008));
#67022=CARTESIAN_POINT('Ctrl Pts',(-3.40238511850491,7.14196727137393,-24.0007231466959));
#67023=CARTESIAN_POINT('Ctrl Pts',(-3.5801856072484,7.05726431573473,-23.9928272758963));
#67024=CARTESIAN_POINT('Ctrl Pts',(-3.75488672539468,6.96588665561444,-23.9849314050967));
#67025=CARTESIAN_POINT('Ctrl Pts',(-3.92596303008034,6.86809546282245,-23.9770355342971));
#67026=CARTESIAN_POINT('Ctrl Pts',(-4.04453935060178,6.80031448145287,-23.97156275238));
#67027=CARTESIAN_POINT('Ctrl Pts',(-4.1613746770671,6.72945334943637,-23.9660899704629));
#67028=CARTESIAN_POINT('Ctrl Pts',(-4.27630092869887,6.65561202048385,-23.9606171885458));
#67029=CARTESIAN_POINT('Ctrl Pts',(-4.45520620594544,6.54066349270248,-23.9520977288724));
#67030=CARTESIAN_POINT('Ctrl Pts',(-4.62930592752166,6.41860602717389,-23.943578269199));
#67031=CARTESIAN_POINT('Ctrl Pts',(-4.79807192893164,6.28986699102598,-23.9350588095256));
#67032=CARTESIAN_POINT('Ctrl Pts',(-4.96714186508217,6.16089610565948,-23.926524006953));
#67033=CARTESIAN_POINT('Ctrl Pts',(-5.13085868478793,6.02521975164363,-23.9179892043803));
#67034=CARTESIAN_POINT('Ctrl Pts',(-5.28872864360726,5.88330437205896,-23.9094544018076));
#67035=CARTESIAN_POINT('Ctrl Pts',(-5.45458844269649,5.73420661766908,-23.9004876506248));
#67036=CARTESIAN_POINT('Ctrl Pts',(-5.61399403640044,5.5782222663753,-23.891520899442));
#67037=CARTESIAN_POINT('Ctrl Pts',(-5.7664199192343,5.41593226647619,-23.8825541482592));
#67038=CARTESIAN_POINT('Ctrl Pts',(-5.9121089970688,5.26081503843405,-23.8739837028289));
#67039=CARTESIAN_POINT('Ctrl Pts',(-6.05142189436461,5.0999377081641,-23.8654132573986));
#67040=CARTESIAN_POINT('Ctrl Pts',(-6.18394305456161,4.93383920471059,-23.8568428119683));
#67041=CARTESIAN_POINT('Ctrl Pts',(-6.31662981763305,4.76753313901139,-23.8482616566228));
#67042=CARTESIAN_POINT('Ctrl Pts',(-6.44250773683942,4.59599306323536,-23.8396805012772));
#67043=CARTESIAN_POINT('Ctrl Pts',(-6.56120404463471,4.41978760628485,-23.8310993459316));
#67044=CARTESIAN_POINT('Ctrl Pts',(-6.6800978412287,4.24328897590152,-23.8225039131237));
#67045=CARTESIAN_POINT('Ctrl Pts',(-6.79178599864974,4.06210965241128,-23.8139084803158));
#67046=CARTESIAN_POINT('Ctrl Pts',(-6.89594010202043,3.87684551012115,-23.8053130475079));
#67047=CARTESIAN_POINT('Ctrl Pts',(-6.90991410357315,3.85198925071088,-23.8041598275433));
#67048=CARTESIAN_POINT('Ctrl Pts',(-6.92375255642822,3.82705949472394,-23.8030066075787));
#67049=CARTESIAN_POINT('Ctrl Pts',(-6.93745473218874,3.80205771113906,-23.8018533876141));
#67050=CARTESIAN_POINT('Ctrl Pts',(-7.03379924037634,3.62626194078864,-23.7937447184316));
#67051=CARTESIAN_POINT('Ctrl Pts',(-7.12357291241415,3.44659227278591,-23.785636049249));
#67052=CARTESIAN_POINT('Ctrl Pts',(-7.20645898554778,3.26356704996506,-23.7775273800665));
#67053=CARTESIAN_POINT('Ctrl Pts',(-7.28924071827079,3.08077222685048,-23.7694289184115));
#67054=CARTESIAN_POINT('Ctrl Pts',(-7.3651520015754,2.89463055742132,-23.7613304567565));
#67055=CARTESIAN_POINT('Ctrl Pts',(-7.43392104025364,2.70568641332919,-23.7532319951014));
#67056=CARTESIAN_POINT('Ctrl Pts',(-7.50261247886534,2.51695547678565,-23.7451426718781));
#67057=CARTESIAN_POINT('Ctrl Pts',(-7.5641776284856,2.32542866839131,-23.7370533486548));
#67058=CARTESIAN_POINT('Ctrl Pts',(-7.61839182259162,2.1316723569698,-23.7289640254315));
#67059=CARTESIAN_POINT('Ctrl Pts',(-7.67253510355213,1.93816948230466,-23.7208852831891));
#67060=CARTESIAN_POINT('Ctrl Pts',(-7.71934652298509,1.742443229068,-23.7128065409468));
#67061=CARTESIAN_POINT('Ctrl Pts',(-7.75865048988188,1.54507720708569,-23.7047277987044));
#67062=CARTESIAN_POINT('Ctrl Pts',(-7.79792430116788,1.34786261238697,-23.6966552548035));
#67063=CARTESIAN_POINT('Ctrl Pts',(-7.8297020772218,1.14901106940106,-23.6885827109026));
#67064=CARTESIAN_POINT('Ctrl Pts',(-7.85385845500804,0.949119786275016,
-23.6805101670016));
#67065=CARTESIAN_POINT('Ctrl Pts',(-7.87799513818082,0.749391473838983,
-23.6724442046186));
#67066=CARTESIAN_POINT('Ctrl Pts',(-7.89452277826737,0.548625429427025,
-23.6643782422355));
#67067=CARTESIAN_POINT('Ctrl Pts',(-7.90336732057149,0.347427684738319,
-23.6563122798524));
#67068=CARTESIAN_POINT('Ctrl Pts',(-7.90847741655782,0.231182010034144,
-23.6516520226472));
#67069=CARTESIAN_POINT('Ctrl Pts',(-7.91102372207927,0.114792392926225,
-23.646991765442));
#67070=CARTESIAN_POINT('Ctrl Pts',(-7.91099983344385,-0.00162334571786968,
-23.6423315082368));
#67071=CARTESIAN_POINT('',(-7.91099783789749,0.00584882734057925,-19.6423315082367));
#67072=CARTESIAN_POINT('Ctrl Pts',(-7.91099989428398,-0.00129330542618517,
-23.6332372668359));
#67073=CARTESIAN_POINT('Ctrl Pts',(-7.91084051574585,-0.976193412347082,
-23.5954971353885));
#67074=CARTESIAN_POINT('Ctrl Pts',(-7.73051367551189,-1.94252686240568,
-23.5651777674233));
#67075=CARTESIAN_POINT('Ctrl Pts',(-7.31965879842538,-3.00561085447395,
-23.5251964480447));
#67076=CARTESIAN_POINT('Ctrl Pts',(-7.25543627084996,-3.15748978254176,
-23.5192774622992));
#67077=CARTESIAN_POINT('Ctrl Pts',(-7.13185426759604,-3.42602882992272,
-23.5082611349174));
#67078=CARTESIAN_POINT('Ctrl Pts',(-7.07425570650893,-3.54343361337518,
-23.5032486046814));
#67079=CARTESIAN_POINT('Ctrl Pts',(-7.00349681319634,-3.67905522057872,
-23.4971674565624));
#67080=CARTESIAN_POINT('Ctrl Pts',(-6.99313365172071,-3.69871553899137,
-23.4962786298811));
#67081=CARTESIAN_POINT('Ctrl Pts',(-6.97941705219739,-3.72447406193392,
-23.4951042094122));
#67082=CARTESIAN_POINT('Ctrl Pts',(-6.97613812619126,-3.73061205034906,
-23.4948236164228));
#67083=CARTESIAN_POINT('Ctrl Pts',(-6.97077561820131,-3.74061861032806,
-23.4943649532074));
#67084=CARTESIAN_POINT('Ctrl Pts',(-6.96869689823961,-3.74448979803012,
-23.4941872136849));
#67085=CARTESIAN_POINT('Ctrl Pts',(-6.96468708761452,-3.75194234055934,
-23.4938444624876));
#67086=CARTESIAN_POINT('Ctrl Pts',(-6.96275645652134,-3.75552394244948,
-23.4936794823449));
#67087=CARTESIAN_POINT('Ctrl Pts',(-6.95832008244876,-3.76373888265737,
-23.4933004798326));
#67088=CARTESIAN_POINT('Ctrl Pts',(-6.95581249244202,-3.76837117548673,
-23.4930863291968));
#67089=CARTESIAN_POINT('Ctrl Pts',(-6.94775177045063,-3.78322635863038,
-23.4923981761767));
#67090=CARTESIAN_POINT('Ctrl Pts',(-6.94218074931008,-3.79343944006282,
-23.4919229399362));
#67091=CARTESIAN_POINT('Ctrl Pts',(-6.89157876012235,-3.88572080741014,
-23.4876099472335));
#67092=CARTESIAN_POINT('Ctrl Pts',(-6.84511865525178,-3.96699296793113,
-23.4836757812747));
#67093=CARTESIAN_POINT('Ctrl Pts',(-6.57541061302697,-4.41994032987668,
-23.4610721512));
#67094=CARTESIAN_POINT('Ctrl Pts',(-6.32335693955479,-4.77357371037152,
-23.4408567516678));
#67095=CARTESIAN_POINT('Ctrl Pts',(-5.7850238442565,-5.41091796863225,-23.4019014654934));
#67096=CARTESIAN_POINT('Ctrl Pts',(-5.50351236041864,-5.69701027385652,
-23.3832241324591));
#67097=CARTESIAN_POINT('Ctrl Pts',(-4.93807177513233,-6.19044624449914,
-23.3497588865095));
#67098=CARTESIAN_POINT('Ctrl Pts',(-4.65965692572858,-6.40264156999199,
-23.3348086493368));
#67099=CARTESIAN_POINT('Ctrl Pts',(-4.34701574022773,-6.60969089504712,
-23.3196266583546));
#67100=CARTESIAN_POINT('Ctrl Pts',(-4.32588018113389,-6.62354287741171,
-23.3186076290462));
#67101=CARTESIAN_POINT('Ctrl Pts',(-4.29596035252199,-6.64294766089435,
-23.3171753079233));
#67102=CARTESIAN_POINT('Ctrl Pts',(-4.28723107677333,-6.64858471190051,
-23.3167586424165));
#67103=CARTESIAN_POINT('Ctrl Pts',(-4.27281963899332,-6.65785091372609,
-23.3160727623474));
#67104=CARTESIAN_POINT('Ctrl Pts',(-4.2671439127178,-6.66149001990078,-23.3158031504573));
#67105=CARTESIAN_POINT('Ctrl Pts',(-4.25535726192769,-6.66902602351231,
-23.3152443119733));
#67106=CARTESIAN_POINT('Ctrl Pts',(-4.2492456189772,-6.67292178876048,-23.3149551306023));
#67107=CARTESIAN_POINT('Ctrl Pts',(-4.23467195658778,-6.68218338700676,
-23.3142669548159));
#67108=CARTESIAN_POINT('Ctrl Pts',(-4.22620506967614,-6.68754155931461,
-23.3138682649928));
#67109=CARTESIAN_POINT('Ctrl Pts',(-4.19848077058032,-6.70501288541247,
-23.3125664282954));
#67110=CARTESIAN_POINT('Ctrl Pts',(-4.17918119788709,-6.71705911106172,
-23.3116659320452));
#67111=CARTESIAN_POINT('Ctrl Pts',(-3.95191828272223,-6.85755130339652,
-23.3011287875819));
#67112=CARTESIAN_POINT('Ctrl Pts',(-3.73815358238242,-6.97638075731118,
-23.2918776879057));
#67113=CARTESIAN_POINT('Ctrl Pts',(-3.31370427016879,-7.18720669631126,
-23.2745481922498));
#67114=CARTESIAN_POINT('Ctrl Pts',(-3.10384312130114,-7.28029811729927,
-23.2664402409466));
#67115=CARTESIAN_POINT('Ctrl Pts',(-2.57752173916738,-7.48686503018814,
-23.2468498041398));
#67116=CARTESIAN_POINT('Ctrl Pts',(-2.25731716572849,-7.58955100482637,
-23.2355757754633));
#67117=CARTESIAN_POINT('Ctrl Pts',(-1.67936939007355,-7.73506767771934,
-23.2151519638779));
#67118=CARTESIAN_POINT('Ctrl Pts',(-1.42421081325541,-7.78608789002875,
-23.2061038995402));
#67119=CARTESIAN_POINT('Ctrl Pts',(-1.04113369466977,-7.84322387867413,
-23.1918924784364));
#67120=CARTESIAN_POINT('Ctrl Pts',(-0.914820465146266,-7.85895801013937,
-23.1871055225053));
#67121=CARTESIAN_POINT('Ctrl Pts',(-0.729428076826358,-7.87752137782858,
-23.1798598037081));
#67122=CARTESIAN_POINT('Ctrl Pts',(-0.670605293340097,-7.88274676572456,
-23.177528553565));
#67123=CARTESIAN_POINT('Ctrl Pts',(-0.602180157707596,-7.88805374126582,
-23.1747734298128));
#67124=CARTESIAN_POINT('Ctrl Pts',(-0.592628105192426,-7.88877713547769,
-23.1743878329442));
#67125=CARTESIAN_POINT('Ctrl Pts',(-0.577971896351022,-7.8898603073054,
-23.1737946931248));
#67126=CARTESIAN_POINT('Ctrl Pts',(-0.572868648418705,-7.89023248663708,
-23.1735878855771));
#67127=CARTESIAN_POINT('Ctrl Pts',(-0.563549365801968,-7.89090305201829,
-23.1732097212759));
#67128=CARTESIAN_POINT('Ctrl Pts',(-0.559333442395606,-7.89120301121004,
-23.1730384565854));
#67129=CARTESIAN_POINT('Ctrl Pts',(-0.550204907701421,-7.89184514612619,
-23.1726672213147));
#67130=CARTESIAN_POINT('Ctrl Pts',(-0.54529221595035,-7.89218611348633,
-23.17246718073));
#67131=CARTESIAN_POINT('Ctrl Pts',(-0.531942772604608,-7.89310011300755,
-23.171922920315));
#67132=CARTESIAN_POINT('Ctrl Pts',(-0.523505436032349,-7.89366420394659,
-23.1715781871559));
#67133=CARTESIAN_POINT('Ctrl Pts',(-0.483533326667343,-7.89627223080815,
-23.1699415480746));
#67134=CARTESIAN_POINT('Ctrl Pts',(-0.451987788904008,-7.89814070562536,
-23.1686397421444));
#67135=CARTESIAN_POINT('Ctrl Pts',(0.0816944352461355,-7.9265435375431,
-23.1464533554239));
#67136=CARTESIAN_POINT('Ctrl Pts',(0.585182534074961,-7.9053296285658,-23.1231420560138));
#67137=CARTESIAN_POINT('Ctrl Pts',(1.49190222727378,-7.77999887878778,-23.0804691799043));
#67138=CARTESIAN_POINT('Ctrl Pts',(1.8955886470672,-7.6916146280026,-23.0612116250202));
#67139=CARTESIAN_POINT('Ctrl Pts',(2.66534341494268,-7.45876579349694,-23.0251686377036));
#67140=CARTESIAN_POINT('Ctrl Pts',(3.03122701283588,-7.31771570413891,-23.0083552476783));
#67141=CARTESIAN_POINT('Ctrl Pts',(3.40810512020531,-7.13928448250228,-22.9914361243897));
#67142=CARTESIAN_POINT('Ctrl Pts',(3.43096148138346,-7.12832846895099,-22.9904114965507));
#67143=CARTESIAN_POINT('Ctrl Pts',(3.46349110267295,-7.1125429528667,-22.9889552326629));
#67144=CARTESIAN_POINT('Ctrl Pts',(3.47320761126438,-7.10780323059943,-22.9885205070163));
#67145=CARTESIAN_POINT('Ctrl Pts',(3.48997260496885,-7.0995826646975,-22.9877708605858));
#67146=CARTESIAN_POINT('Ctrl Pts',(3.49702566180411,-7.09611121089908,-22.9874556165575));
#67147=CARTESIAN_POINT('Ctrl Pts',(3.51129968309165,-7.08905921104586,-22.9868178899528));
#67148=CARTESIAN_POINT('Ctrl Pts',(3.5185203739923,-7.08547813069001,-22.9864954263375));
#67149=CARTESIAN_POINT('Ctrl Pts',(3.53620143579023,-7.07667556753425,-22.985706154469));
#67150=CARTESIAN_POINT('Ctrl Pts',(3.54665574351732,-7.07144191244539,-22.9852397674271));
#67151=CARTESIAN_POINT('Ctrl Pts',(3.58309866424427,-7.05309664482877,-22.9836149559846));
#67152=CARTESIAN_POINT('Ctrl Pts',(3.60902662196105,-7.03986471345453,-22.9824606959615));
#67153=CARTESIAN_POINT('Ctrl Pts',(4.05595964764183,-6.80866130332363,-22.9625923036997));
#67154=CARTESIAN_POINT('Ctrl Pts',(4.45662792461579,-6.55341173095615,-22.9452928760393));
#67155=CARTESIAN_POINT('Ctrl Pts',(4.91888357792768,-6.19681629661714,-22.9247473390674));
#67156=CARTESIAN_POINT('Ctrl Pts',(5.00431449693323,-6.12803268761209,-22.9209190930447));
#67157=CARTESIAN_POINT('Ctrl Pts',(5.4325393369979,-5.7683243354554,-22.9014696783125));
#67158=CARTESIAN_POINT('Ctrl Pts',(5.75149633563491,-5.45034871983454,-22.8861467948277));
#67159=CARTESIAN_POINT('Ctrl Pts',(6.09275604566406,-5.04663240105663,-22.8667378087672));
#67160=CARTESIAN_POINT('Ctrl Pts',(6.14289823663191,-4.98547646606103,-22.8637977633662));
#67161=CARTESIAN_POINT('Ctrl Pts',(6.27102358523628,-4.82434031455888,-22.8560250074591));
#67162=CARTESIAN_POINT('Ctrl Pts',(6.34752650342914,-4.72322987791262,-22.8511121972765));
#67163=CARTESIAN_POINT('Ctrl Pts',(6.4383219813994,-4.59703751595736,-22.8449376903231));
#67164=CARTESIAN_POINT('Ctrl Pts',(6.45494850985224,-4.57366194299804,-22.8437925872339));
#67165=CARTESIAN_POINT('Ctrl Pts',(6.47779738291332,-4.54116548366674,-22.842199285572));
#67166=CARTESIAN_POINT('Ctrl Pts',(6.48412843280144,-4.53212106520379,-22.841755689226));
#67167=CARTESIAN_POINT('Ctrl Pts',(6.49479756797413,-4.51681122312205,-22.8410045780519));
#67168=CARTESIAN_POINT('Ctrl Pts',(6.4991455800311,-4.51055271595362,-22.8406974700386));
#67169=CARTESIAN_POINT('Ctrl Pts',(6.50774307078379,-4.49813928928504,-22.8400882278452));
#67170=CARTESIAN_POINT('Ctrl Pts',(6.51199287803341,-4.49198460562465,-22.8397861072629));
#67171=CARTESIAN_POINT('Ctrl Pts',(6.52135816336594,-4.47838032883842,-22.8391181975303));
#67172=CARTESIAN_POINT('Ctrl Pts',(6.52646961469048,-4.47092798336397,-22.8387522515846));
#67173=CARTESIAN_POINT('Ctrl Pts',(6.54436295633191,-4.44474394640974,-22.8374662843723));
#67174=CARTESIAN_POINT('Ctrl Pts',(6.5570770071564,-4.42596615041604,-22.836543689582));
#67175=CARTESIAN_POINT('Ctrl Pts',(6.76432861909984,-4.11701639132446,-22.8213608936073));
#67176=CARTESIAN_POINT('Ctrl Pts',(6.93950979941507,-3.81433505291634,-22.8064583039197));
#67177=CARTESIAN_POINT('Ctrl Pts',(7.37422346845891,-2.93349181234954,-22.7642753501626));
#67178=CARTESIAN_POINT('Ctrl Pts',(7.58522803413551,-2.3342953817592,-22.7371205485005));
#67179=CARTESIAN_POINT('Ctrl Pts',(7.80967299601987,-1.3244344980061,-22.6940905673222));
#67180=CARTESIAN_POINT('Ctrl Pts',(7.86682090775009,-0.92642465767085,-22.6775978506539));
#67181=CARTESIAN_POINT('Ctrl Pts',(7.89694819995191,-0.47414181696498,-22.6592280992672));
#67182=CARTESIAN_POINT('Ctrl Pts',(7.89988202566965,-0.422451605532426,
-22.6571350301828));
#67183=CARTESIAN_POINT('Ctrl Pts',(7.90355661638236,-0.344127030931268,
-22.6539730082449));
#67184=CARTESIAN_POINT('Ctrl Pts',(7.90467057463607,-0.317511754710679,
-22.6529001945161));
#67185=CARTESIAN_POINT('Ctrl Pts',(7.90636927135538,-0.27134570666822,-22.6510421762088));
#67186=CARTESIAN_POINT('Ctrl Pts',(7.90701597186309,-0.251797479580481,
-22.6502563161218));
#67187=CARTESIAN_POINT('Ctrl Pts',(7.90821151590552,-0.211091372095154,
-22.6486217082265));
#67188=CARTESIAN_POINT('Ctrl Pts',(7.90874796043926,-0.189933275316337,
-22.6477731013576));
#67189=CARTESIAN_POINT('Ctrl Pts',(7.90999222863793,-0.131623289698204,
-22.6454371865066));
#67190=CARTESIAN_POINT('Ctrl Pts',(7.91052321549963,-0.0944680990550924,
-22.6439518458459));
#67191=CARTESIAN_POINT('Ctrl Pts',(7.91159562359502,0.0535607596952131,
-22.6380460540293));
#67192=CARTESIAN_POINT('Ctrl Pts',(7.91006794023323,0.164437517092207,-22.6336492903225));
#67193=CARTESIAN_POINT('Ctrl Pts',(7.88117583046183,0.994337554661038,-22.6009046547237));
#67194=CARTESIAN_POINT('Ctrl Pts',(7.75815828832591,1.70662002243985,-22.574056958052));
#67195=CARTESIAN_POINT('Ctrl Pts',(7.51234785293637,2.48138342621886,-22.5420656792621));
#67196=CARTESIAN_POINT('Ctrl Pts',(7.48254725891005,2.56984824459782,-22.5383643831634));
#67197=CARTESIAN_POINT('Ctrl Pts',(7.44441096772453,2.67676546400133,-22.5338166259961));
#67198=CARTESIAN_POINT('Ctrl Pts',(7.43756062350818,2.69574108065189,-22.5330065951247));
#67199=CARTESIAN_POINT('Ctrl Pts',(7.42647815555818,2.72607595979644,-22.5317069085926));
#67200=CARTESIAN_POINT('Ctrl Pts',(7.42229242210684,2.73745194168732,-22.5312184469923));
#67201=CARTESIAN_POINT('Ctrl Pts',(7.41425149018237,2.75915155067683,-22.5302847133134));
#67202=CARTESIAN_POINT('Ctrl Pts',(7.41040083213919,2.76947683604567,-22.5298395514715));
#67203=CARTESIAN_POINT('Ctrl Pts',(7.40154016876304,2.7930853323432,-22.5288197485293));
#67204=CARTESIAN_POINT('Ctrl Pts',(7.39651596083298,2.80636315946921,-22.5282447768672));
#67205=CARTESIAN_POINT('Ctrl Pts',(7.38128637350956,2.84628645820132,-22.5265117843791));
#67206=CARTESIAN_POINT('Ctrl Pts',(7.37097258579096,2.87289022676991,-22.5253513404579));
#67207=CARTESIAN_POINT('Ctrl Pts',(7.26805159049797,3.13416557612076,-22.5139012392555));
#67208=CARTESIAN_POINT('Ctrl Pts',(7.16441453200506,3.36433153902463,-22.5033932031116));
#67209=CARTESIAN_POINT('Ctrl Pts',(6.85128875591306,3.97938713184054,-22.474473743837));
#67210=CARTESIAN_POINT('Ctrl Pts',(6.62055271442245,4.35246763972521,-22.4560163624423));
#67211=CARTESIAN_POINT('Ctrl Pts',(6.22857203166411,4.88239202367224,-22.4287463610505));
#67212=CARTESIAN_POINT('Ctrl Pts',(6.08960891259975,5.05465410361187,-22.4196841489124));
#67213=CARTESIAN_POINT('Ctrl Pts',(5.91028409020812,5.25880332711376,-22.4086708350538));
#67214=CARTESIAN_POINT('Ctrl Pts',(5.8765992036506,5.29641881846097,-22.4066294083844));
#67215=CARTESIAN_POINT('Ctrl Pts',(5.82260416059552,5.35556510108791,-22.4033992654985));
#67216=CARTESIAN_POINT('Ctrl Pts',(5.80252941559471,5.37730872761792,-22.4022073664768));
#67217=CARTESIAN_POINT('Ctrl Pts',(5.76445535173527,5.41808653770854,-22.3999635075256));
#67218=CARTESIAN_POINT('Ctrl Pts',(5.74648258251383,5.43714494624809,-22.3989112047847));
#67219=CARTESIAN_POINT('Ctrl Pts',(5.7056408383252,5.48002500487059,-22.3965352665139));
#67220=CARTESIAN_POINT('Ctrl Pts',(5.68271668598925,5.50379346516537,-22.3952123974081));
#67221=CARTESIAN_POINT('Ctrl Pts',(5.62297201499754,5.56496734486013,-22.3917918756111));
#67222=CARTESIAN_POINT('Ctrl Pts',(5.58592678674641,5.60215117639909,-22.389697248834));
#67223=CARTESIAN_POINT('Ctrl Pts',(5.3772485281138,5.80748221318233,-22.3780387654395));
#67224=CARTESIAN_POINT('Ctrl Pts',(5.19839109571368,5.96811394540662,-22.3685563541904));
#67225=CARTESIAN_POINT('Ctrl Pts',(4.37138269417036,6.64542419015001,-22.3267015104359));
#67226=CARTESIAN_POINT('Ctrl Pts',(3.65177385603422,7.06647964446705,-22.2965018722598));
#67227=CARTESIAN_POINT('Ctrl Pts',(2.70191170831728,7.43775153801269,-22.2581994294924));
#67228=CARTESIAN_POINT('Ctrl Pts',(2.52138058201012,7.50087398837203,-22.2509387627355));
#67229=CARTESIAN_POINT('Ctrl Pts',(2.25848251306327,7.58223166325244,-22.2402112474926));
#67230=CARTESIAN_POINT('Ctrl Pts',(2.17782954689089,7.6057897789489,-22.2368994663054));
#67231=CARTESIAN_POINT('Ctrl Pts',(2.08242666126868,7.63201434564827,-22.2329435918397));
#67232=CARTESIAN_POINT('Ctrl Pts',(2.06802383360748,7.635929621974,-22.2323453523953));
#67233=CARTESIAN_POINT('Ctrl Pts',(2.04591819467087,7.64187170663615,-22.231425486507));
#67234=CARTESIAN_POINT('Ctrl Pts',(2.03822321639418,7.6439276919373,-22.231104969135));
#67235=CARTESIAN_POINT('Ctrl Pts',(2.02479068657937,7.64749494141583,-22.2305449042382));
#67236=CARTESIAN_POINT('Ctrl Pts',(2.01905450835133,7.64901138026938,-22.230305557382));
#67237=CARTESIAN_POINT('Ctrl Pts',(2.00613624963292,7.65241095841575,-22.2297661198211));
#67238=CARTESIAN_POINT('Ctrl Pts',(1.9989532187864,7.65429044113134,-22.2294658857942));
#67239=CARTESIAN_POINT('Ctrl Pts',(1.97970632349646,7.65929756517387,-22.2286606192096));
#67240=CARTESIAN_POINT('Ctrl Pts',(1.96763772593491,7.66240680832761,-22.2281548521215));
#67241=CARTESIAN_POINT('Ctrl Pts',(1.91536699272888,7.67574172708604,-22.2259605296573));
#67242=CARTESIAN_POINT('Ctrl Pts',(1.87509260962544,7.68567950085647,-22.2242601552386));
#67243=CARTESIAN_POINT('Ctrl Pts',(1.21237203377993,7.84368784525397,-22.1960965708982));
#67244=CARTESIAN_POINT('Ctrl Pts',(0.57438533820619,7.91600567465618,-22.16613042399));
#67245=CARTESIAN_POINT('Ctrl Pts',(-0.430327308261512,7.90772028401306,
-22.1199923195091));
#67246=CARTESIAN_POINT('Ctrl Pts',(-0.794792461017725,7.87943897231964,
-22.1034501397239));
#67247=CARTESIAN_POINT('Ctrl Pts',(-1.34482866753871,7.79819102942153,-22.079236893331));
#67248=CARTESIAN_POINT('Ctrl Pts',(-1.53257303275275,7.76347690042345,-22.0711030495767));
#67249=CARTESIAN_POINT('Ctrl Pts',(-1.81359268262661,7.70092307848371,-22.0591373163976));
#67250=CARTESIAN_POINT('Ctrl Pts',(-1.9079049794263,7.67810094410115,-22.0551572315127));
#67251=CARTESIAN_POINT('Ctrl Pts',(-2.01930230789671,7.64896511835098,-22.0504968028438));
#67252=CARTESIAN_POINT('Ctrl Pts',(-2.03681310442316,7.64432087078328,-22.0497654149583));
#67253=CARTESIAN_POINT('Ctrl Pts',(-2.06373603137056,7.63708124289795,-22.0486427180843));
#67254=CARTESIAN_POINT('Ctrl Pts',(-2.07315951569555,7.63452853430494,-22.048250097854));
#67255=CARTESIAN_POINT('Ctrl Pts',(-2.08963516340578,7.63003272546929,-22.0475642511235));
#67256=CARTESIAN_POINT('Ctrl Pts',(-2.09668939321013,7.62809727891814,-22.0472707893284));
#67257=CARTESIAN_POINT('Ctrl Pts',(-2.11261290983539,7.62370463717358,-22.0466087865065));
#67258=CARTESIAN_POINT('Ctrl Pts',(-2.12148062020833,7.62124174137317,-22.0462404217226));
#67259=CARTESIAN_POINT('Ctrl Pts',(-2.14533845510019,7.61457065924654,-22.0452501693155));
#67260=CARTESIAN_POINT('Ctrl Pts',(-2.16032052078207,7.61033367615802,-22.0446291714907));
#67261=CARTESIAN_POINT('Ctrl Pts',(-2.22612395999562,7.59151424703583,-22.0419053517552));
#67262=CARTESIAN_POINT('Ctrl Pts',(-2.27681142968143,7.5764666099866,-22.0398169419149));
#67263=CARTESIAN_POINT('Ctrl Pts',(-3.20878527784575,7.28959320209711,-22.0015858713703));
#67264=CARTESIAN_POINT('Ctrl Pts',(-4.03589018235152,6.86628985562685,-21.9714063754079));
#67265=CARTESIAN_POINT('Ctrl Pts',(-5.04632440838532,6.10223592929356,-21.9265305360208));
#67266=CARTESIAN_POINT('Ctrl Pts',(-5.30731040620941,5.87665850646896,-21.9139019888801));
#67267=CARTESIAN_POINT('Ctrl Pts',(-5.56453915577041,5.62317517220759,-21.8994823445023));
#67268=CARTESIAN_POINT('Ctrl Pts',(-5.57629353057887,5.61151900005601,-21.8988189627167));
#67269=CARTESIAN_POINT('Ctrl Pts',(-5.59332656727204,5.59452190090836,-21.8978512874785));
#67270=CARTESIAN_POINT('Ctrl Pts',(-5.59863440074843,5.58921016191732,-21.897548834385));
#67271=CARTESIAN_POINT('Ctrl Pts',(-5.60790837810292,5.57990289497959,-21.8970188063976));
#67272=CARTESIAN_POINT('Ctrl Pts',(-5.61187784079932,5.57591066950652,-21.8967914364459));
#67273=CARTESIAN_POINT('Ctrl Pts',(-5.61955734312656,5.56817062220024,-21.8963505804115));
#67274=CARTESIAN_POINT('Ctrl Pts',(-5.62326790417411,5.56442332037533,-21.8961371262027));
#67275=CARTESIAN_POINT('Ctrl Pts',(-5.63208627988719,5.55549979920899,-21.8956287914814));
#67276=CARTESIAN_POINT('Ctrl Pts',(-5.63719070342746,5.55032024803654,-21.8953337089978));
#67277=CARTESIAN_POINT('Ctrl Pts',(-5.65525578417121,5.5319386555328,-21.8942864308354));
#67278=CARTESIAN_POINT('Ctrl Pts',(-5.66817720190492,5.51869825890218,-21.8935319473368));
#67279=CARTESIAN_POINT('Ctrl Pts',(-5.88412147885672,5.29586470930945,-21.8808339689964));
#67280=CARTESIAN_POINT('Ctrl Pts',(-6.07543200940952,5.0752513930314,-21.8682700522114));
#67281=CARTESIAN_POINT('Ctrl Pts',(-6.58990625490721,4.41109250300468,-21.8315558646562));
#67282=CARTESIAN_POINT('Ctrl Pts',(-6.87975077987268,3.94381775880358,-21.8071511957049));
#67283=CARTESIAN_POINT('Ctrl Pts',(-7.23135185271398,3.21837067568155,-21.7728822125021));
#67284=CARTESIAN_POINT('Ctrl Pts',(-7.33237056327463,2.98105878774141,-21.7621589383175));
#67285=CARTESIAN_POINT('Ctrl Pts',(-7.44064482000948,2.68770205201674,-21.7494384026835));
#67286=CARTESIAN_POINT('Ctrl Pts',(-7.45912562423524,2.63597850386946,-21.7472148616269));
#67287=CARTESIAN_POINT('Ctrl Pts',(-7.48389680483133,2.56430241570359,-21.744158853042));
#67288=CARTESIAN_POINT('Ctrl Pts',(-7.49064880782332,2.54451148697386,-21.7433176807792));
#67289=CARTESIAN_POINT('Ctrl Pts',(-7.50191917932764,2.5110430315408,-21.7418995294627));
#67290=CARTESIAN_POINT('Ctrl Pts',(-7.50647879443288,2.49737954458699,-21.7413217916635));
#67291=CARTESIAN_POINT('Ctrl Pts',(-7.51543841824509,2.47028462770188,-21.7401785069937));
#67292=CARTESIAN_POINT('Ctrl Pts',(-7.51983979973477,2.45685370913308,-21.739612937059));
#67293=CARTESIAN_POINT('Ctrl Pts',(-7.529485322523,2.42715142360607,-21.7383646925643));
#67294=CARTESIAN_POINT('Ctrl Pts',(-7.53471276508316,2.41087469716293,-21.7376823173708));
#67295=CARTESIAN_POINT('Ctrl Pts',(-7.55279928086023,2.35392515735811,-21.7353004581754));
#67296=CARTESIAN_POINT('Ctrl Pts',(-7.56538219985673,2.31316511146344,-21.7336057092668));
#67297=CARTESIAN_POINT('Ctrl Pts',(-7.68569922518216,1.91193445873651,-21.7170177936768));
#67298=CARTESIAN_POINT('Ctrl Pts',(-7.76792201408034,1.54430430970014,-21.7026016950373));
#67299=CARTESIAN_POINT('Ctrl Pts',(-7.88207626752522,0.782401121233623,
-21.6737517325164));
#67300=CARTESIAN_POINT('Ctrl Pts',(-7.91126590000934,0.388781467887902,
-21.6593907303491));
#67301=CARTESIAN_POINT('Ctrl Pts',(-7.9107453481563,-0.377594936895521,
-21.6310986099574));
#67302=CARTESIAN_POINT('Ctrl Pts',(-7.88422256037135,-0.74931394523605,
-21.6172139151197));
#67303=CARTESIAN_POINT('Ctrl Pts',(-7.82709551820483,-1.14957815692969,
-21.6011465364909));
#67304=CARTESIAN_POINT('Ctrl Pts',(-7.82236008985292,-1.18137072028408,
-21.5998624694306));
#67305=CARTESIAN_POINT('Ctrl Pts',(-7.81574373215853,-1.224006531189,-21.5981290760551));
#67306=CARTESIAN_POINT('Ctrl Pts',(-7.81403370580807,-1.23487623596033,
-21.5976861649682));
#67307=CARTESIAN_POINT('Ctrl Pts',(-7.8113183666466,-1.25190467500851,-21.5969907040537));
#67308=CARTESIAN_POINT('Ctrl Pts',(-7.8103284312545,-1.25806587112258,-21.5967387456762));
#67309=CARTESIAN_POINT('Ctrl Pts',(-7.8084163474171,-1.26987712751478,-21.5962550935644));
#67310=CARTESIAN_POINT('Ctrl Pts',(-7.80749535354654,-1.27552737239145,
-21.5960234449693));
#67311=CARTESIAN_POINT('Ctrl Pts',(-7.8053209589131,-1.28877656850025,-21.5954795894983));
#67312=CARTESIAN_POINT('Ctrl Pts',(-7.80406259431449,-1.29637469067541,
-21.5951671868897));
#67313=CARTESIAN_POINT('Ctrl Pts',(-7.80040402963538,-1.31826706755527,
-21.5942655600549));
#67314=CARTESIAN_POINT('Ctrl Pts',(-7.79797564567644,-1.33255653261232,
-21.5936752053667));
#67315=CARTESIAN_POINT('Ctrl Pts',(-7.78141620456644,-1.42840261280558,
-21.5897026151095));
#67316=CARTESIAN_POINT('Ctrl Pts',(-7.76604536180301,-1.5097388793009,-21.5862688377717));
#67317=CARTESIAN_POINT('Ctrl Pts',(-7.71184000235685,-1.77379093475102,
-21.5748850699228));
#67318=CARTESIAN_POINT('Ctrl Pts',(-7.66781245105766,-1.95536575576184,
-21.5666981148979));
#67319=CARTESIAN_POINT('Ctrl Pts',(-7.36151260778159,-3.048100702441,-21.5159179917715));
#67320=CARTESIAN_POINT('Ctrl Pts',(-6.94345973240831,-3.90794187958212,
-21.4706865502298));
#67321=CARTESIAN_POINT('Ctrl Pts',(-6.35960268692158,-4.70541822230912,
-21.430267071367));
#67322=CARTESIAN_POINT('Ctrl Pts',(-6.33583459448097,-4.73737343220393,
-21.4286480529591));
#67323=CARTESIAN_POINT('Ctrl Pts',(-6.30224815468107,-4.78182408831214,
-21.4263966707751));
#67324=CARTESIAN_POINT('Ctrl Pts',(-6.29263213145982,-4.79447121972945,
-21.4257561878589));
#67325=CARTESIAN_POINT('Ctrl Pts',(-6.27708819846478,-4.81478750314993,
-21.4247274382396));
#67326=CARTESIAN_POINT('Ctrl Pts',(-6.27118420340238,-4.82247484593607,
-21.4243382040122));
#67327=CARTESIAN_POINT('Ctrl Pts',(-6.26065547613108,-4.83613182544767,
-21.423646753508));
#67328=CARTESIAN_POINT('Ctrl Pts',(-6.25603630242249,-4.84210572035682,
-21.4233443116545));
#67329=CARTESIAN_POINT('Ctrl Pts',(-6.24638512293663,-4.85455055485945,
-21.4227142938342));
#67330=CARTESIAN_POINT('Ctrl Pts',(-6.24135159748562,-4.86102030759316,
-21.4223867805118));
#67331=CARTESIAN_POINT('Ctrl Pts',(-6.22826277664478,-4.87778994625331,
-21.4215379040403));
#67332=CARTESIAN_POINT('Ctrl Pts',(-6.22019196937048,-4.88807772453234,
-21.4210171776815));
#67333=CARTESIAN_POINT('Ctrl Pts',(-6.18571789394125,-4.93179784503496,
-21.4188043793465));
#67334=CARTESIAN_POINT('Ctrl Pts',(-6.15907007770094,-4.96503692839506,
-21.4171224107468));
#67335=CARTESIAN_POINT('Ctrl Pts',(-5.97655741977728,-5.18896300841103,
-21.4057918523416));
#67336=CARTESIAN_POINT('Ctrl Pts',(-5.81212428790815,-5.37250403766793,
-21.3965137693093));
#67337=CARTESIAN_POINT('Ctrl Pts',(-5.40897519610457,-5.78228743705215,
-21.375593996404));
#67338=CARTESIAN_POINT('Ctrl Pts',(-5.16419176956802,-6.00191637688304,
-21.3642256674013));
#67339=CARTESIAN_POINT('Ctrl Pts',(-4.80116549772192,-6.28893833943299,
-21.3485261259123));
#67340=CARTESIAN_POINT('Ctrl Pts',(-4.69377752270709,-6.36948886963239,
-21.3440099669713));
#67341=CARTESIAN_POINT('Ctrl Pts',(-4.4642599355813,-6.53268954279551,-21.3345381723446));
#67342=CARTESIAN_POINT('Ctrl Pts',(-4.34176465049529,-6.61473572084111,
-21.3295848862548));
#67343=CARTESIAN_POINT('Ctrl Pts',(-3.84086786837393,-6.93032041986989,
-21.3094941013542));
#67344=CARTESIAN_POINT('Ctrl Pts',(-3.44541288476946,-7.13516996035063,
-21.294017865501));
#67345=CARTESIAN_POINT('Ctrl Pts',(-3.00797075166161,-7.31689028865405,
-21.2752787874538));
#67346=CARTESIAN_POINT('Ctrl Pts',(-2.98097686664058,-7.32792934030669,
-21.2741160443696));
#67347=CARTESIAN_POINT('Ctrl Pts',(-2.94654501499779,-7.34178838748635,
-21.2726241013143));
#67348=CARTESIAN_POINT('Ctrl Pts',(-2.9391626799767,-7.34474689773294,-21.2723037084602));
#67349=CARTESIAN_POINT('Ctrl Pts',(-2.92744482765136,-7.34942239403138,
-21.2717943217546));
#67350=CARTESIAN_POINT('Ctrl Pts',(-2.92311221464665,-7.35114669457967,
-21.271605798405));
#67351=CARTESIAN_POINT('Ctrl Pts',(-2.91504043116856,-7.35435085212021,
-21.2712542339505));
#67352=CARTESIAN_POINT('Ctrl Pts',(-2.91130164966327,-7.35583169165633,
-21.2710912565613));
#67353=CARTESIAN_POINT('Ctrl Pts',(-2.90300656327971,-7.35910985676302,
-21.2707293609128));
#67354=CARTESIAN_POINT('Ctrl Pts',(-2.89844974518951,-7.36090579106245,
-21.2705303535507));
#67355=CARTESIAN_POINT('Ctrl Pts',(-2.88510607476708,-7.36615048987092,
-21.269947003274));
#67356=CARTESIAN_POINT('Ctrl Pts',(-2.8763147836479,-7.36958773378039,-21.269561913305));
#67357=CARTESIAN_POINT('Ctrl Pts',(-2.81100485424835,-7.39498813046937,
-21.266695613037));
#67358=CARTESIAN_POINT('Ctrl Pts',(-2.75424295948736,-7.41631600384348,
-21.2641739677269));
#67359=CARTESIAN_POINT('Ctrl Pts',(-2.5661021774853,-7.48455080145951,-21.2557307107967));
#67360=CARTESIAN_POINT('Ctrl Pts',(-2.43373237539814,-7.52863360485083,
-21.2496546623201));
#67361=CARTESIAN_POINT('Ctrl Pts',(-2.02692100712389,-7.65226337220843,
-21.2307340730246));
#67362=CARTESIAN_POINT('Ctrl Pts',(-1.74928006592286,-7.72046299806746,
-21.2174909062702));
#67363=CARTESIAN_POINT('Ctrl Pts',(-0.716985315266224,-7.91548474314031,
-21.1684926338017));
#67364=CARTESIAN_POINT('Ctrl Pts',(0.0514080090607971,-7.94775444566785,
-21.1330290838053));
#67365=CARTESIAN_POINT('Ctrl Pts',(0.861093271274686,-7.86414778730948,
-21.0997509164887));
#67366=CARTESIAN_POINT('Ctrl Pts',(0.909584295851367,-7.85868682231813,
-21.0977711891163));
#67367=CARTESIAN_POINT('Ctrl Pts',(0.971750152234671,-7.85110271871587,
-21.0952498150449));
#67368=CARTESIAN_POINT('Ctrl Pts',(0.985473616269634,-7.84939195177175,
-21.0946942499346));
#67369=CARTESIAN_POINT('Ctrl Pts',(1.00735506278086,-7.84660592127813,-21.0938100757642));
#67370=CARTESIAN_POINT('Ctrl Pts',(1.0155159434255,-7.84555390495557,-21.0934806813097));
#67371=CARTESIAN_POINT('Ctrl Pts',(1.03078586071227,-7.84356124041183,-21.0928650293529));
#67372=CARTESIAN_POINT('Ctrl Pts',(1.03789528425489,-7.84262365551421,-21.0925786686148));
#67373=CARTESIAN_POINT('Ctrl Pts',(1.0537463342409,-7.84051130085311,-21.0919408177637));
#67374=CARTESIAN_POINT('Ctrl Pts',(1.06248729705286,-7.83933157482365,-21.0915894956364));
#67375=CARTESIAN_POINT('Ctrl Pts',(1.0879854703983,-7.83584677827224,-21.0905658659417));
#67376=CARTESIAN_POINT('Ctrl Pts',(1.10473733351307,-7.83350257197665,-21.0898948825024));
#67377=CARTESIAN_POINT('Ctrl Pts',(1.2252407898825,-7.81624543933323,-21.0850790317458));
#67378=CARTESIAN_POINT('Ctrl Pts',(1.32869673371227,-7.79932521820932,-21.0810024810428));
#67379=CARTESIAN_POINT('Ctrl Pts',(1.65784436251976,-7.73875344090587,-21.0681982896105));
#67380=CARTESIAN_POINT('Ctrl Pts',(1.88198772269963,-7.68731970907369,-21.0597328815518));
#67381=CARTESIAN_POINT('Ctrl Pts',(2.59089059771522,-7.49177833125318,-21.0334222430698));
#67382=CARTESIAN_POINT('Ctrl Pts',(3.06420086715347,-7.31095925291493,-21.0166415176531));
#67383=CARTESIAN_POINT('Ctrl Pts',(3.87841461823988,-6.90685290355965,-20.9854044606381));
#67384=CARTESIAN_POINT('Ctrl Pts',(4.22554153965593,-6.70010797695943,-20.9711697654637));
#67385=CARTESIAN_POINT('Ctrl Pts',(4.57651302288907,-6.45291560692468,-20.9541510148781));
#67386=CARTESIAN_POINT('Ctrl Pts',(4.59760628541024,-6.43790398334244,-20.9531174201609));
#67387=CARTESIAN_POINT('Ctrl Pts',(4.62494905240061,-6.4182418100038,-20.95176297662));
#67388=CARTESIAN_POINT('Ctrl Pts',(4.6312660745367,-6.41368507294932,-20.9514490390346));
#67389=CARTESIAN_POINT('Ctrl Pts',(4.64102126382055,-6.40662631265038,-20.9509626702569));
#67390=CARTESIAN_POINT('Ctrl Pts',(4.64446417628442,-6.40413082285546,-20.9507907135492));
#67391=CARTESIAN_POINT('Ctrl Pts',(4.65132699056783,-6.39914807681759,-20.9504473496905));
#67392=CARTESIAN_POINT('Ctrl Pts',(4.65474691372872,-6.39666085166512,-20.9502759447799));
#67393=CARTESIAN_POINT('Ctrl Pts',(4.66233743626961,-6.3911311425309,-20.9498948532737));
#67394=CARTESIAN_POINT('Ctrl Pts',(4.66650705184479,-6.38808731824389,-20.9496850706653));
#67395=CARTESIAN_POINT('Ctrl Pts',(4.67856669156447,-6.37926565904119,-20.9490770506118));
#67396=CARTESIAN_POINT('Ctrl Pts',(4.68644896100156,-6.3734772903279,-20.9486780649796));
#67397=CARTESIAN_POINT('Ctrl Pts',(4.74016475745324,-6.33387740696146,-20.945948396311));
#67398=CARTESIAN_POINT('Ctrl Pts',(4.78564167308849,-6.29958716131757,-20.943584264623));
#67399=CARTESIAN_POINT('Ctrl Pts',(4.92270870249896,-6.1938959013837,-20.936306083309));
#67400=CARTESIAN_POINT('Ctrl Pts',(5.01309782457362,-6.12096850106347,-20.9312958938204));
#67401=CARTESIAN_POINT('Ctrl Pts',(5.26204440718154,-5.91090071255158,-20.9169727484844));
#67402=CARTESIAN_POINT('Ctrl Pts',(5.4168008110311,-5.76941240464089,-20.9074499974814));
#67403=CARTESIAN_POINT('Ctrl Pts',(6.0566700257703,-5.13594023590603,-20.8659544035823));
#67404=CARTESIAN_POINT('Ctrl Pts',(6.48190002103106,-4.58762806025694,-20.8331182224442));
#67405=CARTESIAN_POINT('Ctrl Pts',(6.96337518330853,-3.76360342082201,-20.7915312667113));
#67406=CARTESIAN_POINT('Ctrl Pts',(7.08482737137376,-3.52966619513001,-20.7804318718218));
#67407=CARTESIAN_POINT('Ctrl Pts',(7.20465465993677,-3.26764157597415,-20.7687419920021));
#67408=CARTESIAN_POINT('Ctrl Pts',(7.21481486307336,-3.24514664443682,-20.7677441563533));
#67409=CARTESIAN_POINT('Ctrl Pts',(7.22894556321345,-3.21346653280501,-20.7663468681306));
#67410=CARTESIAN_POINT('Ctrl Pts',(7.23300411495814,-3.20432092451304,-20.7659444221245));
#67411=CARTESIAN_POINT('Ctrl Pts',(7.24002024894259,-3.18842940155423,-20.7652467366101));
#67412=CARTESIAN_POINT('Ctrl Pts',(7.24298577669856,-3.18168701992172,-20.764951227853));
#67413=CARTESIAN_POINT('Ctrl Pts',(7.24913959588187,-3.16764259412185,-20.7643367223005));
#67414=CARTESIAN_POINT('Ctrl Pts',(7.25232628191619,-3.16033985289428,-20.7640177800442));
#67415=CARTESIAN_POINT('Ctrl Pts',(7.25980912798476,-3.14312093502805,-20.7632671278884));
#67416=CARTESIAN_POINT('Ctrl Pts',(7.26409601737321,-3.13320073384158,-20.7628357312266));
#67417=CARTESIAN_POINT('Ctrl Pts',(7.27806551724902,-3.10069143010521,-20.7614254943853));
#67418=CARTESIAN_POINT('Ctrl Pts',(7.28766323495301,-3.07806588716903,-20.7604495105374));
#67419=CARTESIAN_POINT('Ctrl Pts',(7.41945368213048,-2.76331276813066,-20.7469474682724));
#67420=CARTESIAN_POINT('Ctrl Pts',(7.52411015130992,-2.46413886800956,-20.7350279249475));
#67421=CARTESIAN_POINT('Ctrl Pts',(7.83730908795459,-1.36034373403431,-20.6933708981584));
#67422=CARTESIAN_POINT('Ctrl Pts',(7.93675504794735,-0.530610222401086,
-20.6668026261471));
#67423=CARTESIAN_POINT('Ctrl Pts',(7.90099305826384,0.414021654672896,-20.6307363749247));
#67424=CARTESIAN_POINT('Ctrl Pts',(7.89415216561908,0.528642865584702,-20.6262464721065));
#67425=CARTESIAN_POINT('Ctrl Pts',(7.8832934657749,0.661783695376,-20.6209142428322));
#67426=CARTESIAN_POINT('Ctrl Pts',(7.88170061581656,0.680491677098419,-20.6201623780103));
#67427=CARTESIAN_POINT('Ctrl Pts',(7.87921999114664,0.708448771278402,-20.6190350219986));
#67428=CARTESIAN_POINT('Ctrl Pts',(7.87838249044857,0.717702350405974,-20.6186612575323));
#67429=CARTESIAN_POINT('Ctrl Pts',(7.87688183353025,0.73396398629768,-20.6180033610302));
#67430=CARTESIAN_POINT('Ctrl Pts',(7.87622562111443,0.740972683389345,-20.6177194618003));
#67431=CARTESIAN_POINT('Ctrl Pts',(7.87481258675461,0.755850661115741,-20.6171160741727));
#67432=CARTESIAN_POINT('Ctrl Pts',(7.87405332207465,0.763719699270015,-20.6167965057939));
#67433=CARTESIAN_POINT('Ctrl Pts',(7.87205028162581,0.784158731005746,-20.6159653505631));
#67434=CARTESIAN_POINT('Ctrl Pts',(7.87078819566997,0.796726884704747,-20.6154531757187));
#67435=CARTESIAN_POINT('Ctrl Pts',(7.86795676486664,0.824259512673034,-20.6143288443649));
#67436=CARTESIAN_POINT('Ctrl Pts',(7.86637481784451,0.839222628415784,-20.613716298241));
#67437=CARTESIAN_POINT('Ctrl Pts',(7.86160515415308,0.88313862473828,-20.6119142148914));
#67438=CARTESIAN_POINT('Ctrl Pts',(7.85830022453001,0.912078390124585,-20.6107211993675));
#67439=CARTESIAN_POINT('Ctrl Pts',(7.81817691669445,1.24700113475295,-20.5968546234686));
#67440=CARTESIAN_POINT('Ctrl Pts',(7.76366911572295,1.55059080879836,-20.5837208832194));
#67441=CARTESIAN_POINT('Ctrl Pts',(7.56325130360046,2.38375512400206,-20.5469421744943));
#67442=CARTESIAN_POINT('Ctrl Pts',(7.37973385359114,2.90252132761531,-20.5233054107278));
#67443=CARTESIAN_POINT('Ctrl Pts',(6.98089664857006,3.74101422816054,-20.4843757783525));
#67444=CARTESIAN_POINT('Ctrl Pts',(6.79331301614788,4.07173329052805,-20.4687272326319));
#67445=CARTESIAN_POINT('Ctrl Pts',(6.50511686073495,4.50410307119251,-20.4474658234096));
#67446=CARTESIAN_POINT('Ctrl Pts',(6.42445548124228,4.61842639602404,-20.4417706248743));
#67447=CARTESIAN_POINT('Ctrl Pts',(6.31690899550406,4.76258108688293,-20.4344960518572));
#67448=CARTESIAN_POINT('Ctrl Pts',(6.29277115696986,4.79442896003501,-20.432882816315));
#67449=CARTESIAN_POINT('Ctrl Pts',(6.25367334350229,4.84521133733519,-20.4303005970997));
#67450=CARTESIAN_POINT('Ctrl Pts',(6.23886629392961,4.86426259177226,-20.4293296081516));
#67451=CARTESIAN_POINT('Ctrl Pts',(6.21188285561536,4.8986545060229,-20.4275726149645));
#67452=CARTESIAN_POINT('Ctrl Pts',(6.19973622522395,4.91401824593606,-20.426786212725));
#67453=CARTESIAN_POINT('Ctrl Pts',(6.17084754829864,4.9502806562434,-20.4249264894265));
#67454=CARTESIAN_POINT('Ctrl Pts',(6.15405618274825,4.97113976326378,-20.4238538680703));
#67455=CARTESIAN_POINT('Ctrl Pts',(6.10412495373399,5.03252622680137,-20.420688647242));
#67456=CARTESIAN_POINT('Ctrl Pts',(6.07068824774709,5.07281045585719,-20.4186003510109));
#67457=CARTESIAN_POINT('Ctrl Pts',(5.99418852521581,5.16313694408908,-20.4138916384752));
#67458=CARTESIAN_POINT('Ctrl Pts',(5.95089391630132,5.21297811920387,-20.4112747994626));
#67459=CARTESIAN_POINT('Ctrl Pts',(5.80721161052512,5.3742636968294,-20.4027417403601));
#67460=CARTESIAN_POINT('Ctrl Pts',(5.7042772129205,5.48339670637859,-20.3968647903666));
#67461=CARTESIAN_POINT('Ctrl Pts',(5.37641096625898,5.81177695730301,-20.3787971286387));
#67462=CARTESIAN_POINT('Ctrl Pts',(5.14148329493697,6.02060615998056,-20.3667574363342));
#67463=CARTESIAN_POINT('Ctrl Pts',(4.80989059983049,6.28176288770404,-20.3505335275156));
#67464=CARTESIAN_POINT('Ctrl Pts',(4.72365773778135,6.34686142649266,-20.3463776105699));
#67465=CARTESIAN_POINT('Ctrl Pts',(4.4359436146328,6.55494893129596,-20.3326651142168));
#67466=CARTESIAN_POINT('Ctrl Pts',(4.22910167332117,6.69026482467019,-20.3230504807747));
#67467=CARTESIAN_POINT('Ctrl Pts',(3.99396935792509,6.8288212806999,-20.3121408109388));
#67468=CARTESIAN_POINT('Ctrl Pts',(3.97159925208184,6.84185579288376,-20.3111030356709));
#67469=CARTESIAN_POINT('Ctrl Pts',(3.9378045910166,6.86132552181955,-20.3095350987322));
#67470=CARTESIAN_POINT('Ctrl Pts',(3.92642735072553,6.86784254124089,-20.3090072220809));
#67471=CARTESIAN_POINT('Ctrl Pts',(3.9060239274336,6.87946259459299,-20.3080605583273));
#67472=CARTESIAN_POINT('Ctrl Pts',(3.89700380304837,6.88457623026628,-20.3076420510427));
#67473=CARTESIAN_POINT('Ctrl Pts',(3.87723426966975,6.89573255584849,-20.3067248306139));
#67474=CARTESIAN_POINT('Ctrl Pts',(3.86648073822278,6.90176787232023,-20.3062259314803));
#67475=CARTESIAN_POINT('Ctrl Pts',(3.83766500293938,6.91785194590535,-20.3048891500842));
#67476=CARTESIAN_POINT('Ctrl Pts',(3.8195774915809,6.9278550793475,-20.3040501582207));
#67477=CARTESIAN_POINT('Ctrl Pts',(3.73228232334493,6.97568708976241,-20.3000018330512));
#67478=CARTESIAN_POINT('Ctrl Pts',(3.6625514012252,7.01255008414081,-20.2967707193975));
#67479=CARTESIAN_POINT('Ctrl Pts',(3.46027507998527,7.11564259659308,-20.2874178585725));
#67480=CARTESIAN_POINT('Ctrl Pts',(3.3264059547636,7.17919880802401,-20.2812526839266));
#67481=CARTESIAN_POINT('Ctrl Pts',(2.63290182147522,7.48488591026565,-20.2495636306426));
#67482=CARTESIAN_POINT('Ctrl Pts',(2.04837838062254,7.66549970638557,-20.2238251329256));
#67483=CARTESIAN_POINT('Ctrl Pts',(1.34271351908952,7.79696822633186,-20.1944793584911));
#67484=CARTESIAN_POINT('Ctrl Pts',(1.23610840741245,7.81457801328586,-20.1900859008267));
#67485=CARTESIAN_POINT('Ctrl Pts',(1.08859358208747,7.83585133405766,-20.1840562606589));
#67486=CARTESIAN_POINT('Ctrl Pts',(1.04796696585306,7.84138810265809,-20.1824008193943));
#67487=CARTESIAN_POINT('Ctrl Pts',(0.982714543400365,7.84976480429343,-20.1797497791156));
#67488=CARTESIAN_POINT('Ctrl Pts',(0.958115330509714,7.85280525510726,-20.1787521599428));
#67489=CARTESIAN_POINT('Ctrl Pts',(0.907099737642164,7.85886747558489,-20.1766867855437));
#67490=CARTESIAN_POINT('Ctrl Pts',(0.88068158595198,7.86187177983823,-20.1756192172437));
#67491=CARTESIAN_POINT('Ctrl Pts',(0.818502052832379,7.86862556553225,-20.1731109515746));
#67492=CARTESIAN_POINT('Ctrl Pts',(0.782729220383721,7.87226453328173,-20.1716713548421));
#67493=CARTESIAN_POINT('Ctrl Pts',(0.663198480906921,7.88360090730199,-20.1668718152988));
#67494=CARTESIAN_POINT('Ctrl Pts',(0.579342472025407,7.89020645769767,-20.1635223036657));
#67495=CARTESIAN_POINT('Ctrl Pts',(0.215600419622202,7.91302922943297,-20.1490539038602));
#67496=CARTESIAN_POINT('Ctrl Pts',(-0.0649401045239018,7.91569984903088,
-20.1380206206928));
#67497=CARTESIAN_POINT('Ctrl Pts',(-0.639643343900182,7.89061083529653,
-20.1156667564884));
#67498=CARTESIAN_POINT('Ctrl Pts',(-0.933311067778316,7.86128623828794,
-20.1044037217539));
#67499=CARTESIAN_POINT('Ctrl Pts',(-1.82792646956006,7.72110540766969,-20.0703143704002));
#67500=CARTESIAN_POINT('Ctrl Pts',(-2.41817208514105,7.55705879066635,-20.0483120900414));
#67501=CARTESIAN_POINT('Ctrl Pts',(-3.08885099284436,7.28394307118575,-20.0203255745988));
#67502=CARTESIAN_POINT('Ctrl Pts',(-3.19312895352406,7.23883646009229,-20.0158755225567));
#67503=CARTESIAN_POINT('Ctrl Pts',(-3.31225883538221,7.18423043099901,-20.0106431194425));
#67504=CARTESIAN_POINT('Ctrl Pts',(-3.32809696755596,7.17690713657648,-20.0099444070972));
#67505=CARTESIAN_POINT('Ctrl Pts',(-3.3516006379828,7.16594488976823,-20.0089027850107));
#67506=CARTESIAN_POINT('Ctrl Pts',(-3.35928481703079,7.16234588086196,-20.0085614869611));
#67507=CARTESIAN_POINT('Ctrl Pts',(-3.37295154594217,7.15591801672306,-20.0079531021217));
#67508=CARTESIAN_POINT('Ctrl Pts',(-3.3789363717086,7.15309400112611,-20.007686215285));
#67509=CARTESIAN_POINT('Ctrl Pts',(-3.39138667930302,7.14720005445859,-20.0071300202941));
#67510=CARTESIAN_POINT('Ctrl Pts',(-3.39785155057423,7.14412885289988,-20.0068406588782));
#67511=CARTESIAN_POINT('Ctrl Pts',(-3.41455121985151,7.13616771311956,-20.0060917422371));
#67512=CARTESIAN_POINT('Ctrl Pts',(-3.42477966353301,7.13126453844267,-20.0056316202277));
#67513=CARTESIAN_POINT('Ctrl Pts',(-3.4470461926375,7.1205317530212,-20.0046268153225));
#67514=CARTESIAN_POINT('Ctrl Pts',(-3.45908009589968,7.11469358350185,-20.0040817552548));
#67515=CARTESIAN_POINT('Ctrl Pts',(-3.49381540859763,7.09773301505479,-20.0025024848242));
#67516=CARTESIAN_POINT('Ctrl Pts',(-3.51647824851522,7.08653235149519,-20.0014646998304));
#67517=CARTESIAN_POINT('Ctrl Pts',(-3.59182246232518,7.04884453572608,-19.9979886251268));
#67518=CARTESIAN_POINT('Ctrl Pts',(-3.64425795769325,7.02187877165575,-19.9955260730928));
#67519=CARTESIAN_POINT('Ctrl Pts',(-3.79644369257797,6.94145110721241,-19.9882509253494));
#67520=CARTESIAN_POINT('Ctrl Pts',(-3.89534975611109,6.88643425048212,-19.9833636578857));
#67521=CARTESIAN_POINT('Ctrl Pts',(-4.15843189702593,6.73261256767019,-19.9699904613795));
#67522=CARTESIAN_POINT('Ctrl Pts',(-4.32025233356039,6.62993530937215,-19.9613630088308));
#67523=CARTESIAN_POINT('Ctrl Pts',(-5.20800532617891,6.02033268589059,-19.9122868539698));
#67524=CARTESIAN_POINT('Ctrl Pts',(-5.84873270579262,5.40006087464299,-19.8708966477332));
#67525=CARTESIAN_POINT('Ctrl Pts',(-6.40518822040254,4.6433137385199,-19.832356961059));
#67526=CARTESIAN_POINT('Ctrl Pts',(-6.43652691076983,4.59977391635259,-19.8301721881629));
#67527=CARTESIAN_POINT('Ctrl Pts',(-6.4764374973016,4.54311825549699,-19.8273706722278));
#67528=CARTESIAN_POINT('Ctrl Pts',(-6.48541629094354,4.53029156639412,-19.8267391252944));
#67529=CARTESIAN_POINT('Ctrl Pts',(-6.4996235356568,4.50986695546707,-19.8257377576288));
#67530=CARTESIAN_POINT('Ctrl Pts',(-6.50487685933413,4.5022864310135,-19.8253670355673));
#67531=CARTESIAN_POINT('Ctrl Pts',(-6.51468935099316,4.48807402203607,-19.8246737230017));
#67532=CARTESIAN_POINT('Ctrl Pts',(-6.51925167618946,4.48144433750892,-19.8243510185478));
#67533=CARTESIAN_POINT('Ctrl Pts',(-6.52950041363925,4.46650274497195,-19.8236253104933));
#67534=CARTESIAN_POINT('Ctrl Pts',(-6.53518109112651,4.45818691057923,-19.8232225140185));
#67535=CARTESIAN_POINT('Ctrl Pts',(-6.55185361480285,4.43367998177417,-19.8220386899065));
#67536=CARTESIAN_POINT('Ctrl Pts',(-6.56280131433924,4.41745887199966,-19.8212592504074));
#67537=CARTESIAN_POINT('Ctrl Pts',(-6.6459007821758,4.29334036322256,-19.8153264868713));
#67538=CARTESIAN_POINT('Ctrl Pts',(-6.71544918506046,4.18371997009637,-19.8102668042333));
#67539=CARTESIAN_POINT('Ctrl Pts',(-6.94681541375455,3.79840048862551,-19.7930562095523));
#67540=CARTESIAN_POINT('Ctrl Pts',(-7.09460717086365,3.51463503813587,-19.7813853119961));
#67541=CARTESIAN_POINT('Ctrl Pts',(-7.50517421057323,2.59420017488285,-19.7456294864979));
#67542=CARTESIAN_POINT('Ctrl Pts',(-7.70228771360618,1.93187450202906,-19.7230618850797));
#67543=CARTESIAN_POINT('Ctrl Pts',(-7.81624069148619,1.22119047998754,-19.6963157695708));
#67544=CARTESIAN_POINT('Ctrl Pts',(-7.82106856198937,1.18987867115268,-19.695131962656));
#67545=CARTESIAN_POINT('Ctrl Pts',(-7.84670891033747,1.01668304255297,-19.6885506142617));
#67546=CARTESIAN_POINT('Ctrl Pts',(-7.86384841622122,0.874284321794345,
-19.6830143443933));
#67547=CARTESIAN_POINT('Ctrl Pts',(-7.87855451215898,0.715922114166429,
-19.6766601378556));
#67548=CARTESIAN_POINT('Ctrl Pts',(-7.87995466513111,0.700342876605951,
-19.6760330519743));
#67549=CARTESIAN_POINT('Ctrl Pts',(-7.88193677708997,0.677529564703679,
-19.6751119937283));
#67550=CARTESIAN_POINT('Ctrl Pts',(-7.88255500705428,0.670298612067288,
-19.6748196429958));
#67551=CARTESIAN_POINT('Ctrl Pts',(-7.88363349613805,0.657476517706844,
-19.6743005247235));
#67552=CARTESIAN_POINT('Ctrl Pts',(-7.884097760239,0.651885710478061,-19.6740739330226));
#67553=CARTESIAN_POINT('Ctrl Pts',(-7.88498146399501,0.64110484721572,-19.6736365332979));
#67554=CARTESIAN_POINT('Ctrl Pts',(-7.88540172745599,0.635914859959239,
-19.673425761003));
#67555=CARTESIAN_POINT('Ctrl Pts',(-7.88629143351192,0.624791050197756,
-19.6729735747339));
#67556=CARTESIAN_POINT('Ctrl Pts',(-7.88675930346327,0.618857107622825,
-19.6727320938206));
#67557=CARTESIAN_POINT('Ctrl Pts',(-7.88787011912322,0.604562892913924,
-19.6721497652962));
#67558=CARTESIAN_POINT('Ctrl Pts',(-7.8885064702552,0.596202126489903,-19.6718086410937));
#67559=CARTESIAN_POINT('Ctrl Pts',(-7.89018885139518,0.573623679986948,
-19.6708860596147));
#67560=CARTESIAN_POINT('Ctrl Pts',(-7.89120974098865,0.559404198269232,
-19.6703035712985));
#67561=CARTESIAN_POINT('Ctrl Pts',(-7.90459781270049,0.365595129320806,
-19.6623451071192));
#67562=CARTESIAN_POINT('Ctrl Pts',(-7.91086946006672,0.185645462909779,
-19.6547319091537));
#67563=CARTESIAN_POINT('Ctrl Pts',(-7.91099798332788,0.00564869739125604,
-19.6469874507044));
#67564=CARTESIAN_POINT('',(-7.911,-6.46926956449079E-12,-17.6423315082367));
#67565=CARTESIAN_POINT('Ctrl Pts',(-7.91099783789749,0.00584882734057925,
-19.6423315082367));
#67566=CARTESIAN_POINT('Ctrl Pts',(-7.91113802130119,-0.183760224007458,
-19.6346827876976));
#67567=CARTESIAN_POINT('Ctrl Pts',(-7.90445733796416,-0.373649153007014,
-19.6270340671585));
#67568=CARTESIAN_POINT('Ctrl Pts',(-7.89092201232192,-0.563267960613193,
-19.6193853466194));
#67569=CARTESIAN_POINT('Ctrl Pts',(-7.87739780900031,-0.752730953632383,
-19.6117429112282));
#67570=CARTESIAN_POINT('Ctrl Pts',(-7.85703019670372,-0.941923902422047,
-19.6041004758369));
#67571=CARTESIAN_POINT('Ctrl Pts',(-7.82983741969774,-1.13029508585197,
-19.5964580404456));
#67572=CARTESIAN_POINT('Ctrl Pts',(-7.80266318855097,-1.31853779746571,
-19.5888208173035));
#67573=CARTESIAN_POINT('Ctrl Pts',(-7.76867311292221,-1.50595949675737,
-19.5811835941614));
#67574=CARTESIAN_POINT('Ctrl Pts',(-7.72793739081847,-1.69201202229472,
-19.5735463710194));
#67575=CARTESIAN_POINT('Ctrl Pts',(-7.68721797603965,-1.87799006728208,
-19.5659122052106));
#67576=CARTESIAN_POINT('Ctrl Pts',(-7.63975836785712,-2.06259967049416,
-19.5582780394018));
#67577=CARTESIAN_POINT('Ctrl Pts',(-7.58568014811566,-2.24530124715681,
-19.550643873593));
#67578=CARTESIAN_POINT('Ctrl Pts',(-7.53160837032525,-2.42798105988905,
-19.5430106171877));
#67579=CARTESIAN_POINT('Ctrl Pts',(-7.47091965012036,-2.6087529442751,-19.5353773607825));
#67580=CARTESIAN_POINT('Ctrl Pts',(-7.40378590223481,-2.78709083344427,
-19.5277441043772));
#67581=CARTESIAN_POINT('Ctrl Pts',(-7.36710136042364,-2.88454172748486,
-19.5235729904058));
#67582=CARTESIAN_POINT('Ctrl Pts',(-7.32849322939946,-2.98126610392669,
-19.5194018764345));
#67583=CARTESIAN_POINT('Ctrl Pts',(-7.28799573871105,-3.07718038348901,
-19.5152307624631));
#67584=CARTESIAN_POINT('Ctrl Pts',(-7.20528000829565,-3.27308436559757,
-19.5067113027899));
#67585=CARTESIAN_POINT('Ctrl Pts',(-7.11473925117085,-3.46546708114613,
-19.4981918431167));
#67586=CARTESIAN_POINT('Ctrl Pts',(-7.01670438443082,-3.65373515481204,
-19.4896723834434));
#67587=CARTESIAN_POINT('Ctrl Pts',(-6.91849296434608,-3.84234228497093,
-19.4811375808708));
#67588=CARTESIAN_POINT('Ctrl Pts',(-6.81276057591704,-4.02681974194158,
-19.4726027782982));
#67589=CARTESIAN_POINT('Ctrl Pts',(-6.69988251509191,-4.20660139352016,
-19.4640679757255));
#67590=CARTESIAN_POINT('Ctrl Pts',(-6.58129166582463,-4.39548184192196,
-19.4551012245427));
#67591=CARTESIAN_POINT('Ctrl Pts',(-6.45481338712476,-4.57917861971122,
-19.4461344733599));
#67592=CARTESIAN_POINT('Ctrl Pts',(-6.32093037625521,-4.75707475015205,
-19.4371677221771));
#67593=CARTESIAN_POINT('Ctrl Pts',(-6.19296462642121,-4.9271083606645,-19.4285972767469));
#67594=CARTESIAN_POINT('Ctrl Pts',(-6.05823472329184,-5.09184284991683,
-19.4200268313167));
#67595=CARTESIAN_POINT('Ctrl Pts',(-5.91720073374702,-5.2507767498289,-19.4114563858865));
#67596=CARTESIAN_POINT('Ctrl Pts',(-5.77599050341171,-5.40990925885814,
-19.4028752305411));
#67597=CARTESIAN_POINT('Ctrl Pts',(-5.62846061755716,-5.56322651463609,
-19.3942940751957));
#67598=CARTESIAN_POINT('Ctrl Pts',(-5.47510771234711,-5.71026413909175,
-19.3857129198502));
#67599=CARTESIAN_POINT('Ctrl Pts',(-5.3214996561415,-5.8575464070787,-19.3771174870425));
#67600=CARTESIAN_POINT('Ctrl Pts',(-5.16204939113485,-5.99852798302639,
-19.3685220542347));
#67601=CARTESIAN_POINT('Ctrl Pts',(-4.99728797132674,-6.13278353862527,
-19.3599266214269));
#67602=CARTESIAN_POINT('Ctrl Pts',(-4.97518249240011,-6.15079614957831,
-19.3587734014618));
#67603=CARTESIAN_POINT('Ctrl Pts',(-4.95298145337977,-6.16868775034689,
-19.3576201814967));
#67604=CARTESIAN_POINT('Ctrl Pts',(-4.93068617731446,-6.18645737242568,
-19.3564669615317));
#67605=CARTESIAN_POINT('Ctrl Pts',(-4.77778048606164,-6.30832517703603,
-19.3485579365252));
#67606=CARTESIAN_POINT('Ctrl Pts',(-4.6201590200985,-6.42467610326622,-19.3406489115187));
#67607=CARTESIAN_POINT('Ctrl Pts',(-4.45825686135297,-6.53512561150887,
-19.3327398865122));
#67608=CARTESIAN_POINT('Ctrl Pts',(-4.29651973706778,-6.64546253338993,
-19.3248389235457));
#67609=CARTESIAN_POINT('Ctrl Pts',(-4.13051089421535,-6.74990982709944,
-19.3169379605792));
#67610=CARTESIAN_POINT('Ctrl Pts',(-3.96069883546253,-6.84812278911278,
-19.3090369976126));
#67611=CARTESIAN_POINT('Ctrl Pts',(-3.79102837255323,-6.94625385737073,
-19.3011426227737));
#67612=CARTESIAN_POINT('Ctrl Pts',(-3.61756130816164,-7.03816077831389,
-19.2932482479349));
#67613=CARTESIAN_POINT('Ctrl Pts',(-3.44079574015724,-7.12354165247286,
-19.285353873096));
#67614=CARTESIAN_POINT('Ctrl Pts',(-3.26414478364301,-7.20886716726898,
-19.2774646168222));
#67615=CARTESIAN_POINT('Ctrl Pts',(-3.08419989400257,-7.28767491644094,
-19.2695753605483));
#67616=CARTESIAN_POINT('Ctrl Pts',(-2.90148467407429,-7.35970839681247,
-19.2616861042745));
#67617=CARTESIAN_POINT('Ctrl Pts',(-2.7188540441519,-7.43170852849783,-19.253800500418));
#67618=CARTESIAN_POINT('Ctrl Pts',(-2.53345595980279,-7.49694051474591,
-19.2459148965616));
#67619=CARTESIAN_POINT('Ctrl Pts',(-2.34583521100266,-7.55519544173545,
-19.2380292927051));
#67620=CARTESIAN_POINT('Ctrl Pts',(-2.14846392638771,-7.61647784172909,
-19.2297338788286));
#67621=CARTESIAN_POINT('Ctrl Pts',(-1.94863317336111,-7.67003852780308,
-19.221438464952));
#67622=CARTESIAN_POINT('Ctrl Pts',(-1.74699756297276,-7.71569313250386,
-19.2131430510755));
#67623=CARTESIAN_POINT('Ctrl Pts',(-1.55535481583135,-7.75908513973741,
-19.2052587497812));
#67624=CARTESIAN_POINT('Ctrl Pts',(-1.36208214175197,-7.79533564831999,
-19.1973744484868));
#67625=CARTESIAN_POINT('Ctrl Pts',(-1.16775388967623,-7.82433842910351,
-19.1894901471925));
#67626=CARTESIAN_POINT('Ctrl Pts',(-0.973400300964404,-7.8533449912873,
-19.1816048179381));
#67627=CARTESIAN_POINT('Ctrl Pts',(-0.777991201150984,-7.87510189115162,
-19.1737194886838));
#67628=CARTESIAN_POINT('Ctrl Pts',(-0.582108008285773,-7.88955456706458,
-19.1658341594294));
#67629=CARTESIAN_POINT('Ctrl Pts',(-0.386166365426575,-7.90401155554162,
-19.1579464772552));
#67630=CARTESIAN_POINT('Ctrl Pts',(-0.189750691524313,-7.9111599514527,
-19.1500587950811));
#67631=CARTESIAN_POINT('Ctrl Pts',(0.00655538566710729,-7.91099728396608,
-19.1421711129069));
#67632=CARTESIAN_POINT('Ctrl Pts',(0.202953021448065,-7.91083454061016,
-19.1342797518601));
#67633=CARTESIAN_POINT('Ctrl Pts',(0.399240614178055,-7.90335393913915,
-19.1263883908132));
#67634=CARTESIAN_POINT('Ctrl Pts',(0.594837203384454,-7.88860505422028,
-19.1184970297664));
#67635=CARTESIAN_POINT('Ctrl Pts',(0.79065918549798,-7.87383917363671,-19.1105965752236));
#67636=CARTESIAN_POINT('Ctrl Pts',(0.985788229800109,-7.85178830674623,
-19.1026961206807));
#67637=CARTESIAN_POINT('Ctrl Pts',(1.17965000407716,-7.82255373058445,-19.0947956661379));
#67638=CARTESIAN_POINT('Ctrl Pts',(1.37364143181113,-7.79329960253384,-19.0868899278239));
#67639=CARTESIAN_POINT('Ctrl Pts',(1.56636356226909,-7.75685225133657,-19.07898418951));
#67640=CARTESIAN_POINT('Ctrl Pts',(1.75725460729995,-7.7133635493942,-19.071078451196));
#67641=CARTESIAN_POINT('Ctrl Pts',(1.94840298754163,-7.66981622147343,-19.0631620553636));
#67642=CARTESIAN_POINT('Ctrl Pts',(2.13771502059222,-7.61920867337019,-19.0552456595312));
#67643=CARTESIAN_POINT('Ctrl Pts',(2.32464528458301,-7.5617422133306,-19.0473292636988));
#67644=CARTESIAN_POINT('Ctrl Pts',(2.3906823637629,-7.54144096787786,-19.0445326290221));
#67645=CARTESIAN_POINT('Ctrl Pts',(2.45642238919231,-7.52028416092685,-19.0417359943454));
#67646=CARTESIAN_POINT('Ctrl Pts',(2.5218419829114,-7.49828207079632,-19.0389393596686));
#67647=CARTESIAN_POINT('Ctrl Pts',(2.70340762271942,-7.43721743641755,-19.0311775755376));
#67648=CARTESIAN_POINT('Ctrl Pts',(2.88307273704098,-7.36944680384386,-19.0234157914066));
#67649=CARTESIAN_POINT('Ctrl Pts',(3.06029198926213,-7.29510342219067,-19.0156540072756));
#67650=CARTESIAN_POINT('Ctrl Pts',(3.23729843544195,-7.22084931255816,-19.0079015435459));
#67651=CARTESIAN_POINT('Ctrl Pts',(3.41186453889488,-7.14003830056088,-19.0001490798162));
#67652=CARTESIAN_POINT('Ctrl Pts',(3.58345834686008,-7.05285383914333,-18.9923966160865));
#67653=CARTESIAN_POINT('Ctrl Pts',(3.75488090624852,-6.96575638677996,-18.9846518892232));
#67654=CARTESIAN_POINT('Ctrl Pts',(3.92333675815459,-6.8722983081147,-18.97690716236));
#67655=CARTESIAN_POINT('Ctrl Pts',(4.08831214060738,-6.77271177896729,-18.9691624354968));
#67656=CARTESIAN_POINT('Ctrl Pts',(4.25315629166039,-6.67320446696989,-18.9614238692578));
#67657=CARTESIAN_POINT('Ctrl Pts',(4.41452517995679,-6.56757859470346,-18.9536853030189));
#67658=CARTESIAN_POINT('Ctrl Pts',(4.57192787432426,-6.45611311177065,-18.94594673678));
#67659=CARTESIAN_POINT('Ctrl Pts',(4.72923720705595,-6.34471374333391,-18.9382127605844));
#67660=CARTESIAN_POINT('Ctrl Pts',(4.88258473843477,-6.22748186813724,-18.9304787843889));
#67661=CARTESIAN_POINT('Ctrl Pts',(5.03150679496644,-6.10474081122259,-18.9227448081934));
#67662=CARTESIAN_POINT('Ctrl Pts',(5.18037062940206,-5.9820477407632,-18.9150138556488));
#67663=CARTESIAN_POINT('Ctrl Pts',(5.32481215843983,-5.85385000631522,-18.9072829031041));
#67664=CARTESIAN_POINT('Ctrl Pts',(5.4643991360204,-5.72051248423247,-18.8995519505595));
#67665=CARTESIAN_POINT('Ctrl Pts',(5.60398630974189,-5.58717477479024,-18.8918209871516));
#67666=CARTESIAN_POINT('Ctrl Pts',(5.73871865104356,-5.44869750295523,-18.8840900237438));
#67667=CARTESIAN_POINT('Ctrl Pts',(5.86819898947908,-5.3054841079657,-18.876359060336));
#67668=CARTESIAN_POINT('Ctrl Pts',(5.99768603071206,-5.16226329926077,-18.8686276967201));
#67669=CARTESIAN_POINT('Ctrl Pts',(6.12192028602957,-5.01430614496696,-18.8608963331042));
#67670=CARTESIAN_POINT('Ctrl Pts',(6.24054340776541,-4.86205090222179,-18.8531649694882));
#67671=CARTESIAN_POINT('Ctrl Pts',(6.35919439181006,-4.70975989762404,-18.8454317899224));
#67672=CARTESIAN_POINT('Ctrl Pts',(6.47223139693797,-4.55316907739557,-18.8376986103567));
#67673=CARTESIAN_POINT('Ctrl Pts',(6.57933809314507,-4.39274757482036,-18.8299654307909));
#67674=CARTESIAN_POINT('Ctrl Pts',(6.68648956562127,-4.23225900756459,-18.8222290183467));
#67675=CARTESIAN_POINT('Ctrl Pts',(6.78770559325239,-4.06793686735429,-18.8144926059024));
#67676=CARTESIAN_POINT('Ctrl Pts',(6.88271464792874,-3.90027692288474,-18.8067561934582));
#67677=CARTESIAN_POINT('Ctrl Pts',(6.97783676124531,-3.73241746684855,-18.799010574857));
#67678=CARTESIAN_POINT('Ctrl Pts',(7.06673697369494,-3.56121258662182,-18.7912649562558));
#67679=CARTESIAN_POINT('Ctrl Pts',(7.14919052248813,-3.38718111018084,-18.7835193376546));
#67680=CARTESIAN_POINT('Ctrl Pts',(7.23169768157617,-3.21303648058998,-18.7757686829464));
#67681=CARTESIAN_POINT('Ctrl Pts',(7.30774968655235,-3.03606192241102,-18.7680180282382));
#67682=CARTESIAN_POINT('Ctrl Pts',(7.37717098864852,-2.85679351795727,-18.7602673735299));
#67683=CARTESIAN_POINT('Ctrl Pts',(7.44669775289354,-2.67725277589842,-18.7525049443278));
#67684=CARTESIAN_POINT('Ctrl Pts',(7.50957357984035,-2.49541156571472,-18.7447425151256));
#67685=CARTESIAN_POINT('Ctrl Pts',(7.56567325283131,-2.31181946340817,-18.7369800859235));
#67686=CARTESIAN_POINT('Ctrl Pts',(7.60317775447997,-2.18908202241193,-18.7317906432175));
#67687=CARTESIAN_POINT('Ctrl Pts',(7.63765480311116,-2.06556226457843,-18.7266012005115));
#67688=CARTESIAN_POINT('Ctrl Pts',(7.66907988485672,-1.94142595009081,-18.7214117578056));
#67689=CARTESIAN_POINT('Ctrl Pts',(7.71761344961894,-1.74970718521032,-18.713397072094));
#67690=CARTESIAN_POINT('Ctrl Pts',(7.75901339732821,-1.55593159817677,-18.7053823863825));
#67691=CARTESIAN_POINT('Ctrl Pts',(7.79310652659695,-1.36066589033168,-18.697367700671));
#67692=CARTESIAN_POINT('Ctrl Pts',(7.82716089650987,-1.16562217363877,-18.6893621265916));
#67693=CARTESIAN_POINT('Ctrl Pts',(7.85392494334617,-0.969092038447004,
-18.6813565525123));
#67694=CARTESIAN_POINT('Ctrl Pts',(7.87327554829636,-0.77165610254738,-18.673350978433));
#67695=CARTESIAN_POINT('Ctrl Pts',(7.89260743555861,-0.57441114487542,-18.6653531480826));
#67696=CARTESIAN_POINT('Ctrl Pts',(7.90454013903864,-0.376262463360862,
-18.6573553177321));
#67697=CARTESIAN_POINT('Ctrl Pts',(7.90900171680268,-0.177800010158159,
-18.6493574873816));
#67698=CARTESIAN_POINT('Ctrl Pts',(7.9134597349997,0.0205041043489301,-18.6413660379158));
#67699=CARTESIAN_POINT('Ctrl Pts',(7.9104584999826,0.21912115868565,-18.63337458845));
#67700=CARTESIAN_POINT('Ctrl Pts',(7.89997791425322,0.417456529846294,-18.6253831389842));
#67701=CARTESIAN_POINT('Ctrl Pts',(7.8895039150739,0.615667256651865,-18.6173967117646));
#67702=CARTESIAN_POINT('Ctrl Pts',(7.8715599522246,0.813596320106642,-18.609410284545));
#67703=CARTESIAN_POINT('Ctrl Pts',(7.84617800799023,1.01064913146475,-18.6014238573254));
#67704=CARTESIAN_POINT('Ctrl Pts',(7.82001934766407,1.21373198087282,-18.5931930364344));
#67705=CARTESIAN_POINT('Ctrl Pts',(7.7859602545851,1.41588373550776,-18.5849622155435));
#67706=CARTESIAN_POINT('Ctrl Pts',(7.74409353569296,1.61645795195499,-18.5767313946525));
#67707=CARTESIAN_POINT('Ctrl Pts',(7.70349725826311,1.8109457635541,-18.568750337211));
#67708=CARTESIAN_POINT('Ctrl Pts',(7.6555603371452,2.00395002689001,-18.5607692797695));
#67709=CARTESIAN_POINT('Ctrl Pts',(7.60041950030024,2.19489052561985,-18.5527882223281));
#67710=CARTESIAN_POINT('Ctrl Pts',(7.54528297267458,2.38581610247822,-18.5448077886008));
#67711=CARTESIAN_POINT('Ctrl Pts',(7.48294374411727,2.57467791485703,-18.5368273548736));
#67712=CARTESIAN_POINT('Ctrl Pts',(7.41358873430394,2.76090982804612,-18.5288469211464));
#67713=CARTESIAN_POINT('Ctrl Pts',(7.34422849772688,2.94715577612921,-18.5208658859941));
#67714=CARTESIAN_POINT('Ctrl Pts',(7.26785154308614,3.13077111664938,-18.5128848508418));
#67715=CARTESIAN_POINT('Ctrl Pts',(7.18469349463499,3.31120829730623,-18.5049038156896));
#67716=CARTESIAN_POINT('Ctrl Pts',(7.10151641325563,3.49168677580462,-18.4969209538654));
#67717=CARTESIAN_POINT('Ctrl Pts',(7.01155528492848,3.66898534109895,-18.4889380920412));
#67718=CARTESIAN_POINT('Ctrl Pts',(6.91509253864822,3.84257936572971,-18.4809552302171));
#67719=CARTESIAN_POINT('Ctrl Pts',(6.81855821179896,4.01630220650492,-18.4729664446781));
#67720=CARTESIAN_POINT('Ctrl Pts',(6.71551279225942,4.18631472288134,-18.4649776591392));
#67721=CARTESIAN_POINT('Ctrl Pts',(6.60628357838913,4.35211882672178,-18.4569888736003));
#67722=CARTESIAN_POINT('Ctrl Pts',(6.49700619189741,4.51799605402472,-18.4489965648214));
#67723=CARTESIAN_POINT('Ctrl Pts',(6.38153976407568,4.67966089379926,-18.4410042560424));
#67724=CARTESIAN_POINT('Ctrl Pts',(6.26025338279326,4.8366464190827,-18.4330119472634));
#67725=CARTESIAN_POINT('Ctrl Pts',(6.1388535141161,4.99377883536981,-18.4250121600991));
#67726=CARTESIAN_POINT('Ctrl Pts',(6.011623027214,5.14622293407631,-18.4170123729347));
#67727=CARTESIAN_POINT('Ctrl Pts',(5.8789701684774,5.29354614206326,-18.4090125857704));
#67728=CARTESIAN_POINT('Ctrl Pts',(5.85062354443516,5.3250276768698,-18.4073031091611));
#67729=CARTESIAN_POINT('Ctrl Pts',(5.82202944664807,5.35627551060089,-18.4055936325518));
#67730=CARTESIAN_POINT('Ctrl Pts',(5.79319206789574,5.38728564905091,-18.4038841559425));
#67731=CARTESIAN_POINT('Ctrl Pts',(5.65609027711756,5.53471740941624,-18.3957567770139));
#67732=CARTESIAN_POINT('Ctrl Pts',(5.51324576239915,5.67703248099569,-18.3876293980853));
#67733=CARTESIAN_POINT('Ctrl Pts',(5.36506658550671,5.81377515329578,-18.3795020191568));
#67734=CARTESIAN_POINT('Ctrl Pts',(5.21701325071332,5.95040169602036,-18.3713815424559));
#67735=CARTESIAN_POINT('Ctrl Pts',(5.06363451910478,6.08146505899225,-18.3632610657551));
#67736=CARTESIAN_POINT('Ctrl Pts',(4.90537614374601,6.20654540693674,-18.3551405890542));
#67737=CARTESIAN_POINT('Ctrl Pts',(4.74723227226892,6.33153525612987,-18.3470259877208));
#67738=CARTESIAN_POINT('Ctrl Pts',(4.5842160457718,6.45055052450131,-18.3389113863874));
#67739=CARTESIAN_POINT('Ctrl Pts',(4.41680765496922,6.56321042927966,-18.3307967850539));
#67740=CARTESIAN_POINT('Ctrl Pts',(4.24951786113322,6.67579052250915,-18.3226879323398));
#67741=CARTESIAN_POINT('Ctrl Pts',(4.07784237442878,6.78202405691186,-18.3145790796256));
#67742=CARTESIAN_POINT('Ctrl Pts',(3.90229212802461,6.88157228746143,-18.3064702269115));
#67743=CARTESIAN_POINT('Ctrl Pts',(3.72681706449238,6.98107788450851,-18.2983648469742));
#67744=CARTESIAN_POINT('Ctrl Pts',(3.54747082680692,7.07390372955717,-18.290259467037));
#67745=CARTESIAN_POINT('Ctrl Pts',(3.36479155591205,7.15975549758949,-18.2821540870997));
#67746=CARTESIAN_POINT('Ctrl Pts',(3.18216924970129,7.24558049455566,-18.2740512346545));
#67747=CARTESIAN_POINT('Ctrl Pts',(2.99621627128487,7.32443561632654,-18.2659483822093));
#67748=CARTESIAN_POINT('Ctrl Pts',(2.80749398554382,7.3960731825162,-18.2578455297641));
#67749=CARTESIAN_POINT('Ctrl Pts',(2.70870062513665,7.43357440219186,-18.2536038048464));
#67750=CARTESIAN_POINT('Ctrl Pts',(2.60914873979467,7.46909852772734,-18.2493620799287));
#67751=CARTESIAN_POINT('Ctrl Pts',(2.50892104898112,7.50261528868297,-18.2451203550111));
#67752=CARTESIAN_POINT('Ctrl Pts',(2.31306241344616,7.56811163021332,-18.2368314435541));
#67753=CARTESIAN_POINT('Ctrl Pts',(2.11470623800062,7.62591149242828,-18.2285425320972));
#67754=CARTESIAN_POINT('Ctrl Pts',(1.91447278116729,7.67585271941623,-18.2202536206403));
#67755=CARTESIAN_POINT('Ctrl Pts',(1.71412420047218,7.7258226600218,-18.2119599434888));
#67756=CARTESIAN_POINT('Ctrl Pts',(1.51189646780863,7.76792487583658,-18.2036662663373));
#67757=CARTESIAN_POINT('Ctrl Pts',(1.30842066178171,7.80204821645077,-18.1953725891858));
#67758=CARTESIAN_POINT('Ctrl Pts',(1.10481561220036,7.83619323149357,-18.1870736440649));
#67759=CARTESIAN_POINT('Ctrl Pts',(0.899961195157141,7.86234920667333,-18.178774698944));
#67760=CARTESIAN_POINT('Ctrl Pts',(0.694495091660754,7.88045668522194,-18.1704757538232));
#67761=CARTESIAN_POINT('Ctrl Pts',(0.488790603065375,7.89858517236025,-18.1621671801318));
#67762=CARTESIAN_POINT('Ctrl Pts',(0.282473301148333,7.90864647170555,-18.1538586064405));
#67763=CARTESIAN_POINT('Ctrl Pts',(0.0761841028022858,7.9106331593925,-18.1455500327492));
#67764=CARTESIAN_POINT('Ctrl Pts',(-0.130232059834683,7.9126210698211,-18.137236345401));
#67765=CARTESIAN_POINT('Ctrl Pts',(-0.336619792044605,7.90652445229771,
-18.1289226580528));
#67766=CARTESIAN_POINT('Ctrl Pts',(-0.542340377132606,7.89238797293517,
-18.1206089707047));
#67767=CARTESIAN_POINT('Ctrl Pts',(-0.748284859284791,7.8782361080621,-18.1122862351118));
#67768=CARTESIAN_POINT('Ctrl Pts',(-0.953560451745752,7.85602691891948,
-18.103963499519));
#67769=CARTESIAN_POINT('Ctrl Pts',(-1.157534112256,7.82585687186801,-18.0956407639262));
#67770=CARTESIAN_POINT('Ctrl Pts',(-1.23337993827666,7.81463840310113,-18.0925460273106));
#67771=CARTESIAN_POINT('Ctrl Pts',(-1.3090458505169,7.8023197274721,-18.089451290695));
#67772=CARTESIAN_POINT('Ctrl Pts',(-1.38449969906905,7.78890759884066,-18.0863565540795));
#67773=CARTESIAN_POINT('Ctrl Pts',(-1.59654817636536,7.75121540012354,-18.0776593941658));
#67774=CARTESIAN_POINT('Ctrl Pts',(-1.80710879533676,7.70485031972598,-18.0689622342521));
#67775=CARTESIAN_POINT('Ctrl Pts',(-2.0154962282987,7.64994744777464,-18.0602650743384));
#67776=CARTESIAN_POINT('Ctrl Pts',(-2.22370115450324,7.59509266003351,-18.0515755314409));
#67777=CARTESIAN_POINT('Ctrl Pts',(-2.4297364738889,7.53171506966302,-18.0428859885434));
#67778=CARTESIAN_POINT('Ctrl Pts',(-2.63292905642381,7.46000037425195,-18.0341964456459));
#67779=CARTESIAN_POINT('Ctrl Pts',(-2.84066034756584,7.3866837891397,-18.0253128046044));
#67780=CARTESIAN_POINT('Ctrl Pts',(-3.04542018780775,7.30465333833933,-18.0164291635629));
#67781=CARTESIAN_POINT('Ctrl Pts',(-3.24650425733365,7.21416184370121,-18.0075455225214));
#67782=CARTESIAN_POINT('Ctrl Pts',(-3.44261811569614,7.12590703463398,-17.998881459152));
#67783=CARTESIAN_POINT('Ctrl Pts',(-3.63523550764216,7.02960454536081,-17.9902173957826));
#67784=CARTESIAN_POINT('Ctrl Pts',(-3.82372031978712,6.9255385289555,-17.9815533324132));
#67785=CARTESIAN_POINT('Ctrl Pts',(-4.01937042860175,6.81751641724314,-17.9725599025357));
#67786=CARTESIAN_POINT('Ctrl Pts',(-4.21056738759096,6.70112903845224,-17.9635664726581));
#67787=CARTESIAN_POINT('Ctrl Pts',(-4.39662304927001,6.5767489508592,-17.9545730427806));
#67788=CARTESIAN_POINT('Ctrl Pts',(-4.58267871094901,6.45236886326621,-17.9455796129031));
#67789=CARTESIAN_POINT('Ctrl Pts',(-4.76359280865984,6.31999616555474,-17.9365861830256));
#67790=CARTESIAN_POINT('Ctrl Pts',(-4.93870489993438,6.18005784045458,-17.9275927531481));
#67791=CARTESIAN_POINT('Ctrl Pts',(-5.09081459798682,6.05850154915556,-17.9197806832152));
#67792=CARTESIAN_POINT('Ctrl Pts',(-5.23848061369682,5.9312886315483,-17.9119686132824));
#67793=CARTESIAN_POINT('Ctrl Pts',(-5.3812619697026,5.79878785725366,-17.9041565433495));
#67794=CARTESIAN_POINT('Ctrl Pts',(-5.52403314308139,5.66629653241375,-17.896345030544));
#67795=CARTESIAN_POINT('Ctrl Pts',(-5.66192009263191,5.52851834151829,-17.8885335177385));
#67796=CARTESIAN_POINT('Ctrl Pts',(-5.79451699852455,5.38586053976614,-17.880722004933));
#67797=CARTESIAN_POINT('Ctrl Pts',(-5.92712783037265,5.24318775541558,-17.8729096717253));
#67798=CARTESIAN_POINT('Ctrl Pts',(-6.05444727286243,5.09563459783802,-17.8650973385177));
#67799=CARTESIAN_POINT('Ctrl Pts',(-6.1761081695767,4.94364327977737,-17.8572850053101));
#67800=CARTESIAN_POINT('Ctrl Pts',(-6.29785525627783,4.79154428431124,-17.8494671374984));
#67801=CARTESIAN_POINT('Ctrl Pts',(-6.41393556804186,4.63500112189215,-17.8416492696867));
#67802=CARTESIAN_POINT('Ctrl Pts',(-6.52402334711459,4.47448772110324,-17.833831401875));
#67803=CARTESIAN_POINT('Ctrl Pts',(-6.63415186333711,4.31391492354473,-17.8260106411204));
#67804=CARTESIAN_POINT('Ctrl Pts',(-6.7382832372243,4.14936925564053,-17.8181898803659));
#67805=CARTESIAN_POINT('Ctrl Pts',(-6.83613641550175,3.98135151784552,-17.8103691196113));
#67806=CARTESIAN_POINT('Ctrl Pts',(-6.93409798510463,3.81314766790154,-17.8025396958513));
#67807=CARTESIAN_POINT('Ctrl Pts',(-7.02576729762717,3.64146437372884,-17.7947102720912));
#67808=CARTESIAN_POINT('Ctrl Pts',(-7.110909927966,3.46682578107908,-17.7868808483311));
#67809=CARTESIAN_POINT('Ctrl Pts',(-7.17634624294497,3.3326074005729,-17.7808635496262));
#67810=CARTESIAN_POINT('Ctrl Pts',(-7.2379284054702,3.19664390093214,-17.7748462509213));
#67811=CARTESIAN_POINT('Ctrl Pts',(-7.29556977223707,3.05918006962989,-17.7688289522165));
#67812=CARTESIAN_POINT('Ctrl Pts',(-7.38193387321683,2.85321791304765,-17.7598132292709));
#67813=CARTESIAN_POINT('Ctrl Pts',(-7.45958441345405,2.64356761115758,-17.7507975063253));
#67814=CARTESIAN_POINT('Ctrl Pts',(-7.52824618037755,2.43093201213667,-17.7417817833797));
#67815=CARTESIAN_POINT('Ctrl Pts',(-7.59675969153965,2.21875553984734,-17.7327855273505));
#67816=CARTESIAN_POINT('Ctrl Pts',(-7.65632314523847,2.00360679724776,-17.7237892713212));
#67817=CARTESIAN_POINT('Ctrl Pts',(-7.70671131020899,1.78620317464081,-17.7147930152919));
#67818=CARTESIAN_POINT('Ctrl Pts',(-7.75700744217116,1.56919663554395,-17.7058131907502));
#67819=CARTESIAN_POINT('Ctrl Pts',(-7.79816170520086,1.34994359437431,-17.6968333662085));
#67820=CARTESIAN_POINT('Ctrl Pts',(-7.82999912688721,1.12917433239761,-17.6878535416668));
#67821=CARTESIAN_POINT('Ctrl Pts',(-7.86171708867684,0.909233437538468,
-17.6789074110882));
#67822=CARTESIAN_POINT('Ctrl Pts',(-7.88418794059056,0.687787833739226,
-17.6699612805096));
#67823=CARTESIAN_POINT('Ctrl Pts',(-7.8972882567302,0.465574043639957,-17.661015149931));
#67824=CARTESIAN_POINT('Ctrl Pts',(-7.90640808832236,0.310879124711466,
-17.6547872693662));
#67825=CARTESIAN_POINT('Ctrl Pts',(-7.91098770773955,0.155812222309194,
-17.6485593888015));
#67826=CARTESIAN_POINT('Ctrl Pts',(-7.91099997528238,0.00062536565977314,
-17.6423315082367));
#67827=CARTESIAN_POINT('',(-7.91220373638543,-0.00240967797264085,-15.6423315082368));
#67828=CARTESIAN_POINT('Ctrl Pts',(-7.911,-6.46926956449079E-12,-17.6423315082367));
#67829=CARTESIAN_POINT('Ctrl Pts',(-7.9109999999982,-2.20167589667319,-17.553744072504));
#67830=CARTESIAN_POINT('Ctrl Pts',(-6.94214576672017,-4.38610418339242,
-17.4651566367713));
#67831=CARTESIAN_POINT('Ctrl Pts',(-3.67820201487702,-7.34180684107923,
-17.2879817653058));
#67832=CARTESIAN_POINT('Ctrl Pts',(-1.40868175871105,-8.08992666571447,
-17.1993943295731));
#67833=CARTESIAN_POINT('Ctrl Pts',(2.97309270521869,-7.65454228025025,-17.0222194581077));
#67834=CARTESIAN_POINT('Ctrl Pts',(5.05102072676101,-6.47444880833835,-16.933632022375));
#67835=CARTESIAN_POINT('Ctrl Pts',(7.66951518848094,-2.93425195367123,-16.7564571509095));
#67836=CARTESIAN_POINT('Ctrl Pts',(8.18956872247115,-0.601881960092998,
-16.6678697151768));
#67837=CARTESIAN_POINT('Ctrl Pts',(7.32306689761066,3.71537198232993,-16.4906948437113));
#67838=CARTESIAN_POINT('Ctrl Pts',(5.94329958849784,5.66643518936947,-16.4021074079786));
#67839=CARTESIAN_POINT('Ctrl Pts',(2.16154501637273,7.92205913233153,-16.2249325365132));
#67840=CARTESIAN_POINT('Ctrl Pts',(-0.21081652930626,8.20894963712986,-16.1363451007804));
#67841=CARTESIAN_POINT('Ctrl Pts',(-4.42123908576926,6.91982244717518,-15.959170229315));
#67842=CARTESIAN_POINT('Ctrl Pts',(-6.22631625634562,5.35390358803084,-15.8705827935823));
#67843=CARTESIAN_POINT('Ctrl Pts',(-7.6531728085966,2.31334857513963,-15.7354407413119));
#67844=CARTESIAN_POINT('Ctrl Pts',(-7.91100000000092,1.15702837835916,-15.6888861247743));
#67845=CARTESIAN_POINT('Ctrl Pts',(-7.911,-6.29885033021083E-12,-15.6423315082367));
#67846=CARTESIAN_POINT('',(-7.91330192014884,-0.000633965809683563,-13.6423315453791));
#67847=CARTESIAN_POINT('Ctrl Pts',(-7.91220373638543,-0.00240967797264085,
-15.6423315082368));
#67848=CARTESIAN_POINT('Ctrl Pts',(-7.91556428301706,-0.802155651716782,
-15.6102662518829));
#67849=CARTESIAN_POINT('Ctrl Pts',(-7.41652343406805,-4.23985998589394,
-15.4723584615749));
#67850=CARTESIAN_POINT('Ctrl Pts',(-3.58490407290004,-7.95466169869553,
-15.2815294042895));
#67851=CARTESIAN_POINT('Ctrl Pts',(1.86216543943451,-8.01303484465013,-15.0698443363806));
#67852=CARTESIAN_POINT('Ctrl Pts',(6.70329027487364,-5.57407882739102,-14.8581592684722));
#67853=CARTESIAN_POINT('Ctrl Pts',(9.25305049567197,1.41654005527499,-14.5935529335861));
#67854=CARTESIAN_POINT('Ctrl Pts',(3.7987038621997,8.54783779767953,-14.2760253317233));
#67855=CARTESIAN_POINT('Ctrl Pts',(-3.60029715467979,7.94008165336322,-14.0114189968371));
#67856=CARTESIAN_POINT('Ctrl Pts',(-7.24286590766586,3.91248402646697,-13.8001877347225));
#67857=CARTESIAN_POINT('Ctrl Pts',(-7.91272125770078,1.29905138717317,-13.6947990065622));
#67858=CARTESIAN_POINT('Ctrl Pts',(-7.91330192014884,-0.000633965809683564,
-13.6423315453791));
#67859=CARTESIAN_POINT('',(-7.9129081904216,0.00235452960061844,-11.64233118194));
#67860=CARTESIAN_POINT('Ctrl Pts',(-7.9109999745389,-0.000634701186066671,
-13.6423315082368));
#67861=CARTESIAN_POINT('Ctrl Pts',(-7.91099907293056,-0.011872467354115,
-13.6418777148235));
#67862=CARTESIAN_POINT('Ctrl Pts',(-7.91097422604346,-0.0231101033026613,
-13.6414239214103));
#67863=CARTESIAN_POINT('Ctrl Pts',(-7.91092543559937,-0.0343475237379891,
-13.6409701279972));
#67864=CARTESIAN_POINT('Ctrl Pts',(-7.90999034425114,-0.249717865650979,
-13.6322729680831));
#67865=CARTESIAN_POINT('Ctrl Pts',(-7.90025568575849,-0.46510294259373,
-13.623575808169));
#67866=CARTESIAN_POINT('Ctrl Pts',(-7.881737558672,-0.679804424977677,-13.614878648255));
#67867=CARTESIAN_POINT('Ctrl Pts',(-7.86323564985387,-0.894317870729024,
-13.6061891053571));
#67868=CARTESIAN_POINT('Ctrl Pts',(-7.83596565237483,-1.10814868945514,
-13.5974995624592));
#67869=CARTESIAN_POINT('Ctrl Pts',(-7.799995611737,-1.32060192975913,-13.5888100195613));
#67870=CARTESIAN_POINT('Ctrl Pts',(-7.76322210903109,-1.53780073378222,
-13.57992637852));
#67871=CARTESIAN_POINT('Ctrl Pts',(-7.71735535863239,-1.75355946069846,
-13.5710427374787));
#67872=CARTESIAN_POINT('Ctrl Pts',(-7.66252421961339,-1.96714096694624,
-13.5621590964374));
#67873=CARTESIAN_POINT('Ctrl Pts',(-7.60904834627638,-2.17544336189149,
-13.5534950330676));
#67874=CARTESIAN_POINT('Ctrl Pts',(-7.54704599183567,-2.38167463296328,
-13.5448309696978));
#67875=CARTESIAN_POINT('Ctrl Pts',(-7.47668853165346,-2.58515949230247,
-13.5361669063281));
#67876=CARTESIAN_POINT('Ctrl Pts',(-7.40365641525792,-2.79637987879034,
-13.527173476451));
#67877=CARTESIAN_POINT('Ctrl Pts',(-7.32162155643005,-3.00464072724953,
-13.5181800465739));
#67878=CARTESIAN_POINT('Ctrl Pts',(-7.23083355376838,-3.20920038603035,
-13.5091866166968));
#67879=CARTESIAN_POINT('Ctrl Pts',(-7.14004555110671,-3.41376004481117,
-13.5001931868197));
#67880=CARTESIAN_POINT('Ctrl Pts',(-7.04050445631863,-3.61461823432231,
-13.4911997569426));
#67881=CARTESIAN_POINT('Ctrl Pts',(-6.93251822352143,-3.8110513090935,-13.4822063270655));
#67882=CARTESIAN_POINT('Ctrl Pts',(-6.83871685809038,-3.98168130656698,
-13.4743942571328));
#67883=CARTESIAN_POINT('Ctrl Pts',(-6.73858323730594,-4.14889863996573,
-13.4665821872001));
#67884=CARTESIAN_POINT('Ctrl Pts',(-6.63240542684962,-4.31220584549203,
-13.4587701172674));
#67885=CARTESIAN_POINT('Ctrl Pts',(-6.52623518859451,-4.47550140456403,
-13.4509586044621));
#67886=CARTESIAN_POINT('Ctrl Pts',(-6.41402181117272,-4.63488709610619,
-13.4431470916567));
#67887=CARTESIAN_POINT('Ctrl Pts',(-6.29609728332536,-4.78989352688585,
-13.4353355788514));
#67888=CARTESIAN_POINT('Ctrl Pts',(-6.17816037048478,-4.94491623717606,
-13.427523245644));
#67889=CARTESIAN_POINT('Ctrl Pts',(-6.05451132628634,-5.09555849092362,
-13.4197109124365));
#67890=CARTESIAN_POINT('Ctrl Pts',(-5.92552318486841,-5.24138302221722,
-13.4118985792291));
#67891=CARTESIAN_POINT('Ctrl Pts',(-5.79644366251754,-5.38731086209073,
-13.4040807114175));
#67892=CARTESIAN_POINT('Ctrl Pts',(-5.66201771967842,-5.52841389667778,
-13.396262843606));
#67893=CARTESIAN_POINT('Ctrl Pts',(-5.52265670877546,-5.66429023594461,
-13.3884449757944));
#67894=CARTESIAN_POINT('Ctrl Pts',(-5.38324412838404,-5.8002168552235,-13.38062421504));
#67895=CARTESIAN_POINT('Ctrl Pts',(-5.2388930995787,-5.93091268658528,-13.3728034542856));
#67896=CARTESIAN_POINT('Ctrl Pts',(-5.09004908463706,-6.05601530017762,
-13.3649826935312));
#67897=CARTESIAN_POINT('Ctrl Pts',(-4.94104019615443,-6.18125648911609,
-13.3571532697712));
#67898=CARTESIAN_POINT('Ctrl Pts',(-4.78752865471477,-6.30089186431787,
-13.3493238460113));
#67899=CARTESIAN_POINT('Ctrl Pts',(-4.62999088609122,-6.41460095366128,
-13.3414944222514));
#67900=CARTESIAN_POINT('Ctrl Pts',(-4.50891533311088,-6.50199200275023,
-13.3354771235456));
#67901=CARTESIAN_POINT('Ctrl Pts',(-4.38546225278603,-6.58588343819373,
-13.3294598248398));
#67902=CARTESIAN_POINT('Ctrl Pts',(-4.25985804557763,-6.6661480955292,-13.3234425261341));
#67903=CARTESIAN_POINT('Ctrl Pts',(-4.09041527297058,-6.77442684178735,
-13.3153250609713));
#67904=CARTESIAN_POINT('Ctrl Pts',(-3.91672137263509,-6.87631842405461,
-13.3072075958085));
#67905=CARTESIAN_POINT('Ctrl Pts',(-3.7392868796961,-6.97148869548912,-13.2990901306457));
#67906=CARTESIAN_POINT('Ctrl Pts',(-3.56198186606097,-7.06658951830465,
-13.2909785890423));
#67907=CARTESIAN_POINT('Ctrl Pts',(-3.38094198388653,-7.15497865872263,
-13.2828670474388));
#67908=CARTESIAN_POINT('Ctrl Pts',(-3.19670481719188,-7.23636644399261,
-13.2747555058353));
#67909=CARTESIAN_POINT('Ctrl Pts',(-3.01257592684877,-7.31770639758667,
-13.2666487313922));
#67910=CARTESIAN_POINT('Ctrl Pts',(-2.82525379146581,-7.39205307176465,
-13.2585419569492));
#67911=CARTESIAN_POINT('Ctrl Pts',(-2.63529907242501,-7.45916347849247,
-13.2504351825061));
#67912=CARTESIAN_POINT('Ctrl Pts',(-2.44542903967905,-7.52624396581782,
-13.2423320222543));
#67913=CARTESIAN_POINT('Ctrl Pts',(-2.25292906569277,-7.58609451277635,
-13.2342288620026));
#67914=CARTESIAN_POINT('Ctrl Pts',(-2.05837873744876,-7.63852066654394,
-13.2261257017508));
#67915=CARTESIAN_POINT('Ctrl Pts',(-1.8638875648434,-7.69093087943579,-13.2180250053737));
#67916=CARTESIAN_POINT('Ctrl Pts',(-1.66734759070352,-7.73592111844154,
-13.2099243089965));
#67917=CARTESIAN_POINT('Ctrl Pts',(-1.46935302835809,-7.77334694182981,
-13.2018236126194));
#67918=CARTESIAN_POINT('Ctrl Pts',(-1.26983903390524,-7.8110599751143,-13.1936607506049));
#67919=CARTESIAN_POINT('Ctrl Pts',(-1.06884834867439,-7.84109191182901,
-13.1854978885904));
#67920=CARTESIAN_POINT('Ctrl Pts',(-0.866999753941357,-7.86334740595032,
-13.1773350265759));
#67921=CARTESIAN_POINT('Ctrl Pts',(-0.666689167003725,-7.88543332186132,
-13.1692343623954));
#67922=CARTESIAN_POINT('Ctrl Pts',(-0.465534024469435,-7.8998608814698,
-13.161133698215));
#67923=CARTESIAN_POINT('Ctrl Pts',(-0.26414482943276,-7.90658893006864,
-13.1530330340346));
#67924=CARTESIAN_POINT('Ctrl Pts',(-0.0627284509836759,-7.9133178868161,
-13.1449312764306));
#67925=CARTESIAN_POINT('Ctrl Pts',(0.138921722408625,-7.91234524916927,
-13.1368295188267));
#67926=CARTESIAN_POINT('Ctrl Pts',(0.34019401306695,-7.90368199217766,-13.1287277612227));
#67927=CARTESIAN_POINT('Ctrl Pts',(0.541519438305782,-7.89501644814234,
-13.1206238648072));
#67928=CARTESIAN_POINT('Ctrl Pts',(0.742466461505047,-7.87865624964724,
-13.1125199683917));
#67929=CARTESIAN_POINT('Ctrl Pts',(0.942426801007849,-7.85466439287778,
-13.1044160719762));
#67930=CARTESIAN_POINT('Ctrl Pts',(1.14496643880155,-7.83036306396343,-13.0962076430007));
#67931=CARTESIAN_POINT('Ctrl Pts',(1.34649342566749,-7.79823187326288,-13.0879992140253));
#67932=CARTESIAN_POINT('Ctrl Pts',(1.54638469507451,-7.75838999888761,-13.0797907850499));
#67933=CARTESIAN_POINT('Ctrl Pts',(1.74398657279751,-7.71900444086943,-13.0716763687299));
#67934=CARTESIAN_POINT('Ctrl Pts',(1.93998969892463,-7.67208400233859,-13.0635619524099));
#67935=CARTESIAN_POINT('Ctrl Pts',(2.13380566895088,-7.61779458683109,-13.0554475360899));
#67936=CARTESIAN_POINT('Ctrl Pts',(2.33098993189355,-7.56256168532672,-13.0471921007867));
#67937=CARTESIAN_POINT('Ctrl Pts',(2.52590998779532,-7.49970143399945,-13.0389366654836));
#67938=CARTESIAN_POINT('Ctrl Pts',(2.71796534342915,-7.42944044944961,-13.0306812301804));
#67939=CARTESIAN_POINT('Ctrl Pts',(2.91002069906291,-7.3591794648998,-13.0224257948773));
#67940=CARTESIAN_POINT('Ctrl Pts',(3.09921104666504,-7.28151791046009,-13.0141703595741));
#67941=CARTESIAN_POINT('Ctrl Pts',(3.2849598976723,-7.19673255517286,-13.005914924271));
#67942=CARTESIAN_POINT('Ctrl Pts',(3.46327800417173,-7.11533897490726,-12.9979897415116));
#67943=CARTESIAN_POINT('Ctrl Pts',(3.63880594492515,-7.02720596954404,-12.9900645587522));
#67944=CARTESIAN_POINT('Ctrl Pts',(3.8110004953195,-6.93254615741392,-12.9821393759927));
#67945=CARTESIAN_POINT('Ctrl Pts',(3.98301106040099,-6.83798748678398,-12.974222661081));
#67946=CARTESIAN_POINT('Ctrl Pts',(4.15169503192817,-6.73691606278549,-12.9663059461693));
#67947=CARTESIAN_POINT('Ctrl Pts',(4.3165292516452,-6.62959246256445,-12.9583892312576));
#67948=CARTESIAN_POINT('Ctrl Pts',(4.4812145182245,-6.52236584576732,-12.9504796703187));
#67949=CARTESIAN_POINT('Ctrl Pts',(4.6420566781372,-6.40889849316678,-12.9425701093798));
#67950=CARTESIAN_POINT('Ctrl Pts',(4.79855703300233,-6.28949691159984,-12.9346605484409));
#67951=CARTESIAN_POINT('Ctrl Pts',(4.95491977876746,-6.17020031857552,-12.9267579422949));
#67952=CARTESIAN_POINT('Ctrl Pts',(5.10694805947257,-6.04498010562055,-12.918855336149));
#67953=CARTESIAN_POINT('Ctrl Pts',(5.25417201345454,-5.91418611924168,-12.910952730003));
#67954=CARTESIAN_POINT('Ctrl Pts',(5.40132039303578,-5.78345927327627,-12.903054180498));
#67955=CARTESIAN_POINT('Ctrl Pts',(5.54366910364888,-5.64716458020315,-12.895155630993));
#67956=CARTESIAN_POINT('Ctrl Pts',(5.6807807563017,-5.50569259937678,-12.887257081488));
#67957=CARTESIAN_POINT('Ctrl Pts',(5.81784590906124,-5.36426859720055,-12.8793612106883));
#67958=CARTESIAN_POINT('Ctrl Pts',(5.94967730440633,-5.21767105065525,-12.8714653398886));
#67959=CARTESIAN_POINT('Ctrl Pts',(6.07587366988091,-5.06632807343227,-12.8635694690889));
#67960=CARTESIAN_POINT('Ctrl Pts',(6.16334282995445,-4.96142930672895,-12.8580966871724));
#67961=CARTESIAN_POINT('Ctrl Pts',(6.24810558269317,-4.85425156050755,-12.8526239052559));
#67962=CARTESIAN_POINT('Ctrl Pts',(6.33003929358821,-4.74494715899232,-12.8471511233394));
#67963=CARTESIAN_POINT('Ctrl Pts',(6.45758520287067,-4.57479339532725,-12.8386316636662));
#67964=CARTESIAN_POINT('Ctrl Pts',(6.57814689505413,-4.39965454663752,-12.830112203993));
#67965=CARTESIAN_POINT('Ctrl Pts',(6.69137854313384,-4.22011542407173,-12.8215927443197));
#67966=CARTESIAN_POINT('Ctrl Pts',(6.80481411280608,-4.04025296519124,-12.8130579417471));
#67967=CARTESIAN_POINT('Ctrl Pts',(6.91089312188798,-3.85597460529773,-12.8045231391745));
#67968=CARTESIAN_POINT('Ctrl Pts',(7.00931563572188,-3.66788976372311,-12.7959883366019));
#67969=CARTESIAN_POINT('Ctrl Pts',(7.11271933895107,-3.47028589868759,-12.7870215854191));
#67970=CARTESIAN_POINT('Ctrl Pts',(7.20767140385833,-3.26848062986892,-12.7780548342363));
#67971=CARTESIAN_POINT('Ctrl Pts',(7.29388208941897,-3.06320176704917,-12.7690880830534));
#67972=CARTESIAN_POINT('Ctrl Pts',(7.37628249967098,-2.86699566565453,-12.7605176376233));
#67973=CARTESIAN_POINT('Ctrl Pts',(7.45069749633437,-2.66761661204617,-12.7519471921931));
#67974=CARTESIAN_POINT('Ctrl Pts',(7.51692571238235,-2.46571467013624,-12.743376746763));
#67975=CARTESIAN_POINT('Ctrl Pts',(7.58323668942425,-2.26356042480668,-12.7347955914176));
#67976=CARTESIAN_POINT('Ctrl Pts',(7.64134037487582,-2.05887723087956,-12.7262144360722));
#67977=CARTESIAN_POINT('Ctrl Pts',(7.69108586500686,-1.85232805331335,-12.7176332807268));
#67978=CARTESIAN_POINT('Ctrl Pts',(7.74091412247346,-1.64543521594918,-12.709037847919));
#67979=CARTESIAN_POINT('Ctrl Pts',(7.78235632402971,-1.43667043037062,-12.7004424151112));
#67980=CARTESIAN_POINT('Ctrl Pts',(7.81531263808677,-1.22670671676698,-12.6918469823034));
#67981=CARTESIAN_POINT('Ctrl Pts',(7.81973427457653,-1.19853659992721,-12.6906937623383));
#67982=CARTESIAN_POINT('Ctrl Pts',(7.82400323585118,-1.17034490821894,-12.6895405423731));
#67983=CARTESIAN_POINT('Ctrl Pts',(7.82811935192236,-1.14213327245933,-12.688387322408));
#67984=CARTESIAN_POINT('Ctrl Pts',(7.85634854142691,-0.948651942409426,
-12.6804782974015));
#67985=CARTESIAN_POINT('Ctrl Pts',(7.87743627301376,-0.753876758817094,
-12.672569272395));
#67986=CARTESIAN_POINT('Ctrl Pts',(7.89126959376374,-0.55837729049442,-12.6646602473885));
#67987=CARTESIAN_POINT('Ctrl Pts',(7.90508881356139,-0.363077103944612,
-12.656759284422));
#67988=CARTESIAN_POINT('Ctrl Pts',(7.911668328097,-0.167054444395018,-12.6488583214555));
#67989=CARTESIAN_POINT('Ctrl Pts',(7.91094643343843,0.0291123215807306,
-12.640957358489));
#67990=CARTESIAN_POINT('Ctrl Pts',(7.91022514072346,0.225115516141607,-12.6330629836501));
#67991=CARTESIAN_POINT('Ctrl Pts',(7.90221456866037,0.421262234903514,-12.6251686088112));
#67992=CARTESIAN_POINT('Ctrl Pts',(7.88690489857525,0.616970113400794,-12.6172742339723));
#67993=CARTESIAN_POINT('Ctrl Pts',(7.87160515499402,0.812551098568149,-12.6093849776985));
#67994=CARTESIAN_POINT('Ctrl Pts',(7.84901576942605,1.00769346787065,-12.6014957214247));
#67995=CARTESIAN_POINT('Ctrl Pts',(7.81917898680338,1.20181569815528,-12.5936064651508));
#67996=CARTESIAN_POINT('Ctrl Pts',(7.78935601744504,1.39584805743366,-12.5857208612944));
#67997=CARTESIAN_POINT('Ctrl Pts',(7.75229238934904,1.58886087872405,-12.5778352574379));
#67998=CARTESIAN_POINT('Ctrl Pts',(7.70808212992109,1.78027831486852,-12.5699496535814));
#67999=CARTESIAN_POINT('Ctrl Pts',(7.66157429029105,1.98164359835233,-12.5616542397049));
#68000=CARTESIAN_POINT('Ctrl Pts',(7.60715727742886,2.18124286102403,-12.5533588258284));
#68001=CARTESIAN_POINT('Ctrl Pts',(7.54500165400536,2.37841775999431,-12.5450634119518));
#68002=CARTESIAN_POINT('Ctrl Pts',(7.48592640236596,2.56582086420387,-12.5371791106575));
#68003=CARTESIAN_POINT('Ctrl Pts',(7.41986112155096,2.75103372711868,-12.5292948093632));
#68004=CARTESIAN_POINT('Ctrl Pts',(7.34700343068811,2.93350670520064,-12.5214105080688));
#68005=CARTESIAN_POINT('Ctrl Pts',(7.2741362405951,3.11600347422076,-12.5135251788145));
#68006=CARTESIAN_POINT('Ctrl Pts',(7.19447500312477,3.29575932593703,-12.5056398495601));
#68007=CARTESIAN_POINT('Ctrl Pts',(7.1082655293651,3.47224454266111,-12.4977545203058));
#68008=CARTESIAN_POINT('Ctrl Pts',(7.02203033138084,3.64878242117693,-12.4898668381316));
#68009=CARTESIAN_POINT('Ctrl Pts',(6.92924315475177,3.8220474100577,-12.4819791559574));
#68010=CARTESIAN_POINT('Ctrl Pts',(6.83019591979877,3.99153412827251,-12.4740914737832));
#68011=CARTESIAN_POINT('Ctrl Pts',(6.73110248849132,4.1610998963317,-12.4662001127364));
#68012=CARTESIAN_POINT('Ctrl Pts',(6.62574335448452,4.3268835847316,-12.4583087516896));
#68013=CARTESIAN_POINT('Ctrl Pts',(6.51445405098402,4.48840833900146,-12.4504173906428));
#68014=CARTESIAN_POINT('Ctrl Pts',(6.4030365048607,4.65011922399087,-12.4425169360999));
#68015=CARTESIAN_POINT('Ctrl Pts',(6.28567533592799,4.8075610884601,-12.4346164815571));
#68016=CARTESIAN_POINT('Ctrl Pts',(6.16274739818465,4.96028885309801,-12.4267160270143));
#68017=CARTESIAN_POINT('Ctrl Pts',(6.03973724705966,5.11311876104225,-12.4188102887003));
#68018=CARTESIAN_POINT('Ctrl Pts',(5.91115313047215,5.2612280245565,-12.4109045503864));
#68019=CARTESIAN_POINT('Ctrl Pts',(5.77740928637362,5.40420789179356,-12.4029988120725));
#68020=CARTESIAN_POINT('Ctrl Pts',(5.64348514570665,5.54738050643963,-12.3950824162401));
#68021=CARTESIAN_POINT('Ctrl Pts',(5.50438762924163,5.68540967254575,-12.3871660204077));
#68022=CARTESIAN_POINT('Ctrl Pts',(5.3605654315066,5.81792568313969,-12.3792496245753));
#68023=CARTESIAN_POINT('Ctrl Pts',(5.30975719073765,5.86473977357935,-12.3764529898985));
#68024=CARTESIAN_POINT('Ctrl Pts',(5.25835958554602,5.91086620423005,-12.3736563552217));
#68025=CARTESIAN_POINT('Ctrl Pts',(5.20639327305232,5.95628995989244,-12.370859720545));
#68026=CARTESIAN_POINT('Ctrl Pts',(5.06216589040119,6.0823591203734,-12.3630979364139));
#68027=CARTESIAN_POINT('Ctrl Pts',(4.91310344352879,6.20340786624087,-12.3553361522829));
#68028=CARTESIAN_POINT('Ctrl Pts',(4.7595957947092,6.31903227329838,-12.3475743681518));
#68029=CARTESIAN_POINT('Ctrl Pts',(4.60627247888219,6.43451783780875,-12.3398219044221));
#68030=CARTESIAN_POINT('Ctrl Pts',(4.44851486858131,6.5445918153278,-12.3320694406925));
#68031=CARTESIAN_POINT('Ctrl Pts',(4.2867494487054,6.64888713726018,-12.3243169769628));
#68032=CARTESIAN_POINT('Ctrl Pts',(4.12514546879186,6.75307837370347,-12.3165722500995));
#68033=CARTESIAN_POINT('Ctrl Pts',(3.95954194042255,6.85150224225592,-12.3088275232363));
#68034=CARTESIAN_POINT('Ctrl Pts',(3.7903982699531,6.94383193598006,-12.3010827963731));
#68035=CARTESIAN_POINT('Ctrl Pts',(3.62138914659194,7.03608818508007,-12.2933442301342));
#68036=CARTESIAN_POINT('Ctrl Pts',(3.44884580093232,7.12225973996112,-12.2856056638952));
#68037=CARTESIAN_POINT('Ctrl Pts',(3.27325653934698,7.2020630813415,-12.2778670976563));
#68038=CARTESIAN_POINT('Ctrl Pts',(3.09777142655465,7.28181908826869,-12.2701331214607));
#68039=CARTESIAN_POINT('Ctrl Pts',(2.91924432101981,7.35521425521839,-12.2623991452652));
#68040=CARTESIAN_POINT('Ctrl Pts',(2.73818812701339,7.42201096611174,-12.2546651690697));
#68041=CARTESIAN_POINT('Ctrl Pts',(2.55720271816351,7.48878156237441,-12.246934216525));
#68042=CARTESIAN_POINT('Ctrl Pts',(2.37369052635165,7.54895871655249,-12.2392032639803));
#68043=CARTESIAN_POINT('Ctrl Pts',(2.18818451338544,7.6023528946886,-12.2314723114357));
#68044=CARTESIAN_POINT('Ctrl Pts',(2.00267823975531,7.65574714785158,-12.2237413480278));
#68045=CARTESIAN_POINT('Ctrl Pts',(1.8151784810943,7.70235829576359,-12.21601038462));
#68046=CARTESIAN_POINT('Ctrl Pts',(1.62623383725534,7.7420465321881,-12.2082794212122));
#68047=CARTESIAN_POINT('Ctrl Pts',(1.43727941233524,7.78173682315014,-12.2005480575962));
#68048=CARTESIAN_POINT('Ctrl Pts',(1.24688030463003,7.81450341415753,-12.1928166939803));
#68049=CARTESIAN_POINT('Ctrl Pts',(1.05559562915932,7.84025757661697,-12.1850853303644));
#68050=CARTESIAN_POINT('Ctrl Pts',(0.864266024566849,7.86601778823794,-12.1773521507986));
#68051=CARTESIAN_POINT('Ctrl Pts',(0.672050793867611,7.88476224329706,-12.1696189712328));
#68052=CARTESIAN_POINT('Ctrl Pts',(0.479514552664956,7.89645406456484,-12.161885791667));
#68053=CARTESIAN_POINT('Ctrl Pts',(0.286897821121417,7.90815077363282,-12.1541493792228));
#68054=CARTESIAN_POINT('Ctrl Pts',(0.0939601698556643,7.91278895610964,
-12.1464129667785));
#68055=CARTESIAN_POINT('Ctrl Pts',(-0.0987333508868629,7.91038385449294,
-12.1386765543343));
#68056=CARTESIAN_POINT('Ctrl Pts',(-0.291656172589594,7.90797589085937,
-12.1309309357331));
#68057=CARTESIAN_POINT('Ctrl Pts',(-0.484333924576509,7.89850790921964,
-12.1231853171319));
#68058=CARTESIAN_POINT('Ctrl Pts',(-0.676205200263328,7.8820471660056,-12.1154396985307));
#68059=CARTESIAN_POINT('Ctrl Pts',(-0.868201228321395,7.8655757202164,-12.1076890438225));
#68060=CARTESIAN_POINT('Ctrl Pts',(-1.05938938074976,7.84210249983862,-12.0999383891142));
#68061=CARTESIAN_POINT('Ctrl Pts',(-1.24921814267264,7.81174596566078,-12.0921877344059));
#68062=CARTESIAN_POINT('Ctrl Pts',(-1.43933528508502,7.7813433150141,-12.0844253052038));
#68063=CARTESIAN_POINT('Ctrl Pts',(-1.62808856203291,7.74403653578136,-12.0766628760016));
#68064=CARTESIAN_POINT('Ctrl Pts',(-1.81494016212452,7.69999436414777,-12.0689004467995));
#68065=CARTESIAN_POINT('Ctrl Pts',(-1.93985668605306,7.67055070413076,-12.0637110040936));
#68066=CARTESIAN_POINT('Ctrl Pts',(-2.06392362330912,7.63809777611437,-12.0585215613877));
#68067=CARTESIAN_POINT('Ctrl Pts',(-2.18698543962865,7.60269792158365,-12.0533321186819));
#68068=CARTESIAN_POINT('Ctrl Pts',(-2.37704472668374,7.5480256331746,-12.0453174329703));
#68069=CARTESIAN_POINT('Ctrl Pts',(-2.56528649447441,7.48615503709286,-12.0373027472588));
#68070=CARTESIAN_POINT('Ctrl Pts',(-2.751133962191,7.41722204885895,-12.0292880615473));
#68071=CARTESIAN_POINT('Ctrl Pts',(-2.93677014604261,7.34836742826898,-12.021282487468));
#68072=CARTESIAN_POINT('Ctrl Pts',(-3.12001714278529,7.27246652954982,-12.0132769133886));
#68073=CARTESIAN_POINT('Ctrl Pts',(-3.30031138418942,7.18970554107675,-12.0052713393093));
#68074=CARTESIAN_POINT('Ctrl Pts',(-3.48043122839172,7.10702460665697,-11.9972735089589));
#68075=CARTESIAN_POINT('Ctrl Pts',(-3.65760370705829,7.01749694500259,-11.9892756786084));
#68076=CARTESIAN_POINT('Ctrl Pts',(-3.83128297388375,6.92135765395984,-11.9812778482579));
#68077=CARTESIAN_POINT('Ctrl Pts',(-4.00482367470889,6.82529506543477,-11.9732863987921));
#68078=CARTESIAN_POINT('Ctrl Pts',(-4.17487642696911,6.72263152208037,-11.9652949493263));
#68079=CARTESIAN_POINT('Ctrl Pts',(-4.34091747095585,6.61364925818948,-11.9573034998604));
#68080=CARTESIAN_POINT('Ctrl Pts',(-4.50685416603746,6.50473548447212,-11.9493170726408));
#68081=CARTESIAN_POINT('Ctrl Pts',(-4.66878389953174,6.38951108873213,-11.9413306454211));
#68082=CARTESIAN_POINT('Ctrl Pts',(-4.82620918116694,6.26830327438135,-11.9333442182015));
#68083=CARTESIAN_POINT('Ctrl Pts',(-4.98845185379272,6.14338636434545,-11.9251133973106));
#68084=CARTESIAN_POINT('Ctrl Pts',(-5.14590970040969,6.01211420331347,-11.9168825764196));
#68085=CARTESIAN_POINT('Ctrl Pts',(-5.29807108467227,5.87489266129685,-11.9086517555287));
#68086=CARTESIAN_POINT('Ctrl Pts',(-5.44561514671236,5.74183509346086,-11.9006706980872));
#68087=CARTESIAN_POINT('Ctrl Pts',(-5.58817921861217,5.6031841667586,-11.8926896406457));
#68088=CARTESIAN_POINT('Ctrl Pts',(-5.72533099993576,5.4593503222613,-11.8847085832042));
#68089=CARTESIAN_POINT('Ctrl Pts',(-5.86247206294,5.3155277182821,-11.876728149477));
#68090=CARTESIAN_POINT('Ctrl Pts',(-5.99420144753901,5.1665232457812,-11.8687477157498));
#68091=CARTESIAN_POINT('Ctrl Pts',(-6.12012430553447,5.01278360642131,-11.8607672820226));
#68092=CARTESIAN_POINT('Ctrl Pts',(-6.24605665338571,4.85903238086469,-11.8527862468703));
#68093=CARTESIAN_POINT('Ctrl Pts',(-6.3661813907419,4.70054553614335,-11.844805211718));
#68094=CARTESIAN_POINT('Ctrl Pts',(-6.4801442601237,4.5378024822579,-11.8368241765657));
#68095=CARTESIAN_POINT('Ctrl Pts',(-6.59413321293507,4.375022180302,-11.8288413147416));
#68096=CARTESIAN_POINT('Ctrl Pts',(-6.70195729533414,4.2079840016717,-11.8208584529174));
#68097=CARTESIAN_POINT('Ctrl Pts',(-6.8033056343289,4.03719623574439,-11.8128755910932));
#68098=CARTESIAN_POINT('Ctrl Pts',(-6.90472917926648,3.86628173606806,-11.8048868055543));
#68099=CARTESIAN_POINT('Ctrl Pts',(-6.99966721107912,3.6916123789148,-11.7968980200154));
#68100=CARTESIAN_POINT('Ctrl Pts',(-7.087854388323,3.51372184014763,-11.7889092344765));
#68101=CARTESIAN_POINT('Ctrl Pts',(-7.17608045816177,3.33575284751816,-11.7809169256974));
#68102=CARTESIAN_POINT('Ctrl Pts',(-7.25754959619902,3.15456014368803,-11.7729246169184));
#68103=CARTESIAN_POINT('Ctrl Pts',(-7.33204443313085,2.9706978019642,-11.7649323081394));
#68104=CARTESIAN_POINT('Ctrl Pts',(-7.40660897471381,2.78666342066133,-11.756932520975));
#68105=CARTESIAN_POINT('Ctrl Pts',(-7.47418606501852,2.59995472537995,-11.7489327338107));
#68106=CARTESIAN_POINT('Ctrl Pts',(-7.53460773908747,2.41114230564753,-11.7409329466464));
#68107=CARTESIAN_POINT('Ctrl Pts',(-7.54751926240514,2.37079493034541,-11.7392234700372));
#68108=CARTESIAN_POINT('Ctrl Pts',(-7.56010422833779,2.33035153566343,-11.737513993428));
#68109=CARTESIAN_POINT('Ctrl Pts',(-7.57236129918832,2.28981775575155,-11.7358045168188));
#68110=CARTESIAN_POINT('Ctrl Pts',(-7.63487911187803,2.08307315167448,-11.7270852445103));
#68111=CARTESIAN_POINT('Ctrl Pts',(-7.68895729105136,1.87366285074523,-11.7183659722017));
#68112=CARTESIAN_POINT('Ctrl Pts',(-7.73439168130246,1.66225940219912,-11.7096466998932));
#68113=CARTESIAN_POINT('Ctrl Pts',(-7.77976279339094,1.4511503830867,-11.700939571239));
#68114=CARTESIAN_POINT('Ctrl Pts',(-7.81651409668169,1.23805397237733,-11.6922324425848));
#68115=CARTESIAN_POINT('Ctrl Pts',(-7.84449166760319,1.02365593677963,-11.6835253139307));
#68116=CARTESIAN_POINT('Ctrl Pts',(-7.87240253864888,0.80976903641903,-11.6748389434903));
#68117=CARTESIAN_POINT('Ctrl Pts',(-7.89158139911881,0.594586924409034,
-11.66615257305));
#68118=CARTESIAN_POINT('Ctrl Pts',(-7.90192565665978,0.378803269022262,
-11.6574662026097));
#68119=CARTESIAN_POINT('Ctrl Pts',(-7.90793342777937,0.253479744566416,
-11.6524213044854));
#68120=CARTESIAN_POINT('Ctrl Pts',(-7.91096214797229,0.127953536149312,
-11.6473764063611));
#68121=CARTESIAN_POINT('Ctrl Pts',(-7.91099964736161,0.00236208477935112,
-11.6423315082368));
#68122=CARTESIAN_POINT('',(-7.8964170631581,0.000600145041366463,-9.64211896160294));
#68123=CARTESIAN_POINT('Ctrl Pts',(-7.9129081904216,0.00235452960061844,
-11.64233118194));
#68124=CARTESIAN_POINT('Ctrl Pts',(-7.91061145860717,-0.539573416157087,
-11.6205676932558));
#68125=CARTESIAN_POINT('Ctrl Pts',(-7.71358646751875,-2.40039572256556,
-11.5458829375944));
#68126=CARTESIAN_POINT('Ctrl Pts',(-6.28991713969721,-5.34225823726283,
-11.4182769149559));
#68127=CARTESIAN_POINT('Ctrl Pts',(-2.97255753145148,-7.67959952006296,
-11.2595131140243));
#68128=CARTESIAN_POINT('Ctrl Pts',(2.43982948211447,-8.37481141267956,-11.0478280461155));
#68129=CARTESIAN_POINT('Ctrl Pts',(7.22580432018955,-4.89039179196627,-10.8361429782069));
#68130=CARTESIAN_POINT('Ctrl Pts',(8.21331522541468,0.46673392135825,-10.6244579102983));
#68131=CARTESIAN_POINT('Ctrl Pts',(6.63670966247552,5.65318849316478,-10.4127728423895));
#68132=CARTESIAN_POINT('Ctrl Pts',(0.184060152027318,9.35904114020558,-10.1481665075036));
#68133=CARTESIAN_POINT('Ctrl Pts',(-6.6942692761131,5.76619568406868,-9.87371230712702));
#68134=CARTESIAN_POINT('Ctrl Pts',(-7.89134496298745,1.56412139810797,-9.70510064070473));
#68135=CARTESIAN_POINT('Ctrl Pts',(-7.89604907601277,0.00059194571216748,
-9.64233150823677));
#68136=CARTESIAN_POINT('',(-7.91099369906704,0.00998465430474249,-5.64233150823678));
#68137=CARTESIAN_POINT('Ctrl Pts',(-7.91099994591311,0.000925074479515564,
-9.63369599715849));
#68138=CARTESIAN_POINT('Ctrl Pts',(-7.91111146910358,-0.952792678327162,
-9.59709787947992));
#68139=CARTESIAN_POINT('Ctrl Pts',(-7.7387878457638,-1.89854071997732,-9.56687127556384));
#68140=CARTESIAN_POINT('Ctrl Pts',(-7.33879272140064,-2.95948042625145,
-9.52501737594924));
#68141=CARTESIAN_POINT('Ctrl Pts',(-7.26947854741557,-3.12587321044274,
-9.51815174290647));
#68142=CARTESIAN_POINT('Ctrl Pts',(-7.17967042688255,-3.32227796713343,
-9.50960279053886));
#68143=CARTESIAN_POINT('Ctrl Pts',(-7.16458817198334,-3.35467950857822,
-9.50817883091966));
#68144=CARTESIAN_POINT('Ctrl Pts',(-7.14413446458521,-3.39785352697423,
-9.50626408786518));
#68145=CARTESIAN_POINT('Ctrl Pts',(-7.13895710422596,-3.40871783828617,
-9.50578078410131));
#68146=CARTESIAN_POINT('Ctrl Pts',(-7.13036911345293,-3.42663372168387,
-9.50498138672398));
#68147=CARTESIAN_POINT('Ctrl Pts',(-7.12697275548826,-3.43369213802041,
-9.50466582700147));
#68148=CARTESIAN_POINT('Ctrl Pts',(-7.12033654848942,-3.44743144488754,
-9.50405039629591));
#68149=CARTESIAN_POINT('Ctrl Pts',(-7.11709776494728,-3.45411284336901,
-9.50375056454872));
#68150=CARTESIAN_POINT('Ctrl Pts',(-7.10954582026169,-3.46963629433136,
-9.50305267649529));
#68151=CARTESIAN_POINT('Ctrl Pts',(-7.10522556642992,-3.47847487191732,
-9.50265436538665));
#68152=CARTESIAN_POINT('Ctrl Pts',(-7.09111328332791,-3.50721045533762,
-9.50135632669987));
#68153=CARTESIAN_POINT('Ctrl Pts',(-7.08125411622026,-3.52707427002634,
-9.50045424789244));
#68154=CARTESIAN_POINT('Ctrl Pts',(-6.96437624469295,-3.7600892185885,-9.48981757488879));
#68155=CARTESIAN_POINT('Ctrl Pts',(-6.84785753945099,-3.96833045529407,
-9.4797765537756));
#68156=CARTESIAN_POINT('Ctrl Pts',(-6.52697906365773,-4.48547065495884,
-9.45384182609394));
#68157=CARTESIAN_POINT('Ctrl Pts',(-6.31001385031687,-4.7858781736028,-9.43782713961079));
#68158=CARTESIAN_POINT('Ctrl Pts',(-5.7133783690336,-5.5005257014241,-9.39797255921956));
#68159=CARTESIAN_POINT('Ctrl Pts',(-5.30916730476546,-5.89162610501911,
-9.37456360132866));
#68160=CARTESIAN_POINT('Ctrl Pts',(-4.68714923666404,-6.37703621224692,
-9.34210844832806));
#68161=CARTESIAN_POINT('Ctrl Pts',(-4.50132230734823,-6.50953602426058,
-9.33277714194438));
#68162=CARTESIAN_POINT('Ctrl Pts',(-4.27317163993847,-6.65776665445819,
-9.32176470606153));
#68163=CARTESIAN_POINT('Ctrl Pts',(-4.23611721421675,-6.6814043182343,-9.31998945157181));
#68164=CARTESIAN_POINT('Ctrl Pts',(-4.17768165397452,-6.71799984198844,
-9.31721051371941));
#68165=CARTESIAN_POINT('Ctrl Pts',(-4.15643289274584,-6.73116717160455,
-9.31620425571997));
#68166=CARTESIAN_POINT('Ctrl Pts',(-4.11667792524168,-6.75554231221871,
-9.31432946828467));
#68167=CARTESIAN_POINT('Ctrl Pts',(-4.09818746947109,-6.76677534286162,
-9.31346062835265));
#68168=CARTESIAN_POINT('Ctrl Pts',(-4.05690439505437,-6.79162370831924,
-9.31152774493903));
#68169=CARTESIAN_POINT('Ctrl Pts',(-4.03408882927901,-6.80520045184133,
-9.31046420178991));
#68170=CARTESIAN_POINT('Ctrl Pts',(-3.96923602339953,-6.84335132576966,
-9.30745424132499));
#68171=CARTESIAN_POINT('Ctrl Pts',(-3.92703952985801,-6.86765262277037,
-9.30551136533179));
#68172=CARTESIAN_POINT('Ctrl Pts',(-3.6360741887927,-7.03166333392704,-9.2922183802438));
#68173=CARTESIAN_POINT('Ctrl Pts',(-3.38012623738723,-7.15821750428232,
-9.28105239632895));
#68174=CARTESIAN_POINT('Ctrl Pts',(-2.76318777009988,-7.42278047147471,
-9.25504913786305));
#68175=CARTESIAN_POINT('Ctrl Pts',(-2.3978268911422,-7.54872835165053,-9.24035213959236));
#68176=CARTESIAN_POINT('Ctrl Pts',(-1.87723839538427,-7.68655827718115,
-9.21950849351732));
#68177=CARTESIAN_POINT('Ctrl Pts',(-1.72864208566482,-7.72133390378351,
-9.21356596732958));
#68178=CARTESIAN_POINT('Ctrl Pts',(-1.50262553918261,-7.76737627745208,
-9.20446140734854));
#68179=CARTESIAN_POINT('Ctrl Pts',(-1.42588961765196,-7.78182859290269,
-9.20135882455448));
#68180=CARTESIAN_POINT('Ctrl Pts',(-1.33010383776308,-7.7984043704001,-9.19746264789769));
#68181=CARTESIAN_POINT('Ctrl Pts',(-1.31124274253778,-7.80159787542042,
-9.19669431069833));
#68182=CARTESIAN_POINT('Ctrl Pts',(-1.28061288970092,-7.80666981823595,
-9.1954446332873));
#68183=CARTESIAN_POINT('Ctrl Pts',(-1.26885123748803,-7.80859011346885,
-9.19496431638576));
#68184=CARTESIAN_POINT('Ctrl Pts',(-1.24614426854764,-7.81224476507282,
-9.19403618400884));
#68185=CARTESIAN_POINT('Ctrl Pts',(-1.23519955370831,-7.81398271491793,
-9.19358845170125));
#68186=CARTESIAN_POINT('Ctrl Pts',(-1.21003335909776,-7.81792474880978,
-9.19255810892489));
#68187=CARTESIAN_POINT('Ctrl Pts',(-1.19580945690928,-7.82011303300623,
-9.19197515135805));
#68188=CARTESIAN_POINT('Ctrl Pts',(-1.15778451774657,-7.82585683106444,
-9.1904151709958));
#68189=CARTESIAN_POINT('Ctrl Pts',(-1.13397314961645,-7.82934256608816,
-9.18943668138076));
#68190=CARTESIAN_POINT('Ctrl Pts',(-0.954550820358003,-7.85477243621321,
-9.18205235531685));
#68191=CARTESIAN_POINT('Ctrl Pts',(-0.798335317019516,-7.87218370496563,
-9.17555996198196));
#68192=CARTESIAN_POINT('Ctrl Pts',(-0.266273145815036,-7.91548511512804,
-9.15334200228412));
#68193=CARTESIAN_POINT('Ctrl Pts',(0.110864071114688,-7.91918654777777,
-9.13743517566358));
#68194=CARTESIAN_POINT('Ctrl Pts',(0.820653025232097,-7.8754246270628,-9.10769306838539));
#68195=CARTESIAN_POINT('Ctrl Pts',(1.15284512781218,-7.83369282702711,-9.09385218505519));
#68196=CARTESIAN_POINT('Ctrl Pts',(1.55927161372077,-7.75621535738181,-9.07700635531302));
#68197=CARTESIAN_POINT('Ctrl Pts',(1.6369117362078,-7.74020185540177,-9.073791504617));
#68198=CARTESIAN_POINT('Ctrl Pts',(1.7487387152716,-7.71537934730482,-9.06916342571034));
#68199=CARTESIAN_POINT('Ctrl Pts',(1.78312744624312,-7.70750427124339,-9.06774052700572));
#68200=CARTESIAN_POINT('Ctrl Pts',(1.84323865251974,-7.69331487100634,-9.06525355485945));
#68201=CARTESIAN_POINT('Ctrl Pts',(1.86898419570178,-7.68710091754045,-9.06418846602538));
#68202=CARTESIAN_POINT('Ctrl Pts',(1.91896420495767,-7.67477179178819,-9.06212079117716));
#68203=CARTESIAN_POINT('Ctrl Pts',(1.94320185030642,-7.66867082678095,-9.06111807415116));
#68204=CARTESIAN_POINT('Ctrl Pts',(2.00134680521385,-7.6537415414288,-9.05871241149536));
#68205=CARTESIAN_POINT('Ctrl Pts',(2.03522521057297,-7.64480261172378,-9.05731058516441));
#68206=CARTESIAN_POINT('Ctrl Pts',(2.16103006106165,-7.61071303863791,-9.05210358978585));
#68207=CARTESIAN_POINT('Ctrl Pts',(2.25255951199419,-7.58412682808509,-9.04831247995158));
#68208=CARTESIAN_POINT('Ctrl Pts',(3.13207863067836,-7.3113292492368,-9.01180551888132));
#68209=CARTESIAN_POINT('Ctrl Pts',(3.87747030348066,-6.94483835278237,-8.98059485519494));
#68210=CARTESIAN_POINT('Ctrl Pts',(4.83297567192742,-6.27245956658645,-8.93721530852662));
#68211=CARTESIAN_POINT('Ctrl Pts',(5.10016020297037,-6.05720656316104,-8.92451182116437));
#68212=CARTESIAN_POINT('Ctrl Pts',(5.4377939516108,-5.74697528388434,-8.90679201368324));
#68213=CARTESIAN_POINT('Ctrl Pts',(5.52132325219828,-5.66677299050848,-8.90225547573854));
#68214=CARTESIAN_POINT('Ctrl Pts',(5.61447726244746,-5.57331388302702,-8.89698328906251));
#68215=CARTESIAN_POINT('Ctrl Pts',(5.62585945773153,-5.56182415458531,-8.89633536773506));
#68216=CARTESIAN_POINT('Ctrl Pts',(5.64297820151631,-5.54443736538007,-8.89535512148201));
#68217=CARTESIAN_POINT('Ctrl Pts',(5.64874095275725,-5.53856608965044,-8.89502414333639));
#68218=CARTESIAN_POINT('Ctrl Pts',(5.65906121703248,-5.52801861245821,-8.89442960211954));
#68219=CARTESIAN_POINT('Ctrl Pts',(5.66362212403404,-5.52334573185961,-8.89416621679997));
#68220=CARTESIAN_POINT('Ctrl Pts',(5.67270450997495,-5.51401728874818,-8.89364044255779));
#68221=CARTESIAN_POINT('Ctrl Pts',(5.67722605562234,-5.50936179889564,-8.89337805760678));
#68222=CARTESIAN_POINT('Ctrl Pts',(5.68975540483465,-5.49642948322672,-8.89264919971642));
#68223=CARTESIAN_POINT('Ctrl Pts',(5.6977508521369,-5.48814074674302,-8.89218206456847));
#68224=CARTESIAN_POINT('Ctrl Pts',(5.7293023401077,-5.45528862150533,-8.890330513915));
#68225=CARTESIAN_POINT('Ctrl Pts',(5.7527176425841,-5.43059102882144,-8.88893838678116));
#68226=CARTESIAN_POINT('Ctrl Pts',(6.11739914977545,-5.04093317111175,-8.8669586239689));
#68227=CARTESIAN_POINT('Ctrl Pts',(6.42343458998371,-4.64466216723833,-8.84416370263946));
#68228=CARTESIAN_POINT('Ctrl Pts',(6.91027849575349,-3.87327838870377,-8.80218409360877));
#68229=CARTESIAN_POINT('Ctrl Pts',(7.10290522527286,-3.50756380775889,-8.78313759996896));
#68230=CARTESIAN_POINT('Ctrl Pts',(7.37195554501409,-2.88267457002611,-8.75289874219296));
#68231=CARTESIAN_POINT('Ctrl Pts',(7.4652524482483,-2.6316465691275,-8.74130937809952));
#68232=CARTESIAN_POINT('Ctrl Pts',(7.56936046918252,-2.30107214352001,-8.72681007368894));
#68233=CARTESIAN_POINT('Ctrl Pts',(7.59194230301102,-2.22543556226948,-8.72354229734134));
#68234=CARTESIAN_POINT('Ctrl Pts',(7.62225153439803,-2.11808085663359,-8.71897336166544));
#68235=CARTESIAN_POINT('Ctrl Pts',(7.63092004221935,-2.08663468531716,-8.71764335087714));
#68236=CARTESIAN_POINT('Ctrl Pts',(7.64379618663237,-2.03877120581799,-8.71563147135972));
#68237=CARTESIAN_POINT('Ctrl Pts',(7.64814591941504,-2.02239268497117,-8.71494523734481));
#68238=CARTESIAN_POINT('Ctrl Pts',(7.65514744704342,-1.99568342053183,-8.71382974819836));
#68239=CARTESIAN_POINT('Ctrl Pts',(7.65783102615425,-1.98536110744068,-8.71339951693034));
#68240=CARTESIAN_POINT('Ctrl Pts',(7.66295422846914,-1.96548991957802,-8.71257295958142));
#68241=CARTESIAN_POINT('Ctrl Pts',(7.66539689735125,-1.9559418545863,-8.71217654054457));
#68242=CARTESIAN_POINT('Ctrl Pts',(7.66978175012386,-1.93866767897448,-8.71146067913738));
#68243=CARTESIAN_POINT('Ctrl Pts',(7.67173011643462,-1.93094315946402,-8.711141047445));
#68244=CARTESIAN_POINT('Ctrl Pts',(7.67590186180983,-1.91429781692095,-8.71045331486935));
#68245=CARTESIAN_POINT('Ctrl Pts',(7.67812136586917,-1.90537602999729,-8.7100853331549));
#68246=CARTESIAN_POINT('Ctrl Pts',(7.68404734586532,-1.88137674439763,-8.7090971834772));
#68247=CARTESIAN_POINT('Ctrl Pts',(7.68772500369647,-1.86629213649934,-8.70847789873678));
#68248=CARTESIAN_POINT('Ctrl Pts',(7.70364198513721,-1.80016021042395,-8.70577078060274));
#68249=CARTESIAN_POINT('Ctrl Pts',(7.71541757570812,-1.74900210932304,-8.70369714172563));
#68250=CARTESIAN_POINT('Ctrl Pts',(7.92472111834301,-0.796422965650187,
-8.66545419616806));
#68251=CARTESIAN_POINT('Ctrl Pts',(7.96353066047508,0.132466123893695,-8.63525772346025));
#68252=CARTESIAN_POINT('Ctrl Pts',(7.79578293479666,1.38869152312414,-8.59036027384218));
#68253=CARTESIAN_POINT('Ctrl Pts',(7.72789473335369,1.72694076688382,-8.57773004012213));
#68254=CARTESIAN_POINT('Ctrl Pts',(7.63388346889942,2.07557594455706,-8.56331159461872));
#68255=CARTESIAN_POINT('Ctrl Pts',(7.62954532418908,2.0914661026012,-8.56265148428841));
#68256=CARTESIAN_POINT('Ctrl Pts',(7.62316138052284,2.11456561135005,-8.56168771421622));
#68257=CARTESIAN_POINT('Ctrl Pts',(7.62115489431734,2.12178585970747,-8.56138587363048));
#68258=CARTESIAN_POINT('Ctrl Pts',(7.6176237322187,2.13442295275313,-8.56085655697174));
#68259=CARTESIAN_POINT('Ctrl Pts',(7.61610352783852,2.13984105015289,-8.56062928415217));
#68260=CARTESIAN_POINT('Ctrl Pts',(7.61314633062187,2.15033760238937,-8.56018835073044));
#68261=CARTESIAN_POINT('Ctrl Pts',(7.6117100338266,2.15541625132694,-8.55997472140545));
#68262=CARTESIAN_POINT('Ctrl Pts',(7.60827820997389,2.16750474041263,-8.55946554857952));
#68263=CARTESIAN_POINT('Ctrl Pts',(7.60627807840751,2.17451325897941,-8.55916980157582));
#68264=CARTESIAN_POINT('Ctrl Pts',(7.59913994109129,2.19939514698995,-8.55811791860994));
#68265=CARTESIAN_POINT('Ctrl Pts',(7.5939486232358,2.21725306549521,-8.55735946864107));
#68266=CARTESIAN_POINT('Ctrl Pts',(7.50023256674871,2.53544237721292,-8.54378497258415));
#68267=CARTESIAN_POINT('Ctrl Pts',(7.39402160617019,2.83026155617129,-8.53025709486578));
#68268=CARTESIAN_POINT('Ctrl Pts',(6.9786427361017,3.79885445481074,-8.48410769816022));
#68269=CARTESIAN_POINT('Ctrl Pts',(6.59240937102754,4.43544148713559,-8.45134003963956));
#68270=CARTESIAN_POINT('Ctrl Pts',(6.06599090516504,5.07896134402616,-8.41725403750887));
#68271=CARTESIAN_POINT('Ctrl Pts',(6.00755370971461,5.14795035365396,-8.41357748663019));
#68272=CARTESIAN_POINT('Ctrl Pts',(5.93133379416083,5.23486726252392,-8.40891187106854));
#68273=CARTESIAN_POINT('Ctrl Pts',(5.91463102600849,5.2537315946749,-8.40789716828971));
#68274=CARTESIAN_POINT('Ctrl Pts',(5.88761739846727,5.28394904923023,-8.4062682601092));
#68275=CARTESIAN_POINT('Ctrl Pts',(5.87736318983997,5.29535250216881,-8.40565272745955));
#68276=CARTESIAN_POINT('Ctrl Pts',(5.85778329956495,5.3169998794336,-8.4044826481386));
#68277=CARTESIAN_POINT('Ctrl Pts',(5.84846374719143,5.32724926221128,-8.40392796180242));
#68278=CARTESIAN_POINT('Ctrl Pts',(5.82715316516277,5.35056272195397,-8.40266464361834));
#68279=CARTESIAN_POINT('Ctrl Pts',(5.81514502533279,5.36361107734446,-8.40195640977902));
#68280=CARTESIAN_POINT('Ctrl Pts',(5.78383678146588,5.39740269515026,-8.40011913878099));
#68281=CARTESIAN_POINT('Ctrl Pts',(5.76446889888869,5.41808287969694,-8.39899164335768));
#68282=CARTESIAN_POINT('Ctrl Pts',(5.65498639428042,5.53373197062209,-8.39266794800234));
#68283=CARTESIAN_POINT('Ctrl Pts',(5.56263504826618,5.62655783325126,-8.3875226496088));
#68284=CARTESIAN_POINT('Ctrl Pts',(5.33999579641027,5.83949912457571,-8.37553856295915));
#68285=CARTESIAN_POINT('Ctrl Pts',(5.20789144587378,5.95761481405866,-8.36874747607629));
#68286=CARTESIAN_POINT('Ctrl Pts',(4.67295729417637,6.40450333756107,-8.34235253655104));
#68287=CARTESIAN_POINT('Ctrl Pts',(4.24210855755709,6.69766424664624,-8.32352909040257));
#68288=CARTESIAN_POINT('Ctrl Pts',(3.47680754795278,7.11473248328316,-8.29124734570365));
#68289=CARTESIAN_POINT('Ctrl Pts',(3.15713370250557,7.26223694366356,-8.27802975843393));
#68290=CARTESIAN_POINT('Ctrl Pts',(2.81136341930225,7.39462660592953,-8.26322131561842));
#68291=CARTESIAN_POINT('Ctrl Pts',(2.79397091309997,7.40121567352775,-8.26247508256938));
#68292=CARTESIAN_POINT('Ctrl Pts',(2.76857336190541,7.41073513249896,-8.26138323758826));
#68293=CARTESIAN_POINT('Ctrl Pts',(2.76058648891211,7.41371404228849,-8.26103957099277));
#68294=CARTESIAN_POINT('Ctrl Pts',(2.74656848135597,7.41891662552823,-8.26043582802538));
#68295=CARTESIAN_POINT('Ctrl Pts',(2.74053941337218,7.42114587127686,-8.26017597905425));
#68296=CARTESIAN_POINT('Ctrl Pts',(2.72883499531462,7.42545736731242,-8.25967116257569));
#68297=CARTESIAN_POINT('Ctrl Pts',(2.72315996147496,7.42754046568385,-8.25942623034276));
#68298=CARTESIAN_POINT('Ctrl Pts',(2.70806083691074,7.43306317396299,-8.25877410666161));
#68299=CARTESIAN_POINT('Ctrl Pts',(2.69863260018575,7.43649135900221,-8.25836643857916));
#68300=CARTESIAN_POINT('Ctrl Pts',(2.66505528995629,7.44862808298485,-8.25691285777611));
#68301=CARTESIAN_POINT('Ctrl Pts',(2.64087054654533,7.45723693816457,-8.25586270670017));
#68302=CARTESIAN_POINT('Ctrl Pts',(2.33833843624085,7.56327067084448,-8.24268249784932));
#68303=CARTESIAN_POINT('Ctrl Pts',(2.05485290784931,7.64515567850627,-8.22975886696338));
#68304=CARTESIAN_POINT('Ctrl Pts',(1.36028883474807,7.80436263415105,-8.1976056377951));
#68305=CARTESIAN_POINT('Ctrl Pts',(0.946316264859822,7.86530056050492,-8.17812299066803));
#68306=CARTESIAN_POINT('Ctrl Pts',(0.260351581594936,7.91131381233239,-8.14683361910993));
#68307=CARTESIAN_POINT('Ctrl Pts',(-0.0095215141165007,7.91559178866877,
-8.13476431806485));
#68308=CARTESIAN_POINT('Ctrl Pts',(-0.449815331528298,7.90004856165765,
-8.11566431366983));
#68309=CARTESIAN_POINT('Ctrl Pts',(-0.620296928394362,7.88849400079298,
-8.10841193808687));
#68310=CARTESIAN_POINT('Ctrl Pts',(-0.876808488475988,7.86274066949055,
-8.09772869653342));
#68311=CARTESIAN_POINT('Ctrl Pts',(-0.963191348003113,7.85262676042513,
-8.0941701434276));
#68312=CARTESIAN_POINT('Ctrl Pts',(-1.06581426677893,7.83889249038618,-8.08998843837432));
#68313=CARTESIAN_POINT('Ctrl Pts',(-1.08222982753657,7.83664303971876,-8.08932093046988));
#68314=CARTESIAN_POINT('Ctrl Pts',(-1.10752207628625,7.83309621571392,-8.08829460897441));
#68315=CARTESIAN_POINT('Ctrl Pts',(-1.11640377873893,7.83183529433681,-8.08793460997713));
#68316=CARTESIAN_POINT('Ctrl Pts',(-1.1326062032396,7.82950693978519,-8.08727862262025));
#68317=CARTESIAN_POINT('Ctrl Pts',(-1.13992760303218,7.82844434048065,-8.08698247706419));
#68318=CARTESIAN_POINT('Ctrl Pts',(-1.15589885968758,7.82610345445331,-8.08633705054059));
#68319=CARTESIAN_POINT('Ctrl Pts',(-1.16454811472015,7.82482109334066,-8.08598790301029));
#68320=CARTESIAN_POINT('Ctrl Pts',(-1.18814471920527,7.82128260828196,-8.08503641381896));
#68321=CARTESIAN_POINT('Ctrl Pts',(-1.20308779196449,7.81899797164459,-8.08443500522825));
#68322=CARTESIAN_POINT('Ctrl Pts',(-1.27496247739644,7.80779817604485,-8.08154774296773));
#68323=CARTESIAN_POINT('Ctrl Pts',(-1.33180277900806,7.79830386803138,-8.07928091571683));
#68324=CARTESIAN_POINT('Ctrl Pts',(-2.31141807965984,7.62365091937267,-8.04048609622535));
#68325=CARTESIAN_POINT('Ctrl Pts',(-3.19755127425543,7.29644944788206,-8.01075817549438));
#68326=CARTESIAN_POINT('Ctrl Pts',(-4.24536322075041,6.68116546425609,-7.96878832356702));
#68327=CARTESIAN_POINT('Ctrl Pts',(-4.47730609162477,6.52800046502394,-7.95889938225381));
#68328=CARTESIAN_POINT('Ctrl Pts',(-4.77603497816572,6.30731197842756,-7.94471456086275));
#68329=CARTESIAN_POINT('Ctrl Pts',(-4.85037592285122,6.25032372009586,-7.94105632472342));
#68330=CARTESIAN_POINT('Ctrl Pts',(-4.93197140277605,6.18544187349491,-7.93687592763071));
#68331=CARTESIAN_POINT('Ctrl Pts',(-4.94024482834538,6.17883598439501,-7.93645013072549));
#68332=CARTESIAN_POINT('Ctrl Pts',(-4.95254290076452,6.16897613887925,-7.93581429581939));
#68333=CARTESIAN_POINT('Ctrl Pts',(-4.95657768442432,6.16573478540631,-7.93560522207446));
#68334=CARTESIAN_POINT('Ctrl Pts',(-4.96346831218112,6.16018804783274,-7.93524735992625));
#68335=CARTESIAN_POINT('Ctrl Pts',(-4.96632574377207,6.15788462683106,-7.93509872331718));
#68336=CARTESIAN_POINT('Ctrl Pts',(-4.97216763612319,6.15316867358971,-7.93479435504914));
#68337=CARTESIAN_POINT('Ctrl Pts',(-4.97515194587128,6.15075595701394,-7.93463860902059));
#68338=CARTESIAN_POINT('Ctrl Pts',(-4.98229482630522,6.14497257267629,-7.93426520680609));
#68339=CARTESIAN_POINT('Ctrl Pts',(-4.98645171442332,6.14159986927912,-7.93404738994458));
#68340=CARTESIAN_POINT('Ctrl Pts',(-5.00158286556078,6.12929767670716,-7.93325268036782));
#68341=CARTESIAN_POINT('Ctrl Pts',(-5.01253653709344,6.12034301570558,-7.93267382440147));
#68342=CARTESIAN_POINT('Ctrl Pts',(-5.19136163452159,5.973350866209,-7.92316635459734));
#68343=CARTESIAN_POINT('Ctrl Pts',(-5.35348634995471,5.8284925367666,-7.91372014773208));
#68344=CARTESIAN_POINT('Ctrl Pts',(-5.97856549207776,5.22188103332268,-7.87468207224398));
#68345=CARTESIAN_POINT('Ctrl Pts',(-6.38947296911945,4.71020569644179,-7.84313546437352));
#68346=CARTESIAN_POINT('Ctrl Pts',(-6.83156429926105,3.99362668756256,-7.80517238711811));
#68347=CARTESIAN_POINT('Ctrl Pts',(-6.92461870032747,3.83001135100573,-7.79684959117924));
#68348=CARTESIAN_POINT('Ctrl Pts',(-7.07375450093531,3.54455156760922,-7.78295536721175));
#68349=CARTESIAN_POINT('Ctrl Pts',(-7.13273373678086,3.42431897943836,-7.77728451172786));
#68350=CARTESIAN_POINT('Ctrl Pts',(-7.22794034794548,3.21708931240285,-7.76781757688386));
#68351=CARTESIAN_POINT('Ctrl Pts',(-7.26571626920314,3.1308390695662,-7.76396534641699));
#68352=CARTESIAN_POINT('Ctrl Pts',(-7.30827010206746,3.02875871954841,-7.75950666282897));
#68353=CARTESIAN_POINT('Ctrl Pts',(-7.31454837927487,3.01356487864667,-7.75884560983604));
#68354=CARTESIAN_POINT('Ctrl Pts',(-7.32408409446083,2.99028246302253,-7.75783657059551));
#68355=CARTESIAN_POINT('Ctrl Pts',(-7.32737557747535,2.98220793686286,-7.75748734945598));
#68356=CARTESIAN_POINT('Ctrl Pts',(-7.333347424145,2.96748848281314,-7.75685204649727));
#68357=CARTESIAN_POINT('Ctrl Pts',(-7.33603212043261,2.96084532983361,-7.75656580797129));
#68358=CARTESIAN_POINT('Ctrl Pts',(-7.34180984620272,2.94649252288695,-7.75594842173445));
#68359=CARTESIAN_POINT('Ctrl Pts',(-7.34489976676788,2.9387816220232,-7.75561738665688));
#68360=CARTESIAN_POINT('Ctrl Pts',(-7.35322605953946,2.91790818710773,-7.75472302348134));
#68361=CARTESIAN_POINT('Ctrl Pts',(-7.35843924407603,2.90473640201388,-7.75416053247616));
#68362=CARTESIAN_POINT('Ctrl Pts',(-7.38261656196437,2.84316649289902,-7.75153995106515));
#68363=CARTESIAN_POINT('Ctrl Pts',(-7.40113897744871,2.79459567423399,-7.74949776075982));
#68364=CARTESIAN_POINT('Ctrl Pts',(-7.74561361436762,1.86383675987184,-7.7108281406531));
#68365=CARTESIAN_POINT('Ctrl Pts',(-7.91210823868078,0.93091089069761,-7.68126784400183));
#68366=CARTESIAN_POINT('Ctrl Pts',(-7.91067420643559,-0.279726549592703,
-7.63828233622777));
#68367=CARTESIAN_POINT('Ctrl Pts',(-7.89649511889754,-0.549866780207448,
-7.62830255983803));
#68368=CARTESIAN_POINT('Ctrl Pts',(-7.86685871385677,-0.834693178137426,
-7.61687089892598));
#68369=CARTESIAN_POINT('Ctrl Pts',(-7.86514867750749,-0.850655633416672,
-7.61622717993366));
#68370=CARTESIAN_POINT('Ctrl Pts',(-7.86275367237782,-0.872387205033589,
-7.61534653216811));
#68371=CARTESIAN_POINT('Ctrl Pts',(-7.86211093201363,-0.878160828301624,
-7.61511215409261));
#68372=CARTESIAN_POINT('Ctrl Pts',(-7.86100444735419,-0.888001596550004,
-7.6147119815516));
#68373=CARTESIAN_POINT('Ctrl Pts',(-7.86054390395179,-0.892069106468237,
-7.61454637613297));
#68374=CARTESIAN_POINT('Ctrl Pts',(-7.85964576465246,-0.899946755579525,
-7.61422525684078));
#68375=CARTESIAN_POINT('Ctrl Pts',(-7.85920855454718,-0.903756938963826,
-7.61406976559411));
#68376=CARTESIAN_POINT('Ctrl Pts',(-7.8581626124287,-0.912813921972404,
-7.61369974098891));
#68377=CARTESIAN_POINT('Ctrl Pts',(-7.85755139664994,-0.918060427349082,
-7.61348506319907));
#68378=CARTESIAN_POINT('Ctrl Pts',(-7.85572704962464,-0.933584826776816,
-7.61284886052932));
#68379=CARTESIAN_POINT('Ctrl Pts',(-7.85449900784106,-0.943860922420935,
-7.61242647723079));
#68380=CARTESIAN_POINT('Ctrl Pts',(-7.84468699522595,-1.02462122764104,
-7.60909719439772));
#68381=CARTESIAN_POINT('Ctrl Pts',(-7.83517483661326,-1.09498739903813,
-7.60613799259582));
#68382=CARTESIAN_POINT('Ctrl Pts',(-7.79364284498898,-1.3738856234091,-7.59420221452049));
#68383=CARTESIAN_POINT('Ctrl Pts',(-7.75423548794202,-1.58121826535327,
-7.58486954036107));
#68384=CARTESIAN_POINT('Ctrl Pts',(-7.56013635059216,-2.41842178745667,
-7.54594751398681));
#68385=CARTESIAN_POINT('Ctrl Pts',(-7.33656599118316,-3.02974145159812,
-7.51485800424289));
#68386=CARTESIAN_POINT('Ctrl Pts',(-6.98647935857242,-3.71311946838392,
-7.48035363647049));
#68387=CARTESIAN_POINT('Ctrl Pts',(-6.92969666724075,-3.81804341851617,
-7.47505505358298));
#68388=CARTESIAN_POINT('Ctrl Pts',(-6.72907406849213,-4.16952591649218,
-7.45732453864063));
#68389=CARTESIAN_POINT('Ctrl Pts',(-6.57426815021812,-4.40958103911321,
-7.44525689302093));
#68390=CARTESIAN_POINT('Ctrl Pts',(-6.39204380645067,-4.66115123603427,
-7.43265107135979));
#68391=CARTESIAN_POINT('Ctrl Pts',(-6.37717724909139,-4.68147041191776,
-7.43163312196305));
#68392=CARTESIAN_POINT('Ctrl Pts',(-6.35621640852931,-4.70983394606143,
-7.43021239324831));
#68393=CARTESIAN_POINT('Ctrl Pts',(-6.35020342601233,-4.71793803273492,
-7.42980648574624));
#68394=CARTESIAN_POINT('Ctrl Pts',(-6.33976154478517,-4.73195510681788,
-7.4291044542237));
#68395=CARTESIAN_POINT('Ctrl Pts',(-6.33533984549562,-4.73787342804324,
-7.42880805275665));
#68396=CARTESIAN_POINT('Ctrl Pts',(-6.32614124215157,-4.75014960028148,
-7.42819325871944));
#68397=CARTESIAN_POINT('Ctrl Pts',(-6.32136302722869,-4.75650646159298,
-7.42787491735421));
#68398=CARTESIAN_POINT('Ctrl Pts',(-6.31012278217441,-4.77141345262321,
-7.42712842259818));
#68399=CARTESIAN_POINT('Ctrl Pts',(-6.30365293930875,-4.77995768641166,
-7.42670057258357));
#68400=CARTESIAN_POINT('Ctrl Pts',(-6.28258845217747,-4.80765881991446,
-7.42531348809021));
#68401=CARTESIAN_POINT('Ctrl Pts',(-6.26792362646865,-4.82676231171841,
-7.42435698043247));
#68402=CARTESIAN_POINT('Ctrl Pts',(-6.00637740843168,-5.16426981685921,
-7.40745807197932));
#68403=CARTESIAN_POINT('Ctrl Pts',(-5.73560624594877,-5.46343448781761,
-7.39252106889034));
#68404=CARTESIAN_POINT('Ctrl Pts',(-5.1801956419447,-5.99006260043586,-7.36522659529685));
#68405=CARTESIAN_POINT('Ctrl Pts',(-4.9003651219561,-6.22106923450769,-7.35278293889922));
#68406=CARTESIAN_POINT('Ctrl Pts',(-4.44899597586979,-6.54427195683834,
-7.33347693460576));
#68407=CARTESIAN_POINT('Ctrl Pts',(-4.28826250143942,-6.6507039009242,-7.32673147769319));
#68408=CARTESIAN_POINT('Ctrl Pts',(-3.86881273578883,-6.90691622078107,
-7.30910513803278));
#68409=CARTESIAN_POINT('Ctrl Pts',(-3.6052539477848,-7.04807425490654,-7.29795838794914));
#68410=CARTESIAN_POINT('Ctrl Pts',(-3.31655998018063,-7.1822512402361,-7.28527062250137));
#68411=CARTESIAN_POINT('Ctrl Pts',(-3.29880603938023,-7.19042291430389,
-7.28448906702831));
#68412=CARTESIAN_POINT('Ctrl Pts',(-3.27223103826429,-7.20253555145514,
-7.28331743085811));
#68413=CARTESIAN_POINT('Ctrl Pts',(-3.26343267189909,-7.20652631527845,
-7.28292924126929));
#68414=CARTESIAN_POINT('Ctrl Pts',(-3.24828413876978,-7.21336395747949,
-7.28226040517025));
#68415=CARTESIAN_POINT('Ctrl Pts',(-3.24193747421054,-7.21621859717651,
-7.28198004548194));
#68416=CARTESIAN_POINT('Ctrl Pts',(-3.228846715707,-7.22208587911677,-7.28140148600468));
#68417=CARTESIAN_POINT('Ctrl Pts',(-3.22210215428629,-7.22509745718269,
-7.28110324813216));
#68418=CARTESIAN_POINT('Ctrl Pts',(-3.20642350641933,-7.23207195900676,
-7.28040960679588));
#68419=CARTESIAN_POINT('Ctrl Pts',(-3.19748628207698,-7.23602777757139,
-7.28001395245277));
#68420=CARTESIAN_POINT('Ctrl Pts',(-3.16909208596204,-7.24853281802285,
-7.27875614278746));
#68421=CARTESIAN_POINT('Ctrl Pts',(-3.14960805820633,-7.25702016904315,
-7.27789186470762));
#68422=CARTESIAN_POINT('Ctrl Pts',(-2.72887923290979,-7.4382784517682,-7.25920665431084));
#68423=CARTESIAN_POINT('Ctrl Pts',(-2.3140513120038,-7.57759274281634,-7.24039864737228));
#68424=CARTESIAN_POINT('Ctrl Pts',(-1.62057758538033,-7.74819680808196,
-7.20967601638181));
#68425=CARTESIAN_POINT('Ctrl Pts',(-1.34798951283231,-7.80024061888691,
-7.19776053405291));
#68426=CARTESIAN_POINT('Ctrl Pts',(-0.446219176843177,-7.92371900068378,
-7.15905792973044));
#68427=CARTESIAN_POINT('Ctrl Pts',(0.188846440655802,-7.934028686977,-7.13294710741225));
#68428=CARTESIAN_POINT('Ctrl Pts',(0.894323082355043,-7.86065789268268,
-7.10410376547628));
#68429=CARTESIAN_POINT('Ctrl Pts',(0.970184268632368,-7.85165580628152,
-7.10100765877162));
#68430=CARTESIAN_POINT('Ctrl Pts',(1.0744599350618,-7.83774756032486,-7.09675943684174));
#68431=CARTESIAN_POINT('Ctrl Pts',(1.10299531505903,-7.83378275892561,-7.09559767333884));
#68432=CARTESIAN_POINT('Ctrl Pts',(1.15195926578635,-7.82670670332844,-7.09360549901223));
#68433=CARTESIAN_POINT('Ctrl Pts',(1.17239844178364,-7.82367112464099,-7.09277428874872));
#68434=CARTESIAN_POINT('Ctrl Pts',(1.2145131979512,-7.8172475967819,-7.0910623669303));
#68435=CARTESIAN_POINT('Ctrl Pts',(1.23618705655701,-7.8138494906213,-7.09018177356707));
#68436=CARTESIAN_POINT('Ctrl Pts',(1.28667622021142,-7.80571828931236,-7.08813139075801));
#68437=CARTESIAN_POINT('Ctrl Pts',(1.31548004241416,-7.80091571381796,-7.08696238469085));
#68438=CARTESIAN_POINT('Ctrl Pts',(1.40832849394681,-7.78490585082924,-7.08319630510584));
#68439=CARTESIAN_POINT('Ctrl Pts',(1.47226200528582,-7.77306843743495,-7.08060644036147));
#68440=CARTESIAN_POINT('Ctrl Pts',(1.79559888224548,-7.70906962129087,-7.06752168639807));
#68441=CARTESIAN_POINT('Ctrl Pts',(2.05241796124809,-7.64470505467777,-7.05717840789458));
#68442=CARTESIAN_POINT('Ctrl Pts',(2.64190703786296,-7.46511202571952,-7.03331244957922));
#68443=CARTESIAN_POINT('Ctrl Pts',(2.971072121005,-7.34032014217191,-7.01989729717553));
#68444=CARTESIAN_POINT('Ctrl Pts',(3.51762356168421,-7.09030590046178,-6.99669071652824));
#68445=CARTESIAN_POINT('Ctrl Pts',(3.73936811678915,-6.97590369364318,-6.98698748684759));
#68446=CARTESIAN_POINT('Ctrl Pts',(3.97815201314763,-6.83804956817386,-6.97596592779701));
#68447=CARTESIAN_POINT('Ctrl Pts',(4.00090630676524,-6.82476109876138,-6.97490967479221));
#68448=CARTESIAN_POINT('Ctrl Pts',(4.03500955689731,-6.8046156887428,-6.97331717850109));
#68449=CARTESIAN_POINT('Ctrl Pts',(4.04640836473416,-6.79784349186522,-6.97278331474776));
#68450=CARTESIAN_POINT('Ctrl Pts',(4.06717789657399,-6.78543326211514,-6.97180772352972));
#68451=CARTESIAN_POINT('Ctrl Pts',(4.07655406735528,-6.77980438744584,-6.97136624007879));
#68452=CARTESIAN_POINT('Ctrl Pts',(4.09682851716392,-6.76757559485421,-6.97040932454151));
#68453=CARTESIAN_POINT('Ctrl Pts',(4.1077225798117,-6.76096875728948,-6.96989371483942));
#68454=CARTESIAN_POINT('Ctrl Pts',(4.13782914980523,-6.74261063236277,-6.96846487679374));
#68455=CARTESIAN_POINT('Ctrl Pts',(4.15700746423446,-6.73080360341254,-6.96755026431551));
#68456=CARTESIAN_POINT('Ctrl Pts',(4.26387730647417,-6.6643787566169,-6.96242946575371));
#68457=CARTESIAN_POINT('Ctrl Pts',(4.35054176666697,-6.60812981620152,-6.95818560532621));
#68458=CARTESIAN_POINT('Ctrl Pts',(4.8002581476746,-6.30356247507699,-6.93572780376755));
#68459=CARTESIAN_POINT('Ctrl Pts',(5.14323303337616,-6.02698356156208,-6.91711733154376));
#68460=CARTESIAN_POINT('Ctrl Pts',(5.62035679582944,-5.57169287437059,-6.88953790763791));
#68461=CARTESIAN_POINT('Ctrl Pts',(5.77289124600718,-5.41349253441233,-6.88041017360203));
#68462=CARTESIAN_POINT('Ctrl Pts',(6.02736796030635,-5.12655877909454,-6.86462800436428));
#68463=CARTESIAN_POINT('Ctrl Pts',(6.13225624872269,-5.00062037580189,-6.85793749115287));
#68464=CARTESIAN_POINT('Ctrl Pts',(6.26273054819979,-4.8336769845101,-6.84935359368948));
#68465=CARTESIAN_POINT('Ctrl Pts',(6.29195696899521,-4.79557135753092,-6.84741267676751));
#68466=CARTESIAN_POINT('Ctrl Pts',(6.338307652517,-4.73398578266172,-6.84430446332542));
#68467=CARTESIAN_POINT('Ctrl Pts',(6.35565257611613,-4.7106735853434,-6.84313439116604));
#68468=CARTESIAN_POINT('Ctrl Pts',(6.38688601933766,-4.66820818654298,-6.841014528845));
#68469=CARTESIAN_POINT('Ctrl Pts',(6.40081779391338,-4.64908725128004,-6.84006421447154));
#68470=CARTESIAN_POINT('Ctrl Pts',(6.43372722239032,-4.60349172491967,-6.83780790684811));
#68471=CARTESIAN_POINT('Ctrl Pts',(6.45262756650621,-4.57696182325523,-6.83650285801946));
#68472=CARTESIAN_POINT('Ctrl Pts',(6.50657196257102,-4.50024323757508,-6.83275077888843));
#68473=CARTESIAN_POINT('Ctrl Pts',(6.54119815672911,-4.44976343616691,-6.83030863296799));
#68474=CARTESIAN_POINT('Ctrl Pts',(6.73934823275084,-4.15357864077196,-6.81612608438649));
#68475=CARTESIAN_POINT('Ctrl Pts',(6.88960972709752,-3.89927100359156,-6.80449718637532));
#68476=CARTESIAN_POINT('Ctrl Pts',(7.20120056770127,-3.2974220662573,-6.77811472530825));
#68477=CARTESIAN_POINT('Ctrl Pts',(7.35221888813989,-2.94536503772033,-6.76356602237524));
#68478=CARTESIAN_POINT('Ctrl Pts',(7.62620681516148,-2.15246605789814,-6.73217600937995));
#68479=CARTESIAN_POINT('Ctrl Pts',(7.73763950277963,-1.70910858941191,-6.71550966543826));
#68480=CARTESIAN_POINT('Ctrl Pts',(7.81258143095871,-1.24406995030568,-6.69762218793949));
#68481=CARTESIAN_POINT('Ctrl Pts',(7.81488790120096,-1.22949816859579,-6.69706121136641));
#68482=CARTESIAN_POINT('Ctrl Pts',(7.81921356072185,-1.20166560061616,-6.69598870245183));
#68483=CARTESIAN_POINT('Ctrl Pts',(7.82123981214889,-1.18840595899742,-6.69547730730544));
#68484=CARTESIAN_POINT('Ctrl Pts',(7.8277380122532,-1.14514568797451,-6.69380726468019));
#68485=CARTESIAN_POINT('Ctrl Pts',(7.83207112820847,-1.1151245942258,-6.6926458242466));
#68486=CARTESIAN_POINT('Ctrl Pts',(7.8550890115713,-0.948893947528234,-6.68619817136802));
#68487=CARTESIAN_POINT('Ctrl Pts',(7.87039268466067,-0.812243716793359,
-6.6808366680563));
#68488=CARTESIAN_POINT('Ctrl Pts',(7.88353927771674,-0.658789061602054,
-6.67469009621958));
#68489=CARTESIAN_POINT('Ctrl Pts',(7.88489940862359,-0.642305131528015,
-6.67402821121943));
#68490=CARTESIAN_POINT('Ctrl Pts',(7.886874633313,-0.617414422055768,-6.67302616807881));
#68491=CARTESIAN_POINT('Ctrl Pts',(7.88752800636605,-0.609010671729094,
-6.6726874054418));
#68492=CARTESIAN_POINT('Ctrl Pts',(7.88863901477921,-0.594419038913248,
-6.67209840628921));
#68493=CARTESIAN_POINT('Ctrl Pts',(7.88910280430723,-0.588231622861941,
-6.67184839901681));
#68494=CARTESIAN_POINT('Ctrl Pts',(7.89005320214173,-0.575349050020596,
-6.67132734025234));
#68495=CARTESIAN_POINT('Ctrl Pts',(7.89053856887669,-0.568653809173042,
-6.67105624208396));
#68496=CARTESIAN_POINT('Ctrl Pts',(7.89164978450106,-0.553050116266937,
-6.67042372291975));
#68497=CARTESIAN_POINT('Ctrl Pts',(7.892269070931,-0.544141216501954,-6.67006205013621));
#68498=CARTESIAN_POINT('Ctrl Pts',(7.89418810657139,-0.515841853599745,
-6.66891143278159));
#68499=CARTESIAN_POINT('Ctrl Pts',(7.89543148405543,-0.496447732732629,
-6.66812027695225));
#68500=CARTESIAN_POINT('Ctrl Pts',(7.89815391279287,-0.451383338122713,
-6.66627550041345));
#68501=CARTESIAN_POINT('Ctrl Pts',(7.89957929282201,-0.425710138581909,
-6.66521968041488));
#68502=CARTESIAN_POINT('Ctrl Pts',(7.91256459359305,-0.169241561297714,
-6.65462020418663));
#68503=CARTESIAN_POINT('Ctrl Pts',(7.91413036463311,0.0619164898409031,
-6.64460483783473));
#68504=CARTESIAN_POINT('Ctrl Pts',(7.8923505532015,0.650005682747266,-6.61838909212137));
#68505=CARTESIAN_POINT('Ctrl Pts',(7.85492407844523,1.00591212387657,-6.60185687551704));
#68506=CARTESIAN_POINT('Ctrl Pts',(7.67830094638278,2.0195106240426,-6.55450047506731));
#68507=CARTESIAN_POINT('Ctrl Pts',(7.47928431222842,2.66369992711587,-6.52430445917238));
#68508=CARTESIAN_POINT('Ctrl Pts',(7.18326907162709,3.31458162294114,-6.49506861655921));
#68509=CARTESIAN_POINT('Ctrl Pts',(7.16497043859591,3.35395357444207,-6.49330410123121));
#68510=CARTESIAN_POINT('Ctrl Pts',(7.14017219389706,3.4061810564505,-6.49096848668932));
#68511=CARTESIAN_POINT('Ctrl Pts',(7.1339604270953,3.41917197215601,-6.4903879500562));
#68512=CARTESIAN_POINT('Ctrl Pts',(7.12422191116144,3.43939644707031,-6.48948479890236));
#68513=CARTESIAN_POINT('Ctrl Pts',(7.1207195498117,3.44664167748648,-6.48916138135952));
#68514=CARTESIAN_POINT('Ctrl Pts',(7.11369264876076,3.46112159010717,-6.48851526998474));
#68515=CARTESIAN_POINT('Ctrl Pts',(7.1101681127232,3.46835626368343,-6.48819257654265));
#68516=CARTESIAN_POINT('Ctrl Pts',(7.10220952267399,3.4846294280235,-6.48746701381496));
#68517=CARTESIAN_POINT('Ctrl Pts',(7.09776923861415,3.49366486528267,-6.4870643512981));
#68518=CARTESIAN_POINT('Ctrl Pts',(7.08465418284861,3.52022420402518,-6.48588130511104));
#68519=CARTESIAN_POINT('Ctrl Pts',(7.07593164784833,3.53772450295838,-6.48510250638997));
#68520=CARTESIAN_POINT('Ctrl Pts',(7.00900876765221,3.67075630605786,-6.47918764708619));
#68521=CARTESIAN_POINT('Ctrl Pts',(6.94804598526991,3.78487973336984,-6.47414458428931));
#68522=CARTESIAN_POINT('Ctrl Pts',(6.72663625118153,4.17596860061387,-6.45693300332377));
#68523=CARTESIAN_POINT('Ctrl Pts',(6.55220089327432,4.44466334375616,-6.44524673685178));
#68524=CARTESIAN_POINT('Ctrl Pts',(5.99681230940147,5.19611172136657,-6.41209590930528));
#68525=CARTESIAN_POINT('Ctrl Pts',(5.57538658223575,5.64591251024441,-6.39173290189985));
#68526=CARTESIAN_POINT('Ctrl Pts',(4.91838685278472,6.20111723891688,-6.36051517407707));
#68527=CARTESIAN_POINT('Ctrl Pts',(4.72328127439732,6.35098364469872,-6.35127594927098));
#68528=CARTESIAN_POINT('Ctrl Pts',(4.507418197582,6.50133812660327,-6.34077891523004));
#68529=CARTESIAN_POINT('Ctrl Pts',(4.49328676043122,6.51111283313583,-6.34009067427706));
#68530=CARTESIAN_POINT('Ctrl Pts',(4.47331793050744,6.52482929300462,-6.3391167826426));
#68531=CARTESIAN_POINT('Ctrl Pts',(4.46750687590672,6.52880945682542,-6.338833213155));
#68532=CARTESIAN_POINT('Ctrl Pts',(4.4573848190239,6.53572251260635,-6.33833900535508));
#68533=CARTESIAN_POINT('Ctrl Pts',(4.45307621264733,6.53865891684223,-6.33812855377261));
#68534=CARTESIAN_POINT('Ctrl Pts',(4.44407768582917,6.54477857920941,-6.33768885446171));
#68535=CARTESIAN_POINT('Ctrl Pts',(4.43938724129558,6.54796106052377,-6.3374595662355));
#68536=CARTESIAN_POINT('Ctrl Pts',(4.42841707301928,6.55538714879808,-6.33692308084262));
#68537=CARTESIAN_POINT('Ctrl Pts',(4.42213466940937,6.55962677355026,-6.3366156790331));
#68538=CARTESIAN_POINT('Ctrl Pts',(4.40173506148046,6.57335064448131,-6.33561699790959));
#68539=CARTESIAN_POINT('Ctrl Pts',(4.38759342296387,6.58279835596632,-6.33492388124573));
#68540=CARTESIAN_POINT('Ctrl Pts',(4.35415590536986,6.60498159539983,-6.33328334739964));
#68541=CARTESIAN_POINT('Ctrl Pts',(4.33483450040769,6.6176782456542,-6.33233407602561));
#68542=CARTESIAN_POINT('Ctrl Pts',(4.26701367169305,6.66182079917276,-6.32899817589466));
#68543=CARTESIAN_POINT('Ctrl Pts',(4.21822610840024,6.6928193105453,-6.32659166425935));
#68544=CARTESIAN_POINT('Ctrl Pts',(3.98985622621272,6.83443141243784,-6.31531072553219));
#68545=CARTESIAN_POINT('Ctrl Pts',(3.80624057010353,6.93836667378796,-6.3061968545563));
#68546=CARTESIAN_POINT('Ctrl Pts',(3.31377034648752,7.1916918735842,-6.28200069492805));
#68547=CARTESIAN_POINT('Ctrl Pts',(2.9989650574765,7.32855506027376,-6.26679406440977));
#68548=CARTESIAN_POINT('Ctrl Pts',(2.2191234370551,7.60890288476552,-6.23062978736214));
#68549=CARTESIAN_POINT('Ctrl Pts',(1.74778556160344,7.7307971844164,-6.21004761986399));
#68550=CARTESIAN_POINT('Ctrl Pts',(1.22815964623729,7.815189779488,-6.18870757379603));
#68551=CARTESIAN_POINT('Ctrl Pts',(1.18805882691241,7.82138630083705,-6.18706852957345));
#68552=CARTESIAN_POINT('Ctrl Pts',(1.12979341214207,7.82993123758557,-6.18469781123338));
#68553=CARTESIAN_POINT('Ctrl Pts',(1.11166572885928,7.83252549628893,-6.18396173610088));
#68554=CARTESIAN_POINT('Ctrl Pts',(1.07968299366997,7.83698928695997,-6.18266566509778));
#68555=CARTESIAN_POINT('Ctrl Pts',(1.0658317075291,7.8388850752775,-6.18210520963947));
#68556=CARTESIAN_POINT('Ctrl Pts',(1.03718744258772,7.84272821347573,-6.18094792420604));
#68557=CARTESIAN_POINT('Ctrl Pts',(1.02239383049002,7.84467045060511,-6.18035118484791));
#68558=CARTESIAN_POINT('Ctrl Pts',(0.984455661850834,7.84954217121539,-6.17882322750161));
#68559=CARTESIAN_POINT('Ctrl Pts',(0.961303443864271,7.85241115473449,-6.17789304132472));
#68560=CARTESIAN_POINT('Ctrl Pts',(0.870908014071688,7.86320702261716,-6.17426969528348));
#68561=CARTESIAN_POINT('Ctrl Pts',(0.803576091411761,7.87037299555759,-6.17158888697343));
#68562=CARTESIAN_POINT('Ctrl Pts',(0.423701556982069,7.90587636413933,-6.15656241190318));
#68563=CARTESIAN_POINT('Ctrl Pts',(0.109774555492435,7.91646176373229,-6.14453291973393));
#68564=CARTESIAN_POINT('Ctrl Pts',(-0.72373035540576,7.89496509585911,-6.11320465811824));
#68565=CARTESIAN_POINT('Ctrl Pts',(-1.24089743969202,7.83035244597318,-6.09445532131167));
#68566=CARTESIAN_POINT('Ctrl Pts',(-1.91007313801748,7.67874769603705,-6.0688693420363));
#68567=CARTESIAN_POINT('Ctrl Pts',(-2.07097038843757,7.63692507535028,-6.06260398268898));
#68568=CARTESIAN_POINT('Ctrl Pts',(-2.35358145886287,7.55387663278453,-6.05125959381908));
#68569=CARTESIAN_POINT('Ctrl Pts',(-2.47583373593865,7.51469515203176,-6.04623671087654));
#68570=CARTESIAN_POINT('Ctrl Pts',(-2.6120973979039,7.46733694994792,-6.04046412943302));
#68571=CARTESIAN_POINT('Ctrl Pts',(-2.62710421253011,7.46207058343734,-6.03982599134947));
#68572=CARTESIAN_POINT('Ctrl Pts',(-2.64974614242114,7.45404804589112,-6.03885944194462));
#68573=CARTESIAN_POINT('Ctrl Pts',(-2.65739311282282,7.4513253004438,-6.03853235843499));
#68574=CARTESIAN_POINT('Ctrl Pts',(-2.67066560124264,7.44657652868678,-6.03796351498088));
#68575=CARTESIAN_POINT('Ctrl Pts',(-2.6762930464999,7.44455588200309,-6.03772197284453));
#68576=CARTESIAN_POINT('Ctrl Pts',(-2.68800695926523,7.4403347689571,-6.03721843558106));
#68577=CARTESIAN_POINT('Ctrl Pts',(-2.69409302596184,7.43813321031149,-6.03695639577885));
#68578=CARTESIAN_POINT('Ctrl Pts',(-2.70614892979334,7.43375539985482,-6.03643647257837));
#68579=CARTESIAN_POINT('Ctrl Pts',(-2.71211886053426,7.43157941901413,-6.03617860059287));
#68580=CARTESIAN_POINT('Ctrl Pts',(-2.73235935578889,7.42417432067414,-6.03530289304797));
#68581=CARTESIAN_POINT('Ctrl Pts',(-2.7466174145811,7.41891129253307,-6.03468362599165));
#68582=CARTESIAN_POINT('Ctrl Pts',(-2.85822826901568,7.3773469162973,-6.02981678525168));
#68583=CARTESIAN_POINT('Ctrl Pts',(-2.95486226950634,7.33917603771479,-6.02548504179587));
#68584=CARTESIAN_POINT('Ctrl Pts',(-3.19424323362779,7.23912473227185,-6.01442979544173));
#68585=CARTESIAN_POINT('Ctrl Pts',(-3.33595529210755,7.17492263037374,-6.00760562078298));
#68586=CARTESIAN_POINT('Ctrl Pts',(-3.60462697218734,7.04352122134955,-5.99424858274313));
#68587=CARTESIAN_POINT('Ctrl Pts',(-3.73183466796555,6.97695742594686,-5.98773619813309));
#68588=CARTESIAN_POINT('Ctrl Pts',(-4.34789100008118,6.63292437542874,-5.95548552826682));
#68589=CARTESIAN_POINT('Ctrl Pts',(-4.80807413654674,6.30732654307403,-5.92928534305092));
#68590=CARTESIAN_POINT('Ctrl Pts',(-5.43886368862264,5.75154511367466,-5.89255629731899));
#68591=CARTESIAN_POINT('Ctrl Pts',(-5.637999870792,5.55648160860257,-5.88078665514577));
#68592=CARTESIAN_POINT('Ctrl Pts',(-5.84279391990271,5.33350394575173,-5.86851244551114));
#68593=CARTESIAN_POINT('Ctrl Pts',(-5.85906104673971,5.31562872991664,-5.8675361607289));
#68594=CARTESIAN_POINT('Ctrl Pts',(-5.88172418509079,5.29049479641489,-5.86617411198189));
#68595=CARTESIAN_POINT('Ctrl Pts',(-5.88818910186304,5.2832985607415,-5.86578535335069));
#68596=CARTESIAN_POINT('Ctrl Pts',(-5.89936069479567,5.27081724941683,-5.8651131821257));
#68597=CARTESIAN_POINT('Ctrl Pts',(-5.90407350197084,5.26553769027882,-5.86482950373143));
#68598=CARTESIAN_POINT('Ctrl Pts',(-5.91384140091286,5.25456552383236,-5.86424129516887));
#68599=CARTESIAN_POINT('Ctrl Pts',(-5.91889537404334,5.24887192746876,-5.86393681350339));
#68600=CARTESIAN_POINT('Ctrl Pts',(-5.93073572847056,5.23549422871883,-5.86322315051854));
#68601=CARTESIAN_POINT('Ctrl Pts',(-5.93751541497462,5.22780420424265,-5.86281425851499));
#68602=CARTESIAN_POINT('Ctrl Pts',(-5.95945688594461,5.20281881597365,-5.86149010130662));
#68603=CARTESIAN_POINT('Ctrl Pts',(-5.97455826324583,5.18547042978625,-5.86057743816256));
#68604=CARTESIAN_POINT('Ctrl Pts',(-6.24102363280973,4.87664704009835,-5.84444950590886));
#68605=CARTESIAN_POINT('Ctrl Pts',(-6.4708730901511,4.56726475939106,-5.83019586386764));
#68606=CARTESIAN_POINT('Ctrl Pts',(-6.81468299319699,4.02612020945823,-5.8075519417491));
#68607=CARTESIAN_POINT('Ctrl Pts',(-6.94147973386592,3.80334240948382,-5.79879925262536));
#68608=CARTESIAN_POINT('Ctrl Pts',(-7.10799882641336,3.47460621699002,-5.78634938312584));
#68609=CARTESIAN_POINT('Ctrl Pts',(-7.1566120820879,3.3733424523138,-5.78257397301007));
#68610=CARTESIAN_POINT('Ctrl Pts',(-7.22659820657343,3.21923002309951,-5.77688128262631));
#68611=CARTESIAN_POINT('Ctrl Pts',(-7.24958302592744,3.16712953886381,-5.7749656889427));
#68612=CARTESIAN_POINT('Ctrl Pts',(-7.29710025289357,3.05619238770104,-5.77089856835598));
#68613=CARTESIAN_POINT('Ctrl Pts',(-7.32148803492552,2.99729826849927,-5.76874633273013));
#68614=CARTESIAN_POINT('Ctrl Pts',(-7.51363986592407,2.51692711964419,-5.75120755913347));
#68615=CARTESIAN_POINT('Ctrl Pts',(-7.64556065209967,2.08207034366566,-5.7354574096765));
#68616=CARTESIAN_POINT('Ctrl Pts',(-7.74542488003577,1.61032179897296,-5.71637531943821));
#68617=CARTESIAN_POINT('Ctrl Pts',(-7.75120950260038,1.58224336761794,-5.71523212198671));
#68618=CARTESIAN_POINT('Ctrl Pts',(-7.75839358635542,1.54638688361047,-5.71376209934516));
#68619=CARTESIAN_POINT('Ctrl Pts',(-7.75993425178953,1.5386370077482,-5.71344377097987));
#68620=CARTESIAN_POINT('Ctrl Pts',(-7.76236334877504,1.52632168114289,-5.71293693922529));
#68621=CARTESIAN_POINT('Ctrl Pts',(-7.76325937285701,1.52175771471533,-5.71274889837766));
#68622=CARTESIAN_POINT('Ctrl Pts',(-7.76484569049828,1.51363982165464,-5.7124140490435));
#68623=CARTESIAN_POINT('Ctrl Pts',(-7.76553757106239,1.51008620259842,-5.71226733799124));
#68624=CARTESIAN_POINT('Ctrl Pts',(-7.76712948980867,1.50187980444965,-5.71192823384938));
#68625=CARTESIAN_POINT('Ctrl Pts',(-7.76802778597014,1.49722669454849,-5.71173573316251));
#68626=CARTESIAN_POINT('Ctrl Pts',(-7.77055799879294,1.48405680009977,-5.71119024848579));
#68627=CARTESIAN_POINT('Ctrl Pts',(-7.77218008486971,1.47553818170409,-5.71083665822949));
#68628=CARTESIAN_POINT('Ctrl Pts',(-7.77577285308339,1.45649994290278,-5.71004475959999));
#68629=CARTESIAN_POINT('Ctrl Pts',(-7.77773619732157,1.44597897254671,-5.70960600625238));
#68630=CARTESIAN_POINT('Ctrl Pts',(-7.8664562891401,0.965145930965705,-5.68950341812358));
#68631=CARTESIAN_POINT('Ctrl Pts',(-7.91039819384677,0.487989914473766,
-5.66740103070192));
#68632=CARTESIAN_POINT('Ctrl Pts',(-7.91099386085047,0.00985563728471597,
-5.64509922291617));
#68633=CARTESIAN_POINT('',(-7.8993869982124,-0.00109440781040144,-3.6423308392815));
#68634=CARTESIAN_POINT('Ctrl Pts',(-7.91099369906704,0.00998465430474249,
-5.64233150823678));
#68635=CARTESIAN_POINT('Ctrl Pts',(-7.91123261204234,-0.179309735316508,
-5.63470551807132));
#68636=CARTESIAN_POINT('Ctrl Pts',(-7.90467340181398,-0.368885852312452,
-5.62707952790585));
#68637=CARTESIAN_POINT('Ctrl Pts',(-7.89128247331207,-0.558195240393375,
-5.61945353774039));
#68638=CARTESIAN_POINT('Ctrl Pts',(-7.87790258564991,-0.747348542612155,
-5.61183383521476));
#68639=CARTESIAN_POINT('Ctrl Pts',(-7.85770221405668,-0.936235187822579,
-5.60421413268913));
#68640=CARTESIAN_POINT('Ctrl Pts',(-7.83069978419073,-1.12430506975433,
-5.5965944301635));
#68641=CARTESIAN_POINT('Ctrl Pts',(-7.80371389730901,-1.31225973105197,
-5.58897939583327));
#68642=CARTESIAN_POINT('Ctrl Pts',(-7.76993429822317,-1.49939826089422,
-5.58136436150303));
#68643=CARTESIAN_POINT('Ctrl Pts',(-7.72943137028393,-1.68517408360999,
-5.5737493271728));
#68644=CARTESIAN_POINT('Ctrl Pts',(-7.68765724127902,-1.87678055699289,
-5.56589529185552));
#68645=CARTESIAN_POINT('Ctrl Pts',(-7.63873089817577,-2.06693698902139,
-5.55804125653824));
#68646=CARTESIAN_POINT('Ctrl Pts',(-7.58278696986399,-2.25505271992938,
-5.55018722122097));
#68647=CARTESIAN_POINT('Ctrl Pts',(-7.52856777780362,-2.43736889348865,
-5.54257532369845));
#68648=CARTESIAN_POINT('Ctrl Pts',(-7.46775740041643,-2.61776795328872,
-5.53496342617593));
#68649=CARTESIAN_POINT('Ctrl Pts',(-7.40052952258955,-2.79572598537134,
-5.52735152865341));
#68650=CARTESIAN_POINT('Ctrl Pts',(-7.33329737157989,-2.97369532893992,
-5.51973914729843));
#68651=CARTESIAN_POINT('Ctrl Pts',(-7.25964703846863,-3.14922299010687,
-5.51212676594345));
#68652=CARTESIAN_POINT('Ctrl Pts',(-7.17980084906094,-3.32180384246629,
-5.50451438458848));
#68653=CARTESIAN_POINT('Ctrl Pts',(-7.09993430708423,-3.49442868519939,
-5.49690006285891));
#68654=CARTESIAN_POINT('Ctrl Pts',(-7.0138689212237,-3.66410488922804,-5.48928574112935));
#68655=CARTESIAN_POINT('Ctrl Pts',(-6.92187352593928,-3.83035088352241,
-5.48167141939978));
#68656=CARTESIAN_POINT('Ctrl Pts',(-6.82983705938048,-3.99667109821472,
-5.47405369826206));
#68657=CARTESIAN_POINT('Ctrl Pts',(-6.73186549383551,-4.15955773322744,
-5.46643597712434));
#68658=CARTESIAN_POINT('Ctrl Pts',(-6.62827156178449,-4.31855729419432,
-5.45881825598662));
#68659=CARTESIAN_POINT('Ctrl Pts',(-6.52455768577843,-4.4777409493047,-5.45119171483808));
#68660=CARTESIAN_POINT('Ctrl Pts',(-6.41520865221714,-4.63302823903928,
-5.44356517368953));
#68661=CARTESIAN_POINT('Ctrl Pts',(-6.30057859266597,-4.78399732416724,
-5.43593863254099));
#68662=CARTESIAN_POINT('Ctrl Pts',(-6.1858692800476,-4.93507078648121,-5.42830681854534));
#68663=CARTESIAN_POINT('Ctrl Pts',(-6.0658719063937,-5.08181981811388,-5.42067500454968));
#68664=CARTESIAN_POINT('Ctrl Pts',(-5.94097787625705,-5.22385900210029,
-5.41304319055403));
#68665=CARTESIAN_POINT('Ctrl Pts',(-5.81591352806535,-5.36609188499714,
-5.40540096904959));
#68666=CARTESIAN_POINT('Ctrl Pts',(-5.68593945274347,-5.5036018409918,-5.39775874754515));
#68667=CARTESIAN_POINT('Ctrl Pts',(-5.55148105358028,-5.6360428592887,-5.39011652604071));
#68668=CARTESIAN_POINT('Ctrl Pts',(-5.52295479747683,-5.66414111443715,
-5.38849517721318));
#68669=CARTESIAN_POINT('Ctrl Pts',(-5.49422680642355,-5.69201136762667,
-5.38687382838564));
#68670=CARTESIAN_POINT('Ctrl Pts',(-5.46530130986985,-5.71965056557959,
-5.38525247955811));
#68671=CARTESIAN_POINT('Ctrl Pts',(-5.32231618543271,-5.85627723165268,
-5.3772377938489));
#68672=CARTESIAN_POINT('Ctrl Pts',(-5.17402891933669,-5.98770713879432,
-5.3692231081397));
#68673=CARTESIAN_POINT('Ctrl Pts',(-5.02084751991195,-6.1135105448338,-5.36120842243049));
#68674=CARTESIAN_POINT('Ctrl Pts',(-4.8678402673753,-6.23917092912419,-5.35320284835351));
#68675=CARTESIAN_POINT('Ctrl Pts',(-4.70995022464793,-6.35921734775696,
-5.34519727427653));
#68676=CARTESIAN_POINT('Ctrl Pts',(-4.547622168603,-6.4732568009952,-5.33719170019955));
#68677=CARTESIAN_POINT('Ctrl Pts',(-4.38545113121013,-6.58718594476712,
-5.32919386985141));
#68678=CARTESIAN_POINT('Ctrl Pts',(-4.21885090741432,-6.6951195114049,-5.32119603950328));
#68679=CARTESIAN_POINT('Ctrl Pts',(-4.04829959295944,-6.79670445183874,
-5.31319820915514));
#68680=CARTESIAN_POINT('Ctrl Pts',(-3.87788434894009,-6.89820834506907,
-5.30520675969163));
#68681=CARTESIAN_POINT('Ctrl Pts',(-3.7035245830723,-6.99337353676238,-5.29721531022811));
#68682=CARTESIAN_POINT('Ctrl Pts',(-3.52572797934315,-7.0818898053893,-5.28922386076459));
#68683=CARTESIAN_POINT('Ctrl Pts',(-3.34804311232999,-7.17035044574795,
-5.28123743354728));
#68684=CARTESIAN_POINT('Ctrl Pts',(-3.16692601136339,-7.25217034356515,
-5.27325100632998));
#68685=CARTESIAN_POINT('Ctrl Pts',(-2.98290996906238,-7.32708462599336,
-5.26526457911267));
#68686=CARTESIAN_POINT('Ctrl Pts',(-2.79326282844557,-7.40429136990665,
-5.25703375822027));
#68687=CARTESIAN_POINT('Ctrl Pts',(-2.60053682217364,-7.47416296818509,
-5.24880293732788));
#68688=CARTESIAN_POINT('Ctrl Pts',(-2.40534032221803,-7.53646196396638,
-5.24057211643549));
#68689=CARTESIAN_POINT('Ctrl Pts',(-2.21606704092048,-7.59687050282723,
-5.23259105899629));
#68690=CARTESIAN_POINT('Ctrl Pts',(-2.02447134576737,-7.65015918501625,
-5.22461000155709));
#68691=CARTESIAN_POINT('Ctrl Pts',(-1.83112558464695,-7.69616138690265,
-5.2166289441179));
#68692=CARTESIAN_POINT('Ctrl Pts',(-1.63779493336743,-7.74215999374799,
-5.20864851039296));
#68693=CARTESIAN_POINT('Ctrl Pts',(-1.44271481404433,-7.78087317774757,
-5.20066807666802));
#68694=CARTESIAN_POINT('Ctrl Pts',(-1.24647002645959,-7.81218493592784,
-5.19268764294308));
#68695=CARTESIAN_POINT('Ctrl Pts',(-1.05021044938547,-7.84349905383914,
-5.18470660779305));
#68696=CARTESIAN_POINT('Ctrl Pts',(-0.852786359456356,-7.86741058177904,
-5.17672557264302));
#68697=CARTESIAN_POINT('Ctrl Pts',(-0.654790358630198,-7.88385505867814,
-5.16874453749299));
#68698=CARTESIAN_POINT('Ctrl Pts',(-0.456749041158314,-7.90030329933273,
-5.160761675671));
#68699=CARTESIAN_POINT('Ctrl Pts',(-0.258135885144651,-7.90928105529107,
-5.15277881384901));
#68700=CARTESIAN_POINT('Ctrl Pts',(-0.0595465796660957,-7.91077589145654,
-5.14479595202703));
#68701=CARTESIAN_POINT('Ctrl Pts',(0.139190089805901,-7.91227183687121,
-5.13680716649029));
#68702=CARTESIAN_POINT('Ctrl Pts',(0.337902538740874,-7.90627376810992,
-5.12881838095356));
#68703=CARTESIAN_POINT('Ctrl Pts',(0.535996089866923,-7.89282137081838,
-5.12082959541682));
#68704=CARTESIAN_POINT('Ctrl Pts',(0.73417700485295,-7.87936304070699,-5.11283728664));
#68705=CARTESIAN_POINT('Ctrl Pts',(0.931738145131561,-7.8584438580623,-5.10484497786318));
#68706=CARTESIAN_POINT('Ctrl Pts',(1.12809138442311,-7.83015522377369,-5.09685266908636));
#68707=CARTESIAN_POINT('Ctrl Pts',(1.32462835100054,-7.80184011987339,-5.08885288192413));
#68708=CARTESIAN_POINT('Ctrl Pts',(1.51995483020641,-7.76614184924864,-5.0808530947619));
#68709=CARTESIAN_POINT('Ctrl Pts',(1.71349332094594,-7.7232028096557,-5.07285330759967));
#68710=CARTESIAN_POINT('Ctrl Pts',(1.75485061222708,-7.7140271549268,-5.07114383096486));
#68711=CARTESIAN_POINT('Ctrl Pts',(1.7961263123398,-7.70452104243178,-5.06943435433005));
#68712=CARTESIAN_POINT('Ctrl Pts',(1.83731488053543,-7.69468615537782,-5.06772487769524));
#68713=CARTESIAN_POINT('Ctrl Pts',(2.03313803202395,-7.64792807026323,-5.0595974987479));
#68714=CARTESIAN_POINT('Ctrl Pts',(2.22733455925563,-7.59365244057301,-5.05147011980056));
#68715=CARTESIAN_POINT('Ctrl Pts',(2.41930691256971,-7.53199011303071,-5.04334274085322));
#68716=CARTESIAN_POINT('Ctrl Pts',(2.61111623215242,-7.47038015260884,-5.03522226413369));
#68717=CARTESIAN_POINT('Ctrl Pts',(2.8007048415114,-7.4013960978811,-5.02710178741417));
#68718=CARTESIAN_POINT('Ctrl Pts',(2.98748786274063,-7.32521926429356,-5.01898131069464));
#68719=CARTESIAN_POINT('Ctrl Pts',(3.17413574179092,-7.24909754654689,-5.01086670934275));
#68720=CARTESIAN_POINT('Ctrl Pts',(3.35798178591649,-7.16579354636245,-5.00275210799086));
#68721=CARTESIAN_POINT('Ctrl Pts',(3.53845815631536,-7.07553777998572,-4.99463750663897));
#68722=CARTESIAN_POINT('Ctrl Pts',(3.71880667200424,-6.98534595341901,-4.98652865390669));
#68723=CARTESIAN_POINT('Ctrl Pts',(3.89578999206551,-6.88821232810952,-4.97841980117441));
#68724=CARTESIAN_POINT('Ctrl Pts',(4.06886173436035,-6.78441487430258,-4.97031094844213));
#68725=CARTESIAN_POINT('Ctrl Pts',(4.2418593552487,-6.68066187381404,-4.96220556848688));
#68726=CARTESIAN_POINT('Ctrl Pts',(4.41094846573746,-6.5702508989291,-4.95410018853162));
#68727=CARTESIAN_POINT('Ctrl Pts',(4.57560795403869,-6.4535054699704,-4.94599480857636));
#68728=CARTESIAN_POINT('Ctrl Pts',(4.74021609673627,-6.33679644562211,-4.93789195611363));
#68729=CARTESIAN_POINT('Ctrl Pts',(4.90039711233585,-6.213757090812,-4.9297891036509));
#68730=CARTESIAN_POINT('Ctrl Pts',(5.05565905699076,-6.08475410345129,-4.92168625118817));
#68731=CARTESIAN_POINT('Ctrl Pts',(5.13693641523488,-6.01722292546957,-4.91744452637997));
#68732=CARTESIAN_POINT('Ctrl Pts',(5.21686626674374,-5.9480581972277,-4.91320280157177));
#68733=CARTESIAN_POINT('Ctrl Pts',(5.29538154110007,-5.87731701834916,-4.90896107676356));
#68734=CARTESIAN_POINT('Ctrl Pts',(5.44881114414081,-5.73907906295835,-4.90067216535281));
#68735=CARTESIAN_POINT('Ctrl Pts',(5.59677101776082,-5.59487825941542,-4.89238325394205));
#68736=CARTESIAN_POINT('Ctrl Pts',(5.73881466834484,-5.44517467143067,-4.8840943425313));
#68737=CARTESIAN_POINT('Ctrl Pts',(5.8809399866588,-5.29538501164937,-4.8758006654265));
#68738=CARTESIAN_POINT('Ctrl Pts',(6.01714209097839,-5.1400864644989,-4.86750698832171));
#68739=CARTESIAN_POINT('Ctrl Pts',(6.14701355777908,-4.97977362140893,-4.85921331121692));
#68740=CARTESIAN_POINT('Ctrl Pts',(6.2769675161996,-4.81935895097819,-4.85091436614314));
#68741=CARTESIAN_POINT('Ctrl Pts',(6.40058262654685,-4.65392385420555,-4.84261542106937));
#68742=CARTESIAN_POINT('Ctrl Pts',(6.51749321069374,-4.48399411781071,-4.83431647599559));
#68743=CARTESIAN_POINT('Ctrl Pts',(6.63453943639035,-4.31386722618859,-4.82600790235158));
#68744=CARTESIAN_POINT('Ctrl Pts',(6.74486542128345,-4.13923551257753,-4.81769932870756));
#68745=CARTESIAN_POINT('Ctrl Pts',(6.84814918525661,-3.9606531956824,-4.80939075506355));
#68746=CARTESIAN_POINT('Ctrl Pts',(6.95149651702649,-3.78196096718084,-4.80107706776275));
#68747=CARTESIAN_POINT('Ctrl Pts',(7.04779283552652,-3.59931353819006,-4.79276338046196));
#68748=CARTESIAN_POINT('Ctrl Pts',(7.13676258446991,-3.41328885576806,-4.78444969316117));
#68749=CARTESIAN_POINT('Ctrl Pts',(7.22582916410519,-3.22706171240935,-4.77612695761529));
#68750=CARTESIAN_POINT('Ctrl Pts',(7.30755311650373,-3.0374502357919,-4.76780422206941));
#68751=CARTESIAN_POINT('Ctrl Pts',(7.38170676735722,-2.84505293461346,-4.75948148652353));
#68752=CARTESIAN_POINT('Ctrl Pts',(7.4092801581117,-2.77351166989566,-4.7563867496264));
#68753=CARTESIAN_POINT('Ctrl Pts',(7.43580732530892,-2.7015853846223,-4.75329201272928));
#68754=CARTESIAN_POINT('Ctrl Pts',(7.46127832057214,-2.62930538792285,-4.75019727583216));
#68755=CARTESIAN_POINT('Ctrl Pts',(7.5328596305709,-2.42617642507772,-4.74150011583082));
#68756=CARTESIAN_POINT('Ctrl Pts',(7.59615934173458,-2.22007295003041,-4.73280295582949));
#68757=CARTESIAN_POINT('Ctrl Pts',(7.65095765935272,-2.01165799647753,-4.72410579582815));
#68758=CARTESIAN_POINT('Ctrl Pts',(7.70570798432838,-1.80342557379033,-4.71541625284334));
#68759=CARTESIAN_POINT('Ctrl Pts',(7.7519717245781,-1.59288593608751,-4.70672670985852));
#68760=CARTESIAN_POINT('Ctrl Pts',(7.7895791404599,-1.38071641350137,-4.69803716687371));
#68761=CARTESIAN_POINT('Ctrl Pts',(7.82802659185421,-1.16380766782672,-4.68915352587594));
#68762=CARTESIAN_POINT('Ctrl Pts',(7.85742641042037,-0.945195597718181,
-4.68026988487818));
#68763=CARTESIAN_POINT('Ctrl Pts',(7.87765192902944,-0.725617726532843,
-4.67138624388042));
#68764=CARTESIAN_POINT('Ctrl Pts',(7.89737753215061,-0.511467176185646,
-4.66272218042772));
#68765=CARTESIAN_POINT('Ctrl Pts',(7.90837690929062,-0.296398248404238,
-4.65405811697503));
#68766=CARTESIAN_POINT('Ctrl Pts',(7.91058424242814,-0.0811045217454267,
-4.64539405352233));
#68767=CARTESIAN_POINT('Ctrl Pts',(7.91287548783053,0.142373644274772,-4.63640062375203));
#68768=CARTESIAN_POINT('Ctrl Pts',(7.90569310299304,0.366093807003429,-4.62740719398174));
#68769=CARTESIAN_POINT('Ctrl Pts',(7.88902260448897,0.589273574719011,-4.61841376421144));
#68770=CARTESIAN_POINT('Ctrl Pts',(7.87235210598489,0.812453342434667,-4.60942033444114));
#68771=CARTESIAN_POINT('Ctrl Pts',(7.84619344843791,1.03509243444895,-4.60042690467084));
#68772=CARTESIAN_POINT('Ctrl Pts',(7.81059316005786,1.25640578160776,-4.59143347490053));
#68773=CARTESIAN_POINT('Ctrl Pts',(7.77966925806201,1.44864782708929,-4.5836214050135));
#68774=CARTESIAN_POINT('Ctrl Pts',(7.74163406916984,1.6398066683164,-4.57580933512647));
#68775=CARTESIAN_POINT('Ctrl Pts',(7.69659149203198,1.82931692300185,-4.56799726523944));
#68776=CARTESIAN_POINT('Ctrl Pts',(7.6515521271619,2.01881366252621,-4.56018575247995));
#68777=CARTESIAN_POINT('Ctrl Pts',(7.59950645090055,2.20666170722864,-4.55237423972046));
#68778=CARTESIAN_POINT('Ctrl Pts',(7.54060916867453,2.39230733086315,-4.54456272696097));
#68779=CARTESIAN_POINT('Ctrl Pts',(7.48170570077726,2.57797245187945,-4.53675039379945));
#68780=CARTESIAN_POINT('Ctrl Pts',(7.41594930084795,2.76143435579824,-4.52893806063793));
#68781=CARTESIAN_POINT('Ctrl Pts',(7.34354413609901,2.94215576086071,-4.5211257274764));
#68782=CARTESIAN_POINT('Ctrl Pts',(7.27108767631271,3.12300519700019,-4.51330785971079));
#68783=CARTESIAN_POINT('Ctrl Pts',(7.19197317234486,3.30110992830876,-4.50548999194517));
#68784=CARTESIAN_POINT('Ctrl Pts',(7.10645277805662,3.47595309422486,-4.49767212417955));
#68785=CARTESIAN_POINT('Ctrl Pts',(7.02090073759362,3.65086095953145,-4.48985136347112));
#68786=CARTESIAN_POINT('Ctrl Pts',(6.92893824656883,3.82250454277251,-4.4820306027627));
#68787=CARTESIAN_POINT('Ctrl Pts',(6.83086285658323,3.99039266671234,-4.47420984205427));
#68788=CARTESIAN_POINT('Ctrl Pts',(6.73267882912726,4.15846675923299,-4.46638041834017));
#68789=CARTESIAN_POINT('Ctrl Pts',(6.62836856151648,4.32277678325011,-4.45855099462607));
#68790=CARTESIAN_POINT('Ctrl Pts',(6.51827288047181,4.48286065539693,-4.45072157091198));
#68791=CARTESIAN_POINT('Ctrl Pts',(6.43365890969315,4.60589302098509,-4.44470427193101));
#68792=CARTESIAN_POINT('Ctrl Pts',(6.34562856635552,4.72642972358259,-4.43868697295005));
#68793=CARTESIAN_POINT('Ctrl Pts',(6.25435226710092,4.84427483933453,-4.43266967396909));
#68794=CARTESIAN_POINT('Ctrl Pts',(6.13121858566079,5.00325042292825,-4.42455220884504));
#68795=CARTESIAN_POINT('Ctrl Pts',(6.00193263824056,5.15764151385946,-4.41643474372099));
#68796=CARTESIAN_POINT('Ctrl Pts',(5.86686277145616,5.30696167509261,-4.40831727859694));
#68797=CARTESIAN_POINT('Ctrl Pts',(5.73189146923524,5.45617287289179,-4.40020573703249));
#68798=CARTESIAN_POINT('Ctrl Pts',(5.59114487751525,5.60032028221937,-4.39209419546804));
#68799=CARTESIAN_POINT('Ctrl Pts',(5.44503177828627,5.73895024664377,-4.3839826539036));
#68800=CARTESIAN_POINT('Ctrl Pts',(5.29900454986435,5.87749873810655,-4.37587587949982));
#68801=CARTESIAN_POINT('Ctrl Pts',(5.14761733501422,6.0105360304936,-4.36776910509605));
#68802=CARTESIAN_POINT('Ctrl Pts',(4.99131635487761,6.13764466595544,-4.35966233069228));
#68803=CARTESIAN_POINT('Ctrl Pts',(4.83508505740861,6.26469663338624,-4.35155917047996));
#68804=CARTESIAN_POINT('Ctrl Pts',(4.67394461178193,6.3858250130613,-4.34345601026764));
#68805=CARTESIAN_POINT('Ctrl Pts',(4.50837539117766,6.50065168519462,-4.33535285005532));
#68806=CARTESIAN_POINT('Ctrl Pts',(4.3428565141186,6.61544344273609,-4.32725215371769));
#68807=CARTESIAN_POINT('Ctrl Pts',(4.17291181116822,6.72393713197965,-4.31915145738006));
#68808=CARTESIAN_POINT('Ctrl Pts',(3.99905225549968,6.82579680753705,-4.31105076104244));
#68809=CARTESIAN_POINT('Ctrl Pts',(3.82385848104658,6.92843816628692,-4.30288789900342));
#68810=CARTESIAN_POINT('Ctrl Pts',(3.64468978221517,7.02434306920593,-4.2947250369644));
#68811=CARTESIAN_POINT('Ctrl Pts',(3.46209678621075,7.11321353840226,-4.28656217492539));
#68812=CARTESIAN_POINT('Ctrl Pts',(3.2808950792492,7.20140684849209,-4.27846151078422));
#68813=CARTESIAN_POINT('Ctrl Pts',(3.09632138097202,7.28267243392682,-4.27036084664305));
#68814=CARTESIAN_POINT('Ctrl Pts',(2.90893675580733,7.35676613402337,-4.26226018250188));
#68815=CARTESIAN_POINT('Ctrl Pts',(2.72152683755482,7.43086983525241,-4.25415842493691));
#68816=CARTESIAN_POINT('Ctrl Pts',(2.53130553399829,7.49779960256221,-4.24605666737194));
#68817=CARTESIAN_POINT('Ctrl Pts',(2.33885255485682,7.55735997069345,-4.23795490980697));
#68818=CARTESIAN_POINT('Ctrl Pts',(2.1463487693696,7.6169360623779,-4.22985101343024));
#68819=CARTESIAN_POINT('Ctrl Pts',(1.95161243970321,7.66913878029209,-4.2217471170535));
#68820=CARTESIAN_POINT('Ctrl Pts',(1.75523758018288,7.71382279010309,-4.21364322067677));
#68821=CARTESIAN_POINT('Ctrl Pts',(1.55632966895585,7.75908318177676,-4.20543479162921));
#68822=CARTESIAN_POINT('Ctrl Pts',(1.35574099512005,7.79662948006481,-4.19722636258165));
#68823=CARTESIAN_POINT('Ctrl Pts',(1.15409839849683,7.82636428276802,-4.1890179335341));
#68824=CARTESIAN_POINT('Ctrl Pts',(0.954765254507595,7.85575852688107,-4.18090351725171));
#68825=CARTESIAN_POINT('Ctrl Pts',(0.754402526398841,7.87751926678977,-4.17278910096933));
#68826=CARTESIAN_POINT('Ctrl Pts',(0.553620133605896,7.8916047637769,-4.16467468468694));
#68827=CARTESIAN_POINT('Ctrl Pts',(0.349348375597913,7.90593505037201,-4.1564192492568));
#68828=CARTESIAN_POINT('Ctrl Pts',(0.14464258160877,7.91232085992563,-4.14816381382666));
#68829=CARTESIAN_POINT('Ctrl Pts',(-0.0598555178725263,7.91077355996114,
-4.13990837839652));
#68830=CARTESIAN_POINT('Ctrl Pts',(-0.264353617353823,7.90922625999665,
-4.13165294296637));
#68831=CARTESIAN_POINT('Ctrl Pts',(-0.468643677552347,7.89974590077665,
-4.12339750753623));
#68832=CARTESIAN_POINT('Ctrl Pts',(-0.672089699269375,7.88239915483452,
-4.11514207210609));
#68833=CARTESIAN_POINT('Ctrl Pts',(-0.867397018831502,7.86574635216732,
-4.10721688904244));
#68834=CARTESIAN_POINT('Ctrl Pts',(-1.06234433425082,7.84180827115674,-4.09929170597879));
#68835=CARTESIAN_POINT('Ctrl Pts',(-1.2563485546642,7.81060236532325,-4.09136652291514));
#68836=CARTESIAN_POINT('Ctrl Pts',(-1.45014548666337,7.77942980218056,-4.08344980770145));
#68837=CARTESIAN_POINT('Ctrl Pts',(-1.64300099591074,7.7410049351129,-4.07553309248775));
#68838=CARTESIAN_POINT('Ctrl Pts',(-1.83433475217939,7.69539713185401,-4.06761637727406));
#68839=CARTESIAN_POINT('Ctrl Pts',(-2.02549560883702,7.64983054229206,-4.05970681603574));
#68840=CARTESIAN_POINT('Ctrl Pts',(-2.2151371210944,7.59709402576676,-4.05179725479742));
#68841=CARTESIAN_POINT('Ctrl Pts',(-2.40268653944171,7.53730843160777,-4.04388769355911));
#68842=CARTESIAN_POINT('Ctrl Pts',(-2.59007104747301,7.47757540632003,-4.03598508711838));
#68843=CARTESIAN_POINT('Ctrl Pts',(-2.77536680423015,7.410805763498,-4.02808248067766));
#68844=CARTESIAN_POINT('Ctrl Pts',(-2.95801363401451,7.33717086764267,-4.02017987423693));
#68845=CARTESIAN_POINT('Ctrl Pts',(-3.14056670573212,7.26357377077617,-4.01228132443986));
#68846=CARTESIAN_POINT('Ctrl Pts',(-3.3204732427651,7.18311856880906,-4.00438277464278));
#68847=CARTESIAN_POINT('Ctrl Pts',(-3.49718995100456,7.09602589105992,-3.9964842248457));
#68848=CARTESIAN_POINT('Ctrl Pts',(-3.67384672762452,7.00896274987965,-3.98858835375901));
#68849=CARTESIAN_POINT('Ctrl Pts',(-3.84731552410981,6.91526676854941,-3.98069248267231));
#68850=CARTESIAN_POINT('Ctrl Pts',(-4.01707442205947,6.81520609282181,-3.97279661158562));
#68851=CARTESIAN_POINT('Ctrl Pts',(-4.13473757975116,6.74585211368392,-3.96732383144857));
#68852=CARTESIAN_POINT('Ctrl Pts',(-4.25061888189729,6.67344144305843,-3.96185105131151));
#68853=CARTESIAN_POINT('Ctrl Pts',(-4.36455159383011,6.59807626394202,-3.95637827117446));
#68854=CARTESIAN_POINT('Ctrl Pts',(-4.54191027503512,6.48075553532855,-3.9478588121783));
#68855=CARTESIAN_POINT('Ctrl Pts',(-4.71436916099292,6.35639049379292,-3.93933935318213));
#68856=CARTESIAN_POINT('Ctrl Pts',(-4.88140582515869,6.22541550180442,-3.93081989418597));
#68857=CARTESIAN_POINT('Ctrl Pts',(-5.04874330922775,6.09420463414983,-3.92228509231378));
#68858=CARTESIAN_POINT('Ctrl Pts',(-5.21063885873806,5.95636017846069,-3.91375029044158));
#68859=CARTESIAN_POINT('Ctrl Pts',(-5.36660498450393,5.81235511133805,-3.90521548856939));
#68860=CARTESIAN_POINT('Ctrl Pts',(-5.53046461678876,5.66106189154434,-3.89624873704219));
#68861=CARTESIAN_POINT('Ctrl Pts',(-5.68777890979256,5.5029686325903,-3.88728198551499));
#68862=CARTESIAN_POINT('Ctrl Pts',(-5.83803014074007,5.3386632292935,-3.8783152339878));
#68863=CARTESIAN_POINT('Ctrl Pts',(-5.98164066247767,5.1816196926585,-3.86974478929332));
#68864=CARTESIAN_POINT('Ctrl Pts',(-6.11879886542661,5.01890147419976,-3.86117434459885));
#68865=CARTESIAN_POINT('Ctrl Pts',(-6.24909640662006,4.85105298886419,-3.85260389990438));
#68866=CARTESIAN_POINT('Ctrl Pts',(-6.37955677188634,4.68299475456675,-3.84402274530166));
#68867=CARTESIAN_POINT('Ctrl Pts',(-6.50313919921718,4.50979364545006,-3.83544159069893));
#68868=CARTESIAN_POINT('Ctrl Pts',(-6.61947852636648,4.33202320388211,-3.82686043609621));
#68869=CARTESIAN_POINT('Ctrl Pts',(-6.73601142072992,4.15395698503941,-3.81826500403262));
#68870=CARTESIAN_POINT('Ctrl Pts',(-6.84527698538273,3.97130644314049,-3.80966957196904));
#68871=CARTESIAN_POINT('Ctrl Pts',(-6.94695476963092,3.78467177291536,-3.80107413990545));
#68872=CARTESIAN_POINT('Ctrl Pts',(-6.96059657157506,3.75963156156588,-3.79992091668463));
#68873=CARTESIAN_POINT('Ctrl Pts',(-6.97410185734856,3.73451966479241,-3.79876769346382));
#68874=CARTESIAN_POINT('Ctrl Pts',(-6.98746991817483,3.70933756115587,-3.79761447024301));
#68875=CARTESIAN_POINT('Ctrl Pts',(-7.0819253421148,3.53140702167073,-3.78946607911621));
#68876=CARTESIAN_POINT('Ctrl Pts',(-7.16969060289945,3.34965952500846,-3.78131768798942));
#68877=CARTESIAN_POINT('Ctrl Pts',(-7.25045397823132,3.1646229016345,-3.77316929686262));
#68878=CARTESIAN_POINT('Ctrl Pts',(-7.33111179945917,2.97982811281627,-3.76503155531704));
#68879=CARTESIAN_POINT('Ctrl Pts',(-7.40478585117344,2.79175305277301,-3.75689381377146));
#68880=CARTESIAN_POINT('Ctrl Pts',(-7.47120977818801,2.60095087425884,-3.74875607222588));
#68881=CARTESIAN_POINT('Ctrl Pts',(-7.53755487966607,2.41037512144344,-3.74062798777033));
#68882=CARTESIAN_POINT('Ctrl Pts',(-7.59666690492667,2.21707899775969,-3.73249990331478));
#68883=CARTESIAN_POINT('Ctrl Pts',(-7.64832693960925,2.0216369666306,-3.72437181885923));
#68884=CARTESIAN_POINT('Ctrl Pts',(-7.69991418798707,1.82647030316878,-3.71625518645236));
#68885=CARTESIAN_POINT('Ctrl Pts',(-7.74407031092905,1.62916406731576,-3.7081385540455));
#68886=CARTESIAN_POINT('Ctrl Pts',(-7.78062571210136,1.43030924215263,-3.70002192163863));
#68887=CARTESIAN_POINT('Ctrl Pts',(-7.81715060628764,1.23162036952125,-3.6919120628954));
#68888=CARTESIAN_POINT('Ctrl Pts',(-7.84608736488076,1.03138579234293,-3.68380220415217));
#68889=CARTESIAN_POINT('Ctrl Pts',(-7.86731677212391,0.830209495885109,
-3.67569234540894));
#68890=CARTESIAN_POINT('Ctrl Pts',(-7.8885265146157,0.629219548570451,-3.6675899988093));
#68891=CARTESIAN_POINT('Ctrl Pts',(-7.90204311351956,0.42728993474177,-3.65948765220967));
#68892=CARTESIAN_POINT('Ctrl Pts',(-7.90779875925917,0.225032848844619,
-3.65138530561004));
#68893=CARTESIAN_POINT('Ctrl Pts',(-7.90994260115476,0.149696868479849,
-3.6483673731523));
#68894=CARTESIAN_POINT('Ctrl Pts',(-7.91101021264565,0.0743155299380854,
-3.64534944069455));
#68895=CARTESIAN_POINT('Ctrl Pts',(-7.91099992637351,-0.00107931383712131,
-3.6423315082368));
#68896=CARTESIAN_POINT('',(-7.91472706974257,-0.00545317307574832,-1.6423315082368));
#68897=CARTESIAN_POINT('Ctrl Pts',(-7.89505561641365,-0.00110003754996664,
-3.64233058977502));
#68898=CARTESIAN_POINT('Ctrl Pts',(-7.89694082944445,-1.34945014943438,
-3.58824934930999));
#68899=CARTESIAN_POINT('Ctrl Pts',(-6.93814504690791,-5.33560757785971,
-3.4283255748907));
#68900=CARTESIAN_POINT('Ctrl Pts',(-0.577026428184519,-9.3360978864592,
-3.16255926651691));
#68901=CARTESIAN_POINT('Ctrl Pts',(6.14476370108003,-6.1845707103362,-2.89795293163112));
#68902=CARTESIAN_POINT('Ctrl Pts',(8.15718009137018,-1.12820106384972,-2.6862678637223));
#68903=CARTESIAN_POINT('Ctrl Pts',(7.72063400436892,2.91454907120771,-2.52750406279097));
#68904=CARTESIAN_POINT('Ctrl Pts',(5.38307865781836,6.23175735845454,-2.36874026185935));
#68905=CARTESIAN_POINT('Ctrl Pts',(0.520138418637635,8.70745165738554,-2.15705519395057));
#68906=CARTESIAN_POINT('Ctrl Pts',(-5.15916039566107,7.03642133255631,-1.94537012604193));
#68907=CARTESIAN_POINT('Ctrl Pts',(-7.60147874380101,2.82410070209666,-1.75615514181166));
#68908=CARTESIAN_POINT('Ctrl Pts',(-7.910699221098,0.750269626436475,-1.67278269153563));
#68909=CARTESIAN_POINT('Ctrl Pts',(-7.91472706974257,-0.00545317307574832,
-1.6423315082368));
#68910=CARTESIAN_POINT('',(-7.91099847812363,0.00490704857253402,2.35986635990733));
#68911=CARTESIAN_POINT('Ctrl Pts',(-7.91099806737629,-0.00552973494411184,
-1.64448048805235));
#68912=CARTESIAN_POINT('Ctrl Pts',(-7.91070797338719,-0.420546550464831,
-1.62919126859007));
#68913=CARTESIAN_POINT('Ctrl Pts',(-7.87776006516516,-0.834880730787549,
-1.61380261985671));
#68914=CARTESIAN_POINT('Ctrl Pts',(-7.80961822115242,-1.2625816384502,-1.59654814058759));
#68915=CARTESIAN_POINT('Ctrl Pts',(-7.80670663640616,-1.28046110466453,
-1.59582426432029));
#68916=CARTESIAN_POINT('Ctrl Pts',(-7.80204018361664,-1.30850924782867,
-1.59468447533826));
#68917=CARTESIAN_POINT('Ctrl Pts',(-7.80032677684725,-1.31868481889568,
-1.59427009920818));
#68918=CARTESIAN_POINT('Ctrl Pts',(-7.79740034165437,-1.33585903610092,
-1.5935692111369));
#68919=CARTESIAN_POINT('Ctrl Pts',(-7.79619778471698,-1.34285946901606,
-1.59328309657582));
#68920=CARTESIAN_POINT('Ctrl Pts',(-7.79380471228816,-1.35667867224916,
-1.59271744246618));
#68921=CARTESIAN_POINT('Ctrl Pts',(-7.79261467211045,-1.36349751911817,
-1.59243792144563));
#68922=CARTESIAN_POINT('Ctrl Pts',(-7.79030506680006,-1.3766296076633,-1.59189880576414));
#68923=CARTESIAN_POINT('Ctrl Pts',(-7.78918677252919,-1.3829430692723,-1.59163926102022));
#68924=CARTESIAN_POINT('Ctrl Pts',(-7.78660690665526,-1.39740560501684,
-1.59104388216801));
#68925=CARTESIAN_POINT('Ctrl Pts',(-7.78514021703942,-1.40555374996859,
-1.59070784516098));
#68926=CARTESIAN_POINT('Ctrl Pts',(-7.78048208510383,-1.43120086749349,
-1.58964820311452));
#68927=CARTESIAN_POINT('Ctrl Pts',(-7.77724442717166,-1.44869131035915,
-1.58892273179252));
#68928=CARTESIAN_POINT('Ctrl Pts',(-7.74609651000221,-1.61384418216726,
-1.58204471188636));
#68929=CARTESIAN_POINT('Ctrl Pts',(-7.71404796349201,-1.76067087773591,
-1.57570264336101));
#68930=CARTESIAN_POINT('Ctrl Pts',(-7.63594176891085,-2.07521958455449,
-1.56164255867906));
#68931=CARTESIAN_POINT('Ctrl Pts',(-7.58849780377845,-2.24250734859104,
-1.55388807113807));
#68932=CARTESIAN_POINT('Ctrl Pts',(-7.51907591770018,-2.45974785423633,
-1.5435666628016));
#68933=CARTESIAN_POINT('Ctrl Pts',(-7.50203703623545,-2.51123522946648,
-1.54110150352093));
#68934=CARTESIAN_POINT('Ctrl Pts',(-7.45922759913177,-2.63626960696568,
-1.5350746603938));
#68935=CARTESIAN_POINT('Ctrl Pts',(-7.43289712381474,-2.70961879108291,
-1.53150485168172));
#68936=CARTESIAN_POINT('Ctrl Pts',(-7.36532492957683,-2.88945458350693,
-1.52268421783884));
#68937=CARTESIAN_POINT('Ctrl Pts',(-7.32285296860632,-2.99546046890896,
-1.51742517160671));
#68938=CARTESIAN_POINT('Ctrl Pts',(-7.18565287245346,-3.31752243423368,
-1.50132109060421));
#68939=CARTESIAN_POINT('Ctrl Pts',(-7.08354217897075,-3.53029717590608,
-1.49050810119889));
#68940=CARTESIAN_POINT('Ctrl Pts',(-6.82375730326767,-4.01481952908864,
-1.46576483303475));
#68941=CARTESIAN_POINT('Ctrl Pts',(-6.65910084583029,-4.28238753609946,
-1.45201518061746));
#68942=CARTESIAN_POINT('Ctrl Pts',(-6.40511121052275,-4.64489370772051,
-1.4334397463345));
#68943=CARTESIAN_POINT('Ctrl Pts',(-6.32869156950222,-4.7484894754258,-1.42813554445422));
#68944=CARTESIAN_POINT('Ctrl Pts',(-6.23851566709738,-4.86468709911592,
-1.4221897027533));
#68945=CARTESIAN_POINT('Ctrl Pts',(-6.22720521216287,-4.87915705349189,
-1.42144932952035));
#68946=CARTESIAN_POINT('Ctrl Pts',(-6.21006046937387,-4.90093433908402,
-1.42033513199003));
#68947=CARTESIAN_POINT('Ctrl Pts',(-6.20426348639517,-4.90827087898391,
-1.41995978154105));
#68948=CARTESIAN_POINT('Ctrl Pts',(-6.19423953133169,-4.92091085283253,
-1.41931311369865));
#68949=CARTESIAN_POINT('Ctrl Pts',(-6.19001872832958,-4.92621915227707,
-1.4190415430525));
#68950=CARTESIAN_POINT('Ctrl Pts',(-6.18128269008229,-4.93717708926443,
-1.41848094731223));
#68951=CARTESIAN_POINT('Ctrl Pts',(-6.1767665218171,-4.94282597719233,-1.41819196111892));
#68952=CARTESIAN_POINT('Ctrl Pts',(-6.16451846990933,-4.95810301596886,
-1.41741042693284));
#68953=CARTESIAN_POINT('Ctrl Pts',(-6.15677176433111,-4.96771928822333,
-1.41691849344619));
#68954=CARTESIAN_POINT('Ctrl Pts',(-6.12789659537512,-5.00339181478394,
-1.4150936351285));
#68955=CARTESIAN_POINT('Ctrl Pts',(-6.10662483825247,-5.02933190960061,
-1.41376668592546));
#68956=CARTESIAN_POINT('Ctrl Pts',(-5.7593053323447,-5.44742246665148,-1.39237807758397));
#68957=CARTESIAN_POINT('Ctrl Pts',(-5.39624641578874,-5.80728976398713,
-1.37406020294677));
#68958=CARTESIAN_POINT('Ctrl Pts',(-4.78616714225571,-6.30503123750182,
-1.3470565006893));
#68959=CARTESIAN_POINT('Ctrl Pts',(-4.56223689700481,-6.46891112938595,
-1.33778448707811));
#68960=CARTESIAN_POINT('Ctrl Pts',(-4.18709429947162,-6.71426744763681,
-1.32268488738086));
#68961=CARTESIAN_POINT('Ctrl Pts',(-4.04103041071221,-6.80317701910957,
-1.31690201547228));
#68962=CARTESIAN_POINT('Ctrl Pts',(-3.71554657031063,-6.98711737240301,
-1.30400859775547));
#68963=CARTESIAN_POINT('Ctrl Pts',(-3.5351209785516,-7.0801135735892,-1.29685687576797));
#68964=CARTESIAN_POINT('Ctrl Pts',(-3.24350152532638,-7.21649419617759,
-1.28500652317007));
#68965=CARTESIAN_POINT('Ctrl Pts',(-3.13455401997637,-7.26447929812556,
-1.28051699047033));
#68966=CARTESIAN_POINT('Ctrl Pts',(-2.97088926340818,-7.33219700491838,
-1.27362481377852));
#68967=CARTESIAN_POINT('Ctrl Pts',(-2.91696687728015,-7.35381532568079,
-1.27133060401418));
#68968=CARTESIAN_POINT('Ctrl Pts',(-2.85397638257089,-7.37826738823299,
-1.26861829431712));
#68969=CARTESIAN_POINT('Ctrl Pts',(-2.84513403529233,-7.38168159461096,
-1.26823681565075));
#68970=CARTESIAN_POINT('Ctrl Pts',(-2.83166657786943,-7.38685385493783,
-1.2676546512311));
#68971=CARTESIAN_POINT('Ctrl Pts',(-2.82704589172513,-7.38862348535168,
-1.26745470513146));
#68972=CARTESIAN_POINT('Ctrl Pts',(-2.81866367772374,-7.39182469153875,
-1.26709161307753));
#68973=CARTESIAN_POINT('Ctrl Pts',(-2.81490270832095,-7.39325773533749,
-1.26692856168842));
#68974=CARTESIAN_POINT('Ctrl Pts',(-2.80682114642696,-7.39632999578681,
-1.26657789858199));
#68975=CARTESIAN_POINT('Ctrl Pts',(-2.80250020614774,-7.39796829873965,
-1.26639022741055));
#68976=CARTESIAN_POINT('Ctrl Pts',(-2.79078695822923,-7.40239769196704,
-1.26588098484492));
#68977=CARTESIAN_POINT('Ctrl Pts',(-2.78339193380545,-7.40518148178473,
-1.26555894083732));
#68978=CARTESIAN_POINT('Ctrl Pts',(-2.74826033808485,-7.41834639259286,
-1.26402649227058));
#68979=CARTESIAN_POINT('Ctrl Pts',(-2.72047012891964,-7.42858265868971,
-1.26280684972631));
#68980=CARTESIAN_POINT('Ctrl Pts',(-2.25672778700836,-7.59644664179559,
-1.24233987309187));
#68981=CARTESIAN_POINT('Ctrl Pts',(-1.80784301261029,-7.71559775071775,
-1.22089650925874));
#68982=CARTESIAN_POINT('Ctrl Pts',(-1.01023303491929,-7.85385735937933,
-1.18313489092203));
#68983=CARTESIAN_POINT('Ctrl Pts',(-0.665779263598024,-7.8905261214945,
-1.16692665109964));
#68984=CARTESIAN_POINT('Ctrl Pts',(-0.265874501535279,-7.90671667577206,
-1.14874198714563));
#68985=CARTESIAN_POINT('Ctrl Pts',(-0.211704588242726,-7.90835249162374,
-1.14629152393641));
#68986=CARTESIAN_POINT('Ctrl Pts',(0.0427345111569161,-7.91341981469167,
-1.13484649050152));
#68987=CARTESIAN_POINT('Ctrl Pts',(0.243077960183436,-7.90980152367801,
-1.12602635486139));
#68988=CARTESIAN_POINT('Ctrl Pts',(0.551516011399111,-7.89249940201649,
-1.11278980029884));
#68989=CARTESIAN_POINT('Ctrl Pts',(0.659819631715944,-7.8841839210759,-1.10820674227161));
#68990=CARTESIAN_POINT('Ctrl Pts',(0.861927833652346,-7.86447218643965,
-1.09977622040764));
#68991=CARTESIAN_POINT('Ctrl Pts',(0.955765105246779,-7.85362058545232,
-1.0959114028739));
#68992=CARTESIAN_POINT('Ctrl Pts',(1.06569816945589,-7.83890803611238,-1.09143984305065));
#68993=CARTESIAN_POINT('Ctrl Pts',(1.08200157646206,-7.8366743188745,-1.09077814830186));
#68994=CARTESIAN_POINT('Ctrl Pts',(1.10693709615228,-7.83317862470612,-1.08976830765803));
#68995=CARTESIAN_POINT('Ctrl Pts',(1.11557423733556,-7.83195321890104,-1.08941892415491));
#68996=CARTESIAN_POINT('Ctrl Pts',(1.13061734553261,-7.82979356858565,-1.08881111116596));
#68997=CARTESIAN_POINT('Ctrl Pts',(1.13702421691485,-7.82886574409828,-1.08855246451686));
#68998=CARTESIAN_POINT('Ctrl Pts',(1.15140875222206,-7.82676458729031,-1.08797225298186));
#68999=CARTESIAN_POINT('Ctrl Pts',(1.15938578127427,-7.82558691921988,-1.08765083527731));
#69000=CARTESIAN_POINT('Ctrl Pts',(1.18066045417567,-7.82241284414174,-1.08679452407892));
#69001=CARTESIAN_POINT('Ctrl Pts',(1.19395486002662,-7.82039472193802,-1.08626036677019));
#69002=CARTESIAN_POINT('Ctrl Pts',(1.25075060217756,-7.8116247911155,-1.08398236727343));
#69003=CARTESIAN_POINT('Ctrl Pts',(1.29420072453898,-7.80454377367031,-1.08224969002801));
#69004=CARTESIAN_POINT('Ctrl Pts',(1.99390962814729,-7.68450894480091,-1.05450290009283));
#69005=CARTESIAN_POINT('Ctrl Pts',(2.63342372715673,-7.48949290158658,-1.03169454657));
#69006=CARTESIAN_POINT('Ctrl Pts',(3.54804096151581,-7.07874724116073,-0.997603411465685));
#69007=CARTESIAN_POINT('Ctrl Pts',(3.84601734449962,-6.92137177177645,-0.986165012935075));
#69008=CARTESIAN_POINT('Ctrl Pts',(4.26929569995429,-6.66202429730565,-0.968222392935882));
#69009=CARTESIAN_POINT('Ctrl Pts',(4.40297670666163,-6.57443873215262,-0.962284224711357));
#69010=CARTESIAN_POINT('Ctrl Pts',(4.58794933595095,-6.44507493774083,-0.953539397101558));
#69011=CARTESIAN_POINT('Ctrl Pts',(4.64151544608906,-6.40660627398932,-0.950941890698551));
#69012=CARTESIAN_POINT('Ctrl Pts',(4.70255212323347,-6.36160532519652,-0.947898549032821));
#69013=CARTESIAN_POINT('Ctrl Pts',(4.71050024824058,-6.35572231877995,-0.947500593127752));
#69014=CARTESIAN_POINT('Ctrl Pts',(4.72259587095616,-6.34673428482847,-0.946892459561655));
#69015=CARTESIAN_POINT('Ctrl Pts',(4.72675138046194,-6.3436400614821,-0.94668307933651));
#69016=CARTESIAN_POINT('Ctrl Pts',(4.73429367471911,-6.33801248734628,-0.946302233144981));
#69017=CARTESIAN_POINT('Ctrl Pts',(4.73768147649453,-6.33548049601496,-0.946130866319057));
#69018=CARTESIAN_POINT('Ctrl Pts',(4.74446328711433,-6.3304033926888,-0.945787218853356));
#69019=CARTESIAN_POINT('Ctrl Pts',(4.74785728261048,-6.32785826490852,-0.945614937066853));
#69020=CARTESIAN_POINT('Ctrl Pts',(4.75743391836531,-6.32066478660984,-0.945127972008277));
#69021=CARTESIAN_POINT('Ctrl Pts',(4.76361177588735,-6.31601010766409,-0.944812833507664));
#69022=CARTESIAN_POINT('Ctrl Pts',(4.78921689931841,-6.29665910565342,-0.943502576881805));
#69023=CARTESIAN_POINT('Ctrl Pts',(4.80858287796764,-6.28188228816624,-0.942501742115164));
#69024=CARTESIAN_POINT('Ctrl Pts',(5.14669103442086,-6.02141613817701,-0.924859752744621));
#69025=CARTESIAN_POINT('Ctrl Pts',(5.44626693983657,-5.75186868383697,-0.906612807897746));
#69026=CARTESIAN_POINT('Ctrl Pts',(6.08365513783509,-5.08375134754329,-0.863855741845309));
#69027=CARTESIAN_POINT('Ctrl Pts',(6.40521083473923,-4.67212253638894,-0.839252687477308));
#69028=CARTESIAN_POINT('Ctrl Pts',(6.83377908709746,-3.99522530621722,-0.803341020633583));
#69029=CARTESIAN_POINT('Ctrl Pts',(6.97093574530893,-3.75079153685194,-0.791149445951952));
#69030=CARTESIAN_POINT('Ctrl Pts',(7.14891434369575,-3.38996795678371,-0.774294417744485));
#69031=CARTESIAN_POINT('Ctrl Pts',(7.20043523327538,-3.27911470671699,-0.76926181884632));
#69032=CARTESIAN_POINT('Ctrl Pts',(7.25686990584812,-3.14993829522916,-0.763559020995201));
#69033=CARTESIAN_POINT('Ctrl Pts',(7.26431033023114,-3.13274121601342,-0.762803066681044));
#69034=CARTESIAN_POINT('Ctrl Pts',(7.27549875626116,-3.10662717431008,-0.761660024652058));
#69035=CARTESIAN_POINT('Ctrl Pts',(7.27929159372575,-3.09772956322609,-0.761271423293779));
#69036=CARTESIAN_POINT('Ctrl Pts',(7.28582859548832,-3.08231611988869,-0.760599721328862));
#69037=CARTESIAN_POINT('Ctrl Pts',(7.2885803562698,-3.07580353343402,-0.760316365093108));
#69038=CARTESIAN_POINT('Ctrl Pts',(7.29426881849362,-3.06229016235067,-0.759729352880095));
#69039=CARTESIAN_POINT('Ctrl Pts',(7.29720418124347,-3.05528881982398,-0.759425742083725));
#69040=CARTESIAN_POINT('Ctrl Pts',(7.30431188846066,-3.03826704768689,-0.758688864540792));
#69041=CARTESIAN_POINT('Ctrl Pts',(7.30847370236117,-3.02824222281788,-0.758255951145201));
#69042=CARTESIAN_POINT('Ctrl Pts',(7.32401005144308,-2.99060024919289,-0.756634383527918));
#69043=CARTESIAN_POINT('Ctrl Pts',(7.33524885315496,-2.96292716261822,-0.755450266260491));
#69044=CARTESIAN_POINT('Ctrl Pts',(7.51550318496999,-2.51177833255245,-0.736273666809861));
#69045=CARTESIAN_POINT('Ctrl Pts',(7.64776299826329,-2.07451085555215,-0.719582059124541));
#69046=CARTESIAN_POINT('Ctrl Pts',(7.79292047012449,-1.38435250328366,-0.694699569320171));
#69047=CARTESIAN_POINT('Ctrl Pts',(7.83266473521504,-1.13815920357356,-0.686085388431047));
#69048=CARTESIAN_POINT('Ctrl Pts',(7.91934534706452,-0.373002445267586,
-0.659375255157014));
#69049=CARTESIAN_POINT('Ctrl Pts',(7.92672547430411,0.149034433640475,-0.641213532891909));
#69050=CARTESIAN_POINT('Ctrl Pts',(7.88063527444379,0.692916739309235,-0.619628888839742));
#69051=CARTESIAN_POINT('Ctrl Pts',(7.87840632985506,0.717815868184812,-0.618635786452306));
#69052=CARTESIAN_POINT('Ctrl Pts',(7.87423697717383,0.762030086392197,-0.616863911955863));
#69053=CARTESIAN_POINT('Ctrl Pts',(7.87234341424318,0.781349464499339,-0.616086843472297));
#69054=CARTESIAN_POINT('Ctrl Pts',(7.86942490156779,0.810037990224005,-0.614928849662038));
#69055=CARTESIAN_POINT('Ctrl Pts',(7.8684542765683,0.819412669972078,-0.614549799489582));
#69056=CARTESIAN_POINT('Ctrl Pts',(7.86669658832682,0.836097991930503,-0.613874023862187));
#69057=CARTESIAN_POINT('Ctrl Pts',(7.86591608005126,0.843409322994656,-0.613577519258362));
#69058=CARTESIAN_POINT('Ctrl Pts',(7.86437300180108,0.857675486291132,-0.612998223314184));
#69059=CARTESIAN_POINT('Ctrl Pts',(7.86361139635321,0.864630417012092,-0.612715464047579));
#69060=CARTESIAN_POINT('Ctrl Pts',(7.86154128276495,0.883305573064439,-0.611955293238206));
#69061=CARTESIAN_POINT('Ctrl Pts',(7.86021579430281,0.895023877570837,-0.611477332697259));
#69062=CARTESIAN_POINT('Ctrl Pts',(7.85527834342043,0.937817613733295,-0.60972842908592));
#69063=CARTESIAN_POINT('Ctrl Pts',(7.85150827837333,0.968874324003153,-0.608452542842762));
#69064=CARTESIAN_POINT('Ctrl Pts',(7.84356292826639,1.03123164928963,-0.605878202209843));
#69065=CARTESIAN_POINT('Ctrl Pts',(7.83938424566032,1.06253129201032,-0.604579670384274));
#69066=CARTESIAN_POINT('Ctrl Pts',(7.75261196159212,1.68408862618775,-0.578674569797432));
#69067=CARTESIAN_POINT('Ctrl Pts',(7.60376388218453,2.26316815993202,-0.55261160637913));
#69068=CARTESIAN_POINT('Ctrl Pts',(7.15417413758989,3.44154374197199,-0.498711264590512));
#69069=CARTESIAN_POINT('Ctrl Pts',(6.83959516893831,4.03068441704745,-0.471170276337293));
#69070=CARTESIAN_POINT('Ctrl Pts',(6.4139531919229,4.63143249114936,-0.441142251657658));
#69071=CARTESIAN_POINT('Ctrl Pts',(6.37212654461508,4.68881284209148,-0.438254545741428));
#69072=CARTESIAN_POINT('Ctrl Pts',(6.29692254954123,4.7891171013521,-0.433172184716333));
#69073=CARTESIAN_POINT('Ctrl Pts',(6.26386459953239,4.83227446798347,-0.43097385477294));
#69074=CARTESIAN_POINT('Ctrl Pts',(6.2136318266942,4.8964719726484,-0.427686223426096));
#69075=CARTESIAN_POINT('Ctrl Pts',(6.19678932474537,4.91776985307694,-0.42659258467885));
#69076=CARTESIAN_POINT('Ctrl Pts',(6.16758927180125,4.95430605239585,-0.424711328350378));
#69077=CARTESIAN_POINT('Ctrl Pts',(6.15528408700467,4.96958586777552,-0.423923004641953));
#69078=CARTESIAN_POINT('Ctrl Pts',(6.12786459876445,5.00337561139661,-0.422176206930491));
#69079=CARTESIAN_POINT('Ctrl Pts',(6.11272299731516,5.02186316143138,-0.421218124267794));
#69080=CARTESIAN_POINT('Ctrl Pts',(6.0727212031794,5.07025546564848,-0.418704026470672));
#69081=CARTESIAN_POINT('Ctrl Pts',(6.04772382071143,5.10004606906802,-0.417150003606786));
#69082=CARTESIAN_POINT('Ctrl Pts',(5.94130586239131,5.22498691686365,-0.410605034737791));
#69083=CARTESIAN_POINT('Ctrl Pts',(5.85785097371095,5.31838191993731,-0.405645029565959));
#69084=CARTESIAN_POINT('Ctrl Pts',(5.28910544649948,5.92523363192547,-0.372910332478139));
#69085=CARTESIAN_POINT('Ctrl Pts',(4.73914782770694,6.37365214872079,-0.346545664554225));
#69086=CARTESIAN_POINT('Ctrl Pts',(4.05955766140335,6.79059419927379,-0.315153461703626));
#69087=CARTESIAN_POINT('Ctrl Pts',(3.98129287275165,6.83677442889766,-0.31154927778594));
#69088=CARTESIAN_POINT('Ctrl Pts',(3.88493148963935,6.89141674451312,-0.307111023233599));
#69089=CARTESIAN_POINT('Ctrl Pts',(3.86757498566901,6.90117244776157,-0.306311568841941));
#69090=CARTESIAN_POINT('Ctrl Pts',(3.83976479654112,6.91666606831036,-0.305030404086682));
#69091=CARTESIAN_POINT('Ctrl Pts',(3.82933476459057,6.92244598771006,-0.304549876060715));
#69092=CARTESIAN_POINT('Ctrl Pts',(3.80937824556347,6.93344621290674,-0.303630411447882));
#69093=CARTESIAN_POINT('Ctrl Pts',(3.79985399128274,6.93867052460989,-0.303191580958624));
#69094=CARTESIAN_POINT('Ctrl Pts',(3.77800862509917,6.95059483268709,-0.302185046728234));
#69095=CARTESIAN_POINT('Ctrl Pts',(3.76568040663823,6.95728170859277,-0.301617013265249));
#69096=CARTESIAN_POINT('Ctrl Pts',(3.73337458576308,6.97469349359763,-0.300128547657119));
#69097=CARTESIAN_POINT('Ctrl Pts',(3.71336858364658,6.98536533632033,-0.299206840023063));
#69098=CARTESIAN_POINT('Ctrl Pts',(3.57795223578291,7.0568546174443,-0.292969089914638));
#69099=CARTESIAN_POINT('Ctrl Pts',(3.46110034055326,7.11489442279348,-0.287592067721501));
#69100=CARTESIAN_POINT('Ctrl Pts',(3.11730751590049,7.27518055312138,-0.271843227594982));
#69101=CARTESIAN_POINT('Ctrl Pts',(2.88691136656942,7.36964033663553,-0.261379964145884));
#69102=CARTESIAN_POINT('Ctrl Pts',(2.28903260266111,7.58241716673477,-0.234700740342802));
#69103=CARTESIAN_POINT('Ctrl Pts',(1.91663440211766,7.68500136030606,-0.218537919435358));
#69104=CARTESIAN_POINT('Ctrl Pts',(1.43211994361865,7.78104468231371,-0.198210587883744));
#69105=CARTESIAN_POINT('Ctrl Pts',(1.32558365282905,7.79990078581564,-0.193781397102882));
#69106=CARTESIAN_POINT('Ctrl Pts',(1.1396822247639,7.82888497326154,-0.186118667146628));
#69107=CARTESIAN_POINT('Ctrl Pts',(1.06048844325414,7.84000509733572,-0.182874985068759));
#69108=CARTESIAN_POINT('Ctrl Pts',(0.94650435057953,7.8542516400622,-0.178233557223966));
#69109=CARTESIAN_POINT('Ctrl Pts',(0.911841153463279,7.85835129244421,-0.176825669192673));
#69110=CARTESIAN_POINT('Ctrl Pts',(0.851388987199748,7.8650956624587,-0.174376295178121));
#69111=CARTESIAN_POINT('Ctrl Pts',(0.825612086663567,7.86784326705346,-0.173333764103313));
#69112=CARTESIAN_POINT('Ctrl Pts',(0.775698376311015,7.87291566021252,-0.171318532955375));
#69113=CARTESIAN_POINT('Ctrl Pts',(0.751563469653224,7.87525627006728,-0.170345683737458));
#69114=CARTESIAN_POINT('Ctrl Pts',(0.693938180257213,7.88057747043656,-0.168026485486995));
#69115=CARTESIAN_POINT('Ctrl Pts',(0.660438771445761,7.88345559420831,-0.166681168220933));
#69116=CARTESIAN_POINT('Ctrl Pts',(0.538143229680081,7.89317770837378,-0.161779729055377));
#69117=CARTESIAN_POINT('Ctrl Pts',(0.449251168430254,7.89873572445625,-0.158236103399708));
#69118=CARTESIAN_POINT('Ctrl Pts',(-0.30262101528901,7.9330131444457,-0.128388214473181));
#69119=CARTESIAN_POINT('Ctrl Pts',(-0.966736730704283,7.87970754686613,
-0.102855618202846));
#69120=CARTESIAN_POINT('Ctrl Pts',(-1.9540922700405,7.67362031966792,-0.0652276877533536));
#69121=CARTESIAN_POINT('Ctrl Pts',(-2.28680759055869,7.58112335208946,-0.0525468330231455));
#69122=CARTESIAN_POINT('Ctrl Pts',(-2.7998068750244,7.40164946148996,-0.0321688780311245));
#69123=CARTESIAN_POINT('Ctrl Pts',(-2.98465607916731,7.32906247329563,-0.024642950121644));
#69124=CARTESIAN_POINT('Ctrl Pts',(-3.24550481312258,7.21512566718817,-0.013555465931551));
#69125=CARTESIAN_POINT('Ctrl Pts',(-3.32386677737193,7.17936271035362,-0.0101619727218306));
#69126=CARTESIAN_POINT('Ctrl Pts',(-3.41514486759214,7.13589032284088,-0.00611989928989754));
#69127=CARTESIAN_POINT('Ctrl Pts',(-3.42864392055163,7.12941414343657,-0.00551980286280021));
#69128=CARTESIAN_POINT('Ctrl Pts',(-3.44928301762863,7.11944034854871,-0.00459863848856003));
#69129=CARTESIAN_POINT('Ctrl Pts',(-3.45643634911771,7.11597020624632,-0.00427869598880589));
#69130=CARTESIAN_POINT('Ctrl Pts',(-3.46889405952197,7.1099036478456,-0.00372031236871105));
#69131=CARTESIAN_POINT('Ctrl Pts',(-3.47420079147166,7.10731206139989,-0.00348207349073311));
#69132=CARTESIAN_POINT('Ctrl Pts',(-3.48612209820756,7.10147365065413,-0.00294602020970374));
#69133=CARTESIAN_POINT('Ctrl Pts',(-3.49273504356157,7.09822352490751,-0.00264806555199162));
#69134=CARTESIAN_POINT('Ctrl Pts',(-3.51038891211625,7.08951637046142,-0.00185102932588452));
#69135=CARTESIAN_POINT('Ctrl Pts',(-3.52142162238392,7.08404280312358,-0.00135123093661767));
#69136=CARTESIAN_POINT('Ctrl Pts',(-3.56873522819477,7.0604316544988,0.000799598868601299));
#69137=CARTESIAN_POINT('Ctrl Pts',(-3.604888685537,7.04204116392354,0.00246194632964015));
#69138=CARTESIAN_POINT('Ctrl Pts',(-4.42321899247683,6.6178208658783,0.0405517306117198));
#69139=CARTESIAN_POINT('Ctrl Pts',(-5.13222291348374,6.08445269227029,0.0833100832995876));
#69140=CARTESIAN_POINT('Ctrl Pts',(-6.01696175696256,5.15203959842608,0.140699852691159));
#69141=CARTESIAN_POINT('Ctrl Pts',(-6.27234988840713,4.83787424741975,0.158048075558377));
#69142=CARTESIAN_POINT('Ctrl Pts',(-6.51612066530618,4.48605105140301,0.175413745633794));
#69143=CARTESIAN_POINT('Ctrl Pts',(-6.52952938742779,4.46651189985413,0.176372000855372));
#69144=CARTESIAN_POINT('Ctrl Pts',(-6.54895316415056,4.43793322739295,0.177764649949383));
#69145=CARTESIAN_POINT('Ctrl Pts',(-6.55503766567519,4.42894119172777,0.178201553671758));
#69146=CARTESIAN_POINT('Ctrl Pts',(-6.5656764029701,4.41314868974018,0.178966640012359));
#69147=CARTESIAN_POINT('Ctrl Pts',(-6.57023862568318,4.40635363859298,0.179295110308285));
#69148=CARTESIAN_POINT('Ctrl Pts',(-6.57907100052883,4.39315433580018,0.179931759899439));
#69149=CARTESIAN_POINT('Ctrl Pts',(-6.5833423662229,4.38675090900764,0.180239982664855));
#69150=CARTESIAN_POINT('Ctrl Pts',(-6.593508171665,4.3714625328864,0.180974358684691));
#69151=CARTESIAN_POINT('Ctrl Pts',(-6.59939401452939,4.36257187084997,0.181400203239108));
#69152=CARTESIAN_POINT('Ctrl Pts',(-6.61710444506986,4.33570211496103,0.182683552246976));
#69153=CARTESIAN_POINT('Ctrl Pts',(-6.62887370779771,4.31768658446259,0.183539077684414));
#69154=CARTESIAN_POINT('Ctrl Pts',(-6.74800299509092,4.1336969031297,0.192226736964433));
#69155=CARTESIAN_POINT('Ctrl Pts',(-6.84918358459858,3.96379679945411,0.199836259942572));
#69156=CARTESIAN_POINT('Ctrl Pts',(-7.26177346692412,3.20792015919807,0.232134480405514));
#69157=CARTESIAN_POINT('Ctrl Pts',(-7.50511823228193,2.58791694293089,0.254454982516534));
#69158=CARTESIAN_POINT('Ctrl Pts',(-7.77669296721741,1.51711918286306,0.29294060734452));
#69159=CARTESIAN_POINT('Ctrl Pts',(-7.84918681734211,1.08112487855704,0.308685458497038));
#69160=CARTESIAN_POINT('Ctrl Pts',(-7.8863038062427,0.624827576467823,0.326964441133551));
#69161=CARTESIAN_POINT('Ctrl Pts',(-7.88759907778965,0.608258173998842,
0.327630519167729));
#69162=CARTESIAN_POINT('Ctrl Pts',(-7.889397511442,0.584279940193138,0.328597658169758));
#69163=CARTESIAN_POINT('Ctrl Pts',(-7.88994247683504,0.576874209623265,
0.328896806957226));
#69164=CARTESIAN_POINT('Ctrl Pts',(-7.89087448147038,0.563960464715188,
0.329419211895097));
#69165=CARTESIAN_POINT('Ctrl Pts',(-7.89126618336089,0.558452783327961,
0.329642258651101));
#69166=CARTESIAN_POINT('Ctrl Pts',(-7.89201132765303,0.547818049938513,
0.330073399551271));
#69167=CARTESIAN_POINT('Ctrl Pts',(-7.89236554094427,0.542691053542111,
0.330281459459491));
#69168=CARTESIAN_POINT('Ctrl Pts',(-7.89319281065941,0.530544765385646,
0.330774856047037));
#69169=CARTESIAN_POINT('Ctrl Pts',(-7.89366149960529,0.523525188965229,
0.331060383232331));
#69170=CARTESIAN_POINT('Ctrl Pts',(-7.89503201352728,0.502578630475558,
0.33191352820109));
#69171=CARTESIAN_POINT('Ctrl Pts',(-7.89590634595267,0.488649922588824,
0.332482323923043));
#69172=CARTESIAN_POINT('Ctrl Pts',(-7.90387826652317,0.356040506440882,
0.337911262116892));
#69173=CARTESIAN_POINT('Ctrl Pts',(-7.90833619723854,0.237219840392893,
0.342879684112651));
#69174=CARTESIAN_POINT('Ctrl Pts',(-7.91067802142328,0.080697658441547,
0.349523829075627));
#69175=CARTESIAN_POINT('Ctrl Pts',(-7.91097250897623,0.0430440070615793,
0.351129753580282));
#69176=CARTESIAN_POINT('Ctrl Pts',(-7.91113408027291,-0.194096696370491,
0.361286214600696));
#69177=CARTESIAN_POINT('Ctrl Pts',(-7.90372443035215,-0.39351272728581,
0.370013797739556));
#69178=CARTESIAN_POINT('Ctrl Pts',(-7.86327959725429,-0.932075543662419,
0.393795777188776));
#69179=CARTESIAN_POINT('Ctrl Pts',(-7.81586396527105,-1.26972848142478,
0.408917764487408));
#69180=CARTESIAN_POINT('Ctrl Pts',(-7.66021932085351,-2.02178451207977,
0.442337527682981));
#69181=CARTESIAN_POINT('Ctrl Pts',(-7.53983025666885,-2.43260784721639,
0.460384148701842));
#69182=CARTESIAN_POINT('Ctrl Pts',(-7.37323433896409,-2.86719013982119,
0.479250342479628));
#69183=CARTESIAN_POINT('Ctrl Pts',(-7.35938209004656,-2.90256080052845,
0.480784677243386));
#69184=CARTESIAN_POINT('Ctrl Pts',(-7.33955573220331,-2.95213141400793,
0.482933725846532));
#69185=CARTESIAN_POINT('Ctrl Pts',(-7.33379415562166,-2.96641560082236,
0.483552844624101));
#69186=CARTESIAN_POINT('Ctrl Pts',(-7.32313780372092,-2.99261417751219,
0.484688136423428));
#69187=CARTESIAN_POINT('Ctrl Pts',(-7.31825557981575,-3.00453360398302,
0.485204565716377));
#69188=CARTESIAN_POINT('Ctrl Pts',(-7.30828851683016,-3.02869869158878,
0.486251406362699));
#69189=CARTESIAN_POINT('Ctrl Pts',(-7.30320195745272,-3.04094360020834,
0.48678178062176));
#69190=CARTESIAN_POINT('Ctrl Pts',(-7.2905666746271,-3.07114604279159,0.488089805146977));
#69191=CARTESIAN_POINT('Ctrl Pts',(-7.28298235371228,-3.08908861850425,
0.488866732386426));
#69192=CARTESIAN_POINT('Ctrl Pts',(-7.25499059363136,-3.15463388500575,
0.491704564453053));
#69193=CARTESIAN_POINT('Ctrl Pts',(-7.23418190737374,-3.20206428257444,
0.493757565627394));
#69194=CARTESIAN_POINT('Ctrl Pts',(-7.1158391955095,-3.46476658125485,0.505128828410783));
#69195=CARTESIAN_POINT('Ctrl Pts',(-7.0091601478767,-3.67579319138934,0.514257890867353));
#69196=CARTESIAN_POINT('Ctrl Pts',(-6.72152872753648,-4.18656960944573,
0.536478714487409));
#69197=CARTESIAN_POINT('Ctrl Pts',(-6.52983221270056,-4.47968921005404,
0.549331851355685));
#69198=CARTESIAN_POINT('Ctrl Pts',(-6.0109180945819,-5.16871926905778,0.580807858824923));
#69199=CARTESIAN_POINT('Ctrl Pts',(-5.66341238307279,-5.5472953081069,0.59922546479623));
#69200=CARTESIAN_POINT('Ctrl Pts',(-5.22679142747073,-5.93885713485855,
0.622136843487409));
#69201=CARTESIAN_POINT('Ctrl Pts',(-5.17113611814522,-5.98738035444429,
0.625054929994005));
#69202=CARTESIAN_POINT('Ctrl Pts',(-5.10496151252808,-6.04346387813062,
0.6285308288425));
#69203=CARTESIAN_POINT('Ctrl Pts',(-5.09509172781592,-6.0517871718369,0.629049412596094));
#69204=CARTESIAN_POINT('Ctrl Pts',(-5.07923919828449,-6.06508950883681,
0.629882670596337));
#69205=CARTESIAN_POINT('Ctrl Pts',(-5.07326937940912,-6.07008396869089,
0.630196536410737));
#69206=CARTESIAN_POINT('Ctrl Pts',(-5.06267466904515,-6.07892115030153,
0.630753704546092));
#69207=CARTESIAN_POINT('Ctrl Pts',(-5.05805274330983,-6.08276742953376,
0.630996817583994));
#69208=CARTESIAN_POINT('Ctrl Pts',(-5.04844293474478,-6.09074600435306,
0.631502404111061));
#69209=CARTESIAN_POINT('Ctrl Pts',(-5.04345435446418,-6.09487744987591,
0.631764922866609));
#69210=CARTESIAN_POINT('Ctrl Pts',(-5.03057657313571,-6.10551594241911,
0.632442775909948));
#69211=CARTESIAN_POINT('Ctrl Pts',(-5.02267983443925,-6.11201381384533,
0.63285860724703));
#69212=CARTESIAN_POINT('Ctrl Pts',(-4.98967655326645,-6.1390635779207,0.634597299212861));
#69213=CARTESIAN_POINT('Ctrl Pts',(-4.96445654791544,-6.15947602129014,
0.635927839550689));
#69214=CARTESIAN_POINT('Ctrl Pts',(-4.52838240647946,-6.5080055099179,0.658977828626436));
#69215=CARTESIAN_POINT('Ctrl Pts',(-4.08603059740957,-6.79444747358901,
0.683308073093284));
#69216=CARTESIAN_POINT('Ctrl Pts',(-3.19496179601415,-7.25280305552963,
0.729680837587388));
#69217=CARTESIAN_POINT('Ctrl Pts',(-2.75241107654865,-7.43204171326891,
0.751598835914133));
#69218=CARTESIAN_POINT('Ctrl Pts',(-2.06504167107419,-7.64054781812181,
0.782743862105871));
#69219=CARTESIAN_POINT('Ctrl Pts',(-1.83058633857419,-7.70008674145379,
0.792903000473528));
#69220=CARTESIAN_POINT('Ctrl Pts',(-1.57112006888485,-7.75345321823026,
0.803635496280399));
#69221=CARTESIAN_POINT('Ctrl Pts',(-1.54846335417354,-7.75800981768439,
0.804568504197486));
#69222=CARTESIAN_POINT('Ctrl Pts',(-1.51655999575588,-7.76428072674086,
0.805876484469635));
#69223=CARTESIAN_POINT('Ctrl Pts',(-1.50732987950346,-7.76607790712419,
0.806254220020084));
#69224=CARTESIAN_POINT('Ctrl Pts',(-1.49128717428575,-7.76917187711368,
0.806909573807847));
#69225=CARTESIAN_POINT('Ctrl Pts',(-1.48447605323501,-7.77047617202754,
0.807187442230658));
#69226=CARTESIAN_POINT('Ctrl Pts',(-1.47028193034725,-7.77317493037592,
0.807765741329133));
#69227=CARTESIAN_POINT('Ctrl Pts',(-1.46289863695209,-7.77456783566554,
0.808066119789815));
#69228=CARTESIAN_POINT('Ctrl Pts',(-1.44547582574641,-7.77782906209976,
0.808773923495439));
#69229=CARTESIAN_POINT('Ctrl Pts',(-1.43543464129414,-7.77968846893555,
0.809181051015383));
#69230=CARTESIAN_POINT('Ctrl Pts',(-1.40245943380679,-7.78572873811413,
0.81051545232933));
#69231=CARTESIAN_POINT('Ctrl Pts',(-1.3795104257884,-7.78982769030095,0.8114399931544));
#69232=CARTESIAN_POINT('Ctrl Pts',(-0.978932484073002,-7.85954973204209,
0.827506727321981));
#69233=CARTESIAN_POINT('Ctrl Pts',(-0.597028528464808,-7.8977484596977,
0.84168419610726));
#69234=CARTESIAN_POINT('Ctrl Pts',(0.301190809625515,-7.92203506861667,
0.873400238837709));
#69235=CARTESIAN_POINT('Ctrl Pts',(0.81631598619467,-7.88561832759274,0.890304356520257));
#69236=CARTESIAN_POINT('Ctrl Pts',(1.61982881854081,-7.74919126816101,0.918117963333181));
#69237=CARTESIAN_POINT('Ctrl Pts',(1.91230550033713,-7.68224420467472,0.928581740609763));
#69238=CARTESIAN_POINT('Ctrl Pts',(2.2418608423217,-7.58682127191102,0.941428481064208));
#69239=CARTESIAN_POINT('Ctrl Pts',(2.28336503064313,-7.57443338318042,0.943066079640623));
#69240=CARTESIAN_POINT('Ctrl Pts',(2.41171215342113,-7.53497444466144,0.948197036242251));
#69241=CARTESIAN_POINT('Ctrl Pts',(2.49818886956554,-7.50674673645679,0.951749500546143));
#69242=CARTESIAN_POINT('Ctrl Pts',(2.59410636589023,-7.47359645612732,0.955815888665348));
#69243=CARTESIAN_POINT('Ctrl Pts',(2.60404937473593,-7.47013779514324,0.956238941930233));
#69244=CARTESIAN_POINT('Ctrl Pts',(2.61895953425925,-7.46491793205423,0.956875663367475));
#69245=CARTESIAN_POINT('Ctrl Pts',(2.62393188039337,-7.46317159532852,0.957088391231943));
#69246=CARTESIAN_POINT('Ctrl Pts',(2.63255876116346,-7.4601320629529,0.95745814621254));
#69247=CARTESIAN_POINT('Ctrl Pts',(2.6362140586181,-7.45884116097915,0.957615026163655));
#69248=CARTESIAN_POINT('Ctrl Pts',(2.64382959650188,-7.45614536620189,0.957942311150955));
#69249=CARTESIAN_POINT('Ctrl Pts',(2.64778966820685,-7.45474000419017,0.958112745672993));
#69250=CARTESIAN_POINT('Ctrl Pts',(2.65713077838812,-7.45141662108601,0.95851534931639));
#69251=CARTESIAN_POINT('Ctrl Pts',(2.66251085660703,-7.4494959274147,0.958747685145861));
#69252=CARTESIAN_POINT('Ctrl Pts',(2.68016674107373,-7.44317118783274,0.959511622120159));
#69253=CARTESIAN_POINT('Ctrl Pts',(2.69243368049453,-7.43874263323731,0.960044735265224));
#69254=CARTESIAN_POINT('Ctrl Pts',(3.01165668557476,-7.32260513465293,0.973977959528962));
#69255=CARTESIAN_POINT('Ctrl Pts',(3.31138566483445,-7.19203077666982,0.988497039594466));
#69256=CARTESIAN_POINT('Ctrl Pts',(3.78865342200688,-6.94794253030611,1.01298277459154));
#69257=CARTESIAN_POINT('Ctrl Pts',(3.97128725472937,-6.84519357638455,1.02270760994379));
#69258=CARTESIAN_POINT('Ctrl Pts',(4.34780607817477,-6.6132206446582,1.04323951818558));
#69259=CARTESIAN_POINT('Ctrl Pts',(4.54050589649925,-6.48243131828122,1.05403563300145));
#69260=CARTESIAN_POINT('Ctrl Pts',(5.11866494297116,-6.05157720954975,1.08693784811189));
#69261=CARTESIAN_POINT('Ctrl Pts',(5.48235588577568,-5.72417726992167,1.10830267994569));
#69262=CARTESIAN_POINT('Ctrl Pts',(5.83549947986606,-5.34152711247806,1.12946528710456));
#69263=CARTESIAN_POINT('Ctrl Pts',(5.85727857190797,-5.31763611366062,1.13077276203441));
#69264=CARTESIAN_POINT('Ctrl Pts',(5.8870596111589,-5.28456227489341,1.13256398865709));
#69265=CARTESIAN_POINT('Ctrl Pts',(5.89518755413347,-5.27549362675442,1.13305320598128));
#69266=CARTESIAN_POINT('Ctrl Pts',(5.90809544553832,-5.26102473054823,1.13383069403956));
#69267=CARTESIAN_POINT('Ctrl Pts',(5.9128889893362,-5.25563667020221,1.13411955155512));
#69268=CARTESIAN_POINT('Ctrl Pts',(5.92219769285639,-5.24514460467396,1.13468073806562));
#69269=CARTESIAN_POINT('Ctrl Pts',(5.92671363823681,-5.24004130593262,1.13495310080827));
#69270=CARTESIAN_POINT('Ctrl Pts',(5.93749464532129,-5.22782633255479,1.13560359237155));
#69271=CARTESIAN_POINT('Ctrl Pts',(5.94375353854363,-5.22070921431547,1.13598145644064));
#69272=CARTESIAN_POINT('Ctrl Pts',(5.96246377845384,-5.19935615123396,1.13711171506887));
#69273=CARTESIAN_POINT('Ctrl Pts',(5.97487692086391,-5.18508673830982,1.13786247747011));
#69274=CARTESIAN_POINT('Ctrl Pts',(6.082045867785,-5.0609957958204,1.14435229051958));
#69275=CARTESIAN_POINT('Ctrl Pts',(6.17381847618985,-4.94862895776917,1.14996415952195));
#69276=CARTESIAN_POINT('Ctrl Pts',(6.39930133272391,-4.65650345354465,1.16394163762249));
#69277=CARTESIAN_POINT('Ctrl Pts',(6.52856351607667,-4.47347159755049,1.17213566413985));
#69278=CARTESIAN_POINT('Ctrl Pts',(6.8853248807192,-3.91983877512422,1.19563993270673));
#69279=CARTESIAN_POINT('Ctrl Pts',(7.09025293168861,-3.5356965918727,1.21031707315098));
#69280=CARTESIAN_POINT('Ctrl Pts',(7.4028938548105,-2.81181516262591,1.23755131853022));
#69281=CARTESIAN_POINT('Ctrl Pts',(7.52123541730029,-2.4779272566285,1.2499838263971));
#69282=CARTESIAN_POINT('Ctrl Pts',(7.64235820823402,-2.04626861047108,1.26711097783196));
#69283=CARTESIAN_POINT('Ctrl Pts',(7.66625918263362,-1.95482047471425,1.27079840807742));
#69284=CARTESIAN_POINT('Ctrl Pts',(7.6914005157306,-1.85106164863855,1.27507067218087));
#69285=CARTESIAN_POINT('Ctrl Pts',(7.69425811604767,-1.83914740096191,1.27556255849954));
#69286=CARTESIAN_POINT('Ctrl Pts',(7.69841653386357,-1.82163030066871,1.27628771891884));
#69287=CARTESIAN_POINT('Ctrl Pts',(7.69973889644629,-1.81603276606096,1.27651973258855));
#69288=CARTESIAN_POINT('Ctrl Pts',(7.702083840748,-1.80605805982674,1.27693368862337));
#69289=CARTESIAN_POINT('Ctrl Pts',(7.70310879968537,-1.80168144393878,1.27711549613169));
#69290=CARTESIAN_POINT('Ctrl Pts',(7.70524164793555,-1.79253900584068,1.27749564183167));
#69291=CARTESIAN_POINT('Ctrl Pts',(7.70634884675568,-1.78777302598855,1.27769401868533));
#69292=CARTESIAN_POINT('Ctrl Pts',(7.70921700132435,-1.77537477147594,1.27821060709812));
#69293=CARTESIAN_POINT('Ctrl Pts',(7.71097104119072,-1.76774091818448,1.2785292024733));
#69294=CARTESIAN_POINT('Ctrl Pts',(7.71843976117335,-1.73501325952487,1.27989727257737));
#69295=CARTESIAN_POINT('Ctrl Pts',(7.72404325284918,-1.7098944874602,1.28095280910065));
#69296=CARTESIAN_POINT('Ctrl Pts',(7.80280442489478,-1.34854312837109,1.2962123110058));
#69297=CARTESIAN_POINT('Ctrl Pts',(7.85406543932431,-1.00793969377509,1.31151386769961));
#69298=CARTESIAN_POINT('Ctrl Pts',(7.92949326281809,-0.113963894222885,
1.35225740440064));
#69299=CARTESIAN_POINT('Ctrl Pts',(7.91806835812111,0.440600274355359,1.37799794823071));
#69300=CARTESIAN_POINT('Ctrl Pts',(7.83210139939867,1.12254467519836,1.40818862001701));
#69301=CARTESIAN_POINT('Ctrl Pts',(7.81193879079907,1.25520247804307,1.41399988141834));
#69302=CARTESIAN_POINT('Ctrl Pts',(7.76443214114257,1.52191099476298,1.42554434086491));
#69303=CARTESIAN_POINT('Ctrl Pts',(7.73696559959172,1.65589408415447,1.43127189912038));
#69304=CARTESIAN_POINT('Ctrl Pts',(7.69155541436089,1.85148527022574,1.43952691416695));
#69305=CARTESIAN_POINT('Ctrl Pts',(7.67631485624526,1.91369090229151,1.44213648360352));
#69306=CARTESIAN_POINT('Ctrl Pts',(7.65622013014844,1.99160334154202,1.44538568792651));
#69307=CARTESIAN_POINT('Ctrl Pts',(7.65207037315818,2.00748837098475,1.44604713615625));
#69308=CARTESIAN_POINT('Ctrl Pts',(7.64546084737434,2.03247096976761,1.44708583474866));
#69309=CARTESIAN_POINT('Ctrl Pts',(7.64303423244067,2.04157721729774,1.4474641152804));
#69310=CARTESIAN_POINT('Ctrl Pts',(7.63872294567616,2.05764056914736,1.44813082337534));
#69311=CARTESIAN_POINT('Ctrl Pts',(7.63684502910415,2.06459946584801,1.44841946083274));
#69312=CARTESIAN_POINT('Ctrl Pts',(7.63252722730391,2.08051322192979,1.44907908909235));
#69313=CARTESIAN_POINT('Ctrl Pts',(7.6300810864038,2.08946638111303,1.44944988448129));
#69314=CARTESIAN_POINT('Ctrl Pts',(7.62340214184059,2.11374396206957,1.45045449464372));
#69315=CARTESIAN_POINT('Ctrl Pts',(7.61913888065585,2.1290599978215,1.45108735842495));
#69316=CARTESIAN_POINT('Ctrl Pts',(7.5969978138326,2.20768494960582,1.45433153583404));
#69317=CARTESIAN_POINT('Ctrl Pts',(7.57837677796811,2.27078274681001,1.45691956027937));
#69318=CARTESIAN_POINT('Ctrl Pts',(7.52483261717145,2.44421927038467,1.46399406323524));
#69319=CARTESIAN_POINT('Ctrl Pts',(7.48827164313876,2.55403657479191,1.46842920652532));
#69320=CARTESIAN_POINT('Ctrl Pts',(7.35250329062869,2.93382453463047,1.48364750039816));
#69321=CARTESIAN_POINT('Ctrl Pts',(7.24099469376575,3.19916239604902,1.49405608761019));
#69322=CARTESIAN_POINT('Ctrl Pts',(6.98303509029311,3.72997058145068,1.51492775467666));
#69323=CARTESIAN_POINT('Ctrl Pts',(6.83528780563502,3.99428364284762,1.5253484602029));
#69324=CARTESIAN_POINT('Ctrl Pts',(6.42659214822958,4.6360394260103,1.55183257787725));
#69325=CARTESIAN_POINT('Ctrl Pts',(6.14731621122736,5.00043674921337,1.56797806795701));
#69326=CARTESIAN_POINT('Ctrl Pts',(5.81940161360902,5.359034860021,1.58723247941226));
#69327=CARTESIAN_POINT('Ctrl Pts',(5.80058357072736,5.37939773367214,1.58833846278712));
#69328=CARTESIAN_POINT('Ctrl Pts',(5.77592680644698,5.40579883625361,1.58978955651309));
#69329=CARTESIAN_POINT('Ctrl Pts',(5.7701847865595,5.41192748098696,1.59012762127));
#69330=CARTESIAN_POINT('Ctrl Pts',(5.76133851614269,5.42133931036578,1.59064868102908));
#69331=CARTESIAN_POINT('Ctrl Pts',(5.75824117996673,5.42462901301864,1.59083116248052));
#69332=CARTESIAN_POINT('Ctrl Pts',(5.75211708184382,5.43112230584879,1.59119205698398));
#69333=CARTESIAN_POINT('Ctrl Pts',(5.74909045730042,5.43432602426156,1.59137045974044));
#69334=CARTESIAN_POINT('Ctrl Pts',(5.74238107431875,5.44141610832319,1.59176604027809));
#69335=CARTESIAN_POINT('Ctrl Pts',(5.73869704725166,5.4453012649639,1.59198331422795));
#69336=CARTESIAN_POINT('Ctrl Pts',(5.72816199187676,5.45638891644689,1.59260484223571));
#69337=CARTESIAN_POINT('Ctrl Pts',(5.7213014216135,5.46358214500764,1.59300983283677));
#69338=CARTESIAN_POINT('Ctrl Pts',(5.6733740144914,5.51364421215869,1.59584082693093));
#69339=CARTESIAN_POINT('Ctrl Pts',(5.63184040106756,5.55606142519326,1.59830291972939));
#69340=CARTESIAN_POINT('Ctrl Pts',(5.52249352897605,5.66524867711007,1.60479696528814));
#69341=CARTESIAN_POINT('Ctrl Pts',(5.45394699079058,5.73126847812177,1.60887958943954));
#69342=CARTESIAN_POINT('Ctrl Pts',(5.14181593027705,6.02122280938211,1.62744910633205));
#69343=CARTESIAN_POINT('Ctrl Pts',(4.8855256183909,6.23097211184154,1.64262759848161));
#69344=CARTESIAN_POINT('Ctrl Pts',(4.34967110798423,6.61608313900535,1.67307017565107));
#69345=CARTESIAN_POINT('Ctrl Pts',(4.07073868440935,6.79126613214633,1.68830113079214));
#69346=CARTESIAN_POINT('Ctrl Pts',(3.40527424525268,7.15343944058758,1.72243051756395));
#69347=CARTESIAN_POINT('Ctrl Pts',(3.01279290394992,7.32739678014616,1.74096206394387));
#69348=CARTESIAN_POINT('Ctrl Pts',(2.58265222392357,7.47760358057917,1.75943742532252));
#69349=CARTESIAN_POINT('Ctrl Pts',(2.55715446717307,7.48636152403647,1.76052622264357));
#69350=CARTESIAN_POINT('Ctrl Pts',(2.52199475121543,7.49823756122175,1.76201890289129));
#69351=CARTESIAN_POINT('Ctrl Pts',(2.51237096836658,7.50146760094104,1.76242657931731));
#69352=CARTESIAN_POINT('Ctrl Pts',(2.49589586770674,7.50696189440581,1.76312296303653));
#69353=CARTESIAN_POINT('Ctrl Pts',(2.48904763154708,7.50923531092091,1.7634119804516));
#69354=CARTESIAN_POINT('Ctrl Pts',(2.47572727428686,7.51363706078377,1.76397327034386));
#69355=CARTESIAN_POINT('Ctrl Pts',(2.46925549594348,7.51576640895075,1.76424557700168));
#69356=CARTESIAN_POINT('Ctrl Pts',(2.45378398475232,7.52083471354659,1.7648956047355));
#69357=CARTESIAN_POINT('Ctrl Pts',(2.44478170159639,7.52376588316435,1.76527306228048));
#69358=CARTESIAN_POINT('Ctrl Pts',(2.41818662800142,7.53237254444137,1.76638590942943));
#69359=CARTESIAN_POINT('Ctrl Pts',(2.4005791260392,7.53800255915434,1.76711976290587));
#69360=CARTESIAN_POINT('Ctrl Pts',(2.25588156018059,7.583711329935,1.77312681150086));
#69361=CARTESIAN_POINT('Ctrl Pts',(2.12781383138726,7.62063577498225,1.77829291440644));
#69362=CARTESIAN_POINT('Ctrl Pts',(1.81277731687962,7.70290540083898,1.79066719239981));
#69363=CARTESIAN_POINT('Ctrl Pts',(1.62496848516576,7.74470115482851,1.79776015246552));
#69364=CARTESIAN_POINT('Ctrl Pts',(1.15238130106175,7.83192248198373,1.81506245537962));
#69365=CARTESIAN_POINT('Ctrl Pts',(0.866293443997138,7.86870617413613,1.82504378371942));
#69366=CARTESIAN_POINT('Ctrl Pts',(-0.0524261159683648,7.93610743082871,
1.85658204200696));
#69367=CARTESIAN_POINT('Ctrl Pts',(-0.686871950875746,7.90648721083647,
1.87747032809366));
#69368=CARTESIAN_POINT('Ctrl Pts',(-1.34816033135247,7.7953711819752,1.90387280606141));
#69369=CARTESIAN_POINT('Ctrl Pts',(-1.38536970957351,7.78884451128901,1.90537474700557));
#69370=CARTESIAN_POINT('Ctrl Pts',(-1.43048245795619,7.78059806743851,1.90721709088383));
#69371=CARTESIAN_POINT('Ctrl Pts',(-1.43843233814451,7.77913226248515,1.90754256108662));
#69372=CARTESIAN_POINT('Ctrl Pts',(-1.45148191255063,7.77670548420166,1.90807816134065));
#69373=CARTESIAN_POINT('Ctrl Pts',(-1.45658294707071,7.77575167096252,1.9082878638964));
#69374=CARTESIAN_POINT('Ctrl Pts',(-1.465738948893,7.77403031674311,1.90866487862788));
#69375=CARTESIAN_POINT('Ctrl Pts',(-1.46979426541629,7.7732646197826,1.90883207960772));
#69376=CARTESIAN_POINT('Ctrl Pts',(-1.47840429542076,7.77163195451163,1.90918753416234));
#69377=CARTESIAN_POINT('Ctrl Pts',(-1.48295884755782,7.77076415504748,1.90937583817795));
#69378=CARTESIAN_POINT('Ctrl Pts',(-1.49522619049994,7.76841562476377,1.9098837678716));
#69379=CARTESIAN_POINT('Ctrl Pts',(-1.50293750640738,7.76692741888601,1.91020385210367));
#69380=CARTESIAN_POINT('Ctrl Pts',(-1.54136074899968,7.75945275801042,1.91180266677277));
#69381=CARTESIAN_POINT('Ctrl Pts',(-1.57203879797313,7.75329568796154,1.91309171154383));
#69382=CARTESIAN_POINT('Ctrl Pts',(-1.83549708248724,7.69879182440814,1.92426448270721));
#69383=CARTESIAN_POINT('Ctrl Pts',(-2.06600781666357,7.6401595897593,1.93472808542587));
#69384=CARTESIAN_POINT('Ctrl Pts',(-2.52469654079835,7.50121195800753,1.95645562050984));
#69385=CARTESIAN_POINT('Ctrl Pts',(-2.75254864587117,7.42062948669689,1.96771748595835));
#69386=CARTESIAN_POINT('Ctrl Pts',(-3.18833776494563,7.24367121757269,1.98975947015524));
#69387=CARTESIAN_POINT('Ctrl Pts',(-3.39649559556496,7.14843272975139,2.00052344681072));
#69388=CARTESIAN_POINT('Ctrl Pts',(-3.61059264032584,7.03901108946279,2.01170154648894));
#69389=CARTESIAN_POINT('Ctrl Pts',(-3.62093970458779,7.03369404995895,2.01224205106997));
#69390=CARTESIAN_POINT('Ctrl Pts',(-3.96544901597128,6.85569959776057,2.03024720333538));
#69391=CARTESIAN_POINT('Ctrl Pts',(-4.28690767162199,6.65941980550538,2.04729133160068));
#69392=CARTESIAN_POINT('Ctrl Pts',(-4.76585900725941,6.31786970092608,2.0726408058102));
#69393=CARTESIAN_POINT('Ctrl Pts',(-4.93350029482871,6.18784891863283,2.08151139185494));
#69394=CARTESIAN_POINT('Ctrl Pts',(-5.11145106485326,6.03799732800331,2.09093429012564));
#69395=CARTESIAN_POINT('Ctrl Pts',(-5.12712624877658,6.02469253648826,2.09176442033273));
#69396=CARTESIAN_POINT('Ctrl Pts',(-5.15031389465427,6.0048552760769,2.09299257989854));
#69397=CARTESIAN_POINT('Ctrl Pts',(-5.15786611694894,5.99836954685847,2.09339262077767));
#69398=CARTESIAN_POINT('Ctrl Pts',(-5.17076850775989,5.98724679336051,2.09407611574168));
#69399=CARTESIAN_POINT('Ctrl Pts',(-5.17612472163907,5.98261681807077,2.09435987391054));
#69400=CARTESIAN_POINT('Ctrl Pts',(-5.18652834594398,5.97359937078779,2.0949110655382));
#69401=CARTESIAN_POINT('Ctrl Pts',(-5.19157642193942,5.96921267684744,2.09517853232561));
#69402=CARTESIAN_POINT('Ctrl Pts',(-5.20362936303686,5.95871201691534,2.09581718544443));
#69403=CARTESIAN_POINT('Ctrl Pts',(-5.21062903145754,5.95259208628538,2.09618811251325));
#69404=CARTESIAN_POINT('Ctrl Pts',(-5.23155346318051,5.93423230700284,2.09729705197242));
#69405=CARTESIAN_POINT('Ctrl Pts',(-5.24544605218195,5.92195579445637,2.09803346861905));
#69406=CARTESIAN_POINT('Ctrl Pts',(-5.36488350044488,5.81566203810158,2.10436610445773));
#69407=CARTESIAN_POINT('Ctrl Pts',(-5.46793717313559,5.71887800009418,2.10983959434883));
#69408=CARTESIAN_POINT('Ctrl Pts',(-5.78893962350264,5.40079090319609,2.12697558305169));
#69409=CARTESIAN_POINT('Ctrl Pts',(-5.99647920700682,5.16939260293312,2.13817683724625));
#69410=CARTESIAN_POINT('Ctrl Pts',(-6.22360909018243,4.88400894421965,2.15096342024755));
#69411=CARTESIAN_POINT('Ctrl Pts',(-6.25689534504864,4.84129261450204,2.15285242656162));
#69412=CARTESIAN_POINT('Ctrl Pts',(-6.31320851777073,4.76747483548044,2.15607831746115));
#69413=CARTESIAN_POINT('Ctrl Pts',(-6.33645053399966,4.7365401660442,2.15741881856307));
#69414=CARTESIAN_POINT('Ctrl Pts',(-6.43409090880158,4.60457779256147,2.16309290320925));
#69415=CARTESIAN_POINT('Ctrl Pts',(-6.50630752206593,4.50195793057714,2.16739587818395));
#69416=CARTESIAN_POINT('Ctrl Pts',(-6.89647201577676,3.91852483104086,2.19143871543941));
#69417=CARTESIAN_POINT('Ctrl Pts',(-7.16356297767803,3.40580563186794,2.21093928248211));
#69418=CARTESIAN_POINT('Ctrl Pts',(-7.38551731810349,2.83537117864144,2.23513968744872));
#69419=CARTESIAN_POINT('Ctrl Pts',(-7.39823855945185,2.80201033778206,2.2365624603226));
#69420=CARTESIAN_POINT('Ctrl Pts',(-7.41460145233,2.75821109906044,2.23843922483164));
#69421=CARTESIAN_POINT('Ctrl Pts',(-7.41844780933309,2.74784920662286,2.23888386768796));
#69422=CARTESIAN_POINT('Ctrl Pts',(-7.42434668166966,2.7318552821801,2.2395711485841));
#69423=CARTESIAN_POINT('Ctrl Pts',(-7.42641454175537,2.7262288946686,2.23981310510466));
#69424=CARTESIAN_POINT('Ctrl Pts',(-7.43049858028765,2.71507761175493,2.2402930093324));
#69425=CARTESIAN_POINT('Ctrl Pts',(-7.43251499669349,2.70955280686344,2.24053094643773));
#69426=CARTESIAN_POINT('Ctrl Pts',(-7.43698316688266,2.69726789284315,2.24106039858926));
#69427=CARTESIAN_POINT('Ctrl Pts',(-7.43943186637629,2.69050668375757,2.24135204496635));
#69428=CARTESIAN_POINT('Ctrl Pts',(-7.44643682110039,2.6710823245341,2.24219063071053));
#69429=CARTESIAN_POINT('Ctrl Pts',(-7.45096997327485,2.65841091057888,2.24273854646207));
#69430=CARTESIAN_POINT('Ctrl Pts',(-7.48049409382297,2.57521406887332,2.24634144595223));
#69431=CARTESIAN_POINT('Ctrl Pts',(-7.50451529450351,2.50435004019854,2.24943586494628));
#69432=CARTESIAN_POINT('Ctrl Pts',(-7.57745191539672,2.27870398008065,2.25935047053162));
#69433=CARTESIAN_POINT('Ctrl Pts',(-7.62260959672493,2.12275504683166,2.26629273175166));
#69434=CARTESIAN_POINT('Ctrl Pts',(-7.82724748024627,1.32494236079879,2.30197280470235));
#69435=CARTESIAN_POINT('Ctrl Pts',(-7.91058737473885,0.666279616503375,
2.33170392820332));
#69436=CARTESIAN_POINT('Ctrl Pts',(-7.91099847169151,0.00491740731324478,
2.35986591881366));
#69437=CARTESIAN_POINT('',(-7.92581838649827,-0.00396439408934276,6.35738248087998));
#69438=CARTESIAN_POINT('Ctrl Pts',(-7.91099847812363,0.00490704857253402,
2.35986635990733));
#69439=CARTESIAN_POINT('Ctrl Pts',(-7.91117119108635,-0.273535678266459,
2.37172294511405));
#69440=CARTESIAN_POINT('Ctrl Pts',(-7.89664345732018,-0.551807601433357,
2.38331463608623));
#69441=CARTESIAN_POINT('Ctrl Pts',(-7.86391655216152,-0.862489658471575,
2.39600992918712));
#69442=CARTESIAN_POINT('Ctrl Pts',(-7.86014551404695,-0.896205594465593,
2.39738452163096));
#69443=CARTESIAN_POINT('Ctrl Pts',(-7.85384577448809,-0.949428459081086,
2.39954968758841));
#69444=CARTESIAN_POINT('Ctrl Pts',(-7.85146101062526,-0.968951934492959,
2.40034290928089));
#69445=CARTESIAN_POINT('Ctrl Pts',(-7.84728274747829,-1.00212979760632,
2.4016891634594));
#69446=CARTESIAN_POINT('Ctrl Pts',(-7.84552636178184,-1.01578873700424,
2.40224290064964));
#69447=CARTESIAN_POINT('Ctrl Pts',(-7.84219237196741,-1.04119172589804,
2.4032718138032));
#69448=CARTESIAN_POINT('Ctrl Pts',(-7.84062403131142,-1.05293694474951,
2.40374716712783));
#69449=CARTESIAN_POINT('Ctrl Pts',(-7.83732090476096,-1.07725724708036,
2.40473069278164));
#69450=CARTESIAN_POINT('Ctrl Pts',(-7.8355822280402,-1.08983177115391,2.40523878776886));
#69451=CARTESIAN_POINT('Ctrl Pts',(-7.8315399552441,-1.1185566900726,2.40639849673642));
#69452=CARTESIAN_POINT('Ctrl Pts',(-7.82921665080356,-1.13470426845318,
2.40704972023831));
#69453=CARTESIAN_POINT('Ctrl Pts',(-7.82193230767062,-1.18424476577751,
2.40904551913824));
#69454=CARTESIAN_POINT('Ctrl Pts',(-7.81680743576341,-1.21761333199256,
2.41038681807528));
#69455=CARTESIAN_POINT('Ctrl Pts',(-7.77454789171875,-1.48150044693227,
2.42097083009402));
#69456=CARTESIAN_POINT('Ctrl Pts',(-7.7274369826424,-1.71031090341293,2.43000152228597));
#69457=CARTESIAN_POINT('Ctrl Pts',(-7.65363108968939,-2.00261644581014,
2.44141846896412));
#69458=CARTESIAN_POINT('Ctrl Pts',(-7.63614130903436,-2.06830547756909,
2.44397665093341));
#69459=CARTESIAN_POINT('Ctrl Pts',(-7.58519352139753,-2.25019572634655,
2.45104585456814));
#69460=CARTESIAN_POINT('Ctrl Pts',(-7.54991457310734,-2.3658681696567,2.45552489361593));
#69461=CARTESIAN_POINT('Ctrl Pts',(-7.30324896783043,-3.11281883083619,
2.48445052846274));
#69462=CARTESIAN_POINT('Ctrl Pts',(-7.01557423291366,-3.71599447268652,
2.50754428369342));
#69463=CARTESIAN_POINT('Ctrl Pts',(-6.62879385889571,-4.31804530076434,
2.53567959958025));
#69464=CARTESIAN_POINT('Ctrl Pts',(-6.6013581777931,-4.3598730826848,2.53766455655686));
#69465=CARTESIAN_POINT('Ctrl Pts',(-6.56729567507356,-4.41074528848481,
2.54011935719801));
#69466=CARTESIAN_POINT('Ctrl Pts',(-6.56104351334651,-4.42004010138089,
2.5405695473902));
#69467=CARTESIAN_POINT('Ctrl Pts',(-6.55122760858426,-4.43456625697984,
2.54127579131269));
#69468=CARTESIAN_POINT('Ctrl Pts',(-6.54767727673166,-4.43980667895011,
2.54153112095232));
#69469=CARTESIAN_POINT('Ctrl Pts',(-6.54138019229956,-4.4490774288657,2.54198379958337));
#69470=CARTESIAN_POINT('Ctrl Pts',(-6.5386359919988,-4.45310949250267,2.54218100851659));
#69471=CARTESIAN_POINT('Ctrl Pts',(-6.53279198570338,-4.46167906391326,
2.542600852415));
#69472=CARTESIAN_POINT('Ctrl Pts',(-6.52969117829312,-4.46621588301787,
2.5428235429785));
#69473=CARTESIAN_POINT('Ctrl Pts',(-6.52082061427943,-4.47916550060539,
2.54346039102214));
#69474=CARTESIAN_POINT('Ctrl Pts',(-6.5150393240681,-4.48757035262232,2.54387519790678));
#69475=CARTESIAN_POINT('Ctrl Pts',(-6.49003457069698,-4.52377215214289,
2.54566830743923));
#69476=CARTESIAN_POINT('Ctrl Pts',(-6.47064960212792,-4.55145657290654,
2.54705601557109));
#69477=CARTESIAN_POINT('Ctrl Pts',(-6.12238390190193,-5.04210618191876,
2.57195565846574));
#69478=CARTESIAN_POINT('Ctrl Pts',(-5.74479645450918,-5.46842162690606,
2.59831288653491));
#69479=CARTESIAN_POINT('Ctrl Pts',(-5.19479843158625,-5.96899708172098,
2.63260082061013));
#69480=CARTESIAN_POINT('Ctrl Pts',(-5.06080746830011,-6.08301622487178,
2.6406920219968));
#69481=CARTESIAN_POINT('Ctrl Pts',(-4.76965145577883,-6.31449031398618,
2.65763138149675));
#69482=CARTESIAN_POINT('Ctrl Pts',(-4.61168972765105,-6.43076090356348,
2.66645361315393));
#69483=CARTESIAN_POINT('Ctrl Pts',(-4.16858514620309,-6.73218410544912,
2.69010467797355));
#69484=CARTESIAN_POINT('Ctrl Pts',(-3.87556336288559,-6.90503073090581,
2.70455630689548));
#69485=CARTESIAN_POINT('Ctrl Pts',(-3.55156860830657,-7.06900429112808,
2.71928683854302));
#69486=CARTESIAN_POINT('Ctrl Pts',(-3.53078381537044,-7.07940865526012,
2.72022664447055));
#69487=CARTESIAN_POINT('Ctrl Pts',(-3.50030023416997,-7.09450035538991,
2.72159747573838));
#69488=CARTESIAN_POINT('Ctrl Pts',(-3.49063733640822,-7.09925968033115,
2.72203091100409));
#69489=CARTESIAN_POINT('Ctrl Pts',(-3.47362699271886,-7.10759476091169,
2.72279199413157));
#69490=CARTESIAN_POINT('Ctrl Pts',(-3.46628368133205,-7.1111788903741,2.72311992155211));
#69491=CARTESIAN_POINT('Ctrl Pts',(-3.4519892222961,-7.11812833914228,2.72375704314912));
#69492=CARTESIAN_POINT('Ctrl Pts',(-3.44503867496338,-7.12149486918206,
2.72406627749625));
#69493=CARTESIAN_POINT('Ctrl Pts',(-3.4283935381111,-7.12952694782317,2.72480549479299));
#69494=CARTESIAN_POINT('Ctrl Pts',(-3.41869432778078,-7.13418291370693,
2.72523515829234));
#69495=CARTESIAN_POINT('Ctrl Pts',(-3.38374378761735,-7.15087277340537,
2.72677954923168));
#69496=CARTESIAN_POINT('Ctrl Pts',(-3.35843804304892,-7.16279256800083,
2.72789048431469));
#69497=CARTESIAN_POINT('Ctrl Pts',(-2.94919511069632,-7.35291317448888,
2.74574083558877));
#69498=CARTESIAN_POINT('Ctrl Pts',(-2.55161309007714,-7.5001602409424,2.76139689896681));
#69499=CARTESIAN_POINT('Ctrl Pts',(-1.93604453840895,-7.67348566024924,
2.78411063902228));
#69500=CARTESIAN_POINT('Ctrl Pts',(-1.72564832041538,-7.72352195122062,
2.79162663923935));
#69501=CARTESIAN_POINT('Ctrl Pts',(-1.15139415152783,-7.83545070034438,
2.81184979276966));
#69502=CARTESIAN_POINT('Ctrl Pts',(-0.784841921303233,-7.88060937406926,
2.82443900279151));
#69503=CARTESIAN_POINT('Ctrl Pts',(-0.14942285776977,-7.91410873902272,
2.84721744480106));
#69504=CARTESIAN_POINT('Ctrl Pts',(0.118183083009651,-7.91463671372961,
2.8571117548681));
#69505=CARTESIAN_POINT('Ctrl Pts',(0.427350238322998,-7.8995610819512,2.86930421417937));
#69506=CARTESIAN_POINT('Ctrl Pts',(0.469383939686272,-7.89717494674567,
2.87097695038183));
#69507=CARTESIAN_POINT('Ctrl Pts',(0.523325906304419,-7.89368063168055,
2.87314133026004));
#69508=CARTESIAN_POINT('Ctrl Pts',(0.535253974643467,-7.89288078586238,
2.87362105059203));
#69509=CARTESIAN_POINT('Ctrl Pts',(0.55445036392076,-7.89154984170729,2.87439483770193));
#69510=CARTESIAN_POINT('Ctrl Pts',(0.561719870444779,-7.89103573030265,
2.87468826854016));
#69511=CARTESIAN_POINT('Ctrl Pts',(0.575550766760856,-7.89003837761832,
2.8752473048616));
#69512=CARTESIAN_POINT('Ctrl Pts',(0.58211228760229,-7.88955699451595,2.87551284199279));
#69513=CARTESIAN_POINT('Ctrl Pts',(0.597052117007533,-7.8884422015333,2.87611816805273));
#69514=CARTESIAN_POINT('Ctrl Pts',(0.605430025316074,-7.88780362846049,
2.87645814265024));
#69515=CARTESIAN_POINT('Ctrl Pts',(0.627126312571109,-7.88611514434115,
2.87733990274209));
#69516=CARTESIAN_POINT('Ctrl Pts',(0.640443050246937,-7.88504484315655,
2.87788240465538));
#69517=CARTESIAN_POINT('Ctrl Pts',(0.721412953104962,-7.87833060732248,
2.88118863598486));
#69518=CARTESIAN_POINT('Ctrl Pts',(0.788992885828264,-7.87184982946218,
2.88398058120636));
#69519=CARTESIAN_POINT('Ctrl Pts',(1.63904736994006,-7.77927502567528,2.91944875299837));
#69520=CARTESIAN_POINT('Ctrl Pts',(2.40455097742003,-7.57772491893492,2.95443807846174));
#69521=CARTESIAN_POINT('Ctrl Pts',(3.39534916642152,-7.15125324548186,2.99980583738341));
#69522=CARTESIAN_POINT('Ctrl Pts',(3.6564173292753,-7.02135588881491,3.01185295123205));
#69523=CARTESIAN_POINT('Ctrl Pts',(4.0943334926834,-6.77240329330084,3.03248126314873));
#69524=CARTESIAN_POINT('Ctrl Pts',(4.27464074163336,-6.66006471556015,3.04113002341403));
#69525=CARTESIAN_POINT('Ctrl Pts',(4.49076480480736,-6.51301455204948,3.05170349413296));
#69526=CARTESIAN_POINT('Ctrl Pts',(4.53106222637471,-6.48504450390937,3.05368393037118));
#69527=CARTESIAN_POINT('Ctrl Pts',(4.59426448330008,-6.44029972930029,3.05680433801208));
#69528=CARTESIAN_POINT('Ctrl Pts',(4.61734353629094,-6.42377345643984,3.0579468470729));
#69529=CARTESIAN_POINT('Ctrl Pts',(4.65979178282747,-6.39303048522686,3.06005391324991));
#69530=CARTESIAN_POINT('Ctrl Pts',(4.67918611056879,-6.37884908041973,3.06101883902535));
#69531=CARTESIAN_POINT('Ctrl Pts',(4.72298911172012,-6.34651244576885,3.06320325951784));
#69532=CARTESIAN_POINT('Ctrl Pts',(4.7473582963467,-6.32830432166698,3.06442214377139));
#69533=CARTESIAN_POINT('Ctrl Pts',(4.81667963656603,-6.27588316017457,3.06789992083251));
#69534=CARTESIAN_POINT('Ctrl Pts',(4.86137129216246,-6.24132849415861,3.07015477446153));
#69535=CARTESIAN_POINT('Ctrl Pts',(5.2359751824811,-5.94522762080542,3.08916682101756));
#69536=CARTESIAN_POINT('Ctrl Pts',(5.54489849507036,-5.65820485443976,3.10555008502351));
#69537=CARTESIAN_POINT('Ctrl Pts',(6.12811823599195,-5.02246891966692,3.13890647479704));
#69538=CARTESIAN_POINT('Ctrl Pts',(6.398926856496,-4.67255186088155,3.15581394655312));
#69539=CARTESIAN_POINT('Ctrl Pts',(6.66018457722227,-4.26935178765177,3.17489461780981));
#69540=CARTESIAN_POINT('Ctrl Pts',(6.68102188037722,-4.236669669806,3.17643881478327));
#69541=CARTESIAN_POINT('Ctrl Pts',(6.71670740825333,-4.17978096574632,3.17912396493538));
#69542=CARTESIAN_POINT('Ctrl Pts',(6.73166707402852,-4.15564504259226,3.18026232398707));
#69543=CARTESIAN_POINT('Ctrl Pts',(6.75387975371021,-4.11937242215445,3.18197230549185));
#69544=CARTESIAN_POINT('Ctrl Pts',(6.7612307551626,-4.10729589311127,3.18254149137813));
#69545=CARTESIAN_POINT('Ctrl Pts',(6.77420219959194,-4.08585667969533,3.18355179338039));
#69546=CARTESIAN_POINT('Ctrl Pts',(6.77983571035995,-4.07650193028374,3.18399257238239));
#69547=CARTESIAN_POINT('Ctrl Pts',(6.7907480937362,-4.05829613687344,3.18485032715158));
#69548=CARTESIAN_POINT('Ctrl Pts',(6.79602907689711,-4.04944638096903,3.18526724613924));
#69549=CARTESIAN_POINT('Ctrl Pts',(6.8086795705797,-4.0281525133272,3.18627037838236));
#69550=CARTESIAN_POINT('Ctrl Pts',(6.81603223810991,-4.01569853108739,3.1868570499081));
#69551=CARTESIAN_POINT('Ctrl Pts',(6.84526434029541,-3.96587347398827,3.18920411243838));
#69552=CARTESIAN_POINT('Ctrl Pts',(6.86687073859161,-3.92834348108647,3.19097178729382));
#69553=CARTESIAN_POINT('Ctrl Pts',(7.05554687711995,-3.59430243083595,3.20669557740396));
#69554=CARTESIAN_POINT('Ctrl Pts',(7.2036254157549,-3.28747981349787,3.22105585821392));
#69555=CARTESIAN_POINT('Ctrl Pts',(7.50810465608365,-2.53639610702728,3.25524742932266));
#69556=CARTESIAN_POINT('Ctrl Pts',(7.64554453932837,-2.08581413408517,3.27497262594183));
#69557=CARTESIAN_POINT('Ctrl Pts',(7.75433998029619,-1.56768772902354,3.29658720617295));
#69558=CARTESIAN_POINT('Ctrl Pts',(7.76586669750839,-1.50955220488174,3.29899875893063));
#69559=CARTESIAN_POINT('Ctrl Pts',(7.78299812064975,-1.41775360174582,3.30278608454479));
#69560=CARTESIAN_POINT('Ctrl Pts',(7.78904009666747,-1.38417463074033,3.30416712400916));
#69561=CARTESIAN_POINT('Ctrl Pts',(7.79891723108562,-1.32716785757236,3.30650461162907));
#69562=CARTESIAN_POINT('Ctrl Pts',(7.80286449363473,-1.30376002328595,3.30746239696744));
#69563=CARTESIAN_POINT('Ctrl Pts',(7.81038090660719,-1.25792948567564,3.30933380841486));
#69564=CARTESIAN_POINT('Ctrl Pts',(7.81395900206547,-1.23550848456939,3.31024753259054));
#69565=CARTESIAN_POINT('Ctrl Pts',(7.82071315614648,-1.19198247552003,3.31201796040784));
#69566=CARTESIAN_POINT('Ctrl Pts',(7.82390042775347,-1.17087940996271,3.31287478834747));
#69567=CARTESIAN_POINT('Ctrl Pts',(7.83110730764892,-1.1218186621085,3.31486327872281));
#69568=CARTESIAN_POINT('Ctrl Pts',(7.83506266749147,-1.09385180840138,3.31599418864444));
#69569=CARTESIAN_POINT('Ctrl Pts',(7.84523147749112,-1.01906558960532,3.31901166697977));
#69570=CARTESIAN_POINT('Ctrl Pts',(7.85117558632553,-0.972210655273763,
3.32089517302241));
#69571=CARTESIAN_POINT('Ctrl Pts',(7.89477883026822,-0.601978622556918,
3.3357275431221));
#69572=CARTESIAN_POINT('Ctrl Pts',(7.91286345269262,-0.276602854153996,
3.34847621657132));
#69573=CARTESIAN_POINT('Ctrl Pts',(7.91001956246774,0.182893264006606,3.36634124389311));
#69574=CARTESIAN_POINT('Ctrl Pts',(7.90578954108794,0.316783449614114,3.37152171445215));
#69575=CARTESIAN_POINT('Ctrl Pts',(7.86686859743088,0.999140972472912,3.39780256674687));
#69576=CARTESIAN_POINT('Ctrl Pts',(7.77849572381311,1.54302082852759,3.41820712580402));
#69577=CARTESIAN_POINT('Ctrl Pts',(7.54549753889202,2.40096629918483,3.4515399777985));
#69578=CARTESIAN_POINT('Ctrl Pts',(7.43553052472111,2.72250565524463,3.46434922331243));
#69579=CARTESIAN_POINT('Ctrl Pts',(7.29351948429944,3.06421773268418,3.47898153986713));
#69580=CARTESIAN_POINT('Ctrl Pts',(7.28161621806224,3.09239745321008,3.48019613629088));
#69581=CARTESIAN_POINT('Ctrl Pts',(7.26065538980941,3.14122790785675,3.48231552431692));
#69582=CARTESIAN_POINT('Ctrl Pts',(7.25167238465197,3.16191035188239,3.48321781660625));
#69583=CARTESIAN_POINT('Ctrl Pts',(7.23857690169577,3.19171200169049,3.48452492194868));
#69584=CARTESIAN_POINT('Ctrl Pts',(7.23453532058555,3.20086234594562,3.48492721076003));
#69585=CARTESIAN_POINT('Ctrl Pts',(7.22746816379373,3.21678098495243,3.48562875691541));
#69586=CARTESIAN_POINT('Ctrl Pts',(7.22445040397407,3.22355274874229,3.48592772833631));
#69587=CARTESIAN_POINT('Ctrl Pts',(7.21861380171799,3.23660054937353,3.48650483155131));
#69588=CARTESIAN_POINT('Ctrl Pts',(7.21579628196911,3.24287717178979,3.48678291385445));
#69589=CARTESIAN_POINT('Ctrl Pts',(7.20911473914521,3.2577099035395,3.48744119121204));
#69590=CARTESIAN_POINT('Ctrl Pts',(7.20524367080158,3.26626281570605,3.48782165341119));
#69591=CARTESIAN_POINT('Ctrl Pts',(7.19167390179325,3.29610295677496,3.48915218547146));
#69592=CARTESIAN_POINT('Ctrl Pts',(7.18189606841672,3.31735392435872,3.49010532991368));
#69593=CARTESIAN_POINT('Ctrl Pts',(7.01714768936195,3.67127267413449,3.50607684616359));
#69594=CARTESIAN_POINT('Ctrl Pts',(6.83934332957474,3.99272791060968,3.52225070098082));
#69595=CARTESIAN_POINT('Ctrl Pts',(6.35551397120063,4.73973229419203,3.56259390955272));
#69596=CARTESIAN_POINT('Ctrl Pts',(6.02822946432228,5.14957519898245,3.58694305838343));
#69597=CARTESIAN_POINT('Ctrl Pts',(5.40996110519929,5.78337530592687,3.62617854477727));
#69598=CARTESIAN_POINT('Ctrl Pts',(5.13952089636872,6.02498777118756,3.6416487917214));
#69599=CARTESIAN_POINT('Ctrl Pts',(4.83367092808728,6.26260118485098,3.65735972996765));
#69600=CARTESIAN_POINT('Ctrl Pts',(4.81382034473135,6.27787240591909,3.65837201047308));
#69601=CARTESIAN_POINT('Ctrl Pts',(4.78523467972665,6.29964829588114,3.65981919486222));
#69602=CARTESIAN_POINT('Ctrl Pts',(4.77655826305,6.30622951951161,3.66025706519359));
#69603=CARTESIAN_POINT('Ctrl Pts',(4.76149894632268,6.31760338212437,3.66101467053474));
#69604=CARTESIAN_POINT('Ctrl Pts',(4.75512234191113,6.32240430719077,3.66133472583254));
#69605=CARTESIAN_POINT('Ctrl Pts',(4.74286348276394,6.33160492621358,3.6619486082152));
#69606=CARTESIAN_POINT('Ctrl Pts',(4.73698234716823,6.3360060922281,3.66224249198448));
#69607=CARTESIAN_POINT('Ctrl Pts',(4.72313814712758,6.34633639257582,3.66293283218992));
#69608=CARTESIAN_POINT('Ctrl Pts',(4.71517002566562,6.35225874745336,3.66332902717017));
#69609=CARTESIAN_POINT('Ctrl Pts',(4.6877075603652,6.37259024883434,3.66469063914138));
#69610=CARTESIAN_POINT('Ctrl Pts',(4.66815805874853,6.38692484712394,3.66565318897203));
#69611=CARTESIAN_POINT('Ctrl Pts',(4.45010041231214,6.54527877384177,3.67631554406752));
#69612=CARTESIAN_POINT('Ctrl Pts',(4.24505636357455,6.68008807100873,3.68565616258135));
#69613=CARTESIAN_POINT('Ctrl Pts',(3.91670519074361,6.87473314761765,3.69971916906134));
#69614=CARTESIAN_POINT('Ctrl Pts',(3.79755961984533,6.9412591075866,3.70465048431178));
#69615=CARTESIAN_POINT('Ctrl Pts',(3.1580822444697,7.27692060455967,3.730353911298));
#69616=CARTESIAN_POINT('Ctrl Pts',(2.61081017483483,7.49070724770031,3.74958215182077));
#69617=CARTESIAN_POINT('Ctrl Pts',(1.85476871750775,7.69301762122654,3.77688909637846));
#69618=CARTESIAN_POINT('Ctrl Pts',(1.6627428849949,7.73679307335058,3.78390077453241));
#69619=CARTESIAN_POINT('Ctrl Pts',(1.35524022414728,7.79491614191002,3.79549970454625));
#69620=CARTESIAN_POINT('Ctrl Pts',(1.24073119804129,7.81396044405406,3.79989968273087));
#69621=CARTESIAN_POINT('Ctrl Pts',(1.06962068979217,7.83856234077358,3.80664443465385));
#69622=CARTESIAN_POINT('Ctrl Pts',(1.01330811241883,7.84604068105439,3.80889137889274));
#69623=CARTESIAN_POINT('Ctrl Pts',(0.947221135914901,7.85409374831722,3.81156486221682));
#69624=CARTESIAN_POINT('Ctrl Pts',(0.937518966538457,7.85525777256611,3.81195827497018));
#69625=CARTESIAN_POINT('Ctrl Pts',(0.922689783331571,7.85700904892436,3.81256102073576));
#69626=CARTESIAN_POINT('Ctrl Pts',(0.917564281063219,7.85760926879306,3.81276961387849));
#69627=CARTESIAN_POINT('Ctrl Pts',(0.908643596861281,7.85864507450734,3.81313312171755));
#69628=CARTESIAN_POINT('Ctrl Pts',(0.904848674809405,7.85908292797527,3.81328790590078));
#69629=CARTESIAN_POINT('Ctrl Pts',(0.896932264124252,7.85999050386975,3.81361109973172));
#69630=CARTESIAN_POINT('Ctrl Pts',(0.892810721160892,7.86045973359108,3.81377953785291));
#69631=CARTESIAN_POINT('Ctrl Pts',(0.882719046163696,7.86160061178409,3.8141923885795));
#69632=CARTESIAN_POINT('Ctrl Pts',(0.876748523155292,7.86226870059873,3.81443700851683));
#69633=CARTESIAN_POINT('Ctrl Pts',(0.853447245596857,7.86484919192799,3.81539313651795));
#69634=CARTESIAN_POINT('Ctrl Pts',(0.836111262273416,7.86671106313678,3.81610763240073));
#69635=CARTESIAN_POINT('Ctrl Pts',(0.528966353275871,7.89867145949238,3.82882045732331));
#69636=CARTESIAN_POINT('Ctrl Pts',(0.237742187972288,7.91279119943711,3.84171714842958));
#69637=CARTESIAN_POINT('Ctrl Pts',(-0.560954793583377,7.90738293822852,
3.87808166650427));
#69638=CARTESIAN_POINT('Ctrl Pts',(-1.06684049781057,7.85514270765737,3.90213283668487));
#69639=CARTESIAN_POINT('Ctrl Pts',(-1.84139764805392,7.69890288191097,3.93796218045429));
#69640=CARTESIAN_POINT('Ctrl Pts',(-2.11535357974377,7.62818138055529,3.95045526521643));
#69641=CARTESIAN_POINT('Ctrl Pts',(-2.49314758242171,7.50872906595663,3.96728829589015));
#69642=CARTESIAN_POINT('Ctrl Pts',(-2.60059523152472,7.47219532704595,3.97203117891056));
#69643=CARTESIAN_POINT('Ctrl Pts',(-2.76672409838413,7.41169135421003,3.97929440108609));
#69644=CARTESIAN_POINT('Ctrl Pts',(-2.82596367574222,7.38930717540576,3.9818703630484));
#69645=CARTESIAN_POINT('Ctrl Pts',(-2.89852969435713,7.36088717201735,3.98500910521081));
#69646=CARTESIAN_POINT('Ctrl Pts',(-2.91211554745962,7.35552291748696,3.98559601842834));
#69647=CARTESIAN_POINT('Ctrl Pts',(-2.93341837757752,7.34704341048817,3.98651518390495));
#69648=CARTESIAN_POINT('Ctrl Pts',(-2.94114539283368,7.34395356959053,3.98684835329543));
#69649=CARTESIAN_POINT('Ctrl Pts',(-2.95484863078439,7.33844889028748,3.98743879252541));
#69650=CARTESIAN_POINT('Ctrl Pts',(-2.96082679824562,7.33603893237216,3.98769623861385));
#69651=CARTESIAN_POINT('Ctrl Pts',(-2.97459135014448,7.33047051034533,3.98828868307784));
#69652=CARTESIAN_POINT('Ctrl Pts',(-2.98237566784237,7.3273069391053,3.98862349606506));
#69653=CARTESIAN_POINT('Ctrl Pts',(-3.00364808128175,7.31862224837698,3.98953781295383));
#69654=CARTESIAN_POINT('Ctrl Pts',(-3.01712601561208,7.31307623505106,3.99011641295266));
#69655=CARTESIAN_POINT('Ctrl Pts',(-3.08237844998437,7.28601452129017,3.99291432300602));
#69656=CARTESIAN_POINT('Ctrl Pts',(-3.13393918473677,7.26398581181785,3.99511493160931));
#69657=CARTESIAN_POINT('Ctrl Pts',(-3.28196079343056,7.1988758967759,4.00140515101398));
#69658=CARTESIAN_POINT('Ctrl Pts',(-3.37779989801451,7.1544077162641,4.00544389789004));
#69659=CARTESIAN_POINT('Ctrl Pts',(-4.15028569256747,6.77699967275721,4.03777872328744));
#69660=CARTESIAN_POINT('Ctrl Pts',(-4.77695807943907,6.350841928595,4.06211737850159));
#69661=CARTESIAN_POINT('Ctrl Pts',(-5.48188780997847,5.70727705391847,4.09501733817585));
#69662=CARTESIAN_POINT('Ctrl Pts',(-5.62473551899532,5.56654732875783,4.10206445045347));
#69663=CARTESIAN_POINT('Ctrl Pts',(-5.87231430093308,5.30336961937923,4.11531729681671));
#69664=CARTESIAN_POINT('Ctrl Pts',(-5.97894410927416,5.18285886469941,4.12141195755589));
#69665=CARTESIAN_POINT('Ctrl Pts',(-6.09782029081979,5.03995383940207,4.1287843580056));
#69666=CARTESIAN_POINT('Ctrl Pts',(-6.11372941587572,5.02064334560323,4.12978354440819));
#69667=CARTESIAN_POINT('Ctrl Pts',(-6.13408375182362,4.99569705203258,4.13107864072407));
#69668=CARTESIAN_POINT('Ctrl Pts',(-6.1386134300646,4.9901300249205,4.13136792868201));
#69669=CARTESIAN_POINT('Ctrl Pts',(-6.14592138157936,4.98112345969848,4.13183640693174));
#69670=CARTESIAN_POINT('Ctrl Pts',(-6.14870436679462,4.9776877321599,4.13201522404845));
#69671=CARTESIAN_POINT('Ctrl Pts',(-6.15403751286836,4.97109241280141,4.13235868854814));
#69672=CARTESIAN_POINT('Ctrl Pts',(-6.15658812591725,4.96793318534904,4.13252330045944));
#69673=CARTESIAN_POINT('Ctrl Pts',(-6.16239561906418,4.96072859632745,4.13289889576014));
#69674=CARTESIAN_POINT('Ctrl Pts',(-6.16565094701837,4.95668199217514,4.13310999953099));
#69675=CARTESIAN_POINT('Ctrl Pts',(-6.17576442127482,4.94408484545787,4.13376760538043));
#69676=CARTESIAN_POINT('Ctrl Pts',(-6.18260875644006,4.93552328619168,4.13421516667474));
#69677=CARTESIAN_POINT('Ctrl Pts',(-6.23458928152608,4.87022320149393,4.13763332837882));
#69678=CARTESIAN_POINT('Ctrl Pts',(-6.27896000081939,4.81288252428012,4.14066097469018));
#69679=CARTESIAN_POINT('Ctrl Pts',(-6.42172617847592,4.62304968210538,4.15074557537173));
#69680=CARTESIAN_POINT('Ctrl Pts',(-6.51676080179441,4.48809291980044,4.15801036155191));
#69681=CARTESIAN_POINT('Ctrl Pts',(-6.65584212091184,4.27684636632203,4.16940102319782));
#69682=CARTESIAN_POINT('Ctrl Pts',(-6.70295579040209,4.20262206405166,4.17340685674299));
#69683=CARTESIAN_POINT('Ctrl Pts',(-7.06433040015784,3.61176169014668,4.20523372057327));
#69684=CARTESIAN_POINT('Ctrl Pts',(-7.31966226481008,3.0614092505138,4.23432343874945));
#69685=CARTESIAN_POINT('Ctrl Pts',(-7.57006758041437,2.30536906055945,4.27035471830639));
#69686=CARTESIAN_POINT('Ctrl Pts',(-7.62369492804355,2.12130426988319,4.27885786594408));
#69687=CARTESIAN_POINT('Ctrl Pts',(-7.72172097485857,1.73280983378444,4.29619840651706));
#69688=CARTESIAN_POINT('Ctrl Pts',(-7.76480657157006,1.52819923012435,4.30498895881389));
#69689=CARTESIAN_POINT('Ctrl Pts',(-7.80615474789803,1.28426722346424,4.31507579345122));
#69690=CARTESIAN_POINT('Ctrl Pts',(-7.81229398093943,1.24637757565016,4.31663156101586));
#69691=CARTESIAN_POINT('Ctrl Pts',(-7.82007779944335,1.19601934785357,4.31868495208943));
#69692=CARTESIAN_POINT('Ctrl Pts',(-7.82196870671538,1.18358971899486,4.31919062124964));
#69693=CARTESIAN_POINT('Ctrl Pts',(-7.82502694811659,1.16315933311269,4.32001989338746));
#69694=CARTESIAN_POINT('Ctrl Pts',(-7.82621165830959,1.1551612237325,4.32034406262532));
#69695=CARTESIAN_POINT('Ctrl Pts',(-7.82848502417897,1.13964944876765,4.32097184944036));
#69696=CARTESIAN_POINT('Ctrl Pts',(-7.8295751291473,1.13213600655403,4.3212755138998));
#69697=CARTESIAN_POINT('Ctrl Pts',(-7.83206894597459,1.11477174082932,4.32197635227435));
#69698=CARTESIAN_POINT('Ctrl Pts',(-7.83346489322489,1.10491980533502,4.32237327340145));
#69699=CARTESIAN_POINT('Ctrl Pts',(-7.83788198838691,1.07331689932008,4.32364424171172));
#69700=CARTESIAN_POINT('Ctrl Pts',(-7.8408311715568,1.05155588514363,4.32451595357579));
#69701=CARTESIAN_POINT('Ctrl Pts',(-7.86672410431421,0.854333578555812,
4.332385623939));
#69702=CARTESIAN_POINT('Ctrl Pts',(-7.88386606828014,0.67815533263219,4.33919367111561));
#69703=CARTESIAN_POINT('Ctrl Pts',(-7.90579533365887,0.332953684635162,
4.35217546162546));
#69704=CARTESIAN_POINT('Ctrl Pts',(-7.91110266801687,0.164060522392913,
4.3583607118558));
#69705=CARTESIAN_POINT('Ctrl Pts',(-7.91074839564088,-0.410472873522453,
4.37900619817625));
#69706=CARTESIAN_POINT('Ctrl Pts',(-7.87930631962955,-0.815455084703749,
4.39285851388627));
#69707=CARTESIAN_POINT('Ctrl Pts',(-7.74419887009957,-1.68381264150579,
4.42327619276572));
#69708=CARTESIAN_POINT('Ctrl Pts',(-7.62964143285399,-2.14392825483457,
4.43989634087291));
#69709=CARTESIAN_POINT('Ctrl Pts',(-7.46527634657199,-2.6180888647318,4.45980631812643));
#69710=CARTESIAN_POINT('Ctrl Pts',(-7.45575524147669,-2.64508109214738,
4.46094852808306));
#69711=CARTESIAN_POINT('Ctrl Pts',(-7.44201401661616,-2.68337359665407,
4.46258097425397));
#69712=CARTESIAN_POINT('Ctrl Pts',(-7.43791413720657,-2.69471701077335,
4.46306606348556));
#69713=CARTESIAN_POINT('Ctrl Pts',(-7.43133644876903,-2.71278656834385,
4.46384115545806));
#69714=CARTESIAN_POINT('Ctrl Pts',(-7.428875402385,-2.71951882427602,4.46413045957101));
#69715=CARTESIAN_POINT('Ctrl Pts',(-7.42443488239403,-2.73161497411448,
4.46465119934292));
#69716=CARTESIAN_POINT('Ctrl Pts',(-7.42245873525908,-2.73698008996829,
4.4648824985253));
#69717=CARTESIAN_POINT('Ctrl Pts',(-7.41782130634378,-2.74952845935181,
4.46542424765462));
#69718=CARTESIAN_POINT('Ctrl Pts',(-7.41515540646165,-2.75670999184286,
4.46573488431364));
#69719=CARTESIAN_POINT('Ctrl Pts',(-7.40748146960362,-2.77729074771746,
4.46662677539982));
#69720=CARTESIAN_POINT('Ctrl Pts',(-7.40244752962748,-2.79068023744827,
4.46720905898022));
#69721=CARTESIAN_POINT('Ctrl Pts',(-7.36940067298264,-2.87786111852038,
4.4710133907859));
#69722=CARTESIAN_POINT('Ctrl Pts',(-7.34032157618289,-2.95124203637413,
4.4742762891005));
#69723=CARTESIAN_POINT('Ctrl Pts',(-7.24418216528634,-3.18363392541702,
4.48478263843739));
#69724=CARTESIAN_POINT('Ctrl Pts',(-7.17301626018948,-3.34088827172534,
4.49215241876972));
#69725=CARTESIAN_POINT('Ctrl Pts',(-6.78413671106209,-4.13037251404046,
4.5301734889989));
#69726=CARTESIAN_POINT('Ctrl Pts',(-6.3877302182522,-4.72033205108303,4.56166780993951));
#69727=CARTESIAN_POINT('Ctrl Pts',(-5.77330113470282,-5.41300017162005,
4.60047854676485));
#69728=CARTESIAN_POINT('Ctrl Pts',(-5.62173591794911,-5.57024844453724,
4.60946947752466));
#69729=CARTESIAN_POINT('Ctrl Pts',(-5.43682942528658,-5.74684291485599,
4.61982008260452));
#69730=CARTESIAN_POINT('Ctrl Pts',(-5.40961998548378,-5.77246302107295,
4.62132849454857));
#69731=CARTESIAN_POINT('Ctrl Pts',(-5.36907920851549,-5.81009736821291,
4.62355441143365));
#69732=CARTESIAN_POINT('Ctrl Pts',(-5.35588694928053,-5.82226055454719,
4.62427540043048));
#69733=CARTESIAN_POINT('Ctrl Pts',(-5.3324179890581,-5.84375153492287,4.62555212364906));
#69734=CARTESIAN_POINT('Ctrl Pts',(-5.32215792297588,-5.85309735578473,
4.62610828829591));
#69735=CARTESIAN_POINT('Ctrl Pts',(-5.30059161979503,-5.87263835511359,
4.62727316623914));
#69736=CARTESIAN_POINT('Ctrl Pts',(-5.28928043528483,-5.88282799753943,
4.62788174433197));
#69737=CARTESIAN_POINT('Ctrl Pts',(-5.25954296079113,-5.90946180096811,
4.629475486206));
#69738=CARTESIAN_POINT('Ctrl Pts',(-5.24106892020545,-5.9258524716276,4.63045934234861));
#69739=CARTESIAN_POINT('Ctrl Pts',(-5.15835423109427,-5.99854981454305,
4.63483674545658));
#69740=CARTESIAN_POINT('Ctrl Pts',(-5.09328018615468,-6.05390085373992,
4.63820656783975));
#69741=CARTESIAN_POINT('Ctrl Pts',(-4.45247477792675,-6.58131340308698,
4.67069153614563));
#69742=CARTESIAN_POINT('Ctrl Pts',(-3.81376255761221,-6.97089665206033,
4.69714850013192));
#69743=CARTESIAN_POINT('Ctrl Pts',(-2.84025291126275,-7.39029335677249,
4.73610917112075));
#69744=CARTESIAN_POINT('Ctrl Pts',(-2.54328992862581,-7.49767448158712,
4.74791489070535));
#69745=CARTESIAN_POINT('Ctrl Pts',(-2.22289051899876,-7.59230036683773,
4.76124404717879));
#69746=CARTESIAN_POINT('Ctrl Pts',(-2.20502967632595,-7.59750690937414,
4.76198903270666));
#69747=CARTESIAN_POINT('Ctrl Pts',(-2.18014531588567,-7.60466570857732,
4.7630298759672));
#69748=CARTESIAN_POINT('Ctrl Pts',(-2.17313712339672,-7.60667136006428,
4.76332332897935));
#69749=CARTESIAN_POINT('Ctrl Pts',(-2.16104972016486,-7.61011254622313,
4.76383002930704));
#69750=CARTESIAN_POINT('Ctrl Pts',(-2.15597181943808,-7.61155269132217,
4.76404306552176));
#69751=CARTESIAN_POINT('Ctrl Pts',(-2.14547728904073,-7.61451770418703,
4.76448371122279));
#69752=CARTESIAN_POINT('Ctrl Pts',(-2.1400604677349,-7.61604187615527,4.76471135271007));
#69753=CARTESIAN_POINT('Ctrl Pts',(-2.12742715727273,-7.61958206417113,
4.76524274044985));
#69754=CARTESIAN_POINT('Ctrl Pts',(-2.12020942934569,-7.6215936074593,4.76554669586726));
#69755=CARTESIAN_POINT('Ctrl Pts',(-2.09712116476968,-7.6279928517625,4.76652017849778));
#69756=CARTESIAN_POINT('Ctrl Pts',(-2.08123985773627,-7.63234123807238,
4.76719157448971));
#69757=CARTESIAN_POINT('Ctrl Pts',(-1.73261972908868,-7.72662627781598,
4.78197110650287));
#69758=CARTESIAN_POINT('Ctrl Pts',(-1.39441808818264,-7.79475795519613,
4.79720071794645));
#69759=CARTESIAN_POINT('Ctrl Pts',(-0.139062961115238,-7.96333819606989,
4.8546936661156));
#69760=CARTESIAN_POINT('Ctrl Pts',(0.789506630207529,-7.92536897953664,
4.89811185553703));
#69761=CARTESIAN_POINT('Ctrl Pts',(1.74228601220451,-7.71693961788635,4.93812188301683));
#69762=CARTESIAN_POINT('Ctrl Pts',(1.7938333232978,-7.70512035978467,4.94027548742045));
#69763=CARTESIAN_POINT('Ctrl Pts',(1.86040006586186,-7.68915307695565,4.94304273199312));
#69764=CARTESIAN_POINT('Ctrl Pts',(1.87553054069765,-7.68547647451182,4.94367079124955));
#69765=CARTESIAN_POINT('Ctrl Pts',(1.89958692028265,-7.67955566662255,4.94466789870903));
#69766=CARTESIAN_POINT('Ctrl Pts',(1.90851989756494,-7.67734052297875,4.94503783840902));
#69767=CARTESIAN_POINT('Ctrl Pts',(1.92454564794662,-7.67333685918713,4.94570093737707));
#69768=CARTESIAN_POINT('Ctrl Pts',(1.93163983721816,-7.67155408279231,4.94599427276674));
#69769=CARTESIAN_POINT('Ctrl Pts',(1.94819637669238,-7.66736898711918,4.94667839624049));
#69770=CARTESIAN_POINT('Ctrl Pts',(1.95765678214055,-7.66495898429893,4.94706894741789));
#69771=CARTESIAN_POINT('Ctrl Pts',(1.98465771530557,-7.65802734827585,4.94818260874155));
#69772=CARTESIAN_POINT('Ctrl Pts',(2.00218725630916,-7.65346296194613,4.9489044008849));
#69773=CARTESIAN_POINT('Ctrl Pts',(2.11347435530932,-7.62407723592029,4.9534791217359));
#69774=CARTESIAN_POINT('Ctrl Pts',(2.20678620744848,-7.59759323582987,4.95728042920969));
#69775=CARTESIAN_POINT('Ctrl Pts',(2.48212956667434,-7.51394370660503,4.96840754023745));
#69776=CARTESIAN_POINT('Ctrl Pts',(2.662609237899,-7.45190139793182,4.9755818999431));
#69777=CARTESIAN_POINT('Ctrl Pts',(3.09726108354482,-7.28467403485139,4.99269328139777));
#69778=CARTESIAN_POINT('Ctrl Pts',(3.34853240814211,-7.17264539450853,5.00243780354241));
#69779=CARTESIAN_POINT('Ctrl Pts',(4.24356083883718,-6.71629375586315,5.03747526303579));
#69780=CARTESIAN_POINT('Ctrl Pts',(4.84463319251512,-6.29649356921655,5.0614962856532));
#69781=CARTESIAN_POINT('Ctrl Pts',(5.41042146742667,-5.7717438363351,5.09188247036127));
#69782=CARTESIAN_POINT('Ctrl Pts',(5.44100778586675,-5.74291925339349,5.09355171564732));
#69783=CARTESIAN_POINT('Ctrl Pts',(5.48040985294967,-5.70518937025563,5.09573521223236));
#69784=CARTESIAN_POINT('Ctrl Pts',(5.48943652183164,-5.69650459293307,5.0962377173195));
#69785=CARTESIAN_POINT('Ctrl Pts',(5.50379088947734,-5.68262810525776,5.09704040874343));
#69786=CARTESIAN_POINT('Ctrl Pts',(5.5091319795083,-5.6774502348903,5.09733987891205));
#69787=CARTESIAN_POINT('Ctrl Pts',(5.5191472233807,-5.66771360926592,5.09790291298832));
#69788=CARTESIAN_POINT('Ctrl Pts',(5.52382305509085,-5.6631565831918,5.09816638896673));
#69789=CARTESIAN_POINT('Ctrl Pts',(5.53437447764849,-5.65284775551494,5.09876231842716));
#69790=CARTESIAN_POINT('Ctrl Pts',(5.54024674906531,-5.64709257625073,5.09909494088358));
#69791=CARTESIAN_POINT('Ctrl Pts',(5.55762765089376,-5.63000504130767,5.1000822835887));
#69792=CARTESIAN_POINT('Ctrl Pts',(5.56911052508693,-5.6186466187212,5.1007382818236));
#69793=CARTESIAN_POINT('Ctrl Pts',(5.66215685978641,-5.52604325342921,5.10608349094295));
#69794=CARTESIAN_POINT('Ctrl Pts',(5.74197095106509,-5.44306371720488,5.11085401342704));
#69795=CARTESIAN_POINT('Ctrl Pts',(6.04915225041551,-5.10942188123228,5.12987305247875));
#69796=CARTESIAN_POINT('Ctrl Pts',(6.26214694578054,-4.84602337905215,5.14451897909836));
#69797=CARTESIAN_POINT('Ctrl Pts',(6.7636711562799,-4.13731648081782,5.18202184418714));
#69798=CARTESIAN_POINT('Ctrl Pts',(7.02551888685204,-3.67515602344842,5.20464840308578));
#69799=CARTESIAN_POINT('Ctrl Pts',(7.31864840013873,-3.0100029401262,5.23478538434852));
#69800=CARTESIAN_POINT('Ctrl Pts',(7.39133397209335,-2.82682084189524,5.24287017474098));
#69801=CARTESIAN_POINT('Ctrl Pts',(7.51671099857692,-2.47282258723944,5.25820774134906));
#69802=CARTESIAN_POINT('Ctrl Pts',(7.57060228220667,-2.30255904770196,5.26547125232975));
#69803=CARTESIAN_POINT('Ctrl Pts',(7.63165973204635,-2.08422908957248,5.27463824237077));
#69804=CARTESIAN_POINT('Ctrl Pts',(7.6442086187375,-2.03772318632278,5.27658253525373));
#69805=CARTESIAN_POINT('Ctrl Pts',(7.66364703086753,-1.96297730195073,5.27969418683678));
#69806=CARTESIAN_POINT('Ctrl Pts',(7.67080698517684,-1.93480900974373,5.28086381816623));
#69807=CARTESIAN_POINT('Ctrl Pts',(7.68414892181248,-1.88108154932852,5.28308906408046));
#69808=CARTESIAN_POINT('Ctrl Pts',(7.69035901209496,-1.85552976740456,5.28414491299281));
#69809=CARTESIAN_POINT('Ctrl Pts',(7.70428922004837,-1.7969417288493,5.28656036385985));
#69810=CARTESIAN_POINT('Ctrl Pts',(7.71192446116997,-1.76388578961946,5.28791917680736));
#69811=CARTESIAN_POINT('Ctrl Pts',(7.73505880636972,-1.66070580088093,5.2921482787337));
#69812=CARTESIAN_POINT('Ctrl Pts',(7.749815892315,-1.59041888584172,5.29501154222261));
#69813=CARTESIAN_POINT('Ctrl Pts',(7.81668704688395,-1.2488516680876,5.30884517877739));
#69814=CARTESIAN_POINT('Ctrl Pts',(7.85552568122707,-0.975165635290019,
5.31967730011351));
#69815=CARTESIAN_POINT('Ctrl Pts',(7.91131647906015,-0.347127784117426,
5.34420503526885));
#69816=CARTESIAN_POINT('Ctrl Pts',(7.9189247760439,0.00745533517541197,
5.35781155369968));
#69817=CARTESIAN_POINT('Ctrl Pts',(7.89153099412876,0.606556623570824,5.38109845982058));
#69818=CARTESIAN_POINT('Ctrl Pts',(7.86891303796264,0.851101749908046,5.39069342226176));
#69819=CARTESIAN_POINT('Ctrl Pts',(7.83102340598378,1.12241044308791,5.40164958931195));
#69820=CARTESIAN_POINT('Ctrl Pts',(7.82693021591501,1.15060686984834,5.40279205113136));
#69821=CARTESIAN_POINT('Ctrl Pts',(7.82057075989004,1.19280982656045,5.40450823146574));
#69822=CARTESIAN_POINT('Ctrl Pts',(7.81841897574612,1.20683346432946,5.40507952936244));
#69823=CARTESIAN_POINT('Ctrl Pts',(7.81452906453894,1.23173775941384,5.40609598372799));
#69824=CARTESIAN_POINT('Ctrl Pts',(7.81280590639158,1.24262072920156,5.40654081045102));
#69825=CARTESIAN_POINT('Ctrl Pts',(7.80913871762963,1.26547244881944,5.40747623797684));
#69826=CARTESIAN_POINT('Ctrl Pts',(7.80718989539551,1.27744039622054,5.40796694606765));
#69827=CARTESIAN_POINT('Ctrl Pts',(7.80192180217572,1.30933001295187,5.40927669168564));
#69828=CARTESIAN_POINT('Ctrl Pts',(7.79855377105532,1.32924337940081,5.4100968918124));
#69829=CARTESIAN_POINT('Ctrl Pts',(7.77912988947296,1.44147108001134,5.41473238358788));
#69830=CARTESIAN_POINT('Ctrl Pts',(7.76151139590888,1.53350613787863,5.41858307090073));
#69831=CARTESIAN_POINT('Ctrl Pts',(7.59421099140825,2.3305031632011,5.45228414745399));
#69832=CARTESIAN_POINT('Ctrl Pts',(7.35047704466483,3.01228631617945,5.48319147548354));
#69833=CARTESIAN_POINT('Ctrl Pts',(6.96719498926358,3.74888385590859,5.5172037358831));
#69834=CARTESIAN_POINT('Ctrl Pts',(6.91458227867885,3.84506028301337,5.5216662472084));
#69835=CARTESIAN_POINT('Ctrl Pts',(6.84156086658007,3.9721951987542,5.5275989093398));
#69836=CARTESIAN_POINT('Ctrl Pts',(6.82290936848958,4.00414754422264,5.52909286787867));
#69837=CARTESIAN_POINT('Ctrl Pts',(6.79325287620942,4.05414392504598,5.53143540538389));
#69838=CARTESIAN_POINT('Ctrl Pts',(6.7823985932055,4.07227662755972,5.53228602304595));
#69839=CARTESIAN_POINT('Ctrl Pts',(6.76135490576954,4.10711379062192,5.53392231565219));
#69840=CARTESIAN_POINT('Ctrl Pts',(6.75117593148488,4.1238243652781,5.53470812495331));
#69841=CARTESIAN_POINT('Ctrl Pts',(6.72695763458914,4.16325295683886,5.536564498572));
#69842=CARTESIAN_POINT('Ctrl Pts',(6.7128650506098,4.18593800945797,5.53763433592764));
#69843=CARTESIAN_POINT('Ctrl Pts',(6.6709384789533,4.25267160409983,5.54078707604022));
#69844=CARTESIAN_POINT('Ctrl Pts',(6.64278379238153,4.29651713555425,5.54286567926148));
#69845=CARTESIAN_POINT('Ctrl Pts',(6.38996135009806,4.6818135086468,5.56120248707517));
#69846=CARTESIAN_POINT('Ctrl Pts',(6.1395688481963,5.00566609815102,5.57716985458573));
#69847=CARTESIAN_POINT('Ctrl Pts',(5.43621167111037,5.78276201186043,5.61766462165159));
#69848=CARTESIAN_POINT('Ctrl Pts',(4.9512693118493,6.20303670041,5.64133322261512));
#69849=CARTESIAN_POINT('Ctrl Pts',(4.20769704034764,6.7041328506683,5.67502867288368));
#69850=CARTESIAN_POINT('Ctrl Pts',(3.98746554895735,6.83741339066503,5.68477307302276));
#69851=CARTESIAN_POINT('Ctrl Pts',(3.70277068015722,6.99126686776119,5.69741633349765));
#69852=CARTESIAN_POINT('Ctrl Pts',(3.64400662985024,7.02207509011529,5.70002878484663));
#69853=CARTESIAN_POINT('Ctrl Pts',(3.55780442068837,7.06589485180721,5.70387265113061));
#69854=CARTESIAN_POINT('Ctrl Pts',(3.53066724667832,7.0794937050405,5.70508439183675));
#69855=CARTESIAN_POINT('Ctrl Pts',(3.49321144664688,7.09799445339141,5.70675987416452));
#69856=CARTESIAN_POINT('Ctrl Pts',(3.48295929886775,7.10303076104196,5.70721878269879));
#69857=CARTESIAN_POINT('Ctrl Pts',(3.46583519250046,7.11139689017797,5.70798585320047));
#69858=CARTESIAN_POINT('Ctrl Pts',(3.4589692395527,7.11473900509223,5.70829356135694));
#69859=CARTESIAN_POINT('Ctrl Pts',(3.44541676830162,7.12131163750869,5.708901246944));
#69860=CARTESIAN_POINT('Ctrl Pts',(3.43873051822722,7.12454269187827,5.70920120379815));
#69861=CARTESIAN_POINT('Ctrl Pts',(3.42301394984646,7.132110266346,5.70990664439253));
#69862=CARTESIAN_POINT('Ctrl Pts',(3.41397993541542,7.13643905261351,5.71031242233383));
#69863=CARTESIAN_POINT('Ctrl Pts',(3.384566760328,7.15046419295984,5.71163455235557));
#69864=CARTESIAN_POINT('Ctrl Pts',(3.36415442775782,7.16009045356691,5.71255363186411));
#69865=CARTESIAN_POINT('Ctrl Pts',(2.86166095835166,7.39443842791785,5.73522192258381));
#69866=CARTESIAN_POINT('Ctrl Pts',(2.35829510538361,7.570006128427,5.7594334516651));
#69867=CARTESIAN_POINT('Ctrl Pts',(1.59472603826666,7.75274364326049,5.79541604440773));
#69868=CARTESIAN_POINT('Ctrl Pts',(1.34548551814666,7.79986275922093,5.80703781460866));
#69869=CARTESIAN_POINT('Ctrl Pts',(0.637617840821994,7.89874002508715,5.83925560321977));
#69870=CARTESIAN_POINT('Ctrl Pts',(0.176082918226642,7.92248280954953,5.85928803879936));
#69871=CARTESIAN_POINT('Ctrl Pts',(-0.315086690177379,7.90478028737376,
5.87927124828294));
#69872=CARTESIAN_POINT('Ctrl Pts',(-0.345227301746537,7.90352131331452,
5.8804924710024));
#69873=CARTESIAN_POINT('Ctrl Pts',(-0.386248435682548,7.90157275276713,
5.8821477474101));
#69874=CARTESIAN_POINT('Ctrl Pts',(-0.397135624726235,7.90103304119698,
5.88258641302048));
#69875=CARTESIAN_POINT('Ctrl Pts',(-0.415616436023386,7.90007859530998,
5.88332993837988));
#69876=CARTESIAN_POINT('Ctrl Pts',(-0.423210625524627,7.89967541110753,
5.88363515410429));
#69877=CARTESIAN_POINT('Ctrl Pts',(-0.437860912850174,7.89887642426437,
5.88422335192427));
#69878=CARTESIAN_POINT('Ctrl Pts',(-0.44491708321792,7.89848211583716,5.88450637988196));
#69879=CARTESIAN_POINT('Ctrl Pts',(-0.461602087948332,7.89752730546941,
5.8851749864428));
#69880=CARTESIAN_POINT('Ctrl Pts',(-0.471230454278757,7.8969586479883,5.88556031254988));
#69881=CARTESIAN_POINT('Ctrl Pts',(-0.499428925545599,7.89524147286145,
5.88668734125412));
#69882=CARTESIAN_POINT('Ctrl Pts',(-0.517996104394526,7.89404504726751,
5.88742756017706));
#69883=CARTESIAN_POINT('Ctrl Pts',(-0.655086522677808,7.88472550908008,
5.89287929798806));
#69884=CARTESIAN_POINT('Ctrl Pts',(-0.773420350430547,7.87399880435287,
5.89750940817328));
#69885=CARTESIAN_POINT('Ctrl Pts',(-1.15755434499525,7.83043420750406,5.91231764890264));
#69886=CARTESIAN_POINT('Ctrl Pts',(-1.42194396437552,7.78676575283191,5.92215572795283));
#69887=CARTESIAN_POINT('Ctrl Pts',(-2.10950521061917,7.6370078620693,5.94722612192232));
#69888=CARTESIAN_POINT('Ctrl Pts',(-2.52700115225641,7.50920602060341,5.96189690810108));
#69889=CARTESIAN_POINT('Ctrl Pts',(-3.13746701447804,7.26562014724769,5.98433122219344));
#69890=CARTESIAN_POINT('Ctrl Pts',(-3.33955422127151,7.17497791687253,5.99194135161082));
#69891=CARTESIAN_POINT('Ctrl Pts',(-3.79798889690992,6.94578800764415,6.01012358242564));
#69892=CARTESIAN_POINT('Ctrl Pts',(-4.05100283669737,6.80132621315834,6.02085977275839));
#69893=CARTESIAN_POINT('Ctrl Pts',(-4.30995323735038,6.63389192585832,6.03316864472254));
#69894=CARTESIAN_POINT('Ctrl Pts',(-4.32441856068365,6.62447153329727,6.03386077978817));
#69895=CARTESIAN_POINT('Ctrl Pts',(-4.34435638105539,6.61139410067184,6.03482120650253));
#69896=CARTESIAN_POINT('Ctrl Pts',(-4.34985540959995,6.60777740508074,6.03508678045295));
#69897=CARTESIAN_POINT('Ctrl Pts',(-4.3590305620555,6.60172651647461,6.03553103794525));
#69898=CARTESIAN_POINT('Ctrl Pts',(-4.36270918469568,6.59929609950054,6.03570946377086));
#69899=CARTESIAN_POINT('Ctrl Pts',(-4.36989708083729,6.59453851559377,6.03605870804953));
#69900=CARTESIAN_POINT('Ctrl Pts',(-4.3734065323073,6.5922116193123,6.03622950786512));
#69901=CARTESIAN_POINT('Ctrl Pts',(-4.38171789636009,6.58669131909051,6.03663468485052));
#69902=CARTESIAN_POINT('Ctrl Pts',(-4.38651817235953,6.58349546817502,6.03686923187691));
#69903=CARTESIAN_POINT('Ctrl Pts',(-4.40208258957126,6.57310865964512,6.03763147702867));
#69904=CARTESIAN_POINT('Ctrl Pts',(-4.41283236573116,6.56589667011022,6.0381606646453));
#69905=CARTESIAN_POINT('Ctrl Pts',(-4.66405224746038,6.39645845956242,6.05059138130058));
#69906=CARTESIAN_POINT('Ctrl Pts',(-4.89541685187881,6.22116769284531,6.06339832303223));
#69907=CARTESIAN_POINT('Ctrl Pts',(-5.64766672541784,5.58324390055841,6.10823586258162));
#69908=CARTESIAN_POINT('Ctrl Pts',(-6.11704678303744,5.06465489144723,6.14153870453736));
#69909=CARTESIAN_POINT('Ctrl Pts',(-6.66273704585592,4.2733976523693,6.18349748480281));
#69910=CARTESIAN_POINT('Ctrl Pts',(-6.80199705355515,4.0480671484131,6.19465738866081));
#69911=CARTESIAN_POINT('Ctrl Pts',(-6.94090056341677,3.79583440262743,6.20630739188017));
#69912=CARTESIAN_POINT('Ctrl Pts',(-6.95200462835084,3.77545905866299,6.20724276820934));
#69913=CARTESIAN_POINT('Ctrl Pts',(-6.9674239703305,3.74686673673796,6.2085474350096));
#69914=CARTESIAN_POINT('Ctrl Pts',(-6.97181462226908,3.73869067973158,6.20891960461373));
#69915=CARTESIAN_POINT('Ctrl Pts',(-6.97939114585035,3.72452229022356,6.20956298307715));
#69916=CARTESIAN_POINT('Ctrl Pts',(-6.98258370784065,3.71853355779991,6.2098344469564));
#69917=CARTESIAN_POINT('Ctrl Pts',(-6.98919340766281,3.70609629803709,6.2103972212356));
#69918=CARTESIAN_POINT('Ctrl Pts',(-6.99260933750081,3.6996471336524,6.2106884854944));
#69919=CARTESIAN_POINT('Ctrl Pts',(-7.00060184668952,3.68450692265038,6.21137096790856));
#69920=CARTESIAN_POINT('Ctrl Pts',(-7.00517117852559,3.67581205170315,6.21176191032794));
#69921=CARTESIAN_POINT('Ctrl Pts',(-7.01992905276472,3.6476021896075,6.21302706549719));
#69922=CARTESIAN_POINT('Ctrl Pts',(-7.03005237677896,3.62805309084041,6.21389880416742));
#69923=CARTESIAN_POINT('Ctrl Pts',(-7.21418835136842,3.26880457517399,6.22982780551063));
#69924=CARTESIAN_POINT('Ctrl Pts',(-7.36348162021659,2.91698089216684,6.24390563404368));
#69925=CARTESIAN_POINT('Ctrl Pts',(-7.76822058489126,1.73132607939897,6.28804145891455));
#69926=CARTESIAN_POINT('Ctrl Pts',(-7.91147119677858,0.866368619473638,
6.31458488693133));
#69927=CARTESIAN_POINT('Ctrl Pts',(-7.91099883573547,-0.00429196832219148,
6.34885622675283));
#69928=CARTESIAN_POINT('',(-7.90785232982224,0.00748026227384232,8.35766849176316));
#69929=CARTESIAN_POINT('Ctrl Pts',(-7.92631550431099,-0.00395340570050814,
6.35766849176318));
#69930=CARTESIAN_POINT('Ctrl Pts',(-7.92638474181553,-0.0501225147052013,
6.35953525763348));
#69931=CARTESIAN_POINT('Ctrl Pts',(-7.92601146905589,-0.0962875653539168,
6.36140202350379));
#69932=CARTESIAN_POINT('Ctrl Pts',(-7.9251921263217,-0.14244181639041,6.3632687893741));
#69933=CARTESIAN_POINT('Ctrl Pts',(-7.87873674991768,-2.75931143039582,
6.46911132332844));
#69934=CARTESIAN_POINT('Ctrl Pts',(-5.65808046510112,-6.63253954498222,
6.62787512426005));
#69935=CARTESIAN_POINT('Ctrl Pts',(-0.472789767622867,-8.21296885635869,
6.83956019216859));
#69936=CARTESIAN_POINT('Ctrl Pts',(4.88506260381215,-7.22940821924057,7.05124526007741));
#69937=CARTESIAN_POINT('Ctrl Pts',(8.37301016309629,-2.44600387829248,7.26293032798607));
#69938=CARTESIAN_POINT('Ctrl Pts',(7.68178920747253,2.96689427180967,7.47461539589462));
#69939=CARTESIAN_POINT('Ctrl Pts',(5.34689457404341,6.2859763852109,7.63337919682633));
#69940=CARTESIAN_POINT('Ctrl Pts',(1.68801954593999,8.05996376630325,7.79214299775764));
#69941=CARTESIAN_POINT('Ctrl Pts',(-3.75079024074277,7.87010856532681,8.00382806566654));
#69942=CARTESIAN_POINT('Ctrl Pts',(-7.47900960997268,4.11875362579123,8.19233656366825));
#69943=CARTESIAN_POINT('Ctrl Pts',(-7.91308753929871,0.751099506788409,
8.32792379469287));
#69944=CARTESIAN_POINT('Ctrl Pts',(-7.90669357492867,0.0102339785243165,
8.35766849176316));
#69945=CARTESIAN_POINT('',(-7.911,-4.08117983852208E-12,10.3576684917632));
#69946=CARTESIAN_POINT('Ctrl Pts',(-7.911,-4.02677891031544E-12,8.35766849176316));
#69947=CARTESIAN_POINT('Ctrl Pts',(-7.91099999999888,-2.20167589667082,
8.44625592749589));
#69948=CARTESIAN_POINT('Ctrl Pts',(-6.94214576672145,-4.38610418339042,
8.53484336322862));
#69949=CARTESIAN_POINT('Ctrl Pts',(-3.67820201487902,-7.34180684107825,
8.71201823469407));
#69950=CARTESIAN_POINT('Ctrl Pts',(-1.40868175871317,-8.08992666571412,
8.8006056704268));
#69951=CARTESIAN_POINT('Ctrl Pts',(2.97309270521684,-7.65454228025099,8.97778054189226));
#69952=CARTESIAN_POINT('Ctrl Pts',(5.05102072675952,-6.47444880833954,9.06636797762498));
#69953=CARTESIAN_POINT('Ctrl Pts',(7.66951518848033,-2.93425195367289,9.24354284909043));
#69954=CARTESIAN_POINT('Ctrl Pts',(8.18956872247105,-0.601881960094668,
9.33213028482316));
#69955=CARTESIAN_POINT('Ctrl Pts',(7.32306689761137,3.71537198232857,9.50930515628861));
#69956=CARTESIAN_POINT('Ctrl Pts',(5.94329958849885,5.66643518936844,9.59789259202134));
#69957=CARTESIAN_POINT('Ctrl Pts',(2.16154501637399,7.92205913233121,9.77506746348679));
#69958=CARTESIAN_POINT('Ctrl Pts',(-0.210816529305054,8.20894963712991,
9.86365489921953));
#69959=CARTESIAN_POINT('Ctrl Pts',(-4.42123908576837,6.91982244717576,10.040829770685));
#69960=CARTESIAN_POINT('Ctrl Pts',(-6.226316256345,5.35390358803159,10.1294172064177));
#69961=CARTESIAN_POINT('Ctrl Pts',(-7.65317280859616,2.31334857514088,10.264559258688));
#69962=CARTESIAN_POINT('Ctrl Pts',(-7.9110000000006,1.15702837836093,10.3111138752256));
#69963=CARTESIAN_POINT('Ctrl Pts',(-7.911,-4.08117983852208E-12,10.3576684917632));
#69964=CARTESIAN_POINT('',(-7.90990495318262,0.00414520974019739,14.3576684917631));
#69965=CARTESIAN_POINT('Ctrl Pts',(-7.91099906521622,-0.00384579616109687,
10.3649678417381));
#69966=CARTESIAN_POINT('Ctrl Pts',(-7.91057198107668,-0.88237967762714,
10.3971597508701));
#69967=CARTESIAN_POINT('Ctrl Pts',(-7.76382265767731,-1.75459616253359,
10.4245499411469));
#69968=CARTESIAN_POINT('Ctrl Pts',(-7.42063542251528,-2.74729858307459,
10.4631505107621));
#69969=CARTESIAN_POINT('Ctrl Pts',(-7.35918199542276,-2.90790531779804,
10.4696709074192));
#69970=CARTESIAN_POINT('Ctrl Pts',(-7.28217855326639,-3.09103743038594,
10.4775539654887));
#69971=CARTESIAN_POINT('Ctrl Pts',(-7.27168279065158,-3.11564860632312,
10.478622896393));
#69972=CARTESIAN_POINT('Ctrl Pts',(-7.2580098789783,-3.14726432605392,10.4800088752525));
#69973=CARTESIAN_POINT('Ctrl Pts',(-7.25494697983428,-3.15431838285341,
10.4803189375722));
#69974=CARTESIAN_POINT('Ctrl Pts',(-7.24999433227957,-3.16567927971392,
10.4808196533531));
#69975=CARTESIAN_POINT('Ctrl Pts',(-7.24811101415213,-3.16998893475049,
10.4810099079065));
#69976=CARTESIAN_POINT('Ctrl Pts',(-7.24451681547553,-3.17819370230368,
10.4813727162146));
#69977=CARTESIAN_POINT('Ctrl Pts',(-7.24280663323189,-3.18208912077373,
10.4815452262445));
#69978=CARTESIAN_POINT('Ctrl Pts',(-7.2389013680173,-3.19096499628663,10.4819388890561));
#69979=CARTESIAN_POINT('Ctrl Pts',(-7.23670428791175,-3.19594456654695,
10.4821601677828));
#69980=CARTESIAN_POINT('Ctrl Pts',(-7.22997348399945,-3.2111570637923,10.4828374799755));
#69981=CARTESIAN_POINT('Ctrl Pts',(-7.22542326095984,-3.22138246183518,
10.4832945694224));
#69982=CARTESIAN_POINT('Ctrl Pts',(-7.18917239218993,-3.30238328913814,
10.4869298822154));
#69983=CARTESIAN_POINT('Ctrl Pts',(-7.15645535268782,-3.37269640978962,
10.4901727994694));
#69984=CARTESIAN_POINT('Ctrl Pts',(-6.96388570389769,-3.77113128654321,
10.5089958458147));
#69985=CARTESIAN_POINT('Ctrl Pts',(-6.78251942879694,-4.088340361109,10.525708802195));
#69986=CARTESIAN_POINT('Ctrl Pts',(-6.49586472584326,-4.51780793709011,
10.5496412318384));
#69987=CARTESIAN_POINT('Ctrl Pts',(-6.40820777726173,-4.64130586388238,
10.5566921658941));
#69988=CARTESIAN_POINT('Ctrl Pts',(-6.09263619212748,-5.05991069205952,
10.5810253734471));
#69989=CARTESIAN_POINT('Ctrl Pts',(-5.84743392889067,-5.34139178205895,
10.598133917764));
#69990=CARTESIAN_POINT('Ctrl Pts',(-5.45962329474864,-5.72773073201286,
10.6221563188856));
#69991=CARTESIAN_POINT('Ctrl Pts',(-5.33192165571878,-5.8467942188939,10.629651844648));
#69992=CARTESIAN_POINT('Ctrl Pts',(-5.14016721926627,-6.01406570574888,
10.6403050544507));
#69993=CARTESIAN_POINT('Ctrl Pts',(-5.0791613997734,-6.06567600184165,10.6436106207689));
#69994=CARTESIAN_POINT('Ctrl Pts',(-4.99270644395592,-6.13659694391542,
10.648180050761));
#69995=CARTESIAN_POINT('Ctrl Pts',(-4.96790757188951,-6.15669018859719,
10.6494778069736));
#69996=CARTESIAN_POINT('Ctrl Pts',(-4.9303876047021,-6.18671637474069,10.651421976789));
#69997=CARTESIAN_POINT('Ctrl Pts',(-4.9177567639647,-6.19676123865373,10.6520732079638));
#69998=CARTESIAN_POINT('Ctrl Pts',(-4.89731755057989,-6.21291397663385,
10.6531217966822));
#69999=CARTESIAN_POINT('Ctrl Pts',(-4.88952831309075,-6.21904591949265,
10.6535201861312));
#70000=CARTESIAN_POINT('Ctrl Pts',(-4.87458935844933,-6.23076093865924,
10.6542819280721));
#70001=CARTESIAN_POINT('Ctrl Pts',(-4.86744152739758,-6.23634638761809,
10.6546453818307));
#70002=CARTESIAN_POINT('Ctrl Pts',(-4.85469826742705,-6.24626895442537,
10.6552915495564));
#70003=CARTESIAN_POINT('Ctrl Pts',(-4.84910660079537,-6.25061087360696,
10.6555744681356));
#70004=CARTESIAN_POINT('Ctrl Pts',(-4.83802525529555,-6.25919169970944,
10.6561339291831));
#70005=CARTESIAN_POINT('Ctrl Pts',(-4.83253581552,-6.26343090459634,10.6564104842418));
#70006=CARTESIAN_POINT('Ctrl Pts',(-4.81765418072823,-6.27489199615742,
10.6571586229789));
#70007=CARTESIAN_POINT('Ctrl Pts',(-4.8082513075627,-6.28210002575037,10.6576296184672));
#70008=CARTESIAN_POINT('Ctrl Pts',(-4.77321890196462,-6.30883034346367,
10.6593780798998));
#70009=CARTESIAN_POINT('Ctrl Pts',(-4.74748620720042,-6.32821726354204,
10.6606498240613));
#70010=CARTESIAN_POINT('Ctrl Pts',(-4.3821600137862,-6.5999701845109,10.6785298478837));
#70011=CARTESIAN_POINT('Ctrl Pts',(-4.02295612873389,-6.82486696335122,
10.6939285093056));
#70012=CARTESIAN_POINT('Ctrl Pts',(-3.45335361420601,-7.12082281742278,
10.7162598821874));
#70013=CARTESIAN_POINT('Ctrl Pts',(-3.255147461332,-7.21358347489035,10.723690514822));
#70014=CARTESIAN_POINT('Ctrl Pts',(-2.64675924382396,-7.46812155108779,
10.7459884338386));
#70015=CARTESIAN_POINT('Ctrl Pts',(-2.22669151838874,-7.60394421978643,
10.7606793946627));
#70016=CARTESIAN_POINT('Ctrl Pts',(-1.63530614273069,-7.74192777876334,
10.7828948287936));
#70017=CARTESIAN_POINT('Ctrl Pts',(-1.47193143421454,-7.77464361101532,
10.7891929564004));
#70018=CARTESIAN_POINT('Ctrl Pts',(-1.28245416720249,-7.80640027732479,
10.7968099077025));
#70019=CARTESIAN_POINT('Ctrl Pts',(-1.25723216285564,-7.81050198383651,
10.7978301772157));
#70020=CARTESIAN_POINT('Ctrl Pts',(-1.22484812179071,-7.815607485517,10.7991488245032));
#70021=CARTESIAN_POINT('Ctrl Pts',(-1.21770370712999,-7.81672380029247,
10.7994402785277));
#70022=CARTESIAN_POINT('Ctrl Pts',(-1.20617701075306,-7.81850866023468,
10.7999113924637));
#70023=CARTESIAN_POINT('Ctrl Pts',(-1.20179566649169,-7.81918332226885,
10.8000906712723));
#70024=CARTESIAN_POINT('Ctrl Pts',(-1.19340369004479,-7.82046834213657,
10.8004344520695));
#70025=CARTESIAN_POINT('Ctrl Pts',(-1.18939314801595,-7.82107929873497,
10.8005989170863));
#70026=CARTESIAN_POINT('Ctrl Pts',(-1.18018520979318,-7.82247476819439,
10.8009769085944));
#70027=CARTESIAN_POINT('Ctrl Pts',(-1.17498750318287,-7.82325718582399,
10.8011905633478));
#70028=CARTESIAN_POINT('Ctrl Pts',(-1.15891472086327,-7.82566026376077,
10.8018521191351));
#70029=CARTESIAN_POINT('Ctrl Pts',(-1.14803708549907,-7.82726342612241,
10.8023010804277));
#70030=CARTESIAN_POINT('Ctrl Pts',(-1.06466752194235,-7.83937303223978,
10.8057513466935));
#70031=CARTESIAN_POINT('Ctrl Pts',(-0.992038362476137,-7.8488945515213,
10.8088108938967));
#70032=CARTESIAN_POINT('Ctrl Pts',(-0.103821166611422,-7.95281294854144,
10.8467927485948));
#70033=CARTESIAN_POINT('Ctrl Pts',(0.721532118973731,-7.92070372895431,
10.8873515855274));
#70034=CARTESIAN_POINT('Ctrl Pts',(1.80897967830843,-7.70674926601612,10.9378394405189));
#70035=CARTESIAN_POINT('Ctrl Pts',(2.08754287887858,-7.6360054188718,10.9505639761255));
#70036=CARTESIAN_POINT('Ctrl Pts',(2.47394692210884,-7.51514132093443,10.9678101210924));
#70037=CARTESIAN_POINT('Ctrl Pts',(2.58543741558046,-7.4775181356851,10.972738937587));
#70038=CARTESIAN_POINT('Ctrl Pts',(2.73661868904119,-7.42271521514538,10.9793596680852));
#70039=CARTESIAN_POINT('Ctrl Pts',(2.77706600975968,-7.40767760317586,10.9811248052535));
#70040=CARTESIAN_POINT('Ctrl Pts',(2.84523319138744,-7.38169743488428,10.9840895319938));
#70041=CARTESIAN_POINT('Ctrl Pts',(2.87301768329552,-7.3709279165727,10.9852950742376));
#70042=CARTESIAN_POINT('Ctrl Pts',(2.91149917241148,-7.35576150295803,10.9869608980344));
#70043=CARTESIAN_POINT('Ctrl Pts',(2.92224819315074,-7.35149782143082,10.9874257934812));
#70044=CARTESIAN_POINT('Ctrl Pts',(2.9394884951408,-7.34461553653067,10.9881707743588));
#70045=CARTESIAN_POINT('Ctrl Pts',(2.94598569698152,-7.3420118677396,10.9884513774215));
#70046=CARTESIAN_POINT('Ctrl Pts',(2.95950352296517,-7.33657394288449,10.9890348769518));
#70047=CARTESIAN_POINT('Ctrl Pts',(2.96652355291728,-7.33373822359823,10.9893377222511));
#70048=CARTESIAN_POINT('Ctrl Pts',(2.98264084566769,-7.32720076484524,10.9900326256078));
#70049=CARTESIAN_POINT('Ctrl Pts',(2.99173531592787,-7.32349214944242,10.9904244444667));
#70050=CARTESIAN_POINT('Ctrl Pts',(3.02050447388234,-7.31169790078577,10.9916629976298));
#70051=CARTESIAN_POINT('Ctrl Pts',(3.04015354553766,-7.30354981484479,10.992507562343));
#70052=CARTESIAN_POINT('Ctrl Pts',(3.20534463079779,-7.23426615245253,10.9995968274794));
#70053=CARTESIAN_POINT('Ctrl Pts',(3.34906382947605,-7.16886433954886,11.0056911959243));
#70054=CARTESIAN_POINT('Ctrl Pts',(3.97418435713948,-6.86148755777984,11.0319862738834));
#70055=CARTESIAN_POINT('Ctrl Pts',(4.43210578649819,-6.5750001461634,11.0505615150084));
#70056=CARTESIAN_POINT('Ctrl Pts',(5.2604983339992,-5.93059435755964,11.0867961756885));
#70057=CARTESIAN_POINT('Ctrl Pts',(5.63231715549257,-5.5786895005302,11.1044371889084));
#70058=CARTESIAN_POINT('Ctrl Pts',(5.9984953533835,-5.15792482240521,11.1263939660171));
#70059=CARTESIAN_POINT('Ctrl Pts',(6.02906695479708,-5.12215643060492,11.1282648486462));
#70060=CARTESIAN_POINT('Ctrl Pts',(6.06715026846275,-5.07678609570064,11.130641491682));
#70061=CARTESIAN_POINT('Ctrl Pts',(6.0749617568578,-5.06743614583681,11.1311314585084));
#70062=CARTESIAN_POINT('Ctrl Pts',(6.08735237463813,-5.05253538795189,11.1319125593831));
#70063=CARTESIAN_POINT('Ctrl Pts',(6.09194560259897,-5.04699629027516,11.132202975701));
#70064=CARTESIAN_POINT('Ctrl Pts',(6.10057877144233,-5.0365563625102,11.1327504382646));
#70065=CARTESIAN_POINT('Ctrl Pts',(6.10462038261891,-5.03165691627802,11.1330074008693));
#70066=CARTESIAN_POINT('Ctrl Pts',(6.11368695668513,-5.02063895159478,11.1335853424039));
#70067=CARTESIAN_POINT('Ctrl Pts',(6.11870863940272,-5.01451775070527,11.1339064815764));
#70068=CARTESIAN_POINT('Ctrl Pts',(6.13145362880036,-4.99893454418843,11.1347241509884));
#70069=CARTESIAN_POINT('Ctrl Pts',(6.13916421242646,-4.98946219045832,11.1352212897778));
#70070=CARTESIAN_POINT('Ctrl Pts',(6.18178447069619,-4.93685537835804,11.1379827412921));
#70071=CARTESIAN_POINT('Ctrl Pts',(6.21626101838585,-4.89337297184899,11.1402670132772));
#70072=CARTESIAN_POINT('Ctrl Pts',(6.72723971401613,-4.23480258149033,11.1748544908382));
#70073=CARTESIAN_POINT('Ctrl Pts',(7.11092020475321,-3.55305999768354,11.2100684648503));
#70074=CARTESIAN_POINT('Ctrl Pts',(7.49911171463348,-2.53818489126325,11.2564450684829));
#70075=CARTESIAN_POINT('Ctrl Pts',(7.59236722520927,-2.24388830013566,11.2693215400156));
#70076=CARTESIAN_POINT('Ctrl Pts',(7.68378649476927,-1.88344469292061,11.2844644648059));
#70077=CARTESIAN_POINT('Ctrl Pts',(7.6986308353565,-1.82181837246644,11.2870324566008));
#70078=CARTESIAN_POINT('Ctrl Pts',(7.71773763324199,-1.73808884760496,11.2904944817907));
#70079=CARTESIAN_POINT('Ctrl Pts',(7.72264868039951,-1.71613646976979,11.2913996361497));
#70080=CARTESIAN_POINT('Ctrl Pts',(7.73062230238228,-1.67976695906232,11.2928950521766));
#70081=CARTESIAN_POINT('Ctrl Pts',(7.73373833035206,-1.66536171993156,11.2934862699581));
#70082=CARTESIAN_POINT('Ctrl Pts',(7.73969588991651,-1.63744289052289,11.2946300039706));
#70083=CARTESIAN_POINT('Ctrl Pts',(7.74254232975586,-1.62393040537018,11.2951826077042));
#70084=CARTESIAN_POINT('Ctrl Pts',(7.74864596436921,-1.59457465622449,11.2963810626688));
#70085=CARTESIAN_POINT('Ctrl Pts',(7.75188998181096,-1.57872870615324,11.2970266688636));
#70086=CARTESIAN_POINT('Ctrl Pts',(7.7620978026828,-1.52807677961243,11.2990861891692));
#70087=CARTESIAN_POINT('Ctrl Pts',(7.76887598438157,-1.49323370811335,11.3004966262842));
#70088=CARTESIAN_POINT('Ctrl Pts',(7.82076704947028,-1.21656768287698,11.3116464343408));
#70089=CARTESIAN_POINT('Ctrl Pts',(7.85481398576106,-0.972799779315094,
11.3211640080145));
#70090=CARTESIAN_POINT('Ctrl Pts',(7.93735418621054,-0.0794542015955126,
11.3551489064448));
#70091=CARTESIAN_POINT('Ctrl Pts',(7.91698191507798,0.573790600533551,11.3780373641599));
#70092=CARTESIAN_POINT('Ctrl Pts',(7.7916441161491,1.37875264098124,11.4084106170939));
#70093=CARTESIAN_POINT('Ctrl Pts',(7.76147214170448,1.5395530377404,11.4146063532321));
#70094=CARTESIAN_POINT('Ctrl Pts',(7.71048244740145,1.77139228805234,11.4238564857108));
#70095=CARTESIAN_POINT('Ctrl Pts',(7.69361804883746,1.84326098592666,11.4267689169675));
#70096=CARTESIAN_POINT('Ctrl Pts',(7.67266439806903,1.92725312723281,11.430235853212));
#70097=CARTESIAN_POINT('Ctrl Pts',(7.66954814545796,1.939617184811,11.4307478179174));
#70098=CARTESIAN_POINT('Ctrl Pts',(7.66473624434677,1.95851598979028,11.4315329119258));
#70099=CARTESIAN_POINT('Ctrl Pts',(7.66306209036361,1.96505622730898,11.4318050725991));
#70100=CARTESIAN_POINT('Ctrl Pts',(7.65999841307298,1.97696131073191,11.4323013437489));
#70101=CARTESIAN_POINT('Ctrl Pts',(7.65861161919257,1.98232685966465,11.4325253291397));
#70102=CARTESIAN_POINT('Ctrl Pts',(7.65581652179868,1.99309446594069,11.4329754721483));
#70103=CARTESIAN_POINT('Ctrl Pts',(7.6544081359219,1.99849649839561,11.4332016334942));
#70104=CARTESIAN_POINT('Ctrl Pts',(7.65039507508952,2.01382260060149,11.4338442171972));
#70105=CARTESIAN_POINT('Ctrl Pts',(7.64777681667737,2.02374307470288,11.4342612779022));
#70106=CARTESIAN_POINT('Ctrl Pts',(7.63666411512549,2.06551909346673,11.4360223865732));
#70107=CARTESIAN_POINT('Ctrl Pts',(7.62798991759016,2.09732633233515,11.4373751142866));
#70108=CARTESIAN_POINT('Ctrl Pts',(7.47348647456869,2.65023211936364,11.4611093242326));
#70109=CARTESIAN_POINT('Ctrl Pts',(7.27478073763207,3.15502775450272,11.486080446767));
#70110=CARTESIAN_POINT('Ctrl Pts',(6.81583682560413,4.04199488327738,11.5321143910098));
#70111=CARTESIAN_POINT('Ctrl Pts',(6.57063887336521,4.42946025006581,11.5530960249361));
#70112=CARTESIAN_POINT('Ctrl Pts',(6.1759529603678,4.94762879171046,11.5814992826194));
#70113=CARTESIAN_POINT('Ctrl Pts',(6.05298461998006,5.09733355109033,11.5897607923683));
#70114=CARTESIAN_POINT('Ctrl Pts',(5.85944317081221,5.31606305274151,11.6019061868513));
#70115=CARTESIAN_POINT('Ctrl Pts',(5.79287604273786,5.38852379458448,11.6059433428859));
#70116=CARTESIAN_POINT('Ctrl Pts',(5.71242087999194,5.47288767321996,11.6106620901336));
#70117=CARTESIAN_POINT('Ctrl Pts',(5.69982332502911,5.48600636736837,11.6113964067281));
#70118=CARTESIAN_POINT('Ctrl Pts',(5.6803833857919,5.50611126014726,11.6125226422606));
#70119=CARTESIAN_POINT('Ctrl Pts',(5.67357314077606,5.51312837106187,11.6129158903508));
#70120=CARTESIAN_POINT('Ctrl Pts',(5.66164470997077,5.52537362597298,11.6136024223074));
#70121=CARTESIAN_POINT('Ctrl Pts',(5.65653225593739,5.53060732347208,11.6138959439219));
#70122=CARTESIAN_POINT('Ctrl Pts',(5.64498045529267,5.54240030567731,11.6145575445469));
#70123=CARTESIAN_POINT('Ctrl Pts',(5.63853691769707,5.54895547986091,11.6149254479938));
#70124=CARTESIAN_POINT('Ctrl Pts',(5.62118455127312,5.56654704857579,11.6159131712153));
#70125=CARTESIAN_POINT('Ctrl Pts',(5.61025462628477,5.5775626249371,11.6165321058928));
#70126=CARTESIAN_POINT('Ctrl Pts',(5.56226147264403,5.62564806545191,11.6192358736856));
#70127=CARTESIAN_POINT('Ctrl Pts',(5.52486235894881,5.66238155624846,11.6213065051225));
#70128=CARTESIAN_POINT('Ctrl Pts',(4.85920827364071,6.3033144930139,11.6575382885572));
#70129=CARTESIAN_POINT('Ctrl Pts',(4.13578890552273,6.79991876020181,11.6864662867405));
#70130=CARTESIAN_POINT('Ctrl Pts',(3.1660099092786,7.25256796548579,11.723969375297));
#70131=CARTESIAN_POINT('Ctrl Pts',(2.98295922726337,7.32975511855154,11.7310347468575));
#70132=CARTESIAN_POINT('Ctrl Pts',(2.6237870063464,7.46552299979584,11.7451569221899));
#70133=CARTESIAN_POINT('Ctrl Pts',(2.44812134767194,7.52495808925122,11.7521852291177));
#70134=CARTESIAN_POINT('Ctrl Pts',(2.23744172255077,7.58808067783243,11.7608815521763));
#70135=CARTESIAN_POINT('Ctrl Pts',(2.20429311554061,7.59777636195549,11.7622566101809));
#70136=CARTESIAN_POINT('Ctrl Pts',(2.16036174754652,7.61031421259078,11.7640869759373));
#70137=CARTESIAN_POINT('Ctrl Pts',(2.14963463567596,7.61335118237301,11.7645345434598));
#70138=CARTESIAN_POINT('Ctrl Pts',(2.13203533252269,7.61829358835381,11.765269836125));
#70139=CARTESIAN_POINT('Ctrl Pts',(2.12516690018039,7.62021243164845,11.7655570453459));
#70140=CARTESIAN_POINT('Ctrl Pts',(2.11186875887065,7.62390817388876,11.7661135876519));
#70141=CARTESIAN_POINT('Ctrl Pts',(2.10543937640416,7.62568623341806,11.7663828767579));
#70142=CARTESIAN_POINT('Ctrl Pts',(2.09061122007195,7.62976680951593,11.7670044191273));
#70143=CARTESIAN_POINT('Ctrl Pts',(2.08221088544915,7.6320635917742,11.7673568837643));
#70144=CARTESIAN_POINT('Ctrl Pts',(2.05970137190924,7.63817811410851,11.7683022642162));
#70145=CARTESIAN_POINT('Ctrl Pts',(2.04558540991467,7.64197062096955,11.7688960868105));
#70146=CARTESIAN_POINT('Ctrl Pts',(1.94567850599283,7.66851575747277,11.7731053806426));
#70147=CARTESIAN_POINT('Ctrl Pts',(1.85952206105141,7.68986188733611,11.7767689295909));
#70148=CARTESIAN_POINT('Ctrl Pts',(1.75646751673716,7.71356153581915,11.781178443165));
#70149=CARTESIAN_POINT('Ctrl Pts',(1.73989628461707,7.71731628347817,11.7818883391061));
#70150=CARTESIAN_POINT('Ctrl Pts',(1.19662365178015,7.83857346934994,11.8051869973082));
#70151=CARTESIAN_POINT('Ctrl Pts',(0.659287836616959,7.90192992536936,11.8288601208207));
#70152=CARTESIAN_POINT('Ctrl Pts',(-0.193433763272482,7.91483235956703,
11.8653841944395));
#70153=CARTESIAN_POINT('Ctrl Pts',(-0.506566162748853,7.90097395295921,
11.878608853835));
#70154=CARTESIAN_POINT('Ctrl Pts',(-1.18639068096993,7.83029574412889,11.90701524613));
#70155=CARTESIAN_POINT('Ctrl Pts',(-1.5515856657425,7.76618602852799,11.9221207739951));
#70156=CARTESIAN_POINT('Ctrl Pts',(-1.97461207186458,7.66088327830881,11.9397847546885));
#70157=CARTESIAN_POINT('Ctrl Pts',(-2.03807805662243,7.64424380431644,11.9424372272892));
#70158=CARTESIAN_POINT('Ctrl Pts',(-2.13281889971316,7.618140938867,11.9464003764097));
#70159=CARTESIAN_POINT('Ctrl Pts',(-2.16425388325388,7.6092701989806,11.9477159477078));
#70160=CARTESIAN_POINT('Ctrl Pts',(-2.21837236470394,7.59363584063085,11.9499819163305));
#70161=CARTESIAN_POINT('Ctrl Pts',(-2.2410820753947,7.58696463438578,11.950933113499));
#70162=CARTESIAN_POINT('Ctrl Pts',(-2.29155339858204,7.57189179107308,11.953047875865));
#70163=CARTESIAN_POINT('Ctrl Pts',(-2.3192994555088,7.56343918574742,11.954210962553));
#70164=CARTESIAN_POINT('Ctrl Pts',(-2.39263055412286,7.540658013955,11.9572864034181));
#70165=CARTESIAN_POINT('Ctrl Pts',(-2.43813342565547,7.52606867365385,11.9591962642178));
#70166=CARTESIAN_POINT('Ctrl Pts',(-2.63688177368224,7.46035340928852,11.9675458226683));
#70167=CARTESIAN_POINT('Ctrl Pts',(-2.78867415734696,7.40495213052502,11.9739419401032));
#70168=CARTESIAN_POINT('Ctrl Pts',(-3.44855094367339,7.14093954473215,12.0018995022386));
#70169=CARTESIAN_POINT('Ctrl Pts',(-3.93580363057525,6.88440027061463,12.0228549884201));
#70170=CARTESIAN_POINT('Ctrl Pts',(-4.56677976971644,6.4631517682881,12.052395624773));
#70171=CARTESIAN_POINT('Ctrl Pts',(-4.73631930609016,6.33995929165136,12.0606159343692));
#70172=CARTESIAN_POINT('Ctrl Pts',(-4.92173374058754,6.19363959813403,12.0700683409608));
#70173=CARTESIAN_POINT('Ctrl Pts',(-4.94261813161492,6.17698635890976,12.0711399214685));
#70174=CARTESIAN_POINT('Ctrl Pts',(-4.97403329337885,6.15167453987365,12.0727626973159));
#70175=CARTESIAN_POINT('Ctrl Pts',(-4.98462674283243,6.14309393393588,12.0733117912938));
#70176=CARTESIAN_POINT('Ctrl Pts',(-5.00288523790929,6.12822638076048,12.0742615070649));
#70177=CARTESIAN_POINT('Ctrl Pts',(-5.01056075394301,6.12195231996527,12.0746617667322));
#70178=CARTESIAN_POINT('Ctrl Pts',(-5.02759280759495,6.10797662248854,12.0755522430866));
#70179=CARTESIAN_POINT('Ctrl Pts',(-5.03694347586652,6.10026788588286,12.0760426643604));
#70180=CARTESIAN_POINT('Ctrl Pts',(-5.06180135993526,6.07967880477147,12.077350596979));
#70181=CARTESIAN_POINT('Ctrl Pts',(-5.07727700003152,6.06676071996899,12.0781692647516));
#70182=CARTESIAN_POINT('Ctrl Pts',(-5.15280988895577,6.00321920634209,12.0821864400853));
#70183=CARTESIAN_POINT('Ctrl Pts',(-5.21215960622338,5.95176297700436,12.0854093566284));
#70184=CARTESIAN_POINT('Ctrl Pts',(-5.31910344464904,5.8562160927036,12.0913304058303));
#70185=CARTESIAN_POINT('Ctrl Pts',(-5.36694070752205,5.81240704824798,12.0940219602861));
#70186=CARTESIAN_POINT('Ctrl Pts',(-5.56876835864034,5.62295851015435,12.1055521658863));
#70187=CARTESIAN_POINT('Ctrl Pts',(-5.71740995080261,5.47175156197472,12.114483056172));
#70188=CARTESIAN_POINT('Ctrl Pts',(-6.04007051853839,5.11600158583701,12.1347400885826));
#70189=CARTESIAN_POINT('Ctrl Pts',(-6.21011521253505,4.90819686212203,12.1460554319916));
#70190=CARTESIAN_POINT('Ctrl Pts',(-6.52007920837321,4.48744213779018,12.1678586904135));
#70191=CARTESIAN_POINT('Ctrl Pts',(-6.66093216206234,4.27557695239898,12.1783468107694));
#70192=CARTESIAN_POINT('Ctrl Pts',(-6.82398314142684,4.00265238843444,12.191276675271));
#70193=CARTESIAN_POINT('Ctrl Pts',(-6.85596565550101,3.94762043292549,12.1938559182505));
#70194=CARTESIAN_POINT('Ctrl Pts',(-6.90152585455357,3.86700144580556,12.197595282332));
#70195=CARTESIAN_POINT('Ctrl Pts',(-6.91563249153241,3.84171661549174,12.1987625543951));
#70196=CARTESIAN_POINT('Ctrl Pts',(-6.94016521726196,3.79717097338337,12.2008095087994));
#70197=CARTESIAN_POINT('Ctrl Pts',(-6.95065070835634,3.77794327354758,12.2016899748308));
#70198=CARTESIAN_POINT('Ctrl Pts',(-6.97090900099191,3.74042494120677,12.2034021008175));
#70199=CARTESIAN_POINT('Ctrl Pts',(-6.98068999305033,3.72213893681264,12.2042338621265));
#70200=CARTESIAN_POINT('Ctrl Pts',(-7.00401924416201,3.67810844697983,12.2062302492886));
#70201=CARTESIAN_POINT('Ctrl Pts',(-7.01749763227976,3.65232724568943,12.2073939691314));
#70202=CARTESIAN_POINT('Ctrl Pts',(-7.06685203017204,3.55664126362344,12.2116942605815));
#70203=CARTESIAN_POINT('Ctrl Pts',(-7.10182837993177,3.48627717017877,12.2148195260181));
#70204=CARTESIAN_POINT('Ctrl Pts',(-7.48134210319676,2.6933648350003,12.2496590140817));
#70205=CARTESIAN_POINT('Ctrl Pts',(-7.71536966193981,1.92299114742071,12.2802299309106));
#70206=CARTESIAN_POINT('Ctrl Pts',(-7.88398953567299,0.755288528951129,
12.3243985687035));
#70207=CARTESIAN_POINT('Ctrl Pts',(-7.91112897766017,0.376530074955401,
12.3384731604433));
#70208=CARTESIAN_POINT('Ctrl Pts',(-7.91094292353554,-0.168573338039825,
12.3593972147587));
#70209=CARTESIAN_POINT('Ctrl Pts',(-7.9056694122443,-0.334398991950649,
12.3658561422641));
#70210=CARTESIAN_POINT('Ctrl Pts',(-7.89389772941376,-0.520304129314716,
12.3732917211989));
#70211=CARTESIAN_POINT('Ctrl Pts',(-7.89252880157451,-0.540672597338497,
12.3741090324915));
#70212=CARTESIAN_POINT('Ctrl Pts',(-7.89039630589137,-0.570666596264693,
12.3753167054481));
#70213=CARTESIAN_POINT('Ctrl Pts',(-7.88969392519024,-0.580296470804183,
12.3757050676165));
#70214=CARTESIAN_POINT('Ctrl Pts',(-7.88842254330443,-0.597298459763331,
12.3763918755042));
#70215=CARTESIAN_POINT('Ctrl Pts',(-7.88786083240934,-0.604671117117169,
12.3766900769387));
#70216=CARTESIAN_POINT('Ctrl Pts',(-7.88667732202812,-0.619922804888298,
12.3773077579349));
#70217=CARTESIAN_POINT('Ctrl Pts',(-7.88605404986315,-0.62780171067851,
12.3776272873688));
#70218=CARTESIAN_POINT('Ctrl Pts',(-7.88442622267742,-0.647994427748542,
12.3784473563314));
#70219=CARTESIAN_POINT('Ctrl Pts',(-7.88340462880942,-0.660306819336622,
12.3789484872272));
#70220=CARTESIAN_POINT('Ctrl Pts',(-7.87909898430925,-0.710764403442265,
12.3810068301706));
#70221=CARTESIAN_POINT('Ctrl Pts',(-7.87556691566925,-0.748887530610363,
12.3825729055543));
#70222=CARTESIAN_POINT('Ctrl Pts',(-7.81998220310333,-1.3048707935045,12.4055873459321));
#70223=CARTESIAN_POINT('Ctrl Pts',(-7.71723551499487,-1.81627550322845,
12.429366737792));
#70224=CARTESIAN_POINT('Ctrl Pts',(-7.49214956433761,-2.55221191251773,
12.4646396354337));
#70225=CARTESIAN_POINT('Ctrl Pts',(-7.40799074989495,-2.78707175986403,
12.4760624524673));
#70226=CARTESIAN_POINT('Ctrl Pts',(-7.13891279354165,-3.43916453018471,
12.5078365070028));
#70227=CARTESIAN_POINT('Ctrl Pts',(-6.92880049308469,-3.84496267450702,
12.527628013733));
#70228=CARTESIAN_POINT('Ctrl Pts',(-6.66888418691902,-4.25567824466761,
12.5473877997429));
#70229=CARTESIAN_POINT('Ctrl Pts',(-6.65276449799541,-4.28083381831811,
12.548597206193));
#70230=CARTESIAN_POINT('Ctrl Pts',(-6.6305936048464,-4.31500490212036,12.5502389688052));
#70231=CARTESIAN_POINT('Ctrl Pts',(-6.62466587966553,-4.32410000369459,
12.5506758412599));
#70232=CARTESIAN_POINT('Ctrl Pts',(-6.61456062214397,-4.33953527747424,
12.5514170826851));
#70233=CARTESIAN_POINT('Ctrl Pts',(-6.61039265800405,-4.3458816776194,12.5517218030335));
#70234=CARTESIAN_POINT('Ctrl Pts',(-6.60232570275485,-4.3581264675895,12.5523096380675));
#70235=CARTESIAN_POINT('Ctrl Pts',(-6.59842792876036,-4.36402564864764,
12.5525927972494));
#70236=CARTESIAN_POINT('Ctrl Pts',(-6.58917934580003,-4.37798242395774,
12.5532626204084));
#70237=CARTESIAN_POINT('Ctrl Pts',(-6.58382165223542,-4.38603545448579,
12.5536490290804));
#70238=CARTESIAN_POINT('Ctrl Pts',(-6.56804246605141,-4.4096587399761,12.5547823240929));
#70239=CARTESIAN_POINT('Ctrl Pts',(-6.5575803808945,-4.42520187032525,12.5555277012866));
#70240=CARTESIAN_POINT('Ctrl Pts',(-6.47849450338701,-4.54180045354959,
12.5611172555531));
#70241=CARTESIAN_POINT('Ctrl Pts',(-6.40759196883169,-4.64129391263505,
12.5658752410872));
#70242=CARTESIAN_POINT('Ctrl Pts',(-6.16678465574467,-4.96316303609849,
12.5812565634968));
#70243=CARTESIAN_POINT('Ctrl Pts',(-5.98738170385845,-5.1781749519126,12.5915054056492));
#70244=CARTESIAN_POINT('Ctrl Pts',(-5.58494692041342,-5.61153772323387,
12.6125009678628));
#70245=CARTESIAN_POINT('Ctrl Pts',(-5.35963578123574,-5.82711761938126,
12.6231523282668));
#70246=CARTESIAN_POINT('Ctrl Pts',(-5.01219605947817,-6.12230720410174,
12.6386752315774));
#70247=CARTESIAN_POINT('Ctrl Pts',(-4.89966060832409,-6.21273534339769,
12.6435798729402));
#70248=CARTESIAN_POINT('Ctrl Pts',(-4.64617666636072,-6.40524993083205,
12.6544782755039));
#70249=CARTESIAN_POINT('Ctrl Pts',(-4.50420823607487,-6.50586581502865,
12.6604857838361));
#70250=CARTESIAN_POINT('Ctrl Pts',(-4.10722463127369,-6.76798974426168,
12.6773082800426));
#70251=CARTESIAN_POINT('Ctrl Pts',(-3.84612065961206,-6.91970404113166,
12.6883973511577));
#70252=CARTESIAN_POINT('Ctrl Pts',(-3.56092790012047,-7.0642790755253,12.7011535073613));
#70253=CARTESIAN_POINT('Ctrl Pts',(-3.54481145964228,-7.07237994401317,
12.7018764823961));
#70254=CARTESIAN_POINT('Ctrl Pts',(-3.52254522154923,-7.08347675616798,
12.702878422273));
#70255=CARTESIAN_POINT('Ctrl Pts',(-3.51641892892075,-7.08651999988749,
12.7031544156759));
#70256=CARTESIAN_POINT('Ctrl Pts',(-3.50664698823074,-7.09135843216561,
12.7035951709909));
#70257=CARTESIAN_POINT('Ctrl Pts',(-3.5030038790084,-7.09315877004391,12.7037596061665));
#70258=CARTESIAN_POINT('Ctrl Pts',(-3.4959088763605,-7.09665815229578,12.7040800738716));
#70259=CARTESIAN_POINT('Ctrl Pts',(-3.49245712767554,-7.09835748702438,
12.7042360877296));
#70260=CARTESIAN_POINT('Ctrl Pts',(-3.48419173287023,-7.10241914564412,
12.7046099252819));
#70261=CARTESIAN_POINT('Ctrl Pts',(-3.47937692708046,-7.10477909233291,
12.7048279014368));
#70262=CARTESIAN_POINT('Ctrl Pts',(-3.46487486402493,-7.11186890989261,
12.705485069899));
#70263=CARTESIAN_POINT('Ctrl Pts',(-3.45518049500035,-7.11658379844696,
12.7059252266967));
#70264=CARTESIAN_POINT('Ctrl Pts',(-3.35452710587119,-7.16528275858591,
12.7105041082501));
#70265=CARTESIAN_POINT('Ctrl Pts',(-3.26274681950491,-7.20753845690531,
12.7147537572039));
#70266=CARTESIAN_POINT('Ctrl Pts',(-2.99872330643792,-7.3230187430057,12.7271290693311));
#70267=CARTESIAN_POINT('Ctrl Pts',(-2.82466134133931,-7.39190272322281,
12.73546609378));
#70268=CARTESIAN_POINT('Ctrl Pts',(-2.04211206372408,-7.66991422459173,
12.773180158934));
#70269=CARTESIAN_POINT('Ctrl Pts',(-1.41178166387862,-7.81055909177022,
12.803908750693));
#70270=CARTESIAN_POINT('Ctrl Pts',(-0.511743733597448,-7.8987405318854,
12.8439323632822));
#70271=CARTESIAN_POINT('Ctrl Pts',(-0.250985591616078,-7.91132149617307,
12.8551236232527));
#70272=CARTESIAN_POINT('Ctrl Pts',(0.0831678784627014,-7.91090177594154,
12.8689047692178));
#70273=CARTESIAN_POINT('Ctrl Pts',(0.156395476740914,-7.90979295973493,
12.8718910202751));
#70274=CARTESIAN_POINT('Ctrl Pts',(0.244206198407208,-7.90724338156028,
12.8754322832596));
#70275=CARTESIAN_POINT('Ctrl Pts',(0.25881267319208,-7.90677877305069,12.8760200224908));
#70276=CARTESIAN_POINT('Ctrl Pts',(0.282618152018711,-7.90595552272274,
12.8769757827018));
#70277=CARTESIAN_POINT('Ctrl Pts',(0.291817931135807,-7.90562129392657,
12.8773446234972));
#70278=CARTESIAN_POINT('Ctrl Pts',(0.308219602131311,-7.90499675064557,
12.8780012842433));
#70279=CARTESIAN_POINT('Ctrl Pts',(0.315421711564824,-7.90471265101458,
12.8782893127928));
#70280=CARTESIAN_POINT('Ctrl Pts',(0.330598305899951,-7.9040932095109,12.8788955942288));
#70281=CARTESIAN_POINT('Ctrl Pts',(0.338572694712872,-7.90375564117537,
12.8792137719128));
#70282=CARTESIAN_POINT('Ctrl Pts',(0.359617582645859,-7.90283287017822,
12.8800524454896));
#70283=CARTESIAN_POINT('Ctrl Pts',(0.372687190791276,-7.90222730879096,
12.880572256141));
#70284=CARTESIAN_POINT('Ctrl Pts',(0.431599913346708,-7.89935119199268,
12.8829107320863));
#70285=CARTESIAN_POINT('Ctrl Pts',(0.477424700038748,-7.89671409458951,
12.8847170513157));
#70286=CARTESIAN_POINT('Ctrl Pts',(0.80845729397981,-7.87477193400816,12.8976772563508));
#70287=CARTESIAN_POINT('Ctrl Pts',(1.09246692385802,-7.84041907516085,12.9083098943244));
#70288=CARTESIAN_POINT('Ctrl Pts',(1.90866642295981,-7.69647050323325,12.9379890495746));
#70289=CARTESIAN_POINT('Ctrl Pts',(2.43216735476726,-7.54739815922646,12.955831510622));
#70290=CARTESIAN_POINT('Ctrl Pts',(3.14643934839447,-7.2618911314956,12.9821345141041));
#70291=CARTESIAN_POINT('Ctrl Pts',(3.35288634969586,-7.16891122001979,12.9900062118686));
#70292=CARTESIAN_POINT('Ctrl Pts',(3.7271766991155,-6.98063019661283,13.0052637446836));
#70293=CARTESIAN_POINT('Ctrl Pts',(3.89606783157521,-6.88779278415899,13.0125437376599));
#70294=CARTESIAN_POINT('Ctrl Pts',(4.07318536589359,-6.78183388975971,13.0207941242038));
#70295=CARTESIAN_POINT('Ctrl Pts',(4.08496252187106,-6.77474657262915,13.0213457126258));
#70296=CARTESIAN_POINT('Ctrl Pts',(4.10124360262773,-6.76489097177664,13.0221124810346));
#70297=CARTESIAN_POINT('Ctrl Pts',(4.10576338174277,-6.76214877100989,13.0223257965578));
#70298=CARTESIAN_POINT('Ctrl Pts',(4.1135450087943,-6.7574168924967,13.0226938454136));
#70299=CARTESIAN_POINT('Ctrl Pts',(4.11680815829377,-6.75542938576662,13.0228484215376));
#70300=CARTESIAN_POINT('Ctrl Pts',(4.12355977958542,-6.75131042515161,13.0231687389019));
#70301=CARTESIAN_POINT('Ctrl Pts',(4.12704804072541,-6.74917863017348,13.0233345045565));
#70302=CARTESIAN_POINT('Ctrl Pts',(4.13519525631529,-6.74419091176789,13.0237223011931));
#70303=CARTESIAN_POINT('Ctrl Pts',(4.13985290210613,-6.741332866047,13.0239444830674));
#70304=CARTESIAN_POINT('Ctrl Pts',(4.15480392247154,-6.7321372152446,13.0246592318724));
#70305=CARTESIAN_POINT('Ctrl Pts',(4.16508568870247,-6.72578087076789,13.0251531189568));
#70306=CARTESIAN_POINT('Ctrl Pts',(4.36799340736201,-6.59969652094499,13.0349458197738));
#70307=CARTESIAN_POINT('Ctrl Pts',(4.55538192507872,-6.47177247722091,13.0448083376605));
#70308=CARTESIAN_POINT('Ctrl Pts',(5.2003773730214,-5.9895519752051,13.0809877119812));
#70309=CARTESIAN_POINT('Ctrl Pts',(5.6243494887328,-5.5933328140834,13.1088561423947));
#70310=CARTESIAN_POINT('Ctrl Pts',(6.34581639885618,-4.75332357639945,13.1599965414283));
#70311=CARTESIAN_POINT('Ctrl Pts',(6.64926751996135,-4.31866419020705,13.1833288148501));
#70312=CARTESIAN_POINT('Ctrl Pts',(6.92370875687746,-3.82718399292746,13.2062462508969));
#70313=CARTESIAN_POINT('Ctrl Pts',(6.94011649178461,-3.79734952118029,13.2076252764666));
#70314=CARTESIAN_POINT('Ctrl Pts',(6.96224822833813,-3.75648439130198,13.2094978426363));
#70315=CARTESIAN_POINT('Ctrl Pts',(6.96813947927014,-3.74554503035532,13.2099975310944));
#70316=CARTESIAN_POINT('Ctrl Pts',(6.97742625535198,-3.72820283452315,13.210787191168));
#70317=CARTESIAN_POINT('Ctrl Pts',(6.98083878334621,-3.72180915758926,13.2110777851002));
#70318=CARTESIAN_POINT('Ctrl Pts',(6.98742534323375,-3.70942771868935,13.2116394907264));
#70319=CARTESIAN_POINT('Ctrl Pts',(6.9906004758436,-3.70344055101387,13.2119106424804));
#70320=CARTESIAN_POINT('Ctrl Pts',(6.99812114837816,-3.68921511233897,13.2125537918746));
#70321=CARTESIAN_POINT('Ctrl Pts',(7.00245984484999,-3.68097322382787,13.2129255400676));
#70322=CARTESIAN_POINT('Ctrl Pts',(7.01522912263288,-3.65661212862132,13.2140217621512));
#70323=CARTESIAN_POINT('Ctrl Pts',(7.02361870030412,-3.64047143386169,13.2147447476181));
#70324=CARTESIAN_POINT('Ctrl Pts',(7.08860692581546,-3.51437980706251,13.2203670509686));
#70325=CARTESIAN_POINT('Ctrl Pts',(7.14267749232969,-3.40314171565699,13.2251747264478));
#70326=CARTESIAN_POINT('Ctrl Pts',(7.32373600397322,-3.00730947563662,13.2417938038197));
#70327=CARTESIAN_POINT('Ctrl Pts',(7.43650200595465,-2.71651907479519,13.2531180230539));
#70328=CARTESIAN_POINT('Ctrl Pts',(7.68074788304711,-1.95629004921626,13.2813300127674));
#70329=CARTESIAN_POINT('Ctrl Pts',(7.78655714297726,-1.48002151445437,13.29766845675));
#70330=CARTESIAN_POINT('Ctrl Pts',(7.88800319004038,-0.68153548830664,13.3262218467346));
#70331=CARTESIAN_POINT('Ctrl Pts',(7.90902565384798,-0.363878220777233,
13.3379312660078));
#70332=CARTESIAN_POINT('Ctrl Pts',(7.91100511558555,-0.0220198555669485,
13.3515476374036));
#70333=CARTESIAN_POINT('Ctrl Pts',(7.91103556269699,0.00176689301103428,
13.3524995600894));
#70334=CARTESIAN_POINT('Ctrl Pts',(7.91093050328304,0.034291954984522,13.3538070446172));
#70335=CARTESIAN_POINT('Ctrl Pts',(7.91088779676659,0.0430305951357745,
13.3541589105356));
#70336=CARTESIAN_POINT('Ctrl Pts',(7.91079040641116,0.0579127981321211,
13.35475911931));
#70337=CARTESIAN_POINT('Ctrl Pts',(7.91074304487798,0.0640564126838488,
13.3550071764854));
#70338=CARTESIAN_POINT('Ctrl Pts',(7.91063754482319,0.0759449968300303,
13.355487732757));
#70339=CARTESIAN_POINT('Ctrl Pts',(7.91058030465561,0.0816899717049817,
13.3557201971834));
#70340=CARTESIAN_POINT('Ctrl Pts',(7.91042951927387,0.0953320152892803,
13.3562727788523));
#70341=CARTESIAN_POINT('Ctrl Pts',(7.9103304067409,0.103229008297088,13.3565931067895));
#70342=CARTESIAN_POINT('Ctrl Pts',(7.91000276441198,0.126551425152569,13.3575404605473));
#70343=CARTESIAN_POINT('Ctrl Pts',(7.90974093909563,0.141976295464001,13.3581687223974));
#70344=CARTESIAN_POINT('Ctrl Pts',(7.90736403277617,0.261416929245609,13.3630463935562));
#70345=CARTESIAN_POINT('Ctrl Pts',(7.90324243665916,0.365380144076104,13.3673670887883));
#70346=CARTESIAN_POINT('Ctrl Pts',(7.88085197158054,0.742209174616122,13.3832446307259));
#70347=CARTESIAN_POINT('Ctrl Pts',(7.85048909334578,1.01415669672764,13.3951102836394));
#70348=CARTESIAN_POINT('Ctrl Pts',(7.75621939416736,1.5872825190564,13.4204932609149));
#70349=CARTESIAN_POINT('Ctrl Pts',(7.68869444826428,1.88742870221137,13.4340077710592));
#70350=CARTESIAN_POINT('Ctrl Pts',(7.55643929391266,2.34812723892847,13.4547945815904));
#70351=CARTESIAN_POINT('Ctrl Pts',(7.50362768984153,2.51178223856262,13.4621902346964));
#70352=CARTESIAN_POINT('Ctrl Pts',(7.34003922498173,2.96735030229902,13.4827742878316));
#70353=CARTESIAN_POINT('Ctrl Pts',(7.21725733351476,3.25462080078784,13.4957402822217));
#70354=CARTESIAN_POINT('Ctrl Pts',(7.06130130625612,3.56697515752773,13.5098862036261));
#70355=CARTESIAN_POINT('Ctrl Pts',(7.04455398198891,3.59993710111737,13.5113798331956));
#70356=CARTESIAN_POINT('Ctrl Pts',(7.01917349858612,3.64903538236361,13.513606109142));
#70357=CARTESIAN_POINT('Ctrl Pts',(7.01071444890233,3.66526107449348,13.5143420626276));
#70358=CARTESIAN_POINT('Ctrl Pts',(6.9960767480636,3.69310224928894,13.5156052464317));
#70359=CARTESIAN_POINT('Ctrl Pts',(6.98992528675756,3.7047319167885,13.5161330124327));
#70360=CARTESIAN_POINT('Ctrl Pts',(6.97718613108572,3.72867129371056,13.5172196417223));
#70361=CARTESIAN_POINT('Ctrl Pts',(6.97059480183289,3.7409790208575,13.5177784295066));
#70362=CARTESIAN_POINT('Ctrl Pts',(6.95536350046394,3.76923980696297,13.5190618047613));
#70363=CARTESIAN_POINT('Ctrl Pts',(6.94670115424453,3.78518073846935,13.5197859303597));
#70364=CARTESIAN_POINT('Ctrl Pts',(6.91928725453774,3.83521825656811,13.5220596027478));
#70365=CARTESIAN_POINT('Ctrl Pts',(6.90033884811351,3.86920650784861,13.5236050155179));
#70366=CARTESIAN_POINT('Ctrl Pts',(6.85600984341112,3.9473591855416,13.5271609944496));
#70367=CARTESIAN_POINT('Ctrl Pts',(6.83045186110074,3.99142117049217,13.5291676551678));
#70368=CARTESIAN_POINT('Ctrl Pts',(6.42445478118277,4.67603951395493,13.5603788505829));
#70369=CARTESIAN_POINT('Ctrl Pts',(5.95585745240629,5.25991456050197,13.5869036925496));
#70370=CARTESIAN_POINT('Ctrl Pts',(5.17560209973628,5.99187707791571,13.6261808213525));
#70371=CARTESIAN_POINT('Ctrl Pts',(4.92523381000498,6.19931379996694,13.6383121588653));
#70372=CARTESIAN_POINT('Ctrl Pts',(4.6477968454869,6.40173824060358,13.6520143020839));
#70373=CARTESIAN_POINT('Ctrl Pts',(4.63270956515399,6.41266482008458,13.6527602464552));
#70374=CARTESIAN_POINT('Ctrl Pts',(4.61166170459041,6.42779515222198,13.653802216833));
#70375=CARTESIAN_POINT('Ctrl Pts',(4.60573361396373,6.43204415977029,13.6540958312776));
#70376=CARTESIAN_POINT('Ctrl Pts',(4.59550455780423,6.43935452739607,13.6546027351572));
#70377=CARTESIAN_POINT('Ctrl Pts',(4.59120638237387,6.44241979573845,13.6548158130943));
#70378=CARTESIAN_POINT('Ctrl Pts',(4.58232091980058,6.44874310591347,13.6552564745998));
#70379=CARTESIAN_POINT('Ctrl Pts',(4.57773322008242,6.45200055979598,13.6554840900156));
#70380=CARTESIAN_POINT('Ctrl Pts',(4.56703116388776,6.45958229554746,13.6560152958301));
#70381=CARTESIAN_POINT('Ctrl Pts',(4.56091414147107,6.4639027899879,13.6563190949626));
#70382=CARTESIAN_POINT('Ctrl Pts',(4.54134477863286,6.4776831550029,13.6572915888545));
#70383=CARTESIAN_POINT('Ctrl Pts',(4.5278691348644,6.48710972206702,13.6579621470252));
#70384=CARTESIAN_POINT('Ctrl Pts',(4.49676662714164,6.50872261767476,13.6595121082597));
#70385=CARTESIAN_POINT('Ctrl Pts',(4.47911943699744,6.52087948676193,13.6603932216758));
#70386=CARTESIAN_POINT('Ctrl Pts',(4.4187223680554,6.56212521401816,13.6634152104931));
#70387=CARTESIAN_POINT('Ctrl Pts',(4.3757376535872,6.5908659881499,13.6655765939995));
#70388=CARTESIAN_POINT('Ctrl Pts',(4.16637816783898,6.72789872996754,13.6761440554093));
#70389=CARTESIAN_POINT('Ctrl Pts',(3.9962567659548,6.83031855292808,13.6848521688649));
#70390=CARTESIAN_POINT('Ctrl Pts',(3.52119675655663,7.09249662130454,13.7091634006234));
#70391=CARTESIAN_POINT('Ctrl Pts',(3.20939841942565,7.23892856657625,13.7251013611657));
#70392=CARTESIAN_POINT('Ctrl Pts',(2.27195763366182,7.60667854130153,13.7714745325932));
#70393=CARTESIAN_POINT('Ctrl Pts',(1.62677800316817,7.77027657844395,13.8012503850251));
#70394=CARTESIAN_POINT('Ctrl Pts',(0.92677360516341,7.85664016368797,13.8300788304247));
#70395=CARTESIAN_POINT('Ctrl Pts',(0.884824922468746,7.86147498264042,13.8317946270485));
#70396=CARTESIAN_POINT('Ctrl Pts',(0.828681361628141,7.86749076545296,13.8340755264006));
#70397=CARTESIAN_POINT('Ctrl Pts',(0.814519481856601,7.86896954879795,13.8346495533726));
#70398=CARTESIAN_POINT('Ctrl Pts',(0.792379770655545,7.87122096876801,13.8355449044463));
#70399=CARTESIAN_POINT('Ctrl Pts',(0.784404658984386,7.87201972631806,13.8358670114656));
#70400=CARTESIAN_POINT('Ctrl Pts',(0.769146049729517,7.87352455394798,13.8364825029414));
#70401=CARTESIAN_POINT('Ctrl Pts',(0.761862761907683,7.87423264069644,13.8367759475751));
#70402=CARTESIAN_POINT('Ctrl Pts',(0.744830788677803,7.8758646500763,13.8374613675367));
#70403=CARTESIAN_POINT('Ctrl Pts',(0.735081339892921,7.87678058058522,13.8378531028979));
#70404=CARTESIAN_POINT('Ctrl Pts',(0.707154712912288,7.87935189978771,13.8389734560641));
#70405=CARTESIAN_POINT('Ctrl Pts',(0.688973421235429,7.88096249064679,13.8397007306963));
#70406=CARTESIAN_POINT('Ctrl Pts',(0.571513940217959,7.89095806939856,13.8443857330652));
#70407=CARTESIAN_POINT('Ctrl Pts',(0.472088540911872,7.89753003822413,13.8482888984392));
#70408=CARTESIAN_POINT('Ctrl Pts',(0.176714189488021,7.91145594826203,13.8597134977731));
#70409=CARTESIAN_POINT('Ctrl Pts',(-0.019416305734166,7.91340582274937,
13.8670749875113));
#70410=CARTESIAN_POINT('Ctrl Pts',(-0.347925794187607,7.90445686131532,
13.8791255750927));
#70411=CARTESIAN_POINT('Ctrl Pts',(-0.480317729926491,7.89751776345304,
13.8839063631969));
#70412=CARTESIAN_POINT('Ctrl Pts',(-0.84892559843332,7.86889396315792,13.8970742118697));
#70413=CARTESIAN_POINT('Ctrl Pts',(-1.08443423228592,7.83990898624841,13.9053203770593));
#70414=CARTESIAN_POINT('Ctrl Pts',(-1.50263648320707,7.76923160068669,13.9199857568496));
#70415=CARTESIAN_POINT('Ctrl Pts',(-1.68582187551429,7.73155095242213,13.926418659946));
#70416=CARTESIAN_POINT('Ctrl Pts',(-2.30228634592221,7.58179362510882,13.9484616739566));
#70417=CARTESIAN_POINT('Ctrl Pts',(-2.72732533387491,7.439476070655,13.9643341635458));
#70418=CARTESIAN_POINT('Ctrl Pts',(-3.1702944621503,7.24806101527795,13.9834022714797));
#70419=CARTESIAN_POINT('Ctrl Pts',(-3.20245338658352,7.23390957313716,13.9848004020707));
#70420=CARTESIAN_POINT('Ctrl Pts',(-3.24516269989113,7.21477485026682,13.9866747013566));
#70421=CARTESIAN_POINT('Ctrl Pts',(-3.25579817876838,7.20998164395142,13.9871428911578));
#70422=CARTESIAN_POINT('Ctrl Pts',(-3.27236107149047,7.20247294514798,13.9878742390647));
#70423=CARTESIAN_POINT('Ctrl Pts',(-3.2782958212829,7.19977360863918,13.9881367388999));
#70424=CARTESIAN_POINT('Ctrl Pts',(-3.29021997117679,7.19433227845172,13.9886650441898));
#70425=CARTESIAN_POINT('Ctrl Pts',(-3.29620929665295,7.19159013458303,13.9889308555334));
#70426=CARTESIAN_POINT('Ctrl Pts',(-3.30964356169433,7.18541910253192,13.9895280827967));
#70427=CARTESIAN_POINT('Ctrl Pts',(-3.31708660623242,7.18198612019348,13.9898596597143));
#70428=CARTESIAN_POINT('Ctrl Pts',(-3.33906716957666,7.17180648749431,13.9908408840315));
#70429=CARTESIAN_POINT('Ctrl Pts',(-3.35358949291768,7.16502724109791,13.9914917859102));
#70430=CARTESIAN_POINT('Ctrl Pts',(-3.46699352433759,7.11166817130854,13.9965946310388));
#70431=CARTESIAN_POINT('Ctrl Pts',(-3.56491873156037,7.06308867132844,14.0011198256364));
#70432=CARTESIAN_POINT('Ctrl Pts',(-3.92791176111297,6.87354005795813,14.0182716057813));
#70433=CARTESIAN_POINT('Ctrl Pts',(-4.18588943512417,6.71955101106894,14.0312174971903));
#70434=CARTESIAN_POINT('Ctrl Pts',(-4.62733864500261,6.42073915520068,14.0542418758444));
#70435=CARTESIAN_POINT('Ctrl Pts',(-4.81433589561284,6.28174547402739,14.0643044833392));
#70436=CARTESIAN_POINT('Ctrl Pts',(-5.2929588896299,5.89204644265265,14.0907438012491));
#70437=CARTESIAN_POINT('Ctrl Pts',(-5.57291658280146,5.62798768354655,14.106909344237));
#70438=CARTESIAN_POINT('Ctrl Pts',(-6.03317027384588,5.12571294755363,14.1350405623342));
#70439=CARTESIAN_POINT('Ctrl Pts',(-6.22128262891421,4.89568423554769,14.1471474375716));
#70440=CARTESIAN_POINT('Ctrl Pts',(-6.43660198069764,4.59987296973472,14.1619778642588));
#70441=CARTESIAN_POINT('Ctrl Pts',(-6.47645402657645,4.54359105927815,14.1647665498412));
#70442=CARTESIAN_POINT('Ctrl Pts',(-6.53445206264249,4.45936836077071,14.1688911910025));
#70443=CARTESIAN_POINT('Ctrl Pts',(-6.55316552531535,4.43182259834525,14.1702326423048));
#70444=CARTESIAN_POINT('Ctrl Pts',(-6.58630364509432,4.38237526675871,14.1726272915516));
#70445=CARTESIAN_POINT('Ctrl Pts',(-6.60079436457796,4.36051859821404,14.1736811482571));
#70446=CARTESIAN_POINT('Ctrl Pts',(-6.6285553272511,4.31819064185481,14.1757132065426));
#70447=CARTESIAN_POINT('Ctrl Pts',(-6.64184007920961,4.2977292273864,14.1766915496187));
#70448=CARTESIAN_POINT('Ctrl Pts',(-6.67053604489903,4.2530803414051,14.1788178566927));
#70449=CARTESIAN_POINT('Ctrl Pts',(-6.68591081478279,4.22886983719592,14.1799654227316));
#70450=CARTESIAN_POINT('Ctrl Pts',(-6.74606033479842,4.13300496208066,14.18448828381));
#70451=CARTESIAN_POINT('Ctrl Pts',(-6.78981779721852,4.06071847143417,14.187852450383));
#70452=CARTESIAN_POINT('Ctrl Pts',(-6.9518038119753,3.78317944427748,14.2006008887999));
#70453=CARTESIAN_POINT('Ctrl Pts',(-7.06195251964445,3.5733531414311,14.2098917535242));
#70454=CARTESIAN_POINT('Ctrl Pts',(-7.25126217980454,3.16966882281385,14.2272552711131));
#70455=CARTESIAN_POINT('Ctrl Pts',(-7.33246878775492,2.9769961361698,14.2353365447301));
#70456=CARTESIAN_POINT('Ctrl Pts',(-7.43576586967369,2.70194349037944,14.2466936980983));
#70457=CARTESIAN_POINT('Ctrl Pts',(-7.46430252799417,2.62207941174306,14.2499709647801));
#70458=CARTESIAN_POINT('Ctrl Pts',(-7.59569624133899,2.23481316966507,14.2657946939803));
#70459=CARTESIAN_POINT('Ctrl Pts',(-7.68087562455405,1.92175157049473,14.2783729672968));
#70460=CARTESIAN_POINT('Ctrl Pts',(-7.75232917856588,1.57673995305073,14.2924655405697));
#70461=CARTESIAN_POINT('Ctrl Pts',(-7.75790158680702,1.54908990318224,14.2935966034708));
#70462=CARTESIAN_POINT('Ctrl Pts',(-7.76604301512412,1.50754651239229,14.29529893697));
#70463=CARTESIAN_POINT('Ctrl Pts',(-7.76872289889706,1.49367503765232,14.2958678434983));
#70464=CARTESIAN_POINT('Ctrl Pts',(-7.7734253348885,1.46897951394598,14.2968816187653));
#70465=CARTESIAN_POINT('Ctrl Pts',(-7.77546247579389,1.45815826853639,14.297326163986));
#70466=CARTESIAN_POINT('Ctrl Pts',(-7.77934118168447,1.43731541513366,14.2981830619638));
#70467=CARTESIAN_POINT('Ctrl Pts',(-7.78118599136153,1.42729443028998,14.2985953400622));
#70468=CARTESIAN_POINT('Ctrl Pts',(-7.78512765935432,1.40564855573744,14.2994865465338));
#70469=CARTESIAN_POINT('Ctrl Pts',(-7.78721784540623,1.39402251145441,14.2999656296989));
#70470=CARTESIAN_POINT('Ctrl Pts',(-7.79225814712182,1.36562221892125,14.3011369976424));
#70471=CARTESIAN_POINT('Ctrl Pts',(-7.79518013244954,1.34884312483217,14.3018299367363));
#70472=CARTESIAN_POINT('Ctrl Pts',(-7.80934752160713,1.2659051096327,14.3052592022005));
#70473=CARTESIAN_POINT('Ctrl Pts',(-7.81980486559591,1.19961499648297,14.3080130139937));
#70474=CARTESIAN_POINT('Ctrl Pts',(-7.88353766025106,0.759277547792316,
14.326369812278));
#70475=CARTESIAN_POINT('Ctrl Pts',(-7.91079964517495,0.381969395142818,
14.3423822839279));
#70476=CARTESIAN_POINT('Ctrl Pts',(-7.9109988997264,0.00417235277290443,
14.3582990582019));
#70477=CARTESIAN_POINT('',(-7.90819530369822,-0.000235767854399078,16.3575721401914));
#70478=CARTESIAN_POINT('Ctrl Pts',(-7.90990495318262,0.00414520974019739,
14.3576684917631));
#70479=CARTESIAN_POINT('Ctrl Pts',(-7.90763939544643,-0.844290181882231,
14.3918532068026));
#70480=CARTESIAN_POINT('Ctrl Pts',(-7.55560401264065,-3.01018261765953,
14.4789591888192));
#70481=CARTESIAN_POINT('Ctrl Pts',(-4.90838355554223,-7.20519306720496,
14.6719077047901));
#70482=CARTESIAN_POINT('Ctrl Pts',(2.27684130052813,-9.07257823005059,14.9365140396761));
#70483=CARTESIAN_POINT('Ctrl Pts',(8.87314431977926,-2.98208636427268,15.2540416415389));
#70484=CARTESIAN_POINT('Ctrl Pts',(7.55975124971049,4.34219026825647,15.518647976425));
#70485=CARTESIAN_POINT('Ctrl Pts',(3.20850006480449,7.5750851400838,15.7303330443335));
#70486=CARTESIAN_POINT('Ctrl Pts',(-2.16791332744556,8.4515283681303,15.9420181122423));
#70487=CARTESIAN_POINT('Ctrl Pts',(-7.00166927530617,5.16152017814356,16.1510978108616));
#70488=CARTESIAN_POINT('Ctrl Pts',(-7.91003961585176,1.25389860036366,16.3072562425037));
#70489=CARTESIAN_POINT('Ctrl Pts',(-7.90819530369822,-0.000235767854399078,
16.3575721401914));
#70490=CARTESIAN_POINT('',(-7.91099999795386,-0.000179927557964477,20.3534744230576));
#70491=CARTESIAN_POINT('Ctrl Pts',(-7.91099999818148,-0.000169625007045761,
16.3591892934433));
#70492=CARTESIAN_POINT('Ctrl Pts',(-7.91099702810346,-0.138688629851337,
16.3648599814544));
#70493=CARTESIAN_POINT('Ctrl Pts',(-7.90735590079701,-0.277186163552383,
16.3705089826685));
#70494=CARTESIAN_POINT('Ctrl Pts',(-7.89566147356344,-0.499527941317111,
16.3795600850917));
#70495=CARTESIAN_POINT('Ctrl Pts',(-7.88990300868537,-0.583462861242157,
16.3829714920976));
#70496=CARTESIAN_POINT('Ctrl Pts',(-7.87986244070676,-0.702073691726116,
16.387784110266));
#70497=CARTESIAN_POINT('Ctrl Pts',(-7.87668778112999,-0.736837269673295,
16.3891936542688));
#70498=CARTESIAN_POINT('Ctrl Pts',(-7.87072527718944,-0.797679381472114,
16.391658891131));
#70499=CARTESIAN_POINT('Ctrl Pts',(-7.86803764990721,-0.823767156926277,
16.3927153825496));
#70500=CARTESIAN_POINT('Ctrl Pts',(-7.86252930117675,-0.874746540085974,
16.3947788755023));
#70501=CARTESIAN_POINT('Ctrl Pts',(-7.859719973982,-0.899639069822063,16.395785961393));
#70502=CARTESIAN_POINT('Ctrl Pts',(-7.85391791030823,-0.948946510252506,
16.397779873353));
#70503=CARTESIAN_POINT('Ctrl Pts',(-7.85092944394953,-0.973361644653989,
16.39876672544));
#70504=CARTESIAN_POINT('Ctrl Pts',(-7.84360537018038,-1.03096860616319,
16.4010941542709));
#70505=CARTESIAN_POINT('Ctrl Pts',(-7.83917286517155,-1.06414767311025,
16.4024338441374));
#70506=CARTESIAN_POINT('Ctrl Pts',(-7.82282553032091,-1.18086502861993,
16.4071440094059));
#70507=CARTESIAN_POINT('Ctrl Pts',(-7.8097847811458,-1.26424021908153,16.4105038977454));
#70508=CARTESIAN_POINT('Ctrl Pts',(-7.76685881046335,-1.51259098135986,
16.4205026969115));
#70509=CARTESIAN_POINT('Ctrl Pts',(-7.73306062228825,-1.67684282546261,
16.427102509766));
#70510=CARTESIAN_POINT('Ctrl Pts',(-7.56912444529879,-2.36238953531032,
16.4546830847381));
#70511=CARTESIAN_POINT('Ctrl Pts',(-7.39128540198393,-2.87078667416051,
16.475140701656));
#70512=CARTESIAN_POINT('Ctrl Pts',(-7.09711954390062,-3.49844828073813,
16.5022715884294));
#70513=CARTESIAN_POINT('Ctrl Pts',(-7.02677112315478,-3.63768223284488,
16.5084248019897));
#70514=CARTESIAN_POINT('Ctrl Pts',(-6.94373720427147,-3.79061483349588,
16.5153920383527));
#70515=CARTESIAN_POINT('Ctrl Pts',(-6.93506536196415,-3.80645709283556,
16.5161163256904));
#70516=CARTESIAN_POINT('Ctrl Pts',(-6.92037229639406,-3.83308241562713,
16.5173380451424));
#70517=CARTESIAN_POINT('Ctrl Pts',(-6.91437992174831,-3.84388134861235,
16.517834797546));
#70518=CARTESIAN_POINT('Ctrl Pts',(-6.90331006903885,-3.8637208235337,16.5187497427036));
#70519=CARTESIAN_POINT('Ctrl Pts',(-6.89824005400551,-3.8727655064668,16.5191677526948));
#70520=CARTESIAN_POINT('Ctrl Pts',(-6.88832730817703,-3.89036818134578,
16.5199830515246));
#70521=CARTESIAN_POINT('Ctrl Pts',(-6.88348637337637,-3.89892716499044,
16.5203802946748));
#70522=CARTESIAN_POINT('Ctrl Pts',(-6.87215987251667,-3.91886606705995,
16.5213076503013));
#70523=CARTESIAN_POINT('Ctrl Pts',(-6.86566198309094,-3.93023893641888,
16.5218380807621));
#70524=CARTESIAN_POINT('Ctrl Pts',(-6.84687391321031,-3.96293379858266,
16.5233673273332));
#70525=CARTESIAN_POINT('Ctrl Pts',(-6.83451252399377,-3.98421450451254,
16.5243680892133));
#70526=CARTESIAN_POINT('Ctrl Pts',(-6.73564155043303,-4.15261134221547,
16.532329031178));
#70527=CARTESIAN_POINT('Ctrl Pts',(-6.6444927364507,-4.29694797612673,16.5394052933685));
#70528=CARTESIAN_POINT('Ctrl Pts',(-6.31328910573177,-4.78565053455505,
16.564088017228));
#70529=CARTESIAN_POINT('Ctrl Pts',(-6.0505532695961,-5.11379327346394,16.5819190240991));
#70530=CARTESIAN_POINT('Ctrl Pts',(-5.62491406399624,-5.56640879857414,
16.6078912520514));
#70531=CARTESIAN_POINT('Ctrl Pts',(-5.4812367991102,-5.7079427972747,16.6162505186416));
#70532=CARTESIAN_POINT('Ctrl Pts',(-5.27246869853824,-5.89843680842886,
16.6278437875401));
#70533=CARTESIAN_POINT('Ctrl Pts',(-5.21179429089689,-5.95211587797516,
16.6311520188961));
#70534=CARTESIAN_POINT('Ctrl Pts',(-5.10385257482604,-6.0446964530064,16.6369335892106));
#70535=CARTESIAN_POINT('Ctrl Pts',(-5.05693840622139,-6.08399871420263,
16.6394130929294));
#70536=CARTESIAN_POINT('Ctrl Pts',(-4.98761386913091,-6.14071932874993,
16.6430298534107));
#70537=CARTESIAN_POINT('Ctrl Pts',(-4.96555852829936,-6.15856756821716,
16.6441736540967));
#70538=CARTESIAN_POINT('Ctrl Pts',(-4.92730165749428,-6.18918774583637,
16.6461460400135));
#70539=CARTESIAN_POINT('Ctrl Pts',(-4.91114533206358,-6.2020156487724,16.6469754561016));
#70540=CARTESIAN_POINT('Ctrl Pts',(-4.87883630728768,-6.22746316244811,
16.6486271330586));
#70541=CARTESIAN_POINT('Ctrl Pts',(-4.86268436924029,-6.24008348350396,
16.6494493994557));
#70542=CARTESIAN_POINT('Ctrl Pts',(-4.81988491349509,-6.27325776307819,
16.6516192904687));
#70543=CARTESIAN_POINT('Ctrl Pts',(-4.79315493287898,-6.29370473915348,
16.6529653660239));
#70544=CARTESIAN_POINT('Ctrl Pts',(-4.6966830559512,-6.36652939223119,16.6577916797023));
#70545=CARTESIAN_POINT('Ctrl Pts',(-4.62620618402064,-6.41792371226835,
16.6612581834255));
#70546=CARTESIAN_POINT('Ctrl Pts',(-3.88575563128781,-6.93935213906297,
16.6971122496134));
#70547=CARTESIAN_POINT('Ctrl Pts',(-3.14749277660903,-7.30391137957557,
16.728279656686));
#70548=CARTESIAN_POINT('Ctrl Pts',(-2.00280354864637,-7.66276491964995,
16.7731609227091));
#70549=CARTESIAN_POINT('Ctrl Pts',(-1.63136414884033,-7.75034328118297,
16.7873270927641));
#70550=CARTESIAN_POINT('Ctrl Pts',(-1.11848195793934,-7.83275549591297,
16.8073858368042));
#70551=CARTESIAN_POINT('Ctrl Pts',(-0.981339535757896,-7.85111655824607,
16.812800484503));
#70552=CARTESIAN_POINT('Ctrl Pts',(-0.825697836469471,-7.86781260507817,
16.8190559927588));
#70553=CARTESIAN_POINT('Ctrl Pts',(-0.807598761753455,-7.86969099393013,
16.8197851165736));
#70554=CARTESIAN_POINT('Ctrl Pts',(-0.780366014791391,-7.87242237377243,
16.8208849029204));
#70555=CARTESIAN_POINT('Ctrl Pts',(-0.771237016371916,-7.8733219553073,
16.8212540327628));
#70556=CARTESIAN_POINT('Ctrl Pts',(-0.755519377502438,-7.87484318998133,
16.8218903866215));
#70557=CARTESIAN_POINT('Ctrl Pts',(-0.748931473157895,-7.87547245851339,
16.8221573543464));
#70558=CARTESIAN_POINT('Ctrl Pts',(-0.735347293658637,-7.87675280363303,
16.8227083566559));
#70559=CARTESIAN_POINT('Ctrl Pts',(-0.728350927388893,-7.8774028269485,
16.8229924269215));
#70560=CARTESIAN_POINT('Ctrl Pts',(-0.709474536288181,-7.87913124528543,
16.8237596381439));
#70561=CARTESIAN_POINT('Ctrl Pts',(-0.697592948207542,-7.8801920899717,
16.8242433879757));
#70562=CARTESIAN_POINT('Ctrl Pts',(-0.653834811043981,-7.88399928319668,
16.8260281606536));
#70563=CARTESIAN_POINT('Ctrl Pts',(-0.621944335365847,-7.88657909766544,
16.8273351214225));
#70564=CARTESIAN_POINT('Ctrl Pts',(-0.0903071567596755,-7.92634183716924,
16.8492374933701));
#70565=CARTESIAN_POINT('Ctrl Pts',(0.411734134838231,-7.91614184292397,
16.872006878316));
#70566=CARTESIAN_POINT('Ctrl Pts',(1.24217752392004,-7.82005078107087,16.9103094987087));
#70567=CARTESIAN_POINT('Ctrl Pts',(1.57226479924577,-7.76042510119439,16.9256856146406));
#70568=CARTESIAN_POINT('Ctrl Pts',(2.28209549621272,-7.58504030034019,16.9583254813782));
#70569=CARTESIAN_POINT('Ctrl Pts',(2.65895724579031,-7.46128669114439,16.9753637315994));
#70570=CARTESIAN_POINT('Ctrl Pts',(3.05365971936996,-7.29794803104929,16.992733206555));
#70571=CARTESIAN_POINT('Ctrl Pts',(3.08225116141491,-7.28591867589262,16.9939888831089));
#70572=CARTESIAN_POINT('Ctrl Pts',(3.12169079924542,-7.26905142348819,16.9957175600027));
#70573=CARTESIAN_POINT('Ctrl Pts',(3.13259977252125,-7.26435686831149,16.9961953464088));
#70574=CARTESIAN_POINT('Ctrl Pts',(3.15099891434594,-7.25638984977537,16.9970005751208));
#70575=CARTESIAN_POINT('Ctrl Pts',(3.15849464116724,-7.25313031817039,16.9973284506703));
#70576=CARTESIAN_POINT('Ctrl Pts',(3.17331759029196,-7.24665719390785,16.9979764953645));
#70577=CARTESIAN_POINT('Ctrl Pts',(3.18064501428476,-7.24344409162011,16.9982966804312));
#70578=CARTESIAN_POINT('Ctrl Pts',(3.19678381663278,-7.23633795681649,16.9990015390025));
#70579=CARTESIAN_POINT('Ctrl Pts',(3.20559299097138,-7.23243993218401,16.9993860436491));
#70580=CARTESIAN_POINT('Ctrl Pts',(3.23633073649572,-7.21877141119608,17.0007268822206));
#70581=CARTESIAN_POINT('Ctrl Pts',(3.25822203453082,-7.20891715236306,17.001680381894));
#70582=CARTESIAN_POINT('Ctrl Pts',(3.47876496686351,-7.10843103539184,17.0112722642425));
#70583=CARTESIAN_POINT('Ctrl Pts',(3.67363570175245,-7.00970805591823,17.0196280194292));
#70584=CARTESIAN_POINT('Ctrl Pts',(4.1872412039892,-6.72220222693817,17.04148233463));
#70585=CARTESIAN_POINT('Ctrl Pts',(4.49721821290795,-6.51889893336964,17.0544703233563));
#70586=CARTESIAN_POINT('Ctrl Pts',(5.20527690965082,-5.9798841755385,17.0850167760022));
#70587=CARTESIAN_POINT('Ctrl Pts',(5.58668393047818,-5.62519541838529,17.1022049095917));
#70588=CARTESIAN_POINT('Ctrl Pts',(6.03743088833185,-5.11462943019445,17.1269185787962));
#70589=CARTESIAN_POINT('Ctrl Pts',(6.14058355596565,-4.99031408046956,17.1329406386608));
#70590=CARTESIAN_POINT('Ctrl Pts',(6.28155261096253,-4.80943025078405,17.1418374071634));
#70591=CARTESIAN_POINT('Ctrl Pts',(6.32255993577157,-4.75539250875926,17.1445115868247));
#70592=CARTESIAN_POINT('Ctrl Pts',(6.36894726810647,-4.69260443965641,17.1476451825453));
#70593=CARTESIAN_POINT('Ctrl Pts',(6.37501235210579,-4.68436156158629,17.1480570809009));
#70594=CARTESIAN_POINT('Ctrl Pts',(6.38416935597897,-4.67186582437189,17.1486823119456));
#70595=CARTESIAN_POINT('Ctrl Pts',(6.38727307773992,-4.66762158672706,17.1488948168666));
#70596=CARTESIAN_POINT('Ctrl Pts',(6.39284633457129,-4.65998437266837,17.1492774659704));
#70597=CARTESIAN_POINT('Ctrl Pts',(6.39531740808339,-4.65659251606692,17.1494475013763));
#70598=CARTESIAN_POINT('Ctrl Pts',(6.4006107549468,-4.64931457642787,17.1498125495163));
#70599=CARTESIAN_POINT('Ctrl Pts',(6.40343218919807,-4.64542788826497,17.1500076216993));
#70600=CARTESIAN_POINT('Ctrl Pts',(6.41102302813513,-4.63495101490992,17.1505337916938));
#70601=CARTESIAN_POINT('Ctrl Pts',(6.41578580199248,-4.62835604940675,17.1508653636647));
#70602=CARTESIAN_POINT('Ctrl Pts',(6.43756895737701,-4.59809489915312,17.1523884874238));
#70603=CARTESIAN_POINT('Ctrl Pts',(6.45446841460836,-4.57434238152234,17.1535887605723));
#70604=CARTESIAN_POINT('Ctrl Pts',(6.73467368021476,-4.17586408957423,17.1737952787741));
#70605=CARTESIAN_POINT('Ctrl Pts',(6.96506024633229,-3.77909177602197,17.1949036364035));
#70606=CARTESIAN_POINT('Ctrl Pts',(7.28429701470246,-3.0997744242288,17.2297629008882));
#70607=CARTESIAN_POINT('Ctrl Pts',(7.39398690718939,-2.82817096907393,17.2434048336608));
#70608=CARTESIAN_POINT('Ctrl Pts',(7.58545761683625,-2.26613914600669,17.2704729157486));
#70609=CARTESIAN_POINT('Ctrl Pts',(7.66619988865757,-1.97584361723614,17.2838583388304));
#70610=CARTESIAN_POINT('Ctrl Pts',(7.76536433583358,-1.51999954895285,17.3037604201321));
#70611=CARTESIAN_POINT('Ctrl Pts',(7.79544894919056,-1.35729962154772,17.3106524319193));
#70612=CARTESIAN_POINT('Ctrl Pts',(7.8236939273539,-1.17226595175835,17.3182540366684));
#70613=CARTESIAN_POINT('Ctrl Pts',(7.82688755578149,-1.15074989912175,17.3191343941096));
#70614=CARTESIAN_POINT('Ctrl Pts',(7.8324640516627,-1.11208259908737,17.320710150935));
#70615=CARTESIAN_POINT('Ctrl Pts',(7.83487941760931,-1.09493622856667,17.3214066493033));
#70616=CARTESIAN_POINT('Ctrl Pts',(7.83845155346,-1.06896095636231,17.3224584086927));
#70617=CARTESIAN_POINT('Ctrl Pts',(7.8396497368357,-1.06013786208114,17.3228150736291));
#70618=CARTESIAN_POINT('Ctrl Pts',(7.84169604593879,-1.04487621126205,17.3234309960499));
#70619=CARTESIAN_POINT('Ctrl Pts',(7.84255114299337,-1.03843860846858,17.3236904896607));
#70620=CARTESIAN_POINT('Ctrl Pts',(7.84430618695515,-1.02509993644775,17.324227514181));
#70621=CARTESIAN_POINT('Ctrl Pts',(7.84520495632541,-1.01819871732988,17.3245050049444));
#70622=CARTESIAN_POINT('Ctrl Pts',(7.84736355331006,-1.00145134463913,17.3251775352615));
#70623=CARTESIAN_POINT('Ctrl Pts',(7.84861395983336,-0.991603975401235,
17.3255722553875));
#70624=CARTESIAN_POINT('Ctrl Pts',(7.85321706983824,-0.954798732396256,
17.3270448574326));
#70625=CARTESIAN_POINT('Ctrl Pts',(7.85644946406174,-0.92782584786468,17.3281186641683));
#70626=CARTESIAN_POINT('Ctrl Pts',(7.90865925038612,-0.472310356602522,
17.3461633498642));
#70627=CARTESIAN_POINT('Ctrl Pts',(7.9226502100186,-0.0404622924064998,
17.3618699252433));
#70628=CARTESIAN_POINT('Ctrl Pts',(7.87595141836899,0.904661507713193,17.3947809663055));
#70629=CARTESIAN_POINT('Ctrl Pts',(7.80040147377598,1.41517678471952,17.4115913930652));
#70630=CARTESIAN_POINT('Ctrl Pts',(7.63061198213414,2.09583566924965,17.4360565856003));
#70631=CARTESIAN_POINT('Ctrl Pts',(7.57903745982945,2.27529150654023,17.4427206575297));
#70632=CARTESIAN_POINT('Ctrl Pts',(7.48150276259319,2.5743744947767,17.4544438171782));
#70633=CARTESIAN_POINT('Ctrl Pts',(7.43889570300004,2.69501673808782,17.4593467960221));
#70634=CARTESIAN_POINT('Ctrl Pts',(7.38565548057392,2.83486967331362,17.4652951046804));
#70635=CARTESIAN_POINT('Ctrl Pts',(7.37784293489364,2.85514037341621,17.4661638555165));
#70636=CARTESIAN_POINT('Ctrl Pts',(7.36747092639055,2.88172510143414,17.4673122021937));
#70637=CARTESIAN_POINT('Ctrl Pts',(7.36498658808689,2.8880685532803,17.4675868865842));
#70638=CARTESIAN_POINT('Ctrl Pts',(7.36090454050823,2.89845203859809,17.4680376301149));
#70639=CARTESIAN_POINT('Ctrl Pts',(7.35931169140283,2.90249397986553,17.4682133667684));
#70640=CARTESIAN_POINT('Ctrl Pts',(7.35621362150004,2.91033655535251,17.4685548839712));
#70641=CARTESIAN_POINT('Ctrl Pts',(7.35470878239149,2.91413734004587,17.4687206394324));
#70642=CARTESIAN_POINT('Ctrl Pts',(7.35122063214955,2.92292747852222,17.4691045473338));
#70643=CARTESIAN_POINT('Ctrl Pts',(7.34923518834108,2.92791597785922,17.4693228388062));
#70644=CARTESIAN_POINT('Ctrl Pts',(7.34300010021262,2.94353556254634,17.4700076409165));
#70645=CARTESIAN_POINT('Ctrl Pts',(7.33873247227389,2.954159402831,17.4704753129156));
#70646=CARTESIAN_POINT('Ctrl Pts',(7.30150956009607,3.04624375538912,17.4745451732579));
#70647=CARTESIAN_POINT('Ctrl Pts',(7.26722336194286,3.12715626855057,17.4782314601976));
#70648=CARTESIAN_POINT('Ctrl Pts',(7.22334557379982,3.22608338243671,17.4828594515673));
#70649=CARTESIAN_POINT('Ctrl Pts',(7.21502159476869,3.24465693763958,17.4837336669822));
#70650=CARTESIAN_POINT('Ctrl Pts',(7.19415050125701,3.29074980925187,17.4859159926649));
#70651=CARTESIAN_POINT('Ctrl Pts',(7.18151714380436,3.31822953011595,17.4872284779585));
#70652=CARTESIAN_POINT('Ctrl Pts',(7.00721425272674,3.69171004288188,17.505215827643));
#70653=CARTESIAN_POINT('Ctrl Pts',(6.82086301693795,4.02561370088062,17.5230257312923));
#70654=CARTESIAN_POINT('Ctrl Pts',(6.35137969424957,4.74000152318988,17.5631520154991));
#70655=CARTESIAN_POINT('Ctrl Pts',(6.05666676107285,5.11121240409239,17.5854105581209));
#70656=CARTESIAN_POINT('Ctrl Pts',(5.48321881064938,5.7137491525905,17.6225408925745));
#70657=CARTESIAN_POINT('Ctrl Pts',(5.21849290152389,5.95650873577452,17.6378732339556));
#70658=CARTESIAN_POINT('Ctrl Pts',(4.92105304906423,6.19416161396239,17.6532903018575));
#70659=CARTESIAN_POINT('Ctrl Pts',(4.90387605468125,6.20776939506738,17.6541747285777));
#70660=CARTESIAN_POINT('Ctrl Pts',(4.87873881765007,6.22751391500264,17.6554604979247));
#70661=CARTESIAN_POINT('Ctrl Pts',(4.8708231464093,6.23370707442999,17.655864159489));
#70662=CARTESIAN_POINT('Ctrl Pts',(4.8569165970475,6.24454478973123,17.6565711888736));
#70663=CARTESIAN_POINT('Ctrl Pts',(4.85093081432213,6.24919584400352,17.6568748224422));
#70664=CARTESIAN_POINT('Ctrl Pts',(4.83930040894617,6.25820608608209,17.6574634451409));
#70665=CARTESIAN_POINT('Ctrl Pts',(4.83365656032202,6.26256625682203,17.6577484742177));
#70666=CARTESIAN_POINT('Ctrl Pts',(4.82017742648523,6.27295052253683,17.6584277557478));
#70667=CARTESIAN_POINT('Ctrl Pts',(4.81233672380333,6.27896758541555,17.6588217224322));
#70668=CARTESIAN_POINT('Ctrl Pts',(4.78862743881198,6.29709191996949,17.6600095252908));
#70669=CARTESIAN_POINT('Ctrl Pts',(4.77272423632373,6.30915388684902,17.6608015302592));
#70670=CARTESIAN_POINT('Ctrl Pts',(4.61018975181843,6.43146380920138,17.6688483969515));
#70671=CARTESIAN_POINT('Ctrl Pts',(4.45980660161947,6.53664338324402,17.6758982292768));
#70672=CARTESIAN_POINT('Ctrl Pts',(4.15740369424774,6.73284840960087,17.6894011334408));
#70673=CARTESIAN_POINT('Ctrl Pts',(4.0057161314352,6.82418457566719,17.6958627333373));
#70674=CARTESIAN_POINT('Ctrl Pts',(3.37278812031355,7.17691032472051,17.7218145940418));
#70675=CARTESIAN_POINT('Ctrl Pts',(2.8681323167152,7.39307311013705,17.7400876528261));
#70676=CARTESIAN_POINT('Ctrl Pts',(2.05715598890869,7.64480224006212,17.7701564873003));
#70677=CARTESIAN_POINT('Ctrl Pts',(1.76422260143587,7.71766881886595,17.7811900259877));
#70678=CARTESIAN_POINT('Ctrl Pts',(1.42487295648765,7.78174597191026,17.7948069529935));
#70679=CARTESIAN_POINT('Ctrl Pts',(1.38183633622384,7.78950329269495,17.7965472355436));
#70680=CARTESIAN_POINT('Ctrl Pts',(1.32703189787337,7.79891328456964,17.7987787778896));
#70681=CARTESIAN_POINT('Ctrl Pts',(1.31532109862832,7.80089690251622,17.7992565139291));
#70682=CARTESIAN_POINT('Ctrl Pts',(1.29657599491621,7.80402860634351,17.8000225991004));
#70683=CARTESIAN_POINT('Ctrl Pts',(1.289544501767,7.80519357714808,17.8003102783273));
#70684=CARTESIAN_POINT('Ctrl Pts',(1.27623398435503,7.80738037292326,17.8008554320334));
#70685=CARTESIAN_POINT('Ctrl Pts',(1.26995527982548,7.80840412999174,17.8011128310155));
#70686=CARTESIAN_POINT('Ctrl Pts',(1.25575353898104,7.81070217379605,17.8016955836962));
#70687=CARTESIAN_POINT('Ctrl Pts',(1.24782979135952,7.81197197957118,17.8020211088937));
#70688=CARTESIAN_POINT('Ctrl Pts',(1.22749853342217,7.81519840601153,17.8028573254095));
#70689=CARTESIAN_POINT('Ctrl Pts',(1.21508829568487,7.81713753277578,17.8033686731912));
#70690=CARTESIAN_POINT('Ctrl Pts',(1.14330075726487,7.82817941188841,17.806331737665));
#70691=CARTESIAN_POINT('Ctrl Pts',(1.08382678987283,7.83663504259709,17.8088069136173));
#70692=CARTESIAN_POINT('Ctrl Pts',(0.335215391968185,7.93438298243581,17.8401798896467));
#70693=CARTESIAN_POINT('Ctrl Pts',(-0.36268576712055,7.9331773453036,17.8714463155295));
#70694=CARTESIAN_POINT('Ctrl Pts',(-1.42384920662199,7.79087618750982,17.9175715109498));
#70695=CARTESIAN_POINT('Ctrl Pts',(-1.79223564925196,7.71446808135062,17.9333744887431));
#70696=CARTESIAN_POINT('Ctrl Pts',(-2.22245126700878,7.59274124496653,17.9516120691243));
#70697=CARTESIAN_POINT('Ctrl Pts',(-2.29082339836031,7.57239312040085,17.9545048388973));
#70698=CARTESIAN_POINT('Ctrl Pts',(-2.38146509711709,7.54407736541356,17.9583343337344));
#70699=CARTESIAN_POINT('Ctrl Pts',(-2.40398707191292,7.5369307724812,17.9592853832973));
#70700=CARTESIAN_POINT('Ctrl Pts',(-2.44074081429855,7.52508670181965,17.9608366093582));
#70701=CARTESIAN_POINT('Ctrl Pts',(-2.45499180498145,7.5204495099541,17.961437889352));
#70702=CARTESIAN_POINT('Ctrl Pts',(-2.48248703952698,7.51141623334938,17.9625975896548));
#70703=CARTESIAN_POINT('Ctrl Pts',(-2.49573299446361,7.50702554637102,17.96315610853));
#70704=CARTESIAN_POINT('Ctrl Pts',(-2.52618374703081,7.49684241734209,17.9644396745417));
#70705=CARTESIAN_POINT('Ctrl Pts',(-2.5433803798618,7.49102575091314,17.9651642577805));
#70706=CARTESIAN_POINT('Ctrl Pts',(-2.59813354089362,7.47229552044047,17.9674703621151));
#70707=CARTESIAN_POINT('Ctrl Pts',(-2.635613070304,7.45915826482264,17.9690475305864));
#70708=CARTESIAN_POINT('Ctrl Pts',(-3.03496554567734,7.31579223334455,17.9858381527423));
#70709=CARTESIAN_POINT('Ctrl Pts',(-3.38699055211238,7.15961963885377,18.0004715540782));
#70710=CARTESIAN_POINT('Ctrl Pts',(-4.13058380294964,6.76256384061525,18.0317019445917));
#70711=CARTESIAN_POINT('Ctrl Pts',(-4.51535159556521,6.51195652307564,18.048062185909));
#70712=CARTESIAN_POINT('Ctrl Pts',(-5.07640921246084,6.07277544297216,18.0743971781));
#70713=CARTESIAN_POINT('Ctrl Pts',(-5.2688895764366,5.90654900197727,18.0839712595894));
#70714=CARTESIAN_POINT('Ctrl Pts',(-5.47928471007736,5.7063713520879,18.0954598621463));
#70715=CARTESIAN_POINT('Ctrl Pts',(-5.5053735585937,5.68120558186405,18.0969035748097));
#70716=CARTESIAN_POINT('Ctrl Pts',(-5.53857482387999,5.64873559267836,18.0987669027846));
#70717=CARTESIAN_POINT('Ctrl Pts',(-5.54584761259681,5.64159544208592,18.0991766846171));
#70718=CARTESIAN_POINT('Ctrl Pts',(-5.55751462251857,5.63009684868889,18.0998366985648));
#70719=CARTESIAN_POINT('Ctrl Pts',(-5.56191757774558,5.62574725375826,18.1000863852519));
#70720=CARTESIAN_POINT('Ctrl Pts',(-5.57027409329137,5.61747261339971,18.1005614393047));
#70721=CARTESIAN_POINT('Ctrl Pts',(-5.57422862230835,5.61354854817251,18.1007867452334));
#70722=CARTESIAN_POINT('Ctrl Pts',(-5.58320722387668,5.60462027070444,18.1012994342072));
#70723=CARTESIAN_POINT('Ctrl Pts',(-5.58822871493128,5.59961347886257,18.1015869814342));
#70724=CARTESIAN_POINT('Ctrl Pts',(-5.60342206173172,5.58442381593077,18.1024594967923));
#70725=CARTESIAN_POINT('Ctrl Pts',(-5.61357282601606,5.5742199705936,18.10304582524));
#70726=CARTESIAN_POINT('Ctrl Pts',(-5.69468263256046,5.4922397755936,18.1077587137666));
#70727=CARTESIAN_POINT('Ctrl Pts',(-5.76428331940084,5.41914595231678,18.111979302164));
#70728=CARTESIAN_POINT('Ctrl Pts',(-6.41124964062997,4.71314268091962,18.1528039455147));
#70729=CARTESIAN_POINT('Ctrl Pts',(-6.88362467736341,3.99171133190357,18.1942800854542));
#70730=CARTESIAN_POINT('Ctrl Pts',(-7.37241183897025,2.8901229520899,18.2475761987917));
#70731=CARTESIAN_POINT('Ctrl Pts',(-7.49251825864636,2.56270861303139,18.2624197972734));
#70732=CARTESIAN_POINT('Ctrl Pts',(-7.59790735582282,2.20372119393185,18.2776139991284));
#70733=CARTESIAN_POINT('Ctrl Pts',(-7.60503602920081,2.1789929551116,18.2786553749989));
#70734=CARTESIAN_POINT('Ctrl Pts',(-7.6151111784191,2.14339208114612,18.2801471563036));
#70735=CARTESIAN_POINT('Ctrl Pts',(-7.61815526079389,2.13254737273164,18.2806005873791));
#70736=CARTESIAN_POINT('Ctrl Pts',(-7.62339806484694,2.11371511300971,18.2813862715456));
#70737=CARTESIAN_POINT('Ctrl Pts',(-7.62560741630043,2.10573055423663,18.2817188535643));
#70738=CARTESIAN_POINT('Ctrl Pts',(-7.62983134776988,2.09037150900919,18.2823575819921));
#70739=CARTESIAN_POINT('Ctrl Pts',(-7.63184778804856,2.08299754717225,18.2826637856598));
#70740=CARTESIAN_POINT('Ctrl Pts',(-7.63657262885299,2.06562021836922,18.283384315082));
#70741=CARTESIAN_POINT('Ctrl Pts',(-7.63927207055801,2.05561441795856,18.2837983634969));
#70742=CARTESIAN_POINT('Ctrl Pts',(-7.64853548242268,2.02100822291067,18.2852275440433));
#70743=CARTESIAN_POINT('Ctrl Pts',(-7.65500037772436,1.99638135003596,18.286239615371));
#70744=CARTESIAN_POINT('Ctrl Pts',(-7.72842126909674,1.71109649157515,18.2979069587214));
#70745=CARTESIAN_POINT('Ctrl Pts',(-7.78215622093737,1.44720632931898,18.3081436475568));
#70746=CARTESIAN_POINT('Ctrl Pts',(-7.88136205928372,0.790159333628197,
18.3325973940439));
#70747=CARTESIAN_POINT('Ctrl Pts',(-7.91100066395141,0.395357546547743,
18.3463792010137));
#70748=CARTESIAN_POINT('Ctrl Pts',(-7.91099895747553,-0.620768414657839,
18.3814975743519));
#70749=CARTESIAN_POINT('Ctrl Pts',(-7.83793470667573,-1.23935196704252,
18.4025337088538));
#70750=CARTESIAN_POINT('Ctrl Pts',(-7.68456469624239,-1.87957482020434,
18.4285148712731));
#70751=CARTESIAN_POINT('Ctrl Pts',(-7.67554038797965,-1.91609388168929,
18.4300107443672));
#70752=CARTESIAN_POINT('Ctrl Pts',(-7.66329653234707,-1.96416675474369,
18.4319970305218));
#70753=CARTESIAN_POINT('Ctrl Pts',(-7.66031058841938,-1.97577996499985,
18.4324781920922));
#70754=CARTESIAN_POINT('Ctrl Pts',(-7.65564393055039,-1.99376036024174,
18.4332251693793));
#70755=CARTESIAN_POINT('Ctrl Pts',(-7.65398164291206,-2.00013233939653,
18.4334902781251));
#70756=CARTESIAN_POINT('Ctrl Pts',(-7.65064297576142,-2.01286520378321,
18.434020807257));
#70757=CARTESIAN_POINT('Ctrl Pts',(-7.64896661480329,-2.01922608849729,
18.4342862267831));
#70758=CARTESIAN_POINT('Ctrl Pts',(-7.64521507037805,-2.03338946417253,
18.434878069516));
#70759=CARTESIAN_POINT('Ctrl Pts',(-7.64313587341957,-2.04119087917306,
18.4352046410989));
#70760=CARTESIAN_POINT('Ctrl Pts',(-7.63704606022468,-2.06390087579453,
18.4361569451007));
#70761=CARTESIAN_POINT('Ctrl Pts',(-7.6330037517108,-2.07880087396382,18.4367838240967));
#70762=CARTESIAN_POINT('Ctrl Pts',(-7.60364017823742,-2.18579494184249,
18.4412998184791));
#70763=CARTESIAN_POINT('Ctrl Pts',(-7.57669702925659,-2.27743382700996,
18.4452448418068));
#70764=CARTESIAN_POINT('Ctrl Pts',(-7.47936647338979,-2.58760577567366,
18.4588174027484));
#70765=CARTESIAN_POINT('Ctrl Pts',(-7.40113003448595,-2.80355051812288,
18.4686379817823));
#70766=CARTESIAN_POINT('Ctrl Pts',(-7.10545968553398,-3.52058524759278,
18.5020390327163));
#70767=CARTESIAN_POINT('Ctrl Pts',(-6.84558342480646,-4.00251392977768,
18.5256957681537));
#70768=CARTESIAN_POINT('Ctrl Pts',(-6.43888024955435,-4.59954643588493,
18.5559918399502));
#70769=CARTESIAN_POINT('Ctrl Pts',(-6.33477430618393,-4.74190284477679,
18.5633148542309));
#70770=CARTESIAN_POINT('Ctrl Pts',(-6.05189693576716,-5.10275410166161,
18.5822156708884));
#70771=CARTESIAN_POINT('Ctrl Pts',(-5.86603368768708,-5.31537478333532,
18.5937198703796));
#70772=CARTESIAN_POINT('Ctrl Pts',(-5.62382342421901,-5.56423986047458,
18.6077917217352));
#70773=CARTESIAN_POINT('Ctrl Pts',(-5.57786576639218,-5.61030914376227,
18.6104225724697));
#70774=CARTESIAN_POINT('Ctrl Pts',(-5.50776425937407,-5.67886799850951,
18.6143772501603));
#70775=CARTESIAN_POINT('Ctrl Pts',(-5.48403966757122,-5.70178198591922,
18.6157058252478));
#70776=CARTESIAN_POINT('Ctrl Pts',(-5.4412190988007,-5.74262498876983,18.6180863191342));
#70777=CARTESIAN_POINT('Ctrl Pts',(-5.42217608013372,-5.76060878757986,
18.6191388662858));
#70778=CARTESIAN_POINT('Ctrl Pts',(-5.3814100504924,-5.79872607438953,18.6213792009594));
#70779=CARTESIAN_POINT('Ctrl Pts',(-5.3596625628735,-5.81883282424091,18.6225666557676));
#70780=CARTESIAN_POINT('Ctrl Pts',(-5.30045254546596,-5.87296217717641,
18.6257790029644));
#70781=CARTESIAN_POINT('Ctrl Pts',(-5.26277556191809,-5.90674828833299,
18.6278009787152));
#70782=CARTESIAN_POINT('Ctrl Pts',(-5.0573190287319,-6.08746103216223,18.6387098973539));
#70783=CARTESIAN_POINT('Ctrl Pts',(-4.88370570197996,-6.22760620491813,
18.6475080789913));
#70784=CARTESIAN_POINT('Ctrl Pts',(-4.35866848654732,-6.61595463538525,
18.6730628800961));
#70785=CARTESIAN_POINT('Ctrl Pts',(-3.9926617600959,-6.84306214523772,18.6895562191977));
#70786=CARTESIAN_POINT('Ctrl Pts',(-3.38035122590235,-7.15707793102041,
18.7162559178597));
#70787=CARTESIAN_POINT('Ctrl Pts',(-3.14506579476865,-7.26354551726059,
18.726332984537));
#70788=CARTESIAN_POINT('Ctrl Pts',(-2.87843585220965,-7.36880885804074,
18.7377974326141));
#70789=CARTESIAN_POINT('Ctrl Pts',(-2.85181025247576,-7.37915409862963,
18.7389427961303));
#70790=CARTESIAN_POINT('Ctrl Pts',(-2.81186263547759,-7.39442704009274,
18.7406625114606));
#70791=CARTESIAN_POINT('Ctrl Pts',(-2.7985823400193,-7.39946346813889,18.7412344282876));
#70792=CARTESIAN_POINT('Ctrl Pts',(-2.77497344036099,-7.40834427272926,
18.7422515913481));
#70793=CARTESIAN_POINT('Ctrl Pts',(-2.76465021860639,-7.41220288617679,
18.7426965062654));
#70794=CARTESIAN_POINT('Ctrl Pts',(-2.74295896261043,-7.42025902381596,
18.7436317213732));
#70795=CARTESIAN_POINT('Ctrl Pts',(-2.73158928291619,-7.42445202283006,
18.7441221278759));
#70796=CARTESIAN_POINT('Ctrl Pts',(-2.70128219938187,-7.43554986406698,
18.7454299701171));
#70797=CARTESIAN_POINT('Ctrl Pts',(-2.68232810889937,-7.44240842803317,
18.7462485619804));
#70798=CARTESIAN_POINT('Ctrl Pts',(-2.57571836695739,-7.48052514631642,
18.7508564175114));
#70799=CARTESIAN_POINT('Ctrl Pts',(-2.48754383602839,-7.51030670182811,
18.7546805902781));
#70800=CARTESIAN_POINT('Ctrl Pts',(-1.71414275115884,-7.75641390476471,
18.7882642415646));
#70801=CARTESIAN_POINT('Ctrl Pts',(-1.00290549535961,-7.88000742256015,
18.819081944281));
#70802=CARTESIAN_POINT('Ctrl Pts',(-0.172974304941317,-7.90989956029704,
18.8531094984428));
#70803=CARTESIAN_POINT('Ctrl Pts',(-0.0611240664904855,-7.91155455823628,
18.8576638600065));
#70804=CARTESIAN_POINT('Ctrl Pts',(0.0880060991340752,-7.91059832630897,
18.8636988889013));
#70805=CARTESIAN_POINT('Ctrl Pts',(0.125285382710805,-7.91009573553948,
18.8652044268233));
#70806=CARTESIAN_POINT('Ctrl Pts',(0.183744452697223,-7.90889423075326,
18.8675607828463));
#70807=CARTESIAN_POINT('Ctrl Pts',(0.204927264084802,-7.90837371379046,
18.8684136815279));
#70808=CARTESIAN_POINT('Ctrl Pts',(0.245652796800963,-7.90720924371385,
18.8700517252497));
#70809=CARTESIAN_POINT('Ctrl Pts',(0.265195719170338,-7.90657792939589,
18.8708370110468));
#70810=CARTESIAN_POINT('Ctrl Pts',(0.311306212102885,-7.90491722455827,
18.8726881371742));
#70811=CARTESIAN_POINT('Ctrl Pts',(0.337871357212215,-7.90382634154128,
18.873753263055));
#70812=CARTESIAN_POINT('Ctrl Pts',(0.415896568159029,-7.90022818832662,
18.8768779993726));
#70813=CARTESIAN_POINT('Ctrl Pts',(0.467338373483844,-7.89735210512718,
18.8789334255746));
#70814=CARTESIAN_POINT('Ctrl Pts',(0.913984744327948,-7.86800095702388,
18.8967455356701));
#70815=CARTESIAN_POINT('Ctrl Pts',(1.30672606453444,-7.81238038356054,18.9122247141363));
#70816=CARTESIAN_POINT('Ctrl Pts',(2.30741323347474,-7.59306058693808,18.9518486290778));
#70817=CARTESIAN_POINT('Ctrl Pts',(2.90296219211652,-7.38590149261466,18.9751741379433));
#70818=CARTESIAN_POINT('Ctrl Pts',(3.65812523151308,-7.01761487599907,19.0066976603031));
#70819=CARTESIAN_POINT('Ctrl Pts',(3.84472186169952,-6.91714601369213,19.0146879414807));
#70820=CARTESIAN_POINT('Ctrl Pts',(4.15748119652173,-6.73217878418793,19.028674304431));
#70821=CARTESIAN_POINT('Ctrl Pts',(4.2856590217366,-6.65131605084177,19.0345883297743));
#70822=CARTESIAN_POINT('Ctrl Pts',(4.42822708541558,-6.55554233222859,19.0414454075995));
#70823=CARTESIAN_POINT('Ctrl Pts',(4.44497913926222,-6.54419520133423,19.0422556136045));
#70824=CARTESIAN_POINT('Ctrl Pts',(4.46951303763605,-6.52743931512137,19.0434490137914));
#70825=CARTESIAN_POINT('Ctrl Pts',(4.47732905250439,-6.52208060061623,19.0438302303607));
#70826=CARTESIAN_POINT('Ctrl Pts',(4.49120313822218,-6.51253173725278,19.0445087705006));
#70827=CARTESIAN_POINT('Ctrl Pts',(4.49726502838217,-6.50834714206152,19.0448058686449));
#70828=CARTESIAN_POINT('Ctrl Pts',(4.50988344543191,-6.49961045127315,19.0454256354309));
#70829=CARTESIAN_POINT('Ctrl Pts',(4.51643894314147,-6.49505688828202,19.0457483646651));
#70830=CARTESIAN_POINT('Ctrl Pts',(4.53341299362928,-6.48322829319567,19.0465859712395));
#70831=CARTESIAN_POINT('Ctrl Pts',(4.54382090749996,-6.47593808114644,19.0471014903024));
#70832=CARTESIAN_POINT('Ctrl Pts',(4.58795866855565,-6.44486304565221,19.0492960635452));
#70833=CARTESIAN_POINT('Ctrl Pts',(4.62151930947078,-6.42083979022933,19.0509855410284));
#70834=CARTESIAN_POINT('Ctrl Pts',(5.10456540682449,-6.06931833160826,19.0756251430737));
#70835=CARTESIAN_POINT('Ctrl Pts',(5.51838944790545,-5.6956422967183,19.10122066532));
#70836=CARTESIAN_POINT('Ctrl Pts',(6.32431783895333,-4.79697637723482,19.1565291787788));
#70837=CARTESIAN_POINT('Ctrl Pts',(6.69763130678205,-4.26027672490204,19.1857740695928));
#70838=CARTESIAN_POINT('Ctrl Pts',(7.02029585313811,-3.647066273651,19.2140679424585));
#70839=CARTESIAN_POINT('Ctrl Pts',(7.03934800413248,-3.61015595430483,19.2157539641006));
#70840=CARTESIAN_POINT('Ctrl Pts',(7.06435345568218,-3.56076149331376,19.2179877962457));
#70841=CARTESIAN_POINT('Ctrl Pts',(7.07056581696743,-3.54840967047123,19.2185445410687));
#70842=CARTESIAN_POINT('Ctrl Pts',(7.08020488044858,-3.52911883346136,19.2194111693633));
#70843=CARTESIAN_POINT('Ctrl Pts',(7.08365382150165,-3.5221909981392,19.2197218191441));
#70844=CARTESIAN_POINT('Ctrl Pts',(7.090220431135,-3.50895209243333,19.2203143604352));
#70845=CARTESIAN_POINT('Ctrl Pts',(7.09333985184895,-3.50264190227501,19.2205963121248));
#70846=CARTESIAN_POINT('Ctrl Pts',(7.10059678348885,-3.48791260187965,19.2212533361912));
#70847=CARTESIAN_POINT('Ctrl Pts',(7.10472775378018,-3.47949027092903,19.2216281832074));
#70848=CARTESIAN_POINT('Ctrl Pts',(7.11646149836042,-3.45545918461187,19.2226953197855));
#70849=CARTESIAN_POINT('Ctrl Pts',(7.12402790446088,-3.43983267841626,19.2233863584308));
#70850=CARTESIAN_POINT('Ctrl Pts',(7.17133596099948,-3.34130418368985,19.2277255090623));
#70851=CARTESIAN_POINT('Ctrl Pts',(7.2096821264332,-3.25773808857364,19.2313255735565));
#70852=CARTESIAN_POINT('Ctrl Pts',(7.31835108781493,-3.00959836498081,19.2417910353267));
#70853=CARTESIAN_POINT('Ctrl Pts',(7.3845578131383,-2.84328251513537,19.2485178402016));
#70854=CARTESIAN_POINT('Ctrl Pts',(7.5610823503117,-2.35195267370947,19.2676789580178));
#70855=CARTESIAN_POINT('Ctrl Pts',(7.65596893332244,-2.02183201718658,19.2796532809663));
#70856=CARTESIAN_POINT('Ctrl Pts',(7.83930168108754,-1.18167051899068,19.3091241765175));
#70857=CARTESIAN_POINT('Ctrl Pts',(7.89973172729658,-0.667211031505966,
19.3262456895624));
#70858=CARTESIAN_POINT('Ctrl Pts',(7.91356201733813,0.0592879994883373,
19.3527252606395));
#70859=CARTESIAN_POINT('Ctrl Pts',(7.90920299650626,0.269211687218983,19.3606560268355));
#70860=CARTESIAN_POINT('Ctrl Pts',(7.89560757777464,0.493478709939184,19.3696403493004));
#70861=CARTESIAN_POINT('Ctrl Pts',(7.89467008425227,0.508256347393159,19.3702347394251));
#70862=CARTESIAN_POINT('Ctrl Pts',(7.89331662608523,0.528683008859509,19.371059742036));
#70863=CARTESIAN_POINT('Ctrl Pts',(7.89293606985189,0.534334427503551,19.3712883539665));
#70864=CARTESIAN_POINT('Ctrl Pts',(7.89227270679021,0.544030292583091,19.3716811959742));
#70865=CARTESIAN_POINT('Ctrl Pts',(7.89199285931805,0.548074945553286,19.3718452571678));
#70866=CARTESIAN_POINT('Ctrl Pts',(7.89144112073751,0.555961212584904,19.3721655097354));
#70867=CARTESIAN_POINT('Ctrl Pts',(7.89116953342111,0.559802846234865,19.3723216835727));
#70868=CARTESIAN_POINT('Ctrl Pts',(7.89052177283564,0.568871351135959,19.3726907479961));
#70869=CARTESIAN_POINT('Ctrl Pts',(7.89014321138746,0.574098045016697,19.372903776637));
#70870=CARTESIAN_POINT('Ctrl Pts',(7.88904902098002,0.588999713081414,19.3735120456783));
#70871=CARTESIAN_POINT('Ctrl Pts',(7.88832079838922,0.598673616091708,19.3739080199639));
#70872=CARTESIAN_POINT('Ctrl Pts',(7.88659820821451,0.621008032109794,19.3748247680247));
#70873=CARTESIAN_POINT('Ctrl Pts',(7.88559116133486,0.633667346763451,19.3753462712858));
#70874=CARTESIAN_POINT('Ctrl Pts',(7.84234861705062,1.16118621118185,19.3971542762921));
#70875=CARTESIAN_POINT('Ctrl Pts',(7.7498176529061,1.67063603797218,19.4211839647866));
#70876=CARTESIAN_POINT('Ctrl Pts',(7.53924714487542,2.40981738083116,19.4569099173629));
#70877=CARTESIAN_POINT('Ctrl Pts',(7.45863336832276,2.6488227644166,19.4686175784548));
#70878=CARTESIAN_POINT('Ctrl Pts',(7.19801475742954,3.31463166133814,19.501189047015));
#70879=CARTESIAN_POINT('Ctrl Pts',(6.99176350902266,3.73008623819,19.5213991651837));
#70880=CARTESIAN_POINT('Ctrl Pts',(6.734131664389,4.15166911621944,19.5414574533513));
#70881=CARTESIAN_POINT('Ctrl Pts',(6.71777945401352,4.17807670609057,19.5427122763766));
#70882=CARTESIAN_POINT('Ctrl Pts',(6.69507077161803,4.21427152802927,19.5444300426139));
#70883=CARTESIAN_POINT('Ctrl Pts',(6.68884765430728,4.22414183095521,19.5448982580326));
#70884=CARTESIAN_POINT('Ctrl Pts',(6.67890955150117,4.23982733365198,19.5456419875196));
#70885=CARTESIAN_POINT('Ctrl Pts',(6.67520876808631,4.24565148347183,19.5459180652106));
#70886=CARTESIAN_POINT('Ctrl Pts',(6.6679996673331,4.25696416104126,19.5464541676916));
#70887=CARTESIAN_POINT('Ctrl Pts',(6.66449218238999,4.26245321183774,19.5467142253226));
#70888=CARTESIAN_POINT('Ctrl Pts',(6.65609583050655,4.27555741235422,19.5473349144811));
#70889=CARTESIAN_POINT('Ctrl Pts',(6.6512006638116,4.28316852594872,19.5476952942952));
#70890=CARTESIAN_POINT('Ctrl Pts',(6.63651890719506,4.3059101829803,19.5487717241254));
#70891=CARTESIAN_POINT('Ctrl Pts',(6.6266936370525,4.3210157551202,19.5494862263836));
#70892=CARTESIAN_POINT('Ctrl Pts',(6.54216857955549,4.44999995920475,19.5555832488658));
#70893=CARTESIAN_POINT('Ctrl Pts',(6.46458914370474,4.56196876072596,19.5608485454711));
#70894=CARTESIAN_POINT('Ctrl Pts',(6.1796861519972,4.95129034598981,19.5791068605381));
#70895=CARTESIAN_POINT('Ctrl Pts',(5.95708724142328,5.21698516489592,19.5914542449298));
#70896=CARTESIAN_POINT('Ctrl Pts',(5.39997727330915,5.79962376245188,19.6192894662721));
#70897=CARTESIAN_POINT('Ctrl Pts',(5.05381080760213,6.10363539631836,19.6344037552009));
#70898=CARTESIAN_POINT('Ctrl Pts',(4.41555495422948,6.57244888613843,19.6618989951938));
#70899=CARTESIAN_POINT('Ctrl Pts',(4.13581138685182,6.75197982226366,19.673867548586));
#70900=CARTESIAN_POINT('Ctrl Pts',(3.82669028774661,6.92393190887077,19.6879239888571));
#70901=CARTESIAN_POINT('Ctrl Pts',(3.80768873970237,6.93439961929832,19.6887912713313));
#70902=CARTESIAN_POINT('Ctrl Pts',(3.78241985451737,6.94818475018462,19.6899492304948));
#70903=CARTESIAN_POINT('Ctrl Pts',(3.7761906016219,6.95157218319537,19.6902350601175));
#70904=CARTESIAN_POINT('Ctrl Pts',(3.76647330309772,6.95683948050068,19.6906815304173));
#70905=CARTESIAN_POINT('Ctrl Pts',(3.76298837329954,6.95872511331611,19.6908417671113));
#70906=CARTESIAN_POINT('Ctrl Pts',(3.75630755653767,6.96233349691772,19.6911491747973));
#70907=CARTESIAN_POINT('Ctrl Pts',(3.75311189632321,6.96405666800563,19.6912963165729));
#70908=CARTESIAN_POINT('Ctrl Pts',(3.74562059721355,6.96808948914809,19.6916414759559));
#70909=CARTESIAN_POINT('Ctrl Pts',(3.74132401081695,6.970397365496,19.6918396155207));
#70910=CARTESIAN_POINT('Ctrl Pts',(3.72912582057772,6.97693499615886,19.6924026339749));
#70911=CARTESIAN_POINT('Ctrl Pts',(3.72121918197264,6.98115528581892,19.6927681570472));
#70912=CARTESIAN_POINT('Ctrl Pts',(3.67130342042662,7.00768969663006,19.69507935826));
#70913=CARTESIAN_POINT('Ctrl Pts',(3.62910177127783,7.02963753208244,19.6970494455339));
#70914=CARTESIAN_POINT('Ctrl Pts',(3.50101031292845,7.0947932735981,19.7030712814589));
#70915=CARTESIAN_POINT('Ctrl Pts',(3.41453057215005,7.13681612435584,19.7071936075786));
#70916=CARTESIAN_POINT('Ctrl Pts',(3.15177246381048,7.25862845346571,19.7198387525893));
#70917=CARTESIAN_POINT('Ctrl Pts',(2.97331724045881,7.33353486026401,19.7285857498669));
#70918=CARTESIAN_POINT('Ctrl Pts',(2.60528294164501,7.47237427417238,19.7466900795438));
#70919=CARTESIAN_POINT('Ctrl Pts',(2.41565646611307,7.53581297432056,19.7560512933824));
#70920=CARTESIAN_POINT('Ctrl Pts',(1.9515705563846,7.67175220281575,19.7787592119042));
#70921=CARTESIAN_POINT('Ctrl Pts',(1.67520536201082,7.73680195171031,19.7921094744262));
#70922=CARTESIAN_POINT('Ctrl Pts',(0.885752837641893,7.87832578089778,19.8290932648749));
#70923=CARTESIAN_POINT('Ctrl Pts',(0.367761812392883,7.91943596649023,19.8519229113806));
#70924=CARTESIAN_POINT('Ctrl Pts',(-0.18410591415826,7.90892845039262,19.8743899595941));
#70925=CARTESIAN_POINT('Ctrl Pts',(-0.217610215226007,7.90807751941728,
19.8757471966372));
#70926=CARTESIAN_POINT('Ctrl Pts',(-0.263445723050402,7.9066218901948,19.8775948964575));
#70927=CARTESIAN_POINT('Ctrl Pts',(-0.275782167516644,7.90620120926819,
19.8780912988361));
#70928=CARTESIAN_POINT('Ctrl Pts',(-0.295344110721614,7.90548829281707,
19.8788770322433));
#70929=CARTESIAN_POINT('Ctrl Pts',(-0.302570254724032,7.90521502129598,
19.8791669747076));
#70930=CARTESIAN_POINT('Ctrl Pts',(-0.316572948043356,7.90466625264866,
19.879728230175));
#70931=CARTESIAN_POINT('Ctrl Pts',(-0.323349536571749,7.90439194844929,
19.8799995813946));
#70932=CARTESIAN_POINT('Ctrl Pts',(-0.339470304493258,7.9037186428237,19.8806444625774));
#70933=CARTESIAN_POINT('Ctrl Pts',(-0.348814155299892,7.90331178420844,
19.8810177391247));
#70934=CARTESIAN_POINT('Ctrl Pts',(-0.376515413210523,7.90205636886534,
19.8821228820909));
#70935=CARTESIAN_POINT('Ctrl Pts',(-0.394870667695896,7.90116041318558,
19.88285322299));
#70936=CARTESIAN_POINT('Ctrl Pts',(-0.542089644753295,7.89346007374551,
19.8886955956486));
#70937=CARTESIAN_POINT('Ctrl Pts',(-0.670775665315519,7.88356740775545,
19.8937076395799));
#70938=CARTESIAN_POINT('Ctrl Pts',(-1.11271523487854,7.83869328851252,19.9106394730681));
#70939=CARTESIAN_POINT('Ctrl Pts',(-1.4240937000983,7.78814635790689,19.9220683836599));
#70940=CARTESIAN_POINT('Ctrl Pts',(-1.88544910206653,7.68465028393059,19.9387463941926));
#70941=CARTESIAN_POINT('Ctrl Pts',(-2.03819271530998,7.64555686964193,19.9442279785561));
#70942=CARTESIAN_POINT('Ctrl Pts',(-2.24087854721437,7.58717499844503,19.9515265993637));
#70943=CARTESIAN_POINT('Ctrl Pts',(-2.29193893746326,7.57190709409158,19.953367479697));
#70944=CARTESIAN_POINT('Ctrl Pts',(-2.38702620974348,7.54242446938941,19.9568045636771));
#70945=CARTESIAN_POINT('Ctrl Pts',(-2.43109018994791,7.52833723278806,19.9584009320506));
#70946=CARTESIAN_POINT('Ctrl Pts',(-2.51369859096942,7.50112645250372,19.9614037631316));
#70947=CARTESIAN_POINT('Ctrl Pts',(-2.5522701671939,7.48809025386366,19.9628100046962));
#70948=CARTESIAN_POINT('Ctrl Pts',(-2.62499849376896,7.4628827267102,19.9654717306857));
#70949=CARTESIAN_POINT('Ctrl Pts',(-2.65917554562323,7.45077318766046,19.966726839643));
#70950=CARTESIAN_POINT('Ctrl Pts',(-3.02216606235357,7.31934345248576,19.980112487768));
#70951=CARTESIAN_POINT('Ctrl Pts',(-3.34278391400817,7.17858207328368,19.9924081500867));
#70952=CARTESIAN_POINT('Ctrl Pts',(-3.68391828357103,7.00099144196255,20.0070001626933));
#70953=CARTESIAN_POINT('Ctrl Pts',(-3.71471786544114,6.98469800471286,20.0083317955208));
#70954=CARTESIAN_POINT('Ctrl Pts',(-3.80275645685197,6.93737726200084,20.012181682755));
#70955=CARTESIAN_POINT('Ctrl Pts',(-3.85971793100382,6.90584801050679,20.0147272284603));
#70956=CARTESIAN_POINT('Ctrl Pts',(-3.9444610210877,6.85756516644299,20.0185938111878));
#70957=CARTESIAN_POINT('Ctrl Pts',(-3.97253988025756,6.84133756042702,20.0198880713221));
#70958=CARTESIAN_POINT('Ctrl Pts',(-4.01005361096654,6.81934844466994,20.0216341749185));
#70959=CARTESIAN_POINT('Ctrl Pts',(-4.01957759258095,6.81373899912817,20.0220789497719));
#70960=CARTESIAN_POINT('Ctrl Pts',(-4.03446581458019,6.80492803896768,20.0227765168939));
#70961=CARTESIAN_POINT('Ctrl Pts',(-4.03983809386328,6.80174008615711,20.0230286934172));
#70962=CARTESIAN_POINT('Ctrl Pts',(-4.05058892675396,6.79534322697834,20.023534267309));
#70963=CARTESIAN_POINT('Ctrl Pts',(-4.05596745680672,6.79213429011894,20.0237876659624));
#70964=CARTESIAN_POINT('Ctrl Pts',(-4.06801317310468,6.78492816855124,20.0243562112798));
#70965=CARTESIAN_POINT('Ctrl Pts',(-4.07467828516519,6.78092753985872,20.0246715099846));
#70966=CARTESIAN_POINT('Ctrl Pts',(-4.09415790210251,6.76919611546709,20.0255950753167));
#70967=CARTESIAN_POINT('Ctrl Pts',(-4.10695634035251,6.76143879597122,20.0262044931457));
#70968=CARTESIAN_POINT('Ctrl Pts',(-4.13604812709682,6.74369276712165,20.0275956106835));
#70969=CARTESIAN_POINT('Ctrl Pts',(-4.15232741701016,6.73368125629367,20.0283782659263));
#70970=CARTESIAN_POINT('Ctrl Pts',(-4.20466911568278,6.70122993698245,20.0309079578919));
#70971=CARTESIAN_POINT('Ctrl Pts',(-4.24058683784758,6.67855884409813,20.0326642625336));
#70972=CARTESIAN_POINT('Ctrl Pts',(-4.38444532617381,6.58612766993456,20.0397768806848));
#70973=CARTESIAN_POINT('Ctrl Pts',(-4.49085920574644,6.51403257822305,20.0452167592483));
#70974=CARTESIAN_POINT('Ctrl Pts',(-4.75244729291475,6.32735009177143,20.0589745419437));
#70975=CARTESIAN_POINT('Ctrl Pts',(-4.90527605067203,6.20961984429675,20.0673643380829));
#70976=CARTESIAN_POINT('Ctrl Pts',(-5.35371286729974,5.83727628879885,20.0928428194602));
#70977=CARTESIAN_POINT('Ctrl Pts',(-5.63495209810417,5.56627032365979,20.1099954908831));
#70978=CARTESIAN_POINT('Ctrl Pts',(-6.15760899631907,4.98224617347384,20.1436809414318));
#70979=CARTESIAN_POINT('Ctrl Pts',(-6.39790479730613,4.66966510344618,20.1601579924094));
#70980=CARTESIAN_POINT('Ctrl Pts',(-6.63751823856307,4.30454637233406,20.1778613672382));
#70981=CARTESIAN_POINT('Ctrl Pts',(-6.66080398296911,4.26842572607273,20.1795974791336));
#70982=CARTESIAN_POINT('Ctrl Pts',(-6.69296906445738,4.21762732222437,20.1820180834329));
#70983=CARTESIAN_POINT('Ctrl Pts',(-6.7020966813757,4.20310780293963,20.1827075694078));
#70984=CARTESIAN_POINT('Ctrl Pts',(-6.71866786701452,4.17655638779867,20.1839640587366));
#70985=CARTESIAN_POINT('Ctrl Pts',(-6.7261265052807,4.16453399604354,20.1845313728532));
#70986=CARTESIAN_POINT('Ctrl Pts',(-6.74110506156459,4.14024522934447,20.1856742496819));
#70987=CARTESIAN_POINT('Ctrl Pts',(-6.74862384836337,4.12797821761278,20.1862497871313));
#70988=CARTESIAN_POINT('Ctrl Pts',(-6.76694653524783,4.09790062426173,20.1876568680118));
#70989=CARTESIAN_POINT('Ctrl Pts',(-6.77771364887792,4.08006772444066,20.1884876292816));
#70990=CARTESIAN_POINT('Ctrl Pts',(-6.8163418458834,4.01551537966389,20.1914822859254));
#70991=CARTESIAN_POINT('Ctrl Pts',(-6.84379149191096,3.96855112473484,20.1936373171496));
#70992=CARTESIAN_POINT('Ctrl Pts',(-6.99647324467392,3.70102837043541,20.2057807290713));
#70993=CARTESIAN_POINT('Ctrl Pts',(-7.1115288525968,3.47482586168494,20.2155362286519));
#70994=CARTESIAN_POINT('Ctrl Pts',(-7.46083915781616,2.69774145944402,20.2476265767177));
#70995=CARTESIAN_POINT('Ctrl Pts',(-7.64343776973488,2.12596944621827,20.2687624682831));
#70996=CARTESIAN_POINT('Ctrl Pts',(-7.76749778782643,1.50048291702491,20.2924514456719));
#70997=CARTESIAN_POINT('Ctrl Pts',(-7.77486857067629,1.46181036484864,20.29391921236));
#70998=CARTESIAN_POINT('Ctrl Pts',(-7.80725199715692,1.28472587417353,20.3006598962358));
#70999=CARTESIAN_POINT('Ctrl Pts',(-7.82885854493788,1.14572069482018,20.3060055377072));
#71000=CARTESIAN_POINT('Ctrl Pts',(-7.84966453041497,0.983470247404358,
20.3123748030812));
#71001=CARTESIAN_POINT('Ctrl Pts',(-7.85248260576773,0.96071009200969,20.3132712356937));
#71002=CARTESIAN_POINT('Ctrl Pts',(-7.86159573620695,0.884387919116747,
20.3162880714843));
#71003=CARTESIAN_POINT('Ctrl Pts',(-7.8674419583904,0.830774551294097,20.3184250975977));
#71004=CARTESIAN_POINT('Ctrl Pts',(-7.87382942149011,0.766064201971669,
20.32103006895));
#71005=CARTESIAN_POINT('Ctrl Pts',(-7.87489615293663,0.755019667917537,
20.3214755751515));
#71006=CARTESIAN_POINT('Ctrl Pts',(-7.87660287823664,0.736951719146519,
20.3222059064409));
#71007=CARTESIAN_POINT('Ctrl Pts',(-7.8772567248818,0.729929604573375,20.3224901252637));
#71008=CARTESIAN_POINT('Ctrl Pts',(-7.87840986522335,0.717363216146676,
20.3229994331137));
#71009=CARTESIAN_POINT('Ctrl Pts',(-7.8789126991669,0.711819265684822,20.3232243646281));
#71010=CARTESIAN_POINT('Ctrl Pts',(-7.87987278277401,0.701108290196049,
20.3236594034014));
#71011=CARTESIAN_POINT('Ctrl Pts',(-7.88033080297295,0.69594133575079,20.3238694758583));
#71012=CARTESIAN_POINT('Ctrl Pts',(-7.88131334914259,0.684731830895633,
20.3243256833692));
#71013=CARTESIAN_POINT('Ctrl Pts',(-7.88183600821365,0.678689123916538,
20.3245719032586));
#71014=CARTESIAN_POINT('Ctrl Pts',(-7.88308805129682,0.664017147319941,
20.3251704581343));
#71015=CARTESIAN_POINT('Ctrl Pts',(-7.88381021490033,0.655387283169653,
20.3255231259719));
#71016=CARTESIAN_POINT('Ctrl Pts',(-7.88572999626808,0.631983488466599,
20.3264812269822));
#71017=CARTESIAN_POINT('Ctrl Pts',(-7.88690026056012,0.617207403467188,
20.3270879451169));
#71018=CARTESIAN_POINT('Ctrl Pts',(-7.90334433779482,0.401893183150274,
20.3359564659492));
#71019=CARTESIAN_POINT('Ctrl Pts',(-7.91100527114318,0.200868484566958,
20.3445978728846));
#71020=CARTESIAN_POINT('Ctrl Pts',(-7.91099999727893,-0.000207491421311337,
20.3534756400368));
#71021=CARTESIAN_POINT('',(-7.91099868333906,-0.00456423132557518,24.3648581729618));
#71022=CARTESIAN_POINT('Ctrl Pts',(-7.91099999795386,-0.000179927557964477,
20.3534744230576));
#71023=CARTESIAN_POINT('Ctrl Pts',(-7.91098172587622,-0.80356106444437,
20.388944664795));
#71024=CARTESIAN_POINT('Ctrl Pts',(-7.78859805973727,-1.6023406876584,20.4274466847679));
#71025=CARTESIAN_POINT('Ctrl Pts',(-7.48828697629528,-2.5591306577211,20.471266686629));
#71026=CARTESIAN_POINT('Ctrl Pts',(-7.42148272694363,-2.7468514261103,20.4797783367217));
#71027=CARTESIAN_POINT('Ctrl Pts',(-7.3097870754086,-3.02677677424593,20.4923253103193));
#71028=CARTESIAN_POINT('Ctrl Pts',(-7.270076738684,-3.12095336833719,20.4965213640672));
#71029=CARTESIAN_POINT('Ctrl Pts',(-7.22108293721243,-3.23113294702392,
20.5014026443798));
#71030=CARTESIAN_POINT('Ctrl Pts',(-7.21355544809895,-3.24790343303585,
20.5021448633821));
#71031=CARTESIAN_POINT('Ctrl Pts',(-7.20191703467251,-3.2735925924565,20.5032806550884));
#71032=CARTESIAN_POINT('Ctrl Pts',(-7.19784786627995,-3.28253005019517,
20.5036755925323));
#71033=CARTESIAN_POINT('Ctrl Pts',(-7.19071636593886,-3.29811654302511,
20.5043639768595));
#71034=CARTESIAN_POINT('Ctrl Pts',(-7.18766143114841,-3.30476893871632,
20.504657665782));
#71035=CARTESIAN_POINT('Ctrl Pts',(-7.18076252454994,-3.31973711216809,
20.5053182175351));
#71036=CARTESIAN_POINT('Ctrl Pts',(-7.17691332969104,-3.32805047838612,
20.5056849083068));
#71037=CARTESIAN_POINT('Ctrl Pts',(-7.16656291403311,-3.35030350538055,
20.5066659780709));
#71038=CARTESIAN_POINT('Ctrl Pts',(-7.16003545182479,-3.36423095385105,
20.5072794926979));
#71039=CARTESIAN_POINT('Ctrl Pts',(-7.1315869688662,-3.42447278390364,20.5099310581098));
#71040=CARTESIAN_POINT('Ctrl Pts',(-7.1092566698663,-3.47059307083007,20.5119555769473));
#71041=CARTESIAN_POINT('Ctrl Pts',(-6.64564081022046,-4.40487722587664,
20.5528671247981));
#71042=CARTESIAN_POINT('Ctrl Pts',(-6.04177901096497,-5.20231919269601,
20.5846798560224));
#71043=CARTESIAN_POINT('Ctrl Pts',(-5.17252924212299,-5.9884389260997,20.6267740073886));
#71044=CARTESIAN_POINT('Ctrl Pts',(-5.03464761291745,-6.10481593453984,
20.6334020493709));
#71045=CARTESIAN_POINT('Ctrl Pts',(-4.80503883200239,-6.28554128561496,
20.6445460924391));
#71046=CARTESIAN_POINT('Ctrl Pts',(-4.71571585455712,-6.35283003132572,
20.6489127200964));
#71047=CARTESIAN_POINT('Ctrl Pts',(-4.61229549057141,-6.42735530960186,
20.6540038254323));
#71048=CARTESIAN_POINT('Ctrl Pts',(-4.59957036958959,-6.4364678496016,20.654630727467));
#71049=CARTESIAN_POINT('Ctrl Pts',(-4.58018642294146,-6.45026197815132,
20.6555863059638));
#71050=CARTESIAN_POINT('Ctrl Pts',(-4.57354723237446,-6.45497118260902,
20.6559137127795));
#71051=CARTESIAN_POINT('Ctrl Pts',(-4.56166962846795,-6.46336849048662,
20.6564996320999));
#71052=CARTESIAN_POINT('Ctrl Pts',(-4.55643397458303,-6.4670604974821,20.6567579693477));
#71053=CARTESIAN_POINT('Ctrl Pts',(-4.54593646372188,-6.47444391291601,
20.6572760557511));
#71054=CARTESIAN_POINT('Ctrl Pts',(-4.54067458146822,-6.47813527634243,
20.6575358065459));
#71055=CARTESIAN_POINT('Ctrl Pts',(-4.52624362056184,-6.48823279470624,
20.6582483372506));
#71056=CARTESIAN_POINT('Ctrl Pts',(-4.51706546237797,-6.49462591055676,
20.6587016777658));
#71057=CARTESIAN_POINT('Ctrl Pts',(-4.48177952571629,-6.51909361725839,
20.6604451275905));
#71058=CARTESIAN_POINT('Ctrl Pts',(-4.45557674666313,-6.53703029899564,
20.6617409525715));
#71059=CARTESIAN_POINT('Ctrl Pts',(-4.30764676436469,-6.63699071216031,
20.6690603704238));
#71060=CARTESIAN_POINT('Ctrl Pts',(-4.18376596376306,-6.71576997496561,
20.6752032922685));
#71061=CARTESIAN_POINT('Ctrl Pts',(-4.03960840254393,-6.80190653624829,
20.6823162670694));
#71062=CARTESIAN_POINT('Ctrl Pts',(-4.02140406465349,-6.81268507398716,
20.6832138820106));
#71063=CARTESIAN_POINT('Ctrl Pts',(-3.52751132096905,-7.10244279766773,
20.7075467832909));
#71064=CARTESIAN_POINT('Ctrl Pts',(-3.02398591932898,-7.33100100829271,
20.7316868105654));
#71065=CARTESIAN_POINT('Ctrl Pts',(-2.18333850272882,-7.61110404665538,
20.76932522613));
#71066=CARTESIAN_POINT('Ctrl Pts',(-1.85950886494569,-7.69662983954183,
20.7832767490004));
#71067=CARTESIAN_POINT('Ctrl Pts',(-1.28476040294153,-7.81002063025915,
20.8073648427572));
#71068=CARTESIAN_POINT('Ctrl Pts',(-1.03611105453133,-7.84687890968481,
20.8176044074162));
#71069=CARTESIAN_POINT('Ctrl Pts',(-0.720252426499742,-7.8784224680025,
20.830467372978));
#71070=CARTESIAN_POINT('Ctrl Pts',(-0.654294576333215,-7.88417420011935,
20.8331441119363));
#71071=CARTESIAN_POINT('Ctrl Pts',(-0.555585418267175,-7.89153471766616,
20.8371360895608));
#71072=CARTESIAN_POINT('Ctrl Pts',(-0.522883880347012,-7.89376892325486,
20.8384563277763));
#71073=CARTESIAN_POINT('Ctrl Pts',(-0.466530782709033,-7.89726730986283,
20.8407275691585));
#71074=CARTESIAN_POINT('Ctrl Pts',(-0.442885723285561,-7.89862862617552,
20.8416793828187));
#71075=CARTESIAN_POINT('Ctrl Pts',(-0.393941093099465,-7.90122604360499,
20.8436472198839));
#71076=CARTESIAN_POINT('Ctrl Pts',(-0.368640972180599,-7.90244686252048,
20.8446630992689));
#71077=CARTESIAN_POINT('Ctrl Pts',(-0.29951822442489,-7.90544960136094,
20.8474350525814));
#71078=CARTESIAN_POINT('Ctrl Pts',(-0.255685867429983,-7.90698863833048,
20.8491889230253));
#71079=CARTESIAN_POINT('Ctrl Pts',(-0.0838622507045206,-7.91159142715724,
20.8560495436711));
#71080=CARTESIAN_POINT('Ctrl Pts',(0.0441837431742176,-7.91191254734126,
20.861130213061));
#71081=CARTESIAN_POINT('Ctrl Pts',(0.688460287949695,-7.89788660717095,
20.8865674217526));
#71082=CARTESIAN_POINT('Ctrl Pts',(1.20239718353165,-7.83612388225894,20.9063722790975));
#71083=CARTESIAN_POINT('Ctrl Pts',(1.89891798392786,-7.68223961041667,20.9340179828592));
#71084=CARTESIAN_POINT('Ctrl Pts',(2.08953662122669,-7.63259650565974,20.9416804405368));
#71085=CARTESIAN_POINT('Ctrl Pts',(2.36888426145028,-7.54859557502793,20.9531920657983));
#71086=CARTESIAN_POINT('Ctrl Pts',(2.45916826291393,-7.5196674668373,20.9569574865461));
#71087=CARTESIAN_POINT('Ctrl Pts',(2.56967751196085,-7.48205585129312,20.9616362704421));
#71088=CARTESIAN_POINT('Ctrl Pts',(2.59041607784389,-7.47490112405543,20.9625173665108));
#71089=CARTESIAN_POINT('Ctrl Pts',(2.62303035973587,-7.46349729085645,20.9639080694315));
#71090=CARTESIAN_POINT('Ctrl Pts',(2.63492617962997,-7.45930587288788,20.9644163809634));
#71091=CARTESIAN_POINT('Ctrl Pts',(2.65634803820866,-7.45170037645811,20.9653337109129));
#71092=CARTESIAN_POINT('Ctrl Pts',(2.66587765497354,-7.44829643130626,20.9657424931357));
#71093=CARTESIAN_POINT('Ctrl Pts',(2.68733066257378,-7.44058704766428,20.9666643600721));
#71094=CARTESIAN_POINT('Ctrl Pts',(2.69925027871608,-7.43627121851401,20.9671776921112));
#71095=CARTESIAN_POINT('Ctrl Pts',(2.73326697543591,-7.42386196161241,20.9686459704829));
#71096=CARTESIAN_POINT('Ctrl Pts',(2.75533823405328,-7.41569861746346,20.9696026788189));
#71097=CARTESIAN_POINT('Ctrl Pts',(2.90914325702542,-7.35803037651737,20.9762969798641));
#71098=CARTESIAN_POINT('Ctrl Pts',(3.03956979444996,-7.30511735096004,20.9821137401974));
#71099=CARTESIAN_POINT('Ctrl Pts',(3.55496082049081,-7.07983409478263,21.0055532422737));
#71100=CARTESIAN_POINT('Ctrl Pts',(3.92728162067759,-6.8802804842894,21.0234814595417));
#71101=CARTESIAN_POINT('Ctrl Pts',(4.46793977866948,-6.53225668660148,21.0504155080742));
#71102=CARTESIAN_POINT('Ctrl Pts',(4.64885941082402,-6.40476173729586,21.0596070787767));
#71103=CARTESIAN_POINT('Ctrl Pts',(4.89253544780301,-6.21727047351181,21.0722327717848));
#71104=CARTESIAN_POINT('Ctrl Pts',(4.96000697041814,-6.16357739768896,21.0757568598084));
#71105=CARTESIAN_POINT('Ctrl Pts',(5.07657521382355,-6.06765981811501,21.0818974506092));
#71106=CARTESIAN_POINT('Ctrl Pts',(5.12605614234644,-6.02591570594786,21.0845210426706));
#71107=CARTESIAN_POINT('Ctrl Pts',(5.19706757293003,-5.96449992726538,21.0883124607802));
#71108=CARTESIAN_POINT('Ctrl Pts',(5.21901020269072,-5.94530934881373,21.0894877241172));
#71109=CARTESIAN_POINT('Ctrl Pts',(5.25727418922191,-5.91146936488328,21.0915438779844));
#71110=CARTESIAN_POINT('Ctrl Pts',(5.27364160612686,-5.89687257505842,21.0924255746682));
#71111=CARTESIAN_POINT('Ctrl Pts',(5.30532332439834,-5.86838078250689,21.0941365740435));
#71112=CARTESIAN_POINT('Ctrl Pts',(5.32064425812621,-5.85449342526256,21.0949659863577));
#71113=CARTESIAN_POINT('Ctrl Pts',(5.35722187000292,-5.82107619641557,21.0969510379614));
#71114=CARTESIAN_POINT('Ctrl Pts',(5.37842647296293,-5.80148971661407,21.0981057939752));
#71115=CARTESIAN_POINT('Ctrl Pts',(5.45566595402274,-5.72935694033224,21.1023272283551));
#71116=CARTESIAN_POINT('Ctrl Pts',(5.5110421269326,-5.67611106023804,21.1053831487359));
#71117=CARTESIAN_POINT('Ctrl Pts',(6.02482459224143,-5.16748577357066,21.1340423214596));
#71118=CARTESIAN_POINT('Ctrl Pts',(6.4266274589081,-4.65832184857035,21.1590072098058));
#71119=CARTESIAN_POINT('Ctrl Pts',(6.90124393906994,-3.87668754684734,21.1935195477238));
#71120=CARTESIAN_POINT('Ctrl Pts',(7.02871502931433,-3.64047255180341,21.2035306392816));
#71121=CARTESIAN_POINT('Ctrl Pts',(7.32508974723458,-3.01741931310199,21.2293476475888));
#71122=CARTESIAN_POINT('Ctrl Pts',(7.4754882053651,-2.62274555077706,21.2451277900368));
#71123=CARTESIAN_POINT('Ctrl Pts',(7.5991415943857,-2.19939617874741,21.2626752941814));
#71124=CARTESIAN_POINT('Ctrl Pts',(7.60450630480875,-2.18077517776791,21.2634484269859));
#71125=CARTESIAN_POINT('Ctrl Pts',(7.61404109434782,-2.14721673936626,21.2648443453518));
#71126=CARTESIAN_POINT('Ctrl Pts',(7.6182357779132,-2.13228636461093,21.2654663200664));
#71127=CARTESIAN_POINT('Ctrl Pts',(7.62458246582442,-2.10943844159508,21.2664196407676));
#71128=CARTESIAN_POINT('Ctrl Pts',(7.62676611189578,-2.10152967880901,21.2667499077475));
#71129=CARTESIAN_POINT('Ctrl Pts',(7.63082851190424,-2.08672669077147,21.2673686123297));
#71130=CARTESIAN_POINT('Ctrl Pts',(7.6327102373227,-2.07983328485176,21.267656946361));
#71131=CARTESIAN_POINT('Ctrl Pts',(7.63649313982912,-2.06590093822609,21.2682401554886));
#71132=CARTESIAN_POINT('Ctrl Pts',(7.63839393026194,-2.05886190088904,21.2685350438691));
#71133=CARTESIAN_POINT('Ctrl Pts',(7.64372270878547,-2.03901933117859,21.2693669933348));
#71134=CARTESIAN_POINT('Ctrl Pts',(7.64712824574418,-2.02620982929596,21.2699048598986));
#71135=CARTESIAN_POINT('Ctrl Pts',(7.66104809578373,-1.97331707863493,21.2721292744339));
#71136=CARTESIAN_POINT('Ctrl Pts',(7.67127946166076,-1.93316050981997,21.2738262696188));
#71137=CARTESIAN_POINT('Ctrl Pts',(7.8786236470392,-1.09179051453554,21.3095821042463));
#71138=CARTESIAN_POINT('Ctrl Pts',(7.94948169478973,-0.264825296249611,
21.3491856437994));
#71139=CARTESIAN_POINT('Ctrl Pts',(7.86336667347681,0.952964761167712,21.4036851468227));
#71140=CARTESIAN_POINT('Ctrl Pts',(7.80582868617316,1.34527775489399,21.4207178947119));
#71141=CARTESIAN_POINT('Ctrl Pts',(7.71230866792631,1.76215553761376,21.4380919002179));
#71142=CARTESIAN_POINT('Ctrl Pts',(7.70528916941435,1.7926003382245,21.4393567376548));
#71143=CARTESIAN_POINT('Ctrl Pts',(7.69534481036431,1.83459290001176,21.4410958870381));
#71144=CARTESIAN_POINT('Ctrl Pts',(7.69257399662633,1.84617663488404,21.4415750617184));
#71145=CARTESIAN_POINT('Ctrl Pts',(7.68785590217273,1.86570618097345,21.4423819634324));
#71146=CARTESIAN_POINT('Ctrl Pts',(7.68592244139155,1.87365529159508,21.4427101277936));
#71147=CARTESIAN_POINT('Ctrl Pts',(7.68207506802009,1.88936697584728,21.4433582267641));
#71148=CARTESIAN_POINT('Ctrl Pts',(7.68016171189104,1.89712967394649,21.4436781785292));
#71149=CARTESIAN_POINT('Ctrl Pts',(7.67592249946423,1.91421710942443,21.4443819040726));
#71150=CARTESIAN_POINT('Ctrl Pts',(7.67359141078608,1.92354054310399,21.4447655109902));
#71151=CARTESIAN_POINT('Ctrl Pts',(7.66541147506815,1.95600553602064,21.4460999912667));
#71152=CARTESIAN_POINT('Ctrl Pts',(7.65947486133289,1.97912495822983,21.4470480664334));
#71153=CARTESIAN_POINT('Ctrl Pts',(7.59935015440447,2.20895039186463,21.4564506782376));
#71154=CARTESIAN_POINT('Ctrl Pts',(7.53691063332288,2.41341480076733,21.4646348472004));
#71155=CARTESIAN_POINT('Ctrl Pts',(7.32886485941783,3.00739542832371,21.4880345009394));
#71156=CARTESIAN_POINT('Ctrl Pts',(7.16075669613831,3.38825621791586,21.5025162340452));
#71157=CARTESIAN_POINT('Ctrl Pts',(6.78560033245285,4.08412465583359,21.5295450543203));
#71158=CARTESIAN_POINT('Ctrl Pts',(6.58448455573352,4.40102198453725,21.5421212676687));
#71159=CARTESIAN_POINT('Ctrl Pts',(6.16678675370185,4.96609991279743,21.5668432395028));
#71160=CARTESIAN_POINT('Ctrl Pts',(5.95572189139081,5.21735033538304,21.5788313592145));
#71161=CARTESIAN_POINT('Ctrl Pts',(5.72013504507011,5.46481186311343,21.5925063006117));
#71162=CARTESIAN_POINT('Ctrl Pts',(5.71053871461802,5.47483892159157,21.5930638101822));
#71163=CARTESIAN_POINT('Ctrl Pts',(5.69678658009283,5.48913282193774,21.5938635200462));
#71164=CARTESIAN_POINT('Ctrl Pts',(5.69265222112983,5.49342035210292,21.5941040382163));
#71165=CARTESIAN_POINT('Ctrl Pts',(5.68550084226022,5.50081993524719,21.5945202502279));
#71166=CARTESIAN_POINT('Ctrl Pts',(5.68248609441766,5.50393419055534,21.5946957635984));
#71167=CARTESIAN_POINT('Ctrl Pts',(5.6767078096007,5.5098933905579,21.5950322725535));
#71168=CARTESIAN_POINT('Ctrl Pts',(5.67394468846056,5.5127387388738,21.5951932348163));
#71169=CARTESIAN_POINT('Ctrl Pts',(5.66746640929436,5.51939977365708,21.5955707319528));
#71170=CARTESIAN_POINT('Ctrl Pts',(5.66374953996047,5.52321378458636,21.5957874051983));
#71171=CARTESIAN_POINT('Ctrl Pts',(5.65097619436663,5.53629451373348,21.5965323305311));
#71172=CARTESIAN_POINT('Ctrl Pts',(5.64190097851535,5.54554255541434,21.5970621311982));
#71173=CARTESIAN_POINT('Ctrl Pts',(5.53181953112572,5.65717045554271,21.6034949151164));
#71174=CARTESIAN_POINT('Ctrl Pts',(5.42806769394745,5.75679436526213,21.6096211480092));
#71175=CARTESIAN_POINT('Ctrl Pts',(4.80755521091041,6.32092570902297,21.6462706226067));
#71176=CARTESIAN_POINT('Ctrl Pts',(4.23411022750957,6.71856488375504,21.6798465459883));
#71177=CARTESIAN_POINT('Ctrl Pts',(3.34644969566059,7.17475296938914,21.7248370762101));
#71178=CARTESIAN_POINT('Ctrl Pts',(3.0690878847468,7.29770733949958,21.7380916626012));
#71179=CARTESIAN_POINT('Ctrl Pts',(2.67447344759015,7.44614941148397,21.755728411644));
#71180=CARTESIAN_POINT('Ctrl Pts',(2.56269079358081,7.48535683176492,21.7605954224736));
#71181=CARTESIAN_POINT('Ctrl Pts',(2.43348273002804,7.5274422609158,21.7660767897983));
#71182=CARTESIAN_POINT('Ctrl Pts',(2.41688135166986,7.53278897395631,21.7667783670003));
#71183=CARTESIAN_POINT('Ctrl Pts',(2.39175316816391,7.54079024572829,21.7678362332365));
#71184=CARTESIAN_POINT('Ctrl Pts',(2.38323938310447,7.54348532119207,21.7681939509841));
#71185=CARTESIAN_POINT('Ctrl Pts',(2.36852315922854,7.54811640490491,21.7688110633448));
#71186=CARTESIAN_POINT('Ctrl Pts',(2.36232287468557,7.55005919538418,21.7690706967667));
#71187=CARTESIAN_POINT('Ctrl Pts',(2.34948719790915,7.55406375310155,21.7696074194585));
#71188=CARTESIAN_POINT('Ctrl Pts',(2.34285146706557,7.55612442212799,21.7698844699015));
#71189=CARTESIAN_POINT('Ctrl Pts',(2.32483302084007,7.56169387786597,21.7706356215995));
#71190=CARTESIAN_POINT('Ctrl Pts',(2.31344505984468,7.56518571048549,21.7711091261618));
#71191=CARTESIAN_POINT('Ctrl Pts',(2.27082619529148,7.57814848460779,21.7728765967029));
#71192=CARTESIAN_POINT('Ctrl Pts',(2.23954445640299,7.58745192581547,21.7741646778632));
#71193=CARTESIAN_POINT('Ctrl Pts',(1.73687607224747,7.73357003688371,21.7947176048506));
#71194=CARTESIAN_POINT('Ctrl Pts',(1.25379314513056,7.82642431393164,21.8123206757606));
#71195=CARTESIAN_POINT('Ctrl Pts',(0.495492891238331,7.90011568418972,21.8384921888617));
#71196=CARTESIAN_POINT('Ctrl Pts',(0.224631824181886,7.91245111358229,21.847580094274));
#71197=CARTESIAN_POINT('Ctrl Pts',(-0.536758470382203,7.90799233933541,
21.8733683806937));
#71198=CARTESIAN_POINT('Ctrl Pts',(-1.02580444749758,7.85952028132506,21.8901880399758));
#71199=CARTESIAN_POINT('Ctrl Pts',(-1.5294978563163,7.7617701496894,21.9105685716016));
#71200=CARTESIAN_POINT('Ctrl Pts',(-1.551833396365,7.75733540835425,21.9114788074538));
#71201=CARTESIAN_POINT('Ctrl Pts',(-1.58094381607892,7.75142475418711,21.912673989271));
#71202=CARTESIAN_POINT('Ctrl Pts',(-1.58773655305818,7.75003623908245,21.9129535071313));
#71203=CARTESIAN_POINT('Ctrl Pts',(-1.5988076513715,7.74775801054076,21.913410117321));
#71204=CARTESIAN_POINT('Ctrl Pts',(-1.60308712165481,7.74687367756892,21.9135868706715));
#71205=CARTESIAN_POINT('Ctrl Pts',(-1.61135829544614,7.74515733020936,21.9139289784644));
#71206=CARTESIAN_POINT('Ctrl Pts',(-1.61535009395602,7.74432577438658,21.9140943042724));
#71207=CARTESIAN_POINT('Ctrl Pts',(-1.6245353210695,7.74240493315269,21.9144752246521));
#71208=CARTESIAN_POINT('Ctrl Pts',(-1.6297282949823,7.74131350886696,21.9146909515765));
#71209=CARTESIAN_POINT('Ctrl Pts',(-1.64581697443108,7.73791519241831,21.9153604442928));
#71210=CARTESIAN_POINT('Ctrl Pts',(-1.65670886653204,7.73559052480158,21.9158152994355));
#71211=CARTESIAN_POINT('Ctrl Pts',(-1.745679926237,7.71640481395985,21.9195437970396));
#71212=CARTESIAN_POINT('Ctrl Pts',(-1.8235019587745,7.69838563539463,21.9228868436706));
#71213=CARTESIAN_POINT('Ctrl Pts',(-2.15548700202678,7.61620052755629,21.9374584631671));
#71214=CARTESIAN_POINT('Ctrl Pts',(-2.4066332077301,7.54060547228964,21.9492618771522));
#71215=CARTESIAN_POINT('Ctrl Pts',(-3.31127806423235,7.21850519785562,21.9935252897246));
#71216=CARTESIAN_POINT('Ctrl Pts',(-3.93523849053538,6.89822453043655,22.0271712160521));
#71217=CARTESIAN_POINT('Ctrl Pts',(-4.68656063589212,6.37704844730224,22.0675613583843));
#71218=CARTESIAN_POINT('Ctrl Pts',(-4.85896833464568,6.24668186226148,22.0768522775412));
#71219=CARTESIAN_POINT('Ctrl Pts',(-5.10607804207177,6.04340011844219,22.090190143348));
#71220=CARTESIAN_POINT('Ctrl Pts',(-5.18501675166131,5.97581127363246,22.0944550180567));
#71221=CARTESIAN_POINT('Ctrl Pts',(-5.27560044008503,5.89510508982503,22.0993572111415));
#71222=CARTESIAN_POINT('Ctrl Pts',(-5.28855946199602,5.88348220407366,22.1000587306561));
#71223=CARTESIAN_POINT('Ctrl Pts',(-5.30827149163427,5.86568482728106,22.101126159855));
#71224=CARTESIAN_POINT('Ctrl Pts',(-5.31505228381499,5.85954127410598,22.1014934102048));
#71225=CARTESIAN_POINT('Ctrl Pts',(-5.32682207678129,5.84884033134909,22.1021309812048));
#71226=CARTESIAN_POINT('Ctrl Pts',(-5.33181591829319,5.84428829482554,22.1024015341109));
#71227=CARTESIAN_POINT('Ctrl Pts',(-5.34220910495313,5.834790184338,22.1029646867348));
#71228=CARTESIAN_POINT('Ctrl Pts',(-5.34760742826367,5.82984300044389,22.1032572375904));
#71229=CARTESIAN_POINT('Ctrl Pts',(-5.36079099456491,5.81772746932402,22.1039718049777));
#71230=CARTESIAN_POINT('Ctrl Pts',(-5.36856874798952,5.81055097164049,22.1043934652861));
#71231=CARTESIAN_POINT('Ctrl Pts',(-5.3982254406198,5.78307649831113,22.1060016482041));
#71232=CARTESIAN_POINT('Ctrl Pts',(-5.42000398666191,5.76267025805648,22.1071834289799));
#71233=CARTESIAN_POINT('Ctrl Pts',(-5.77178270156673,5.42929939907984,22.1262874451495));
#71234=CARTESIAN_POINT('Ctrl Pts',(-6.07432386215653,5.08855708464409,22.1428666797978));
#71235=CARTESIAN_POINT('Ctrl Pts',(-6.49490231894895,4.52354009847755,22.1675967687351));
#71236=CARTESIAN_POINT('Ctrl Pts',(-6.63432902944382,4.31646280750821,22.1761747300734));
#71237=CARTESIAN_POINT('Ctrl Pts',(-7.02478769757883,3.67281966465503,22.20218167004));
#71238=CARTESIAN_POINT('Ctrl Pts',(-7.24417883742072,3.21855988807715,22.219679622657));
#71239=CARTESIAN_POINT('Ctrl Pts',(-7.43134308939176,2.71299479324775,22.2410221629067));
#71240=CARTESIAN_POINT('Ctrl Pts',(-7.44353565794962,2.67936143727599,22.24244898413));
#71241=CARTESIAN_POINT('Ctrl Pts',(-7.45919326751457,2.63523789994686,22.2443290573173));
#71242=CARTESIAN_POINT('Ctrl Pts',(-7.46286518274943,2.6248211851347,22.244773504281));
#71243=CARTESIAN_POINT('Ctrl Pts',(-7.46880911285582,2.60784578033238,22.2454987300479));
#71244=CARTESIAN_POINT('Ctrl Pts',(-7.47109433925842,2.6012917083211,22.245778962155));
#71245=CARTESIAN_POINT('Ctrl Pts',(-7.47547218254493,2.58868261676965,22.2463185174433));
#71246=CARTESIAN_POINT('Ctrl Pts',(-7.47756607655164,2.58262804384704,22.2465777884844));
#71247=CARTESIAN_POINT('Ctrl Pts',(-7.48233682719779,2.56877880069575,22.2471712711227));
#71248=CARTESIAN_POINT('Ctrl Pts',(-7.48500886010623,2.56098248452242,22.2475056750852));
#71249=CARTESIAN_POINT('Ctrl Pts',(-7.49204625026789,2.54034406332725,22.2483917025645));
#71250=CARTESIAN_POINT('Ctrl Pts',(-7.4963907609046,2.52749491260642,22.2489441402271));
#71251=CARTESIAN_POINT('Ctrl Pts',(-7.52464776918806,2.44320934869856,22.2525729998191));
#71252=CARTESIAN_POINT('Ctrl Pts',(-7.5475714637052,2.37144692942415,22.2556865353714));
#71253=CARTESIAN_POINT('Ctrl Pts',(-7.68148761241604,1.93059835245026,22.2749224573472));
#71254=CARTESIAN_POINT('Ctrl Pts',(-7.76640663932383,1.5541459584239,22.2917880522237));
#71255=CARTESIAN_POINT('Ctrl Pts',(-7.88151128349742,0.786447781953037,
22.3257917354479));
#71256=CARTESIAN_POINT('Ctrl Pts',(-7.91074265904272,0.396095247116501,
22.3428783831706));
#71257=CARTESIAN_POINT('Ctrl Pts',(-7.91120615143957,-0.312646158696349,
22.3730416757368));
#71258=CARTESIAN_POINT('Ctrl Pts',(-7.89226171799543,-0.630200445195317,
22.3862510241615));
#71259=CARTESIAN_POINT('Ctrl Pts',(-7.84982478831273,-0.982623972669835,
22.4006343752917));
#71260=CARTESIAN_POINT('Ctrl Pts',(-7.84512736365174,-1.01944874916272,
22.4021341353553));
#71261=CARTESIAN_POINT('Ctrl Pts',(-7.83772256119207,-1.07441254576667,
22.404368102185));
#71262=CARTESIAN_POINT('Ctrl Pts',(-7.83521103564284,-1.09257736336207,
22.4051056463718));
#71263=CARTESIAN_POINT('Ctrl Pts',(-7.83078771632382,-1.12376959544013,
22.4063708386694));
#71264=CARTESIAN_POINT('Ctrl Pts',(-7.82890651893481,-1.13680124945904,
22.4068990262957));
#71265=CARTESIAN_POINT('Ctrl Pts',(-7.82496433168676,-1.16363610356916,
22.4079858651169));
#71266=CARTESIAN_POINT('Ctrl Pts',(-7.82289933143595,-1.17743867160734,
22.4085444422408));
#71267=CARTESIAN_POINT('Ctrl Pts',(-7.8180151827501,-1.20950448228181,22.4098410896835));
#71268=CARTESIAN_POINT('Ctrl Pts',(-7.81516854225128,-1.22776347479674,
22.4105786553262));
#71269=CARTESIAN_POINT('Ctrl Pts',(-7.8058959287635,-1.28590097808107,22.412924634599));
#71270=CARTESIAN_POINT('Ctrl Pts',(-7.79922847262497,-1.32574048918317,
22.4145285459894));
#71271=CARTESIAN_POINT('Ctrl Pts',(-7.70505704204403,-1.86312106482157,
22.4361138129765));
#71272=CARTESIAN_POINT('Ctrl Pts',(-7.57039667832971,-2.35122629731901,
22.455029107944));
#71273=CARTESIAN_POINT('Ctrl Pts',(-7.19506049946698,-3.3337244033677,22.4934923418002));
#71274=CARTESIAN_POINT('Ctrl Pts',(-6.94765886811018,-3.82263745751245,
22.5128668109563));
#71275=CARTESIAN_POINT('Ctrl Pts',(-6.64766207167355,-4.28865603963787,
22.5344447536521));
#71276=CARTESIAN_POINT('Ctrl Pts',(-6.64343714282686,-4.2951978504266,22.534748344715));
#71277=CARTESIAN_POINT('Ctrl Pts',(-6.60238204916128,-4.35856139672346,
22.5376956753082));
#71278=CARTESIAN_POINT('Ctrl Pts',(-6.56483412584911,-4.41491321661571,
22.5403696674405));
#71279=CARTESIAN_POINT('Ctrl Pts',(-6.51979758087205,-4.48065888443176,
22.5435601010937));
#71280=CARTESIAN_POINT('Ctrl Pts',(-6.51300453306289,-4.49052741715739,
22.5440408877308));
#71281=CARTESIAN_POINT('Ctrl Pts',(-6.50206871376163,-4.50633730467339,
22.5448142428635));
#71282=CARTESIAN_POINT('Ctrl Pts',(-6.49794013760245,-4.51228849139713,
22.5451060603173));
#71283=CARTESIAN_POINT('Ctrl Pts',(-6.49060067728028,-4.52283708462651,
22.5456245878453));
#71284=CARTESIAN_POINT('Ctrl Pts',(-6.48739306292013,-4.52743676851696,
22.5458511216128));
#71285=CARTESIAN_POINT('Ctrl Pts',(-6.480713082694,-4.53699411236018,22.5463227251958));
#71286=CARTESIAN_POINT('Ctrl Pts',(-6.47723991338176,-4.54195120405089,
22.546567838919));
#71287=CARTESIAN_POINT('Ctrl Pts',(-6.46825378552984,-4.55474541322106,
22.5472018010601));
#71288=CARTESIAN_POINT('Ctrl Pts',(-6.46273228247843,-4.56257649328165,
22.5475911239951));
#71289=CARTESIAN_POINT('Ctrl Pts',(-6.43951067083552,-4.59538469246332,
22.5492276774471));
#71290=CARTESIAN_POINT('Ctrl Pts',(-6.42168000652413,-4.62026882514597,
22.5504823370517));
#71291=CARTESIAN_POINT('Ctrl Pts',(-6.29440415596683,-4.79573244779552,
22.5594289322657));
#71292=CARTESIAN_POINT('Ctrl Pts',(-6.17982464696088,-4.94250264721055,
22.5674335341006));
#71293=CARTESIAN_POINT('Ctrl Pts',(-5.9183359451113,-5.25413345182559,22.5853756527728));
#71294=CARTESIAN_POINT('Ctrl Pts',(-5.7694824073621,-5.41716570056153,22.5953874800186));
#71295=CARTESIAN_POINT('Ctrl Pts',(-5.4777200974479,-5.71103542410882,22.6143657890295));
#71296=CARTESIAN_POINT('Ctrl Pts',(-5.33643600819178,-5.84326905712422,
22.623302822943));
#71297=CARTESIAN_POINT('Ctrl Pts',(-4.69199355000562,-6.40354348810939,
22.6626228591802));
#71298=CARTESIAN_POINT('Ctrl Pts',(-4.14115851632649,-6.77283036320718,
22.6922714304811));
#71299=CARTESIAN_POINT('Ctrl Pts',(-3.51383773837286,-7.0879173770017,22.7209555663216));
#71300=CARTESIAN_POINT('Ctrl Pts',(-3.47676801136364,-7.10617426290782,
22.7226342739608));
#71301=CARTESIAN_POINT('Ctrl Pts',(-3.42684509289811,-7.1302772004995,22.724873489262));
#71302=CARTESIAN_POINT('Ctrl Pts',(-3.41411715504994,-7.13638033605583,
22.7254425143634));
#71303=CARTESIAN_POINT('Ctrl Pts',(-3.39415893121352,-7.14588482928227,
22.7263318754924));
#71304=CARTESIAN_POINT('Ctrl Pts',(-3.38693973970159,-7.14930934033406,
22.7266529769068));
#71305=CARTESIAN_POINT('Ctrl Pts',(-3.37309506086123,-7.15585105518575,
22.7272676381245));
#71306=CARTESIAN_POINT('Ctrl Pts',(-3.36647041187674,-7.15897000831293,
22.7275612554895));
#71307=CARTESIAN_POINT('Ctrl Pts',(-3.35093419820725,-7.16625828435632,
22.7282486904962));
#71308=CARTESIAN_POINT('Ctrl Pts',(-3.34201915807507,-7.1704201931791,22.7286422634024));
#71309=CARTESIAN_POINT('Ctrl Pts',(-3.31634690120914,-7.18234678388407,
22.729773060101));
#71310=CARTESIAN_POINT('Ctrl Pts',(-3.29957017925254,-7.19006945244487,
22.7305089009041));
#71311=CARTESIAN_POINT('Ctrl Pts',(-3.18819468969066,-7.24086596140615,
22.7353733627831));
#71312=CARTESIAN_POINT('Ctrl Pts',(-3.09278004232527,-7.28213140727594,
22.7394424475358));
#71313=CARTESIAN_POINT('Ctrl Pts',(-2.81291659814369,-7.39667513556913,
22.7511103199443));
#71314=CARTESIAN_POINT('Ctrl Pts',(-2.62648667654647,-7.46490966636221,
22.7585490165663));
#71315=CARTESIAN_POINT('Ctrl Pts',(-1.88210020738159,-7.70601530284374,
22.7871918872537));
#71316=CARTESIAN_POINT('Ctrl Pts',(-1.30831987783538,-7.82389123765218,
22.8068494484479));
#71317=CARTESIAN_POINT('Ctrl Pts',(-0.58686246957568,-7.8904537389032,22.8321243279684));
#71318=CARTESIAN_POINT('Ctrl Pts',(-0.446616737987543,-7.89963289652462,
22.8370706997292));
#71319=CARTESIAN_POINT('Ctrl Pts',(-0.0189262071950909,-7.91619952801481,
22.852411181903));
#71320=CARTESIAN_POINT('Ctrl Pts',(0.268741777340459,-7.91165939057682,
22.8630985646318));
#71321=CARTESIAN_POINT('Ctrl Pts',(0.579585591892116,-7.88977712288962,
22.8754830065679));
#71322=CARTESIAN_POINT('Ctrl Pts',(0.603632484769886,-7.88797377746221,
22.8764458327305));
#71323=CARTESIAN_POINT('Ctrl Pts',(0.636617338469257,-7.88534843338616,
22.8777727512764));
#71324=CARTESIAN_POINT('Ctrl Pts',(0.645562854808283,-7.88462111652887,
22.8781332408271));
#71325=CARTESIAN_POINT('Ctrl Pts',(0.6608338028638,-7.88335334665052,22.8787496874603));
#71326=CARTESIAN_POINT('Ctrl Pts',(0.667159869008805,-7.88282049853148,
22.8790053620629));
#71327=CARTESIAN_POINT('Ctrl Pts',(0.67943143400787,-7.88177197979014,22.8795019207765));
#71328=CARTESIAN_POINT('Ctrl Pts',(0.685377005224254,-7.88125719510468,
22.8797427724058));
#71329=CARTESIAN_POINT('Ctrl Pts',(0.69954380828997,-7.88001444027691,22.8803172942931));
#71330=CARTESIAN_POINT('Ctrl Pts',(0.707764486543604,-7.87928033196305,
22.8806511845306));
#71331=CARTESIAN_POINT('Ctrl Pts',(0.732219032594326,-7.87705795598791,
22.8816459128797));
#71332=CARTESIAN_POINT('Ctrl Pts',(0.748449415066305,-7.87553237706649,
22.8823080574863));
#71333=CARTESIAN_POINT('Ctrl Pts',(0.884049307936662,-7.86236366932037,
22.8878557804203));
#71334=CARTESIAN_POINT('Ctrl Pts',(1.00314182887592,-7.84805776294403,22.8928296052281));
#71335=CARTESIAN_POINT('Ctrl Pts',(1.48948692221074,-7.77838499562673,22.913454715745));
#71336=CARTESIAN_POINT('Ctrl Pts',(1.85294383724109,-7.69989846061144,22.9295734938286));
#71337=CARTESIAN_POINT('Ctrl Pts',(2.9791241347201,-7.37232104929163,22.9802036375432));
#71338=CARTESIAN_POINT('Ctrl Pts',(3.71027367737872,-7.032801364994,23.0135445544));
#71339=CARTESIAN_POINT('Ctrl Pts',(4.45185123773458,-6.54009342820564,23.0497055887872));
#71340=CARTESIAN_POINT('Ctrl Pts',(4.52495942948383,-6.48972601968616,23.0533011167772));
#71341=CARTESIAN_POINT('Ctrl Pts',(4.62493759251298,-6.41833580659422,23.0582606765467));
#71342=CARTESIAN_POINT('Ctrl Pts',(4.65254221462104,-6.39835394550075,23.059634636335));
#71343=CARTESIAN_POINT('Ctrl Pts',(4.69996937625198,-6.36355414034355,23.0620032232721));
#71344=CARTESIAN_POINT('Ctrl Pts',(4.71985305385803,-6.34882040923402,23.0629987025124));
#71345=CARTESIAN_POINT('Ctrl Pts',(4.76098952569798,-6.3180383777337,23.0650633557095));
#71346=CARTESIAN_POINT('Ctrl Pts',(4.78223108706012,-6.30197556654246,23.0661323590951));
#71347=CARTESIAN_POINT('Ctrl Pts',(4.83214612017109,-6.26383225795724,23.0686512693773));
#71348=CARTESIAN_POINT('Ctrl Pts',(4.86075001927093,-6.24166163337496,23.0701001451148));
#71349=CARTESIAN_POINT('Ctrl Pts',(4.95568937871483,-6.16702655618315,23.0749275480354));
#71350=CARTESIAN_POINT('Ctrl Pts',(5.02133581461236,-6.11369451041662,23.078295764278));
#71351=CARTESIAN_POINT('Ctrl Pts',(5.17463438154379,-5.98501767205325,23.0862376702482));
#71352=CARTESIAN_POINT('Ctrl Pts',(5.26151570867085,-5.90878417028714,23.0907996989384));
#71353=CARTESIAN_POINT('Ctrl Pts',(5.58861721896062,-5.60883386968437,23.1082384850568));
#71354=CARTESIAN_POINT('Ctrl Pts',(5.81649884194595,-5.37215092027798,23.1209394018081));
#71355=CARTESIAN_POINT('Ctrl Pts',(6.28173242759376,-4.82453174847245,23.148715823079));
#71356=CARTESIAN_POINT('Ctrl Pts',(6.51207663856423,-4.50878141877307,23.1637448717277));
#71357=CARTESIAN_POINT('Ctrl Pts',(6.74145640679847,-4.13988302276304,23.181047900546));
#71358=CARTESIAN_POINT('Ctrl Pts',(6.76443000200072,-4.10223751447841,23.1828111039054));
#71359=CARTESIAN_POINT('Ctrl Pts',(6.79505207899578,-4.05110214243058,23.185204316452));
#71360=CARTESIAN_POINT('Ctrl Pts',(6.8029775572945,-4.03777880489369,23.1858277038117));
#71361=CARTESIAN_POINT('Ctrl Pts',(6.81631523438678,-4.01520640323484,23.1868836569137));
#71362=CARTESIAN_POINT('Ctrl Pts',(6.82174790513662,-4.00596946481896,23.1873157139473));
#71363=CARTESIAN_POINT('Ctrl Pts',(6.8321624762226,-3.98817939335677,23.1881477736466));
#71364=CARTESIAN_POINT('Ctrl Pts',(6.83714712648454,-3.97962789029868,23.1885477053694));
#71365=CARTESIAN_POINT('Ctrl Pts',(6.84885669347463,-3.95945240325309,23.1894912208817));
#71366=CARTESIAN_POINT('Ctrl Pts',(6.85556808000964,-3.94782061902841,23.1900351552152));
#71367=CARTESIAN_POINT('Ctrl Pts',(6.87585782351141,-3.91244785221126,23.1916892939209));
#71368=CARTESIAN_POINT('Ctrl Pts',(6.8893426270714,-3.88865364248772,23.1928020380197));
#71369=CARTESIAN_POINT('Ctrl Pts',(6.92057543881955,-3.83287031746905,23.195410397647));
#71370=CARTESIAN_POINT('Ctrl Pts',(6.93822546948616,-3.80082709137985,23.1969084117865));
#71371=CARTESIAN_POINT('Ctrl Pts',(7.15928429260873,-3.39282869953811,23.215972058358));
#71372=CARTESIAN_POINT('Ctrl Pts',(7.33211758677791,-3.00111346891349,23.2341256964937));
#71373=CARTESIAN_POINT('Ctrl Pts',(7.61086672054827,-2.199169079531,23.2698653959958));
#71374=CARTESIAN_POINT('Ctrl Pts',(7.71723037376971,-1.79053539711598,23.2873958969421));
#71375=CARTESIAN_POINT('Ctrl Pts',(7.79926621871597,-1.3258562245647,23.3065452459883));
#71376=CARTESIAN_POINT('Ctrl Pts',(7.80753418056874,-1.27626734831667,23.3085795977167));
#71377=CARTESIAN_POINT('Ctrl Pts',(7.81941077848575,-1.20059532227504,23.3116706741806));
#71378=CARTESIAN_POINT('Ctrl Pts',(7.82336277393056,-1.1745675649381,23.3127314729844));
#71379=CARTESIAN_POINT('Ctrl Pts',(7.83033237691482,-1.1270696141196,23.3146630986422));
#71380=CARTESIAN_POINT('Ctrl Pts',(7.83339178068934,-1.10560583476223,23.3155344092165));
#71381=CARTESIAN_POINT('Ctrl Pts',(7.83972868879752,-1.05980106500253,23.3173905825955));
#71382=CARTESIAN_POINT('Ctrl Pts',(7.84298115345093,-1.03545682820167,23.3183751458748));
#71383=CARTESIAN_POINT('Ctrl Pts',(7.85148000659213,-0.969505716347193,
23.3210373443951));
#71384=CARTESIAN_POINT('Ctrl Pts',(7.85650902451848,-0.927871542886805,
23.3227124818463));
#71385=CARTESIAN_POINT('Ctrl Pts',(7.88210177274179,-0.70084596653946,23.3318191407429));
#71386=CARTESIAN_POINT('Ctrl Pts',(7.89643501282665,-0.514809836578552,
23.33917984715));
#71387=CARTESIAN_POINT('Ctrl Pts',(7.92877855106349,0.26356654612102,23.3697480910059));
#71388=CARTESIAN_POINT('Ctrl Pts',(7.88679135747681,0.856487282413173,23.3924787464047));
#71389=CARTESIAN_POINT('Ctrl Pts',(7.68394771174086,1.95290454328115,23.4343579205409));
#71390=CARTESIAN_POINT('Ctrl Pts',(7.53824744648573,2.45594445503094,23.4535460998312));
#71391=CARTESIAN_POINT('Ctrl Pts',(7.30465067374258,3.03928051752987,23.4779753859744));
#71392=CARTESIAN_POINT('Ctrl Pts',(7.26329039781512,3.13683904001587,23.482142496315));
#71393=CARTESIAN_POINT('Ctrl Pts',(7.2132233632447,3.24863098935327,23.4870371636609));
#71394=CARTESIAN_POINT('Ctrl Pts',(7.20641525223859,3.26370553220862,23.487699729943));
#71395=CARTESIAN_POINT('Ctrl Pts',(7.19551888031526,3.28763199144062,23.488755549197));
#71396=CARTESIAN_POINT('Ctrl Pts',(7.19146142702185,3.29649793126628,23.4891476994164));
#71397=CARTESIAN_POINT('Ctrl Pts',(7.18429162999197,3.31208841689563,23.4898389292233));
#71398=CARTESIAN_POINT('Ctrl Pts',(7.18118620551502,3.31881614245334,23.490137754466));
#71399=CARTESIAN_POINT('Ctrl Pts',(7.17476479296949,3.33267655746222,23.4907545229749));
#71400=CARTESIAN_POINT('Ctrl Pts',(7.17144761078337,3.33980868260003,23.4910725107582));
#71401=CARTESIAN_POINT('Ctrl Pts',(7.16296508547,3.3579756749499,23.4918840922758));
#71402=CARTESIAN_POINT('Ctrl Pts',(7.15778488647676,3.36900355686768,23.4923782535389));
#71403=CARTESIAN_POINT('Ctrl Pts',(7.13680999380535,3.41338927325529,23.4943734072684));
#71404=CARTESIAN_POINT('Ctrl Pts',(7.12080756971057,3.44664804055914,23.4958825856642));
#71405=CARTESIAN_POINT('Ctrl Pts',(7.02106126503938,3.65029661103432,23.5052169252257));
#71406=CARTESIAN_POINT('Ctrl Pts',(6.93145261984057,3.81771075567021,23.5133305183864));
#71407=CARTESIAN_POINT('Ctrl Pts',(6.77862428799867,4.08008952507064,23.5266739473422));
#71408=CARTESIAN_POINT('Ctrl Pts',(6.71921808174932,4.17719821268043,23.5317505649124));
#71409=CARTESIAN_POINT('Ctrl Pts',(6.61147894941804,4.34506642757134,23.5407318260381));
#71410=CARTESIAN_POINT('Ctrl Pts',(6.56405207665741,4.41638722957821,23.5446149554398));
#71411=CARTESIAN_POINT('Ctrl Pts',(6.12904193172172,5.04806702939568,23.5795370095158));
#71412=CARTESIAN_POINT('Ctrl Pts',(5.67166590504446,5.55702874414432,23.6111498576263));
#71413=CARTESIAN_POINT('Ctrl Pts',(5.02672858974368,6.11100476619619,23.6472191217833));
#71414=CARTESIAN_POINT('Ctrl Pts',(4.89527196509317,6.2168075786396,23.6542203536619));
#71415=CARTESIAN_POINT('Ctrl Pts',(4.74268081558628,6.3317769210229,23.6619615610662));
#71416=CARTESIAN_POINT('Ctrl Pts',(4.724777457135,6.34514761744716,23.6628640245789));
#71417=CARTESIAN_POINT('Ctrl Pts',(4.69855409812888,6.3645593791199,23.6641774652524));
#71418=CARTESIAN_POINT('Ctrl Pts',(4.69027866588356,6.37066030649616,23.6645907381541));
#71419=CARTESIAN_POINT('Ctrl Pts',(4.67561495802314,6.38142682643755,23.6653208961907));
#71420=CARTESIAN_POINT('Ctrl Pts',(4.66923154197052,6.38609899585017,23.6656380329438));
#71421=CARTESIAN_POINT('Ctrl Pts',(4.65612110420082,6.39566466144694,23.6662879122424));
#71422=CARTESIAN_POINT('Ctrl Pts',(4.64939334922257,6.40055713851608,23.6666206156598));
#71423=CARTESIAN_POINT('Ctrl Pts',(4.63222486269812,6.41300084598711,23.667467633827));
#71424=CARTESIAN_POINT('Ctrl Pts',(4.62177335841787,6.42053720919399,23.6679813810798));
#71425=CARTESIAN_POINT('Ctrl Pts',(4.59909572836672,6.43680551232517,23.6690920474437));
#71426=CARTESIAN_POINT('Ctrl Pts',(4.58686303558996,6.44552823421536,23.6696886154088));
#71427=CARTESIAN_POINT('Ctrl Pts',(4.55173524446504,6.47042603516095,23.6713944951618));
#71428=CARTESIAN_POINT('Ctrl Pts',(4.52877882227899,6.48651441155713,23.6725005250598));
#71429=CARTESIAN_POINT('Ctrl Pts',(4.45217889305156,6.53959248698265,23.6761622605801));
#71430=CARTESIAN_POINT('Ctrl Pts',(4.39816335931221,6.57604182653211,23.6786977051158));
#71431=CARTESIAN_POINT('Ctrl Pts',(4.18747564078016,6.71445527622746,23.6884131467903));
#71432=CARTESIAN_POINT('Ctrl Pts',(4.02765516701556,6.81152412512922,23.6954139551315));
#71433=CARTESIAN_POINT('Ctrl Pts',(3.6346555170252,7.03154396873902,23.7118728288845));
#71434=CARTESIAN_POINT('Ctrl Pts',(3.39847963177191,7.14868355680275,23.7211496677));
#71435=CARTESIAN_POINT('Ctrl Pts',(2.70858062390757,7.44893018829526,23.7471397187575));
#71436=CARTESIAN_POINT('Ctrl Pts',(2.243169230144,7.60204761736952,23.7633231211076));
#71437=CARTESIAN_POINT('Ctrl Pts',(1.53560572187946,7.76414878679049,23.7890273418242));
#71438=CARTESIAN_POINT('Ctrl Pts',(1.30233994350359,7.80666305662586,23.7976844718643));
#71439=CARTESIAN_POINT('Ctrl Pts',(0.998277790035399,7.8480728742975,23.8095687776602));
#71440=CARTESIAN_POINT('Ctrl Pts',(0.928901479797764,7.85658627503436,23.812320486009));
#71441=CARTESIAN_POINT('Ctrl Pts',(0.848270607176247,7.86539788230396,23.8155736477568));
#71442=CARTESIAN_POINT('Ctrl Pts',(0.837115302974101,7.86659296246253,23.8160249442697));
#71443=CARTESIAN_POINT('Ctrl Pts',(0.820528641148601,7.86833422948586,23.8166978300939));
#71444=CARTESIAN_POINT('Ctrl Pts',(0.815099158920377,7.86889853528994,23.8169183887842));
#71445=CARTESIAN_POINT('Ctrl Pts',(0.805435194367477,7.86989283684836,23.8173114954916));
#71446=CARTESIAN_POINT('Ctrl Pts',(0.80120093591569,7.87032503623294,23.8174839169804));
#71447=CARTESIAN_POINT('Ctrl Pts',(0.792295569322927,7.87122676401817,23.8178469351468));
#71448=CARTESIAN_POINT('Ctrl Pts',(0.78762438966661,7.87169555180985,23.8180375745378));
#71449=CARTESIAN_POINT('Ctrl Pts',(0.775338199530305,7.87291751716785,23.8185395901324));
#71450=CARTESIAN_POINT('Ctrl Pts',(0.767722525272494,7.87366380277699,23.8188513674404));
#71451=CARTESIAN_POINT('Ctrl Pts',(0.732536457642459,7.87706026950344,23.8202946608434));
#71452=CARTESIAN_POINT('Ctrl Pts',(0.704953759796035,7.87957665736916,23.8214340766096));
#71453=CARTESIAN_POINT('Ctrl Pts',(0.488827753901776,7.89815009389373,23.8304212661561));
#71454=CARTESIAN_POINT('Ctrl Pts',(0.299787799166418,7.90758150313049,23.8386338580007));
#71455=CARTESIAN_POINT('Ctrl Pts',(-0.120729563006223,7.91346142537141,
23.8573852362886));
#71456=CARTESIAN_POINT('Ctrl Pts',(-0.352087218733693,7.90654628231055,
23.8680241801041));
#71457=CARTESIAN_POINT('Ctrl Pts',(-0.65105880425389,7.88446118747239,23.881918907157));
#71458=CARTESIAN_POINT('Ctrl Pts',(-0.71924979366994,7.87853320517207,23.8850983236977));
#71459=CARTESIAN_POINT('Ctrl Pts',(-1.09604502441676,7.84084492532695,23.9026977017609));
#71460=CARTESIAN_POINT('Ctrl Pts',(-1.4026630453346,7.79183636428385,23.917120256516));
#71461=CARTESIAN_POINT('Ctrl Pts',(-2.11664858668259,7.63419290565653,23.9502008801544));
#71462=CARTESIAN_POINT('Ctrl Pts',(-2.51981349726183,7.51077348649919,23.9684536193038));
#71463=CARTESIAN_POINT('Ctrl Pts',(-2.94036906228805,7.34432631318953,23.9868175858454));
#71464=CARTESIAN_POINT('Ctrl Pts',(-2.96938237553174,7.33264396765908,23.9880812258696));
#71465=CARTESIAN_POINT('Ctrl Pts',(-3.00915499015354,7.3163545694439,23.9898090959107));
#71466=CARTESIAN_POINT('Ctrl Pts',(-3.01997427489917,7.31189533029402,23.9902786789134));
#71467=CARTESIAN_POINT('Ctrl Pts',(-3.03716377430616,7.30476590427185,23.9910240407974));
#71468=CARTESIAN_POINT('Ctrl Pts',(-3.0435404331586,7.30211136180672,23.9913003877579));
#71469=CARTESIAN_POINT('Ctrl Pts',(-3.05631996584912,7.29677171580894,23.9918539102653));
#71470=CARTESIAN_POINT('Ctrl Pts',(-3.06272279800345,7.29408652740122,23.9921310824059));
#71471=CARTESIAN_POINT('Ctrl Pts',(-3.0774821986731,7.28787394177867,23.9927696467572));
#71472=CARTESIAN_POINT('Ctrl Pts',(-3.08583625987789,7.2843405914596,23.9931308215867));
#71473=CARTESIAN_POINT('Ctrl Pts',(-3.11105452801021,7.27362335649574,23.9942203069956));
#71474=CARTESIAN_POINT('Ctrl Pts',(-3.12789991788475,7.26639519420163,23.9949470003055));
#71475=CARTESIAN_POINT('Ctrl Pts',(-3.16633395964868,7.2497451739042,23.9966026228445));
#71476=CARTESIAN_POINT('Ctrl Pts',(-3.18790600519988,7.24028529449018,23.9975301561475));
#71477=CARTESIAN_POINT('Ctrl Pts',(-3.25800683985186,7.20917029763962,24.0005388355236));
#71478=CARTESIAN_POINT('Ctrl Pts',(-3.30636020693329,7.18712232237946,24.0026055864361));
#71479=CARTESIAN_POINT('Ctrl Pts',(-3.49663728033995,7.09803385163271,24.0107076555686));
#71480=CARTESIAN_POINT('Ctrl Pts',(-3.63677803213146,7.0272616109383,24.0166054729994));
#71481=CARTESIAN_POINT('Ctrl Pts',(-3.94385852656225,6.86053492260607,24.0294363261122));
#71482=CARTESIAN_POINT('Ctrl Pts',(-4.10958850413554,6.76256212043791,24.0362967993362));
#71483=CARTESIAN_POINT('Ctrl Pts',(-4.63589686827892,6.42492986833089,24.0581297817026));
#71484=CARTESIAN_POINT('Ctrl Pts',(-4.98040439427615,6.16172309248277,24.0724535638952));
#71485=CARTESIAN_POINT('Ctrl Pts',(-5.52756918400236,5.66767561438524,24.0976380874301));
#71486=CARTESIAN_POINT('Ctrl Pts',(-5.74150971493769,5.45083571940355,24.1082604598443));
#71487=CARTESIAN_POINT('Ctrl Pts',(-6.02353300551831,5.12991937375214,24.1243069739131));
#71488=CARTESIAN_POINT('Ctrl Pts',(-6.10248894611335,5.03573712885225,24.1290532292525));
#71489=CARTESIAN_POINT('Ctrl Pts',(-6.18703868328447,4.92997264760374,24.1344726365829));
#71490=CARTESIAN_POINT('Ctrl Pts',(-6.19483866167622,4.92016787587154,24.1349758653105));
#71491=CARTESIAN_POINT('Ctrl Pts',(-6.20568060660859,4.90647262275271,24.135679993006));
#71492=CARTESIAN_POINT('Ctrl Pts',(-6.20874230601726,4.90259771616207,24.1358793535303));
#71493=CARTESIAN_POINT('Ctrl Pts',(-6.21434610689373,4.8954918409712,24.1362451970532));
#71494=CARTESIAN_POINT('Ctrl Pts',(-6.21688930762985,4.89226177118805,24.1364115909687));
#71495=CARTESIAN_POINT('Ctrl Pts',(-6.2220413309239,4.88570778196178,24.1367494030047));
#71496=CARTESIAN_POINT('Ctrl Pts',(-6.22465001032928,4.88238375214546,24.1369208320856));
#71497=CARTESIAN_POINT('Ctrl Pts',(-6.23107045755304,4.87418918434719,24.1373436873592));
#71498=CARTESIAN_POINT('Ctrl Pts',(-6.23487917345583,4.86931627066528,24.1375953471596));
#71499=CARTESIAN_POINT('Ctrl Pts',(-6.2487650879767,4.85150747322559,24.1385158189377));
#71500=CARTESIAN_POINT('Ctrl Pts',(-6.25880771009156,4.8385448150794,24.1391872407626));
#71501=CARTESIAN_POINT('Ctrl Pts',(-6.47597989011398,4.55641929758985,24.1538295358105));
#71502=CARTESIAN_POINT('Ctrl Pts',(-6.66558337008851,4.27425115991201,24.1690395234084));
#71503=CARTESIAN_POINT('Ctrl Pts',(-7.18503379951001,3.38217198963414,24.2166621385544));
#71504=CARTESIAN_POINT('Ctrl Pts',(-7.45353448312411,2.74022632557994,24.2500217232447));
#71505=CARTESIAN_POINT('Ctrl Pts',(-7.6457392424917,2.03181794326608,24.2824492078524));
#71506=CARTESIAN_POINT('Ctrl Pts',(-7.65619972334459,1.99203879997181,24.2842573851819));
#71507=CARTESIAN_POINT('Ctrl Pts',(-7.73259036098254,1.69204725906104,24.2977966740719));
#71508=CARTESIAN_POINT('Ctrl Pts',(-7.78555191866778,1.42869818541259,24.3091257566545));
#71509=CARTESIAN_POINT('Ctrl Pts',(-7.82856292048183,1.13934309435532,24.320985714229));
#71510=CARTESIAN_POINT('Ctrl Pts',(-7.8319924517737,1.11552424257621,24.3219577645945));
#71511=CARTESIAN_POINT('Ctrl Pts',(-7.83664570468078,1.08212676226932,24.323314872601));
#71512=CARTESIAN_POINT('Ctrl Pts',(-7.83796063480691,1.07256110240004,24.3237029022796));
#71513=CARTESIAN_POINT('Ctrl Pts',(-7.8402083464816,1.05598489611933,24.3243741572717));
#71514=CARTESIAN_POINT('Ctrl Pts',(-7.84114924464035,1.0489754719331,24.3246576464972));
#71515=CARTESIAN_POINT('Ctrl Pts',(-7.84302304457943,1.03487279720169,24.3252272980427));
#71516=CARTESIAN_POINT('Ctrl Pts',(-7.84395572626761,1.02777952349394,24.3255134529837));
#71517=CARTESIAN_POINT('Ctrl Pts',(-7.84583429129169,1.0133410677833,24.326095186239));
#71518=CARTESIAN_POINT('Ctrl Pts',(-7.84677948536533,1.00599580243136,24.3263907419387));
#71519=CARTESIAN_POINT('Ctrl Pts',(-7.84893635826412,0.989046384850755,
24.3270718522219));
#71520=CARTESIAN_POINT('Ctrl Pts',(-7.85014072725494,0.979441305353303,
24.3274571697809));
#71521=CARTESIAN_POINT('Ctrl Pts',(-7.85319884954731,0.954684162242196,
24.3284486346545));
#71522=CARTESIAN_POINT('Ctrl Pts',(-7.85502638631633,0.939528868030736,
24.3290539347043));
#71523=CARTESIAN_POINT('Ctrl Pts',(-7.89308436335134,0.616049266785744,
24.3419391860885));
#71524=CARTESIAN_POINT('Ctrl Pts',(-7.91117986940194,0.305855064022118,
24.3536116502532));
#71525=CARTESIAN_POINT('Ctrl Pts',(-7.91099865242614,-0.00461750059333042,
24.3648601029169));
#71526=CARTESIAN_POINT('',(-7.911,-2.54574139546548E-12,28.3576684917631));
#71527=CARTESIAN_POINT('Ctrl Pts',(-7.91099868333906,-0.00456423132557518,
24.3648581729618));
#71528=CARTESIAN_POINT('Ctrl Pts',(-7.91057280418394,-0.74272345138825,
24.3916018705913));
#71529=CARTESIAN_POINT('Ctrl Pts',(-7.80684320026678,-1.4771488358149,24.4154648676329));
#71530=CARTESIAN_POINT('Ctrl Pts',(-7.56811091958988,-2.30724848110784,
24.447304034168));
#71531=CARTESIAN_POINT('Ctrl Pts',(-7.53052499884332,-2.42711544366794,
24.4520358224672));
#71532=CARTESIAN_POINT('Ctrl Pts',(-7.46568562111904,-2.61786464781053,
24.4598522725625));
#71533=CARTESIAN_POINT('Ctrl Pts',(-7.44023716408572,-2.68933955186086,
24.4628475646539));
#71534=CARTESIAN_POINT('Ctrl Pts',(-7.40882571863918,-2.77370201921998,
24.466454506756));
#71535=CARTESIAN_POINT('Ctrl Pts',(-7.40385024548674,-2.78695585891665,
24.4670232896717));
#71536=CARTESIAN_POINT('Ctrl Pts',(-7.39613871846185,-2.8073316984716,24.4679008983619));
#71537=CARTESIAN_POINT('Ctrl Pts',(-7.39342787799656,-2.81446325616779,
24.4682086643088));
#71538=CARTESIAN_POINT('Ctrl Pts',(-7.38866736450488,-2.82693266111981,
24.4687478307165));
#71539=CARTESIAN_POINT('Ctrl Pts',(-7.38662221030384,-2.83227223547321,
24.4689790443924));
#71540=CARTESIAN_POINT('Ctrl Pts',(-7.38231899087612,-2.84347089747421,
24.4694646652473));
#71541=CARTESIAN_POINT('Ctrl Pts',(-7.38005973579183,-2.84932952177866,
24.4697191208459));
#71542=CARTESIAN_POINT('Ctrl Pts',(-7.37375230336661,-2.86562791465739,
24.4704281102938));
#71543=CARTESIAN_POINT('Ctrl Pts',(-7.36968894157625,-2.87606176558802,
24.470883254155));
#71544=CARTESIAN_POINT('Ctrl Pts',(-7.35335451956991,-2.91774318610118,
24.4727064574208));
#71545=CARTESIAN_POINT('Ctrl Pts',(-7.34090686230723,-2.94892088541314,
24.4740814241713));
#71546=CARTESIAN_POINT('Ctrl Pts',(-7.02618161225528,-3.72287217082697,
24.5084798205973));
#71547=CARTESIAN_POINT('Ctrl Pts',(-6.61290490762547,-4.41549731126929,
24.5448642602979));
#71548=CARTESIAN_POINT('Ctrl Pts',(-5.90484596763496,-5.27382606389827,
24.5923710786458));
#71549=CARTESIAN_POINT('Ctrl Pts',(-5.6931873058509,-5.50164353888001,24.6053443713055));
#71550=CARTESIAN_POINT('Ctrl Pts',(-5.42266693281738,-5.76043897508899,
24.6205907434687));
#71551=CARTESIAN_POINT('Ctrl Pts',(-5.37613535644784,-5.80389029820227,
24.623170000312));
#71552=CARTESIAN_POINT('Ctrl Pts',(-5.31242847210986,-5.86195637962692,
24.6266448495277));
#71553=CARTESIAN_POINT('Ctrl Pts',(-5.29570802569502,-5.8770660520855,24.6275516671449));
#71554=CARTESIAN_POINT('Ctrl Pts',(-5.26793945656868,-5.90194479501025,
24.6290491025975));
#71555=CARTESIAN_POINT('Ctrl Pts',(-5.25692820328638,-5.91175476052918,
24.6296406817606));
#71556=CARTESIAN_POINT('Ctrl Pts',(-5.23560056281896,-5.93064892687557,
24.6307822485686));
#71557=CARTESIAN_POINT('Ctrl Pts',(-5.22528780580952,-5.93973714023708,
24.6313323304907));
#71558=CARTESIAN_POINT('Ctrl Pts',(-5.20118048409164,-5.96087056947665,
24.6326137666886));
#71559=CARTESIAN_POINT('Ctrl Pts',(-5.18736766212209,-5.97289486894715,
24.6333446170841));
#71560=CARTESIAN_POINT('Ctrl Pts',(-5.14396246651794,-6.01041570216597,
24.6356306867513));
#71561=CARTESIAN_POINT('Ctrl Pts',(-5.11422281464742,-6.03574119766234,
24.6371817506539));
#71562=CARTESIAN_POINT('Ctrl Pts',(-4.78273737141377,-6.31381631427511,
24.65430281125));
#71563=CARTESIAN_POINT('Ctrl Pts',(-4.46271148451399,-6.54393516552441,
24.6692622136227));
#71564=CARTESIAN_POINT('Ctrl Pts',(-3.54124720150995,-7.10736674454685,
24.7092287078701));
#71565=CARTESIAN_POINT('Ctrl Pts',(-2.91159064066481,-7.38766060745645,
24.7330569426243));
#71566=CARTESIAN_POINT('Ctrl Pts',(-2.20447659406172,-7.59781857764282,
24.7620519783176));
#71567=CARTESIAN_POINT('Ctrl Pts',(-2.15505423245597,-7.61198431975259,
24.7640914166593));
#71568=CARTESIAN_POINT('Ctrl Pts',(-2.09444467739586,-7.628719026526,24.7666118803012));
#71569=CARTESIAN_POINT('Ctrl Pts',(-2.08338467545342,-7.63174690254177,
24.7670725997542));
#71570=CARTESIAN_POINT('Ctrl Pts',(-2.06607118397764,-7.63644634386728,
24.7677950992663));
#71571=CARTESIAN_POINT('Ctrl Pts',(-2.05982213117272,-7.63813430672697,
24.7680561360051));
#71572=CARTESIAN_POINT('Ctrl Pts',(-2.04875728857251,-7.64110852029014,
24.7685188116157));
#71573=CARTESIAN_POINT('Ctrl Pts',(-2.04394233644181,-7.64239789408099,
24.7687203068061));
#71574=CARTESIAN_POINT('Ctrl Pts',(-2.03288457655398,-7.64534780297848,
24.7691834195844));
#71575=CARTESIAN_POINT('Ctrl Pts',(-2.02664095278821,-7.64700524245969,
24.7694451807607));
#71576=CARTESIAN_POINT('Ctrl Pts',(-2.00965764677336,-7.65149138961377,
24.7701579500033));
#71577=CARTESIAN_POINT('Ctrl Pts',(-1.99891405493644,-7.65430512467304,
24.7706096625556));
#71578=CARTESIAN_POINT('Ctrl Pts',(-1.94694966130662,-7.66779767665567,
24.772798592575));
#71579=CARTESIAN_POINT('Ctrl Pts',(-1.90565114741246,-7.67816565644995,
24.7745509536764));
#71580=CARTESIAN_POINT('Ctrl Pts',(-1.14061337383398,-7.86367545737623,
24.8072617473561));
#71581=CARTESIAN_POINT('Ctrl Pts',(-0.395833514475741,-7.9360988753032,
24.8428048346375));
#71582=CARTESIAN_POINT('Ctrl Pts',(0.580362777294007,-7.89310941372685,
24.8872368707984));
#71583=CARTESIAN_POINT('Ctrl Pts',(0.812124855088617,-7.87263991554324,
24.8976542536977));
#71584=CARTESIAN_POINT('Ctrl Pts',(1.24019296708237,-7.81572467997065,24.916528247909));
#71585=CARTESIAN_POINT('Ctrl Pts',(1.43667267779269,-7.78200549687933,24.9250461319951));
#71586=CARTESIAN_POINT('Ctrl Pts',(1.69777864429009,-7.72696784047774,24.9361576998387));
#71587=CARTESIAN_POINT('Ctrl Pts',(1.76369840599539,-7.71218857071168,24.9389452366668));
#71588=CARTESIAN_POINT('Ctrl Pts',(1.85768236901427,-7.6898492180152,24.9428946964361));
#71589=CARTESIAN_POINT('Ctrl Pts',(1.88590586808909,-7.68297623705975,24.9440775099758));
#71590=CARTESIAN_POINT('Ctrl Pts',(1.93563880087852,-7.67057472479855,24.9461561788123));
#71591=CARTESIAN_POINT('Ctrl Pts',(1.95716392549673,-7.66511079860863,24.9470540059836));
#71592=CARTESIAN_POINT('Ctrl Pts',(1.98890646314267,-7.65691086201822,24.9483753185498));
#71593=CARTESIAN_POINT('Ctrl Pts',(1.99914176747386,-7.6542449047991,24.9488009589429));
#71594=CARTESIAN_POINT('Ctrl Pts',(2.01731033406585,-7.64947366711465,24.9495557796115));
#71595=CARTESIAN_POINT('Ctrl Pts',(2.02524571390958,-7.64737655451795,24.9498852111278));
#71596=CARTESIAN_POINT('Ctrl Pts',(2.04068906644963,-7.64326955843328,24.9505258528143));
#71597=CARTESIAN_POINT('Ctrl Pts',(2.04819736802509,-7.6412609529352,24.9508371019934));
#71598=CARTESIAN_POINT('Ctrl Pts',(2.06618157076311,-7.63642144427841,24.9515820953173));
#71599=CARTESIAN_POINT('Ctrl Pts',(2.07665464327614,-7.63358004161279,24.952015514621));
#71600=CARTESIAN_POINT('Ctrl Pts',(2.10850720898211,-7.62486786090342,24.9533324220028));
#71601=CARTESIAN_POINT('Ctrl Pts',(2.1298679767266,-7.61892872771783,24.9542137952552));
#71602=CARTESIAN_POINT('Ctrl Pts',(2.3609904755439,-7.55361963892546,24.9637315555435));
#71603=CARTESIAN_POINT('Ctrl Pts',(2.56824481651057,-7.48569119055802,24.9720962281796));
#71604=CARTESIAN_POINT('Ctrl Pts',(3.18927518032591,-7.25331133215228,24.9968311235325));
#71605=CARTESIAN_POINT('Ctrl Pts',(3.59222096964228,-7.0624343638207,25.0123821974582));
#71606=CARTESIAN_POINT('Ctrl Pts',(4.26880091771409,-6.66897414393222,25.0394358086205));
#71607=CARTESIAN_POINT('Ctrl Pts',(4.54944875954921,-6.48077018322996,25.0509985159481));
#71608=CARTESIAN_POINT('Ctrl Pts',(5.06113495334599,-6.08797150006487,25.0740260343391));
#71609=CARTESIAN_POINT('Ctrl Pts',(5.29393425210766,-5.88665853749663,25.0854177797673));
#71610=CARTESIAN_POINT('Ctrl Pts',(5.53019444191725,-5.65697391424798,25.0985318157757));
#71611=CARTESIAN_POINT('Ctrl Pts',(5.54589543263123,-5.64158207152078,25.0994105434988));
#71612=CARTESIAN_POINT('Ctrl Pts',(5.5681651846667,-5.61956799686196,25.1006669696907));
#71613=CARTESIAN_POINT('Ctrl Pts',(5.57478680053978,-5.61299920921923,25.1010418289023));
#71614=CARTESIAN_POINT('Ctrl Pts',(5.58618134954588,-5.60165551516449,25.1016890739585));
#71615=CARTESIAN_POINT('Ctrl Pts',(5.59095982426596,-5.59688617212325,25.1019611706111));
#71616=CARTESIAN_POINT('Ctrl Pts',(5.60008495211548,-5.58775513483806,25.1024820381891));
#71617=CARTESIAN_POINT('Ctrl Pts',(5.60443263074964,-5.58339446975902,25.102730756456));
#71618=CARTESIAN_POINT('Ctrl Pts',(5.61458719454918,-5.57318576349309,25.103312949429));
#71619=CARTESIAN_POINT('Ctrl Pts',(5.62039003650966,-5.56733372059712,25.1036466257482));
#71620=CARTESIAN_POINT('Ctrl Pts',(5.64094662244933,-5.54653794642556,25.1048321302628));
#71621=CARTESIAN_POINT('Ctrl Pts',(5.65564993067959,-5.53154461615034,25.1056864069206));
#71622=CARTESIAN_POINT('Ctrl Pts',(5.90146310147021,-5.27887815383104,25.1200726748901));
#71623=CARTESIAN_POINT('Ctrl Pts',(6.11746049448109,-5.0269753881479,25.134249044076));
#71624=CARTESIAN_POINT('Ctrl Pts',(6.55917400858412,-4.44105678080844,25.1658737865343));
#71625=CARTESIAN_POINT('Ctrl Pts',(6.77649152296901,-4.10181989985027,25.1833100046639));
#71626=CARTESIAN_POINT('Ctrl Pts',(7.23703448889201,-3.24561948833542,25.2246095169069));
#71627=CARTESIAN_POINT('Ctrl Pts',(7.45198461487632,-2.71600323355572,25.2479730860838));
#71628=CARTESIAN_POINT('Ctrl Pts',(7.62939279128401,-2.0933911265076,25.2742362256997));
#71629=CARTESIAN_POINT('Ctrl Pts',(7.64952386379584,-2.01858998718013,25.2773705458916));
#71630=CARTESIAN_POINT('Ctrl Pts',(7.67711152940006,-1.90973640188646,25.2819013974262));
#71631=CARTESIAN_POINT('Ctrl Pts',(7.6854466510456,-1.87591160350011,25.2833050894432));
#71632=CARTESIAN_POINT('Ctrl Pts',(7.69970888978824,-1.81634297718084,25.2857697823978));
#71633=CARTESIAN_POINT('Ctrl Pts',(7.70573097929015,-1.79062248334811,25.286831589573));
#71634=CARTESIAN_POINT('Ctrl Pts',(7.71781795265164,-1.73780835204953,25.2890070242199));
#71635=CARTESIAN_POINT('Ctrl Pts',(7.72386926207246,-1.71071197075203,25.290120516651));
#71636=CARTESIAN_POINT('Ctrl Pts',(7.73901764214081,-1.64116177599236,25.2929719740408));
#71637=CARTESIAN_POINT('Ctrl Pts',(7.74790810464243,-1.59866383731985,25.2947080161914));
#71638=CARTESIAN_POINT('Ctrl Pts',(7.78224438332102,-1.4275125808803,25.3016748788065));
#71639=CARTESIAN_POINT('Ctrl Pts',(7.80483935090458,-1.29830779536354,25.3068780602028));
#71640=CARTESIAN_POINT('Ctrl Pts',(7.9000304207093,-0.660968121277869,25.3323056701324));
#71641=CARTESIAN_POINT('Ctrl Pts',(7.92626698574461,-0.147163008991056,
25.3519894929041));
#71642=CARTESIAN_POINT('Ctrl Pts',(7.88986299150046,0.639812488650948,25.3825238973486));
#71643=CARTESIAN_POINT('Ctrl Pts',(7.86290839865452,0.913215186299687,25.3932212701483));
#71644=CARTESIAN_POINT('Ctrl Pts',(7.81702505766936,1.21616441837616,25.4054654802047));
#71645=CARTESIAN_POINT('Ctrl Pts',(7.81206238070383,1.24764497564341,25.4067426317572));
#71646=CARTESIAN_POINT('Ctrl Pts',(7.80454175468626,1.29354685884412,25.4086125362271));
#71647=CARTESIAN_POINT('Ctrl Pts',(7.80213374443213,1.30799254914851,25.40920212347));
#71648=CARTESIAN_POINT('Ctrl Pts',(7.79783296193881,1.33335851563333,25.4102394459991));
#71649=CARTESIAN_POINT('Ctrl Pts',(7.79595732560442,1.34428167061491,25.4106868039568));
#71650=CARTESIAN_POINT('Ctrl Pts',(7.7922671195098,1.36550485945748,25.411557327662));
#71651=CARTESIAN_POINT('Ctrl Pts',(7.79045506577337,1.37580530976172,25.4119804356678));
#71652=CARTESIAN_POINT('Ctrl Pts',(7.78606071856236,1.40049751067626,25.412996207441));
#71653=CARTESIAN_POINT('Ctrl Pts',(7.78345895449406,1.41488568199054,25.4135893266697));
#71654=CARTESIAN_POINT('Ctrl Pts',(7.77293131128146,1.47219736053309,25.4159568607082));
#71655=CARTESIAN_POINT('Ctrl Pts',(7.76469020079339,1.51506180355613,25.4177386432284));
#71656=CARTESIAN_POINT('Ctrl Pts',(7.66879175300856,1.99251137683444,25.4376988104559));
#71657=CARTESIAN_POINT('Ctrl Pts',(7.54510701946391,2.41905347451808,25.4565372503823));
#71658=CARTESIAN_POINT('Ctrl Pts',(7.23598835250862,3.22501008889486,25.4928701956944));
#71659=CARTESIAN_POINT('Ctrl Pts',(7.05465115731419,3.60446099832577,25.510325987878));
#71660=CARTESIAN_POINT('Ctrl Pts',(6.81874135146916,4.01138797281012,25.5294115341544));
#71661=CARTESIAN_POINT('Ctrl Pts',(6.79301674932022,4.0547984631937,25.5314531073103));
#71662=CARTESIAN_POINT('Ctrl Pts',(6.75320840415856,4.12053317739695,25.5345537597579));
#71663=CARTESIAN_POINT('Ctrl Pts',(6.73942543881044,4.14303779578966,25.5356169445171));
#71664=CARTESIAN_POINT('Ctrl Pts',(6.7152406250969,4.18208634784794,25.5374647443686));
#71665=CARTESIAN_POINT('Ctrl Pts',(6.7048896191626,4.19866146185758,25.5382500461887));
#71666=CARTESIAN_POINT('Ctrl Pts',(6.68183351577716,4.23527861660687,25.5399871075836));
#71667=CARTESIAN_POINT('Ctrl Pts',(6.66909943421595,4.25530220243095,25.5409384642154));
#71668=CARTESIAN_POINT('Ctrl Pts',(6.6353576046144,4.30783572760024,25.5434384723009));
#71669=CARTESIAN_POINT('Ctrl Pts',(6.61420098189177,4.34024936928514,25.5449850999709));
#71670=CARTESIAN_POINT('Ctrl Pts',(6.51813209980344,4.48510075313238,25.5519166294206));
#71671=CARTESIAN_POINT('Ctrl Pts',(6.44058417768881,4.59576446092332,25.5572660407516));
#71672=CARTESIAN_POINT('Ctrl Pts',(6.13337057256121,5.0111110997588,25.5776164835313));
#71673=CARTESIAN_POINT('Ctrl Pts',(5.88460119207482,5.30103324847743,25.5924719500433));
#71674=CARTESIAN_POINT('Ctrl Pts',(5.22796585240134,5.9628550767811,25.6282232313017));
#71675=CARTESIAN_POINT('Ctrl Pts',(4.80028440682766,6.31225283562574,25.6486142711579));
#71676=CARTESIAN_POINT('Ctrl Pts',(4.05968869489079,6.7981672170229,25.6818946297322));
#71677=CARTESIAN_POINT('Ctrl Pts',(3.7682122321413,6.963957491497,25.6945983223048));
#71678=CARTESIAN_POINT('Ctrl Pts',(3.44501995440808,7.12154219710119,25.7089268363617));
#71679=CARTESIAN_POINT('Ctrl Pts',(3.42286582245018,7.13221671703125,25.7099102854397));
#71680=CARTESIAN_POINT('Ctrl Pts',(3.39129602995836,7.14724701208313,25.7113138881344));
#71681=CARTESIAN_POINT('Ctrl Pts',(3.38192091051453,7.15168788248264,25.71173098123));
#71682=CARTESIAN_POINT('Ctrl Pts',(3.36576229710609,7.15930312611876,25.7124503723698));
#71683=CARTESIAN_POINT('Ctrl Pts',(3.35898296806823,7.16248633590961,25.7127523447949));
#71684=CARTESIAN_POINT('Ctrl Pts',(3.34602781139467,7.16854694521082,25.7133297142549));
#71685=CARTESIAN_POINT('Ctrl Pts',(3.33985276539943,7.17142600362154,25.7136050488055));
#71686=CARTESIAN_POINT('Ctrl Pts',(3.32542838405404,7.17812856762465,25.7142485304757));
#71687=CARTESIAN_POINT('Ctrl Pts',(3.31717616987855,7.18194583159784,25.714616914209));
#71688=CARTESIAN_POINT('Ctrl Pts',(3.28881776321003,7.19500440455749,25.7158837459417));
#71689=CARTESIAN_POINT('Ctrl Pts',(3.26867949085281,7.20417552778718,25.7167849099572));
#71690=CARTESIAN_POINT('Ctrl Pts',(3.05438306416182,7.30068423842469,25.7263929948997));
#71691=CARTESIAN_POINT('Ctrl Pts',(2.85684972978158,7.38021924102636,25.7354619489356));
#71692=CARTESIAN_POINT('Ctrl Pts',(1.95177791181698,7.70285663117788,25.7777250487018));
#71693=CARTESIAN_POINT('Ctrl Pts',(1.21511682068751,7.85284145258832,25.8132825514916));
#71694=CARTESIAN_POINT('Ctrl Pts',(0.270104089451477,7.90887993498538,25.8546754203215));
#71695=CARTESIAN_POINT('Ctrl Pts',(0.0715352027644414,7.91316799886341,
25.8631696524825));
#71696=CARTESIAN_POINT('Ctrl Pts',(-0.233581190075055,7.90826937787337,
25.8758843356522));
#71697=CARTESIAN_POINT('Ctrl Pts',(-0.340125199037607,7.90440388130973,
25.8802614385258));
#71698=CARTESIAN_POINT('Ctrl Pts',(-0.464618989283191,7.89736521347536,
25.8853038913444));
#71699=CARTESIAN_POINT('Ctrl Pts',(-0.482673137310035,7.8962823384366,25.8860333809009));
#71700=CARTESIAN_POINT('Ctrl Pts',(-0.510240055474146,7.89453399606832,
25.8871445574995));
#71701=CARTESIAN_POINT('Ctrl Pts',(-0.519755542450827,7.89391323148379,
25.8875276226282));
#71702=CARTESIAN_POINT('Ctrl Pts',(-0.537059063589122,7.89275297383559,
25.8882233265403));
#71703=CARTESIAN_POINT('Ctrl Pts',(-0.544847458766876,7.89221915502193,
25.8885361401978));
#71704=CARTESIAN_POINT('Ctrl Pts',(-0.561631446853583,7.89104381242936,
25.8892095537734));
#71705=CARTESIAN_POINT('Ctrl Pts',(-0.570626763352512,7.89039843286804,
25.8895700339791));
#71706=CARTESIAN_POINT('Ctrl Pts',(-0.594882220657005,7.88861650140046,
25.8905408892103));
#71707=CARTESIAN_POINT('Ctrl Pts',(-0.610140234161235,7.88745104964955,
25.8911503685201));
#71708=CARTESIAN_POINT('Ctrl Pts',(-0.680635822924575,7.88186060744194,
25.8939606162287));
#71709=CARTESIAN_POINT('Ctrl Pts',(-0.735829935505321,7.87689953095941,
25.8961447212129));
#71710=CARTESIAN_POINT('Ctrl Pts',(-1.78588003306379,7.77138330028402,25.9374008925704));
#71711=CARTESIAN_POINT('Ctrl Pts',(-2.7526205253803,7.48374815716393,25.9688847971152));
#71712=CARTESIAN_POINT('Ctrl Pts',(-3.78194210678685,6.95027410426895,26.0100509519456));
#71713=CARTESIAN_POINT('Ctrl Pts',(-3.92138991922525,6.87256091035423,26.0158439381851));
#71714=CARTESIAN_POINT('Ctrl Pts',(-4.16382189973761,6.72767385463727,26.0264549272363));
#71715=CARTESIAN_POINT('Ctrl Pts',(-4.26777135806214,6.66221684887756,26.031188742951));
#71716=CARTESIAN_POINT('Ctrl Pts',(-4.38828534924573,6.58235110095856,26.0369437252511));
#71717=CARTESIAN_POINT('Ctrl Pts',(-4.40637065471377,6.57025813486448,26.0378145866603));
#71718=CARTESIAN_POINT('Ctrl Pts',(-4.43030877898876,6.55410831691033,26.0389771864212));
#71719=CARTESIAN_POINT('Ctrl Pts',(-4.43620647782245,6.55011784569408,26.0392644211135));
#71720=CARTESIAN_POINT('Ctrl Pts',(-4.44588536927462,6.54354989468009,26.0397371419005));
#71721=CARTESIAN_POINT('Ctrl Pts',(-4.44966973808012,6.54097708012681,26.0399223069392));
#71722=CARTESIAN_POINT('Ctrl Pts',(-4.45700080282973,6.53598372715914,26.0402816616937));
#71723=CARTESIAN_POINT('Ctrl Pts',(-4.46054776543342,6.53356358125187,26.0404558241495));
#71724=CARTESIAN_POINT('Ctrl Pts',(-4.46873435970091,6.52796797114192,26.0408584916684));
#71725=CARTESIAN_POINT('Ctrl Pts',(-4.47337257519347,6.52479044973977,26.0410871408061));
#71726=CARTESIAN_POINT('Ctrl Pts',(-4.48829626878186,6.51454322080528,26.0418244960686));
#71727=CARTESIAN_POINT('Ctrl Pts',(-4.49856820769432,6.50745425244984,26.042334577621));
#71728=CARTESIAN_POINT('Ctrl Pts',(-4.60315689471571,6.43490853250688,26.0475542894979));
#71729=CARTESIAN_POINT('Ctrl Pts',(-4.69605068602707,6.36743329219995,26.0524061847));
#71730=CARTESIAN_POINT('Ctrl Pts',(-5.4374867102003,5.80382581272292,26.092660597372));
#71731=CARTESIAN_POINT('Ctrl Pts',(-6.00714946539273,5.21201776450046,26.1326284383752));
#71732=CARTESIAN_POINT('Ctrl Pts',(-6.60671485938683,4.35739302211068,26.1788141193332));
#71733=CARTESIAN_POINT('Ctrl Pts',(-6.72914848508708,4.16582855848665,26.1885994188836));
#71734=CARTESIAN_POINT('Ctrl Pts',(-6.89543128386307,3.87914900211362,26.202400558143));
#71735=CARTESIAN_POINT('Ctrl Pts',(-6.94590735121461,3.78802611003953,26.2066698760701));
#71736=CARTESIAN_POINT('Ctrl Pts',(-7.00246025467444,3.68099939710884,26.2115512320661));
#71737=CARTESIAN_POINT('Ctrl Pts',(-7.01030200112158,3.66604310365004,26.2122303973224));
#71738=CARTESIAN_POINT('Ctrl Pts',(-7.02216380753612,3.64324225834743,26.2132612873442));
#71739=CARTESIAN_POINT('Ctrl Pts',(-7.0262187213448,3.6354159560361,26.2136143329046));
#71740=CARTESIAN_POINT('Ctrl Pts',(-7.03354861794924,3.62121060642831,26.2142536861538));
#71741=CARTESIAN_POINT('Ctrl Pts',(-7.03682802073475,3.61483385844223,26.214540160911));
#71742=CARTESIAN_POINT('Ctrl Pts',(-7.04336963570848,3.60207115378337,26.2151124684279));
#71743=CARTESIAN_POINT('Ctrl Pts',(-7.04663184402713,3.59568520274753,26.2153983008876));
#71744=CARTESIAN_POINT('Ctrl Pts',(-7.05579354022095,3.57769032873201,26.2162022629613));
#71745=CARTESIAN_POINT('Ctrl Pts',(-7.06167306730886,3.56607123641736,26.2167196394454));
#71746=CARTESIAN_POINT('Ctrl Pts',(-7.08577345631355,3.51815083593836,26.218846349131));
#71747=CARTESIAN_POINT('Ctrl Pts',(-7.10374346000765,3.48172366793042,26.2204462442268));
#71748=CARTESIAN_POINT('Ctrl Pts',(-7.39310689150369,2.88358526952599,26.2464485099742));
#71749=CARTESIAN_POINT('Ctrl Pts',(-7.5974179773813,2.29181619010096,26.2680574152853));
#71750=CARTESIAN_POINT('Ctrl Pts',(-7.81390931877673,1.29697653796323,26.3024931912484));
#71751=CARTESIAN_POINT('Ctrl Pts',(-7.86882056065629,0.906068509209754,
26.3156481182655));
#71752=CARTESIAN_POINT('Ctrl Pts',(-7.90556323740453,0.340339599843021,
26.3359660510946));
#71753=CARTESIAN_POINT('Ctrl Pts',(-7.91110921672639,0.167647964647231,
26.3423427371046));
#71754=CARTESIAN_POINT('Ctrl Pts',(-7.91095488487696,-0.0728388390359211,
26.351635775486));
#71755=CARTESIAN_POINT('Ctrl Pts',(-7.91004077470606,-0.140595545078708,
26.3542997823184));
#71756=CARTESIAN_POINT('Ctrl Pts',(-7.90797765089617,-0.21891214830021,
26.3574405856538));
#71757=CARTESIAN_POINT('Ctrl Pts',(-7.90767764832572,-0.229493493853941,
26.3578662402143));
#71758=CARTESIAN_POINT('Ctrl Pts',(-7.90720084075094,-0.245198172506846,
26.3584999647099));
#71759=CARTESIAN_POINT('Ctrl Pts',(-7.90704029201898,-0.250321992406321,
26.358707036841));
#71760=CARTESIAN_POINT('Ctrl Pts',(-7.9067443280252,-0.259483041069016,
26.3590778275356));
#71761=CARTESIAN_POINT('Ctrl Pts',(-7.90661080158455,-0.263520301882438,
26.3592414283301));
#71762=CARTESIAN_POINT('Ctrl Pts',(-7.90632170207179,-0.272063356188622,
26.3595880237614));
#71763=CARTESIAN_POINT('Ctrl Pts',(-7.90616536936308,-0.276569120736856,
26.3597710645546));
#71764=CARTESIAN_POINT('Ctrl Pts',(-7.90573976665904,-0.288540375032233,
26.360258014082));
#71765=CARTESIAN_POINT('Ctrl Pts',(-7.9054637743304,-0.296005604907943,
26.3605623280983));
#71766=CARTESIAN_POINT('Ctrl Pts',(-7.90414217693727,-0.330432228911968,
26.3619686816774));
#71767=CARTESIAN_POINT('Ctrl Pts',(-7.90296922761689,-0.357388252526246,
26.363078286255));
#71768=CARTESIAN_POINT('Ctrl Pts',(-7.89294376396666,-0.563503467131169,
26.3716243655331));
#71769=CARTESIAN_POINT('Ctrl Pts',(-7.87813841968225,-0.742309813567676,
26.3793939771249));
#71770=CARTESIAN_POINT('Ctrl Pts',(-7.83461280456575,-1.11386087706274,
26.3960620371927));
#71771=CARTESIAN_POINT('Ctrl Pts',(-7.80482193228937,-1.30636599472182,
26.4049941176159));
#71772=CARTESIAN_POINT('Ctrl Pts',(-7.6255875677926,-2.2360644086917,26.4489870421113));
#71773=CARTESIAN_POINT('Ctrl Pts',(-7.37858777193132,-2.95065617169274,
26.4849685297941));
#71774=CARTESIAN_POINT('Ctrl Pts',(-6.94056586629228,-3.80190626710509,
26.5261272453434));
#71775=CARTESIAN_POINT('Ctrl Pts',(-6.83971592156793,-3.98048246356251,
26.5346912163795));
#71776=CARTESIAN_POINT('Ctrl Pts',(-6.72000931531388,-4.17443651374091,
26.5439248243107));
#71777=CARTESIAN_POINT('Ctrl Pts',(-6.7078974000297,-4.19387146771705,26.5448493269086));
#71778=CARTESIAN_POINT('Ctrl Pts',(-6.69079612143912,-4.22104881343413,
26.5461411475077));
#71779=CARTESIAN_POINT('Ctrl Pts',(-6.68587742581563,-4.2288354037215,26.5465111541231));
#71780=CARTESIAN_POINT('Ctrl Pts',(-6.6768441846859,-4.24308041089931,26.5471878525473));
#71781=CARTESIAN_POINT('Ctrl Pts',(-6.67273384116231,-4.2495414723716,26.5474947040863));
#71782=CARTESIAN_POINT('Ctrl Pts',(-6.66440107022578,-4.26259788184021,
26.5481146339475));
#71783=CARTESIAN_POINT('Ctrl Pts',(-6.66017821767725,-4.26919294906439,
26.5484276955192));
#71784=CARTESIAN_POINT('Ctrl Pts',(-6.64978792483477,-4.28536711970946,
26.5491952813481));
#71785=CARTESIAN_POINT('Ctrl Pts',(-6.6436095626985,-4.29493920513681,26.5496493875526));
#71786=CARTESIAN_POINT('Ctrl Pts',(-6.62117757717204,-4.32952867388575,
26.5512897757357));
#71787=CARTESIAN_POINT('Ctrl Pts',(-6.60480305178352,-4.35446755861476,
26.5524714267361));
#71788=CARTESIAN_POINT('Ctrl Pts',(-6.37316371728363,-4.70294834648023,
26.5689699783768));
#71789=CARTESIAN_POINT('Ctrl Pts',(-6.13447511987585,-5.01030873932337,
26.583324661585));
#71790=CARTESIAN_POINT('Ctrl Pts',(-5.38878599826297,-5.83694910472618,
26.6228787741273));
#71791=CARTESIAN_POINT('Ctrl Pts',(-4.83187460590466,-6.3056919513229,26.6463418048821));
#71792=CARTESIAN_POINT('Ctrl Pts',(-4.11649365350646,-6.75670754013949,
26.6784377683842));
#71793=CARTESIAN_POINT('Ctrl Pts',(-4.01248728966773,-6.81898522664786,
26.683163292731));
#71794=CARTESIAN_POINT('Ctrl Pts',(-3.89224918264555,-6.88727874699043,
26.6886937144669));
#71795=CARTESIAN_POINT('Ctrl Pts',(-3.87738287971627,-6.8956590864508,26.6893785124154));
#71796=CARTESIAN_POINT('Ctrl Pts',(-3.85538512701272,-6.90796589415586,
26.6903931987763));
#71797=CARTESIAN_POINT('Ctrl Pts',(-3.84827448522773,-6.91192959730584,
26.6907214033687));
#71798=CARTESIAN_POINT('Ctrl Pts',(-3.83556976521688,-6.91898593973979,
26.6913081792572));
#71799=CARTESIAN_POINT('Ctrl Pts',(-3.82997802610118,-6.92208279186529,
26.691566563871));
#71800=CARTESIAN_POINT('Ctrl Pts',(-3.81826416955449,-6.92855169444655,
26.6921080975798));
#71801=CARTESIAN_POINT('Ctrl Pts',(-3.8121413260167,-6.93192241453992,26.6923913042075));
#71802=CARTESIAN_POINT('Ctrl Pts',(-3.79614147610415,-6.94070296981067,
26.6931317321994));
#71803=CARTESIAN_POINT('Ctrl Pts',(-3.78625739007331,-6.94609982624964,
26.6935895067553));
#71804=CARTESIAN_POINT('Ctrl Pts',(-3.74321334568618,-6.96948333467801,
26.6955845666008));
#71805=CARTESIAN_POINT('Ctrl Pts',(-3.70993679490908,-6.98725361093644,
26.6971307866421));
#71806=CARTESIAN_POINT('Ctrl Pts',(-3.45521964523936,-7.12094457416614,
26.7089900778491));
#71807=CARTESIAN_POINT('Ctrl Pts',(-3.22853244460029,-7.22654565123714,
26.7196761825378));
#71808=CARTESIAN_POINT('Ctrl Pts',(-2.5753882025136,-7.49393623537764,26.7502793793018));
#71809=CARTESIAN_POINT('Ctrl Pts',(-2.13939733916224,-7.62985577825859,
26.7704470921711));
#71810=CARTESIAN_POINT('Ctrl Pts',(-1.2745741393656,-7.81945412227201,26.8086540803558));
#71811=CARTESIAN_POINT('Ctrl Pts',(-0.848212687349006,-7.87711744554902,
26.8266892207419));
#71812=CARTESIAN_POINT('Ctrl Pts',(-0.380152875301321,-7.90195786298712,
26.8456919894774));
#71813=CARTESIAN_POINT('Ctrl Pts',(-0.341035719444665,-7.90374271743369,
26.8472745359449));
#71814=CARTESIAN_POINT('Ctrl Pts',(-0.28305752755332,-7.9059569471026,26.8496121382941));
#71815=CARTESIAN_POINT('Ctrl Pts',(-0.264205692785964,-7.90660939776337,
26.8503709543125));
#71816=CARTESIAN_POINT('Ctrl Pts',(-0.232050711490708,-7.9076071319199,
26.8516630767828));
#71817=CARTESIAN_POINT('Ctrl Pts',(-0.218748721954937,-7.90798628497822,
26.8521969747193));
#71818=CARTESIAN_POINT('Ctrl Pts',(-0.191557219965009,-7.90869267671559,
26.8532870577256));
#71819=CARTESIAN_POINT('Ctrl Pts',(-0.177667672550743,-7.90901689357426,
26.8538431872197));
#71820=CARTESIAN_POINT('Ctrl Pts',(-0.145734794371737,-7.90967812505064,
26.8551201738712));
#71821=CARTESIAN_POINT('Ctrl Pts',(-0.127691002476367,-7.90998999261756,
26.8558405748922));
#71822=CARTESIAN_POINT('Ctrl Pts',(-0.0715457219873636,-7.91076823951385,
26.8580785617733));
#71823=CARTESIAN_POINT('Ctrl Pts',(-0.0334416744985713,-7.91102108547707,
26.8595922215144));
#71824=CARTESIAN_POINT('Ctrl Pts',(0.586326756623952,-7.91065578024007,
26.8841284243866));
#71825=CARTESIAN_POINT('Ctrl Pts',(1.16618008228814,-7.84616678562703,26.9056770765643));
#71826=CARTESIAN_POINT('Ctrl Pts',(2.14257718764931,-7.62685101651237,26.9421203250294));
#71827=CARTESIAN_POINT('Ctrl Pts',(2.54344147141739,-7.5026904420863,26.9571931032407));
#71828=CARTESIAN_POINT('Ctrl Pts',(2.9512712745099,-7.33991311900215,26.9739988393092));
#71829=CARTESIAN_POINT('Ctrl Pts',(2.96995028088422,-7.33237492577289,26.9747719970411));
#71830=CARTESIAN_POINT('Ctrl Pts',(3.08735006738658,-7.28447427612128,26.9796541415517));
#71831=CARTESIAN_POINT('Ctrl Pts',(3.18527228683115,-7.24219131542487,26.9838276918068));
#71832=CARTESIAN_POINT('Ctrl Pts',(3.29619598237155,-7.19160942155647,26.9887023216859));
#71833=CARTESIAN_POINT('Ctrl Pts',(3.31006682856318,-7.18523566852529,26.9893145470748));
#71834=CARTESIAN_POINT('Ctrl Pts',(3.33043989449225,-7.17580258551042,26.9902177986928));
#71835=CARTESIAN_POINT('Ctrl Pts',(3.33695658599247,-7.17277445482206,26.9905073286058));
#71836=CARTESIAN_POINT('Ctrl Pts',(3.34854354544349,-7.1673710991995,26.9910232236695));
#71837=CARTESIAN_POINT('Ctrl Pts',(3.35361544072023,-7.16499935972748,26.9912494185789));
#71838=CARTESIAN_POINT('Ctrl Pts',(3.36418890859571,-7.16004126691194,26.9917217618622));
#71839=CARTESIAN_POINT('Ctrl Pts',(3.36969002466698,-7.1574539533237,26.9919679576968));
#71840=CARTESIAN_POINT('Ctrl Pts',(3.38396148675098,-7.15072162487563,26.992607834387));
#71841=CARTESIAN_POINT('Ctrl Pts',(3.39272718239887,-7.14656682364324,26.9930020068059));
#71842=CARTESIAN_POINT('Ctrl Pts',(3.43005914486989,-7.12878789923668,26.9946857422024));
#71843=CARTESIAN_POINT('Ctrl Pts',(3.45855102336243,-7.11500860502383,26.9959832928563));
#71844=CARTESIAN_POINT('Ctrl Pts',(3.66437279006198,-7.01394027753768,27.0054526731039));
#71845=CARTESIAN_POINT('Ctrl Pts',(3.83844834247212,-6.92020886319932,27.0139762750983));
#71846=CARTESIAN_POINT('Ctrl Pts',(4.52528286671108,-6.51648893309566,27.0492316629394));
#71847=CARTESIAN_POINT('Ctrl Pts',(5.005590012512,-6.1552339574266,27.0775318515316));
#71848=CARTESIAN_POINT('Ctrl Pts',(5.78600072616481,-5.41595592669741,27.1261681463026));
#71849=CARTESIAN_POINT('Ctrl Pts',(6.10127615309793,-5.05815265024049,27.1468686914432));
#71850=CARTESIAN_POINT('Ctrl Pts',(6.40111423180907,-4.64872559077335,27.1675295849248));
#71851=CARTESIAN_POINT('Ctrl Pts',(6.41957181548765,-4.62320351719952,27.1688062771329));
#71852=CARTESIAN_POINT('Ctrl Pts',(6.44447182745346,-4.58833658849288,27.1705353325365));
#71853=CARTESIAN_POINT('Ctrl Pts',(6.45104717048535,-4.57908726600077,27.170992573409));
#71854=CARTESIAN_POINT('Ctrl Pts',(6.46217047747764,-4.56336895839991,27.1717671866105));
#71855=CARTESIAN_POINT('Ctrl Pts',(6.46672867670651,-4.55690725742493,27.1720849333047));
#71856=CARTESIAN_POINT('Ctrl Pts',(6.47549969374818,-4.54443380464932,27.1726969708252));
#71857=CARTESIAN_POINT('Ctrl Pts',(6.47971384625439,-4.53842300359883,27.1729913102356));
#71858=CARTESIAN_POINT('Ctrl Pts',(6.48965299322679,-4.52420436885574,27.1736861754239));
#71859=CARTESIAN_POINT('Ctrl Pts',(6.49537079816818,-4.51599151226919,27.1740864390894));
#71860=CARTESIAN_POINT('Ctrl Pts',(6.51205040392488,-4.49193629480981,27.1752555997163));
#71861=CARTESIAN_POINT('Ctrl Pts',(6.52296997119519,-4.47606466678041,27.176022962576));
#71862=CARTESIAN_POINT('Ctrl Pts',(6.60256070058121,-4.35946947670472,27.1816307189061));
#71863=CARTESIAN_POINT('Ctrl Pts',(6.66895509352743,-4.25720817427779,27.1863884991745));
#71864=CARTESIAN_POINT('Ctrl Pts',(6.87725908736984,-3.9195364537011,27.2016145316846));
#71865=CARTESIAN_POINT('Ctrl Pts',(7.00927433155034,-3.67825305314022,27.2117419649909));
#71866=CARTESIAN_POINT('Ctrl Pts',(7.34363108223795,-2.98348588499039,27.2393666218784));
#71867=CARTESIAN_POINT('Ctrl Pts',(7.51625138875095,-2.51715483521127,27.2561246702818));
#71868=CARTESIAN_POINT('Ctrl Pts',(7.75124985886786,-1.63561426779284,27.2879858265191));
#71869=CARTESIAN_POINT('Ctrl Pts',(7.82654812954041,-1.22566580896864,27.3029281031745));
#71870=CARTESIAN_POINT('Ctrl Pts',(7.87201465904843,-0.784877867924856,
27.3205124360066));
#71871=CARTESIAN_POINT('Ctrl Pts',(7.87464410623256,-0.758042371290732,
27.3215880472976));
#71872=CARTESIAN_POINT('Ctrl Pts',(7.87810306337385,-0.720779113916123,
27.3230881917766));
#71873=CARTESIAN_POINT('Ctrl Pts',(7.87904918045207,-0.710362174464526,
27.3235082692306));
#71874=CARTESIAN_POINT('Ctrl Pts',(7.88053034281201,-0.693687224063578,
27.3241818193112));
#71875=CARTESIAN_POINT('Ctrl Pts',(7.88107860148629,-0.687430378834518,
27.324434801578));
#71876=CARTESIAN_POINT('Ctrl Pts',(7.8821931309302,-0.674534538549685,27.3249567243227));
#71877=CARTESIAN_POINT('Ctrl Pts',(7.88275846634275,-0.667895469320237,
27.3252256986466));
#71878=CARTESIAN_POINT('Ctrl Pts',(7.88405184871841,-0.65247610716855,27.3258510280238));
#71879=CARTESIAN_POINT('Ctrl Pts',(7.88477361616578,-0.643695304304122,
27.3262076072471));
#71880=CARTESIAN_POINT('Ctrl Pts',(7.88701594725224,-0.615846056928081,
27.3273400086753));
#71881=CARTESIAN_POINT('Ctrl Pts',(7.88848201236248,-0.596773366852653,
27.3281177278352));
#71882=CARTESIAN_POINT('Ctrl Pts',(7.91824595772938,-0.190272250907117,
27.3447377228723));
#71883=CARTESIAN_POINT('Ctrl Pts',(7.91803756237773,0.198702011401427,27.3614604442978));
#71884=CARTESIAN_POINT('Ctrl Pts',(7.86779346753827,0.875055143247997,27.390746074619));
#71885=CARTESIAN_POINT('Ctrl Pts',(7.83046276168631,1.16264920682545,27.403273493816));
#71886=CARTESIAN_POINT('Ctrl Pts',(7.66673512481276,2.04233063562632,27.4414812843643));
#71887=CARTESIAN_POINT('Ctrl Pts',(7.48816939195346,2.6224617220409,27.4663716334106));
#71888=CARTESIAN_POINT('Ctrl Pts',(7.20830468508872,3.26078498540832,27.4946869329944));
#71889=CARTESIAN_POINT('Ctrl Pts',(7.16991911557229,3.34434376269594,27.4984117712935));
#71890=CARTESIAN_POINT('Ctrl Pts',(7.11512265567787,3.45834404167846,27.5035185721234));
#71891=CARTESIAN_POINT('Ctrl Pts',(7.09995605531491,3.48937500690739,27.5049112384976));
#71892=CARTESIAN_POINT('Ctrl Pts',(7.07352213701872,3.54257305297703,27.5073032703575));
#71893=CARTESIAN_POINT('Ctrl Pts',(7.06235264134946,3.56478813280392,27.5083035274183));
#71894=CARTESIAN_POINT('Ctrl Pts',(7.04021607465496,3.60830328124302,27.5102655551532));
#71895=CARTESIAN_POINT('Ctrl Pts',(7.02925661297004,3.62960692361107,27.5112273877182));
#71896=CARTESIAN_POINT('Ctrl Pts',(7.00277848447357,3.68050692818033,27.5135285883812));
#71897=CARTESIAN_POINT('Ctrl Pts',(6.98716870822562,3.71005541790068,27.5148670302288));
#71898=CARTESIAN_POINT('Ctrl Pts',(6.95407896189088,3.77174299054988,27.5176667487735));
#71899=CARTESIAN_POINT('Ctrl Pts',(6.93656231989072,3.8038615367437,27.519127614949));
#71900=CARTESIAN_POINT('Ctrl Pts',(6.88953814026436,3.88868011972685,27.5229941422977));
#71901=CARTESIAN_POINT('Ctrl Pts',(6.85964873048598,3.94116584462289,27.5253956921561));
#71902=CARTESIAN_POINT('Ctrl Pts',(6.61559558811418,4.35853403788827,27.5445701313407));
#71903=CARTESIAN_POINT('Ctrl Pts',(6.37307310690725,4.70604659744921,27.5609746508008));
#71904=CARTESIAN_POINT('Ctrl Pts',(5.84569406806699,5.34570487104086,27.5930251169877));
#71905=CARTESIAN_POINT('Ctrl Pts',(5.56374962610629,5.63856108874527,27.6086357763255));
#71906=CARTESIAN_POINT('Ctrl Pts',(5.22824375308421,5.93727749384892,27.6265323920733));
#71907=CARTESIAN_POINT('Ctrl Pts',(5.195660901891,5.9658113049236,27.6282641942437));
#71908=CARTESIAN_POINT('Ctrl Pts',(5.15118902371042,6.00411603163212,27.6306210384783));
#71909=CARTESIAN_POINT('Ctrl Pts',(5.13950321394401,6.01412207980838,27.6312397082363));
#71910=CARTESIAN_POINT('Ctrl Pts',(5.11965295485321,6.03101888246819,27.6322896339148));
#71911=CARTESIAN_POINT('Ctrl Pts',(5.111503584499,6.03792731354662,27.6327203928369));
#71912=CARTESIAN_POINT('Ctrl Pts',(5.095770812557,6.05120971054573,27.6335514893774));
#71913=CARTESIAN_POINT('Ctrl Pts',(5.08818938170897,6.05758598373248,27.6339517595927));
#71914=CARTESIAN_POINT('Ctrl Pts',(5.0725899856437,6.07065572468458,27.6347749140902));
#71915=CARTESIAN_POINT('Ctrl Pts',(5.06457070269689,6.07734758646254,27.6351978443987));
#71916=CARTESIAN_POINT('Ctrl Pts',(5.04025274747567,6.09755866371282,27.6364796948681));
#71917=CARTESIAN_POINT('Ctrl Pts',(5.02391314593244,6.11102823648242,27.637340131315));
#71918=CARTESIAN_POINT('Ctrl Pts',(4.91169089049873,6.20278452641663,27.6432434062733));
#71919=CARTESIAN_POINT('Ctrl Pts',(4.81403784051086,6.27887584736698,27.6483483071909));
#71920=CARTESIAN_POINT('Ctrl Pts',(4.44698457214418,6.55128601602659,27.6673494806297));
#71921=CARTESIAN_POINT('Ctrl Pts',(4.16704309101618,6.7328128719612,27.681467129918));
#71922=CARTESIAN_POINT('Ctrl Pts',(3.49486788187357,7.11065919210472,27.7139452771799));
#71923=CARTESIAN_POINT('Ctrl Pts',(3.0960837087615,7.29313848138394,27.7321690558418));
#71924=CARTESIAN_POINT('Ctrl Pts',(2.64101898084673,7.45728174067475,27.7518004601329));
#71925=CARTESIAN_POINT('Ctrl Pts',(2.59766161522202,7.47249532521434,27.7536602150912));
#71926=CARTESIAN_POINT('Ctrl Pts',(2.52773453797921,7.49634974497479,27.7566430681176));
#71927=CARTESIAN_POINT('Ctrl Pts',(2.50124743346664,7.50522902234875,27.7577691215931));
#71928=CARTESIAN_POINT('Ctrl Pts',(2.4544968154364,7.5206262667146,27.7597501206918));
#71929=CARTESIAN_POINT('Ctrl Pts',(2.43425301666154,7.52720308712821,27.7606057812059));
#71930=CARTESIAN_POINT('Ctrl Pts',(2.41387195962422,7.5337336809916,27.7614651323739));
#71931=CARTESIAN_POINT('Ctrl Pts',(2.41376107979313,7.53376920692567,27.7614698074712));
#71932=CARTESIAN_POINT('Ctrl Pts',(2.41354279685651,7.53383913953905,27.7614790109518));
#71933=CARTESIAN_POINT('Ctrl Pts',(2.41343539770515,7.53387354511677,27.7614835391717));
#71934=CARTESIAN_POINT('Ctrl Pts',(2.41322400948941,7.53394125885882,27.761492451718));
#71935=CARTESIAN_POINT('Ctrl Pts',(2.41311996890431,7.53397458368491,27.7614968382206));
#71936=CARTESIAN_POINT('Ctrl Pts',(2.41291516925222,7.5340401775665,27.7615054727627));
#71937=CARTESIAN_POINT('Ctrl Pts',(2.41281441009642,7.53407244679959,27.7615097208098));
#71938=CARTESIAN_POINT('Ctrl Pts',(2.41261604714609,7.53413597033904,27.7615180837707));
#71939=CARTESIAN_POINT('Ctrl Pts',(2.41251844356679,7.53416722471391,27.7615221986787));
#71940=CARTESIAN_POINT('Ctrl Pts',(2.41232628704227,7.53422875248035,27.7615302997861));
#71941=CARTESIAN_POINT('Ctrl Pts',(2.41223173403143,7.53425902602164,27.7615342859913));
#71942=CARTESIAN_POINT('Ctrl Pts',(2.41206413926481,7.53431268225275,27.7615413514405));
#71943=CARTESIAN_POINT('Ctrl Pts',(2.41199111416306,7.53433606040207,27.7615444300006));
#71944=CARTESIAN_POINT('Ctrl Pts',(2.41184560964406,7.53438263967457,27.7615505640623));
#71945=CARTESIAN_POINT('Ctrl Pts',(2.4117731312072,7.534405840501,27.7615536195227));
#71946=CARTESIAN_POINT('Ctrl Pts',(2.41162872010481,7.5344520651516,27.7615597073823));
#71947=CARTESIAN_POINT('Ctrl Pts',(2.41155678815637,7.53447508876354,27.7615627397516));
#71948=CARTESIAN_POINT('Ctrl Pts',(2.41141346480107,7.53452096071091,27.7615687816505));
#71949=CARTESIAN_POINT('Ctrl Pts',(2.4113420743052,7.53454380877178,27.7615717911421));
#71950=CARTESIAN_POINT('Ctrl Pts',(2.41119982871127,7.53458933131424,27.7615777875037));
#71951=CARTESIAN_POINT('Ctrl Pts',(2.41112897444595,7.53461200554604,27.761580774339));
#71952=CARTESIAN_POINT('Ctrl Pts',(2.41098779612116,7.53465718214196,27.7615867256079));
#71953=CARTESIAN_POINT('Ctrl Pts',(2.41091747310987,7.5346796841871,27.7615896899978));
#71954=CARTESIAN_POINT('Ctrl Pts',(2.41077735230251,7.53472451805588,27.7615955965875));
#71955=CARTESIAN_POINT('Ctrl Pts',(2.41070755540548,7.53474684960801,27.7615985387497));
#71956=CARTESIAN_POINT('Ctrl Pts',(2.41056848181816,7.53479134414165,27.7616044010965));
#71957=CARTESIAN_POINT('Ctrl Pts',(2.41049920617094,7.53481350680533,27.7616073212373));
#71958=CARTESIAN_POINT('Ctrl Pts',(2.41036117026654,7.53485766515065,27.7616131397453));
#71959=CARTESIAN_POINT('Ctrl Pts',(2.41029241084389,7.53487966058094,27.7616160380777));
#71960=CARTESIAN_POINT('Ctrl Pts',(2.41015540235864,7.53492348611532,27.7616218131818));
#71961=CARTESIAN_POINT('Ctrl Pts',(2.41008715450086,7.53494531584937,27.7616246899032));
#71962=CARTESIAN_POINT('Ctrl Pts',(2.40995116431534,7.53498881158225,27.76163042199));
#71963=CARTESIAN_POINT('Ctrl Pts',(2.40988342305291,7.53501047725542,27.7616332773109));
#71964=CARTESIAN_POINT('Ctrl Pts',(2.40974844132029,7.53505364642708,27.7616389667975));
#71965=CARTESIAN_POINT('Ctrl Pts',(2.40968120197208,7.53507514958157,27.7616418009163));
#71966=CARTESIAN_POINT('Ctrl Pts',(2.40954721931298,7.53511799528097,27.7616474482002));
#71967=CARTESIAN_POINT('Ctrl Pts',(2.4094804771886,7.53513933746103,27.7616502613156));
#71968=CARTESIAN_POINT('Ctrl Pts',(2.40934748432725,7.53518186274223,27.7616558667898));
#71969=CARTESIAN_POINT('Ctrl Pts',(2.40928123475648,7.5352030454848,27.7616586590997));
#71970=CARTESIAN_POINT('Ctrl Pts',(2.40914922245572,7.53524525338779,27.7616642231555));
#71971=CARTESIAN_POINT('Ctrl Pts',(2.40908346083661,7.53526627820712,27.7616669948548));
#71972=CARTESIAN_POINT('Ctrl Pts',(2.40895241984852,7.53530817177361,27.761672517884));
#71973=CARTESIAN_POINT('Ctrl Pts',(2.40888714169459,7.53532904014618,27.7616752691629));
#71974=CARTESIAN_POINT('Ctrl Pts',(2.40875706307799,7.53537062231813,27.7616807515442));
#71975=CARTESIAN_POINT('Ctrl Pts',(2.4086922638823,7.53539133572613,27.7616834825935));
#71976=CARTESIAN_POINT('Ctrl Pts',(2.38653437342672,7.54247390840601,27.7626173494076));
#71977=CARTESIAN_POINT('Ctrl Pts',(2.36441028851278,7.54943858617563,27.7635473069478));
#71978=CARTESIAN_POINT('Ctrl Pts',(2.3057135131476,7.5676330409355,27.7660081373301));
#71979=CARTESIAN_POINT('Ctrl Pts',(2.26908937636123,7.57869501086796,27.7675370059045));
#71980=CARTESIAN_POINT('Ctrl Pts',(2.18800566083259,7.60254511881239,27.7709079917402));
#71981=CARTESIAN_POINT('Ctrl Pts',(2.14351119295588,7.61520983638117,27.7727486686793));
#71982=CARTESIAN_POINT('Ctrl Pts',(2.0090515927684,7.6522100255411,27.7782853861594));
#71983=CARTESIAN_POINT('Ctrl Pts',(1.91876469890791,7.67534682114395,27.7819685960052));
#71984=CARTESIAN_POINT('Ctrl Pts',(1.56587088631675,7.75916276083621,27.7962530929716));
#71985=CARTESIAN_POINT('Ctrl Pts',(1.30063353999508,7.80800328896239,27.8067786896681));
#71986=CARTESIAN_POINT('Ctrl Pts',(0.678545703696835,7.88996956763789,27.8310670562652));
#71987=CARTESIAN_POINT('Ctrl Pts',(0.320900900958636,7.91258977232274,27.8446775408132));
#71988=CARTESIAN_POINT('Ctrl Pts',(-0.610028097376528,7.90822958728728,
27.8796771442475));
#71989=CARTESIAN_POINT('Ctrl Pts',(-1.18098042953533,7.84330529232685,27.900633179886));
#71990=CARTESIAN_POINT('Ctrl Pts',(-1.75903284846369,7.71298323588363,27.923847265959));
#71991=CARTESIAN_POINT('Ctrl Pts',(-1.77818143760208,7.7085911636356,27.9246187549463));
#71992=CARTESIAN_POINT('Ctrl Pts',(-1.82791316106835,7.69698913746483,27.9266292755805));
#71993=CARTESIAN_POINT('Ctrl Pts',(-1.85846992711701,7.68966825100608,27.9278713497798));
#71994=CARTESIAN_POINT('Ctrl Pts',(-1.9213884683283,7.67419709322354,27.9304439553221));
#71995=CARTESIAN_POINT('Ctrl Pts',(-1.95374388393988,7.66602370680407,27.9317751645656));
#71996=CARTESIAN_POINT('Ctrl Pts',(-1.99778133478408,7.6546023875245,27.9335992328));
#71997=CARTESIAN_POINT('Ctrl Pts',(-2.00950926511531,7.65153190441981,27.9340861987137));
#71998=CARTESIAN_POINT('Ctrl Pts',(-2.0280649634662,7.6466282427248,27.9348585967848));
#71999=CARTESIAN_POINT('Ctrl Pts',(-2.03489743565709,7.6448128429998,27.9351434196245));
#72000=CARTESIAN_POINT('Ctrl Pts',(-2.04811319234573,7.64128242109991,27.935695156109));
#72001=CARTESIAN_POINT('Ctrl Pts',(-2.05449677989012,7.639568552528,27.9359620293122));
#72002=CARTESIAN_POINT('Ctrl Pts',(-2.06964832810854,7.63548029353204,27.9365963459412));
#72003=CARTESIAN_POINT('Ctrl Pts',(-2.07841435164152,7.63309880042477,27.9369640410639));
#72004=CARTESIAN_POINT('Ctrl Pts',(-2.1043069575169,7.62601656473729,27.9380522520825));
#72005=CARTESIAN_POINT('Ctrl Pts',(-2.12142177177624,7.62127325826567,27.9387743116736));
#72006=CARTESIAN_POINT('Ctrl Pts',(-2.2597644476746,7.58242999626432,27.9446340948373));
#72007=CARTESIAN_POINT('Ctrl Pts',(-2.38016438947108,7.54550176332656,27.9498832347025));
#72008=CARTESIAN_POINT('Ctrl Pts',(-2.640698181632,7.45873564586007,27.9616174203887));
#72009=CARTESIAN_POINT('Ctrl Pts',(-2.78039584289463,7.40779453023576,27.9681359323521));
#72010=CARTESIAN_POINT('Ctrl Pts',(-3.09682941297819,7.2821941488284,27.9833048501267));
#72011=CARTESIAN_POINT('Ctrl Pts',(-3.27245325530868,7.2049809219385,27.9920195523561));
#72012=CARTESIAN_POINT('Ctrl Pts',(-3.61536808775942,7.0390918117813,28.0094330581364));
#72013=CARTESIAN_POINT('Ctrl Pts',(-3.78263441217647,6.95063861221565,28.0181248111665));
#72014=CARTESIAN_POINT('Ctrl Pts',(-4.4573263159712,6.56227634423336,28.0536943887056));
#72015=CARTESIAN_POINT('Ctrl Pts',(-4.93369485062658,6.21209029757279,28.0798603743371));
#72016=CARTESIAN_POINT('Ctrl Pts',(-5.39382914491411,5.78721720954648,28.1053893570867));
#72017=CARTESIAN_POINT('Ctrl Pts',(-5.42069795320241,5.76205775936328,28.1068818759532));
#72018=CARTESIAN_POINT('Ctrl Pts',(-5.45693447104418,5.72764876718623,28.1088973339125));
#72019=CARTESIAN_POINT('Ctrl Pts',(-5.466455915722,5.71856222709284,28.1094271568823));
#72020=CARTESIAN_POINT('Ctrl Pts',(-5.48144378012906,5.70418731563782,28.1102615556022));
#72021=CARTESIAN_POINT('Ctrl Pts',(-5.48692530482257,5.69891476917314,28.1105668049021));
#72022=CARTESIAN_POINT('Ctrl Pts',(-5.49748538664941,5.68872792153926,28.1111550277991));
#72023=CARTESIAN_POINT('Ctrl Pts',(-5.50256497797338,5.68381470539292,28.1114380473471));
#72024=CARTESIAN_POINT('Ctrl Pts',(-5.51456041234048,5.67218101367929,28.1121065734927));
#72025=CARTESIAN_POINT('Ctrl Pts',(-5.52147057140741,5.66545467930172,28.112491827781));
#72026=CARTESIAN_POINT('Ctrl Pts',(-5.54167072923172,5.64571982770468,28.1136184404968));
#72027=CARTESIAN_POINT('Ctrl Pts',(-5.55492721844101,5.63267702322526,28.1143583169358));
#72028=CARTESIAN_POINT('Ctrl Pts',(-5.65237284011208,5.53612356066904,28.1198010591183));
#72029=CARTESIAN_POINT('Ctrl Pts',(-5.734722754409,5.45077418613406,28.1244228233983));
#72030=CARTESIAN_POINT('Ctrl Pts',(-6.03296525320804,5.12742487426509,28.1412735924021));
#72031=CARTESIAN_POINT('Ctrl Pts',(-6.23622395794494,4.87818493035999,28.1529707174204));
#72032=CARTESIAN_POINT('Ctrl Pts',(-6.4855866561619,4.53125853418781,28.1680159066556));
#72033=CARTESIAN_POINT('Ctrl Pts',(-6.54566914125742,4.44402454730085,28.1717041496508));
#72034=CARTESIAN_POINT('Ctrl Pts',(-6.66328984415847,4.26568783480336,28.1790864355487));
#72035=CARTESIAN_POINT('Ctrl Pts',(-6.72075463821378,4.17456364898016,28.182778718532));
#72036=CARTESIAN_POINT('Ctrl Pts',(-7.09225404166409,3.55789891216932,28.2073618737278));
#72037=CARTESIAN_POINT('Ctrl Pts',(-7.3461939045247,2.99866356383236,28.2276039530862));
#72038=CARTESIAN_POINT('Ctrl Pts',(-7.5570054777368,2.34130619710707,28.2542257774296));
#72039=CARTESIAN_POINT('Ctrl Pts',(-7.57979793510687,2.26643090042485,28.2572991335334));
#72040=CARTESIAN_POINT('Ctrl Pts',(-7.60469059143986,2.18007724130886,28.2609024469297));
#72041=CARTESIAN_POINT('Ctrl Pts',(-7.60788155081493,2.1689154146039,28.261369322989));
#72042=CARTESIAN_POINT('Ctrl Pts',(-7.61254159247629,2.15247798892071,28.2620585665311));
#72043=CARTESIAN_POINT('Ctrl Pts',(-7.61402979607196,2.14720778086619,28.2622798104047));
#72044=CARTESIAN_POINT('Ctrl Pts',(-7.61666889814576,2.13782462727274,28.2626741795955));
#72045=CARTESIAN_POINT('Ctrl Pts',(-7.61782194185423,2.13371228215564,28.2628471777023));
#72046=CARTESIAN_POINT('Ctrl Pts',(-7.62022077929459,2.12513006815882,28.2632085479972));
#72047=CARTESIAN_POINT('Ctrl Pts',(-7.62146597121516,2.12066003433308,28.2633969559858));
#72048=CARTESIAN_POINT('Ctrl Pts',(-7.62468914498746,2.10904986578274,28.263886810072));
#72049=CARTESIAN_POINT('Ctrl Pts',(-7.6266610262553,2.10190805791161,28.264188622482));
#72050=CARTESIAN_POINT('Ctrl Pts',(-7.63529858816319,2.0704521432846,28.2655201277558));
#72051=CARTESIAN_POINT('Ctrl Pts',(-7.64185794446066,2.04610941125025,28.2665562984237));
#72052=CARTESIAN_POINT('Ctrl Pts',(-7.68959802676401,1.86550695766192,28.2742840129058));
#72053=CARTESIAN_POINT('Ctrl Pts',(-7.72609642892959,1.70805789823672,28.2812430857041));
#72054=CARTESIAN_POINT('Ctrl Pts',(-7.85916345205061,1.0418910141892,28.3112600394506));
#72055=CARTESIAN_POINT('Ctrl Pts',(-7.9104895321659,0.525463859223298,28.3358246275417));
#72056=CARTESIAN_POINT('Ctrl Pts',(-7.91099621143461,0.00774226499310415,
28.3596644754603));
#72057=CARTESIAN_POINT('',(-7.911,-2.37587727269783E-12,30.3576684917631));
#72058=CARTESIAN_POINT('Ctrl Pts',(-7.911,-2.54574139546548E-12,28.3576684917631));
#72059=CARTESIAN_POINT('Ctrl Pts',(-7.91099999999929,-2.20167589666934,
28.4462559274958));
#72060=CARTESIAN_POINT('Ctrl Pts',(-6.94214576672227,-4.38610418338912,
28.5348433632286));
#72061=CARTESIAN_POINT('Ctrl Pts',(-3.67820201488039,-7.34180684107757,
28.712018234694));
#72062=CARTESIAN_POINT('Ctrl Pts',(-1.40868175871468,-8.08992666571385,
28.8006056704267));
#72063=CARTESIAN_POINT('Ctrl Pts',(2.9730927052154,-7.65454228025154,28.9777805418922));
#72064=CARTESIAN_POINT('Ctrl Pts',(5.05102072675831,-6.47444880834048,29.0663679776249));
#72065=CARTESIAN_POINT('Ctrl Pts',(7.66951518847978,-2.93425195367432,29.2435428490904));
#72066=CARTESIAN_POINT('Ctrl Pts',(8.18956872247094,-0.601881960096201,
29.3321302848231));
#72067=CARTESIAN_POINT('Ctrl Pts',(7.32306689761206,3.7153719823272,29.5093051562886));
#72068=CARTESIAN_POINT('Ctrl Pts',(5.94329958849991,5.66643518936733,29.5978925920213));
#72069=CARTESIAN_POINT('Ctrl Pts',(2.16154501637547,7.9220591323308,29.7750674634867));
#72070=CARTESIAN_POINT('Ctrl Pts',(-0.210816529303517,8.20894963712995,
29.8636548992195));
#72071=CARTESIAN_POINT('Ctrl Pts',(-4.42123908576708,6.91982244717659,30.0408297706849));
#72072=CARTESIAN_POINT('Ctrl Pts',(-6.226316256344,5.35390358803276,30.1294172064176));
#72073=CARTESIAN_POINT('Ctrl Pts',(-7.65317280859569,2.31334857514238,30.264559258688));
#72074=CARTESIAN_POINT('Ctrl Pts',(-7.91100000000035,1.15702837836256,30.3111138752255));
#72075=CARTESIAN_POINT('Ctrl Pts',(-7.911,-2.37587727269783E-12,30.3576684917631));
#72076=CARTESIAN_POINT('',(-7.91024367631032,0.00400354093750647,34.3576684917631));
#72077=CARTESIAN_POINT('Ctrl Pts',(-7.91099920125805,-0.00355495352692831,
30.3653171807264));
#72078=CARTESIAN_POINT('Ctrl Pts',(-7.91060312412407,-0.884963350813036,
30.3979267782199));
#72079=CARTESIAN_POINT('Ctrl Pts',(-7.76292703746049,-1.76000380474951,
30.4255138963057));
#72080=CARTESIAN_POINT('Ctrl Pts',(-7.42189359812388,-2.74313434757834,
30.463310969466));
#72081=CARTESIAN_POINT('Ctrl Pts',(-7.3651632720638,-2.89199859532217,30.4692547066593));
#72082=CARTESIAN_POINT('Ctrl Pts',(-7.27814038175919,-3.1011479366229,30.4780455188782));
#72083=CARTESIAN_POINT('Ctrl Pts',(-7.2515088280524,-3.16292035659979,30.4806977990225));
#72084=CARTESIAN_POINT('Ctrl Pts',(-7.21993112783547,-3.23366971154254,
30.4838078375857));
#72085=CARTESIAN_POINT('Ctrl Pts',(-7.21575073109272,-3.24298730786078,
30.4842188811017));
#72086=CARTESIAN_POINT('Ctrl Pts',(-7.20939252565837,-3.25708581571384,
30.4848430744588));
#72087=CARTESIAN_POINT('Ctrl Pts',(-7.2072279639431,-3.26187272520651,30.4850554007007));
#72088=CARTESIAN_POINT('Ctrl Pts',(-7.20347653105907,-3.27014702216382,
30.4854230956453));
#72089=CARTESIAN_POINT('Ctrl Pts',(-7.20189188935338,-3.27363542473126,
30.485578324346));
#72090=CARTESIAN_POINT('Ctrl Pts',(-7.19860399699981,-3.28085939197745,
30.485900218467));
#72091=CARTESIAN_POINT('Ctrl Pts',(-7.19690037164981,-3.28459478413672,
30.486066907572));
#72092=CARTESIAN_POINT('Ctrl Pts',(-7.19276087050353,-3.29365242848827,
30.4864716916494));
#72093=CARTESIAN_POINT('Ctrl Pts',(-7.19032199768044,-3.29897329926115,
30.4867099775843));
#72094=CARTESIAN_POINT('Ctrl Pts',(-7.181043549368,-3.31915685402946,30.4876157681417));
#72095=CARTESIAN_POINT('Ctrl Pts',(-7.17416390688409,-3.33400073494111,
30.4882858742115));
#72096=CARTESIAN_POINT('Ctrl Pts',(-7.05147293841193,-3.59658714502922,
30.50020870706));
#72097=CARTESIAN_POINT('Ctrl Pts',(-6.92294710521461,-3.83816193688928,
30.5122567648152));
#72098=CARTESIAN_POINT('Ctrl Pts',(-6.69062791188648,-4.22505042662448,
30.5327246761899));
#72099=CARTESIAN_POINT('Ctrl Pts',(-6.59395503197211,-4.3743922075168,30.5409362172563));
#72100=CARTESIAN_POINT('Ctrl Pts',(-6.25394976808366,-4.86272386638663,
30.5685435971015));
#72101=CARTESIAN_POINT('Ctrl Pts',(-5.9888401199099,-5.18573073278105,30.5880340152787));
#72102=CARTESIAN_POINT('Ctrl Pts',(-5.46211515191264,-5.73291971264871,
30.6220384897984));
#72103=CARTESIAN_POINT('Ctrl Pts',(-5.20897968555213,-5.9638612999378,30.6367919632479));
#72104=CARTESIAN_POINT('Ctrl Pts',(-4.9156159914246,-6.19852823031809,30.6521557821943));
#72105=CARTESIAN_POINT('Ctrl Pts',(-4.88944631697091,-6.21919187266309,
30.6535123647288));
#72106=CARTESIAN_POINT('Ctrl Pts',(-4.85000181318907,-6.24993449193625,
30.655536371107));
#72107=CARTESIAN_POINT('Ctrl Pts',(-4.83682467927748,-6.26013783938651,
30.6562090932728));
#72108=CARTESIAN_POINT('Ctrl Pts',(-4.81558327261646,-6.27647842644345,
30.657288026596));
#72109=CARTESIAN_POINT('Ctrl Pts',(-4.80753931514613,-6.28264191463366,
30.6576953516203));
#72110=CARTESIAN_POINT('Ctrl Pts',(-4.7921505523098,-6.29438632241335,30.6584722030826));
#72111=CARTESIAN_POINT('Ctrl Pts',(-4.78480778885031,-6.29996988217775,
30.6588418410599));
#72112=CARTESIAN_POINT('Ctrl Pts',(-4.77179391518922,-6.30982997239186,
30.6594951356247));
#72113=CARTESIAN_POINT('Ctrl Pts',(-4.7661267875593,-6.31411172650571,30.6597790125707));
#72114=CARTESIAN_POINT('Ctrl Pts',(-4.75496090660317,-6.32252442283372,
30.6603371311269));
#72115=CARTESIAN_POINT('Ctrl Pts',(-4.74946251900478,-6.32665583713298,
30.6606113925113));
#72116=CARTESIAN_POINT('Ctrl Pts',(-4.73625625671035,-6.33655192618142,
30.6612687577214));
#72117=CARTESIAN_POINT('Ctrl Pts',(-4.72854322573208,-6.34230972168188,
30.6616515724326));
#72118=CARTESIAN_POINT('Ctrl Pts',(-4.70054433966655,-6.36313148914015,
30.6630371933592));
#72119=CARTESIAN_POINT('Ctrl Pts',(-4.68019674598859,-6.37811240668014,
30.6640365212823));
#72120=CARTESIAN_POINT('Ctrl Pts',(-4.35089928347479,-6.61813336331553,
30.6800874699453));
#72121=CARTESIAN_POINT('Ctrl Pts',(-4.02609970597036,-6.82059945136334,
30.6941588217865));
#72122=CARTESIAN_POINT('Ctrl Pts',(-3.50426161557939,-7.09557323358911,
30.7149094042061));
#72123=CARTESIAN_POINT('Ctrl Pts',(-3.31687961446773,-7.18507633364875,
30.7220279541172));
#72124=CARTESIAN_POINT('Ctrl Pts',(-2.7866794233017,-7.41315979245692,30.7416262099554));
#72125=CARTESIAN_POINT('Ctrl Pts',(-2.43736177314507,-7.53523537258662,
30.7539137988252));
#72126=CARTESIAN_POINT('Ctrl Pts',(-1.77539942391532,-7.71570356526808,
30.7779107272071));
#72127=CARTESIAN_POINT('Ctrl Pts',(-1.46530143179927,-7.78055123014887,
30.7894383335952));
#72128=CARTESIAN_POINT('Ctrl Pts',(-1.14011820973023,-7.82842259364277,
30.8025971405579));
#72129=CARTESIAN_POINT('Ctrl Pts',(-1.12804440008767,-7.83017149651902,
30.8030872413475));
#72130=CARTESIAN_POINT('Ctrl Pts',(-1.11059275765077,-7.83265818173073,
30.803797905035));
#72131=CARTESIAN_POINT('Ctrl Pts',(-1.10521811742434,-7.83341837118187,
30.8040170814458));
#72132=CARTESIAN_POINT('Ctrl Pts',(-1.09580323035483,-7.83474013091302,
30.8044015653175));
#72133=CARTESIAN_POINT('Ctrl Pts',(-1.0917633699312,-7.83530410274844,30.804566720435));
#72134=CARTESIAN_POINT('Ctrl Pts',(-1.08392166453407,-7.83639263656369,
30.8048876390319));
#72135=CARTESIAN_POINT('Ctrl Pts',(-1.08011986964507,-7.83691755707138,
30.8050433804356));
#72136=CARTESIAN_POINT('Ctrl Pts',(-1.07104908786558,-7.83816324996986,
30.8054153330873));
#72137=CARTESIAN_POINT('Ctrl Pts',(-1.06577975970749,-7.83888147539604,
30.8056316994712));
#72138=CARTESIAN_POINT('Ctrl Pts',(-1.04986684595157,-7.84103411224908,
30.8062859877939));
#72139=CARTESIAN_POINT('Ctrl Pts',(-1.03922109876303,-7.84245215792203,
30.8067248962862));
#72140=CARTESIAN_POINT('Ctrl Pts',(-0.932363279012059,-7.85646454226463,
30.8111421826469));
#72141=CARTESIAN_POINT('Ctrl Pts',(-0.83593389435246,-7.86730890289019,
30.8152234589616));
#72142=CARTESIAN_POINT('Ctrl Pts',(-0.589066249673858,-7.8904816816879,
30.825870624684));
#72143=CARTESIAN_POINT('Ctrl Pts',(-0.438433075831382,-7.90028304646046,
30.8325548575094));
#72144=CARTESIAN_POINT('Ctrl Pts',(0.472141298527506,-7.93341064097906,
30.8737208893049));
#72145=CARTESIAN_POINT('Ctrl Pts',(1.23195256747041,-7.85139931491644,30.910799115841));
#72146=CARTESIAN_POINT('Ctrl Pts',(2.20185962885061,-7.60222349820075,30.9553548133858));
#72147=CARTESIAN_POINT('Ctrl Pts',(2.43240155306293,-7.53162827794695,30.9657728874423));
#72148=CARTESIAN_POINT('Ctrl Pts',(2.72732737222575,-7.42635927286325,30.9788503146075));
#72149=CARTESIAN_POINT('Ctrl Pts',(2.79494487333692,-7.40117627003489,30.9818315289005));
#72150=CARTESIAN_POINT('Ctrl Pts',(2.89011392967679,-7.36424187520213,30.9860043232094));
#72151=CARTESIAN_POINT('Ctrl Pts',(2.91795668595226,-7.35325409113056,30.9872222962018));
#72152=CARTESIAN_POINT('Ctrl Pts',(2.96019326116399,-7.33630830137857,30.9890657459639));
#72153=CARTESIAN_POINT('Ctrl Pts',(2.97463279217727,-7.33046542804557,30.9896952257405));
#72154=CARTESIAN_POINT('Ctrl Pts',(3.00112624968517,-7.31965383158318,30.9908488408604));
#72155=CARTESIAN_POINT('Ctrl Pts',(3.01318531350744,-7.31469789187549,30.9913734195874));
#72156=CARTESIAN_POINT('Ctrl Pts',(3.03279621646187,-7.30658163064384,30.9922256858691));
#72157=CARTESIAN_POINT('Ctrl Pts',(3.04035547449334,-7.30343936820892,30.9925540025439));
#72158=CARTESIAN_POINT('Ctrl Pts',(3.05484172840246,-7.29739127641125,30.9931827965578));
#72159=CARTESIAN_POINT('Ctrl Pts',(3.06176948716682,-7.29448730443067,30.9934833382366));
#72160=CARTESIAN_POINT('Ctrl Pts',(3.07749529313766,-7.28786902475474,30.9941651848802));
#72161=CARTESIAN_POINT('Ctrl Pts',(3.08629077944693,-7.28414864118051,30.9945462772635));
#72162=CARTESIAN_POINT('Ctrl Pts',(3.10895269339301,-7.27451451295729,30.9955274994458));
#72163=CARTESIAN_POINT('Ctrl Pts',(3.12280902241621,-7.26857703142814,30.9961267998536));
#72164=CARTESIAN_POINT('Ctrl Pts',(3.20463617693524,-7.23323665602835,30.999662125855));
#72165=CARTESIAN_POINT('Ctrl Pts',(3.27220943062045,-7.20291964207612,31.0025661082263));
#72166=CARTESIAN_POINT('Ctrl Pts',(3.84491603132704,-6.93624952811896,31.027064766771));
#72167=CARTESIAN_POINT('Ctrl Pts',(4.32419932658879,-6.64802971885325,31.0466563131154));
#72168=CARTESIAN_POINT('Ctrl Pts',(5.06994459708018,-6.08454387233539,31.0789532875692));
#72169=CARTESIAN_POINT('Ctrl Pts',(5.35405536947215,-5.83610152476604,31.0918362443326));
#72170=CARTESIAN_POINT('Ctrl Pts',(5.73842597110009,-5.44821092649485,31.1116499078771));
#72171=CARTESIAN_POINT('Ctrl Pts',(5.8536015138051,-5.32427262605735,31.1179455178552));
#72172=CARTESIAN_POINT('Ctrl Pts',(6.01711679478501,-5.13659332998736,31.1275841946935));
#72173=CARTESIAN_POINT('Ctrl Pts',(6.06860768793099,-5.07565612653685,31.1307307844488));
#72174=CARTESIAN_POINT('Ctrl Pts',(6.12826319842071,-5.00285090648096,31.1345016672797));
#72175=CARTESIAN_POINT('Ctrl Pts',(6.13733007459012,-4.99172380781719,31.135078291832));
#72176=CARTESIAN_POINT('Ctrl Pts',(6.15119639623407,-4.97461181878337,31.1359654656859));
#72177=CARTESIAN_POINT('Ctrl Pts',(6.15601753073699,-4.96864448449911,31.1362749178635));
#72178=CARTESIAN_POINT('Ctrl Pts',(6.16480419856887,-4.95773641188236,31.1368407096842));
#72179=CARTESIAN_POINT('Ctrl Pts',(6.16877249515417,-4.95279790008913,31.137096912204));
#72180=CARTESIAN_POINT('Ctrl Pts',(6.17735149161495,-4.94209510578575,31.1376522493715));
#72181=CARTESIAN_POINT('Ctrl Pts',(6.18196006238769,-4.93632912923834,31.1379514871591));
#72182=CARTESIAN_POINT('Ctrl Pts',(6.19446434434433,-4.92063952221115,31.1387658745215));
#72183=CARTESIAN_POINT('Ctrl Pts',(6.20234425614442,-4.91070336579804,31.1392817756522));
#72184=CARTESIAN_POINT('Ctrl Pts',(6.23974344267957,-4.86331133093884,31.1417430354073));
#72185=CARTESIAN_POINT('Ctrl Pts',(6.26894717859584,-4.82560840612285,31.1437028445916));
#72186=CARTESIAN_POINT('Ctrl Pts',(6.59752545899825,-4.39338688429603,31.1661722291948));
#72187=CARTESIAN_POINT('Ctrl Pts',(6.85954967461005,-3.97186851748783,31.1880379696263));
#72188=CARTESIAN_POINT('Ctrl Pts',(7.24213491691667,-3.20418789103403,31.2255722810119));
#72189=CARTESIAN_POINT('Ctrl Pts',(7.38134480055917,-2.86899050018733,31.2413027165437));
#72190=CARTESIAN_POINT('Ctrl Pts',(7.57607418417918,-2.29090732904578,31.2670837268361));
#72191=CARTESIAN_POINT('Ctrl Pts',(7.64402531897234,-2.05281308150819,31.2773444918702));
#72192=CARTESIAN_POINT('Ctrl Pts',(7.71343001058933,-1.75784089072636,31.2896636448816));
#72193=CARTESIAN_POINT('Ctrl Pts',(7.72558385120725,-1.70363181445123,31.2919119648223));
#72194=CARTESIAN_POINT('Ctrl Pts',(7.74160035335889,-1.62849544674163,31.2950075332478));
#72195=CARTESIAN_POINT('Ctrl Pts',(7.74595103764545,-1.60767408969779,31.2958631477727));
#72196=CARTESIAN_POINT('Ctrl Pts',(7.75312173895509,-1.57265187065761,31.2972985925961));
#72197=CARTESIAN_POINT('Ctrl Pts',(7.75598683743078,-1.55846038915843,31.2978792279422));
#72198=CARTESIAN_POINT('Ctrl Pts',(7.76154234292019,-1.53054792786461,31.2990192289511));
#72199=CARTESIAN_POINT('Ctrl Pts',(7.76423536262972,-1.51682752335679,31.2995786402218));
#72200=CARTESIAN_POINT('Ctrl Pts',(7.77008979712634,-1.48657620296027,31.3008099435709));
#72201=CARTESIAN_POINT('Ctrl Pts',(7.77323486412581,-1.47004218047487,31.301481532466));
#72202=CARTESIAN_POINT('Ctrl Pts',(7.78349876186327,-1.41512953856948,31.3037074112258));
#72203=CARTESIAN_POINT('Ctrl Pts',(7.79038634373476,-1.37670811553079,31.3052573731454));
#72204=CARTESIAN_POINT('Ctrl Pts',(7.86357900991018,-0.950264665550267,
31.3223786946493));
#72205=CARTESIAN_POINT('Ctrl Pts',(7.90112051485106,-0.55785341012628,31.337339355633));
#72206=CARTESIAN_POINT('Ctrl Pts',(7.92354632733192,0.521992051633251,31.3773062121688));
#72207=CARTESIAN_POINT('Ctrl Pts',(7.84842631290132,1.2070882678104,31.4011337169805));
#72208=CARTESIAN_POINT('Ctrl Pts',(7.67369595031647,1.92378736809428,31.4301286983926));
#72209=CARTESIAN_POINT('Ctrl Pts',(7.66102409454298,1.97364562030095,31.4321693483615));
#72210=CARTESIAN_POINT('Ctrl Pts',(7.64493362965968,2.03446364935185,31.4346911359885));
#72211=CARTESIAN_POINT('Ctrl Pts',(7.64197608579264,2.04554492608356,31.4351519426416));
#72212=CARTESIAN_POINT('Ctrl Pts',(7.63731155154349,2.06287061419628,31.435874548951));
#72213=CARTESIAN_POINT('Ctrl Pts',(7.63562096875154,2.0691194570294,31.4361356049262));
#72214=CARTESIAN_POINT('Ctrl Pts',(7.63261505783495,2.08017624864531,31.4365983004786));
#72215=CARTESIAN_POINT('Ctrl Pts',(7.6313028506043,2.0849850475955,31.4367997963202));
#72216=CARTESIAN_POINT('Ctrl Pts',(7.62850343743843,2.09520591046973,31.4372286270021));
#72217=CARTESIAN_POINT('Ctrl Pts',(7.62701501562688,2.1006176361813,31.437456018396));
#72218=CARTESIAN_POINT('Ctrl Pts',(7.62274968208299,2.11606158730045,31.4381059140786));
#72219=CARTESIAN_POINT('Ctrl Pts',(7.6199587342022,2.12608989565351,31.4385290805968));
#72220=CARTESIAN_POINT('Ctrl Pts',(7.60789738701082,2.16909936319313,31.4403490754998));
#72221=CARTESIAN_POINT('Ctrl Pts',(7.59843265055139,2.20202542030444,31.4417553434923));
#72222=CARTESIAN_POINT('Ctrl Pts',(7.43808248871584,2.74650789195676,31.4652381138569));
#72223=CARTESIAN_POINT('Ctrl Pts',(7.23607042515302,3.2415379525862,31.4898234140032));
#72224=CARTESIAN_POINT('Ctrl Pts',(6.7730884959596,4.11274909002927,31.5353007538303));
#72225=CARTESIAN_POINT('Ctrl Pts',(6.5263190051239,4.49406820842912,31.5561060003558));
#72226=CARTESIAN_POINT('Ctrl Pts',(6.12598075308176,5.00959163936947,31.5846327269059));
#72227=CARTESIAN_POINT('Ctrl Pts',(5.99781986367865,5.16234564288104,31.5931520905564));
#72228=CARTESIAN_POINT('Ctrl Pts',(5.79500322495911,5.38631885309384,31.6057333777597));
#72229=CARTESIAN_POINT('Ctrl Pts',(5.72450579927918,5.46118371065252,31.6099555797658));
#72230=CARTESIAN_POINT('Ctrl Pts',(5.63968493583025,5.5478116297034,31.6148635568323));
#72231=CARTESIAN_POINT('Ctrl Pts',(5.62675667922351,5.56092342445259,31.6156070418903));
#72232=CARTESIAN_POINT('Ctrl Pts',(5.60685884741494,5.58096330679199,31.6167443639161));
#72233=CARTESIAN_POINT('Ctrl Pts',(5.59992198550004,5.58792370418223,31.6171395713646));
#72234=CARTESIAN_POINT('Ctrl Pts',(5.58779458074353,5.60004699264239,31.6178282526309));
#72235=CARTESIAN_POINT('Ctrl Pts',(5.58260981364795,5.60521563058168,31.6181219691736));
#72236=CARTESIAN_POINT('Ctrl Pts',(5.57092425387647,5.61683254136234,31.6187823579931));
#72237=CARTESIAN_POINT('Ctrl Pts',(5.5644194210303,5.6232767447185,31.6191488587621));
#72238=CARTESIAN_POINT('Ctrl Pts',(5.54697296076758,5.64050067753201,31.6201288864096));
#72239=CARTESIAN_POINT('Ctrl Pts',(5.53601107903679,5.65125988225382,31.6207415521513));
#72240=CARTESIAN_POINT('Ctrl Pts',(5.48847565737654,5.69764537363359,31.6233850214464));
#72241=CARTESIAN_POINT('Ctrl Pts',(5.45158867668825,5.73294940352518,31.6254023953576));
#72242=CARTESIAN_POINT('Ctrl Pts',(4.78542844629761,6.35827860027531,31.6612439170891));
#72243=CARTESIAN_POINT('Ctrl Pts',(4.06423647782678,6.84178294074071,31.6899550832066));
#72244=CARTESIAN_POINT('Ctrl Pts',(3.09555083545373,7.28300916836281,31.7271947743833));
#72245=CARTESIAN_POINT('Ctrl Pts',(2.90874531298586,7.35960957936124,31.7343587395591));
#72246=CARTESIAN_POINT('Ctrl Pts',(2.53903534427114,7.49493412840622,31.7488039591175));
#72247=CARTESIAN_POINT('Ctrl Pts',(2.35651177215115,7.5543094178956,31.7560637534897));
#72248=CARTESIAN_POINT('Ctrl Pts',(2.13810348886371,7.61667103095306,31.7650416944534));
#72249=CARTESIAN_POINT('Ctrl Pts',(2.10413647357246,7.62612442664081,31.7664451572457));
#72250=CARTESIAN_POINT('Ctrl Pts',(2.05926331342329,7.63829050592086,31.7683077613857));
#72251=CARTESIAN_POINT('Ctrl Pts',(2.04841263815998,7.64120755568485,31.768758808325));
#72252=CARTESIAN_POINT('Ctrl Pts',(2.0306462938027,7.64594322259052,31.7694983627328));
#72253=CARTESIAN_POINT('Ctrl Pts',(2.02373428693343,7.64777560268952,31.769786342373));
#72254=CARTESIAN_POINT('Ctrl Pts',(2.01037672776945,7.65129732865811,31.7703433494751));
#72255=CARTESIAN_POINT('Ctrl Pts',(2.00393150459491,7.65298790823911,31.7706123303634));
#72256=CARTESIAN_POINT('Ctrl Pts',(1.98910231173995,7.65685758212376,31.7712316895764));
#72257=CARTESIAN_POINT('Ctrl Pts',(1.98071689096315,7.65903105076917,31.7715822745833));
#72258=CARTESIAN_POINT('Ctrl Pts',(1.95832500515489,7.66479570843899,31.7725193808405));
#72259=CARTESIAN_POINT('Ctrl Pts',(1.94431226855425,7.66836226824856,31.7731067844201));
#72260=CARTESIAN_POINT('Ctrl Pts',(1.8471461879325,7.69280978946205,31.7771862787486));
#72261=CARTESIAN_POINT('Ctrl Pts',(1.76366943639669,7.71237583659046,31.7807232189715));
#72262=CARTESIAN_POINT('Ctrl Pts',(1.01545829949418,7.87496576646416,31.8126274012644));
#72263=CARTESIAN_POINT('Ctrl Pts',(0.33516685241311,7.93309448014955,31.8426732427994));
#72264=CARTESIAN_POINT('Ctrl Pts',(-0.891156915128255,7.87968897134275,
31.8946998603581));
#72265=CARTESIAN_POINT('Ctrl Pts',(-1.43418032141702,7.7991548035678,31.9171259763563));
#72266=CARTESIAN_POINT('Ctrl Pts',(-2.03869730178635,7.64418046461702,31.942440576106));
#72267=CARTESIAN_POINT('Ctrl Pts',(-2.11257467746494,7.6240940445047,31.9455381509962));
#72268=CARTESIAN_POINT('Ctrl Pts',(-2.21947736928432,7.59335524080166,31.9500260566281));
#72269=CARTESIAN_POINT('Ctrl Pts',(-2.25274225757413,7.58355298901857,31.9514233615065));
#72270=CARTESIAN_POINT('Ctrl Pts',(-2.31120932181367,7.56590570184017,31.9538807624126));
#72271=CARTESIAN_POINT('Ctrl Pts',(-2.33643867256069,7.55815268121473,31.9549416494663));
#72272=CARTESIAN_POINT('Ctrl Pts',(-2.385640580848,7.54276295489301,31.9570115632458));
#72273=CARTESIAN_POINT('Ctrl Pts',(-2.40961644236547,7.53513786069259,31.9580206827517));
#72274=CARTESIAN_POINT('Ctrl Pts',(-2.47444476902372,7.5141793137717,31.9607505525043));
#72275=CARTESIAN_POINT('Ctrl Pts',(-2.51522570396413,7.50062713073175,31.9624692181688));
#72276=CARTESIAN_POINT('Ctrl Pts',(-2.67127926982586,7.44735210782456,31.9690519517231));
#72277=CARTESIAN_POINT('Ctrl Pts',(-2.7857390612271,7.40529842300519,31.9738926154428));
#72278=CARTESIAN_POINT('Ctrl Pts',(-2.91948193524314,7.35262009395263,31.9795703692867));
#72279=CARTESIAN_POINT('Ctrl Pts',(-2.93974868782772,7.34454046699756,31.9804313485876));
#72280=CARTESIAN_POINT('Ctrl Pts',(-3.25019002610646,7.21928781226467,31.9936295162194));
#72281=CARTESIAN_POINT('Ctrl Pts',(-3.53319775953302,7.08508082954811,32.0057828777964));
#72282=CARTESIAN_POINT('Ctrl Pts',(-4.11811764360785,6.76391806199331,32.0315991691729));
#72283=CARTESIAN_POINT('Ctrl Pts',(-4.4169069248435,6.57270157253297,32.0452182432583));
#72284=CARTESIAN_POINT('Ctrl Pts',(-4.75404129853829,6.32354502005252,32.0616923866786));
#72285=CARTESIAN_POINT('Ctrl Pts',(-4.80574097283294,6.28434434700464,32.0642520867674));
#72286=CARTESIAN_POINT('Ctrl Pts',(-4.89204668846952,6.21721617027423,32.0685880094399));
#72287=CARTESIAN_POINT('Ctrl Pts',(-4.92691021719911,6.18962465542846,32.0703572048615));
#72288=CARTESIAN_POINT('Ctrl Pts',(-4.98696103557478,6.1412707099657,32.0734375063217));
#72289=CARTESIAN_POINT('Ctrl Pts',(-5.0122559267398,6.1206434961833,32.0747453141198));
#72290=CARTESIAN_POINT('Ctrl Pts',(-5.04882466951977,6.09044408380105,32.0766517651363));
#72291=CARTESIAN_POINT('Ctrl Pts',(-5.0602005705987,6.08099579548292,32.0772470665321));
#72292=CARTESIAN_POINT('Ctrl Pts',(-5.08007291976968,6.06439638022556,32.0782909941949));
#72293=CARTESIAN_POINT('Ctrl Pts',(-5.08858093800096,6.05725914611251,32.0787392281378));
#72294=CARTESIAN_POINT('Ctrl Pts',(-5.1050404257405,6.043392405207,32.0796089239101));
#72295=CARTESIAN_POINT('Ctrl Pts',(-5.11299368937797,6.0366650597293,32.0800303222729));
#72296=CARTESIAN_POINT('Ctrl Pts',(-5.13195044569499,6.0205659642021,32.0810375442143));
#72297=CARTESIAN_POINT('Ctrl Pts',(-5.14294153451239,6.01117977421789,32.0816238048612));
#72298=CARTESIAN_POINT('Ctrl Pts',(-5.18571486044419,5.97444894677131,32.0839143156753));
#72299=CARTESIAN_POINT('Ctrl Pts',(-5.21730497889847,5.94688216961574,32.0856253221289));
#72300=CARTESIAN_POINT('Ctrl Pts',(-5.5613355735828,5.64181637249005,32.1044639872128));
#72301=CARTESIAN_POINT('Ctrl Pts',(-5.85153305396377,5.34023373139806,32.1221893502809));
#72302=CARTESIAN_POINT('Ctrl Pts',(-6.40005430444207,4.67151645782309,32.1586285919391));
#72303=CARTESIAN_POINT('Ctrl Pts',(-6.65376687824803,4.30246170590275,32.177247847855));
#72304=CARTESIAN_POINT('Ctrl Pts',(-6.90005081578642,3.86985701182146,32.1974475367171));
#72305=CARTESIAN_POINT('Ctrl Pts',(-6.92472489354689,3.8255299958124,32.1995001637835));
#72306=CARTESIAN_POINT('Ctrl Pts',(-6.96161043211629,3.75773875726609,32.2026140904936));
#72307=CARTESIAN_POINT('Ctrl Pts',(-6.97413332039988,3.73444571688238,32.2036795503167));
#72308=CARTESIAN_POINT('Ctrl Pts',(-6.99570902834766,3.69382705265076,32.2055298663076));
#72309=CARTESIAN_POINT('Ctrl Pts',(-7.00481485312628,3.67652988295461,32.2063154152573));
#72310=CARTESIAN_POINT('Ctrl Pts',(-7.02369699876184,3.6403370834715,32.2079541854236));
#72311=CARTESIAN_POINT('Ctrl Pts',(-7.03346139822558,3.62143540253318,32.2088072465828));
#72312=CARTESIAN_POINT('Ctrl Pts',(-7.06031016518923,3.56894403113251,32.2111686843905));
#72313=CARTESIAN_POINT('Ctrl Pts',(-7.07723098431855,3.53527123974191,32.2126749659109));
#72314=CARTESIAN_POINT('Ctrl Pts',(-7.14568308991905,3.39658894112014,32.2188447821186));
#72315=CARTESIAN_POINT('Ctrl Pts',(-7.19512327348996,3.29056299154068,32.2234823651031));
#72316=CARTESIAN_POINT('Ctrl Pts',(-7.52041560277533,2.55054540145986,32.255380138994));
#72317=CARTESIAN_POINT('Ctrl Pts',(-7.71448142923748,1.88382536400206,32.2819063898042));
#72318=CARTESIAN_POINT('Ctrl Pts',(-7.88052359178331,0.802212600736091,
32.322963547461));
#72319=CARTESIAN_POINT('Ctrl Pts',(-7.91114475720133,0.39996457160148,32.3378710197299));
#72320=CARTESIAN_POINT('Ctrl Pts',(-7.91092746979535,-0.202542422171511,
32.3608634280321));
#72321=CARTESIAN_POINT('Ctrl Pts',(-7.90329461465925,-0.402151086599798,
32.3685972740227));
#72322=CARTESIAN_POINT('Ctrl Pts',(-7.88648412906036,-0.622697182523359,
32.3774230150704));
#72323=CARTESIAN_POINT('Ctrl Pts',(-7.88476183717319,-0.644138541417185,
32.3782840166816));
#72324=CARTESIAN_POINT('Ctrl Pts',(-7.88213466579698,-0.675254409781156,
32.3795380883945));
#72325=CARTESIAN_POINT('Ctrl Pts',(-7.88129936918853,-0.684934785212657,
32.379928883228));
#72326=CARTESIAN_POINT('Ctrl Pts',(-7.87979613395171,-0.701989108547733,
32.3806185279854));
#72327=CARTESIAN_POINT('Ctrl Pts',(-7.87913567232502,-0.70936371336394,
32.3809171271696));
#72328=CARTESIAN_POINT('Ctrl Pts',(-7.87775101888295,-0.724583993489366,
32.3815342078939));
#72329=CARTESIAN_POINT('Ctrl Pts',(-7.87702545738826,-0.732429533999852,
32.3818527358431));
#72330=CARTESIAN_POINT('Ctrl Pts',(-7.87514245282453,-0.752464125736244,
32.3826672946928));
#72331=CARTESIAN_POINT('Ctrl Pts',(-7.87396843283787,-0.764651573912543,
32.3831639014454));
#72332=CARTESIAN_POINT('Ctrl Pts',(-7.86909484946609,-0.814042400135809,
32.3851810266616));
#72333=CARTESIAN_POINT('Ctrl Pts',(-7.86515990484144,-0.851221704328809,
32.3867099632953));
#72334=CARTESIAN_POINT('Ctrl Pts',(-7.802336490884,-1.40712939915158,32.4097435337132));
#72335=CARTESIAN_POINT('Ctrl Pts',(-7.69251757597306,-1.9186998064338,32.4335955396737));
#72336=CARTESIAN_POINT('Ctrl Pts',(-7.45709899350262,-2.65286046525554,
32.4689324038717));
#72337=CARTESIAN_POINT('Ctrl Pts',(-7.3698562800263,-2.88638487778127,32.4803459503612));
#72338=CARTESIAN_POINT('Ctrl Pts',(-7.09222532820695,-3.53440924607822,
32.5120992708572));
#72339=CARTESIAN_POINT('Ctrl Pts',(-6.87682040595874,-3.93714814281155,
32.5318794963912));
#72340=CARTESIAN_POINT('Ctrl Pts',(-6.61159463846393,-4.34414882566462,
32.5516287223159));
#72341=CARTESIAN_POINT('Ctrl Pts',(-6.59514990729964,-4.36907431937963,
32.5528374884528));
#72342=CARTESIAN_POINT('Ctrl Pts',(-6.5725359186241,-4.40293202355548,32.5544785183539));
#72343=CARTESIAN_POINT('Ctrl Pts',(-6.56648892917775,-4.41194537022426,
32.5549152932547));
#72344=CARTESIAN_POINT('Ctrl Pts',(-6.55618071892211,-4.42724214598884,
32.5556564104499));
#72345=CARTESIAN_POINT('Ctrl Pts',(-6.55192897587351,-4.43353192543998,
32.5559611038756));
#72346=CARTESIAN_POINT('Ctrl Pts',(-6.54369993036841,-4.44566780323547,
32.5565489193596));
#72347=CARTESIAN_POINT('Ctrl Pts',(-6.53972383237845,-4.45151470760091,
32.5568320858398));
#72348=CARTESIAN_POINT('Ctrl Pts',(-6.53028924513555,-4.46534847010777,
32.5575019759469));
#72349=CARTESIAN_POINT('Ctrl Pts',(-6.52482392854366,-4.47333067042677,
32.5578884441143));
#72350=CARTESIAN_POINT('Ctrl Pts',(-6.50872660006217,-4.49674886487872,
32.5590220840116));
#72351=CARTESIAN_POINT('Ctrl Pts',(-6.49805432296485,-4.51215717036431,
32.5597677451865));
#72352=CARTESIAN_POINT('Ctrl Pts',(-6.41731051402919,-4.62785199998683,
32.565365025458));
#72353=CARTESIAN_POINT('Ctrl Pts',(-6.34497418135968,-4.72654129832449,
32.5701301805974));
#72354=CARTESIAN_POINT('Ctrl Pts',(-6.09935222264076,-5.04583991640927,
32.5855435842295));
#72355=CARTESIAN_POINT('Ctrl Pts',(-5.91661894577559,-5.2589194258272,32.5958153598227));
#72356=CARTESIAN_POINT('Ctrl Pts',(-5.51204586957432,-5.68283211459569,
32.6166146085642));
#72357=CARTESIAN_POINT('Ctrl Pts',(-5.28852230219091,-5.89141492735127,
32.6270648963156));
#72358=CARTESIAN_POINT('Ctrl Pts',(-4.94467863795966,-6.17689868608441,
32.6422835533191));
#72359=CARTESIAN_POINT('Ctrl Pts',(-4.83346049647168,-6.26431030384937,
32.6470888467411));
#72360=CARTESIAN_POINT('Ctrl Pts',(-4.58378590122663,-6.44993180667817,
32.6577325583592));
#72361=CARTESIAN_POINT('Ctrl Pts',(-4.4443928367037,-6.54676131071564,32.6635826566439));
#72362=CARTESIAN_POINT('Ctrl Pts',(-4.15758219764344,-6.73261048534774,
32.6756289955966));
#72363=CARTESIAN_POINT('Ctrl Pts',(-4.01015760936008,-6.82144890002884,
32.6818259065695));
#72364=CARTESIAN_POINT('Ctrl Pts',(-3.84268395291629,-6.91506274367206,
32.6889897886896));
#72365=CARTESIAN_POINT('Ctrl Pts',(-3.82537197536631,-6.92465464495434,
32.6897317813967));
#72366=CARTESIAN_POINT('Ctrl Pts',(-3.69480966097545,-6.99635517220981,
32.6953398531934));
#72367=CARTESIAN_POINT('Ctrl Pts',(-3.58009453882149,-7.05574405244669,
32.7003358825635));
#72368=CARTESIAN_POINT('Ctrl Pts',(-3.45196991285036,-7.11814605464429,
32.7060420340481));
#72369=CARTESIAN_POINT('Ctrl Pts',(-3.43994251061171,-7.12396624459321,
32.7065788945651));
#72370=CARTESIAN_POINT('Ctrl Pts',(-3.42314300200417,-7.13204324534366,
32.7073305211416));
#72371=CARTESIAN_POINT('Ctrl Pts',(-3.41838323693154,-7.1343258203449,32.707543673969));
#72372=CARTESIAN_POINT('Ctrl Pts',(-3.41005336029733,-7.13831021474073,
32.7079170529731));
#72373=CARTESIAN_POINT('Ctrl Pts',(-3.40648424608221,-7.14001412624842,
32.708077147049));
#72374=CARTESIAN_POINT('Ctrl Pts',(-3.39899078941399,-7.14358463925437,
32.7084135065499));
#72375=CARTESIAN_POINT('Ctrl Pts',(-3.39506618512975,-7.14545068439722,
32.708589807174));
#72376=CARTESIAN_POINT('Ctrl Pts',(-3.38570383838536,-7.14989277709013,
32.7090107111318));
#72377=CARTESIAN_POINT('Ctrl Pts',(-3.38026469768572,-7.15246585300009,
32.7092555040833));
#72378=CARTESIAN_POINT('Ctrl Pts',(-3.36178210175921,-7.16118356061889,
32.7100882436872));
#72379=CARTESIAN_POINT('Ctrl Pts',(-3.34872504734232,-7.16729861492442,
32.7106780990421));
#72380=CARTESIAN_POINT('Ctrl Pts',(-3.04431071796018,-7.30885257951498,
32.7244656720448));
#72381=CARTESIAN_POINT('Ctrl Pts',(-2.74501220678494,-7.42644079699674,
32.7387657857388));
#72382=CARTESIAN_POINT('Ctrl Pts',(-1.85378484549011,-7.71533664684171,
32.7816133063665));
#72383=CARTESIAN_POINT('Ctrl Pts',(-1.24789317764472,-7.83618801848575,
32.8108759286724));
#72384=CARTESIAN_POINT('Ctrl Pts',(-0.494159383322317,-7.8967994722947,
32.844259128784));
#72385=CARTESIAN_POINT('Ctrl Pts',(-0.353924144084563,-7.90432639673571,
32.8503561218869));
#72386=CARTESIAN_POINT('Ctrl Pts',(-0.038728035658005,-7.91283823084119,
32.8637851127222));
#72387=CARTESIAN_POINT('Ctrl Pts',(0.136216875681287,-7.91176081747751,
32.871048403724));
#72388=CARTESIAN_POINT('Ctrl Pts',(0.33011189978663,-7.90413267275771,32.8788903677481));
#72389=CARTESIAN_POINT('Ctrl Pts',(0.349230106061316,-7.90331104760243,
32.8796613652996));
#72390=CARTESIAN_POINT('Ctrl Pts',(0.377810927396445,-7.90197884691433,
32.8808106689884));
#72391=CARTESIAN_POINT('Ctrl Pts',(0.387275838177037,-7.90152062706566,
32.881190734362));
#72392=CARTESIAN_POINT('Ctrl Pts',(0.4035690881239,-7.90070248434555,32.8818440651301));
#72393=CARTESIAN_POINT('Ctrl Pts',(0.410397815562013,-7.90035071299772,
32.8821176044655));
#72394=CARTESIAN_POINT('Ctrl Pts',(0.424483458704019,-7.8996068009482,32.8826812582192));
#72395=CARTESIAN_POINT('Ctrl Pts',(0.431740309144017,-7.89921351288598,
32.8829713337696));
#72396=CARTESIAN_POINT('Ctrl Pts',(0.448616688980382,-7.89827556482687,
32.8836451955218));
#72397=CARTESIAN_POINT('Ctrl Pts',(0.458235795639389,-7.89772332942059,
32.884028726405));
#72398=CARTESIAN_POINT('Ctrl Pts',(0.488820830509399,-7.89591136925101,
32.8852464569668));
#72399=CARTESIAN_POINT('Ctrl Pts',(0.509782846475794,-7.89458571517036,
32.8860784364723));
#72400=CARTESIAN_POINT('Ctrl Pts',(0.872144802056555,-7.87022039384877,
32.9004159330345));
#72401=CARTESIAN_POINT('Ctrl Pts',(1.21171525168398,-7.82513794470721,32.9131420424039));
#72402=CARTESIAN_POINT('Ctrl Pts',(2.06823688875544,-7.6543096548038,32.9442245502106));
#72403=CARTESIAN_POINT('Ctrl Pts',(2.57733356105756,-7.49822645377081,32.9616640397618));
#72404=CARTESIAN_POINT('Ctrl Pts',(3.27934925793857,-7.20297734330344,32.9877571751242));
#72405=CARTESIAN_POINT('Ctrl Pts',(3.4877355277662,-7.10441451813099,32.9958010248579));
#72406=CARTESIAN_POINT('Ctrl Pts',(3.73131165764893,-6.97590561727908,33.005894993658));
#72407=CARTESIAN_POINT('Ctrl Pts',(3.77093031525983,-6.9545690245547,33.0075594850674));
#72408=CARTESIAN_POINT('Ctrl Pts',(3.84041224238881,-6.91638130974689,33.0105225476616));
#72409=CARTESIAN_POINT('Ctrl Pts',(3.87035221868428,-6.8996717503794,33.0118138853848));
#72410=CARTESIAN_POINT('Ctrl Pts',(3.98758141852602,-6.83324277457977,33.0169312516423));
#72411=CARTESIAN_POINT('Ctrl Pts',(4.07402583230292,-6.78205900000284,33.0208388597984));
#72412=CARTESIAN_POINT('Ctrl Pts',(4.16956192988194,-6.72300640420817,33.0253365249781));
#72413=CARTESIAN_POINT('Ctrl Pts',(4.17964113122038,-6.71674488195535,33.0258132968662));
#72414=CARTESIAN_POINT('Ctrl Pts',(4.19420996980241,-6.70764876248092,33.0265057770203));
#72415=CARTESIAN_POINT('Ctrl Pts',(4.19871091421087,-6.70483227607867,33.026720176992));
#72416=CARTESIAN_POINT('Ctrl Pts',(4.20666146061695,-6.69984604024579,33.0270997178114));
#72417=CARTESIAN_POINT('Ctrl Pts',(4.21011219121537,-6.6976781756434,33.0272647210103));
#72418=CARTESIAN_POINT('Ctrl Pts',(4.21726489075554,-6.69317689820336,33.0276073051194));
#72419=CARTESIAN_POINT('Ctrl Pts',(4.22096660083447,-6.69084307871034,33.0277849153057));
#72420=CARTESIAN_POINT('Ctrl Pts',(4.23048157194049,-6.68483313011628,33.0282422527284));
#72421=CARTESIAN_POINT('Ctrl Pts',(4.23629196767401,-6.68115249579342,33.0285223019758));
#72422=CARTESIAN_POINT('Ctrl Pts',(4.2602835399118,-6.6659109931913,33.029681815876));
#72423=CARTESIAN_POINT('Ctrl Pts',(4.27842209132177,-6.6542835527151,33.0305659838422));
#72424=CARTESIAN_POINT('Ctrl Pts',(4.40093364158854,-6.57504141243854,33.0365876888371));
#72425=CARTESIAN_POINT('Ctrl Pts',(4.50374235145094,-6.50505097909369,33.0418867505677));
#72426=CARTESIAN_POINT('Ctrl Pts',(4.75278299010074,-6.32677421678128,33.0552499474867));
#72427=CARTESIAN_POINT('Ctrl Pts',(4.8970087338744,-6.21581185361765,33.0634538502892));
#72428=CARTESIAN_POINT('Ctrl Pts',(5.42327710420013,-5.78122740691778,33.0947884990583));
#72429=CARTESIAN_POINT('Ctrl Pts',(5.77815545307308,-5.42655225955305,33.1187426847549));
#72430=CARTESIAN_POINT('Ctrl Pts',(6.4252785009965,-4.64380472094178,33.165551983905));
#72431=CARTESIAN_POINT('Ctrl Pts',(6.71390762270889,-4.215768901284,33.1882220692318));
#72432=CARTESIAN_POINT('Ctrl Pts',(6.97483644424306,-3.73318888403737,33.2105520296715));
#72433=CARTESIAN_POINT('Ctrl Pts',(6.99057855220665,-3.7036271695444,33.2119083201034));
#72434=CARTESIAN_POINT('Ctrl Pts',(7.01186344541045,-3.66303757813,33.2137549386503));
#72435=CARTESIAN_POINT('Ctrl Pts',(7.01756873799708,-3.65209560187206,33.2142511973975));
#72436=CARTESIAN_POINT('Ctrl Pts',(7.02657639642081,-3.63472109338896,33.2150367592113));
#72437=CARTESIAN_POINT('Ctrl Pts',(7.0298955737428,-3.62829732851342,33.2153266732395));
#72438=CARTESIAN_POINT('Ctrl Pts',(7.03631109045922,-3.61583921636753,33.2158879093494));
#72439=CARTESIAN_POINT('Ctrl Pts',(7.03940848528146,-3.60980542107245,33.2161592695666));
#72440=CARTESIAN_POINT('Ctrl Pts',(7.04675940902331,-3.59544021448345,33.2168042277656));
#72441=CARTESIAN_POINT('Ctrl Pts',(7.05100593216663,-3.58710521868658,33.2171775721551));
#72442=CARTESIAN_POINT('Ctrl Pts',(7.06355475934116,-3.56236623321961,33.2182831119125));
#72443=CARTESIAN_POINT('Ctrl Pts',(7.07181470002205,-3.54594075984663,33.2190137801));
#72444=CARTESIAN_POINT('Ctrl Pts',(7.13769979304879,-3.41377774057424,33.2248662260409));
#72445=CARTESIAN_POINT('Ctrl Pts',(7.1925385244288,-3.29666927826247,33.2298876247549));
#72446=CARTESIAN_POINT('Ctrl Pts',(7.37148054601365,-2.88879191306712,33.2468635717766));
#72447=CARTESIAN_POINT('Ctrl Pts',(7.48101792558783,-2.59195562700374,33.2583240696627));
#72448=CARTESIAN_POINT('Ctrl Pts',(7.71345115790378,-1.82313281118756,33.2866493364581));
#72449=CARTESIAN_POINT('Ctrl Pts',(7.81103761279837,-1.34491930664794,33.3029901075963));
#72450=CARTESIAN_POINT('Ctrl Pts',(7.89740189708789,-0.555904175066547,
33.3312170301369));
#72451=CARTESIAN_POINT('Ctrl Pts',(7.91301602063158,-0.249342549770843,
33.3425395217143));
#72452=CARTESIAN_POINT('Ctrl Pts',(7.91061575368542,0.0816723465747907,
33.3557202794264));
#72453=CARTESIAN_POINT('Ctrl Pts',(7.91032743184258,0.105980554140972,33.3566929646156));
#72454=CARTESIAN_POINT('Ctrl Pts',(7.90978182354199,0.139105320911063,33.3580246285723));
#72455=CARTESIAN_POINT('Ctrl Pts',(7.90962182541215,0.1479235088808,33.3583797302412));
#72456=CARTESIAN_POINT('Ctrl Pts',(7.90932491281167,0.162906242805148,33.3589840719565));
#72457=CARTESIAN_POINT('Ctrl Pts',(7.90919553662948,0.169070942098553,33.3592330177593));
#72458=CARTESIAN_POINT('Ctrl Pts',(7.90893183622479,0.180972767746121,33.3597141909425));
#72459=CARTESIAN_POINT('Ctrl Pts',(7.90879847643914,0.186709912872769,33.3599463810995));
#72460=CARTESIAN_POINT('Ctrl Pts',(7.90846800053546,0.20029091218076,33.3604965984255));
#72461=CARTESIAN_POINT('Ctrl Pts',(7.90826545737063,0.208134620350179,33.3608148310837));
#72462=CARTESIAN_POINT('Ctrl Pts',(7.9076451260912,0.230848098739798,33.3617376519985));
#72463=CARTESIAN_POINT('Ctrl Pts',(7.90719706688842,0.245716964344987,33.3623433648009));
#72464=CARTESIAN_POINT('Ctrl Pts',(7.90365603834653,0.353159596492445,33.3667315418744));
#72465=CARTESIAN_POINT('Ctrl Pts',(7.89897943712547,0.44567200733777,33.3705704429663));
#72466=CARTESIAN_POINT('Ctrl Pts',(7.8785872811178,0.744789499577517,33.3831431884445));
#72467=CARTESIAN_POINT('Ctrl Pts',(7.85638002390072,0.950860974038948,33.3920517516341));
#72468=CARTESIAN_POINT('Ctrl Pts',(7.70495458107232,1.97617346788039,33.437082553918));
#72469=CARTESIAN_POINT('Ctrl Pts',(7.45553304126914,2.77252951500953,33.4736766693005));
#72470=CARTESIAN_POINT('Ctrl Pts',(7.05576612426643,3.57840826362952,33.5103731881086));
#72471=CARTESIAN_POINT('Ctrl Pts',(7.02375981884731,3.64082950274119,33.5132182490646));
#72472=CARTESIAN_POINT('Ctrl Pts',(6.97951017615574,3.72437292666064,33.5170316258426));
#72473=CARTESIAN_POINT('Ctrl Pts',(6.96799335069341,3.74587568777321,33.5180136157243));
#72474=CARTESIAN_POINT('Ctrl Pts',(6.94987979088404,3.77932243258408,33.5195418035732));
#72475=CARTESIAN_POINT('Ctrl Pts',(6.94335132264555,3.79130314916276,33.5200893535031));
#72476=CARTESIAN_POINT('Ctrl Pts',(6.93081893556965,3.81416101381399,33.521134299543));
#72477=CARTESIAN_POINT('Ctrl Pts',(6.92482032554711,3.82504102159432,33.5216318011316));
#72478=CARTESIAN_POINT('Ctrl Pts',(6.91090935455271,3.85013213435724,33.5227794052549));
#72479=CARTESIAN_POINT('Ctrl Pts',(6.90297873923738,3.86433307141723,33.5234291301266));
#72480=CARTESIAN_POINT('Ctrl Pts',(6.88044162310628,3.90439833744,33.5252628015691));
#72481=CARTESIAN_POINT('Ctrl Pts',(6.86573312908299,3.93020507367409,33.5264446038895));
#72482=CARTESIAN_POINT('Ctrl Pts',(6.83254580805027,3.98767889855076,33.5290781898424));
#72483=CARTESIAN_POINT('Ctrl Pts',(6.81399144879621,4.01930165332891,33.530528319358));
#72484=CARTESIAN_POINT('Ctrl Pts',(6.66453174568438,4.27002067971258,33.5420349097794));
#72485=CARTESIAN_POINT('Ctrl Pts',(6.52331018001215,4.48279967952675,33.5518495252379));
#72486=CARTESIAN_POINT('Ctrl Pts',(6.0969138581944,5.0623201048706,33.5789408476289));
#72487=CARTESIAN_POINT('Ctrl Pts',(5.78940794619793,5.41130319298667,33.5956393611481));
#72488=CARTESIAN_POINT('Ctrl Pts',(5.29002954128316,5.88643834552112,33.6208133917479));
#72489=CARTESIAN_POINT('Ctrl Pts',(5.12044501474955,6.03453444817852,33.6290957261962));
#72490=CARTESIAN_POINT('Ctrl Pts',(4.86088141644757,6.24237986006729,33.6417089373373));
#72491=CARTESIAN_POINT('Ctrl Pts',(4.7756202609987,6.30784625938431,33.6458432449112));
#72492=CARTESIAN_POINT('Ctrl Pts',(4.67281650537838,6.38350322025479,33.6508489310775));
#72493=CARTESIAN_POINT('Ctrl Pts',(4.65653341917434,6.39539083737836,33.6516423913928));
#72494=CARTESIAN_POINT('Ctrl Pts',(4.60893800954172,6.42986017087523,33.653963967118));
#72495=CARTESIAN_POINT('Ctrl Pts',(4.5775058843503,6.45227488571555,33.6555000176022));
#72496=CARTESIAN_POINT('Ctrl Pts',(4.53709129367659,6.4806511815563,33.6574803187621));
#72497=CARTESIAN_POINT('Ctrl Pts',(4.52825863548561,6.48682594746188,33.6579134366595));
#72498=CARTESIAN_POINT('Ctrl Pts',(4.51417522042669,6.49662864965488,33.6586045848618));
#72499=CARTESIAN_POINT('Ctrl Pts',(4.50893262291727,6.50026832783638,33.6588619889915));
#72500=CARTESIAN_POINT('Ctrl Pts',(4.49912731577516,6.50705810162583,33.6593436543037));
#72501=CARTESIAN_POINT('Ctrl Pts',(4.49456568504792,6.51020975422795,33.6595678311992));
#72502=CARTESIAN_POINT('Ctrl Pts',(4.48440398107736,6.51721475353447,33.6600674409286));
#72503=CARTESIAN_POINT('Ctrl Pts',(4.47880225136634,6.52106567992592,33.660343005504));
#72504=CARTESIAN_POINT('Ctrl Pts',(4.46249786542099,6.53224326155335,33.6611455205228));
#72505=CARTESIAN_POINT('Ctrl Pts',(4.45178218190412,6.539550797169,33.6616735269393));
#72506=CARTESIAN_POINT('Ctrl Pts',(4.42778463883018,6.55582954956543,33.6628573726563));
#72507=CARTESIAN_POINT('Ctrl Pts',(4.41449341682578,6.56478680213562,33.6635140001783));
#72508=CARTESIAN_POINT('Ctrl Pts',(4.37261852432178,6.59282255622585,33.6655860107285));
#72509=CARTESIAN_POINT('Ctrl Pts',(4.34393860727937,6.61175462886298,33.6670100884214));
#72510=CARTESIAN_POINT('Ctrl Pts',(4.22872894021534,6.68673321991033,33.6727486263584));
#72511=CARTESIAN_POINT('Ctrl Pts',(4.14123306790011,6.74127115710724,33.6771463052817));
#72512=CARTESIAN_POINT('Ctrl Pts',(3.93383020899701,6.86498787279223,33.6876214062948));
#72513=CARTESIAN_POINT('Ctrl Pts',(3.81312434203901,6.93275982156251,33.693756190696));
#72514=CARTESIAN_POINT('Ctrl Pts',(3.40508924640276,7.14797598555145,33.7144870309655));
#72515=CARTESIAN_POINT('Ctrl Pts',(3.11052127233813,7.28099188248554,33.7294311511076));
#72516=CARTESIAN_POINT('Ctrl Pts',(2.18396243818395,7.63287336895979,33.7750829708796));
#72517=CARTESIAN_POINT('Ctrl Pts',(1.53163360906138,7.79004538863906,33.8051315388421));
#72518=CARTESIAN_POINT('Ctrl Pts',(0.824430612135664,7.86804233170642,33.8342211784226));
#72519=CARTESIAN_POINT('Ctrl Pts',(0.781582599764353,7.87241415837215,33.8359715889673));
#72520=CARTESIAN_POINT('Ctrl Pts',(0.724410171690338,7.87777614022145,33.8382913512211));
#72521=CARTESIAN_POINT('Ctrl Pts',(0.710116086697029,7.87907749412359,33.8388700149798));
#72522=CARTESIAN_POINT('Ctrl Pts',(0.68781166301903,7.88104693079272,33.8397709196889));
#72523=CARTESIAN_POINT('Ctrl Pts',(0.679803746825926,7.88174171585242,33.8400939599521));
#72524=CARTESIAN_POINT('Ctrl Pts',(0.664507366012739,7.88304537932679,33.8407102381162));
#72525=CARTESIAN_POINT('Ctrl Pts',(0.657219091346626,7.8836563571945,33.841003538594));
#72526=CARTESIAN_POINT('Ctrl Pts',(0.640211983875246,7.88505831916638,33.8416871667047));
#72527=CARTESIAN_POINT('Ctrl Pts',(0.630492505690202,7.88584144413706,33.8420772586367));
#72528=CARTESIAN_POINT('Ctrl Pts',(0.602767593339027,7.88802373096866,33.8431883033816));
#72529=CARTESIAN_POINT('Ctrl Pts',(0.584758731872752,7.88937921402568,33.8439079480389));
#72530=CARTESIAN_POINT('Ctrl Pts',(0.471023307754614,7.89754822804403,33.8484401433245));
#72531=CARTESIAN_POINT('Ctrl Pts',(0.37518228839042,7.90268118992016,33.8522021853134));
#72532=CARTESIAN_POINT('Ctrl Pts',(0.0908909016374918,7.91272333794625,
33.8632051251299));
#72533=CARTESIAN_POINT('Ctrl Pts',(-0.0976708626531418,7.9126428708132,
33.8702983174578));
#72534=CARTESIAN_POINT('Ctrl Pts',(-0.422168451783075,7.90090155498634,
33.8822389789408));
#72535=CARTESIAN_POINT('Ctrl Pts',(-0.558132440884234,7.89246230388878,
33.8871618897826));
#72536=CARTESIAN_POINT('Ctrl Pts',(-0.971901495377524,7.85603340520139,
33.9019783943688));
#72537=CARTESIAN_POINT('Ctrl Pts',(-1.24850317948589,7.8168470856265,33.9116496690037));
#72538=CARTESIAN_POINT('Ctrl Pts',(-1.69135065204,7.72999844234706,33.9272355686748));
#72539=CARTESIAN_POINT('Ctrl Pts',(-1.85911683229895,7.69137353691499,33.9331662196671));
#72540=CARTESIAN_POINT('Ctrl Pts',(-2.44421628413267,7.53640237963433,33.9542424173627));
#72541=CARTESIAN_POINT('Ctrl Pts',(-2.8531273054934,7.39129329290249,33.9696933264443));
#72542=CARTESIAN_POINT('Ctrl Pts',(-3.27659728510231,7.20061165459805,33.9880813290809));
#72543=CARTESIAN_POINT('Ctrl Pts',(-3.30502116806719,7.18760968688966,33.9893265322627));
#72544=CARTESIAN_POINT('Ctrl Pts',(-3.3434544803934,7.16975291495953,33.9910244601922));
#72545=CARTESIAN_POINT('Ctrl Pts',(-3.35353205478074,7.16504483447363,33.9914710055822));
#72546=CARTESIAN_POINT('Ctrl Pts',(-3.36940245665855,7.15758962140184,33.9921763032658));
#72547=CARTESIAN_POINT('Ctrl Pts',(-3.37520195330211,7.15485666365741,33.9924344752722));
#72548=CARTESIAN_POINT('Ctrl Pts',(-3.38637632447907,7.14957423754186,33.992932749767));
#72549=CARTESIAN_POINT('Ctrl Pts',(-3.39175165927738,7.14702574996537,33.9931728126738));
#72550=CARTESIAN_POINT('Ctrl Pts',(-3.40444567435204,7.14098987364071,33.993740600473));
#72551=CARTESIAN_POINT('Ctrl Pts',(-3.41176187155182,7.13749729641193,33.9940685308334));
#72552=CARTESIAN_POINT('Ctrl Pts',(-3.43313804780068,7.12725244545341,33.9950286464845));
#72553=CARTESIAN_POINT('Ctrl Pts',(-3.44718340122695,7.1204698490191,33.9956620070491));
#72554=CARTESIAN_POINT('Ctrl Pts',(-3.5490867058006,7.07088787668999,34.0002750594893));
#72555=CARTESIAN_POINT('Ctrl Pts',(-3.63616321820791,7.02650610407864,34.0043132648407));
#72556=CARTESIAN_POINT('Ctrl Pts',(-3.92946913765471,6.87009950938167,34.0181989876576));
#72557=CARTESIAN_POINT('Ctrl Pts',(-4.13152446440245,6.75051814337375,34.0282458813579));
#72558=CARTESIAN_POINT('Ctrl Pts',(-4.54237363692547,6.48200380283279,34.0493914998326));
#72559=CARTESIAN_POINT('Ctrl Pts',(-4.74985718774298,6.33153927368154,34.0604884284565));
#72560=CARTESIAN_POINT('Ctrl Pts',(-5.2430600967325,5.93596555342014,34.0876701552954));
#72561=CARTESIAN_POINT('Ctrl Pts',(-5.51929944106448,5.68002803141701,34.1036017923442));
#72562=CARTESIAN_POINT('Ctrl Pts',(-5.830612021902,5.34735493135501,34.1225275990923));
#72563=CARTESIAN_POINT('Ctrl Pts',(-5.88405500723007,5.28849110266729,34.1258167620943));
#72564=CARTESIAN_POINT('Ctrl Pts',(-6.12448351607916,5.01551837361121,34.1408151998826));
#72565=CARTESIAN_POINT('Ctrl Pts',(-6.3007356924843,4.79222882067065,34.1524037587994));
#72566=CARTESIAN_POINT('Ctrl Pts',(-6.50234455584356,4.50640956742863,34.1665773693545));
#72567=CARTESIAN_POINT('Ctrl Pts',(-6.53943582214714,4.45241407624802,34.1692258945061));
#72568=CARTESIAN_POINT('Ctrl Pts',(-6.59423784021253,4.37047389157929,34.1732017612311));
#72569=CARTESIAN_POINT('Ctrl Pts',(-6.61245081372409,4.342868749517,34.1745339257333));
#72570=CARTESIAN_POINT('Ctrl Pts',(-6.64478173051477,4.29319033305393,34.1769183518695));
#72571=CARTESIAN_POINT('Ctrl Pts',(-6.65896411453266,4.27115960929814,34.177971250334));
#72572=CARTESIAN_POINT('Ctrl Pts',(-6.6861494671716,4.2284657169355,34.1800030343796));
#72573=CARTESIAN_POINT('Ctrl Pts',(-6.69916674489275,4.20781201394333,34.180982058088));
#72574=CARTESIAN_POINT('Ctrl Pts',(-6.72733808212606,4.16265221945933,34.1831143356069));
#72575=CARTESIAN_POINT('Ctrl Pts',(-6.74245429776418,4.13812291026708,34.1842671797409));
#72576=CARTESIAN_POINT('Ctrl Pts',(-6.80213400458153,4.04008457750123,34.1888538344518));
#72577=CARTESIAN_POINT('Ctrl Pts',(-6.84563229667065,3.96593356520003,34.1922760810727));
#72578=CARTESIAN_POINT('Ctrl Pts',(-7.0146035680123,3.66682453631923,34.20590217578));
#72579=CARTESIAN_POINT('Ctrl Pts',(-7.13026669950786,3.436504920471,34.2159925132599));
#72580=CARTESIAN_POINT('Ctrl Pts',(-7.32003420274299,3.00761012587288,34.2342321611224));
#72581=CARTESIAN_POINT('Ctrl Pts',(-7.39779439043106,2.81091768888644,34.2423991442973));
#72582=CARTESIAN_POINT('Ctrl Pts',(-7.58604461796744,2.27258461749701,34.2644442599387));
#72583=CARTESIAN_POINT('Ctrl Pts',(-7.68131474043748,1.92616303313631,34.2782982588775));
#72584=CARTESIAN_POINT('Ctrl Pts',(-7.76172219545577,1.53023789837007,34.2943869398474));
#72585=CARTESIAN_POINT('Ctrl Pts',(-7.77032902953044,1.48591594130574,34.2961917417176));
#72586=CARTESIAN_POINT('Ctrl Pts',(-7.78172185144996,1.42443950271301,34.2987020253555));
#72587=CARTESIAN_POINT('Ctrl Pts',(-7.78483147791202,1.40734563181627,34.2994007659));
#72588=CARTESIAN_POINT('Ctrl Pts',(-7.78972120681561,1.37995424720859,34.3005217401465));
#72589=CARTESIAN_POINT('Ctrl Pts',(-7.79153726661345,1.36966317995263,34.3009431900185));
#72590=CARTESIAN_POINT('Ctrl Pts',(-7.79512934678877,1.34906959151864,34.3017871805859));
#72591=CARTESIAN_POINT('Ctrl Pts',(-7.79690534630222,1.33876708801416,34.30220972082));
#72592=CARTESIAN_POINT('Ctrl Pts',(-7.80045395369489,1.31793517542846,34.3030647686239));
#72593=CARTESIAN_POINT('Ctrl Pts',(-7.80222567643297,1.30740563846673,34.3034972955494));
#72594=CARTESIAN_POINT('Ctrl Pts',(-7.80623665932681,1.28326940848313,34.3044895724062));
#72595=CARTESIAN_POINT('Ctrl Pts',(-7.80846166197171,1.26966043754333,34.3050496646688));
#72596=CARTESIAN_POINT('Ctrl Pts',(-7.81423166667276,1.23377998232336,34.3065279158373));
#72597=CARTESIAN_POINT('Ctrl Pts',(-7.81771702853883,1.21149908755133,34.3074474389253));
#72598=CARTESIAN_POINT('Ctrl Pts',(-7.82805901666214,1.14348231499749,34.310258854645));
#72599=CARTESIAN_POINT('Ctrl Pts',(-7.83460987114422,1.0977011798412,34.3121572264864));
#72600=CARTESIAN_POINT('Ctrl Pts',(-7.8873571986243,0.70451493309922,34.3285041600686));
#72601=CARTESIAN_POINT('Ctrl Pts',(-7.91082079892818,0.354462731269747,
34.3433274249038));
#72602=CARTESIAN_POINT('Ctrl Pts',(-7.91099897745234,0.00402228145511663,
34.3581038380725));
#72603=CARTESIAN_POINT('',(-7.90835677968835,8.74328140329327E-7,36.3575767704668));
#72604=CARTESIAN_POINT('Ctrl Pts',(-7.91024367631032,0.00400354093750647,
34.3576684917631));
#72605=CARTESIAN_POINT('Ctrl Pts',(-7.90782998290103,-0.879334447994197,
34.3932661792596));
#72606=CARTESIAN_POINT('Ctrl Pts',(-7.53464189968267,-3.08007093248513,
34.4817851337331));
#72607=CARTESIAN_POINT('Ctrl Pts',(-4.8119999607783,-7.26991696249447,34.6761466221616));
#72608=CARTESIAN_POINT('Ctrl Pts',(2.39745492945816,-9.04145408158046,34.940752957047));
#72609=CARTESIAN_POINT('Ctrl Pts',(8.91206867060443,-2.8636622032058,35.2582805589104));
#72610=CARTESIAN_POINT('Ctrl Pts',(7.50125790307925,4.4424751158228,35.522886893796));
#72611=CARTESIAN_POINT('Ctrl Pts',(3.10734150823604,7.61713964008732,35.7345719617049));
#72612=CARTESIAN_POINT('Ctrl Pts',(-2.28026636838621,8.42190983339057,35.9462570296132));
#72613=CARTESIAN_POINT('Ctrl Pts',(-7.03744966258467,5.09046671418386,36.1539252992009));
#72614=CARTESIAN_POINT('Ctrl Pts',(-7.91033516654623,1.2191874091852,36.308672301811));
#72615=CARTESIAN_POINT('Ctrl Pts',(-7.90835677968835,8.74328140328812E-7,
36.3575767704668));
#72616=CARTESIAN_POINT('',(-7.91892560419408,-0.000477670393038393,40.3576684917631));
#72617=CARTESIAN_POINT('Ctrl Pts',(-7.91099999974567,6.34350998739673E-5,
36.3591007772358));
#72618=CARTESIAN_POINT('Ctrl Pts',(-7.91100128680852,-0.160446349449327,
36.3656875025832));
#72619=CARTESIAN_POINT('Ctrl Pts',(-7.90611756750387,-0.320921897579779,
36.3722377272791));
#72620=CARTESIAN_POINT('Ctrl Pts',(-7.8904555431557,-0.577963795836673,
36.3827140688806));
#72621=CARTESIAN_POINT('Ctrl Pts',(-7.88277542261335,-0.674672258868436,
36.3866495373655));
#72622=CARTESIAN_POINT('Ctrl Pts',(-7.86990544413694,-0.806061535681041,
36.3919871907642));
#72623=CARTESIAN_POINT('Ctrl Pts',(-7.86626086167125,-0.840884632690744,
36.3934010063988));
#72624=CARTESIAN_POINT('Ctrl Pts',(-7.859478196455,-0.901783336511438,36.3958719992469));
#72625=CARTESIAN_POINT('Ctrl Pts',(-7.8564412223582,-0.927869619495753,
36.3969299829559));
#72626=CARTESIAN_POINT('Ctrl Pts',(-7.85025643312285,-0.978785641192203,
36.3989940772854));
#72627=CARTESIAN_POINT('Ctrl Pts',(-7.8471205724269,-1.00361652192462,36.4000002771073));
#72628=CARTESIAN_POINT('Ctrl Pts',(-7.84067389521036,-1.05278542288196,
36.4019918977854));
#72629=CARTESIAN_POINT('Ctrl Pts',(-7.83736746181006,-1.07712373949573,
36.4029773457103));
#72630=CARTESIAN_POINT('Ctrl Pts',(-7.82840941896887,-1.14083709459794,
36.4055560983881));
#72631=CARTESIAN_POINT('Ctrl Pts',(-7.82257407345061,-1.18018565910166,
36.4071477262376));
#72632=CARTESIAN_POINT('Ctrl Pts',(-7.80106401981511,-1.31805663613217,
36.4127215177653));
#72633=CARTESIAN_POINT('Ctrl Pts',(-7.78382266736936,-1.41632556054869,
36.4166887825074));
#72634=CARTESIAN_POINT('Ctrl Pts',(-7.73289634930477,-1.67746530858593,
36.427224340502));
#72635=CARTESIAN_POINT('Ctrl Pts',(-7.69592638373383,-1.83964508464265,
36.4337594446801));
#72636=CARTESIAN_POINT('Ctrl Pts',(-7.49705272225421,-2.60051619191154,
36.4644865102498));
#72637=CARTESIAN_POINT('Ctrl Pts',(-7.27023661998133,-3.17995251326264,
36.4879439620504));
#72638=CARTESIAN_POINT('Ctrl Pts',(-6.9479831059587,-3.78332395732732,36.5150820373445));
#72639=CARTESIAN_POINT('Ctrl Pts',(-6.91717783344546,-3.83935672767541,
36.517631449933));
#72640=CARTESIAN_POINT('Ctrl Pts',(-6.8786142825756,-3.90753035701743,36.520773659593));
#72641=CARTESIAN_POINT('Ctrl Pts',(-6.87149746033779,-3.92003196290222,
36.5213515560707));
#72642=CARTESIAN_POINT('Ctrl Pts',(-6.85891286492553,-3.9419988327894,36.5223700289469));
#72643=CARTESIAN_POINT('Ctrl Pts',(-6.85345949214589,-3.95147231737965,
36.5228102560313));
#72644=CARTESIAN_POINT('Ctrl Pts',(-6.84243450288904,-3.97053321794282,
36.5236980545097));
#72645=CARTESIAN_POINT('Ctrl Pts',(-6.83686232852009,-3.98012028223527,
36.5241456391603));
#72646=CARTESIAN_POINT('Ctrl Pts',(-6.82600117466787,-3.99871705816677,
36.5250159303589));
#72647=CARTESIAN_POINT('Ctrl Pts',(-6.82071446710367,-4.00772807277308,
36.5254385776426));
#72648=CARTESIAN_POINT('Ctrl Pts',(-6.80800891639722,-4.02928629732271,
36.5264520492108));
#72649=CARTESIAN_POINT('Ctrl Pts',(-6.80057325177522,-4.04182346443603,
36.5270433239849));
#72650=CARTESIAN_POINT('Ctrl Pts',(-6.77097861931579,-4.09140968127563,
36.5293894988432));
#72651=CARTESIAN_POINT('Ctrl Pts',(-6.74855138255254,-4.12829732779608,
36.5311515938725));
#72652=CARTESIAN_POINT('Ctrl Pts',(-6.5425058423051,-4.4610287029693,36.5471907051692));
#72653=CARTESIAN_POINT('Ctrl Pts',(-6.33984747248848,-4.74462691636221,
36.5618887958264));
#72654=CARTESIAN_POINT('Ctrl Pts',(-5.94180798011561,-5.23040656238268,
36.5883789342644));
#72655=CARTESIAN_POINT('Ctrl Pts',(-5.75307970086982,-5.43730754710313,
36.6001599706305));
#72656=CARTESIAN_POINT('Ctrl Pts',(-5.4397540626069,-5.74618441616636,36.6184551663497));
#72657=CARTESIAN_POINT('Ctrl Pts',(-5.32233713101884,-5.85510789717026,
36.6250638843976));
#72658=CARTESIAN_POINT('Ctrl Pts',(-5.14962157520898,-6.00583843649464,
36.6344438203726));
#72659=CARTESIAN_POINT('Ctrl Pts',(-5.09695560693799,-6.05059842956173,
36.6372609594777));
#72660=CARTESIAN_POINT('Ctrl Pts',(-5.00221372162009,-6.12900318537022,
36.6422543882455));
#72661=CARTESIAN_POINT('Ctrl Pts',(-4.96036807312028,-6.16291901613924,
36.6444347844668));
#72662=CARTESIAN_POINT('Ctrl Pts',(-4.89706276917497,-6.21316538043723,
36.6476967960334));
#72663=CARTESIAN_POINT('Ctrl Pts',(-4.87586083302529,-6.22981773039324,
36.6487832435795));
#72664=CARTESIAN_POINT('Ctrl Pts',(-4.83795351385324,-6.25927870439202,
36.65071513245));
#72665=CARTESIAN_POINT('Ctrl Pts',(-4.82128136953312,-6.27212962721198,
36.6515611920964));
#72666=CARTESIAN_POINT('Ctrl Pts',(-4.78778191385402,-6.29773858292842,
36.6532540584411));
#72667=CARTESIAN_POINT('Ctrl Pts',(-4.77095441421748,-6.31049608939397,
36.6541008521693));
#72668=CARTESIAN_POINT('Ctrl Pts',(-4.72459897977821,-6.34534833879061,
36.6564239019418));
#72669=CARTESIAN_POINT('Ctrl Pts',(-4.69496725366666,-6.36730426194092,
36.6578981769453));
#72670=CARTESIAN_POINT('Ctrl Pts',(-4.57583330360917,-6.45429395243304,
36.663784022659));
#72671=CARTESIAN_POINT('Ctrl Pts',(-4.4851241895155,-6.51765465868862,36.6681725628441));
#72672=CARTESIAN_POINT('Ctrl Pts',(-3.74574367023264,-7.01136771515209,
36.7032782935725));
#72673=CARTESIAN_POINT('Ctrl Pts',(-3.03806676371634,-7.34575600187266,
36.732945549065));
#72674=CARTESIAN_POINT('Ctrl Pts',(-1.90166291890524,-7.68991409795436,
36.777376187884));
#72675=CARTESIAN_POINT('Ctrl Pts',(-1.50175405456209,-7.77790532378213,
36.7925499150258));
#72676=CARTESIAN_POINT('Ctrl Pts',(-0.977021751312561,-7.85136875372685,
36.8130868687108));
#72677=CARTESIAN_POINT('Ctrl Pts',(-0.856820687275151,-7.86539380505291,
36.8178363282465));
#72678=CARTESIAN_POINT('Ctrl Pts',(-0.7187680762016,-7.87829964037159,36.8233787458573));
#72679=CARTESIAN_POINT('Ctrl Pts',(-0.701182318152164,-7.8798842708637,
36.8240863926316));
#72680=CARTESIAN_POINT('Ctrl Pts',(-0.674563346213154,-7.88219305855269,
36.8251601533033));
#72681=CARTESIAN_POINT('Ctrl Pts',(-0.665533894843102,-7.88296059576792,
36.8255248407219));
#72682=CARTESIAN_POINT('Ctrl Pts',(-0.649923053382483,-7.88426056284363,
36.8261561537298));
#72683=CARTESIAN_POINT('Ctrl Pts',(-0.643342268852679,-7.8848002715951,
36.8264225344935));
#72684=CARTESIAN_POINT('Ctrl Pts',(-0.629711658359943,-7.88590097846509,
36.8269748098343));
#72685=CARTESIAN_POINT('Ctrl Pts',(-0.622661742816073,-7.88646076313511,
36.827260745538));
#72686=CARTESIAN_POINT('Ctrl Pts',(-0.603487885387555,-7.8879573553563,
36.8280392260134));
#72687=CARTESIAN_POINT('Ctrl Pts',(-0.591362545437713,-7.88887566169215,
36.8285324123451));
#72688=CARTESIAN_POINT('Ctrl Pts',(-0.545793449416968,-7.89222116311333,
36.8303893394664));
#72689=CARTESIAN_POINT('Ctrl Pts',(-0.51233676863031,-7.89446365303272,
36.8317596663563));
#72690=CARTESIAN_POINT('Ctrl Pts',(0.0139043092441738,-7.92637649912327,
36.8534346627102));
#72691=CARTESIAN_POINT('Ctrl Pts',(0.508282527678121,-7.91006149081741,
36.8758468277803));
#72692=CARTESIAN_POINT('Ctrl Pts',(1.33548105221676,-7.80488833396626,36.9140470880228));
#72693=CARTESIAN_POINT('Ctrl Pts',(1.67004954912004,-7.74020295352098,36.9296744609613));
#72694=CARTESIAN_POINT('Ctrl Pts',(2.38254560718237,-7.55408498922569,36.9625481662131));
#72695=CARTESIAN_POINT('Ctrl Pts',(2.75764563159093,-7.42537343382496,36.9795830537459));
#72696=CARTESIAN_POINT('Ctrl Pts',(3.15019087989054,-7.25680294962654,36.9969552640543));
#72697=CARTESIAN_POINT('Ctrl Pts',(3.1787452105361,-7.24434058727828,36.9982165067383));
#72698=CARTESIAN_POINT('Ctrl Pts',(3.21810086301006,-7.22688656163997,36.9999515476662));
#72699=CARTESIAN_POINT('Ctrl Pts',(3.22896547211706,-7.22203880637441,37.0004301784889));
#72700=CARTESIAN_POINT('Ctrl Pts',(3.24727994271609,-7.21381735659886,37.0012364247012));
#72701=CARTESIAN_POINT('Ctrl Pts',(3.2547355669171,-7.21045659238659,37.0015644758173));
#72702=CARTESIAN_POINT('Ctrl Pts',(3.26947169811863,-7.20378648852256,37.0022125528971));
#72703=CARTESIAN_POINT('Ctrl Pts',(3.2767524233374,-7.20047765871258,37.0025325955344));
#72704=CARTESIAN_POINT('Ctrl Pts',(3.2927793837052,-7.19316463456151,37.0032367629342));
#72705=CARTESIAN_POINT('Ctrl Pts',(3.30152336496803,-7.1891555137647,37.0036207200573));
#72706=CARTESIAN_POINT('Ctrl Pts',(3.33198780519098,-7.17512024751193,37.0049576784032));
#72707=CARTESIAN_POINT('Ctrl Pts',(3.35367017867262,-7.16501148956461,37.005907867409));
#72708=CARTESIAN_POINT('Ctrl Pts',(3.57019680227172,-7.06286422342636,37.0153835412734));
#72709=CARTESIAN_POINT('Ctrl Pts',(3.76125634517662,-6.96299615427769,37.0236339609932));
#72710=CARTESIAN_POINT('Ctrl Pts',(4.26268021305892,-6.67422921724155,37.0451360617842));
#72711=CARTESIAN_POINT('Ctrl Pts',(4.56451194854539,-6.47155557089894,37.0578994980821));
#72712=CARTESIAN_POINT('Ctrl Pts',(5.17079297006981,-6.00086292009092,37.0842777138259));
#72713=CARTESIAN_POINT('Ctrl Pts',(5.47072712262579,-5.72875079511461,37.097785527289));
#72714=CARTESIAN_POINT('Ctrl Pts',(5.9356987084977,-5.23694767772726,37.1214768117619));
#72715=CARTESIAN_POINT('Ctrl Pts',(6.11249873253866,-5.02946118450261,37.1313008642115));
#72716=CARTESIAN_POINT('Ctrl Pts',(6.327701727509,-4.74876011100447,37.1449308537782));
#72717=CARTESIAN_POINT('Ctrl Pts',(6.37617175245921,-4.68347784265528,37.1481233235664));
#72718=CARTESIAN_POINT('Ctrl Pts',(6.42986051378105,-4.60878822328366,37.1518142236186));
#72719=CARTESIAN_POINT('Ctrl Pts',(6.43607797466473,-4.60010167449692,37.1522440617405));
#72720=CARTESIAN_POINT('Ctrl Pts',(6.44538314027623,-4.58704543285931,37.1528910338218));
#72721=CARTESIAN_POINT('Ctrl Pts',(6.44848405801431,-4.58268512788451,37.1531072502198));
#72722=CARTESIAN_POINT('Ctrl Pts',(6.45380562261194,-4.57518620034406,37.153479368757));
#72723=CARTESIAN_POINT('Ctrl Pts',(6.45602841310377,-4.57204909328216,37.1536351209302));
#72724=CARTESIAN_POINT('Ctrl Pts',(6.46059745470107,-4.565590658881,37.1539559381918));
#72725=CARTESIAN_POINT('Ctrl Pts',(6.46294343310752,-4.56226914117113,37.1541210223437));
#72726=CARTESIAN_POINT('Ctrl Pts',(6.46924034916175,-4.55333914504494,37.1545651029844));
#72727=CARTESIAN_POINT('Ctrl Pts',(6.47318654608231,-4.54772734495588,37.1548444343671));
#72728=CARTESIAN_POINT('Ctrl Pts',(6.48784316130739,-4.52682676658602,37.1558857742386));
#72729=CARTESIAN_POINT('Ctrl Pts',(6.49850656925911,-4.51150549233775,37.1566511454344));
#72730=CARTESIAN_POINT('Ctrl Pts',(6.67752892654667,-4.25233308400209,37.1696298435719));
#72731=CARTESIAN_POINT('Ctrl Pts',(6.83209651678353,-3.99926930485025,37.1827682456569));
#72732=CARTESIAN_POINT('Ctrl Pts',(6.97219703407295,-3.73796596650605,37.1962838440715));
#72733=CARTESIAN_POINT('Ctrl Pts',(6.97230129610631,-3.73777148646186,37.1962939032933));
#72734=CARTESIAN_POINT('Ctrl Pts',(6.97262284963992,-3.73717163216025,37.196324929889));
#72735=CARTESIAN_POINT('Ctrl Pts',(6.97284011393855,-3.73676624329022,37.1963458979422));
#72736=CARTESIAN_POINT('Ctrl Pts',(6.97349023387072,-3.7355529441025,37.1964086534861));
#72737=CARTESIAN_POINT('Ctrl Pts',(6.97392298441589,-3.73474497757456,37.1964504435833));
#72738=CARTESIAN_POINT('Ctrl Pts',(6.97515070243164,-3.73245181029339,37.1965690508874));
#72739=CARTESIAN_POINT('Ctrl Pts',(6.975945335761,-3.73096643113628,37.1966458763341));
#72740=CARTESIAN_POINT('Ctrl Pts',(6.97803306342754,-3.72706091912252,37.1968478698159));
#72741=CARTESIAN_POINT('Ctrl Pts',(6.97932537277535,-3.72464036788215,37.1969730570357));
#72742=CARTESIAN_POINT('Ctrl Pts',(6.98244828661375,-3.71878368326225,37.197275945453));
#72743=CARTESIAN_POINT('Ctrl Pts',(6.98427761372055,-3.71534687109722,37.1974536774068));
#72744=CARTESIAN_POINT('Ctrl Pts',(6.98840760384156,-3.70757390457266,37.1978556282583));
#72745=CARTESIAN_POINT('Ctrl Pts',(6.99070676893085,-3.70323695785707,37.1980798824442));
#72746=CARTESIAN_POINT('Ctrl Pts',(6.9956737490153,-3.69384656583093,37.1985654018961));
#72747=CARTESIAN_POINT('Ctrl Pts',(6.99834012750028,-3.68879236529416,37.1988267000539));
#72748=CARTESIAN_POINT('Ctrl Pts',(7.09853760436693,-3.4983653709777,37.2086706214829));
#72749=CARTESIAN_POINT('Ctrl Pts',(7.18867207167391,-3.30919744495289,37.2184108638924));
#72750=CARTESIAN_POINT('Ctrl Pts',(7.42387594751548,-2.76046832297191,37.2461611695393));
#72751=CARTESIAN_POINT('Ctrl Pts',(7.5501873876328,-2.39349687376259,37.2640956791124));
#72752=CARTESIAN_POINT('Ctrl Pts',(7.72519746143205,-1.73037139967677,37.2944864047326));
#72753=CARTESIAN_POINT('Ctrl Pts',(7.78493765322533,-1.43792689906373,37.3072370785531));
#72754=CARTESIAN_POINT('Ctrl Pts',(7.83472255011574,-1.09690173597895,37.3213121931983));
#72755=CARTESIAN_POINT('Ctrl Pts',(7.84101700906523,-1.05096299749347,37.3231921233004));
#72756=CARTESIAN_POINT('Ctrl Pts',(7.84862397292639,-0.991567114696946,
37.325602277619));
#72757=CARTESIAN_POINT('Ctrl Pts',(7.85030629853086,-0.97815879749513,37.3261450131621));
#72758=CARTESIAN_POINT('Ctrl Pts',(7.85293935211318,-0.956728688156941,
37.3270103149777));
#72759=CARTESIAN_POINT('Ctrl Pts',(7.85391216011091,-0.948709667132181,
37.3273336283052));
#72760=CARTESIAN_POINT('Ctrl Pts',(7.85572758983231,-0.933550600741194,
37.3279439169007));
#72761=CARTESIAN_POINT('Ctrl Pts',(7.85657276328813,-0.926410872849657,
37.3282309782548));
#72762=CARTESIAN_POINT('Ctrl Pts',(7.85845877543905,-0.910290290740692,
37.3288782778832));
#72763=CARTESIAN_POINT('Ctrl Pts',(7.85949395493788,-0.90130877713249,37.3292383243573));
#72764=CARTESIAN_POINT('Ctrl Pts',(7.86210176090017,-0.878336560303134,
37.3301577117613));
#72765=CARTESIAN_POINT('Ctrl Pts',(7.86365244365131,-0.864343369377637,
37.3307163101667));
#72766=CARTESIAN_POINT('Ctrl Pts',(7.87224717002346,-0.784847561057308,
37.333881650503));
#72767=CARTESIAN_POINT('Ctrl Pts',(7.87851022866422,-0.719262162811634,
37.3364619464332));
#72768=CARTESIAN_POINT('Ctrl Pts',(7.90622274111874,-0.384986669870525,
37.3494614982831));
#72769=CARTESIAN_POINT('Ctrl Pts',(7.91475029820828,-0.115395698033488,
37.3594383910394));
#72770=CARTESIAN_POINT('Ctrl Pts',(7.90730889460935,0.266494716771104,37.3730861339757));
#72771=CARTESIAN_POINT('Ctrl Pts',(7.902724692449,0.378809513161197,37.3770418158233));
#72772=CARTESIAN_POINT('Ctrl Pts',(7.86503777196913,0.984863040936311,37.3981674873349));
#72773=CARTESIAN_POINT('Ctrl Pts',(7.78806062932387,1.47474085886958,37.4143735496396));
#72774=CARTESIAN_POINT('Ctrl Pts',(7.61829376074975,2.14069080753604,37.4382137105358));
#72775=CARTESIAN_POINT('Ctrl Pts',(7.56396759940108,2.3253698243664,37.4450375592331));
#72776=CARTESIAN_POINT('Ctrl Pts',(7.46876937846004,2.61018017457105,37.4561509423528));
#72777=CARTESIAN_POINT('Ctrl Pts',(7.43248632296349,2.71177098691488,37.4602354730277));
#72778=CARTESIAN_POINT('Ctrl Pts',(7.3751840495486,2.86241571094123,37.466518585957));
#72779=CARTESIAN_POINT('Ctrl Pts',(7.35572630425045,2.91205318346399,37.4686261773634));
#72780=CARTESIAN_POINT('Ctrl Pts',(7.33235245901648,2.9699514643652,37.4711327028303));
#72781=CARTESIAN_POINT('Ctrl Pts',(7.32892150652308,2.97840793608622,37.471500009864));
#72782=CARTESIAN_POINT('Ctrl Pts',(7.32365096332777,2.99133430620729,37.4720633483097));
#72783=CARTESIAN_POINT('Ctrl Pts',(7.32182189549999,2.99580848759161,37.4722586816354));
#72784=CARTESIAN_POINT('Ctrl Pts',(7.31847889903726,3.00396462247884,37.4726153907883));
#72785=CARTESIAN_POINT('Ctrl Pts',(7.31696629110291,3.0076471108665,37.4727766786994));
#72786=CARTESIAN_POINT('Ctrl Pts',(7.31366084912057,3.0156770547789,37.4731288871527));
#72787=CARTESIAN_POINT('Ctrl Pts',(7.31186691807611,3.02002405401504,37.4733198797862));
#72788=CARTESIAN_POINT('Ctrl Pts',(7.30696380538713,3.03187515003108,37.4738414588666));
#72789=CARTESIAN_POINT('Ctrl Pts',(7.3038469483573,3.03937604330163,37.4741725456504));
#72790=CARTESIAN_POINT('Ctrl Pts',(7.28883813553353,3.07533919333979,37.4757645286633));
#72791=CARTESIAN_POINT('Ctrl Pts',(7.27679148092318,3.10373616961389,37.4770353625158));
#72792=CARTESIAN_POINT('Ctrl Pts',(7.07535160434235,3.57096068311142,37.4981635576092));
#72793=CARTESIAN_POINT('Ctrl Pts',(6.84675556793272,3.99176758181895,37.5203402564296));
#72794=CARTESIAN_POINT('Ctrl Pts',(6.3350477932549,4.75905313849894,37.5636009822948));
#72795=CARTESIAN_POINT('Ctrl Pts',(6.05774103805619,5.1073709989602,37.5845651512568));
#72796=CARTESIAN_POINT('Ctrl Pts',(5.62558359873539,5.56515836500273,37.6129417402302));
#72797=CARTESIAN_POINT('Ctrl Pts',(5.49383972766374,5.69525323599682,37.6211234290596));
#72798=CARTESIAN_POINT('Ctrl Pts',(5.21152947102894,5.95510883183441,37.6376769920443));
#72799=CARTESIAN_POINT('Ctrl Pts',(5.06039269599592,6.08406067721272,37.6460129329371));
#72800=CARTESIAN_POINT('Ctrl Pts',(4.87539563984146,6.23023429828023,37.655620932466));
#72801=CARTESIAN_POINT('Ctrl Pts',(4.8460745922381,6.25306829916386,37.6571268088175));
#72802=CARTESIAN_POINT('Ctrl Pts',(4.80674229040214,6.28325582515507,37.6591246006389));
#72803=CARTESIAN_POINT('Ctrl Pts',(4.79687330466832,6.29079340874685,37.6596240213283));
#72804=CARTESIAN_POINT('Ctrl Pts',(4.78057658281538,6.30317962294404,37.660445684369));
#72805=CARTESIAN_POINT('Ctrl Pts',(4.77415913811843,6.30804172050976,37.6607684727417));
#72806=CARTESIAN_POINT('Ctrl Pts',(4.76166388616725,6.31747860329622,37.6613954702727));
#72807=CARTESIAN_POINT('Ctrl Pts',(4.75558688224872,6.32205443457652,37.6616997215624));
#72808=CARTESIAN_POINT('Ctrl Pts',(4.741475206544,6.33264831157299,37.6624046519201));
#72809=CARTESIAN_POINT('Ctrl Pts',(4.73343565318888,6.33865984971924,37.6628050688354));
#72810=CARTESIAN_POINT('Ctrl Pts',(4.70738845261501,6.35805933180136,37.6640985472136));
#72811=CARTESIAN_POINT('Ctrl Pts',(4.68933520595172,6.37138602249232,37.6649891545291));
#72812=CARTESIAN_POINT('Ctrl Pts',(4.5165353143801,6.49781253596613,37.6734581690479));
#72813=CARTESIAN_POINT('Ctrl Pts',(4.35777801693759,6.60533389271473,37.6808129086014));
#72814=CARTESIAN_POINT('Ctrl Pts',(4.02580875454984,6.81298283822459,37.6954447855455));
#72815=CARTESIAN_POINT('Ctrl Pts',(3.85239241672874,6.91252117236997,37.7026996592549));
#72816=CARTESIAN_POINT('Ctrl Pts',(3.1690638887644,7.27103044348587,37.7301567660788));
#72817=CARTESIAN_POINT('Ctrl Pts',(2.63546796499408,7.4809829268591,37.7491358755223));
#72818=CARTESIAN_POINT('Ctrl Pts',(1.84284387199572,7.69742191377548,37.7786343112821));
#72819=CARTESIAN_POINT('Ctrl Pts',(1.59877442321255,7.75179336408153,37.7879179371882));
#72820=CARTESIAN_POINT('Ctrl Pts',(1.31271264063229,7.80143193160307,37.7993850180541));
#72821=CARTESIAN_POINT('Ctrl Pts',(1.27283731290128,7.80803686924428,37.8009949538998));
#72822=CARTESIAN_POINT('Ctrl Pts',(1.22150517506652,7.81613584198696,37.8030809497118));
#72823=CARTESIAN_POINT('Ctrl Pts',(1.21009281712895,7.81791083123741,37.8035455727699));
#72824=CARTESIAN_POINT('Ctrl Pts',(1.19170420479502,7.82072962361312,37.8042955578566));
#72825=CARTESIAN_POINT('Ctrl Pts',(1.18473034454057,7.82178910273695,37.8045802997195));
#72826=CARTESIAN_POINT('Ctrl Pts',(1.17145011824583,7.82378848603372,37.8051231117874));
#72827=CARTESIAN_POINT('Ctrl Pts',(1.16514401170046,7.82473009665043,37.8053811154658));
#72828=CARTESIAN_POINT('Ctrl Pts',(1.15077189851091,7.82685834203353,37.8059696865679));
#72829=CARTESIAN_POINT('Ctrl Pts',(1.14270518907462,7.82804013268324,37.8063004389156));
#72830=CARTESIAN_POINT('Ctrl Pts',(1.11812834011462,7.83160189644056,37.8073093428725));
#72831=CARTESIAN_POINT('Ctrl Pts',(1.10161254513154,7.83394211393584,37.8079889821348));
#72832=CARTESIAN_POINT('Ctrl Pts',(0.981284226205531,7.85060408025789,37.8129521209237));
#72833=CARTESIAN_POINT('Ctrl Pts',(0.877206057646947,7.86291368243202,37.8173073258085));
#72834=CARTESIAN_POINT('Ctrl Pts',(0.165300409073685,7.9328023279853,37.8474142774084));
#72835=CARTESIAN_POINT('Ctrl Pts',(-0.447177677043078,7.92191436211371,
37.8747144257888));
#72836=CARTESIAN_POINT('Ctrl Pts',(-1.45498545193957,7.78665596903055,37.9186810360124));
#72837=CARTESIAN_POINT('Ctrl Pts',(-1.85292262537028,7.70166909409274,37.935827409712));
#72838=CARTESIAN_POINT('Ctrl Pts',(-2.31424785378348,7.56529983021761,37.9554636589941));
#72839=CARTESIAN_POINT('Ctrl Pts',(-2.38560331190508,7.54310292125155,37.9584952241123));
#72840=CARTESIAN_POINT('Ctrl Pts',(-2.47952628870685,7.51241974066353,37.9624804137584));
#72841=CARTESIAN_POINT('Ctrl Pts',(-2.50238419490923,7.50483672871961,37.9634498564228));
#72842=CARTESIAN_POINT('Ctrl Pts',(-2.53950473785945,7.49233370169141,37.9650234837776));
#72843=CARTESIAN_POINT('Ctrl Pts',(-2.5537885076299,7.48747706983161,37.965628833108));
#72844=CARTESIAN_POINT('Ctrl Pts',(-2.5812243836107,7.47806094149906,37.9667912346238));
#72845=CARTESIAN_POINT('Ctrl Pts',(-2.59437851638697,7.47350753518694,37.9673483987745));
#72846=CARTESIAN_POINT('Ctrl Pts',(-2.62444733879125,7.4630100228967,37.9686216682976));
#72847=CARTESIAN_POINT('Ctrl Pts',(-2.64135399337032,7.4570430815986,37.9693373344421));
#72848=CARTESIAN_POINT('Ctrl Pts',(-2.6945126484634,7.43807809402771,37.971586781919));
#72849=CARTESIAN_POINT('Ctrl Pts',(-2.73069024673419,7.42487272307073,37.9731165129498));
#72850=CARTESIAN_POINT('Ctrl Pts',(-3.06857350668557,7.29873665335821,37.9873931792002));
#72851=CARTESIAN_POINT('Ctrl Pts',(-3.36322139417798,7.16773735584352,37.9997455489935));
#72852=CARTESIAN_POINT('Ctrl Pts',(-4.01889341894382,6.8268694930818,38.0273770435127));
#72853=CARTESIAN_POINT('Ctrl Pts',(-4.3729357496788,6.60568592943777,38.0423877387682));
#72854=CARTESIAN_POINT('Ctrl Pts',(-4.81192342978387,6.28061038744971,38.0623321942736));
#72855=CARTESIAN_POINT('Ctrl Pts',(-4.91403457858747,6.20104324498531,38.0670794218106));
#72856=CARTESIAN_POINT('Ctrl Pts',(-5.19402001982697,5.9716125917231,38.0805124594735));
#72857=CARTESIAN_POINT('Ctrl Pts',(-5.367298804267,5.81636430251224,38.089314051897));
#72858=CARTESIAN_POINT('Ctrl Pts',(-5.54980628846175,5.63773830033998,38.0994248920202));
#72859=CARTESIAN_POINT('Ctrl Pts',(-5.56606478973794,5.62168708880586,38.100333339442));
#72860=CARTESIAN_POINT('Ctrl Pts',(-5.59429185564068,5.59357741334053,38.1019245335957));
#72861=CARTESIAN_POINT('Ctrl Pts',(-5.60629157875211,5.58155035566258,38.1026054321085));
#72862=CARTESIAN_POINT('Ctrl Pts',(-5.62359539843265,5.56409502004858,38.1035939305795));
#72863=CARTESIAN_POINT('Ctrl Pts',(-5.62893062517671,5.55869756451686,38.1038996284192));
#72864=CARTESIAN_POINT('Ctrl Pts',(-5.6382192634132,5.54927350026747,38.1044334679941));
#72865=CARTESIAN_POINT('Ctrl Pts',(-5.64217615507197,5.54525031698269,38.1046613939001));
#72866=CARTESIAN_POINT('Ctrl Pts',(-5.64980555553745,5.53747647755059,38.1051018659463));
#72867=CARTESIAN_POINT('Ctrl Pts',(-5.6534786442269,5.53372639131168,38.1053143756318));
#72868=CARTESIAN_POINT('Ctrl Pts',(-5.66216759438751,5.52483761735602,38.1058181552082));
#72869=CARTESIAN_POINT('Ctrl Pts',(-5.66718019036322,5.5196957574207,38.1061096309926));
#72870=CARTESIAN_POINT('Ctrl Pts',(-5.68208549734059,5.50436436779795,38.1069789106145));
#72871=CARTESIAN_POINT('Ctrl Pts',(-5.69195774024892,5.49415505529739,38.1075580232018));
#72872=CARTESIAN_POINT('Ctrl Pts',(-5.80536627073424,5.37624065898127,38.114250229616));
#72873=CARTESIAN_POINT('Ctrl Pts',(-5.90584783122677,5.26566175736592,38.1205733151838));
#72874=CARTESIAN_POINT('Ctrl Pts',(-6.00725855969204,5.14750481089611,38.1273280416066));
#72875=CARTESIAN_POINT('Ctrl Pts',(-6.01138117532429,5.14268971899392,38.1276033021788));
#72876=CARTESIAN_POINT('Ctrl Pts',(-6.54229996296318,4.52108171887196,38.1631370246617));
#72877=CARTESIAN_POINT('Ctrl Pts',(-6.97113206028465,3.82692971621161,38.2021659090481));
#72878=CARTESIAN_POINT('Ctrl Pts',(-7.37820212491066,2.86373938765046,38.2483028712294));
#72879=CARTESIAN_POINT('Ctrl Pts',(-7.45981795345878,2.64386030629179,38.2583949191294));
#72880=CARTESIAN_POINT('Ctrl Pts',(-7.56606917200836,2.31327539743514,38.272894775682));
#72881=CARTESIAN_POINT('Ctrl Pts',(-7.5982857282647,2.20515330447075,38.2775342975795));
#72882=CARTESIAN_POINT('Ctrl Pts',(-7.63318322867374,2.07817017892457,38.2828665581275));
#72883=CARTESIAN_POINT('Ctrl Pts',(-7.63812144861313,2.05994617343988,38.2836290445919));
#72884=CARTESIAN_POINT('Ctrl Pts',(-7.64555621822489,2.03211457481,38.2847893109544));
#72885=CARTESIAN_POINT('Ctrl Pts',(-7.64809999080462,2.02251973111002,38.2851885488024));
#72886=CARTESIAN_POINT('Ctrl Pts',(-7.65249116304121,2.00582994042879,38.2858816897108));
#72887=CARTESIAN_POINT('Ctrl Pts',(-7.654346768445,1.99873717609292,38.2861758457201));
#72888=CARTESIAN_POINT('Ctrl Pts',(-7.6581929341286,1.98395189469187,38.2867881747528));
#72889=CARTESIAN_POINT('Ctrl Pts',(-7.66018177058015,1.97625893519164,38.2871062943631));
#72890=CARTESIAN_POINT('Ctrl Pts',(-7.66561639185071,1.95510597598861,38.2879796914495));
#72891=CARTESIAN_POINT('Ctrl Pts',(-7.66903831985326,1.94163984698425,38.288534233441));
#72892=CARTESIAN_POINT('Ctrl Pts',(-7.68211621208046,1.88960116864405,38.2906715810454));
#72893=CARTESIAN_POINT('Ctrl Pts',(-7.69151685916195,1.85096475753186,38.2922465283114));
#72894=CARTESIAN_POINT('Ctrl Pts',(-7.84039088122147,1.21837123857555,38.3178426403182));
#72895=CARTESIAN_POINT('Ctrl Pts',(-7.91099079599388,0.610306051304702,
38.3395066691258));
#72896=CARTESIAN_POINT('Ctrl Pts',(-7.91100981824995,-0.65091673621086,
38.3831754832856));
#72897=CARTESIAN_POINT('Ctrl Pts',(-7.83065472643843,-1.29943978580713,
38.4050395380097));
#72898=CARTESIAN_POINT('Ctrl Pts',(-7.66160866396208,-1.97114432808144,
38.4323189790172));
#72899=CARTESIAN_POINT('Ctrl Pts',(-7.6511201427678,-2.01147153957299,38.4339741085834));
#72900=CARTESIAN_POINT('Ctrl Pts',(-7.63707579532795,-2.06377085953423,
38.4361416128402));
#72901=CARTESIAN_POINT('Ctrl Pts',(-7.63380940543998,-2.07582051811485,
38.436642456131));
#72902=CARTESIAN_POINT('Ctrl Pts',(-7.62855366735773,-2.09502867411696,
38.437443112728));
#72903=CARTESIAN_POINT('Ctrl Pts',(-7.62658272644618,-2.10219221703006,
38.4377422163453));
#72904=CARTESIAN_POINT('Ctrl Pts',(-7.62301986472479,-2.11507076418925,
38.4382808376318));
#72905=CARTESIAN_POINT('Ctrl Pts',(-7.62143159967058,-2.12078678014625,
38.4385202170476));
#72906=CARTESIAN_POINT('Ctrl Pts',(-7.61769773513827,-2.13416624191905,
38.4390812678936));
#72907=CARTESIAN_POINT('Ctrl Pts',(-7.61554700086746,-2.14182823986773,
38.4394031300336));
#72908=CARTESIAN_POINT('Ctrl Pts',(-7.60933793479913,-2.1638204684871,38.4403285732887));
#72909=CARTESIAN_POINT('Ctrl Pts',(-7.60525070176967,-2.17814246218283,
38.4409332049806));
#72910=CARTESIAN_POINT('Ctrl Pts',(-7.5780187615719,-2.27255422395595,38.444931552894));
#72911=CARTESIAN_POINT('Ctrl Pts',(-7.55365013972952,-2.35228401521999,
38.4483677745479));
#72912=CARTESIAN_POINT('Ctrl Pts',(-7.46994773376024,-2.61141824179472,
38.4597034060154));
#72913=CARTESIAN_POINT('Ctrl Pts',(-7.40544689783887,-2.78908175963155,
38.4677380148503));
#72914=CARTESIAN_POINT('Ctrl Pts',(-7.07771495103241,-3.60000882275987,
38.5052547123691));
#72915=CARTESIAN_POINT('Ctrl Pts',(-6.73918001943477,-4.19972462246992,
38.5350422230333));
#72916=CARTESIAN_POINT('Ctrl Pts',(-6.3101459695669,-4.77145896535504,38.5647594968143));
#72917=CARTESIAN_POINT('Ctrl Pts',(-6.29260390016519,-4.79456973868993,
38.5659639729351));
#72918=CARTESIAN_POINT('Ctrl Pts',(-6.13163730855142,-5.00422980959778,
38.5769217729587));
#72919=CARTESIAN_POINT('Ctrl Pts',(-5.98008222606419,-5.18439110800345,
38.5865565243785));
#72920=CARTESIAN_POINT('Ctrl Pts',(-5.76715154438655,-5.41573087583818,
38.5993752439367));
#72921=CARTESIAN_POINT('Ctrl Pts',(-5.71271275145341,-5.47312442421492,
38.6025942331002));
#72922=CARTESIAN_POINT('Ctrl Pts',(-5.59876785020851,-5.58970133406722,
38.6092122347445));
#72923=CARTESIAN_POINT('Ctrl Pts',(-5.53916212488614,-5.64877380785448,
38.61260986032));
#72924=CARTESIAN_POINT('Ctrl Pts',(-5.45461804362853,-5.72993636330983,
38.6173404197055));
#72925=CARTESIAN_POINT('Ctrl Pts',(-5.43046318661462,-5.75283393794001,
38.6186821565142));
#72926=CARTESIAN_POINT('Ctrl Pts',(-5.38824152429984,-5.79235504464503,
38.6210105346445));
#72927=CARTESIAN_POINT('Ctrl Pts',(-5.3702405230033,-5.80904815063089,38.6219979609916));
#72928=CARTESIAN_POINT('Ctrl Pts',(-5.33244069181307,-5.84377570419608,
38.6240604986701));
#72929=CARTESIAN_POINT('Ctrl Pts',(-5.31262739089202,-5.86179395947277,
38.6251354101817));
#72930=CARTESIAN_POINT('Ctrl Pts',(-5.26518294675502,-5.90450188944251,
38.6276947288119));
#72931=CARTESIAN_POINT('Ctrl Pts',(-5.23746904751534,-5.9290987523724,38.6291780093822));
#72932=CARTESIAN_POINT('Ctrl Pts',(-5.14197421867869,-6.01266107032881,
38.6342494938536));
#72933=CARTESIAN_POINT('Ctrl Pts',(-5.07336189055058,-6.07066646584998,
38.6378258484435));
#72934=CARTESIAN_POINT('Ctrl Pts',(-4.66993674814903,-6.40010784396557,
38.6584800837229));
#72935=CARTESIAN_POINT('Ctrl Pts',(-4.31437351420493,-6.6449892785218,38.6751810864711));
#72936=CARTESIAN_POINT('Ctrl Pts',(-3.59709648633883,-7.05703758469521,
38.7071584296001));
#72937=CARTESIAN_POINT('Ctrl Pts',(-3.23923220006731,-7.22829439386741,
38.7224061508348));
#72938=CARTESIAN_POINT('Ctrl Pts',(-2.82921270399289,-7.38792244027133,
38.7399332964247));
#72939=CARTESIAN_POINT('Ctrl Pts',(-2.78823298177557,-7.40348561816221,
38.741685928633));
#72940=CARTESIAN_POINT('Ctrl Pts',(-2.73262559852371,-7.42407687466456,
38.744066908039));
#72941=CARTESIAN_POINT('Ctrl Pts',(-2.71810921980288,-7.42940390404958,
38.7446887179512));
#72942=CARTESIAN_POINT('Ctrl Pts',(-2.69351667987478,-7.43834682553775,
38.745742655039));
#72943=CARTESIAN_POINT('Ctrl Pts',(-2.68344860948487,-7.44198489391061,
38.7461742774308));
#72944=CARTESIAN_POINT('Ctrl Pts',(-2.66405480154881,-7.44894831780974,
38.7470060113369));
#72945=CARTESIAN_POINT('Ctrl Pts',(-2.65473014235097,-7.45227662514535,
38.7474060530876));
#72946=CARTESIAN_POINT('Ctrl Pts',(-2.63272172823744,-7.46008567351715,
38.7483506071761));
#72947=CARTESIAN_POINT('Ctrl Pts',(-2.62003275830467,-7.46455158052007,
38.7488954724963));
#72948=CARTESIAN_POINT('Ctrl Pts',(-2.58138292288528,-7.47804377127799,
38.7505560620547));
#72949=CARTESIAN_POINT('Ctrl Pts',(-2.55538651510466,-7.48696708801213,
38.7516743561389));
#72950=CARTESIAN_POINT('Ctrl Pts',(-2.49446155000433,-7.50752542002795,
38.7542978521915));
#72951=CARTESIAN_POINT('Ctrl Pts',(-2.45949725145354,-7.51905243999628,
38.7558054904453));
#72952=CARTESIAN_POINT('Ctrl Pts',(-2.03578699504226,-7.65546948224984,
38.7740938095676));
#72953=CARTESIAN_POINT('Ctrl Pts',(-1.63802077000728,-7.75032395030728,
38.7914140914641));
#72954=CARTESIAN_POINT('Ctrl Pts',(-0.799431495454176,-7.88283181723932,
38.8271765843557));
#72955=CARTESIAN_POINT('Ctrl Pts',(-0.359141497706395,-7.91512309858168,
38.8455247451218));
#72956=CARTESIAN_POINT('Ctrl Pts',(0.127468642125678,-7.91010625107164,
38.8652725906629));
#72957=CARTESIAN_POINT('Ctrl Pts',(0.173376079523153,-7.90923320736555,
38.8671309885941));
#72958=CARTESIAN_POINT('Ctrl Pts',(0.247188518586936,-7.90718652134299,
38.87011209305));
#72959=CARTESIAN_POINT('Ctrl Pts',(0.27509930536438,-7.90626468233021,38.8712377493657));
#72960=CARTESIAN_POINT('Ctrl Pts',(0.324810799355717,-7.90435924976712,
38.8732399593243));
#72961=CARTESIAN_POINT('Ctrl Pts',(0.346613392718665,-7.90343320111091,
38.8741171750243));
#72962=CARTESIAN_POINT('Ctrl Pts',(0.392247566746003,-7.90130572876317,
38.8759514151218));
#72963=CARTESIAN_POINT('Ctrl Pts',(0.416078115186704,-7.90008666913056,
38.8769082272354));
#72964=CARTESIAN_POINT('Ctrl Pts',(0.478584092498757,-7.89660554587436,
38.8794153169725));
#72965=CARTESIAN_POINT('Ctrl Pts',(0.517249127963761,-7.89416716568477,
38.8809635752767));
#72966=CARTESIAN_POINT('Ctrl Pts',(0.697259648302866,-7.88148673556538,
38.8881611271639));
#72967=CARTESIAN_POINT('Ctrl Pts',(0.838332627271029,-7.86773178126254,
38.8937709018608));
#72968=CARTESIAN_POINT('Ctrl Pts',(1.62086629443244,-7.77014564311123,38.9248228976185));
#72969=CARTESIAN_POINT('Ctrl Pts',(2.25056849685423,-7.61166110748908,38.9496646258324));
#72970=CARTESIAN_POINT('Ctrl Pts',(3.31629040743672,-7.19943698053501,38.9925746549227));
#72971=CARTESIAN_POINT('Ctrl Pts',(3.76078971416224,-6.97754230099519,39.0108153383814));
#72972=CARTESIAN_POINT('Ctrl Pts',(4.27592054176512,-6.65678418947294,39.0342895664285));
#72973=CARTESIAN_POINT('Ctrl Pts',(4.36901202842072,-6.5960598147054,39.0386371732951));
#72974=CARTESIAN_POINT('Ctrl Pts',(4.48590999772952,-6.51624566575718,39.0442635493966));
#72975=CARTESIAN_POINT('Ctrl Pts',(4.51092946896942,-6.4989507910021,39.0454777228118));
#72976=CARTESIAN_POINT('Ctrl Pts',(4.54540417469726,-6.47482493360941,39.0471653183678));
#72977=CARTESIAN_POINT('Ctrl Pts',(4.55494512125043,-6.46811657076956,39.0476339187399));
#72978=CARTESIAN_POINT('Ctrl Pts',(4.57017156110797,-6.45736026657286,39.04838429675));
#72979=CARTESIAN_POINT('Ctrl Pts',(4.57586661147937,-6.4533258451668,39.0486655251054));
#72980=CARTESIAN_POINT('Ctrl Pts',(4.58757192078579,-6.44501042061869,39.0492447323563));
#72981=CARTESIAN_POINT('Ctrl Pts',(4.59358154196227,-6.44072853543507,39.0495427476473));
#72982=CARTESIAN_POINT('Ctrl Pts',(4.60749773194266,-6.43078379608512,39.0502343605096));
#72983=CARTESIAN_POINT('Ctrl Pts',(4.61539985797929,-6.42511476409802,39.0506282189203));
#72984=CARTESIAN_POINT('Ctrl Pts',(4.64032673271211,-6.40716236233438,39.0518742716282));
#72985=CARTESIAN_POINT('Ctrl Pts',(4.65731297294972,-6.39482584480044,39.0527287701526));
#72986=CARTESIAN_POINT('Ctrl Pts',(5.06805475228453,-6.09401375459001,39.0735265391759));
#72987=CARTESIAN_POINT('Ctrl Pts',(5.43422506600703,-5.76984843082238,39.095541584117));
#72988=CARTESIAN_POINT('Ctrl Pts',(6.27603840056216,-4.87299267831161,39.1518462263429));
#72989=CARTESIAN_POINT('Ctrl Pts',(6.7053796374883,-4.26297575916533,39.1857209588094));
#72990=CARTESIAN_POINT('Ctrl Pts',(7.06390711950271,-3.56190465030219,39.2179138693967));
#72991=CARTESIAN_POINT('Ctrl Pts',(7.08406663873472,-3.52164002632757,39.219743014043));
#72992=CARTESIAN_POINT('Ctrl Pts',(7.11016576216679,-3.4683811466781,39.2221367142375));
#72993=CARTESIAN_POINT('Ctrl Pts',(7.11641530227057,-3.45554021716885,39.2227118875952));
#72994=CARTESIAN_POINT('Ctrl Pts',(7.12603771020939,-3.43563223722311,39.2236005934681));
#72995=CARTESIAN_POINT('Ctrl Pts',(7.12943489874847,-3.42857701411655,39.2239149585747));
#72996=CARTESIAN_POINT('Ctrl Pts',(7.1361987940855,-3.41447634986946,39.2245420880664));
#72997=CARTESIAN_POINT('Ctrl Pts',(7.1395655560033,-3.40743094493573,39.2248548541176));
#72998=CARTESIAN_POINT('Ctrl Pts',(7.14703424237991,-3.39174204113685,39.2255500443789));
#72999=CARTESIAN_POINT('Ctrl Pts',(7.15113093226423,-3.38309605624769,39.2259322892975));
#73000=CARTESIAN_POINT('Ctrl Pts',(7.16299062105289,-3.35794861834376,39.2270415649767));
#73001=CARTESIAN_POINT('Ctrl Pts',(7.17071228216737,-3.3414276788144,39.2277671830755));
#73002=CARTESIAN_POINT('Ctrl Pts',(7.22457569450785,-3.22513720968939,39.2328529280268));
#73003=CARTESIAN_POINT('Ctrl Pts',(7.2686917478937,-3.12444002289568,39.2371436477149));
#73004=CARTESIAN_POINT('Ctrl Pts',(7.39980491508323,-2.80734608739438,39.2503238604886));
#73005=CARTESIAN_POINT('Ctrl Pts',(7.47934402141128,-2.5879967734711,39.2589641881539));
#73006=CARTESIAN_POINT('Ctrl Pts',(7.77487786782445,-1.64482940394179,39.2945515432749));
#73007=CARTESIAN_POINT('Ctrl Pts',(7.89631324499339,-0.895688255920419,
39.3186354178186));
#73008=CARTESIAN_POINT('Ctrl Pts',(7.91113426286729,-0.0628401258798168,
39.3486620262958));
#73009=CARTESIAN_POINT('Ctrl Pts',(7.91136941031116,0.0150931128500409,
39.3515068206282));
#73010=CARTESIAN_POINT('Ctrl Pts',(7.90914645800753,0.204142758367049,39.3585170221932));
#73011=CARTESIAN_POINT('Ctrl Pts',(7.90549825472322,0.315226201816551,39.3627277977289));
#73012=CARTESIAN_POINT('Ctrl Pts',(7.89757202801532,0.46213966515205,39.3684572545262));
#73013=CARTESIAN_POINT('Ctrl Pts',(7.89538725358157,0.498073340249719,39.3698713652257));
#73014=CARTESIAN_POINT('Ctrl Pts',(7.89109160886784,0.561567634263152,39.3723943908811));
#73015=CARTESIAN_POINT('Ctrl Pts',(7.88908139998445,0.589134633937439,39.3734979116748));
#73016=CARTESIAN_POINT('Ctrl Pts',(7.88629302747159,0.62479547187006,39.3749365247286));
#73017=CARTESIAN_POINT('Ctrl Pts',(7.88564677399291,0.632899716942392,39.375264204287));
#73018=CARTESIAN_POINT('Ctrl Pts',(7.8846378211372,0.645310863453291,39.3757671792674));
#73019=CARTESIAN_POINT('Ctrl Pts',(7.88428408135613,0.649618507527592,39.3759419641523));
#73020=CARTESIAN_POINT('Ctrl Pts',(7.88361246630713,0.657715700628144,39.3762709156675));
#73021=CARTESIAN_POINT('Ctrl Pts',(7.88329538817588,0.661505317019026,39.3764250365274));
#73022=CARTESIAN_POINT('Ctrl Pts',(7.88257593252306,0.670030037517674,39.376772107259));
#73023=CARTESIAN_POINT('Ctrl Pts',(7.88217202098633,0.674765006913782,39.3769651456983));
#73024=CARTESIAN_POINT('Ctrl Pts',(7.88106023655268,0.687661000316005,39.3774916169928));
#73025=CARTESIAN_POINT('Ctrl Pts',(7.88034395449867,0.695821285819502,39.3778255399807));
#73026=CARTESIAN_POINT('Ctrl Pts',(7.8765539268322,0.73824286118144,39.3795655905216));
#73027=CARTESIAN_POINT('Ctrl Pts',(7.87326946013208,0.772484446792259,39.3809841316718));
#73028=CARTESIAN_POINT('Ctrl Pts',(7.83713095376385,1.12503233668865,39.3957251190699));
#73029=CARTESIAN_POINT('Ctrl Pts',(7.78521805078241,1.44106340421453,39.4100707466557));
#73030=CARTESIAN_POINT('Ctrl Pts',(7.5223260687658,2.59792238958884,39.464524897215));
#73031=CARTESIAN_POINT('Ctrl Pts',(7.19275528358834,3.40581461046731,39.5055529444607));
#73032=CARTESIAN_POINT('Ctrl Pts',(6.71077311124079,4.18954426720153,39.5432300339242));
#73033=CARTESIAN_POINT('Ctrl Pts',(6.68241863323018,4.23462374758903,39.545392731348));
#73034=CARTESIAN_POINT('Ctrl Pts',(6.64587770808624,4.29143738712001,39.5481130923226));
#73035=CARTESIAN_POINT('Ctrl Pts',(6.63811208384724,4.30343970838252,39.5486874884755));
#73036=CARTESIAN_POINT('Ctrl Pts',(6.62576606730168,4.32240841766777,39.5495948113172));
#73037=CARTESIAN_POINT('Ctrl Pts',(6.62120714166934,4.32938869766044,39.5499285963988));
#73038=CARTESIAN_POINT('Ctrl Pts',(6.61271057487117,4.34235318326565,39.5505483533919));
#73039=CARTESIAN_POINT('Ctrl Pts',(6.60877582624161,4.34833926851263,39.5508344408915));
#73040=CARTESIAN_POINT('Ctrl Pts',(6.60005359349936,4.36156955246328,39.5514665857459));
#73041=CARTESIAN_POINT('Ctrl Pts',(6.59526229891212,4.36881123502164,39.551812489324));
#73042=CARTESIAN_POINT('Ctrl Pts',(6.58145961970992,4.38959849654459,39.5528051104522));
#73043=CARTESIAN_POINT('Ctrl Pts',(6.57241833435402,4.4031242236997,39.5534506213828));
#73044=CARTESIAN_POINT('Ctrl Pts',(6.51272632871377,4.49182972058001,39.5576817870158));
#73045=CARTESIAN_POINT('Ctrl Pts',(6.46082734931513,4.56616350572395,39.5612165434991));
#73046=CARTESIAN_POINT('Ctrl Pts',(6.30558089509436,4.78057178786957,39.5713907791924));
#73047=CARTESIAN_POINT('Ctrl Pts',(6.19887275518761,4.91814986443986,39.5778906434871));
#73048=CARTESIAN_POINT('Ctrl Pts',(6.01702912271833,5.13726878629127,39.5882628498776));
#73049=CARTESIAN_POINT('Ctrl Pts',(5.94456923086756,5.22094508997288,39.5922292224447));
#73050=CARTESIAN_POINT('Ctrl Pts',(5.81646868286776,5.36274930153257,39.5989861327818));
#73051=CARTESIAN_POINT('Ctrl Pts',(5.76165398796227,5.42159862186811,39.6018013091954));
#73052=CARTESIAN_POINT('Ctrl Pts',(5.35593444996822,5.84407739244176,39.6221418083102));
#73053=CARTESIAN_POINT('Ctrl Pts',(4.97182155525041,6.17415844202331,39.6386593473583));
#73054=CARTESIAN_POINT('Ctrl Pts',(4.35320216799812,6.61036154238549,39.6650441185029));
#73055=CARTESIAN_POINT('Ctrl Pts',(4.14074875590315,6.74547490770903,39.6740908337311));
#73056=CARTESIAN_POINT('Ctrl Pts',(3.85337036410591,6.90954020288023,39.6867981478361));
#73057=CARTESIAN_POINT('Ctrl Pts',(3.78392091849768,6.94781624956217,39.6899038310327));
#73058=CARTESIAN_POINT('Ctrl Pts',(3.70424046642362,6.99018193638044,39.6935200671318));
#73059=CARTESIAN_POINT('Ctrl Pts',(3.69456013274496,6.99530316425914,39.6939602836247));
#73060=CARTESIAN_POINT('Ctrl Pts',(3.68025209831515,7.0028346201805,39.6946122945205));
#73061=CARTESIAN_POINT('Ctrl Pts',(3.67563259059131,7.00526040083783,39.6948230111966));
#73062=CARTESIAN_POINT('Ctrl Pts',(3.66741284780572,7.00956635607492,39.6951983216982));
#73063=CARTESIAN_POINT('Ctrl Pts',(3.66381359176345,7.01144831408973,39.6953627881956));
#73064=CARTESIAN_POINT('Ctrl Pts',(3.6562974809123,7.01537092655476,39.6957064934848));
#73065=CARTESIAN_POINT('Ctrl Pts',(3.65238036448886,7.01741107382281,39.6958857669346));
#73066=CARTESIAN_POINT('Ctrl Pts',(3.6423227292759,7.0226386780009,39.6963464447277));
#73067=CARTESIAN_POINT('Ctrl Pts',(3.63617974540995,7.02582135585667,39.696628173266));
#73068=CARTESIAN_POINT('Ctrl Pts',(3.61066492203174,7.03899815116564,39.6977997830988));
#73069=CARTESIAN_POINT('Ctrl Pts',(3.59125616343564,7.04892015142095,39.6986944826849));
#73070=CARTESIAN_POINT('Ctrl Pts',(3.54126602492629,7.07421568141801,39.7010073182057));
#73071=CARTESIAN_POINT('Ctrl Pts',(3.51062568772735,7.08947105061343,39.7024329640918));
#73072=CARTESIAN_POINT('Ctrl Pts',(3.38406902279584,7.15146011751771,39.7083513555607));
#73073=CARTESIAN_POINT('Ctrl Pts',(3.28731438915655,7.19644823614337,39.7129463705618));
#73074=CARTESIAN_POINT('Ctrl Pts',(2.90152686785163,7.36642493136792,39.7314548387959));
#73075=CARTESIAN_POINT('Ctrl Pts',(2.60606280460498,7.47606096161805,39.7460290344763));
#73076=CARTESIAN_POINT('Ctrl Pts',(1.67352074052255,7.76007921745206,39.7916666038562));
#73077=CARTESIAN_POINT('Ctrl Pts',(1.02047861694388,7.87263359857287,39.822867946901));
#73078=CARTESIAN_POINT('Ctrl Pts',(0.140654800042331,7.91282452431211,39.8608984824239));
#73079=CARTESIAN_POINT('Ctrl Pts',(-0.080028247656927,7.91367058139126,
39.8701365449494));
#73080=CARTESIAN_POINT('Ctrl Pts',(-0.32147299899154,7.90449351925316,39.8799270859024));
#73081=CARTESIAN_POINT('Ctrl Pts',(-0.342470980685254,7.90361159986924,
39.8807759610251));
#73082=CARTESIAN_POINT('Ctrl Pts',(-0.37360047820906,7.90217986517778,39.8820306278958));
#73083=CARTESIAN_POINT('Ctrl Pts',(-0.383734765081152,7.90169422149441,
39.8824384921223));
#73084=CARTESIAN_POINT('Ctrl Pts',(-0.401061400542074,7.90083050222642,
39.8831348076947));
#73085=CARTESIAN_POINT('Ctrl Pts',(-0.408254206519649,7.90046209883756,
39.8834235709902));
#73086=CARTESIAN_POINT('Ctrl Pts',(-0.422229421657502,7.89972717570526,
39.8839840453006));
#73087=CARTESIAN_POINT('Ctrl Pts',(-0.429011880851549,7.89936174266642,
39.8842557911373));
#73088=CARTESIAN_POINT('Ctrl Pts',(-0.445205350891899,7.89846833513182,
39.8849039714005));
#73089=CARTESIAN_POINT('Ctrl Pts',(-0.454615915161151,7.89793227471796,
39.8852801448721));
#73090=CARTESIAN_POINT('Ctrl Pts',(-0.482725710398447,7.89628063032873,
39.8864022930131));
#73091=CARTESIAN_POINT('Ctrl Pts',(-0.50142202161738,7.8951154435487,39.8871466701851));
#73092=CARTESIAN_POINT('Ctrl Pts',(-0.660017048269538,7.88466589658636,
39.8934444269884));
#73093=CARTESIAN_POINT('Ctrl Pts',(-0.799654037753729,7.87173009599693,
39.8988793234973));
#73094=CARTESIAN_POINT('Ctrl Pts',(-1.29594959264021,7.81241045480591,39.9178655120552));
#73095=CARTESIAN_POINT('Ctrl Pts',(-1.64970937858002,7.74543260241374,39.9307648251475));
#73096=CARTESIAN_POINT('Ctrl Pts',(-2.06719586534866,7.63647698437656,39.9458506606912));
#73097=CARTESIAN_POINT('Ctrl Pts',(-2.13644083943982,7.61739457547457,39.9483491978771));
#73098=CARTESIAN_POINT('Ctrl Pts',(-2.26330029100403,7.58056895227552,39.9529303291083));
#73099=CARTESIAN_POINT('Ctrl Pts',(-2.32099010376022,7.56310510427093,39.9550150525149));
#73100=CARTESIAN_POINT('Ctrl Pts',(-2.42793927787715,7.52939052916617,39.9588891968728));
#73101=CARTESIAN_POINT('Ctrl Pts',(-2.47724921620078,7.5133113341546,39.9606791450338));
#73102=CARTESIAN_POINT('Ctrl Pts',(-2.56941876738174,7.48225027809897,39.9640364348168));
#73103=CARTESIAN_POINT('Ctrl Pts',(-2.61231441930413,7.46738209783918,39.9656036477097));
#73104=CARTESIAN_POINT('Ctrl Pts',(-2.69302041430844,7.43862784895288,39.9685644075401));
#73105=CARTESIAN_POINT('Ctrl Pts',(-2.73085730750169,7.42482064315305,39.9699575570814));
#73106=CARTESIAN_POINT('Ctrl Pts',(-2.80250055328276,7.39805530521667,39.9726074176593));
#73107=CARTESIAN_POINT('Ctrl Pts',(-2.83632661821765,7.38515287272247,39.9738636446431));
#73108=CARTESIAN_POINT('Ctrl Pts',(-3.22675793843371,7.23315075950918,39.9884331377066));
#73109=CARTESIAN_POINT('Ctrl Pts',(-3.57288412273344,7.06858542733107,40.0020100056435));
#73110=CARTESIAN_POINT('Ctrl Pts',(-3.96260347854693,6.84733336084427,40.0194769653508));
#73111=CARTESIAN_POINT('Ctrl Pts',(-4.01908862889808,6.8143324478534,40.0220645152471));
#73112=CARTESIAN_POINT('Ctrl Pts',(-4.0862775477239,6.7739519591715,40.0252048793601));
#73113=CARTESIAN_POINT('Ctrl Pts',(-4.09738183142048,6.76724105282791,40.0257259528498));
#73114=CARTESIAN_POINT('Ctrl Pts',(-4.11544395846612,6.75626439923794,40.0265768461123));
#73115=CARTESIAN_POINT('Ctrl Pts',(-4.12241182559444,6.75201513233165,40.0269059046806));
#73116=CARTESIAN_POINT('Ctrl Pts',(-4.13481246030258,6.74442640890183,40.027492952359));
#73117=CARTESIAN_POINT('Ctrl Pts',(-4.14024779589585,6.74109114722834,40.0277507510214));
#73118=CARTESIAN_POINT('Ctrl Pts',(-4.15156223827328,6.7341294683586,40.0282884084115));
#73119=CARTESIAN_POINT('Ctrl Pts',(-4.15744063867017,6.73050191667929,40.0285683178254));
#73120=CARTESIAN_POINT('Ctrl Pts',(-4.17276437549087,6.72101792729627,40.0292994588515));
#73121=CARTESIAN_POINT('Ctrl Pts',(-4.18220211739188,6.71514928799971,40.0297512280887));
#73122=CARTESIAN_POINT('Ctrl Pts',(-4.20285800854994,6.7022444684399,40.0307431666832));
#73123=CARTESIAN_POINT('Ctrl Pts',(-4.21407091010389,6.69519997586373,40.0312836929362));
#73124=CARTESIAN_POINT('Ctrl Pts',(-4.24697253341932,6.67441417092408,40.032875705267));
#73125=CARTESIAN_POINT('Ctrl Pts',(-4.26861200189376,6.66059545265817,40.0339304175673));
#73126=CARTESIAN_POINT('Ctrl Pts',(-4.34366651095584,6.61215051031579,40.037614434611));
#73127=CARTESIAN_POINT('Ctrl Pts',(-4.39672995577182,6.57698552383581,40.040264820952));
#73128=CARTESIAN_POINT('Ctrl Pts',(-4.60177473636943,6.43751253821415,40.050672428993));
#73129=CARTESIAN_POINT('Ctrl Pts',(-4.75051304195258,6.32854804558949,40.0585814619191));
#73130=CARTESIAN_POINT('Ctrl Pts',(-5.2521752520448,5.93337663253643,40.0862706967208));
#73131=CARTESIAN_POINT('Ctrl Pts',(-5.5841705389251,5.62204211675794,40.1063700147992));
#73132=CARTESIAN_POINT('Ctrl Pts',(-6.09332178049453,5.05472091788597,40.1392739320605));
#73133=CARTESIAN_POINT('Ctrl Pts',(-6.28547614589442,4.81368657991219,40.1523293518545));
#73134=CARTESIAN_POINT('Ctrl Pts',(-6.47508990065234,4.54505934433498,40.1659285153721));
#73135=CARTESIAN_POINT('Ctrl Pts',(-6.48701799195423,4.52801846750245,40.1667873749137));
#73136=CARTESIAN_POINT('Ctrl Pts',(-6.56904353959225,4.40984460804113,40.1727170855935));
#73137=CARTESIAN_POINT('Ctrl Pts',(-6.63684131314007,4.30713371889715,40.1777381154848));
#73138=CARTESIAN_POINT('Ctrl Pts',(-6.71694103290499,4.17940094962973,40.1838310159566));
#73139=CARTESIAN_POINT('Ctrl Pts',(-6.73154193568581,4.15584315369801,40.1849485897316));
#73140=CARTESIAN_POINT('Ctrl Pts',(-6.75518160095659,4.11725032742334,40.1867693960527));
#73141=CARTESIAN_POINT('Ctrl Pts',(-6.76429466236532,4.10226113797595,40.187474132729));
#73142=CARTESIAN_POINT('Ctrl Pts',(-6.78050365021546,4.07539967935176,40.1887326768995));
#73143=CARTESIAN_POINT('Ctrl Pts',(-6.78761843187343,4.06353889138136,40.1892868718717));
#73144=CARTESIAN_POINT('Ctrl Pts',(-6.80261145565194,4.0383953346864,40.1904584890285));
#73145=CARTESIAN_POINT('Ctrl Pts',(-6.81048198537449,4.02510802646178,40.1910757485691));
#73146=CARTESIAN_POINT('Ctrl Pts',(-6.83133596730885,3.9896653153138,40.1927172077337));
#73147=CARTESIAN_POINT('Ctrl Pts',(-6.84425056567696,3.96746954998603,40.1937399508534));
#73148=CARTESIAN_POINT('Ctrl Pts',(-6.90468869961299,3.86242378662305,40.1985558008823));
#73149=CARTESIAN_POINT('Ctrl Pts',(-6.95081788858602,3.77877952729895,40.2023187916375));
#73150=CARTESIAN_POINT('Ctrl Pts',(-7.22342233810574,3.26258616503966,40.2251173770489));
#73151=CARTESIAN_POINT('Ctrl Pts',(-7.41096919416746,2.81067056843982,40.2431829927566));
#73152=CARTESIAN_POINT('Ctrl Pts',(-7.6606742474745,2.0058822105014,40.2738934044646));
#73153=CARTESIAN_POINT('Ctrl Pts',(-7.74282301829315,1.66077419386668,40.2866601413561));
#73154=CARTESIAN_POINT('Ctrl Pts',(-7.80776906374627,1.27438878554553,40.3013395267461));
#73155=CARTESIAN_POINT('Ctrl Pts',(-7.81371652344107,1.23739992954977,40.3027488926121));
#73156=CARTESIAN_POINT('Ctrl Pts',(-7.82365348426069,1.17266901230708,40.3052242941165));
#73157=CARTESIAN_POINT('Ctrl Pts',(-7.82775872736925,1.14494530162478,40.3062873651171));
#73158=CARTESIAN_POINT('Ctrl Pts',(-7.83595384321674,1.08749650566718,40.3084971332476));
#73159=CARTESIAN_POINT('Ctrl Pts',(-7.8400220911903,1.05776881672722,40.3096444161343));
#73160=CARTESIAN_POINT('Ctrl Pts',(-7.84592396866892,1.01273670555742,40.3113889521385));
#73161=CARTESIAN_POINT('Ctrl Pts',(-7.84788216963856,0.997448748038592,
40.3119823562326));
#73162=CARTESIAN_POINT('Ctrl Pts',(-7.86215888453117,0.883343266028346,
40.3164205382333));
#73163=CARTESIAN_POINT('Ctrl Pts',(-7.87265492056882,0.784309288593359,
40.3203236668393));
#73164=CARTESIAN_POINT('Ctrl Pts',(-7.88257497961383,0.67019163305026,40.3249046720238));
#73165=CARTESIAN_POINT('Ctrl Pts',(-7.88382915718263,0.65527318748757,40.3255051784838));
#73166=CARTESIAN_POINT('Ctrl Pts',(-7.88562425964197,0.633168983982901,
40.3263974670674));
#73167=CARTESIAN_POINT('Ctrl Pts',(-7.88619773057843,0.625985846685082,
40.3266878280719));
#73168=CARTESIAN_POINT('Ctrl Pts',(-7.88719826268721,0.613233853971028,
40.3272040154966));
#73169=CARTESIAN_POINT('Ctrl Pts',(-7.8876292428401,0.607665304134125,40.3274296678775));
#73170=CARTESIAN_POINT('Ctrl Pts',(-7.88844853387981,0.596931785115121,
40.3278650948511));
#73171=CARTESIAN_POINT('Ctrl Pts',(-7.88883767020609,0.591766880364478,
40.3280748322352));
#73172=CARTESIAN_POINT('Ctrl Pts',(-7.88966549891312,0.5806333884767,40.3285274079213));
#73173=CARTESIAN_POINT('Ctrl Pts',(-7.89010249109803,0.57466468154663,40.3287703233468));
#73174=CARTESIAN_POINT('Ctrl Pts',(-7.89114115045964,0.560253497163474,
40.3293575387927));
#73175=CARTESIAN_POINT('Ctrl Pts',(-7.89173604169649,0.551810551625998,
40.3297021506095));
#73176=CARTESIAN_POINT('Ctrl Pts',(-7.89330297783959,0.529051045923306,
40.3306327295443));
#73177=CARTESIAN_POINT('Ctrl Pts',(-7.8942496179195,0.514732818828182,40.3312198875157));
#73178=CARTESIAN_POINT('Ctrl Pts',(-7.90572984560547,0.333605723165124,
40.3386701185946));
#73179=CARTESIAN_POINT('Ctrl Pts',(-7.9110123521574,0.166522693952854,40.3457953989745));
#73180=CARTESIAN_POINT('Ctrl Pts',(-7.91099997831229,-0.000585784094123132,
40.3531019614398));
#73181=CARTESIAN_POINT('',(-7.90825726396148,0.00539299807561528,42.3576680289075));
#73182=CARTESIAN_POINT('Ctrl Pts',(-7.91892560419408,-0.000477670393038393,
40.3576684917631));
#73183=CARTESIAN_POINT('Ctrl Pts',(-7.9047553262244,-2.46403417491885,40.4571955913693));
#73184=CARTESIAN_POINT('Ctrl Pts',(-6.01794529465323,-6.22621325369113,
40.6096439579526));
#73185=CARTESIAN_POINT('Ctrl Pts',(-1.09061100011871,-8.16228612049071,
40.8150135915134));
#73186=CARTESIAN_POINT('Ctrl Pts',(2.94220442931933,-7.7101370801012,40.9737773924446));
#73187=CARTESIAN_POINT('Ctrl Pts',(6.25649344662756,-5.35431747772407,41.1325411933765));
#73188=CARTESIAN_POINT('Ctrl Pts',(8.70421013023098,-0.493722870432395,
41.3442262612849));
#73189=CARTESIAN_POINT('Ctrl Pts',(6.60205231354672,6.62635550641215,41.608832596171));
#73190=CARTESIAN_POINT('Ctrl Pts',(-2.01662681621539,9.14104728615634,41.9263601980336));
#73191=CARTESIAN_POINT('Ctrl Pts',(-7.29947900301956,4.51893018671728,42.1759720089462));
#73192=CARTESIAN_POINT('Ctrl Pts',(-7.91185655759119,0.949470213429403,
42.319741285904));
#73193=CARTESIAN_POINT('Ctrl Pts',(-7.90825726396148,0.00539299807561528,
42.3576680289075));
#73194=CARTESIAN_POINT('',(-7.91099872614571,-0.004489423238615,44.3576684917631));
#73195=CARTESIAN_POINT('Ctrl Pts',(-7.91099816834962,0.00538334179892528,
42.3576684917631));
#73196=CARTESIAN_POINT('Ctrl Pts',(-7.91113024696707,-0.18871053886295,
42.3654632149619));
#73197=CARTESIAN_POINT('Ctrl Pts',(-7.9041150552579,-0.382973778850431,
42.3732579381608));
#73198=CARTESIAN_POINT('Ctrl Pts',(-7.8899419111821,-0.576834151357323,
42.3810526613597));
#73199=CARTESIAN_POINT('Ctrl Pts',(-7.87685079500157,-0.755894538080088,
42.3882523078493));
#73200=CARTESIAN_POINT('Ctrl Pts',(-7.85765347124877,-0.934610951447137,
42.3954519543389));
#73201=CARTESIAN_POINT('Ctrl Pts',(-7.83238104679367,-1.11253230866672,
42.4026516008285));
#73202=CARTESIAN_POINT('Ctrl Pts',(-7.80466487664022,-1.3076579729809,42.4105474252875));
#73203=CARTESIAN_POINT('Ctrl Pts',(-7.76965417934316,-1.50173723265223,
42.4184432497465));
#73204=CARTESIAN_POINT('Ctrl Pts',(-7.72745945464938,-1.69419342955575,
42.4263390742055));
#73205=CARTESIAN_POINT('Ctrl Pts',(-7.68525522192022,-1.88669299397369,
42.4342366778864));
#73206=CARTESIAN_POINT('Ctrl Pts',(-7.63586380877042,-2.07756843230082,
42.4421342815673));
#73207=CARTESIAN_POINT('Ctrl Pts',(-7.57944638287488,-2.26625539803548,
42.4500318852482));
#73208=CARTESIAN_POINT('Ctrl Pts',(-7.52300695240184,-2.45501595764461,
42.4579325692439));
#73209=CARTESIAN_POINT('Ctrl Pts',(-7.45953614592364,-2.64158601582986,
42.4658332532396));
#73210=CARTESIAN_POINT('Ctrl Pts',(-7.38924442052067,-2.82541818034147,
42.4737339372353));
#73211=CARTESIAN_POINT('Ctrl Pts',(-7.31887553032036,-3.00945215198811,
42.481643294438));
#73212=CARTESIAN_POINT('Ctrl Pts',(-7.24167088411708,-3.19074190532464,
42.4895526516406));
#73213=CARTESIAN_POINT('Ctrl Pts',(-7.15788884657419,-3.36876064155481,
42.4974620088432));
#73214=CARTESIAN_POINT('Ctrl Pts',(-7.07405692569699,-3.5468853690976,42.5053760752308));
#73215=CARTESIAN_POINT('Ctrl Pts',(-6.98363996176963,-3.72173489275421,
42.5132901416184));
#73216=CARTESIAN_POINT('Ctrl Pts',(-6.88694154181228,-3.89280839493293,
42.521204208006));
#73217=CARTESIAN_POINT('Ctrl Pts',(-6.79010815352162,-4.06412067563019,
42.5291293205756));
#73218=CARTESIAN_POINT('Ctrl Pts',(-6.68697596968834,-4.23164611266594,
42.5370544331452));
#73219=CARTESIAN_POINT('Ctrl Pts',(-6.57789179660735,-4.39491302668503,
42.5449795457148));
#73220=CARTESIAN_POINT('Ctrl Pts',(-6.50248206794155,-4.50777920459647,
42.5504581643966));
#73221=CARTESIAN_POINT('Ctrl Pts',(-6.42422879901295,-4.61861091326156,
42.5559367830783));
#73222=CARTESIAN_POINT('Ctrl Pts',(-6.34325741845261,-4.72726203242912,
42.56141540176));
#73223=CARTESIAN_POINT('Ctrl Pts',(-6.22317456187274,-4.88839472733875,
42.5695403488321));
#73224=CARTESIAN_POINT('Ctrl Pts',(-6.09684859963159,-5.04508340046696,
42.5776652959043));
#73225=CARTESIAN_POINT('Ctrl Pts',(-5.96463392833433,-5.19683202547118,
42.5857902429765));
#73226=CARTESIAN_POINT('Ctrl Pts',(-5.83253577703048,-5.34844691532628,
42.5939080295817));
#73227=CARTESIAN_POINT('Ctrl Pts',(-5.69455947321675,-5.49513019650033,
42.6020258161869));
#73228=CARTESIAN_POINT('Ctrl Pts',(-5.55110078110194,-5.63641740097816,
42.6101436027922));
#73229=CARTESIAN_POINT('Ctrl Pts',(-5.40774811398311,-5.77760018532595,
42.6182553898426));
#73230=CARTESIAN_POINT('Ctrl Pts',(-5.25892136528683,-5.91339462065451,
42.6263671768929));
#73231=CARTESIAN_POINT('Ctrl Pts',(-5.10505477600203,-6.04337130532444,
42.6344789639433));
#73232=CARTESIAN_POINT('Ctrl Pts',(-4.95128004829302,-6.17327039119191,
42.642585908087));
#73233=CARTESIAN_POINT('Ctrl Pts',(-4.79247172446257,-6.29735844626082,
42.6506928522306));
#73234=CARTESIAN_POINT('Ctrl Pts',(-4.62909933209039,-6.4152443736494,42.6587997963743));
#73235=CARTESIAN_POINT('Ctrl Pts',(-4.46580129601439,-6.53307664716902,
42.6669030507737));
#73236=CARTESIAN_POINT('Ctrl Pts',(-4.2979435938005,-6.6447122353955,42.6750063051732));
#73237=CARTESIAN_POINT('Ctrl Pts',(-4.12602757531319,-6.74980128950143,
42.6831095595726));
#73238=CARTESIAN_POINT('Ctrl Pts',(-3.95291345593058,-6.8556227203278,42.691269286408));
#73239=CARTESIAN_POINT('Ctrl Pts',(-3.77568449598357,-6.95480581642194,
42.6994290132435));
#73240=CARTESIAN_POINT('Ctrl Pts',(-3.5948819093796,-7.04703803435282,42.7075887400789));
#73241=CARTESIAN_POINT('Ctrl Pts',(-3.41539852283936,-7.13859729317367,
42.7156889306413));
#73242=CARTESIAN_POINT('Ctrl Pts',(-3.23239378349034,-7.22330663852351,
42.7237891212037));
#73243=CARTESIAN_POINT('Ctrl Pts',(-3.04642167655107,-7.30090651690869,
42.7318893117661));
#73244=CARTESIAN_POINT('Ctrl Pts',(-2.86045067859473,-7.37850593255275,
42.7399894540257));
#73245=CARTESIAN_POINT('Ctrl Pts',(-2.67151264429676,-7.4489958424245,42.7480895962853));
#73246=CARTESIAN_POINT('Ctrl Pts',(-2.48018164408593,-7.51216480199544,
42.7561897385449));
#73247=CARTESIAN_POINT('Ctrl Pts',(-2.28882710835914,-7.57534153194366,
42.7642908771983));
#73248=CARTESIAN_POINT('Ctrl Pts',(-2.09507932430806,-7.6311954156024,42.7723920158517));
#73249=CARTESIAN_POINT('Ctrl Pts',(-1.89952815504884,-7.67956468741404,
42.7804931545052));
#73250=CARTESIAN_POINT('Ctrl Pts',(-1.70149032427789,-7.72854903100981,
42.7886973085983));
#73251=CARTESIAN_POINT('Ctrl Pts',(-1.50160325697955,-7.76985702428737,
42.7969014626915));
#73252=CARTESIAN_POINT('Ctrl Pts',(-1.30049100326436,-7.8033738953371,42.8051056167846));
#73253=CARTESIAN_POINT('Ctrl Pts',(-1.10171483656257,-7.83650143990004,
42.813214472767));
#73254=CARTESIAN_POINT('Ctrl Pts',(-0.901742118956392,-7.86201788206749,
42.8213233287494));
#73255=CARTESIAN_POINT('Ctrl Pts',(-0.701181595934555,-7.87986455273964,
42.8294321847318));
#73256=CARTESIAN_POINT('Ctrl Pts',(-0.497085486823625,-7.89802583388256,
42.8376839878803));
#73257=CARTESIAN_POINT('Ctrl Pts',(-0.292381002291157,-7.90824438756082,
42.8459357910288));
#73258=CARTESIAN_POINT('Ctrl Pts',(-0.0877110389684923,-7.91051374903319,
42.8541875941774));
#73259=CARTESIAN_POINT('Ctrl Pts',(0.116958924354173,-7.91278311050555,
42.8624393973259));
#73260=CARTESIAN_POINT('Ctrl Pts',(0.321594019388287,-7.90710331561421,
42.8706912004744));
#73261=CARTESIAN_POINT('Ctrl Pts',(0.525555155170245,-7.89352347047084,
42.878943003623));
#73262=CARTESIAN_POINT('Ctrl Pts',(0.719080167925258,-7.88063846816632,
42.8867725849962));
#73263=CARTESIAN_POINT('Ctrl Pts',(0.912368204998893,-7.86061641127412,
42.8946021663694));
#73264=CARTESIAN_POINT('Ctrl Pts',(1.10484707557039,-7.83346883185244,42.9024317477426));
#73265=CARTESIAN_POINT('Ctrl Pts',(1.29716368498403,-7.80634413804753,42.9102547287189));
#73266=CARTESIAN_POINT('Ctrl Pts',(1.48867213996247,-7.77210593107621,42.9180777096951));
#73267=CARTESIAN_POINT('Ctrl Pts',(1.6788026931358,-7.73081771338065,42.9259006906714));
#73268=CARTESIAN_POINT('Ctrl Pts',(1.86880650906592,-7.68955701758938,42.9337184570043));
#73269=CARTESIAN_POINT('Ctrl Pts',(2.05743390983847,-7.64125574449681,42.9415362233372));
#73270=CARTESIAN_POINT('Ctrl Pts',(2.24412254296994,-7.58602893562463,42.94935398967));
#73271=CARTESIAN_POINT('Ctrl Pts',(2.43072169798444,-7.53082859644576,42.9571680090205));
#73272=CARTESIAN_POINT('Ctrl Pts',(2.61538359950324,-7.46870943292098,42.964982028371));
#73273=CARTESIAN_POINT('Ctrl Pts',(2.79755815857188,-7.3998371164106,42.9727960477216));
#73274=CARTESIAN_POINT('Ctrl Pts',(2.97967965849695,-7.33098485926607,42.9806077912045));
#73275=CARTESIAN_POINT('Ctrl Pts',(3.15931493044627,-7.25538349241912,42.9884195346874));
#73276=CARTESIAN_POINT('Ctrl Pts',(3.33593090555019,-7.1732479389322,42.9962312781704));
#73277=CARTESIAN_POINT('Ctrl Pts',(3.51255675900827,-7.09110779150023,43.0040434585739));
#73278=CARTESIAN_POINT('Ctrl Pts',(3.68616265629164,-7.00243286991442,43.0118556389775));
#73279=CARTESIAN_POINT('Ctrl Pts',(3.85623690647469,-6.90748564393315,43.0196678193811));
#73280=CARTESIAN_POINT('Ctrl Pts',(3.98714218169645,-6.83440525266143,43.025680814439));
#73281=CARTESIAN_POINT('Ctrl Pts',(4.11595559747919,-6.75760994234814,43.0316938094968));
#73282=CARTESIAN_POINT('Ctrl Pts',(4.24245425707339,-6.67723766812593,43.0377068045546));
#73283=CARTESIAN_POINT('Ctrl Pts',(4.42421058285637,-6.56175684560724,43.0463464209123));
#73284=CARTESIAN_POINT('Ctrl Pts',(4.60110107446976,-6.43894548806574,43.0549860372701));
#73285=CARTESIAN_POINT('Ctrl Pts',(4.77257691221894,-6.30923375830653,43.0636256536278));
#73286=CARTESIAN_POINT('Ctrl Pts',(4.9443366844956,-6.17930724820753,43.0722795757059));
#73287=CARTESIAN_POINT('Ctrl Pts',(5.11066369807891,-6.04245766591505,43.0809334977841));
#73288=CARTESIAN_POINT('Ctrl Pts',(5.27104270752504,-5.89915500520601,43.0895874198622));
#73289=CARTESIAN_POINT('Ctrl Pts',(5.43611063166046,-5.75166268181521,43.0984943519975));
#73290=CARTESIAN_POINT('Ctrl Pts',(5.59487731685527,-5.59733445716044,43.1074012841328));
#73291=CARTESIAN_POINT('Ctrl Pts',(5.74682357947842,-5.43672141518681,43.1163082162681));
#73292=CARTESIAN_POINT('Ctrl Pts',(5.89494638410779,-5.28014991532575,43.1249910212661));
#73293=CARTESIAN_POINT('Ctrl Pts',(6.0365877411356,-5.11760625487598,43.133673826264));
#73294=CARTESIAN_POINT('Ctrl Pts',(6.17130825003054,-4.94963387364207,43.142356631262));
#73295=CARTESIAN_POINT('Ctrl Pts',(6.3112450206072,-4.77515774696507,43.151375626966));
#73296=CARTESIAN_POINT('Ctrl Pts',(6.44371419150937,-4.59482438808266,43.16039462267));
#73297=CARTESIAN_POINT('Ctrl Pts',(6.56827233633681,-4.40927652973962,43.169413618374));
#73298=CARTESIAN_POINT('Ctrl Pts',(6.69283048116424,-4.22372867139657,43.1784326140779));
#73299=CARTESIAN_POINT('Ctrl Pts',(6.80947747298286,-4.03296655902076,43.1874516097819));
#73300=CARTESIAN_POINT('Ctrl Pts',(6.91782181590263,-3.83766365428521,43.1964706054859));
#73301=CARTESIAN_POINT('Ctrl Pts',(7.01779401935553,-3.65745247573178,43.2047926724177));
#73302=CARTESIAN_POINT('Ctrl Pts',(7.11078183195034,-3.47322237723703,43.2131147393495));
#73303=CARTESIAN_POINT('Ctrl Pts',(7.1964719594793,-3.28553075414432,43.2214368062813));
#73304=CARTESIAN_POINT('Ctrl Pts',(7.28208606784707,-3.09800563984513,43.2297514903726));
#73305=CARTESIAN_POINT('Ctrl Pts',(7.36041528523218,-2.9070253920006,43.2380661744638));
#73306=CARTESIAN_POINT('Ctrl Pts',(7.43119251262743,-2.71317136212772,43.2463808585551));
#73307=CARTESIAN_POINT('Ctrl Pts',(7.5019112625629,-2.51947749805468,43.2546886728999));
#73308=CARTESIAN_POINT('Ctrl Pts',(7.56509037036864,-2.32291486264367,43.2629964872447));
#73309=CARTESIAN_POINT('Ctrl Pts',(7.62051076398834,-2.12408490789278,43.2713043015896));
#73310=CARTESIAN_POINT('Ctrl Pts',(7.6758754314067,-1.92545488023311,43.2796037622779));
#73311=CARTESIAN_POINT('Ctrl Pts',(7.72349687879767,-1.72456236487494,43.2879032229661));
#73312=CARTESIAN_POINT('Ctrl Pts',(7.76320568484589,-1.52202447246304,43.2962026836544));
#73313=CARTESIAN_POINT('Ctrl Pts',(7.80288919504733,-1.31961560350977,43.3044968573067));
#73314=CARTESIAN_POINT('Ctrl Pts',(7.83467006217641,-1.11556373440944,43.312791030959));
#73315=CARTESIAN_POINT('Ctrl Pts',(7.8584295011605,-0.910498091865268,43.3210852046113));
#73316=CARTESIAN_POINT('Ctrl Pts',(7.88217139453547,-0.705583883940912,
43.3293732532735));
#73317=CARTESIAN_POINT('Ctrl Pts',(7.89790364856776,-0.499657686565649,
43.3376613019357));
#73318=CARTESIAN_POINT('Ctrl Pts',(7.90555899679994,-0.29335635005154,43.3459493505979));
#73319=CARTESIAN_POINT('Ctrl Pts',(7.90841774512349,-0.216316928457862,
43.3490443692045));
#73320=CARTESIAN_POINT('Ctrl Pts',(7.91015067683777,-0.139225261458094,
43.3521393878111));
#73321=CARTESIAN_POINT('Ctrl Pts',(7.91075614355395,-0.0621147102014839,
43.3552344064177));
#73322=CARTESIAN_POINT('Ctrl Pts',(7.9123413244539,0.139769505344386,43.3633375180322));
#73323=CARTESIAN_POINT('Ctrl Pts',(7.9061938450066,0.341698587564988,43.3714406296467));
#73324=CARTESIAN_POINT('Ctrl Pts',(7.89233854919701,0.543059135692251,43.3795437412613));
#73325=CARTESIAN_POINT('Ctrl Pts',(7.87848019615452,0.744464114923822,43.3876486408636));
#73326=CARTESIAN_POINT('Ctrl Pts',(7.85691065662277,0.945299991786688,43.3957535404659));
#73327=CARTESIAN_POINT('Ctrl Pts',(7.82770671799616,1.14495787566083,43.4038584400682));
#73328=CARTESIAN_POINT('Ctrl Pts',(7.7984926778759,1.34468482018025,43.411966143114));
#73329=CARTESIAN_POINT('Ctrl Pts',(7.76163901810054,1.54323264372335,43.4200738461598));
#73330=CARTESIAN_POINT('Ctrl Pts',(7.71727386240876,1.74000147487945,43.4281815492056));
#73331=CARTESIAN_POINT('Ctrl Pts',(7.67286879729545,1.936947312745,43.436296545672));
#73332=CARTESIAN_POINT('Ctrl Pts',(7.62093880373944,2.13211064900299,43.4444115421383));
#73333=CARTESIAN_POINT('Ctrl Pts',(7.5616625759656,2.32490431786801,43.4525265386047));
#73334=CARTESIAN_POINT('Ctrl Pts',(7.50235740918861,2.51779210973645,43.4606454968601));
#73335=CARTESIAN_POINT('Ctrl Pts',(7.43569895437681,2.70830762408483,43.4687644551155));
#73336=CARTESIAN_POINT('Ctrl Pts',(7.3619148464566,2.89588169536014,43.4768834133708));
#73337=CARTESIAN_POINT('Ctrl Pts',(7.28805172311064,3.08365663977086,43.4850110662213));
#73338=CARTESIAN_POINT('Ctrl Pts',(7.20704782178509,3.26848355272822,43.4931387190718));
#73339=CARTESIAN_POINT('Ctrl Pts',(7.11917829022251,3.44981470111432,43.5012663719223));
#73340=CARTESIAN_POINT('Ctrl Pts',(7.07329622826837,3.54449879509452,43.5055103170645));
#73341=CARTESIAN_POINT('Ctrl Pts',(7.02554299595123,3.63823017154937,43.5097542622068));
#73342=CARTESIAN_POINT('Ctrl Pts',(6.97596260869761,3.73093375471247,43.513998207349));
#73343=CARTESIAN_POINT('Ctrl Pts',(6.88251635233599,3.90565612534637,43.5219969505561));
#73344=CARTESIAN_POINT('Ctrl Pts',(6.78241523949474,4.07702803553045,43.5299956937631));
#73345=CARTESIAN_POINT('Ctrl Pts',(6.67592567899843,4.244518503728,43.5379944369702));
#73346=CARTESIAN_POINT('Ctrl Pts',(6.56952285386751,4.41187255153944,43.5459866652296));
#73347=CARTESIAN_POINT('Ctrl Pts',(6.45674212935142,4.57535117686935,43.553978893489));
#73348=CARTESIAN_POINT('Ctrl Pts',(6.3378956964629,4.7344481347626,43.5619711217483));
#73349=CARTESIAN_POINT('Ctrl Pts',(6.21912593332849,4.89344245663771,43.5699581940921));
#73350=CARTESIAN_POINT('Ctrl Pts',(6.09429846048844,5.04806047787279,43.5779452664359));
#73351=CARTESIAN_POINT('Ctrl Pts',(5.96376885304586,5.19782474381736,43.5859323387797));
#73352=CARTESIAN_POINT('Ctrl Pts',(5.83330135281578,5.34751775051837,43.5939156107995));
#73353=CARTESIAN_POINT('Ctrl Pts',(5.69713734546972,5.49236135384377,43.6018988828193));
#73354=CARTESIAN_POINT('Ctrl Pts',(5.555673029076,5.63191070543537,43.6098821548391));
#73355=CARTESIAN_POINT('Ctrl Pts',(5.41425207984176,5.77141727691717,43.617862979515));
#73356=CARTESIAN_POINT('Ctrl Pts',(5.26753429878308,5.9056325977337,43.6258438041909));
#73357=CARTESIAN_POINT('Ctrl Pts',(5.11595340638602,6.03414797164333,43.6338246288668));
#73358=CARTESIAN_POINT('Ctrl Pts',(4.95949651042153,6.16679738521814,43.6420621780479));
#73359=CARTESIAN_POINT('Ctrl Pts',(4.79785868252293,6.29337377059787,43.6502997272289));
#73360=CARTESIAN_POINT('Ctrl Pts',(4.63155514665626,6.41347159684066,43.65853727641));
#73361=CARTESIAN_POINT('Ctrl Pts',(4.47041249070389,6.52984244003419,43.6665191906048));
#73362=CARTESIAN_POINT('Ctrl Pts',(4.30488966491796,6.64013060880149,43.6745011047995));
#73363=CARTESIAN_POINT('Ctrl Pts',(4.13548618829145,6.74401030444428,43.6824830189943));
#73364=CARTESIAN_POINT('Ctrl Pts',(3.96604504855562,6.84791309543559,43.6904667077908));
#73365=CARTESIAN_POINT('Ctrl Pts',(3.79272182307201,6.94540439762522,43.6984503965873));
#73366=CARTESIAN_POINT('Ctrl Pts',(3.61604241025721,7.03620340007459,43.7064340853838));
#73367=CARTESIAN_POINT('Ctrl Pts',(3.43929658853721,7.12703653135793,43.7144207750282));
#73368=CARTESIAN_POINT('Ctrl Pts',(3.25919236202255,7.2111721951554,43.7224074646725));
#73369=CARTESIAN_POINT('Ctrl Pts',(3.07627780477868,7.28837676494746,43.7303941543169));
#73370=CARTESIAN_POINT('Ctrl Pts',(2.8932664045596,7.36562221021905,43.7383850724644));
#73371=CARTESIAN_POINT('Ctrl Pts',(2.70744201509281,7.4359291156739,43.7463759906119));
#73372=CARTESIAN_POINT('Ctrl Pts',(2.51937049646888,7.49911283429728,43.7543669087594));
#73373=CARTESIAN_POINT('Ctrl Pts',(2.33107685659861,7.562371175843,43.7623672645545));
#73374=CARTESIAN_POINT('Ctrl Pts',(2.14053110304867,7.61848941838521,43.7703676203495));
#73375=CARTESIAN_POINT('Ctrl Pts',(1.94831321245926,7.66733308433621,43.7783679761445));
#73376=CARTESIAN_POINT('Ctrl Pts',(1.75596099349397,7.71621088389621,43.7863739228593));
#73377=CARTESIAN_POINT('Ctrl Pts',(1.56193463296585,7.75780389781041,43.7943798695741));
#73378=CARTESIAN_POINT('Ctrl Pts',(1.36682248332548,7.79202908741208,43.8023858162889));
#73379=CARTESIAN_POINT('Ctrl Pts',(1.17145718371103,7.82629868278693,43.8104021503896));
#73380=CARTESIAN_POINT('Ctrl Pts',(0.975003611245265,7.85318131420356,43.8184184844903));
#73381=CARTESIAN_POINT('Ctrl Pts',(0.778054559532989,7.87264581334572,43.8264348185911));
#73382=CARTESIAN_POINT('Ctrl Pts',(0.73636194532399,7.87676629956513,43.8281318154648));
#73383=CARTESIAN_POINT('Ctrl Pts',(0.694647124162059,7.88055453808428,43.8298288123385));
#73384=CARTESIAN_POINT('Ctrl Pts',(0.652915709971441,7.88401053244302,43.8315258092121));
#73385=CARTESIAN_POINT('Ctrl Pts',(0.462030253411381,7.89981874488519,43.8392881156017));
#73386=CARTESIAN_POINT('Ctrl Pts',(0.270232650410157,7.90871816315991,43.8470504219912));
#73387=CARTESIAN_POINT('Ctrl Pts',(0.0780762746324438,7.91061471033317,
43.8548127283807));
#73388=CARTESIAN_POINT('Ctrl Pts',(-0.113847326598659,7.91250896006557,
43.8625656316612));
#73389=CARTESIAN_POINT('Ctrl Pts',(-0.306128481512187,7.90741722029475,
43.8703185349417));
#73390=CARTESIAN_POINT('Ctrl Pts',(-0.49820617021761,7.89529680328467,43.8780714382222));
#73391=CARTESIAN_POINT('Ctrl Pts',(-0.690090140167289,7.88318861024562,
43.8858165223604));
#73392=CARTESIAN_POINT('Ctrl Pts',(-0.881770697586988,7.86406587377253,
43.8935616064987));
#73393=CARTESIAN_POINT('Ctrl Pts',(-1.07268417604572,7.83793784476894,43.9013066906369));
#73394=CARTESIAN_POINT('Ctrl Pts',(-1.26344377770638,7.81183087502986,43.9090455322156));
#73395=CARTESIAN_POINT('Ctrl Pts',(-1.45343717791831,7.7787299026399,43.9167843737943));
#73396=CARTESIAN_POINT('Ctrl Pts',(-1.642103096099,7.73869617065963,43.9245232153731));
#73397=CARTESIAN_POINT('Ctrl Pts',(-1.83065512200523,7.69868660591018,43.9322573852322));
#73398=CARTESIAN_POINT('Ctrl Pts',(-2.01788091174332,7.65175268949037,43.9399915550913));
#73399=CARTESIAN_POINT('Ctrl Pts',(-2.20322658576623,7.59800721319563,43.9477257249504));
#73400=CARTESIAN_POINT('Ctrl Pts',(-2.38849784653986,7.54428331482845,43.9554567896672));
#73401=CARTESIAN_POINT('Ctrl Pts',(-2.5718901508525,7.48375340309149,43.9631878543839));
#73402=CARTESIAN_POINT('Ctrl Pts',(-2.75286196847964,7.41658088221914,43.9709189191006));
#73403=CARTESIAN_POINT('Ctrl Pts',(-2.9338311581051,7.34940933679976,43.9786498715498));
#73404=CARTESIAN_POINT('Ctrl Pts',(-3.1123795908031,7.27559548889696,43.9863808239991));
#73405=CARTESIAN_POINT('Ctrl Pts',(-3.28798262899866,7.19535205750233,43.9941117764483));
#73406=CARTESIAN_POINT('Ctrl Pts',(-3.46359303313458,7.11510526017318,44.0018430531843));
#73407=CARTESIAN_POINT('Ctrl Pts',(-3.63625746961744,7.02842849068314,44.0095743299202));
#73408=CARTESIAN_POINT('Ctrl Pts',(-3.80547310961163,6.93558183658897,44.0173056066562));
#73409=CARTESIAN_POINT('Ctrl Pts',(-3.97472683290778,6.84271428662983,44.0250386233764));
#73410=CARTESIAN_POINT('Ctrl Pts',(-4.14052989917433,6.74367425952843,44.0327716400966));
#73411=CARTESIAN_POINT('Ctrl Pts',(-4.30240578570369,6.63876686253881,44.0405046568168));
#73412=CARTESIAN_POINT('Ctrl Pts',(-4.46434775407009,6.53381663969255,44.0482408303503));
#73413=CARTESIAN_POINT('Ctrl Pts',(-4.62235904934568,6.42299447252852,44.0559770038838));
#73414=CARTESIAN_POINT('Ctrl Pts',(-4.77599369422241,6.30664770165163,44.0637131774173));
#73415=CARTESIAN_POINT('Ctrl Pts',(-4.92980885450255,6.19016422733589,44.0714584406876));
#73416=CARTESIAN_POINT('Ctrl Pts',(-5.07923680822337,6.06814340245827,44.079203703958));
#73417=CARTESIAN_POINT('Ctrl Pts',(-5.2238653520194,5.94097229281295,44.0869489672283));
#73418=CARTESIAN_POINT('Ctrl Pts',(-5.36858671047325,5.81371957173246,44.0946992009832));
#73419=CARTESIAN_POINT('Ctrl Pts',(-5.50850226408887,5.68131022788748,44.1024494347382));
#73420=CARTESIAN_POINT('Ctrl Pts',(-5.64323812714229,5.54416670387603,44.1101996684932));
#73421=CARTESIAN_POINT('Ctrl Pts',(-5.77817690296244,5.4068166411505,44.1179615741323));
#73422=CARTESIAN_POINT('Ctrl Pts',(-5.90792016806836,5.26471842297204,44.1257234797713));
#73423=CARTESIAN_POINT('Ctrl Pts',(-6.03213487910658,5.11832685555211,44.1334853854103));
#73424=CARTESIAN_POINT('Ctrl Pts',(-6.11518054251764,5.02045451231224,44.1386747272986));
#73425=CARTESIAN_POINT('Ctrl Pts',(-6.1957559387252,4.92066375303239,44.1438640691869));
#73426=CARTESIAN_POINT('Ctrl Pts',(-6.27377276627098,4.81909703961195,44.1490534110751));
#73427=CARTESIAN_POINT('Ctrl Pts',(-6.39474680077887,4.66160620743258,44.157100080549));
#73428=CARTESIAN_POINT('Ctrl Pts',(-6.50994226304667,4.49935561946676,44.165146750023));
#73429=CARTESIAN_POINT('Ctrl Pts',(-6.61897066961584,4.33279912698076,44.1731934194969));
#73430=CARTESIAN_POINT('Ctrl Pts',(-6.72781079660562,4.16653025849421,44.1812261932936));
#73431=CARTESIAN_POINT('Ctrl Pts',(-6.83050492667977,3.9959705883102,44.1892589670903));
#73432=CARTESIAN_POINT('Ctrl Pts',(-6.9267053946297,3.82160612517929,44.197291740887));
#73433=CARTESIAN_POINT('Ctrl Pts',(-7.02280644779102,3.64742185250496,44.205316213513));
#73434=CARTESIAN_POINT('Ctrl Pts',(-7.11242705224154,3.46944090855861,44.2133406861389));
#73435=CARTESIAN_POINT('Ctrl Pts',(-7.19526256081308,3.28817847462111,44.2213651587649));
#73436=CARTESIAN_POINT('Ctrl Pts',(-7.278024651545,3.10707669517265,44.2293825192302));
#73437=CARTESIAN_POINT('Ctrl Pts',(-7.3540134943608,2.92269952047661,44.2373998796956));
#73438=CARTESIAN_POINT('Ctrl Pts',(-7.42296995277387,2.73558733734024,44.2454172401609));
#73439=CARTESIAN_POINT('Ctrl Pts',(-7.49187543070865,2.54861348886911,44.253428673279));
#73440=CARTESIAN_POINT('Ctrl Pts',(-7.55375877312745,2.35890897085495,44.2614401063971));
#73441=CARTESIAN_POINT('Ctrl Pts',(-7.60840847115289,2.16703519493545,44.2694515395153));
#73442=CARTESIAN_POINT('Ctrl Pts',(-7.66302119601303,1.97529123091046,44.2774575525112));
#73443=CARTESIAN_POINT('Ctrl Pts',(-7.710409946119,1.78138125261382,44.2854635655071));
#73444=CARTESIAN_POINT('Ctrl Pts',(-7.75041260210287,1.58588319152611,44.2934695785031));
#73445=CARTESIAN_POINT('Ctrl Pts',(-7.79039910156847,1.39046408939542,44.3014723579813));
#73446=CARTESIAN_POINT('Ctrl Pts',(-7.82300538715269,1.19345850598231,44.3094751374596));
#73447=CARTESIAN_POINT('Ctrl Pts',(-7.84811997459449,0.995456610993642,
44.3174779169379));
#73448=CARTESIAN_POINT('Ctrl Pts',(-7.87322921456482,0.797496875148093,
44.3254789924409));
#73449=CARTESIAN_POINT('Ctrl Pts',(-7.890849893012,0.598541577754206,44.3334800679439));
#73450=CARTESIAN_POINT('Ctrl Pts',(-7.90092206350628,0.399188610057576,
44.3414811434469));
#73451=CARTESIAN_POINT('Ctrl Pts',(-7.90771455584179,0.264748520316231,
44.346876926219));
#73452=CARTESIAN_POINT('Ctrl Pts',(-7.91107512021797,0.130127737187862,
44.352272708991));
#73453=CARTESIAN_POINT('Ctrl Pts',(-7.91099872614571,-0.004489423238615,
44.3576684917631));
#73454=CARTESIAN_POINT('',(-7.911,-3.90243393155743E-13,48.357668491763));
#73455=CARTESIAN_POINT('Ctrl Pts',(-7.91099884597975,-0.00427304422863289,
44.3652531274272));
#73456=CARTESIAN_POINT('Ctrl Pts',(-7.91057750947961,-0.784324077631529,
44.3937615432355));
#73457=CARTESIAN_POINT('Ctrl Pts',(-7.79479648296751,-1.55994847174528,
44.4188079269021));
#73458=CARTESIAN_POINT('Ctrl Pts',(-7.53183115076875,-2.42288181788949,
44.4521374585171));
#73459=CARTESIAN_POINT('Ctrl Pts',(-7.49353088856122,-2.53886381240998,
44.4567476485824));
#73460=CARTESIAN_POINT('Ctrl Pts',(-7.42801957037524,-2.72282917360768,
44.4643344212046));
#73461=CARTESIAN_POINT('Ctrl Pts',(-7.40252214680675,-2.79140444063471,
44.4672246802999));
#73462=CARTESIAN_POINT('Ctrl Pts',(-7.37101319255404,-2.87267851311738,
44.4707176672332));
#73463=CARTESIAN_POINT('Ctrl Pts',(-7.36591370256768,-2.88572913620001,
44.4712806453262));
#73464=CARTESIAN_POINT('Ctrl Pts',(-7.35799548059657,-2.90583572118567,
44.4721511683454));
#73465=CARTESIAN_POINT('Ctrl Pts',(-7.35520119375882,-2.91290132510785,
44.4724576806694));
#73466=CARTESIAN_POINT('Ctrl Pts',(-7.35028727784135,-2.92527444794868,
44.4729954858059));
#73467=CARTESIAN_POINT('Ctrl Pts',(-7.34817206561477,-2.93058372283022,
44.4732265951265));
#73468=CARTESIAN_POINT('Ctrl Pts',(-7.34371418790866,-2.9417380200731,44.4737128406693));
#73469=CARTESIAN_POINT('Ctrl Pts',(-7.34137029384775,-2.94758254519611,
44.4739680271478));
#73470=CARTESIAN_POINT('Ctrl Pts',(-7.3348060491135,-2.9638941602868,44.4746813626376));
#73471=CARTESIAN_POINT('Ctrl Pts',(-7.33057028327148,-2.9743550043453,44.475140134089));
#73472=CARTESIAN_POINT('Ctrl Pts',(-7.31340104920725,-3.01649748804308,
44.4769935023396));
#73473=CARTESIAN_POINT('Ctrl Pts',(-7.30028456869861,-3.04810386544434,
44.4783952928077));
#73474=CARTESIAN_POINT('Ctrl Pts',(-6.97504697922301,-3.81767657319244,
44.5128016805283));
#73475=CARTESIAN_POINT('Ctrl Pts',(-6.55281067395682,-4.50407920316199,
44.5491531708751));
#73476=CARTESIAN_POINT('Ctrl Pts',(-5.83385442278534,-5.35224280756966,
44.596624521268));
#73477=CARTESIAN_POINT('Ctrl Pts',(-5.61926957148779,-5.577112696885,44.6095917821584));
#73478=CARTESIAN_POINT('Ctrl Pts',(-5.3454394939657,-5.83217354700291,44.6248317119176));
#73479=CARTESIAN_POINT('Ctrl Pts',(-5.29834588890316,-5.87498958483114,
44.6274102680671));
#73480=CARTESIAN_POINT('Ctrl Pts',(-5.2338860360916,-5.93218894794574,44.6308843197901));
#73481=CARTESIAN_POINT('Ctrl Pts',(-5.21696775593485,-5.94707290963484,
44.6317910341077));
#73482=CARTESIAN_POINT('Ctrl Pts',(-5.18887266315499,-5.97157759312106,
44.6332883441317));
#73483=CARTESIAN_POINT('Ctrl Pts',(-5.17773215972628,-5.9812396832901,44.6338799008416));
#73484=CARTESIAN_POINT('Ctrl Pts',(-5.15615500485754,-5.99984795811422,
44.6350214557659));
#73485=CARTESIAN_POINT('Ctrl Pts',(-5.14572192689813,-6.00879819989468,
44.6355715481778));
#73486=CARTESIAN_POINT('Ctrl Pts',(-5.12133392988368,-6.02960987202533,
44.6368530556845));
#73487=CARTESIAN_POINT('Ctrl Pts',(-5.10736102775537,-6.04145013765289,
44.6375839667308));
#73488=CARTESIAN_POINT('Ctrl Pts',(-5.06345296196222,-6.07839546823662,
44.6398703999343));
#73489=CARTESIAN_POINT('Ctrl Pts',(-5.03337274525318,-6.1033274700671,44.6414217648199));
#73490=CARTESIAN_POINT('Ctrl Pts',(-4.69798878060645,-6.37714481812217,
44.6585542160999));
#73491=CARTESIAN_POINT('Ctrl Pts',(-4.37468245957252,-6.6031247201412,44.6735237484585));
#73492=CARTESIAN_POINT('Ctrl Pts',(-3.44505815631026,-7.15453450261184,
44.7135178874886));
#73493=CARTESIAN_POINT('Ctrl Pts',(-2.81119746222818,-7.42648994964344,
44.7373621636362));
#73494=CARTESIAN_POINT('Ctrl Pts',(-2.10147999290365,-7.62694394025388,
44.7663576576294));
#73495=CARTESIAN_POINT('Ctrl Pts',(-2.05255302192354,-7.6402564069175,44.7683694233245));
#73496=CARTESIAN_POINT('Ctrl Pts',(-1.99245766300421,-7.65598875414102,
44.7708596372374));
#73497=CARTESIAN_POINT('Ctrl Pts',(-1.98140689082546,-7.65885618571279,
44.7713183499096));
#73498=CARTESIAN_POINT('Ctrl Pts',(-1.9640916811857,-7.66330911712793,44.772038391414));
#73499=CARTESIAN_POINT('Ctrl Pts',(-1.95783141404456,-7.6649108873217,44.7722989852096));
#73500=CARTESIAN_POINT('Ctrl Pts',(-1.94673904786902,-7.66773453646699,
44.7727612024936));
#73501=CARTESIAN_POINT('Ctrl Pts',(-1.94190773832127,-7.66895952381403,
44.7729626834628));
#73502=CARTESIAN_POINT('Ctrl Pts',(-1.93080147429702,-7.67176436929156,
44.7734262263224));
#73503=CARTESIAN_POINT('Ctrl Pts',(-1.92452573846798,-7.67334109450874,
44.7736884330451));
#73504=CARTESIAN_POINT('Ctrl Pts',(-1.90742808587944,-7.67761443959303,
44.7744035585324));
#73505=CARTESIAN_POINT('Ctrl Pts',(-1.89660241848049,-7.68029586995761,
44.7748571896351));
#73506=CARTESIAN_POINT('Ctrl Pts',(-1.84388756178559,-7.69323466295953,
44.7770703413092));
#73507=CARTESIAN_POINT('Ctrl Pts',(-1.80192284738801,-7.70317174381062,
44.7788454302143));
#73508=CARTESIAN_POINT('Ctrl Pts',(-0.988963526297145,-7.88867053920941,
44.8135040554103));
#73509=CARTESIAN_POINT('Ctrl Pts',(-0.196051153149005,-7.94800232516257,
44.8514891451777));
#73510=CARTESIAN_POINT('Ctrl Pts',(0.883121294802134,-7.86695484367695,
44.9004001482116));
#73511=CARTESIAN_POINT('Ctrl Pts',(1.17236899251804,-7.82907737292079,44.913281142439));
#73512=CARTESIAN_POINT('Ctrl Pts',(1.58524286892673,-7.75160982274104,44.9311997949603));
#73513=CARTESIAN_POINT('Ctrl Pts',(1.71100887160302,-7.72482364752583,44.9365960407663));
#73514=CARTESIAN_POINT('Ctrl Pts',(1.88169869122541,-7.68409601329739,44.9438352685631));
#73515=CARTESIAN_POINT('Ctrl Pts',(1.92723007394158,-7.67280299783028,44.9457580833418));
#73516=CARTESIAN_POINT('Ctrl Pts',(2.00433036105135,-7.65295043731689,44.9490003694468));
#73517=CARTESIAN_POINT('Ctrl Pts',(2.03595125761321,-7.64459894964962,44.9503261874252));
#73518=CARTESIAN_POINT('Ctrl Pts',(2.0794739064918,-7.63281485767463,44.9521457259189));
#73519=CARTESIAN_POINT('Ctrl Pts',(2.0914205325787,-7.6295500874534,44.9526446227682));
#73520=CARTESIAN_POINT('Ctrl Pts',(2.11068269853752,-7.62423748680386,44.9534481378551));
#73521=CARTESIAN_POINT('Ctrl Pts',(2.11800301975766,-7.62220715526593,44.9537532968507));
#73522=CARTESIAN_POINT('Ctrl Pts',(2.13325371764232,-7.61795362346454,44.9543886196733));
#73523=CARTESIAN_POINT('Ctrl Pts',(2.1411835719791,-7.61572857609072,44.9547187258455));
#73524=CARTESIAN_POINT('Ctrl Pts',(2.15949118577555,-7.61056076617832,44.9554802888589));
#73525=CARTESIAN_POINT('Ctrl Pts',(2.16986644029136,-7.6076091506837,44.9559114706419));
#73526=CARTESIAN_POINT('Ctrl Pts',(2.2030933487687,-7.5980830553634,44.9572910374755));
#73527=CARTESIAN_POINT('Ctrl Pts',(2.22592150374738,-7.59142673618077,44.9582368806852));
#73528=CARTESIAN_POINT('Ctrl Pts',(2.43203929044306,-7.53031646773791,44.9667596176839));
#73529=CARTESIAN_POINT('Ctrl Pts',(2.61333443357915,-7.46933531870476,44.9741294552133));
#73530=CARTESIAN_POINT('Ctrl Pts',(3.25443007485733,-7.22749024658638,44.9998800116175));
#73531=CARTESIAN_POINT('Ctrl Pts',(3.69928297843251,-7.01022631594068,45.0170936213973));
#73532=CARTESIAN_POINT('Ctrl Pts',(4.45682287358665,-6.54793486118525,45.0477478049317));
#73533=CARTESIAN_POINT('Ctrl Pts',(4.77690049979974,-6.31822108393,45.0612294004367));
#73534=CARTESIAN_POINT('Ctrl Pts',(5.18873190136544,-5.97341057495099,45.0808055496746));
#73535=CARTESIAN_POINT('Ctrl Pts',(5.2963792373924,-5.8781746008102,45.0861559128048));
#73536=CARTESIAN_POINT('Ctrl Pts',(5.47242929088031,-5.71365887831471,45.0954032313498));
#73537=CARTESIAN_POINT('Ctrl Pts',(5.54225199798967,-5.64595617263282,45.0992149271494));
#73538=CARTESIAN_POINT('Ctrl Pts',(5.62167455715504,-5.56605189793051,45.1037157614456));
#73539=CARTESIAN_POINT('Ctrl Pts',(5.63250809413296,-5.55508875917418,45.1043332594447));
#73540=CARTESIAN_POINT('Ctrl Pts',(5.64896399507179,-5.53833836851867,45.1052765837661));
#73541=CARTESIAN_POINT('Ctrl Pts',(5.65460969395091,-5.53257402212637,45.1056011867686));
#73542=CARTESIAN_POINT('Ctrl Pts',(5.66484192080888,-5.52209473652575,45.1061912372581));
#73543=CARTESIAN_POINT('Ctrl Pts',(5.66943141038547,-5.51738269014867,45.1064565331326));
#73544=CARTESIAN_POINT('Ctrl Pts',(5.67860965313612,-5.50793580960032,45.1069883539893));
#73545=CARTESIAN_POINT('Ctrl Pts',(5.68319837414563,-5.50320095173255,45.1072548801758));
#73546=CARTESIAN_POINT('Ctrl Pts',(5.69612969468175,-5.48982438513567,45.1080077609376));
#73547=CARTESIAN_POINT('Ctrl Pts',(5.70445852188799,-5.48116942344234,45.1084947882875));
#73548=CARTESIAN_POINT('Ctrl Pts',(5.73899546914147,-5.44511611822613,45.1105230116991));
#73549=CARTESIAN_POINT('Ctrl Pts',(5.76502594871138,-5.41754873463898,45.1120725337521));
#73550=CARTESIAN_POINT('Ctrl Pts',(6.15642395459617,-4.997026313365,45.1356768960343));
#73551=CARTESIAN_POINT('Ctrl Pts',(6.48107897072506,-4.56808906303766,45.1591835217404));
#73552=CARTESIAN_POINT('Ctrl Pts',(6.98709097378206,-3.73575908485551,45.2011100414992));
#73553=CARTESIAN_POINT('Ctrl Pts',(7.18297181307584,-3.3436927505341,45.2196238680416));
#73554=CARTESIAN_POINT('Ctrl Pts',(7.46803712816953,-2.63084878797105,45.2513904451755));
#73555=CARTESIAN_POINT('Ctrl Pts',(7.57132706747662,-2.31688522985853,45.2648523101606));
#73556=CARTESIAN_POINT('Ctrl Pts',(7.6703520681745,-1.93738620675107,45.2807381815993));
#73557=CARTESIAN_POINT('Ctrl Pts',(7.68530238979467,-1.87720361117908,45.2832444217188));
#73558=CARTESIAN_POINT('Ctrl Pts',(7.70688268338584,-1.78574955733624,45.2870333111725));
#73559=CARTESIAN_POINT('Ctrl Pts',(7.71403320866772,-1.75460361360804,45.2883202449156));
#73560=CARTESIAN_POINT('Ctrl Pts',(7.72613323009837,-1.70039485045857,45.2905542209848));
#73561=CARTESIAN_POINT('Ctrl Pts',(7.73116865279933,-1.67735166322344,45.2915019979227));
#73562=CARTESIAN_POINT('Ctrl Pts',(7.74225919391443,-1.62548787914591,45.2936310651142));
#73563=CARTESIAN_POINT('Ctrl Pts',(7.74825659186675,-1.59665527414665,45.294811826373));
#73564=CARTESIAN_POINT('Ctrl Pts',(7.76355875227602,-1.52097269661544,45.2979038414637));
#73565=CARTESIAN_POINT('Ctrl Pts',(7.77260047261892,-1.47407067904797,45.2998126457242));
#73566=CARTESIAN_POINT('Ctrl Pts',(7.81205309372857,-1.25895494761477,45.3085346807306));
#73567=CARTESIAN_POINT('Ctrl Pts',(7.83743199013671,-1.08986340055955,45.3152984140403));
#73568=CARTESIAN_POINT('Ctrl Pts',(7.85974497082825,-0.899314810687137,
45.3228382244148));
#73569=CARTESIAN_POINT('Ctrl Pts',(7.86209429946939,-0.878539335303452,
45.3236592123933));
#73570=CARTESIAN_POINT('Ctrl Pts',(7.8980939122556,-0.548475345758534,45.336686065598));
#73571=CARTESIAN_POINT('Ctrl Pts',(7.9135531057463,-0.237473332399331,45.3487219677521));
#73572=CARTESIAN_POINT('Ctrl Pts',(7.90786946442744,0.373143235492292,45.3723265695618));
#73573=CARTESIAN_POINT('Ctrl Pts',(7.88807395794214,0.672249371242181,45.3838788109277));
#73574=CARTESIAN_POINT('Ctrl Pts',(7.84361225533363,1.03231428757976,45.3981413553201));
#73575=CARTESIAN_POINT('Ctrl Pts',(7.83510323439984,1.095026572812,45.4006389706971));
#73576=CARTESIAN_POINT('Ctrl Pts',(7.81944606970038,1.20087261763275,45.4048829994601));
#73577=CARTESIAN_POINT('Ctrl Pts',(7.81269110979921,1.24406167817418,45.4066227908376));
#73578=CARTESIAN_POINT('Ctrl Pts',(7.80033762180236,1.31897365781012,45.4096564982795));
#73579=CARTESIAN_POINT('Ctrl Pts',(7.79490262952818,1.35072258445195,45.4109472478512));
#73580=CARTESIAN_POINT('Ctrl Pts',(7.78670360178222,1.39691959761215,45.4128333726759));
#73581=CARTESIAN_POINT('Ctrl Pts',(7.78409290620811,1.41139468954072,45.4134255046806));
#73582=CARTESIAN_POINT('Ctrl Pts',(7.7794425172241,1.43677352833108,45.4144657641333));
#73583=CARTESIAN_POINT('Ctrl Pts',(7.77742022784319,1.44768043750186,45.4149135075829));
#73584=CARTESIAN_POINT('Ctrl Pts',(7.77345019920226,1.46884375882291,45.4157836438063));
#73585=CARTESIAN_POINT('Ctrl Pts',(7.77150508436882,1.47910064233368,45.416205976267));
#73586=CARTESIAN_POINT('Ctrl Pts',(7.76680128790469,1.5036390277085,45.4172178744757));
#73587=CARTESIAN_POINT('Ctrl Pts',(7.76402352401531,1.51791675954302,45.4178078873223));
#73588=CARTESIAN_POINT('Ctrl Pts',(7.75290048785266,1.57425987593919,45.420141194224));
#73589=CARTESIAN_POINT('Ctrl Pts',(7.74425266900614,1.61626442066841,45.4218915821549));
#73590=CARTESIAN_POINT('Ctrl Pts',(7.65929371584855,2.0125865754362,45.4385018233856));
#73591=CARTESIAN_POINT('Ctrl Pts',(7.55906029910967,2.36133071088002,45.4538169325443));
#73592=CARTESIAN_POINT('Ctrl Pts',(7.26453991019311,3.17179284040225,45.4901861215191));
#73593=CARTESIAN_POINT('Ctrl Pts',(7.0496503362616,3.6244006673238,45.5110861423262));
#73594=CARTESIAN_POINT('Ctrl Pts',(6.76704340580693,4.09801247154669,45.5334693609034));
#73595=CARTESIAN_POINT('Ctrl Pts',(6.74017436181341,4.14205652975212,45.5355570637587));
#73596=CARTESIAN_POINT('Ctrl Pts',(6.69878983172536,4.20842542456828,45.5387130728685));
#73597=CARTESIAN_POINT('Ctrl Pts',(6.68458940652093,4.23094483972399,45.5397857150991));
#73598=CARTESIAN_POINT('Ctrl Pts',(6.65975522785723,4.26989041701387,45.5416440113488));
#73599=CARTESIAN_POINT('Ctrl Pts',(6.64917372136912,4.28634957673531,45.5424303772755));
#73600=CARTESIAN_POINT('Ctrl Pts',(6.62570375518043,4.32256023353696,45.5441627216013));
#73601=CARTESIAN_POINT('Ctrl Pts',(6.61278780674016,4.3422937085758,45.5451083141454));
#73602=CARTESIAN_POINT('Ctrl Pts',(6.57878727322889,4.39373748564403,45.5475775818405));
#73603=CARTESIAN_POINT('Ctrl Pts',(6.55756159746115,4.42535388337352,45.5490993212964));
#73604=CARTESIAN_POINT('Ctrl Pts',(6.4636745771138,4.56304315692436,45.555746131145));
#73605=CARTESIAN_POINT('Ctrl Pts',(6.3886612499516,4.66748968178442,45.5608392731761));
#73606=CARTESIAN_POINT('Ctrl Pts',(5.89334484955657,5.32282882894237,45.593217947759));
#73607=CARTESIAN_POINT('Ctrl Pts',(5.40471550970584,5.81834652425665,45.6197648905153));
#73608=CARTESIAN_POINT('Ctrl Pts',(4.73372894053072,6.34038168051431,45.6516398926002));
#73609=CARTESIAN_POINT('Ctrl Pts',(4.60681580363533,6.43318566309756,45.6575115695023));
#73610=CARTESIAN_POINT('Ctrl Pts',(4.15288586092148,6.7447924409901,45.6781147056187));
#73611=CARTESIAN_POINT('Ctrl Pts',(3.8124085891106,6.94292417236386,45.6928447036365));
#73612=CARTESIAN_POINT('Ctrl Pts',(3.43647536749856,7.1256694351127,45.7093541933063));
#73613=CARTESIAN_POINT('Ctrl Pts',(3.41426997914466,7.13633577871017,45.7103303581433));
#73614=CARTESIAN_POINT('Ctrl Pts',(3.36498957925658,7.15972492797071,45.7124995555516));
#73615=CARTESIAN_POINT('Ctrl Pts',(3.33789155321998,7.1723981949203,45.7136941989268));
#73616=CARTESIAN_POINT('Ctrl Pts',(3.30052813416966,7.18961480375685,45.715344631879));
#73617=CARTESIAN_POINT('Ctrl Pts',(3.29032381844827,7.19429052507522,45.7157957111405));
#73618=CARTESIAN_POINT('Ctrl Pts',(3.27314012295885,7.20212006241861,45.7165559111763));
#73619=CARTESIAN_POINT('Ctrl Pts',(3.26616603671938,7.20528549594923,45.7168646076689));
#73620=CARTESIAN_POINT('Ctrl Pts',(3.25240156021569,7.21150889562677,45.7174742128078));
#73621=CARTESIAN_POINT('Ctrl Pts',(3.24561142618429,7.21456741117494,45.7177751006302));
#73622=CARTESIAN_POINT('Ctrl Pts',(3.23069329217432,7.22126174124115,45.718436538354));
#73623=CARTESIAN_POINT('Ctrl Pts',(3.22256345801688,7.22489342772004,45.7187972434623));
#73624=CARTESIAN_POINT('Ctrl Pts',(3.19440447338191,7.23741537183106,45.7200475003356));
#73625=CARTESIAN_POINT('Ctrl Pts',(3.1743446289126,7.24623608290017,45.7209397241607));
#73626=CARTESIAN_POINT('Ctrl Pts',(2.85145635442445,7.38661838651852,45.7353295759499));
#73627=CARTESIAN_POINT('Ctrl Pts',(2.54078839503323,7.49914966629145,45.749751145816));
#73628=CARTESIAN_POINT('Ctrl Pts',(1.83646731017107,7.70548013005092,45.7828292425046));
#73629=CARTESIAN_POINT('Ctrl Pts',(1.44075626866214,7.78917594725617,45.8015590765929));
#73630=CARTESIAN_POINT('Ctrl Pts',(0.661277233459787,7.89258413837518,45.8372279830831));
#73631=CARTESIAN_POINT('Ctrl Pts',(0.27899783434158,7.91532548204458,45.8541608908882));
#73632=CARTESIAN_POINT('Ctrl Pts',(-0.250561852634493,7.90839955156583,
45.8764804014484));
#73633=CARTESIAN_POINT('Ctrl Pts',(-0.397589486122487,7.90237244826539,
45.882560146985));
#73634=CARTESIAN_POINT('Ctrl Pts',(-0.563898923852589,7.8909012310378,45.8893062956878));
#73635=CARTESIAN_POINT('Ctrl Pts',(-0.58342391381474,7.88948165459394,45.890096268826));
#73636=CARTESIAN_POINT('Ctrl Pts',(-0.612761029765393,7.88723917901339,
45.8912802014249));
#73637=CARTESIAN_POINT('Ctrl Pts',(-0.622577148427273,7.88647041722237,
45.8916758310846));
#73638=CARTESIAN_POINT('Ctrl Pts',(-0.63946283684016,7.88511627060822,45.8923555181667));
#73639=CARTESIAN_POINT('Ctrl Pts',(-0.646533089669887,7.88453970026072,
45.8926398477572));
#73640=CARTESIAN_POINT('Ctrl Pts',(-0.661097442567303,7.88333227326004,
45.893225009828));
#73641=CARTESIAN_POINT('Ctrl Pts',(-0.668591438132273,7.88270023839644,
45.8935258054852));
#73642=CARTESIAN_POINT('Ctrl Pts',(-0.686638362266085,7.88115226107306,
45.8942494673423));
#73643=CARTESIAN_POINT('Ctrl Pts',(-0.697190388314609,7.88022580681204,
45.8946720074581));
#73644=CARTESIAN_POINT('Ctrl Pts',(-0.729589935950491,7.8773155816449,45.8959676143639));
#73645=CARTESIAN_POINT('Ctrl Pts',(-0.751431175037266,7.87526211922154,
45.8968385180214));
#73646=CARTESIAN_POINT('Ctrl Pts',(-1.00371285999161,7.85048409935978,45.906869653386));
#73647=CARTESIAN_POINT('Ctrl Pts',(-1.23306591436498,7.81774257525262,45.9157102899084));
#73648=CARTESIAN_POINT('Ctrl Pts',(-2.02701538339099,7.66858548421364,45.9455900920633));
#73649=CARTESIAN_POINT('Ctrl Pts',(-2.58006572148429,7.50061868870378,45.9649768172851));
#73650=CARTESIAN_POINT('Ctrl Pts',(-3.56439635706117,7.07977912513883,46.001501560628));
#73651=CARTESIAN_POINT('Ctrl Pts',(-3.99959071719895,6.84334441092453,46.0185549157974));
#73652=CARTESIAN_POINT('Ctrl Pts',(-4.44137047792762,6.54672378963197,46.0395304672268));
#73653=CARTESIAN_POINT('Ctrl Pts',(-4.4727557192844,6.52532146995297,46.0410421494628));
#73654=CARTESIAN_POINT('Ctrl Pts',(-4.51111378165321,6.49875746885079,46.0429176989488));
#73655=CARTESIAN_POINT('Ctrl Pts',(-4.51823430613906,6.49380897037111,46.0432670574857));
#73656=CARTESIAN_POINT('Ctrl Pts',(-4.52938388294148,6.48603321512082,46.0438159926314));
#73657=CARTESIAN_POINT('Ctrl Pts',(-4.53341847496644,6.48321387564279,46.0440150209249));
#73658=CARTESIAN_POINT('Ctrl Pts',(-4.54056547085831,6.47820968057944,46.0443682824281));
#73659=CARTESIAN_POINT('Ctrl Pts',(-4.54367893883055,6.47602634039058,46.0445224096522));
#73660=CARTESIAN_POINT('Ctrl Pts',(-4.55083677027424,6.47099916045976,46.0448772897093));
#73661=CARTESIAN_POINT('Ctrl Pts',(-4.55488004076056,6.4681537751059,46.0450781514588));
#73662=CARTESIAN_POINT('Ctrl Pts',(-4.56590065167555,6.46038274287609,46.0456267308406));
#73663=CARTESIAN_POINT('Ctrl Pts',(-4.57287268495985,6.45544958561868,46.0459749832781));
#73664=CARTESIAN_POINT('Ctrl Pts',(-4.60799657776681,6.43051174113837,46.0477355469237));
#73665=CARTESIAN_POINT('Ctrl Pts',(-4.63602478417644,6.4103344562795,46.0491602907247));
#73666=CARTESIAN_POINT('Ctrl Pts',(-5.14327904667264,6.04009932827313,46.0752923895468));
#73667=CARTESIAN_POINT('Ctrl Pts',(-5.58171917663632,5.63741612530685,46.1033933036455));
#73668=CARTESIAN_POINT('Ctrl Pts',(-6.20840849175219,4.91635825821291,46.1476676374561));
#73669=CARTESIAN_POINT('Ctrl Pts',(-6.42681954871182,4.62719583013448,46.1642000839799));
#73670=CARTESIAN_POINT('Ctrl Pts',(-6.77369285257917,4.09577036752642,46.1919244031957));
#73671=CARTESIAN_POINT('Ctrl Pts',(-6.91081830424044,3.8599042765408,46.203415992642));
#73672=CARTESIAN_POINT('Ctrl Pts',(-7.04483605475889,3.59925308193642,46.2152557640008));
#73673=CARTESIAN_POINT('Ctrl Pts',(-7.05410097209022,3.58106091410784,46.2160778201236));
#73674=CARTESIAN_POINT('Ctrl Pts',(-7.06758436963312,3.5543301579066,46.2172794507875));
#73675=CARTESIAN_POINT('Ctrl Pts',(-7.07185797943865,3.54581956856509,46.2176611010093));
#73676=CARTESIAN_POINT('Ctrl Pts',(-7.07935817207902,3.53081597376968,46.2183322975193));
#73677=CARTESIAN_POINT('Ctrl Pts',(-7.08259121121235,3.52432621992429,46.2186220863228));
#73678=CARTESIAN_POINT('Ctrl Pts',(-7.08887098723624,3.51167714146238,46.2191858703257));
#73679=CARTESIAN_POINT('Ctrl Pts',(-7.09191862882748,3.50551827579673,46.2194598993123));
#73680=CARTESIAN_POINT('Ctrl Pts',(-7.09920609513537,3.49074290641095,46.2201161615786));
#73681=CARTESIAN_POINT('Ctrl Pts',(-7.10343826802851,3.48212262752236,46.2204981079195));
#73682=CARTESIAN_POINT('Ctrl Pts',(-7.1186897027617,3.45091430748992,46.2218775272241));
#73683=CARTESIAN_POINT('Ctrl Pts',(-7.12961706281217,3.42828137634656,46.2228715625175));
#73684=CARTESIAN_POINT('Ctrl Pts',(-7.30077050251995,3.06942787741506,46.2385331585974));
#73685=CARTESIAN_POINT('Ctrl Pts',(-7.43717168480958,2.7223434963412,46.2522723926034));
#73686=CARTESIAN_POINT('Ctrl Pts',(-7.73140575364928,1.7839622617924,46.2869506279857));
#73687=CARTESIAN_POINT('Ctrl Pts',(-7.84603652606527,1.18185961229528,46.3066355853794));
#73688=CARTESIAN_POINT('Ctrl Pts',(-7.90421915415763,0.380111655674429,
46.3349357750042));
#73689=CARTESIAN_POINT('Ctrl Pts',(-7.91113876675237,0.187192613980867,
46.3419197391759));
#73690=CARTESIAN_POINT('Ctrl Pts',(-7.91092438517952,-0.106463557381466,
46.3530711663491));
#73691=CARTESIAN_POINT('Ctrl Pts',(-7.90892860487414,-0.207137165649146,
46.3569875209991));
#73692=CARTESIAN_POINT('Ctrl Pts',(-7.90455023138246,-0.319605406092795,
46.3614947600475));
#73693=CARTESIAN_POINT('Ctrl Pts',(-7.90406164692202,-0.33146863293588,
46.3619718310198));
#73694=CARTESIAN_POINT('Ctrl Pts',(-7.903315870304,-0.348636573166781,46.3626646663252));
#73695=CARTESIAN_POINT('Ctrl Pts',(-7.90308003975752,-0.353942214200977,
46.3628791204729));
#73696=CARTESIAN_POINT('Ctrl Pts',(-7.90265379610153,-0.363318851561732,
46.3632587238618));
#73697=CARTESIAN_POINT('Ctrl Pts',(-7.90246558160337,-0.367389902399768,
46.3634237353023));
#73698=CARTESIAN_POINT('Ctrl Pts',(-7.90206877279715,-0.375831417670163,
46.3637663046779));
#73699=CARTESIAN_POINT('Ctrl Pts',(-7.90185969834156,-0.380201857035287,
46.3639438918128));
#73700=CARTESIAN_POINT('Ctrl Pts',(-7.90131276192169,-0.39143953753321,
46.3644011029528));
#73701=CARTESIAN_POINT('Ctrl Pts',(-7.90096957356911,-0.398306502814553,
46.3646810486293));
#73702=CARTESIAN_POINT('Ctrl Pts',(-7.8995150231373,-0.426669317667521,
46.3658396015365));
#73703=CARTESIAN_POINT('Ctrl Pts',(-7.89832489483122,-0.44816084724729,
46.3667229023449));
#73704=CARTESIAN_POINT('Ctrl Pts',(-7.88967588585884,-0.593592682527613,
46.3727355835338));
#73705=CARTESIAN_POINT('Ctrl Pts',(-7.87938803540697,-0.717341601911624,
46.3780259846235));
#73706=CARTESIAN_POINT('Ctrl Pts',(-7.84691132147111,-1.0211842857287,46.3913575028096));
#73707=CARTESIAN_POINT('Ctrl Pts',(-7.82143086548019,-1.20085273511072,
46.3995374047983));
#73708=CARTESIAN_POINT('Ctrl Pts',(-7.6612078256242,-2.10561997644481,46.4417163598038));
#73709=CARTESIAN_POINT('Ctrl Pts',(-7.43167658263196,-2.81037363486596,
46.4773872271623));
#73710=CARTESIAN_POINT('Ctrl Pts',(-6.97980237278233,-3.73514862784424,
46.5226707617288));
#73711=CARTESIAN_POINT('Ctrl Pts',(-6.83736531071775,-3.98991693100337,
46.5350251519796));
#73712=CARTESIAN_POINT('Ctrl Pts',(-6.66801722831137,-4.25700253781224,
46.5478494028067));
#73713=CARTESIAN_POINT('Ctrl Pts',(-6.65476712248939,-4.27768616475423,
46.548841765082));
#73714=CARTESIAN_POINT('Ctrl Pts',(-6.63612817948381,-4.30648565231065,
46.5502225038351));
#73715=CARTESIAN_POINT('Ctrl Pts',(-6.63082043187822,-4.31465366966558,
46.5506139907741));
#73716=CARTESIAN_POINT('Ctrl Pts',(-6.62162097811,-4.32875351034982,46.5512895951182));
#73717=CARTESIAN_POINT('Ctrl Pts',(-6.61773635968813,-4.33468993183451,
46.5515739846543));
#73718=CARTESIAN_POINT('Ctrl Pts',(-6.60967281002296,-4.34697643553769,
46.5521624622581));
#73719=CARTESIAN_POINT('Ctrl Pts',(-6.60549269985154,-4.3533257377922,46.5524665045054));
#73720=CARTESIAN_POINT('Ctrl Pts',(-6.59569129499238,-4.36816678359865,
46.5531770325824));
#73721=CARTESIAN_POINT('Ctrl Pts',(-6.59006273620931,-4.37665372653862,
46.5535832378424));
#73722=CARTESIAN_POINT('Ctrl Pts',(-6.5718741641315,-4.40396447059652,46.5548900405642));
#73723=CARTESIAN_POINT('Ctrl Pts',(-6.55924971322905,-4.42274533498227,
46.5557881495011));
#73724=CARTESIAN_POINT('Ctrl Pts',(-6.23985431735601,-4.89352086183233,
46.5782885206768));
#73725=CARTESIAN_POINT('Ctrl Pts',(-5.88715043018444,-5.31261397174747,
46.5978875214552));
#73726=CARTESIAN_POINT('Ctrl Pts',(-5.01460293464638,-6.15481217275843,
46.64002241609));
#73727=CARTESIAN_POINT('Ctrl Pts',(-4.47861256683874,-6.55514695185946,
46.6621351255904));
#73728=CARTESIAN_POINT('Ctrl Pts',(-3.86363855933159,-6.90346673138071,
46.6900374956399));
#73729=CARTESIAN_POINT('Ctrl Pts',(-3.82830507630175,-6.92312328268339,
46.6916473563032));
#73730=CARTESIAN_POINT('Ctrl Pts',(-3.78223001818944,-6.94829495558331,
46.6937540451917));
#73731=CARTESIAN_POINT('Ctrl Pts',(-3.77162391796402,-6.95405778805381,
46.6942394950813));
#73732=CARTESIAN_POINT('Ctrl Pts',(-3.7546963419266,-6.96320528180495,46.6950150509662));
#73733=CARTESIAN_POINT('Ctrl Pts',(-3.74838335621728,-6.96660567500622,
46.6953044570555));
#73734=CARTESIAN_POINT('Ctrl Pts',(-3.73702796834733,-6.97270217768246,
46.6958253168329));
#73735=CARTESIAN_POINT('Ctrl Pts',(-3.73198724462923,-6.9754014150143,46.6960566338297));
#73736=CARTESIAN_POINT('Ctrl Pts',(-3.72018781633386,-6.9817033932352,46.6965983428048));
#73737=CARTESIAN_POINT('Ctrl Pts',(-3.71342680422943,-6.9853017851065,46.6969089212829));
#73738=CARTESIAN_POINT('Ctrl Pts',(-3.6940314743821,-6.99558838301792,46.6978003811812));
#73739=CARTESIAN_POINT('Ctrl Pts',(-3.6813842748136,-7.00225215028686,46.698382289962));
#73740=CARTESIAN_POINT('Ctrl Pts',(-3.59897187279327,-7.0453899823371,46.7021778521312));
#73741=CARTESIAN_POINT('Ctrl Pts',(-3.52868488557851,-7.08085454087484,
46.7054321355445));
#73742=CARTESIAN_POINT('Ctrl Pts',(-3.3032605967931,-7.19040642882663,46.7159019766271));
#73743=CARTESIAN_POINT('Ctrl Pts',(-3.1462353220185,-7.26048724336464,46.723242912383));
#73744=CARTESIAN_POINT('Ctrl Pts',(-2.32255867367755,-7.5963557129978,46.7616679288116));
#73745=CARTESIAN_POINT('Ctrl Pts',(-1.6241903381002,-7.7756709199758,46.793615582705));
#73746=CARTESIAN_POINT('Ctrl Pts',(-0.702815268075138,-7.88251210639145,
46.8324399858931));
#73747=CARTESIAN_POINT('Ctrl Pts',(-0.493505512333553,-7.89837981503203,
46.8410747500611));
#73748=CARTESIAN_POINT('Ctrl Pts',(-0.247386413338868,-7.90721500187279,
46.851043259848));
#73749=CARTESIAN_POINT('Ctrl Pts',(-0.210957581140514,-7.9082707369982,
46.8525141179042));
#73750=CARTESIAN_POINT('Ctrl Pts',(-0.156706664247727,-7.9094678446292,
46.8546977621108));
#73751=CARTESIAN_POINT('Ctrl Pts',(-0.138889360984439,-7.90980077576333,
46.8554138248434));
#73752=CARTESIAN_POINT('Ctrl Pts',(-0.10716935936502,-7.9102862799317,46.8566866631407));
#73753=CARTESIAN_POINT('Ctrl Pts',(-0.0932671139113457,-7.91046241056601,
46.8572438519116));
#73754=CARTESIAN_POINT('Ctrl Pts',(-0.0642250363596227,-7.91075378011629,
46.8584064273096));
#73755=CARTESIAN_POINT('Ctrl Pts',(-0.0490851869109706,-7.910862207828,
46.8590116897727));
#73756=CARTESIAN_POINT('Ctrl Pts',(-0.00962913148823917,-7.91103151026808,
46.8605869917113));
#73757=CARTESIAN_POINT('Ctrl Pts',(0.014687256625856,-7.91102373710685,
46.8615557796971));
#73758=CARTESIAN_POINT('Ctrl Pts',(0.12078563549058,-7.91050063791418,46.8657738980452));
#73759=CARTESIAN_POINT('Ctrl Pts',(0.202557662009064,-7.90882925680557,
46.8690016229055));
#73760=CARTESIAN_POINT('Ctrl Pts',(1.02789316519733,-7.87915079458822,46.9013535511242));
#73761=CARTESIAN_POINT('Ctrl Pts',(1.76395562425671,-7.74764565391003,46.9278208788122));
#73762=CARTESIAN_POINT('Ctrl Pts',(2.77509716481213,-7.41521161927144,46.966919054679));
#73763=CARTESIAN_POINT('Ctrl Pts',(3.07302029087386,-7.2967833073106,46.9788925905246));
#73764=CARTESIAN_POINT('Ctrl Pts',(3.37977385048252,-7.15271950803795,46.9924138521336));
#73765=CARTESIAN_POINT('Ctrl Pts',(3.39659809380275,-7.14474555333893,46.9931593940501));
#73766=CARTESIAN_POINT('Ctrl Pts',(3.4199721298164,-7.13356606494813,46.9942008910661));
#73767=CARTESIAN_POINT('Ctrl Pts',(3.42654596181638,-7.13041071347065,46.99449443747));
#73768=CARTESIAN_POINT('Ctrl Pts',(3.43787121282645,-7.12495546579697,46.9950012553116));
#73769=CARTESIAN_POINT('Ctrl Pts',(3.44262471629478,-7.12265989136816,46.9952143154177));
#73770=CARTESIAN_POINT('Ctrl Pts',(3.45244036299211,-7.11790757181787,46.9956549695163));
#73771=CARTESIAN_POINT('Ctrl Pts',(3.45750218832127,-7.1154501810116,46.9958825954204));
#73772=CARTESIAN_POINT('Ctrl Pts',(3.46929634496883,-7.10970885335086,46.9964138763236));
#73773=CARTESIAN_POINT('Ctrl Pts',(3.47602663471061,-7.10642075469948,46.9967177402365));
#73774=CARTESIAN_POINT('Ctrl Pts',(3.49752594478716,-7.09587936764046,46.9976906455691));
#73775=CARTESIAN_POINT('Ctrl Pts',(3.51227694035261,-7.08858959331064,46.9983615526408));
#73776=CARTESIAN_POINT('Ctrl Pts',(3.83554121031371,-6.92757931004217,47.0131408729135));
#73777=CARTESIAN_POINT('Ctrl Pts',(4.13365837205501,-6.75392689746058,47.0283708399069));
#73778=CARTESIAN_POINT('Ctrl Pts',(4.83901013679456,-6.2788359956522,47.0669723848399));
#73779=CARTESIAN_POINT('Ctrl Pts',(5.23049572949256,-5.9566557253507,47.0906647980545));
#73780=CARTESIAN_POINT('Ctrl Pts',(5.90369255078832,-5.28475035041649,47.1334869520434));
#73781=CARTESIAN_POINT('Ctrl Pts',(6.19174528422648,-4.94414211618902,47.152753477639));
#73782=CARTESIAN_POINT('Ctrl Pts',(6.46657121053869,-4.55721773111413,47.1720587530345));
#73783=CARTESIAN_POINT('Ctrl Pts',(6.48337793949777,-4.53327554716637,47.17324379352));
#73784=CARTESIAN_POINT('Ctrl Pts',(6.50631974554313,-4.50020502852142,47.1748676716268));
#73785=CARTESIAN_POINT('Ctrl Pts',(6.51256905884362,-4.49115644182875,47.1753106612022));
#73786=CARTESIAN_POINT('Ctrl Pts',(6.52322516635678,-4.47565810211321,47.1760671492342));
#73787=CARTESIAN_POINT('Ctrl Pts',(6.52764130411679,-4.4692148105917,47.1763809861977));
#73788=CARTESIAN_POINT('Ctrl Pts',(6.53620623093292,-4.45667852143004,47.1769903080739));
#73789=CARTESIAN_POINT('Ctrl Pts',(6.54035606104994,-4.45058624584818,47.1772858305007));
#73790=CARTESIAN_POINT('Ctrl Pts',(6.55024855768903,-4.43601957003588,47.1779910208877));
#73791=CARTESIAN_POINT('Ctrl Pts',(6.55598330846205,-4.42753979692753,47.1784004029431));
#73792=CARTESIAN_POINT('Ctrl Pts',(6.5730822646045,-4.40215011456622,47.1796227775327));
#73793=CARTESIAN_POINT('Ctrl Pts',(6.58439766010758,-4.38520735537097,47.1804340135589));
#73794=CARTESIAN_POINT('Ctrl Pts',(6.68074219307624,-4.23973518679015,47.1873614975962));
#73795=CARTESIAN_POINT('Ctrl Pts',(6.76206667753845,-4.10878668738035,47.1933441548213));
#73796=CARTESIAN_POINT('Ctrl Pts',(6.95812338321501,-3.7714909698889,47.2081757774451));
#73797=CARTESIAN_POINT('Ctrl Pts',(7.06754294893992,-3.56222828415014,47.2168483091004));
#73798=CARTESIAN_POINT('Ctrl Pts',(7.3887225562299,-2.8747199788652,47.2440626368951));
#73799=CARTESIAN_POINT('Ctrl Pts',(7.56249729312747,-2.38030747265492,47.261659105346));
#73800=CARTESIAN_POINT('Ctrl Pts',(7.69743994340137,-1.82635766556305,47.2816347844914));
#73801=CARTESIAN_POINT('Ctrl Pts',(7.70823568311301,-1.78024341356534,47.2833002460176));
#73802=CARTESIAN_POINT('Ctrl Pts',(7.79617768542062,-1.38879197135364,47.2974759940629));
#73803=CARTESIAN_POINT('Ctrl Pts',(7.85048845373822,-1.03873342964161,47.3104247563517));
#73804=CARTESIAN_POINT('Ctrl Pts',(7.8830933049805,-0.664263670995458,47.3253806609481));
#73805=CARTESIAN_POINT('Ctrl Pts',(7.88491244522759,-0.642309892595684,
47.3262608425196));
#73806=CARTESIAN_POINT('Ctrl Pts',(7.88731710943287,-0.611738839610352,
47.3274909575115));
#73807=CARTESIAN_POINT('Ctrl Pts',(7.88798026308885,-0.603127649032909,
47.327837944498));
#73808=CARTESIAN_POINT('Ctrl Pts',(7.88909958375092,-0.588275375029725,
47.3284372433099));
#73809=CARTESIAN_POINT('Ctrl Pts',(7.88956245031833,-0.582034794041768,
47.3286893068093));
#73810=CARTESIAN_POINT('Ctrl Pts',(7.89050378939273,-0.569135760228505,
47.329210824724));
#73811=CARTESIAN_POINT('Ctrl Pts',(7.89098123927813,-0.56247723954678,47.3294803161161));
#73812=CARTESIAN_POINT('Ctrl Pts',(7.8920748739508,-0.546949923917408,47.3301094025728));
#73813=CARTESIAN_POINT('Ctrl Pts',(7.89268453752551,-0.538080686947398,
47.3304692301211));
#73814=CARTESIAN_POINT('Ctrl Pts',(7.89458736286652,-0.509699668737082,
47.3316221943042));
#73815=CARTESIAN_POINT('Ctrl Pts',(7.89582312584518,-0.490184189690269,
47.3324173256791));
#73816=CARTESIAN_POINT('Ctrl Pts',(7.89854535821062,-0.444509541536959,
47.3342834398075));
#73817=CARTESIAN_POINT('Ctrl Pts',(7.89997424569107,-0.418347233825442,
47.335356305222));
#73818=CARTESIAN_POINT('Ctrl Pts',(7.91471886997849,-0.121285286756925,
47.3475800447112));
#73819=CARTESIAN_POINT('Ctrl Pts',(7.91422397503901,0.150111827592864,47.3591335755547));
#73820=CARTESIAN_POINT('Ctrl Pts',(7.88213717775007,0.752292176635892,47.3850676212605));
#73821=CARTESIAN_POINT('Ctrl Pts',(7.84364992909478,1.08221534899094,47.3994689213465));
#73822=CARTESIAN_POINT('Ctrl Pts',(7.66817541820994,2.0518669186074,47.4417041897312));
#73823=CARTESIAN_POINT('Ctrl Pts',(7.47254266879963,2.67810316934097,47.4686537370505));
#73824=CARTESIAN_POINT('Ctrl Pts',(7.16405182416864,3.35689511887418,47.498944179107));
#73825=CARTESIAN_POINT('Ctrl Pts',(7.12453275336198,3.43997334261176,47.5026707887918));
#73826=CARTESIAN_POINT('Ctrl Pts',(7.06822609170747,3.5532082792783,47.5077765432924));
#73827=CARTESIAN_POINT('Ctrl Pts',(7.05267699734957,3.58397214563691,47.5091664147418));
#73828=CARTESIAN_POINT('Ctrl Pts',(7.02557433002293,3.63673530995529,47.5115549395013));
#73829=CARTESIAN_POINT('Ctrl Pts',(7.01411727383044,3.65878357576404,47.5125544784606));
#73830=CARTESIAN_POINT('Ctrl Pts',(6.99044221932511,3.70382457746943,47.5145993608149));
#73831=CARTESIAN_POINT('Ctrl Pts',(6.9782141969543,3.72681171358358,47.5156445933324));
#73832=CARTESIAN_POINT('Ctrl Pts',(6.94949517145449,3.7801629279324,47.5180742917522));
#73833=CARTESIAN_POINT('Ctrl Pts',(6.93291825824692,3.81048019748771,47.5194578717833));
#73834=CARTESIAN_POINT('Ctrl Pts',(6.89756756062527,3.87413819055065,47.5223692646396));
#73835=CARTESIAN_POINT('Ctrl Pts',(6.87874942628791,3.9074533034501,47.5238965792312));
#73836=CARTESIAN_POINT('Ctrl Pts',(6.82755822776219,3.99656486880716,47.5279920448011));
#73837=CARTESIAN_POINT('Ctrl Pts',(6.79474309315436,4.05210420349975,47.5305553842411));
#73838=CARTESIAN_POINT('Ctrl Pts',(6.69082123317496,4.22317834401804,47.5384874015076));
#73839=CARTESIAN_POINT('Ctrl Pts',(6.61741907635322,4.33729057192499,47.543830172373));
#73840=CARTESIAN_POINT('Ctrl Pts',(6.26220495168031,4.85948826144215,47.5685771929264));
#73841=CARTESIAN_POINT('Ctrl Pts',(5.9453583587887,5.24237996327339,47.5875294426775));
#73842=CARTESIAN_POINT('Ctrl Pts',(5.4454286461338,5.74245946195894,47.6150533307147));
#73843=CARTESIAN_POINT('Ctrl Pts',(5.29017838496186,5.88579158358921,47.6233372769485));
#73844=CARTESIAN_POINT('Ctrl Pts',(5.10810818817175,6.04085529265605,47.6329036302303));
#73845=CARTESIAN_POINT('Ctrl Pts',(5.08673748745857,6.05886158030195,47.6340242980488));
#73846=CARTESIAN_POINT('Ctrl Pts',(5.05446190479015,6.08576485758631,47.6357139857829));
#73847=CARTESIAN_POINT('Ctrl Pts',(5.04362788725564,6.09474665444711,47.636280692567));
#73848=CARTESIAN_POINT('Ctrl Pts',(5.02427938807021,6.11070034718542,47.637292001997));
#73849=CARTESIAN_POINT('Ctrl Pts',(5.01577420716808,6.11768348349997,47.6377362868188));
#73850=CARTESIAN_POINT('Ctrl Pts',(4.99936388303139,6.13109987218547,47.6385930393878));
#73851=CARTESIAN_POINT('Ctrl Pts',(4.99146082162064,6.1375356408873,47.6390054333093));
#73852=CARTESIAN_POINT('Ctrl Pts',(4.96960210718145,6.15526589367509,47.6401455166792));
#73853=CARTESIAN_POINT('Ctrl Pts',(4.95562051187254,6.16652808829732,47.6408741682749));
#73854=CARTESIAN_POINT('Ctrl Pts',(4.89133036672143,6.21795402887717,47.6442220235838));
#73855=CARTESIAN_POINT('Ctrl Pts',(4.84057161149337,6.25754994917423,47.6468576381398));
#73856=CARTESIAN_POINT('Ctrl Pts',(4.69742718465366,6.36643018168268,47.6542613891907));
#73857=CARTESIAN_POINT('Ctrl Pts',(4.60400004349902,6.43431723861928,47.6590605041097));
#73858=CARTESIAN_POINT('Ctrl Pts',(3.94959539979625,6.88827560978451,47.692350318289));
#73859=CARTESIAN_POINT('Ctrl Pts',(3.34224324798903,7.20257910155029,47.7213488155023));
#73860=CARTESIAN_POINT('Ctrl Pts',(2.62952386514692,7.46160162406339,47.7522653285838));
#73861=CARTESIAN_POINT('Ctrl Pts',(2.5565000757106,7.48693542689993,47.7554025908963));
#73862=CARTESIAN_POINT('Ctrl Pts',(2.45557636649406,7.52029966452929,47.7596988390509));
#73863=CARTESIAN_POINT('Ctrl Pts',(2.42798652892013,7.52925253662181,47.7608692830322));
#73864=CARTESIAN_POINT('Ctrl Pts',(2.38060862171707,7.54433911900497,47.7628724545998));
#73865=CARTESIAN_POINT('Ctrl Pts',(2.36084458931395,7.55054719743008,47.7637060895749));
#73866=CARTESIAN_POINT('Ctrl Pts',(2.32055730892999,7.56302818435468,47.7654013889756));
#73867=CARTESIAN_POINT('Ctrl Pts',(2.30003246020295,7.56929535867422,47.7662629774537));
#73868=CARTESIAN_POINT('Ctrl Pts',(2.25447917003463,7.58300246821759,47.7681706521633));
#73869=CARTESIAN_POINT('Ctrl Pts',(2.22943886535724,7.59040217069117,47.7692162495657));
#73870=CARTESIAN_POINT('Ctrl Pts',(2.15071001681499,7.61324426967253,47.7724944563385));
#73871=CARTESIAN_POINT('Ctrl Pts',(2.09689408810176,7.62824207310139,47.7747218452096));
#73872=CARTESIAN_POINT('Ctrl Pts',(1.97087206896162,7.66192838942477,47.7799087440057));
#73873=CARTESIAN_POINT('Ctrl Pts',(1.898551442613,7.68016835071773,47.7828632535244));
#73874=CARTESIAN_POINT('Ctrl Pts',(1.63979627083608,7.74155059314109,47.7933655242799));
#73875=CARTESIAN_POINT('Ctrl Pts',(1.45206617090166,7.77894866047001,47.8008617871516));
#73876=CARTESIAN_POINT('Ctrl Pts',(0.737626000234092,7.89450728526039,47.8291020033859));
#73877=CARTESIAN_POINT('Ctrl Pts',(0.204838750260679,7.9262481048425,47.8493553325807));
#73878=CARTESIAN_POINT('Ctrl Pts',(-0.859939844632741,7.88218405516834,
47.8892992384333));
#73879=CARTESIAN_POINT('Ctrl Pts',(-1.38914831036012,7.80631286403357,47.9089053365519));
#73880=CARTESIAN_POINT('Ctrl Pts',(-1.93726913229037,7.67019583393996,47.9311540884416));
#73881=CARTESIAN_POINT('Ctrl Pts',(-1.96783422549068,7.66241112550565,47.9324017006341));
#73882=CARTESIAN_POINT('Ctrl Pts',(-2.02881930333143,7.64648970287581,47.9349060385753));
#73883=CARTESIAN_POINT('Ctrl Pts',(-2.0592388864327,7.63835373108642,47.9361627232395));
#73884=CARTESIAN_POINT('Ctrl Pts',(-2.10102452542016,7.62691005816075,47.937900104747));
#73885=CARTESIAN_POINT('Ctrl Pts',(-2.11243313162462,7.62375808603977,47.9383756032993));
#73886=CARTESIAN_POINT('Ctrl Pts',(-2.13059010255261,7.61869778877025,47.9391342430108));
#73887=CARTESIAN_POINT('Ctrl Pts',(-2.13734309996184,7.61680606648379,47.9394168126078));
#73888=CARTESIAN_POINT('Ctrl Pts',(-2.15118152165493,7.61290964631828,47.9399967239507));
#73889=CARTESIAN_POINT('Ctrl Pts',(-2.15826667828691,7.61090403086734,47.9402940976044));
#73890=CARTESIAN_POINT('Ctrl Pts',(-2.17460179307648,7.60625535918422,47.9409807923337));
#73891=CARTESIAN_POINT('Ctrl Pts',(-2.18384974101013,7.60360531953823,47.9413703623874));
#73892=CARTESIAN_POINT('Ctrl Pts',(-2.21273488247147,7.59527111230424,47.9425897205102));
#73893=CARTESIAN_POINT('Ctrl Pts',(-2.23235480437353,7.5895277157014,47.9434216731564));
#73894=CARTESIAN_POINT('Ctrl Pts',(-2.35275226495463,7.5537761671532,47.9485508081144));
#73895=CARTESIAN_POINT('Ctrl Pts',(-2.45294329064368,7.5218379881809,47.9529236003825));
#73896=CARTESIAN_POINT('Ctrl Pts',(-2.63539211865668,7.4596450655571,47.9611111491081));
#73897=CARTESIAN_POINT('Ctrl Pts',(-2.71783713640815,7.43000380961191,47.9648925874722));
#73898=CARTESIAN_POINT('Ctrl Pts',(-3.00728413053081,7.32047750159764,47.9784195732065));
#73899=CARTESIAN_POINT('Ctrl Pts',(-3.21139474162638,7.23326239146605,47.9884154079134));
#73900=CARTESIAN_POINT('Ctrl Pts',(-3.58952167362219,7.05252864915296,48.0075030091861));
#73901=CARTESIAN_POINT('Ctrl Pts',(-3.76423803385518,6.96084316891591,48.0165656252967));
#73902=CARTESIAN_POINT('Ctrl Pts',(-4.21856237296,6.70031651382927,48.0405420248595));
#73903=CARTESIAN_POINT('Ctrl Pts',(-4.49146807289192,6.52052486342861,48.0553648519783));
#73904=CARTESIAN_POINT('Ctrl Pts',(-4.77241096900344,6.30940847092551,48.0708082145645));
#73905=CARTESIAN_POINT('Ctrl Pts',(-4.7922575592923,6.29434740125348,48.0719003194724));
#73906=CARTESIAN_POINT('Ctrl Pts',(-4.82645107373434,6.26814334629931,48.0737837648297));
#73907=CARTESIAN_POINT('Ctrl Pts',(-4.8408313310634,6.25704427073916,48.0745764337799));
#73908=CARTESIAN_POINT('Ctrl Pts',(-5.07250449198112,6.07695587478927,48.0873556867056));
#73909=CARTESIAN_POINT('Ctrl Pts',(-5.28088137550097,5.8967792716278,48.0989680267563));
#73910=CARTESIAN_POINT('Ctrl Pts',(-5.49738550172323,5.68887437167324,48.1111458096397));
#73911=CARTESIAN_POINT('Ctrl Pts',(-5.51523481217416,5.67157155930505,48.1121507471062));
#73912=CARTESIAN_POINT('Ctrl Pts',(-5.54017564083878,5.64716527101583,48.1135563454284));
#73913=CARTESIAN_POINT('Ctrl Pts',(-5.54733555898057,5.64013208413544,48.1139600226335));
#73914=CARTESIAN_POINT('Ctrl Pts',(-5.55973254446703,5.62790808422978,48.114659254655));
#73915=CARTESIAN_POINT('Ctrl Pts',(-5.56497576724319,5.6227235465513,48.1149550800527));
#73916=CARTESIAN_POINT('Ctrl Pts',(-5.57586565999506,5.61192538608245,48.1155696828542));
#73917=CARTESIAN_POINT('Ctrl Pts',(-5.58151112073804,5.60631055212167,48.1158884071425));
#73918=CARTESIAN_POINT('Ctrl Pts',(-5.59477642000101,5.59307732036313,48.1166375763864));
#73919=CARTESIAN_POINT('Ctrl Pts',(-5.6023891981491,5.58545185056595,48.1170677123635));
#73920=CARTESIAN_POINT('Ctrl Pts',(-5.62719034241709,5.56050764108037,48.1184696815681));
#73921=CARTESIAN_POINT('Ctrl Pts',(-5.64431424186207,5.543124852365,48.1194387050206));
#73922=CARTESIAN_POINT('Ctrl Pts',(-5.93624299982986,5.24402715662592,48.1359773077054));
#73923=CARTESIAN_POINT('Ctrl Pts',(-6.18974169804896,4.94226095450934,48.1505842561011));
#73924=CARTESIAN_POINT('Ctrl Pts',(-6.50460158135436,4.50501553374898,48.1697118311163));
#73925=CARTESIAN_POINT('Ctrl Pts',(-6.58619638650574,4.38486319206651,48.1747812393075));
#73926=CARTESIAN_POINT('Ctrl Pts',(-6.70021841873724,4.20659050242261,48.1820919168049));
#73927=CARTESIAN_POINT('Ctrl Pts',(-6.73529209956454,4.15020131225435,48.18437473216));
#73928=CARTESIAN_POINT('Ctrl Pts',(-6.80974071934134,4.02707772977019,48.1893046423746));
#73929=CARTESIAN_POINT('Ctrl Pts',(-6.84885359504892,3.96019295183269,48.1919487253613));
#73930=CARTESIAN_POINT('Ctrl Pts',(-7.19215682309999,3.35282664222387,48.2157207396363));
#73931=CARTESIAN_POINT('Ctrl Pts',(-7.43274886908881,2.7789599659171,48.2363760643762));
#73932=CARTESIAN_POINT('Ctrl Pts',(-7.61391684432018,2.14791137832844,48.2622672028282));
#73933=CARTESIAN_POINT('Ctrl Pts',(-7.62374482652852,2.11276305868083,48.2637196372793));
#73934=CARTESIAN_POINT('Ctrl Pts',(-7.63546308353798,2.06970783689401,48.2655127148362));
#73935=CARTESIAN_POINT('Ctrl Pts',(-7.63758497791168,2.06186389814465,48.2658399462566));
#73936=CARTESIAN_POINT('Ctrl Pts',(-7.64106500225261,2.04892032111823,48.2663808700951));
#73937=CARTESIAN_POINT('Ctrl Pts',(-7.64243012502068,2.04382255463084,48.2665941524558));
#73938=CARTESIAN_POINT('Ctrl Pts',(-7.64488203191978,2.03462961485323,48.2669792123101));
#73939=CARTESIAN_POINT('Ctrl Pts',(-7.6459706301708,2.03053492312723,48.2671508825104));
#73940=CARTESIAN_POINT('Ctrl Pts',(-7.64828622352328,2.02179670367436,48.2675175734138));
#73941=CARTESIAN_POINT('Ctrl Pts',(-7.64951227982905,2.01715293135447,48.2677126498599));
#73942=CARTESIAN_POINT('Ctrl Pts',(-7.65280370937594,2.004640259806,48.2682388431482));
#73943=CARTESIAN_POINT('Ctrl Pts',(-7.65486117112818,1.99676929950929,48.2685704342234));
#73944=CARTESIAN_POINT('Ctrl Pts',(-7.66529808349809,1.95658897130564,48.2702662612477));
#73945=CARTESIAN_POINT('Ctrl Pts',(-7.67348501698635,1.92423042792129,48.2716421591186));
#73946=CARTESIAN_POINT('Ctrl Pts',(-7.74935125792392,1.61618656523759,48.2848297104512));
#73947=CARTESIAN_POINT('Ctrl Pts',(-7.80234523184467,1.33711852353933,48.2974500386472));
#73948=CARTESIAN_POINT('Ctrl Pts',(-7.88700764005071,0.708447202027818,
48.3263919145905));
#73949=CARTESIAN_POINT('Ctrl Pts',(-7.91064898259738,0.358344491411203,
48.342843249367));
#73950=CARTESIAN_POINT('Ctrl Pts',(-7.91099612024181,0.0078348911301656,
48.3590392895494));
#73951=CARTESIAN_POINT('',(-7.911,-2.19824158875781E-13,50.357668491763));
#73952=CARTESIAN_POINT('Ctrl Pts',(-7.911,-3.90243393155743E-13,48.357668491763));
#73953=CARTESIAN_POINT('Ctrl Pts',(-7.91099999999989,-2.20167589666719,
48.4462559274957));
#73954=CARTESIAN_POINT('Ctrl Pts',(-6.94214576672347,-4.38610418338723,
48.5348433632285));
#73955=CARTESIAN_POINT('Ctrl Pts',(-3.67820201488239,-7.34180684107656,
48.7120182346939));
#73956=CARTESIAN_POINT('Ctrl Pts',(-1.40868175871689,-8.08992666571347,
48.8006056704267));
#73957=CARTESIAN_POINT('Ctrl Pts',(2.97309270521332,-7.65454228025235,48.9777805418921));
#73958=CARTESIAN_POINT('Ctrl Pts',(5.05102072675654,-6.47444880834186,49.0663679776248));
#73959=CARTESIAN_POINT('Ctrl Pts',(7.66951518847898,-2.93425195367641,49.2435428490903));
#73960=CARTESIAN_POINT('Ctrl Pts',(8.18956872247078,-0.601881960098432,
49.332130284823));
#73961=CARTESIAN_POINT('Ctrl Pts',(7.32306689761308,3.71537198232521,49.5093051562885));
#73962=CARTESIAN_POINT('Ctrl Pts',(5.94329958850145,5.66643518936571,49.5978925920212));
#73963=CARTESIAN_POINT('Ctrl Pts',(2.16154501637763,7.92205913233022,49.7750674634866));
#73964=CARTESIAN_POINT('Ctrl Pts',(-0.21081652930128,8.20894963713001,49.8636548992194));
#73965=CARTESIAN_POINT('Ctrl Pts',(-4.42123908576519,6.9198224471778,50.0408297706848));
#73966=CARTESIAN_POINT('Ctrl Pts',(-6.22631625634254,5.35390358803445,50.1294172064176));
#73967=CARTESIAN_POINT('Ctrl Pts',(-7.65317280859507,2.31334857514446,50.2645592586879));
#73968=CARTESIAN_POINT('Ctrl Pts',(-7.91100000000003,1.15702837836471,50.3111138752254));
#73969=CARTESIAN_POINT('Ctrl Pts',(-7.911,-2.19824158875781E-13,50.357668491763));
#73970=CARTESIAN_POINT('',(-7.91058521897938,0.00383761197256053,54.357668491763));
#73971=CARTESIAN_POINT('Ctrl Pts',(-7.91099932750376,-0.00326193729837859,
50.3656282681517));
#73972=CARTESIAN_POINT('Ctrl Pts',(-7.91063423660574,-0.888697058967943,
50.3987126545666));
#73973=CARTESIAN_POINT('Ctrl Pts',(-7.76164164915843,-1.7676886397623,50.4265561435748));
#73974=CARTESIAN_POINT('Ctrl Pts',(-7.39460813755596,-2.82072656698914,
50.4666422517194));
#73975=CARTESIAN_POINT('Ctrl Pts',(-7.30956138900448,-3.03430811676538,
50.4752003333027));
#73976=CARTESIAN_POINT('Ctrl Pts',(-7.20239712110214,-3.27267384299411,
50.4855406317549));
#73977=CARTESIAN_POINT('Ctrl Pts',(-7.18927519264712,-3.30139978270516,
50.4868001333683));
#73978=CARTESIAN_POINT('Ctrl Pts',(-7.17254955064214,-3.33744219837014,
50.4883981547481));
#73979=CARTESIAN_POINT('Ctrl Pts',(-7.16910589495979,-3.3448330526048,50.4887267866171));
#73980=CARTESIAN_POINT('Ctrl Pts',(-7.16361390435419,-3.35657264730443,
50.4892503004327));
#73981=CARTESIAN_POINT('Ctrl Pts',(-7.16157301362628,-3.36092488425353,
50.4894447153364));
#73982=CARTESIAN_POINT('Ctrl Pts',(-7.15772602583966,-3.36910924224991,
50.4898109406299));
#73983=CARTESIAN_POINT('Ctrl Pts',(-7.15592081400479,-3.3729417799237,50.489982694956));
#73984=CARTESIAN_POINT('Ctrl Pts',(-7.15186248429565,-3.38153985525506,
50.4903686028632));
#73985=CARTESIAN_POINT('Ctrl Pts',(-7.1496076819584,-3.38630459066725,50.4905828639103));
#73986=CARTESIAN_POINT('Ctrl Pts',(-7.14387483622987,-3.39838770299386,
50.4911272548192));
#73987=CARTESIAN_POINT('Ctrl Pts',(-7.14039031243064,-3.40570298789622,
50.491457803182));
#73988=CARTESIAN_POINT('Ctrl Pts',(-7.12015774580656,-3.44801097131292,
50.493375179992));
#73989=CARTESIAN_POINT('Ctrl Pts',(-7.10316401870511,-3.48288483935802,
50.4949779653658));
#73990=CARTESIAN_POINT('Ctrl Pts',(-6.71689667658263,-4.26098149611558,
50.5312134315314));
#73991=CARTESIAN_POINT('Ctrl Pts',(-6.23321298979244,-4.94165389363112,
50.5719986646624));
#73992=CARTESIAN_POINT('Ctrl Pts',(-5.38231149584855,-5.81066124078991,
50.6265882289182));
#73993=CARTESIAN_POINT('Ctrl Pts',(-5.0922640082942,-6.06646249653365,50.6432017720806));
#73994=CARTESIAN_POINT('Ctrl Pts',(-4.76400018778417,-6.31576566792567,
50.6598955089649));
#73995=CARTESIAN_POINT('Ctrl Pts',(-4.74326708212672,-6.33135144869598,
50.6609416686046));
#73996=CARTESIAN_POINT('Ctrl Pts',(-4.71403236474659,-6.3531039773494,50.6624053715415));
#73997=CARTESIAN_POINT('Ctrl Pts',(-4.70559467430217,-6.3593561030386,50.6628264946215));
#73998=CARTESIAN_POINT('Ctrl Pts',(-4.69127469031386,-6.36992276213706,
50.6635389582765));
#73999=CARTESIAN_POINT('Ctrl Pts',(-4.68539884482381,-6.37424598528254,
50.6638306620299));
#74000=CARTESIAN_POINT('Ctrl Pts',(-4.67362046080042,-6.38288698561992,
50.6644141212929));
#74001=CARTESIAN_POINT('Ctrl Pts',(-4.66771789811827,-6.38720471777697,
50.6647058748133));
#74002=CARTESIAN_POINT('Ctrl Pts',(-4.65346027807135,-6.39760386633642,
50.6654090685833));
#74003=CARTESIAN_POINT('Ctrl Pts',(-4.64509926483095,-6.40367711640235,
50.6658201688268));
#74004=CARTESIAN_POINT('Ctrl Pts',(-4.61691819233748,-6.42406297357864,
50.6672015420334));
#74005=CARTESIAN_POINT('Ctrl Pts',(-4.59704359721091,-6.43830015324268,
50.6681686863293));
#74006=CARTESIAN_POINT('Ctrl Pts',(-4.30946534927441,-6.64229651524981,
50.682062213375));
#74007=CARTESIAN_POINT('Ctrl Pts',(-4.03026401943296,-6.81532061400327,
50.6942762938282));
#74008=CARTESIAN_POINT('Ctrl Pts',(-3.56714627047105,-7.06387742817192,
50.7130218432213));
#74009=CARTESIAN_POINT('Ctrl Pts',(-3.3897561518577,-7.15069603207906,50.7198766917271));
#74010=CARTESIAN_POINT('Ctrl Pts',(-2.91880780771747,-7.35972083587991,
50.7375115356681));
#74011=CARTESIAN_POINT('Ctrl Pts',(-2.6208141685694,-7.47102807635808,50.7481113814818));
#74012=CARTESIAN_POINT('Ctrl Pts',(-2.07511709197775,-7.63817860538175,
50.767591464366));
#74013=CARTESIAN_POINT('Ctrl Pts',(-1.82989674434693,-7.70060707156553,
50.7763741630215));
#74014=CARTESIAN_POINT('Ctrl Pts',(-1.42178340387637,-7.78390854928552,
50.7916321369029));
#74015=CARTESIAN_POINT('Ctrl Pts',(-1.26047744385343,-7.81165096422,50.7978253555369));
#74016=CARTESIAN_POINT('Ctrl Pts',(-1.07340306882081,-7.83788019074037,
50.805316173043));
#74017=CARTESIAN_POINT('Ctrl Pts',(-1.04835244484867,-7.84127012383302,
50.8063255981188));
#74018=CARTESIAN_POINT('Ctrl Pts',(-1.01614371614511,-7.84547161314059,
50.8076321223189));
#74019=CARTESIAN_POINT('Ctrl Pts',(-1.00899989738426,-7.84639357226209,
50.8079224531657));
#74020=CARTESIAN_POINT('Ctrl Pts',(-0.997463458267445,-7.84786641375185,
50.8083922014527));
#74021=CARTESIAN_POINT('Ctrl Pts',(-0.993071603142432,-7.84842336966654,
50.8085712418834));
#74022=CARTESIAN_POINT('Ctrl Pts',(-0.984652612487927,-7.84948384953678,
50.8089148537254));
#74023=CARTESIAN_POINT('Ctrl Pts',(-0.980625550133025,-7.84998796188372,
50.8090793889136));
#74024=CARTESIAN_POINT('Ctrl Pts',(-0.971456179871651,-7.85112862836833,
50.8094544209483));
#74025=CARTESIAN_POINT('Ctrl Pts',(-0.966313635628383,-7.85176322910566,
50.8096650369379));
#74026=CARTESIAN_POINT('Ctrl Pts',(-0.950350929076437,-7.85371714083951,
50.8103196699765));
#74027=CARTESIAN_POINT('Ctrl Pts',(-0.939528702607679,-7.85501913627895,
50.8107647326468));
#74028=CARTESIAN_POINT('Ctrl Pts',(-0.858014369367423,-7.86465505765254,
50.8141261609303));
#74029=CARTESIAN_POINT('Ctrl Pts',(-0.787217446142281,-7.87205665017447,
50.8170974954753));
#74030=CARTESIAN_POINT('Ctrl Pts',(0.105485361785373,-7.95322335909915,
50.8551308992811));
#74031=CARTESIAN_POINT('Ctrl Pts',(0.933937673404021,-7.89891116636909,
50.8959169165339));
#74032=CARTESIAN_POINT('Ctrl Pts',(2.0094783372895,-7.65655040098159,50.9461236864054));
#74033=CARTESIAN_POINT('Ctrl Pts',(2.27653369032454,-7.58143664270754,50.958413900549));
#74034=CARTESIAN_POINT('Ctrl Pts',(2.65568166224125,-7.45294738704457,50.9755046828491));
#74035=CARTESIAN_POINT('Ctrl Pts',(2.77131593517592,-7.41072734110451,50.9806690258752));
#74036=CARTESIAN_POINT('Ctrl Pts',(2.92748307521145,-7.34954123333943,50.9875799241129));
#74037=CARTESIAN_POINT('Ctrl Pts',(2.96890622451487,-7.33290593255651,50.9894068764352));
#74038=CARTESIAN_POINT('Ctrl Pts',(3.0295342706359,-7.30796009828118,50.992072135664));
#74039=CARTESIAN_POINT('Ctrl Pts',(3.04885015050332,-7.29992270259909,50.9929199705968));
#74040=CARTESIAN_POINT('Ctrl Pts',(3.08358487765025,-7.28530756361843,50.9944422848897));
#74041=CARTESIAN_POINT('Ctrl Pts',(3.09901509461972,-7.27875727320003,50.9951177210501));
#74042=CARTESIAN_POINT('Ctrl Pts',(3.12266878670622,-7.2686271801626,50.9961518923237));
#74043=CARTESIAN_POINT('Ctrl Pts',(3.13090714140652,-7.26508237449968,50.9965118535135));
#74044=CARTESIAN_POINT('Ctrl Pts',(3.14598101444148,-7.25856597482103,50.9971700637796));
#74045=CARTESIAN_POINT('Ctrl Pts',(3.15281838956543,-7.25559871801612,50.9974684645234));
#74046=CARTESIAN_POINT('Ctrl Pts',(3.1665246744098,-7.24962748641381,50.9980663294654));
#74047=CARTESIAN_POINT('Ctrl Pts',(3.17339352792987,-7.24662340146897,50.9983657893837));
#74048=CARTESIAN_POINT('Ctrl Pts',(3.19277367715162,-7.23811467714271,50.9992102607914));
#74049=CARTESIAN_POINT('Ctrl Pts',(3.20527501973949,-7.23258735745982,50.9997544754803));
#74050=CARTESIAN_POINT('Ctrl Pts',(3.25709765267804,-7.20951384674716,51.0020083352734));
#74051=CARTESIAN_POINT('Ctrl Pts',(3.29629003291522,-7.19167901955263,51.0037078287843));
#74052=CARTESIAN_POINT('Ctrl Pts',(3.92440111653819,-6.89963834637898,51.0308695871601));
#74053=CARTESIAN_POINT('Ctrl Pts',(4.47752131993072,-6.55422069360326,51.0534437952189));
#74054=CARTESIAN_POINT('Ctrl Pts',(5.39998542451969,-5.80632317968186,51.094435484315));
#74055=CARTESIAN_POINT('Ctrl Pts',(5.78215959746906,-5.42585122552941,51.1129358520177));
#74056=CARTESIAN_POINT('Ctrl Pts',(6.14724811627211,-4.97963418290188,51.1357270807106));
#74057=CARTESIAN_POINT('Ctrl Pts',(6.17151244847477,-4.94953028314072,51.1372679193379));
#74058=CARTESIAN_POINT('Ctrl Pts',(6.20262220522515,-4.91034906656276,51.1392764267488));
#74059=CARTESIAN_POINT('Ctrl Pts',(6.20967037756325,-4.90143284932954,51.1397336928014));
#74060=CARTESIAN_POINT('Ctrl Pts',(6.22103623580378,-4.88699072340626,51.1404746467236));
#74061=CARTESIAN_POINT('Ctrl Pts',(6.22536584640322,-4.88147418879481,51.1407577416441));
#74062=CARTESIAN_POINT('Ctrl Pts',(6.23362403128001,-4.87092324059049,51.1412993120964));
#74063=CARTESIAN_POINT('Ctrl Pts',(6.2375538578542,-4.86588981062454,51.1415577262579));
#74064=CARTESIAN_POINT('Ctrl Pts',(6.24653522661612,-4.85435746692604,51.1421499041103));
#74065=CARTESIAN_POINT('Ctrl Pts',(6.25158272431997,-4.84785542218394,51.1424838609734));
#74066=CARTESIAN_POINT('Ctrl Pts',(6.26707029842123,-4.82784035278812,51.1435120966067));
#74067=CARTESIAN_POINT('Ctrl Pts',(6.27747673954671,-4.81430144218547,51.1442079468739));
#74068=CARTESIAN_POINT('Ctrl Pts',(6.35682010230064,-4.71038007803364,51.1495509832883));
#74069=CARTESIAN_POINT('Ctrl Pts',(6.423843875146,-4.61855721634384,51.1542825802134));
#74070=CARTESIAN_POINT('Ctrl Pts',(6.52143169782487,-4.47862602200934,51.1614788080948));
#74071=CARTESIAN_POINT('Ctrl Pts',(6.55349398485417,-4.43157747167014,51.1638960303008));
#74072=CARTESIAN_POINT('Ctrl Pts',(6.79779901849484,-4.06463155035454,51.1827126405753));
#74073=CARTESIAN_POINT('Ctrl Pts',(6.9870065341398,-3.73001785183359,51.1996341410474));
#74074=CARTESIAN_POINT('Ctrl Pts',(7.38844920209015,-2.88142591067553,51.240686806223));
#74075=CARTESIAN_POINT('Ctrl Pts',(7.57231676403376,-2.35624767753718,51.2644782673826));
#74076=CARTESIAN_POINT('Ctrl Pts',(7.71897264172309,-1.73447949806625,51.2906027960045));
#74077=CARTESIAN_POINT('Ctrl Pts',(7.73693055376853,-1.65253249969406,51.2940097092983));
#74078=CARTESIAN_POINT('Ctrl Pts',(7.7585901288799,-1.54558622697846,51.2984123155001));
#74079=CARTESIAN_POINT('Ctrl Pts',(7.7634799916461,-1.52083398198157,51.2994282394327));
#74080=CARTESIAN_POINT('Ctrl Pts',(7.77115261856333,-1.48099403773544,51.3010585091507));
#74081=CARTESIAN_POINT('Ctrl Pts',(7.77401004138998,-1.46592095254761,51.3016741795222));
#74082=CARTESIAN_POINT('Ctrl Pts',(7.77936394008192,-1.43722286271735,51.3028442243728));
#74083=CARTESIAN_POINT('Ctrl Pts',(7.78186851133127,-1.42359943212925,51.3033987431802));
#74084=CARTESIAN_POINT('Ctrl Pts',(7.78740038003018,-1.39305839362213,51.3046398036761));
#74085=CARTESIAN_POINT('Ctrl Pts',(7.79040835784552,-1.37613734333906,51.3053259892732));
#74086=CARTESIAN_POINT('Ctrl Pts',(7.79914666109466,-1.32603403008984,51.3073536044046));
#74087=CARTESIAN_POINT('Ctrl Pts',(7.80472031178468,-1.29282472373236,51.308692115306));
#74088=CARTESIAN_POINT('Ctrl Pts',(7.84212571670478,-1.06089097389523,51.318002652047));
#74089=CARTESIAN_POINT('Ctrl Pts',(7.86657669874312,-0.861046421528195,
51.325829613732));
#74090=CARTESIAN_POINT('Ctrl Pts',(7.94183784018527,0.0372569469019125,
51.3602648290222));
#74091=CARTESIAN_POINT('Ctrl Pts',(7.9074062962736,0.73960622461558,51.3848085260178));
#74092=CARTESIAN_POINT('Ctrl Pts',(7.75162801654313,1.58829116898041,51.4169862370396));
#74093=CARTESIAN_POINT('Ctrl Pts',(7.71731590269283,1.74740880518786,51.4231519121374));
#74094=CARTESIAN_POINT('Ctrl Pts',(7.66041220999307,1.97671770845446,51.4323595058966));
#74095=CARTESIAN_POINT('Ctrl Pts',(7.64170805330582,2.04783439099113,51.4352608630616));
#74096=CARTESIAN_POINT('Ctrl Pts',(7.61860440282805,2.13095053792775,51.4387158590626));
#74097=CARTESIAN_POINT('Ctrl Pts',(7.61516352053112,2.14321436043001,51.4392272915709));
#74098=CARTESIAN_POINT('Ctrl Pts',(7.60985437816535,2.16196273846169,51.440011737437));
#74099=CARTESIAN_POINT('Ctrl Pts',(7.6080074037426,2.16845333903307,51.4402837846418));
#74100=CARTESIAN_POINT('Ctrl Pts',(7.60462856238002,2.18026973997827,51.4407799368376));
#74101=CARTESIAN_POINT('Ctrl Pts',(7.60309939848854,2.18559631389278,51.4410039170493));
#74102=CARTESIAN_POINT('Ctrl Pts',(7.60001808473597,2.19628716163343,51.4414541245232));
#74103=CARTESIAN_POINT('Ctrl Pts',(7.59846584944184,2.20165140730623,51.4416803556896));
#74104=CARTESIAN_POINT('Ctrl Pts',(7.59404318161773,2.21687496292786,51.4423233543292));
#74105=CARTESIAN_POINT('Ctrl Pts',(7.5911592380479,2.2267303084558,51.4427407614954));
#74106=CARTESIAN_POINT('Ctrl Pts',(7.57891501485255,2.2682724409519,51.444505150697));
#74107=CARTESIAN_POINT('Ctrl Pts',(7.56937550295443,2.29990590214824,51.4458608538362));
#74108=CARTESIAN_POINT('Ctrl Pts',(7.39497442130201,2.86538780760916,51.4703268676657));
#74109=CARTESIAN_POINT('Ctrl Pts',(7.17422499549569,3.38030937108751,51.4961903902932));
#74110=CARTESIAN_POINT('Ctrl Pts',(6.66939671667504,4.28108686670812,51.5437815146591));
#74111=CARTESIAN_POINT('Ctrl Pts',(6.40097647765962,4.67291429104499,51.5654411550374));
#74112=CARTESIAN_POINT('Ctrl Pts',(5.95550333857063,5.21217020002396,51.5957110302301));
#74113=CARTESIAN_POINT('Ctrl Pts',(5.8045640074937,5.37975699800221,51.6052068379761));
#74114=CARTESIAN_POINT('Ctrl Pts',(5.61775566994624,5.57013877003414,51.6161019565985));
#74115=CARTESIAN_POINT('Ctrl Pts',(5.58861673988847,5.59937386534448,51.6177783266812));
#74116=CARTESIAN_POINT('Ctrl Pts',(5.54957879140493,5.63793233564672,51.6199939762504));
#74117=CARTESIAN_POINT('Ctrl Pts',(5.53988288856258,5.64745990394324,51.6205418343414));
#74118=CARTESIAN_POINT('Ctrl Pts',(5.52389686009039,5.66308760783795,51.6214411109277));
#74119=CARTESIAN_POINT('Ctrl Pts',(5.51762108939954,5.66920235036549,51.6217931397571));
#74120=CARTESIAN_POINT('Ctrl Pts',(5.50542212751849,5.68104885866696,51.6224754715833));
#74121=CARTESIAN_POINT('Ctrl Pts',(5.49950011348128,5.68678181743053,51.6228058241403));
#74122=CARTESIAN_POINT('Ctrl Pts',(5.48578026008289,5.70002220216885,51.6235691255691));
#74123=CARTESIAN_POINT('Ctrl Pts',(5.4779759427878,5.70752290740185,51.6240017953849));
#74124=CARTESIAN_POINT('Ctrl Pts',(5.45695324696115,5.72764491579377,51.6251632181735));
#74125=CARTESIAN_POINT('Ctrl Pts',(5.44370645120136,5.74023650205877,51.6258907436819));
#74126=CARTESIAN_POINT('Ctrl Pts',(5.3489331746052,5.82969901162738,51.631065315766));
#74127=CARTESIAN_POINT('Ctrl Pts',(5.26582350120573,5.90487770732505,51.6354427939177));
#74128=CARTESIAN_POINT('Ctrl Pts',(4.46784028501046,6.59646017467778,51.6760596632883));
#74129=CARTESIAN_POINT('Ctrl Pts',(3.64977825246519,7.08193125345826,51.7062720770154));
#74130=CARTESIAN_POINT('Ctrl Pts',(2.54270612159614,7.49500767279357,51.7489629801311));
#74131=CARTESIAN_POINT('Ctrl Pts',(2.31622778672315,7.56806331576251,51.7578405315634));
#74132=CARTESIAN_POINT('Ctrl Pts',(2.04837679128682,7.64131274478681,51.7687915318567));
#74133=CARTESIAN_POINT('Ctrl Pts',(2.00987291568815,7.65153048277121,51.7703752781873));
#74134=CARTESIAN_POINT('Ctrl Pts',(1.95990874526714,7.66438627129496,51.772441348935));
#74135=CARTESIAN_POINT('Ctrl Pts',(1.94851702038957,7.66729030523684,51.7729131430695));
#74136=CARTESIAN_POINT('Ctrl Pts',(1.93007339448916,7.67194828561836,51.7736781398163));
#74137=CARTESIAN_POINT('Ctrl Pts',(1.92302545144595,7.67371793317806,51.773970741457));
#74138=CARTESIAN_POINT('Ctrl Pts',(1.90954567749892,7.67708279353225,51.774530870607));
#74139=CARTESIAN_POINT('Ctrl Pts',(1.90311425805807,7.67867964129635,51.7747983366184));
#74140=CARTESIAN_POINT('Ctrl Pts',(1.88837417068295,7.68231977989668,51.7754118300176));
#74141=CARTESIAN_POINT('Ctrl Pts',(1.88006418627116,7.68435767412717,51.7757580552635));
#74142=CARTESIAN_POINT('Ctrl Pts',(1.85444800737679,7.69059560326202,51.7768263920191));
#74143=CARTESIAN_POINT('Ctrl Pts',(1.83713098446359,7.69475067074946,51.7775501119269));
#74144=CARTESIAN_POINT('Ctrl Pts',(1.70079499748576,7.72697682673053,51.78325903948));
#74145=CARTESIAN_POINT('Ctrl Pts',(1.58115643454892,7.75234269729421,51.7883350485991));
#74146=CARTESIAN_POINT('Ctrl Pts',(1.45278627155921,7.77646465831772,51.7938234873725));
#74147=CARTESIAN_POINT('Ctrl Pts',(1.4445886457859,7.77799165446749,51.7941741585694));
#74148=CARTESIAN_POINT('Ctrl Pts',(1.42645633685526,7.78133955901198,51.7949501958034));
#74149=CARTESIAN_POINT('Ctrl Pts',(1.41652055434346,7.78315440758768,51.7953756909288));
#74150=CARTESIAN_POINT('Ctrl Pts',(1.36811606380002,7.79190010934326,51.797449778226));
#74151=CARTESIAN_POINT('Ctrl Pts',(1.32960003092727,7.79856477821357,51.7991038036884));
#74152=CARTESIAN_POINT('Ctrl Pts',(1.28397015148832,7.80611253752531,51.8010667402087));
#74153=CARTESIAN_POINT('Ctrl Pts',(1.27690230142591,7.80727179050651,51.8013708866054));
#74154=CARTESIAN_POINT('Ctrl Pts',(1.26133882707402,7.80980277731577,51.8020408233448));
#74155=CARTESIAN_POINT('Ctrl Pts',(1.25284252157402,7.81117024992796,51.8024066839993));
#74156=CARTESIAN_POINT('Ctrl Pts',(0.857517511695545,7.87413585671681,51.8194356759236));
#74157=CARTESIAN_POINT('Ctrl Pts',(0.466650511508528,7.90693308887498,51.8364900694726));
#74158=CARTESIAN_POINT('Ctrl Pts',(-0.629153019894741,7.91731721787121,
51.8835976835022));
#74159=CARTESIAN_POINT('Ctrl Pts',(-1.33103062751872,7.82995393213053,51.9126928418116));
#74160=CARTESIAN_POINT('Ctrl Pts',(-2.09882235532606,7.62803456406769,51.9449342065091));
#74161=CARTESIAN_POINT('Ctrl Pts',(-2.18517603357127,7.60374726396495,51.9485667238278));
#74162=CARTESIAN_POINT('Ctrl Pts',(-2.30639371131205,7.56741876052888,51.9536744990779));
#74163=CARTESIAN_POINT('Ctrl Pts',(-2.34161474811365,7.55659440705687,51.9551596697928));
#74164=CARTESIAN_POINT('Ctrl Pts',(-2.40226245505702,7.53749103215405,51.9577188867632));
#74165=CARTESIAN_POINT('Ctrl Pts',(-2.42772510493538,7.52932844167626,51.9587939360702));
#74166=CARTESIAN_POINT('Ctrl Pts',(-2.47650989011661,7.51341624784282,51.9608548037052));
#74167=CARTESIAN_POINT('Ctrl Pts',(-2.4998382554459,7.5056867540398,51.9618407926653));
#74168=CARTESIAN_POINT('Ctrl Pts',(-2.56090266114423,7.48513773301162,51.9644230995938));
#74169=CARTESIAN_POINT('Ctrl Pts',(-2.59857856846938,7.47214151115732,51.9660177313941));
#74170=CARTESIAN_POINT('Ctrl Pts',(-2.73049014053044,7.42552054402354,51.9716061759972));
#74171=CARTESIAN_POINT('Ctrl Pts',(-2.82418513209205,7.39039311353117,51.9755849936637));
#74172=CARTESIAN_POINT('Ctrl Pts',(-3.4235573176014,7.15261754702738,52.001117643302));
#74173=CARTESIAN_POINT('Ctrl Pts',(-3.90782265814914,6.89997198770932,52.0220186039863));
#74174=CARTESIAN_POINT('Ctrl Pts',(-4.53175182091598,6.48755844986922,52.0509942942786));
#74175=CARTESIAN_POINT('Ctrl Pts',(-4.69684170747475,6.36905525078565,52.0588944000711));
#74176=CARTESIAN_POINT('Ctrl Pts',(-4.93347142297377,6.18499164411376,52.0707216214523));
#74177=CARTESIAN_POINT('Ctrl Pts',(-5.00866345580982,6.12425928896814,52.0745596792913));
#74178=CARTESIAN_POINT('Ctrl Pts',(-5.09963491146074,6.04798576783761,52.0793176655236));
#74179=CARTESIAN_POINT('Ctrl Pts',(-5.11648747214332,6.0337354946045,52.080204025323));
#74180=CARTESIAN_POINT('Ctrl Pts',(-5.14289908414766,6.01121200946461,52.081601173204));
#74181=CARTESIAN_POINT('Ctrl Pts',(-5.15249835023151,6.00298605378961,52.0821106459879));
#74182=CARTESIAN_POINT('Ctrl Pts',(-5.16952888873589,5.98832102956926,52.0830175728484));
#74183=CARTESIAN_POINT('Ctrl Pts',(-5.17696795872535,5.98189104199851,52.0834147640627));
#74184=CARTESIAN_POINT('Ctrl Pts',(-5.1941418395479,5.96699070419095,52.0843341586887));
#74185=CARTESIAN_POINT('Ctrl Pts',(-5.20386794289899,5.9585103796674,52.0848566582438));
#74186=CARTESIAN_POINT('Ctrl Pts',(-5.23131622395633,5.93445937605739,52.0863364559179));
#74187=CARTESIAN_POINT('Ctrl Pts',(-5.24898944035061,5.91883327701004,52.0872955026801));
#74188=CARTESIAN_POINT('Ctrl Pts',(-5.37073344717693,5.81021696158868,52.0939445722017));
#74189=CARTESIAN_POINT('Ctrl Pts',(-5.47239577361877,5.71456752214339,52.0997124422293));
#74190=CARTESIAN_POINT('Ctrl Pts',(-5.67040371384077,5.51813934773089,52.1113335357878));
#74191=CARTESIAN_POINT('Ctrl Pts',(-5.766723458435,5.41740159149943,52.1171846086875));
#74192=CARTESIAN_POINT('Ctrl Pts',(-6.08380218366205,5.06773548654104,52.1370607437187));
#74193=CARTESIAN_POINT('Ctrl Pts',(-6.29150919565183,4.80744309745239,52.1511313475512));
#74194=CARTESIAN_POINT('Ctrl Pts',(-6.63068332247564,4.32262001343453,52.1758280047974));
#74195=CARTESIAN_POINT('Ctrl Pts',(-6.76864502488835,4.10322503159877,52.1865158486716));
#74196=CARTESIAN_POINT('Ctrl Pts',(-6.92710459605693,3.82142315226304,52.199665809545));
#74197=CARTESIAN_POINT('Ctrl Pts',(-6.95792682315671,3.76501094481418,52.2022708713922));
#74198=CARTESIAN_POINT('Ctrl Pts',(-7.0016838603282,3.68255198023705,52.2060405512808));
#74199=CARTESIAN_POINT('Ctrl Pts',(-7.01516785184059,3.65679996533675,52.2072124863238));
#74200=CARTESIAN_POINT('Ctrl Pts',(-7.03856955574081,3.61150107456979,52.2092648044099));
#74201=CARTESIAN_POINT('Ctrl Pts',(-7.04854852220166,3.59198623835311,52.2101459842405));
#74202=CARTESIAN_POINT('Ctrl Pts',(-7.06779505723496,3.55395872541412,52.2118574351296));
#74203=CARTESIAN_POINT('Ctrl Pts',(-7.07707130966179,3.53545064653251,52.2126878123881));
#74204=CARTESIAN_POINT('Ctrl Pts',(-7.09914875751444,3.49096641865701,52.2146775283098));
#74205=CARTESIAN_POINT('Ctrl Pts',(-7.11188019544711,3.46495594652046,52.2158359743576));
#74206=CARTESIAN_POINT('Ctrl Pts',(-7.15817453133749,3.36904596555332,52.2200898348522));
#74207=CARTESIAN_POINT('Ctrl Pts',(-7.19085222120405,3.29872366486285,52.22317426749));
#74208=CARTESIAN_POINT('Ctrl Pts',(-7.49456182337317,2.61917405639613,52.2526779178102));
#74209=CARTESIAN_POINT('Ctrl Pts',(-7.68859618809676,1.97841047593569,52.2784066827412));
#74210=CARTESIAN_POINT('Ctrl Pts',(-7.87401781437724,0.883504242566689,
52.3202553184965));
#74211=CARTESIAN_POINT('Ctrl Pts',(-7.91116630099991,0.440647754662544,
52.3366328182147));
#74212=CARTESIAN_POINT('Ctrl Pts',(-7.91091146870865,-0.23686117930278,
52.3623571067234));
#74213=CARTESIAN_POINT('Ctrl Pts',(-7.90045139121858,-0.470619476705709,
52.3713670367977));
#74214=CARTESIAN_POINT('Ctrl Pts',(-7.8776860694444,-0.725583981570365,
52.3815784090536));
#74215=CARTESIAN_POINT('Ctrl Pts',(-7.87562726922063,-0.747599511082148,
52.3824633127918));
#74216=CARTESIAN_POINT('Ctrl Pts',(-7.87252027729739,-0.77938568083008,
52.3837458252475));
#74217=CARTESIAN_POINT('Ctrl Pts',(-7.87154612836062,-0.789163547105341,
52.384141011737));
#74218=CARTESIAN_POINT('Ctrl Pts',(-7.86980411313111,-0.806324575807061,
52.3848358032406));
#74219=CARTESIAN_POINT('Ctrl Pts',(-7.86904406699321,-0.813708530067096,
52.3851351458108));
#74220=CARTESIAN_POINT('Ctrl Pts',(-7.86746018889364,-0.828886360994354,
52.3857512697866));
#74221=CARTESIAN_POINT('Ctrl Pts',(-7.86663516551494,-0.836680103412573,
52.3860680915631));
#74222=CARTESIAN_POINT('Ctrl Pts',(-7.86451180998406,-0.856457994449369,
52.3868732314877));
#74223=CARTESIAN_POINT('Ctrl Pts',(-7.8631976683079,-0.868440402595209,
52.387362099298));
#74224=CARTESIAN_POINT('Ctrl Pts',(-7.85786194598504,-0.916086633540163,
52.3893104171707));
#74225=CARTESIAN_POINT('Ctrl Pts',(-7.85362511412198,-0.951725588506763,
52.3907775698038));
#74226=CARTESIAN_POINT('Ctrl Pts',(-7.82649880871162,-1.16737531669752,
52.3997202152366));
#74227=CARTESIAN_POINT('Ctrl Pts',(-7.79766789284609,-1.34655515894044,
52.4074569373015));
#74228=CARTESIAN_POINT('Ctrl Pts',(-7.72560153095527,-1.71349609976965,
52.4238472140258));
#74229=CARTESIAN_POINT('Ctrl Pts',(-7.6816154359338,-1.90099105954356,52.4325038168356));
#74230=CARTESIAN_POINT('Ctrl Pts',(-7.41176413279109,-2.88781397967049,
52.4790053354975));
#74231=CARTESIAN_POINT('Ctrl Pts',(-7.06783154185858,-3.6496557410758,52.5175496634499));
#74232=CARTESIAN_POINT('Ctrl Pts',(-6.58447494170611,-4.38532224694807,
52.5535924613072));
#74233=CARTESIAN_POINT('Ctrl Pts',(-6.55696170838169,-4.42635456513446,
52.5556010966783));
#74234=CARTESIAN_POINT('Ctrl Pts',(-6.52070022393679,-4.47935364318578,
52.5581936020238));
#74235=CARTESIAN_POINT('Ctrl Pts',(-6.51230048757717,-4.49155683852869,
52.5587904003297));
#74236=CARTESIAN_POINT('Ctrl Pts',(-6.49884532553628,-4.5109875000027,52.5597404566713));
#74237=CARTESIAN_POINT('Ctrl Pts',(-6.49381202563496,-4.51823020294322,
52.560094541546));
#74238=CARTESIAN_POINT('Ctrl Pts',(-6.48473633164779,-4.53124324509377,
52.5607306519239));
#74239=CARTESIAN_POINT('Ctrl Pts',(-6.4806983255131,-4.53701662452449,52.5610128416981));
#74240=CARTESIAN_POINT('Ctrl Pts',(-6.47122711641679,-4.55051973689208,
52.5616727809475));
#74241=CARTESIAN_POINT('Ctrl Pts',(-6.4657877624151,-4.55824515359724,52.5620502981512));
#74242=CARTESIAN_POINT('Ctrl Pts',(-6.45013284031551,-4.58039515407062,
52.5631325690474));
#74243=CARTESIAN_POINT('Ctrl Pts',(-6.43988272253188,-4.5947953110369,52.5638360148271));
#74244=CARTESIAN_POINT('Ctrl Pts',(-6.37251544534793,-4.68876980845282,
52.568425720765));
#74245=CARTESIAN_POINT('Ctrl Pts',(-6.31397174789172,-4.76731339799664,
52.5722572288625));
#74246=CARTESIAN_POINT('Ctrl Pts',(-6.13862285440356,-4.99366743489113,
52.5832975892021));
#74247=CARTESIAN_POINT('Ctrl Pts',(-6.01797705504314,-5.13842022819045,
52.5903542799024));
#74248=CARTESIAN_POINT('Ctrl Pts',(-5.64039622850543,-5.55988673723276,
52.6110335599202));
#74249=CARTESIAN_POINT('Ctrl Pts',(-5.36871111293165,-5.82266008754804,
52.62408737501));
#74250=CARTESIAN_POINT('Ctrl Pts',(-4.95849819857212,-6.16620163956753,
52.6423474357867));
#74251=CARTESIAN_POINT('Ctrl Pts',(-4.83470608817608,-6.26373403130721,
52.6476950362528));
#74252=CARTESIAN_POINT('Ctrl Pts',(-4.56188362020029,-6.46577418440707,
52.659280614942));
#74253=CARTESIAN_POINT('Ctrl Pts',(-4.41199414302791,-6.56896668581607,
52.6655247754718));
#74254=CARTESIAN_POINT('Ctrl Pts',(-4.02998926679729,-6.81298390877248,
52.6814314309922));
#74255=CARTESIAN_POINT('Ctrl Pts',(-3.79394396793837,-6.94719601549526,
52.6912535999034));
#74256=CARTESIAN_POINT('Ctrl Pts',(-3.4881974379824,-7.10080393371973,52.7044984634341));
#74257=CARTESIAN_POINT('Ctrl Pts',(-3.42448376551835,-7.13174931277163,
52.7072861532002));
#74258=CARTESIAN_POINT('Ctrl Pts',(-3.35016631470537,-7.16661939651233,
52.7105785158961));
#74259=CARTESIAN_POINT('Ctrl Pts',(-3.33995752211889,-7.17138282750633,
52.7110316623185));
#74260=CARTESIAN_POINT('Ctrl Pts',(-3.32477862669815,-7.17842587075175,
52.7117067774549));
#74261=CARTESIAN_POINT('Ctrl Pts',(-3.31981624155733,-7.18072217958851,
52.7119277055095));
#74262=CARTESIAN_POINT('Ctrl Pts',(-3.31098584997606,-7.18479727110418,
52.7123212276778));
#74263=CARTESIAN_POINT('Ctrl Pts',(-3.30711877625735,-7.18657808175755,
52.712493694284));
#74264=CARTESIAN_POINT('Ctrl Pts',(-3.29898886080286,-7.1903140050098,52.7128565597254));
#74265=CARTESIAN_POINT('Ctrl Pts',(-3.29472571587908,-7.19226844961192,
52.713047000671));
#74266=CARTESIAN_POINT('Ctrl Pts',(-3.28352164091144,-7.19739292100713,
52.7135479356325));
#74267=CARTESIAN_POINT('Ctrl Pts',(-3.27657787293121,-7.2005566915006,52.713858827612));
#74268=CARTESIAN_POINT('Ctrl Pts',(-3.24461790400414,-7.21506272428303,
52.7152918116333));
#74269=CARTESIAN_POINT('Ctrl Pts',(-3.21954769029911,-7.22628452805707,
52.7164216659886));
#74270=CARTESIAN_POINT('Ctrl Pts',(-3.02378328216905,-7.31269067630088,
52.725285934628));
#74271=CARTESIAN_POINT('Ctrl Pts',(-2.85054695268026,-7.38194304846303,
52.7333749929432));
#74272=CARTESIAN_POINT('Ctrl Pts',(-2.36545055719456,-7.55624131054427,
52.7563385332667));
#74273=CARTESIAN_POINT('Ctrl Pts',(-2.04923653957772,-7.64805556867829,
52.771642403684));
#74274=CARTESIAN_POINT('Ctrl Pts',(-1.36278552365656,-7.80172969940686,
52.8043398104943));
#74275=CARTESIAN_POINT('Ctrl Pts',(-0.991962282340157,-7.85749414093702,
52.8216771680337));
#74276=CARTESIAN_POINT('Ctrl Pts',(-0.468143799253162,-7.89857762168305,
52.8450295200146));
#74277=CARTESIAN_POINT('Ctrl Pts',(-0.31740998614995,-7.90606989758888,
52.8516233408258));
#74278=CARTESIAN_POINT('Ctrl Pts',(0.0268727533817371,-7.91331960478729,
52.8663684716413));
#74279=CARTESIAN_POINT('Ctrl Pts',(0.220386218160189,-7.91029624748218,
52.8744283055903));
#74280=CARTESIAN_POINT('Ctrl Pts',(0.433243265201537,-7.8991523591783,52.8830446860985));
#74281=CARTESIAN_POINT('Ctrl Pts',(0.452877772139501,-7.89805099069826,
52.8838371716002));
#74282=CARTESIAN_POINT('Ctrl Pts',(0.482098716436841,-7.89630256116391,
52.8850131705834));
#74283=CARTESIAN_POINT('Ctrl Pts',(0.4916883333252,-7.89571123418149,52.8853985580329));
#74284=CARTESIAN_POINT('Ctrl Pts',(0.508135971705641,-7.89466693858191,
52.8860586211209));
#74285=CARTESIAN_POINT('Ctrl Pts',(0.514994512904093,-7.89422250059581,
52.8863335836545));
#74286=CARTESIAN_POINT('Ctrl Pts',(0.529086589694206,-7.89329088160859,
52.8868979716242));
#74287=CARTESIAN_POINT('Ctrl Pts',(0.536320053833781,-7.89280269367809,
52.8871873628878));
#74288=CARTESIAN_POINT('Ctrl Pts',(0.55304987647261,-7.89165048994534,52.8878559655194));
#74289=CARTESIAN_POINT('Ctrl Pts',(0.562545737255798,-7.8909792748233,52.888234934029));
#74290=CARTESIAN_POINT('Ctrl Pts',(0.592382539874137,-7.88881612820768,
52.8894240263736));
#74291=CARTESIAN_POINT('Ctrl Pts',(0.612719016317665,-7.88726266798573,
52.8902320764152));
#74292=CARTESIAN_POINT('Ctrl Pts',(0.902523276459386,-7.86399751489727,
52.9017130711315));
#74293=CARTESIAN_POINT('Ctrl Pts',(1.17072228710984,-7.82856510553256,52.9119080676503));
#74294=CARTESIAN_POINT('Ctrl Pts',(2.00336928413153,-7.67480390174596,52.9426431463326));
#74295=CARTESIAN_POINT('Ctrl Pts',(2.55702002818255,-7.5085116783787,52.9616069419611));
#74296=CARTESIAN_POINT('Ctrl Pts',(3.28984198859882,-7.19785283838048,52.9887598505677));
#74297=CARTESIAN_POINT('Ctrl Pts',(3.48836297319371,-7.10376396476712,52.9963625440606));
#74298=CARTESIAN_POINT('Ctrl Pts',(3.87259114025051,-6.90166583501651,53.0120368329946));
#74299=CARTESIAN_POINT('Ctrl Pts',(4.05832268135722,-6.79411192860422,53.0200880103857));
#74300=CARTESIAN_POINT('Ctrl Pts',(4.25134774694219,-6.67159368385239,53.0292244624158));
#74301=CARTESIAN_POINT('Ctrl Pts',(4.26323600133538,-6.66400320674952,53.0297903718197));
#74302=CARTESIAN_POINT('Ctrl Pts',(4.27960201795007,-6.65349202660539,53.0305739522016));
#74303=CARTESIAN_POINT('Ctrl Pts',(4.28409728606114,-6.65059847109302,53.0307896505857));
#74304=CARTESIAN_POINT('Ctrl Pts',(4.29181292319384,-6.64562093005595,53.0311606897115));
#74305=CARTESIAN_POINT('Ctrl Pts',(4.29503470564462,-6.64353916153848,53.0313158672887));
#74306=CARTESIAN_POINT('Ctrl Pts',(4.30133694051786,-6.63946044503348,53.0316198919052));
#74307=CARTESIAN_POINT('Ctrl Pts',(4.30441751994875,-6.63746369412842,53.031768724593));
#74308=CARTESIAN_POINT('Ctrl Pts',(4.3118422803706,-6.63264381609797,53.0321279747621));
#74309=CARTESIAN_POINT('Ctrl Pts',(4.31618507609126,-6.62981856695199,53.0323385458193));
#74310=CARTESIAN_POINT('Ctrl Pts',(4.3294165753983,-6.62119217204906,53.032981450937));
#74311=CARTESIAN_POINT('Ctrl Pts',(4.33829634827271,-6.61537742346586,53.0334147609935));
#74312=CARTESIAN_POINT('Ctrl Pts',(4.42642604196963,-6.55741363455715,53.0377334562708));
#74313=CARTESIAN_POINT('Ctrl Pts',(4.5047404593236,-6.50386293122169,53.0417175750196));
#74314=CARTESIAN_POINT('Ctrl Pts',(4.81583027305088,-6.2828281836619,53.0580755027561));
#74315=CARTESIAN_POINT('Ctrl Pts',(5.04037109864804,-6.10416137153501,53.0711003003043));
#74316=CARTESIAN_POINT('Ctrl Pts',(5.5935089917586,-5.61266446858285,53.1054158318387));
#74317=CARTESIAN_POINT('Ctrl Pts',(5.90583663661192,-5.28303544791031,53.1270094049721));
#74318=CARTESIAN_POINT('Ctrl Pts',(6.50065739684575,-4.536176241064,53.1709298409977));
#74319=CARTESIAN_POINT('Ctrl Pts',(6.7751177631064,-4.11501484594846,53.1929613732933));
#74320=CARTESIAN_POINT('Ctrl Pts',(7.02354706551575,-3.64072084298831,53.2147570260163));
#74321=CARTESIAN_POINT('Ctrl Pts',(7.03902599642178,-3.61070279839799,53.2161248337041));
#74322=CARTESIAN_POINT('Ctrl Pts',(7.05991704401952,-3.56954418270733,53.2179846026381));
#74323=CARTESIAN_POINT('Ctrl Pts',(7.065495816075,-3.55848889497136,53.21848260408));
#74324=CARTESIAN_POINT('Ctrl Pts',(7.074294757208,-3.54095002687094,53.2192702480707));
#74325=CARTESIAN_POINT('Ctrl Pts',(7.07753201228149,-3.53447506995757,53.2195605073411));
#74326=CARTESIAN_POINT('Ctrl Pts',(7.08378380862506,-3.52192758519965,53.2201219801343));
#74327=CARTESIAN_POINT('Ctrl Pts',(7.08679943981633,-3.51585560893245,53.2203932327728));
#74328=CARTESIAN_POINT('Ctrl Pts',(7.09394826687652,-3.50141487202013,53.2210372640555));
#74329=CARTESIAN_POINT('Ctrl Pts',(7.09807446902357,-3.49304264962655,53.2214097912304));
#74330=CARTESIAN_POINT('Ctrl Pts',(7.11024032837579,-3.46824708371784,53.2225105558616));
#74331=CARTESIAN_POINT('Ctrl Pts',(7.11823789734397,-3.45180309457151,53.2232372860618));
#74332=CARTESIAN_POINT('Ctrl Pts',(7.18105185857193,-3.32150315085255,53.2289701404294));
#74333=CARTESIAN_POINT('Ctrl Pts',(7.23319150776043,-3.20637356214731,53.2338804779716));
#74334=CARTESIAN_POINT('Ctrl Pts',(7.4032846635376,-2.80550108251657,53.2504927780781));
#74335=CARTESIAN_POINT('Ctrl Pts',(7.50724198535421,-2.51411933936105,53.2617219774346));
#74336=CARTESIAN_POINT('Ctrl Pts',(7.73444228659566,-1.73602638424405,53.290359130794));
#74337=CARTESIAN_POINT('Ctrl Pts',(7.82890567151147,-1.24241400299766,53.307155340267));
#74338=CARTESIAN_POINT('Ctrl Pts',(7.90439811097626,-0.442385861624446,
53.3357622020656));
#74339=CARTESIAN_POINT('Ctrl Pts',(7.91552699806406,-0.140195352286917,
53.3469291407129));
#74340=CARTESIAN_POINT('Ctrl Pts',(7.90884165514487,0.186400276337128,53.3599349172691));
#74341=CARTESIAN_POINT('Ctrl Pts',(7.90822638316683,0.210895337762267,53.360915255557));
#74342=CARTESIAN_POINT('Ctrl Pts',(7.90723402563431,0.244232208488808,53.3622558209888));
#74343=CARTESIAN_POINT('Ctrl Pts',(7.90695588356011,0.253076989101888,53.362612103147));
#74344=CARTESIAN_POINT('Ctrl Pts',(7.90645848343005,0.268092093812745,53.3632179539776));
#74345=CARTESIAN_POINT('Ctrl Pts',(7.90624684071046,0.274262674194214,53.3634672252617));
#74346=CARTESIAN_POINT('Ctrl Pts',(7.90582462582754,0.28616584821239,53.363948631165));
#74347=CARTESIAN_POINT('Ctrl Pts',(7.90561504169541,0.291898474336013,53.3641807276375));
#74348=CARTESIAN_POINT('Ctrl Pts',(7.90510470738206,0.305453508636284,53.3647301119666));
#74349=CARTESIAN_POINT('Ctrl Pts',(7.90479858158932,0.31327570054708,53.3650476034728));
#74350=CARTESIAN_POINT('Ctrl Pts',(7.90388051109705,0.335875916121029,53.3659662193524));
#74351=CARTESIAN_POINT('Ctrl Pts',(7.90323873353962,0.350652651154008,53.3665684526872));
#74352=CARTESIAN_POINT('Ctrl Pts',(7.89837205026681,0.455897169903193,53.3708689095517));
#74353=CARTESIAN_POINT('Ctrl Pts',(7.89263540737975,0.546286428797381,53.3746210676822));
#74354=CARTESIAN_POINT('Ctrl Pts',(7.86874012205068,0.842290098590217,53.387067609252));
#74355=CARTESIAN_POINT('Ctrl Pts',(7.84408702860321,1.04729037750051,53.3959383040296));
#74356=CARTESIAN_POINT('Ctrl Pts',(7.68816280133822,2.02084073528794,53.4387633127628));
#74357=CARTESIAN_POINT('Ctrl Pts',(7.45174956790776,2.76826869911474,53.4732321240039));
#74358=CARTESIAN_POINT('Ctrl Pts',(7.0604543846322,3.57023633092141,53.5099428916943));
#74359=CARTESIAN_POINT('Ctrl Pts',(7.00891488283892,3.6703836996937,53.5145331133996));
#74360=CARTESIAN_POINT('Ctrl Pts',(6.94248359634932,3.79296201625059,53.5201658556018));
#74361=CARTESIAN_POINT('Ctrl Pts',(6.92959341567103,3.81646098459874,53.5212463728707));
#74362=CARTESIAN_POINT('Ctrl Pts',(6.90820670300883,3.85498366065826,53.5230188048607));
#74363=CARTESIAN_POINT('Ctrl Pts',(6.89978000408404,3.87004583608858,53.5237120956994));
#74364=CARTESIAN_POINT('Ctrl Pts',(6.88452553876776,3.89710400460602,53.5249580416985));
#74365=CARTESIAN_POINT('Ctrl Pts',(6.87771554690085,3.9091099209415,53.5255110542392));
#74366=CARTESIAN_POINT('Ctrl Pts',(6.86447685888192,3.93230785170827,53.5265799306335));
#74367=CARTESIAN_POINT('Ctrl Pts',(6.85805212684565,3.94350207472681,53.5270958740905));
#74368=CARTESIAN_POINT('Ctrl Pts',(6.84002525119071,3.97473416544961,53.5285357976572));
#74369=CARTESIAN_POINT('Ctrl Pts',(6.82836246409961,3.99473693610125,53.5294585025199));
#74370=CARTESIAN_POINT('Ctrl Pts',(6.77999160323523,4.07686669739666,53.5332491282327));
#74371=CARTESIAN_POINT('Ctrl Pts',(6.74252183670718,4.13854173603428,53.5361005447936));
#74372=CARTESIAN_POINT('Ctrl Pts',(6.48716751893124,4.54617831469246,53.5549831374363));
#74373=CARTESIAN_POINT('Ctrl Pts',(6.2435849213134,4.87532101312232,53.5703565273262));
#74374=CARTESIAN_POINT('Ctrl Pts',(5.71549509033129,5.4840337500939,53.5999705865717));
#74375=CARTESIAN_POINT('Ctrl Pts',(5.43315798971549,5.76387834828152,53.6141963051885));
#74376=CARTESIAN_POINT('Ctrl Pts',(5.04834805423871,6.0917895137516,53.6329044335495));
#74377=CARTESIAN_POINT('Ctrl Pts',(4.96423891889432,6.16052341475607,53.6369588185984));
#74378=CARTESIAN_POINT('Ctrl Pts',(4.84667365193465,6.25262625973452,53.6426134061685));
#74379=CARTESIAN_POINT('Ctrl Pts',(4.81441109404637,6.27750160460581,53.6441639137852));
#74380=CARTESIAN_POINT('Ctrl Pts',(4.77433324925581,6.30791206637467,53.6460902148908));
#74381=CARTESIAN_POINT('Ctrl Pts',(4.76669790809298,6.31368384259794,53.6464572088161));
#74382=CARTESIAN_POINT('Ctrl Pts',(4.66704474683016,6.3887307547958,53.651247410089));
#74383=CARTESIAN_POINT('Ctrl Pts',(4.5735378470788,6.45600009582695,53.6557459518752));
#74384=CARTESIAN_POINT('Ctrl Pts',(4.46702348212226,6.52915150667185,53.660911534883));
#74385=CARTESIAN_POINT('Ctrl Pts',(4.45542700751392,6.53707031964908,53.661474465096));
#74386=CARTESIAN_POINT('Ctrl Pts',(4.43790791797735,6.54896520048776,53.6623258052633));
#74387=CARTESIAN_POINT('Ctrl Pts',(4.43200086830766,6.55296422914947,53.6626130133131));
#74388=CARTESIAN_POINT('Ctrl Pts',(4.42174728560898,6.55988562208506,53.6631118377694));
#74389=CARTESIAN_POINT('Ctrl Pts',(4.41740323870284,6.56281167329298,53.6633232581933));
#74390=CARTESIAN_POINT('Ctrl Pts',(4.40836473620833,6.56888676314192,53.6637633421691));
#74391=CARTESIAN_POINT('Ctrl Pts',(4.40366980646183,6.57203508738537,53.6639920437876));
#74392=CARTESIAN_POINT('Ctrl Pts',(4.39261549567194,6.57943071919132,53.6645307850083));
#74393=CARTESIAN_POINT('Ctrl Pts',(4.38625333027424,6.58367383787253,53.6648410514329));
#74394=CARTESIAN_POINT('Ctrl Pts',(4.36625231930556,6.59697125072774,53.665817111259));
#74395=CARTESIAN_POINT('Ctrl Pts',(4.35259157888546,6.60599239628847,53.6664847275573));
#74396=CARTESIAN_POINT('Ctrl Pts',(4.32067900468416,6.62692454611349,53.6680468090579));
#74397=CARTESIAN_POINT('Ctrl Pts',(4.30240576751939,6.63880264900475,53.668943153341));
#74398=CARTESIAN_POINT('Ctrl Pts',(4.23950584557569,6.67932054444794,53.6720356870173));
#74399=CARTESIAN_POINT('Ctrl Pts',(4.19464137364148,6.70758647186985,53.6742534785974));
#74400=CARTESIAN_POINT('Ctrl Pts',(4.03520075710186,6.80581352501613,53.6821687202132));
#74401=CARTESIAN_POINT('Ctrl Pts',(3.91913514584814,6.8733048582457,53.6879911051885));
#74402=CARTESIAN_POINT('Ctrl Pts',(3.46989365111189,7.11945649961404,53.7106099671231));
#74403=CARTESIAN_POINT('Ctrl Pts',(3.12579149397269,7.27710318875198,53.7280863387573));
#74404=CARTESIAN_POINT('Ctrl Pts',(2.1275130586585,7.65053823675228,53.7772049572006));
#74405=CARTESIAN_POINT('Ctrl Pts',(1.45449039770815,7.80652220677552,53.8082509850101));
#74406=CARTESIAN_POINT('Ctrl Pts',(0.724926364022209,7.87784407095908,53.8382418648805));
#74407=CARTESIAN_POINT('Ctrl Pts',(0.68010908490133,7.88183970631151,53.8400712356032));
#74408=CARTESIAN_POINT('Ctrl Pts',(0.620698786063482,7.88662585728166,53.8424793844219));
#74409=CARTESIAN_POINT('Ctrl Pts',(0.60613461920027,7.88775856768057,53.8430683891811));
#74410=CARTESIAN_POINT('Ctrl Pts',(0.583500680351651,7.88945583631006,53.8439816816215));
#74411=CARTESIAN_POINT('Ctrl Pts',(0.575433073546684,7.89004836584681,53.8443068056817));
#74412=CARTESIAN_POINT('Ctrl Pts',(0.559266933697071,7.89121076941868,53.8449574850958));
#74413=CARTESIAN_POINT('Ctrl Pts',(0.551168403710126,7.89178055331999,53.8452830373867));
#74414=CARTESIAN_POINT('Ctrl Pts',(0.533068559891482,7.89302599721397,53.846009720431));
#74415=CARTESIAN_POINT('Ctrl Pts',(0.523066802445153,7.89369511720152,53.8464106550906));
#74416=CARTESIAN_POINT('Ctrl Pts',(0.49375888117962,7.89559987717363,53.8475836937924));
#74417=CARTESIAN_POINT('Ctrl Pts',(0.474449365073108,7.89678371615031,53.8483542480299));
#74418=CARTESIAN_POINT('Ctrl Pts',(0.33140770431331,7.90502684172079,53.854045542609));
#74419=CARTESIAN_POINT('Ctrl Pts',(0.207526386493655,7.90924869165333,53.8588808247702));
#74420=CARTESIAN_POINT('Ctrl Pts',(-0.198806816706126,7.91354255136767,
53.8744659897639));
#74421=CARTESIAN_POINT('Ctrl Pts',(-0.481174984656377,7.90140272751994,
53.8848540347579));
#74422=CARTESIAN_POINT('Ctrl Pts',(-1.0031671302955,7.85086849885042,53.903606225286));
#74423=CARTESIAN_POINT('Ctrl Pts',(-1.24283899647044,7.81651047139906,53.9120394342415));
#74424=CARTESIAN_POINT('Ctrl Pts',(-1.68824732699333,7.73165186501636,53.9277301144796));
#74425=CARTESIAN_POINT('Ctrl Pts',(-1.89426142536727,7.68377462359536,53.93499628928));
#74426=CARTESIAN_POINT('Ctrl Pts',(-2.51966507277599,7.5117483989968,53.9575561170548));
#74427=CARTESIAN_POINT('Ctrl Pts',(-2.9308788117101,7.36104718615563,53.9731012009326));
#74428=CARTESIAN_POINT('Ctrl Pts',(-3.36013568333052,7.16203192480498,53.9917897435393));
#74429=CARTESIAN_POINT('Ctrl Pts',(-3.39264328892988,7.14669046204214,53.9932198138907));
#74430=CARTESIAN_POINT('Ctrl Pts',(-3.43565905053655,7.12603020895244,53.9951308167761));
#74431=CARTESIAN_POINT('Ctrl Pts',(-3.44626182499317,7.12090858543764,53.9956033652411));
#74432=CARTESIAN_POINT('Ctrl Pts',(-3.46273726587431,7.11290478091368,53.9963399639399));
#74433=CARTESIAN_POINT('Ctrl Pts',(-3.4686178839139,7.11003894292507,53.9966033397048));
#74434=CARTESIAN_POINT('Ctrl Pts',(-3.48040969550706,7.10427425547591,53.9971323746931));
#74435=CARTESIAN_POINT('Ctrl Pts',(-3.48632083828782,7.10137531452811,53.9973980375087));
#74436=CARTESIAN_POINT('Ctrl Pts',(-3.49954463668613,7.09486961258578,53.9979933747893));
#74437=CARTESIAN_POINT('Ctrl Pts',(-3.50685534406378,7.09125892059902,53.998323205855));
#74438=CARTESIAN_POINT('Ctrl Pts',(-3.52833437565151,7.0806092832481,53.9992942973704));
#74439=CARTESIAN_POINT('Ctrl Pts',(-3.54248714022144,7.07353915275968,53.9999367739565));
#74440=CARTESIAN_POINT('Ctrl Pts',(-3.64910413194198,7.01987752311238,54.0047960190748));
#74441=CARTESIAN_POINT('Ctrl Pts',(-3.7406649877458,6.97151819039129,54.009078498709));
#74442=CARTESIAN_POINT('Ctrl Pts',(-3.96642623023701,6.84655067030594,54.0198723669699));
#74443=CARTESIAN_POINT('Ctrl Pts',(-4.09938078832613,6.76778163993273,54.0264403679699));
#74444=CARTESIAN_POINT('Ctrl Pts',(-4.46888130553644,6.53398583364339,54.0451730440766));
#74445=CARTESIAN_POINT('Ctrl Pts',(-4.69954407027545,6.37009860807926,54.0574360640011));
#74446=CARTESIAN_POINT('Ctrl Pts',(-5.21290431051258,5.96226432200247,54.0856922095261));
#74447=CARTESIAN_POINT('Ctrl Pts',(-5.48811496946418,5.70995437245114,54.1015764354976));
#74448=CARTESIAN_POINT('Ctrl Pts',(-6.01396375523818,5.15458564779419,54.1335084954059));
#74449=CARTESIAN_POINT('Ctrl Pts',(-6.26190347264958,4.8503699500397,54.1495159072819));
#74450=CARTESIAN_POINT('Ctrl Pts',(-6.53224800613117,4.46319444551995,54.1686794611109));
#74451=CARTESIAN_POINT('Ctrl Pts',(-6.57721326679625,4.39666173741613,54.1719296470516));
#74452=CARTESIAN_POINT('Ctrl Pts',(-6.63885337734816,4.30239378809915,54.1764750473568));
#74453=CARTESIAN_POINT('Ctrl Pts',(-6.65638265827357,4.27522354841571,54.1777783156152));
#74454=CARTESIAN_POINT('Ctrl Pts',(-6.68810605806227,4.22538443785885,54.1801565568393));
#74455=CARTESIAN_POINT('Ctrl Pts',(-6.70235272579781,4.20274960419499,54.1812320372807));
#74456=CARTESIAN_POINT('Ctrl Pts',(-6.72939248492138,4.15930217489664,54.1832876475169));
#74457=CARTESIAN_POINT('Ctrl Pts',(-6.74220448772337,4.13850171533463,54.1842679599424));
#74458=CARTESIAN_POINT('Ctrl Pts',(-6.76881186979394,4.0948527708737,54.1863171976192));
#74459=CARTESIAN_POINT('Ctrl Pts',(-6.78258838935449,4.07199313476207,54.1873859165957));
#74460=CARTESIAN_POINT('Ctrl Pts',(-6.82920101787034,3.99375504928013,54.1910284636642));
#74461=CARTESIAN_POINT('Ctrl Pts',(-6.86147678863256,3.93804549094485,54.1935963043661));
#74462=CARTESIAN_POINT('Ctrl Pts',(-7.04277400090847,3.61612097466104,54.2082913735722));
#74463=CARTESIAN_POINT('Ctrl Pts',(-7.17697852327385,3.34185310626648,54.2202433760427));
#74464=CARTESIAN_POINT('Ctrl Pts',(-7.38100014548717,2.85554958851309,54.2407348643938));
#74465=CARTESIAN_POINT('Ctrl Pts',(-7.45831444676199,2.64704982734854,54.2493135582315));
#74466=CARTESIAN_POINT('Ctrl Pts',(-7.59110386877714,2.23668517189618,54.2659907290016));
#74467=CARTESIAN_POINT('Ctrl Pts',(-7.64755222543076,2.03532839821273,54.2740812776687));
#74468=CARTESIAN_POINT('Ctrl Pts',(-7.73100335081559,1.68475791503657,54.2881900296456));
#74469=CARTESIAN_POINT('Ctrl Pts',(-7.76181550329163,1.53656777831262,54.2941613465935));
#74470=CARTESIAN_POINT('Ctrl Pts',(-7.79254206089766,1.36410346536889,54.301172482047));
#74471=CARTESIAN_POINT('Ctrl Pts',(-7.79661987037615,1.34060009833285,54.3021292828589));
#74472=CARTESIAN_POINT('Ctrl Pts',(-7.80297700014814,1.30294906815448,54.3036644465768));
#74473=CARTESIAN_POINT('Ctrl Pts',(-7.80532430100294,1.28881297840809,54.3042413703818));
#74474=CARTESIAN_POINT('Ctrl Pts',(-7.8094172057597,1.26374305178853,54.3052655684844));
#74475=CARTESIAN_POINT('Ctrl Pts',(-7.8111782892817,1.25281176826412,54.3057125018919));
#74476=CARTESIAN_POINT('Ctrl Pts',(-7.8145141071538,1.23182541496056,54.3065712535174));
#74477=CARTESIAN_POINT('Ctrl Pts',(-7.8160923982823,1.22177092968828,54.3069829905181));
#74478=CARTESIAN_POINT('Ctrl Pts',(-7.81942895124563,1.20024438175734,54.3078652153464));
#74479=CARTESIAN_POINT('Ctrl Pts',(-7.82118137950966,1.18877143634277,54.3083358383264));
#74480=CARTESIAN_POINT('Ctrl Pts',(-7.82535396814674,1.16104534543449,54.3094742465409));
#74481=CARTESIAN_POINT('Ctrl Pts',(-7.82774874154296,1.14478847701366,54.3101426239251));
#74482=CARTESIAN_POINT('Ctrl Pts',(-7.83962387873191,1.06239465916568,54.3135343609423));
#74483=CARTESIAN_POINT('Ctrl Pts',(-7.84831668596023,0.996147572399339,
54.316275216298));
#74484=CARTESIAN_POINT('Ctrl Pts',(-7.89254157309554,0.622477371073265,
54.3317951551681));
#74485=CARTESIAN_POINT('Ctrl Pts',(-7.91084855024879,0.313295554748577,
54.3448544452596));
#74486=CARTESIAN_POINT('Ctrl Pts',(-7.9109990642057,0.0038478742852386,
54.3579070163678));
#74487=CARTESIAN_POINT('',(-7.90853756536093,-0.0002840522667073,56.3576029905152));
#74488=CARTESIAN_POINT('Ctrl Pts',(-7.91058521897938,0.00383761197256053,
54.357668491763));
#74489=CARTESIAN_POINT('Ctrl Pts',(-7.90804771810951,-0.914391017526965,
54.3946791517166));
#74490=CARTESIAN_POINT('Ctrl Pts',(-7.51315483011075,-3.14994018213361,
54.4846110786474));
#74491=CARTESIAN_POINT('Ctrl Pts',(-4.71476302132917,-7.33335162650933,
54.6803855395325));
#74492=CARTESIAN_POINT('Ctrl Pts',(2.51764341483423,-9.0087265231168,54.9449918744182));
#74493=CARTESIAN_POINT('Ctrl Pts',(8.94941253689187,-2.74473022419253,55.2625194762814));
#74494=CARTESIAN_POINT('Ctrl Pts',(7.44143434588096,4.5419721744467,55.5271258111673));
#74495=CARTESIAN_POINT('Ctrl Pts',(3.00563183108329,7.65784328303428,55.7388108790757));
#74496=CARTESIAN_POINT('Ctrl Pts',(-2.39221485231201,8.3907978832337,55.9504959469847));
#74497=CARTESIAN_POINT('Ctrl Pts',(-7.0727487270325,5.01925377135236,56.1567599841309));
#74498=CARTESIAN_POINT('Ctrl Pts',(-7.91074264020192,1.18409319209995,56.3101027543002));
#74499=CARTESIAN_POINT('Ctrl Pts',(-7.90853756536093,-0.0002840522667073,
56.3576029905152));
#74500=CARTESIAN_POINT('',(-7.911,4.61852778244065E-13,58.357668491763));
#74501=CARTESIAN_POINT('Ctrl Pts',(-7.91099999456027,-0.000285742256253543,
56.3576799889967));
#74502=CARTESIAN_POINT('Ctrl Pts',(-7.91091617089283,-2.20186489793695,
56.4462635923182));
#74503=CARTESIAN_POINT('Ctrl Pts',(-6.94207516543246,-4.38616811721652,
56.5348471956396));
#74504=CARTESIAN_POINT('Ctrl Pts',(-3.67820201488314,-7.34180684107615,
56.7120182346939));
#74505=CARTESIAN_POINT('Ctrl Pts',(-1.40868175871789,-8.08992666571325,
56.8006056704266));
#74506=CARTESIAN_POINT('Ctrl Pts',(2.97309270521207,-7.6545422802528,56.9777805418921));
#74507=CARTESIAN_POINT('Ctrl Pts',(5.05102072675534,-6.47444880834275,57.0663679776248));
#74508=CARTESIAN_POINT('Ctrl Pts',(7.6695151884783,-2.93425195367807,57.2435428490902));
#74509=CARTESIAN_POINT('Ctrl Pts',(8.18956872247059,-0.601881960100388,
57.3321302848229));
#74510=CARTESIAN_POINT('Ctrl Pts',(7.32306689761406,3.71537198232318,57.5093051562884));
#74511=CARTESIAN_POINT('Ctrl Pts',(5.9432995885031,5.66643518936392,57.5978925920211));
#74512=CARTESIAN_POINT('Ctrl Pts',(2.16154501638024,7.92205913232946,57.7750674634865));
#74513=CARTESIAN_POINT('Ctrl Pts',(-0.210816529298383,8.20894963713004,
57.8636548992193));
#74514=CARTESIAN_POINT('Ctrl Pts',(-4.42123908576248,6.91982244717948,58.0408297706847));
#74515=CARTESIAN_POINT('Ctrl Pts',(-6.22631625634031,5.35390358803698,58.1294172064174));
#74516=CARTESIAN_POINT('Ctrl Pts',(-7.65317280859446,2.31334857514692,58.2645592586878));
#74517=CARTESIAN_POINT('Ctrl Pts',(-7.91099999999993,1.1570283783663,58.3111138752254));
#74518=CARTESIAN_POINT('Ctrl Pts',(-7.911,4.61852778244065E-13,58.357668491763));
#74519=CARTESIAN_POINT('',(-3.42067962509687,7.13322310757536,60.));
#74520=CARTESIAN_POINT('Ctrl Pts',(-7.911,4.61852778244065E-13,58.357668491763));
#74521=CARTESIAN_POINT('Ctrl Pts',(-7.91100000000013,-2.20167589666633,
58.4462559274957));
#74522=CARTESIAN_POINT('Ctrl Pts',(-6.94214576672394,-4.38610418338648,
58.5348433632284));
#74523=CARTESIAN_POINT('Ctrl Pts',(-3.67820201488319,-7.34180684107617,
58.7120182346939));
#74524=CARTESIAN_POINT('Ctrl Pts',(-1.40868175871776,-8.08992666571332,
58.8006056704266));
#74525=CARTESIAN_POINT('Ctrl Pts',(2.97309270521249,-7.65454228025267,58.9777805418921));
#74526=CARTESIAN_POINT('Ctrl Pts',(5.05102072675585,-6.4744488083424,59.0663679776248));
#74527=CARTESIAN_POINT('Ctrl Pts',(7.66951518847866,-2.93425195367724,59.2435428490902));
#74528=CARTESIAN_POINT('Ctrl Pts',(8.18956872247071,-0.601881960099315,
59.332130284823));
#74529=CARTESIAN_POINT('Ctrl Pts',(7.32306689761348,3.71537198232442,59.5093051562884));
#74530=CARTESIAN_POINT('Ctrl Pts',(5.94329958850206,5.66643518936507,59.5978925920212));
#74531=CARTESIAN_POINT('Ctrl Pts',(2.16154501637848,7.92205913232998,59.7750674634866));
#74532=CARTESIAN_POINT('Ctrl Pts',(-0.210816529300396,8.20894963713003,
59.8636548992193));
#74533=CARTESIAN_POINT('Ctrl Pts',(-2.69433568776147,7.44855753134885,59.9681615566347));
#74534=CARTESIAN_POINT('Ctrl Pts',(-3.06393494046689,7.30429714460912,59.9840807783173));
#74535=CARTESIAN_POINT('Ctrl Pts',(-3.42067962509687,7.13322310757536,60.));
#74536=CARTESIAN_POINT('',(3.4206796250979,7.13322310757487,60.));
#74537=CARTESIAN_POINT('Origin',(0.,0.,60.));
#74538=CARTESIAN_POINT('',(-7.91099785401453,-0.00429578758769514,58.6423315082368));
#74539=CARTESIAN_POINT('Ctrl Pts',(3.42067962509791,7.13322310757487,60.));
#74540=CARTESIAN_POINT('Ctrl Pts',(3.6144969028105,7.04027959482263,59.9913511809908));
#74541=CARTESIAN_POINT('Ctrl Pts',(3.80447822695433,6.93945490373599,59.9827023619817));
#74542=CARTESIAN_POINT('Ctrl Pts',(3.99001435172825,6.83108384321277,59.9740535429726));
#74543=CARTESIAN_POINT('Ctrl Pts',(4.17560503493687,6.72268091528133,59.9654021807066));
#74544=CARTESIAN_POINT('Ctrl Pts',(4.35674770625185,6.60672730486513,59.9567508184406));
#74545=CARTESIAN_POINT('Ctrl Pts',(4.53285999276488,6.48360249290405,59.9480994561746));
#74546=CARTESIAN_POINT('Ctrl Pts',(4.71414100545881,6.35686408616373,59.939194184749));
#74547=CARTESIAN_POINT('Ctrl Pts',(4.89009165777409,6.22252729526204,59.9302889133236));
#74548=CARTESIAN_POINT('Ctrl Pts',(5.06011034746729,6.08105289168368,59.9213836418981));
#74549=CARTESIAN_POINT('Ctrl Pts',(5.22528660057382,5.94360793233408,59.9127320085417));
#74550=CARTESIAN_POINT('Ctrl Pts',(5.38486395990082,5.79942650828154,59.9040803751852));
#74551=CARTESIAN_POINT('Ctrl Pts',(5.53832440683672,5.64897192103454,59.8954287418289));
#74552=CARTESIAN_POINT('Ctrl Pts',(5.69853330400857,5.49190106676187,59.8863966513688));
#74553=CARTESIAN_POINT('Ctrl Pts',(5.85207498129762,5.32799306622592,59.8773645609088));
#74554=CARTESIAN_POINT('Ctrl Pts',(5.99840172750653,5.15781908517996,59.8683324704487));
#74555=CARTESIAN_POINT('Ctrl Pts',(6.14472847371554,4.98764510413389,59.8593003799887));
#74556=CARTESIAN_POINT('Ctrl Pts',(6.28384008499756,4.81120535093508,59.8502682895286));
#74557=CARTESIAN_POINT('Ctrl Pts',(6.41523454138166,4.62911295812315,59.8412361990686));
#74558=CARTESIAN_POINT('Ctrl Pts',(6.52959511341658,4.47062689426438,59.8333750224245));
#74559=CARTESIAN_POINT('Ctrl Pts',(6.63814345897899,4.30781131701357,59.8255138457805));
#74560=CARTESIAN_POINT('Ctrl Pts',(6.74054212213741,4.14113666759397,59.8176526691365));
#74561=CARTESIAN_POINT('Ctrl Pts',(6.84290875318325,3.97451415695206,59.8097939516075));
#74562=CARTESIAN_POINT('Ctrl Pts',(6.93912935186777,3.80403527535238,59.8019352340786));
#74563=CARTESIAN_POINT('Ctrl Pts',(7.02890993359229,3.63019918812283,59.7940765165496));
#74564=CARTESIAN_POINT('Ctrl Pts',(7.11867789852752,3.45638752993173,59.7862189033995));
#74565=CARTESIAN_POINT('Ctrl Pts',(7.20200749057793,3.2792199158393,59.7783612902495));
#74566=CARTESIAN_POINT('Ctrl Pts',(7.27865072156316,3.09922001050071,59.7705036770995));
#74567=CARTESIAN_POINT('Ctrl Pts',(7.35531794692297,2.9191637533474,59.7626436039995));
#74568=CARTESIAN_POINT('Ctrl Pts',(7.42529448864377,2.73627375252924,59.7547835308995));
#74569=CARTESIAN_POINT('Ctrl Pts',(7.4883802965523,2.55109418371947,59.7469234577995));
#74570=CARTESIAN_POINT('Ctrl Pts',(7.55147576688006,2.36588625222899,59.7390621808261));
#74571=CARTESIAN_POINT('Ctrl Pts',(7.60767829403273,2.17838838584624,59.7312009038528));
#74572=CARTESIAN_POINT('Ctrl Pts',(7.65683766736361,1.98916010809633,59.7233396268795));
#74573=CARTESIAN_POINT('Ctrl Pts',(7.70603329081186,1.79979229343183,59.7154725530012));
#74574=CARTESIAN_POINT('Ctrl Pts',(7.74817530282766,1.60869185706849,59.707605479123));
#74575=CARTESIAN_POINT('Ctrl Pts',(7.78316440777624,1.41642959638844,59.6997384052448));
#74576=CARTESIAN_POINT('Ctrl Pts',(7.80876147830464,1.27577579418892,59.6939830695421));
#74577=CARTESIAN_POINT('Ctrl Pts',(7.83053139013534,1.13450041533383,59.6882277338395));
#74578=CARTESIAN_POINT('Ctrl Pts',(7.84845284800453,0.992828732788119,59.6824723981369));
#74579=CARTESIAN_POINT('Ctrl Pts',(7.87625500018793,0.77304875132874,59.6735439549132));
#74580=CARTESIAN_POINT('Ctrl Pts',(7.89481335201341,0.552161752406579,59.6646155116895));
#74581=CARTESIAN_POINT('Ctrl Pts',(7.90407626183148,0.330907006804204,59.6556870684658));
#74582=CARTESIAN_POINT('Ctrl Pts',(7.913341078962,0.109606702955013,59.6467567867991));
#74583=CARTESIAN_POINT('Ctrl Pts',(7.91330662441942,-0.112061320222985,
59.6378265051325));
#74584=CARTESIAN_POINT('Ctrl Pts',(7.90397335127518,-0.333356059389596,
59.6288962234659));
#74585=CARTESIAN_POINT('Ctrl Pts',(7.89464653280444,-0.554497756288547,
59.6199721177733));
#74586=CARTESIAN_POINT('Ctrl Pts',(7.8760337594932,-0.775266507043604,59.6110480120807));
#74587=CARTESIAN_POINT('Ctrl Pts',(7.84818748145735,-0.994924246310342,
59.6021239063881));
#74588=CARTESIAN_POINT('Ctrl Pts',(7.82036631196139,-1.2143839237354,59.5932078474177));
#74589=CARTESIAN_POINT('Ctrl Pts',(7.78332829005007,-1.43273441374617,59.5842917884473));
#74590=CARTESIAN_POINT('Ctrl Pts',(7.73717753193906,-1.64924371736181,59.5753757294769));
#74591=CARTESIAN_POINT('Ctrl Pts',(7.69113148038629,-1.86526180599125,59.5664798992066));
#74592=CARTESIAN_POINT('Ctrl Pts',(7.63601401610708,-2.07944687526408,59.5575840689364));
#74593=CARTESIAN_POINT('Ctrl Pts',(7.57197991055836,-2.29107861805322,59.5486882386661));
#74594=CARTESIAN_POINT('Ctrl Pts',(7.51204362770563,-2.48916711929377,59.5403616915126));
#74595=CARTESIAN_POINT('Ctrl Pts',(7.44429588276699,-2.68501857300424,59.532035144359));
#74596=CARTESIAN_POINT('Ctrl Pts',(7.36890430184754,-2.87804975464511,59.5237085972055));
#74597=CARTESIAN_POINT('Ctrl Pts',(7.29691304211312,-3.06237481806564,59.5157575950974));
#74598=CARTESIAN_POINT('Ctrl Pts',(7.21798301215634,-3.24404497807909,59.5078065929893));
#74599=CARTESIAN_POINT('Ctrl Pts',(7.13234293140335,-3.42251447168024,59.4998555908812));
#74600=CARTESIAN_POINT('Ctrl Pts',(7.04671046143499,-3.60096810480033,59.4919052953741));
#74601=CARTESIAN_POINT('Ctrl Pts',(6.95436927559734,-3.77622133369333,59.483954999867));
#74602=CARTESIAN_POINT('Ctrl Pts',(6.85559526707494,-3.94775056634277,59.4760047043599));
#74603=CARTESIAN_POINT('Ctrl Pts',(6.75681432711654,-4.11929183600394,59.4680538509432));
#74604=CARTESIAN_POINT('Ctrl Pts',(6.65159983424772,-4.28710829600644,59.4601029975266));
#74605=CARTESIAN_POINT('Ctrl Pts',(6.54027262080183,-4.45070275862026,59.4521521441099));
#74606=CARTESIAN_POINT('Ctrl Pts',(6.42888006511491,-4.6143932411422,59.4441966240303));
#74607=CARTESIAN_POINT('Ctrl Pts',(6.31136781008364,-4.77385649474633,59.4362411039507));
#74608=CARTESIAN_POINT('Ctrl Pts',(6.1880994011085,-4.92862524462965,59.4282855838711));
#74609=CARTESIAN_POINT('Ctrl Pts',(6.06479256849094,-5.08344223703635,59.4203275839991));
#74610=CARTESIAN_POINT('Ctrl Pts',(5.93572622138635,-5.23356154866874,59.4123695841271));
#74611=CARTESIAN_POINT('Ctrl Pts',(5.80130319447833,-5.37855019923916,59.4044115842551));
#74612=CARTESIAN_POINT('Ctrl Pts',(5.66675620563104,-5.52367255513306,59.3964462456919));
#74613=CARTESIAN_POINT('Ctrl Pts',(5.52684290303172,-5.66365455413246,59.3884809071287));
#74614=CARTESIAN_POINT('Ctrl Pts',(5.38200266167046,-5.79810040873493,59.3805155685654));
#74615=CARTESIAN_POINT('Ctrl Pts',(5.28762398171985,-5.88570605039196,59.3753253111349));
#74616=CARTESIAN_POINT('Ctrl Pts',(5.19115408975717,-5.9709618953036,59.3701350537044));
#74617=CARTESIAN_POINT('Ctrl Pts',(5.092721828791,-6.05376786592909,59.3649447962739));
#74618=CARTESIAN_POINT('Ctrl Pts',(4.94082909758122,-6.18154736540747,59.3569356093563));
#74619=CARTESIAN_POINT('Ctrl Pts',(4.7839914327906,-6.30371885951764,59.3489264224387));
#74620=CARTESIAN_POINT('Ctrl Pts',(4.62265619092145,-6.41988868599259,59.3409172355211));
#74621=CARTESIAN_POINT('Ctrl Pts',(4.4614459590171,-6.53596849874362,59.3329142544899));
#74622=CARTESIAN_POINT('Ctrl Pts',(4.29574536459703,-6.64605571840741,59.3249112734586));
#74623=CARTESIAN_POINT('Ctrl Pts',(4.12603491430888,-6.74979680330483,59.3169082924273));
#74624=CARTESIAN_POINT('Ctrl Pts',(3.95642764726029,-6.85347481405922,59.3089101771749));
#74625=CARTESIAN_POINT('Ctrl Pts',(3.78281566708038,-6.95081420759235,59.3009120619224));
#74626=CARTESIAN_POINT('Ctrl Pts',(3.60570889961232,-7.04150440823951,59.29291394667));
#74627=CARTESIAN_POINT('Ctrl Pts',(3.42868027581228,-7.13215459423883,59.2849193603739));
#74628=CARTESIAN_POINT('Ctrl Pts',(3.24816023449609,-7.21616128422545,59.2769247740778));
#74629=CARTESIAN_POINT('Ctrl Pts',(3.06468414449047,-7.29325936015639,59.2689301877818));
#74630=CARTESIAN_POINT('Ctrl Pts',(2.88125842054413,-7.37033627187861,59.2609377960813));
#74631=CARTESIAN_POINT('Ctrl Pts',(2.69487857250448,-7.44050822182869,59.2529454043807));
#74632=CARTESIAN_POINT('Ctrl Pts',(2.50610122433952,-7.50355766642491,59.2449530126802));
#74633=CARTESIAN_POINT('Ctrl Pts',(2.31169608808739,-7.56848672696366,59.2367223535857));
#74634=CARTESIAN_POINT('Ctrl Pts',(2.11474863075838,-7.62586189743682,59.2284916944911));
#74635=CARTESIAN_POINT('Ctrl Pts',(1.91588563862165,-7.67550019345471,59.2202610353966));
#74636=CARTESIAN_POINT('Ctrl Pts',(1.72274030109593,-7.72371130269914,59.2122670219715));
#74637=CARTESIAN_POINT('Ctrl Pts',(1.52778839519012,-7.76462421241166,59.2042730085466));
#74638=CARTESIAN_POINT('Ctrl Pts',(1.33161656030211,-7.79812274437439,59.1962789951216));
#74639=CARTESIAN_POINT('Ctrl Pts',(1.13539687205975,-7.83162944783188,59.1882830316696));
#74640=CARTESIAN_POINT('Ctrl Pts',(0.937956989962921,-7.85771811123421,
59.1802870682177));
#74641=CARTESIAN_POINT('Ctrl Pts',(0.739891227397327,-7.87632414084264,
59.1722911047658));
#74642=CARTESIAN_POINT('Ctrl Pts',(0.541747183716112,-7.89493752407309,
59.164291981086));
#74643=CARTESIAN_POINT('Ctrl Pts',(0.342977097954888,-7.90606234616173,
59.1562928574063));
#74644=CARTESIAN_POINT('Ctrl Pts',(0.144178255435468,-7.90968606397622,
59.1482937337265));
#74645=CARTESIAN_POINT('Ctrl Pts',(-0.0647419135745792,-7.91349427396705,
59.1398873554502));
#74646=CARTESIAN_POINT('Ctrl Pts',(-0.273693419980003,-7.90901767035084,
59.1314809771739));
#74647=CARTESIAN_POINT('Ctrl Pts',(-0.481986362343147,-7.89630357487066,
59.1230745988976));
#74648=CARTESIAN_POINT('Ctrl Pts',(-0.680540574478752,-7.88418392654056,
59.1150612605836));
#74649=CARTESIAN_POINT('Ctrl Pts',(-0.878496077585479,-7.86457956597611,
59.1070479222697));
#74650=CARTESIAN_POINT('Ctrl Pts',(-1.07526337780495,-7.83758442814822,
59.0990345839557));
#74651=CARTESIAN_POINT('Ctrl Pts',(-1.27217167258296,-7.81056994682405,
59.0910155036455));
#74652=CARTESIAN_POINT('Ctrl Pts',(-1.46788973933417,-7.77615418291552,
59.0829964233353));
#74653=CARTESIAN_POINT('Ctrl Pts',(-1.66183968641545,-7.73448187383322,
59.0749773430251));
#74654=CARTESIAN_POINT('Ctrl Pts',(-1.85603937954027,-7.69275590402826,
59.0669479366818));
#74655=CARTESIAN_POINT('Ctrl Pts',(-2.04846608396256,-7.6437548073047,59.0589185303385));
#74656=CARTESIAN_POINT('Ctrl Pts',(-2.23855734038304,-7.58767303155699,
59.0508891239951));
#74657=CARTESIAN_POINT('Ctrl Pts',(-2.26595593951001,-7.57958974502938,
59.0497318141337));
#74658=CARTESIAN_POINT('Ctrl Pts',(-2.29330605522693,-7.5713594416439,59.0485745042723));
#74659=CARTESIAN_POINT('Ctrl Pts',(-2.32060603944214,-7.56298278523128,
59.0474171944108));
#74660=CARTESIAN_POINT('Ctrl Pts',(-2.50330547103492,-7.50692376508056,
59.0396721403407));
#74661=CARTESIAN_POINT('Ctrl Pts',(-2.68430227468656,-7.44413919422109,
59.0319270862705));
#74662=CARTESIAN_POINT('Ctrl Pts',(-2.86304941426585,-7.37474535502562,
59.0241820322003));
#74663=CARTESIAN_POINT('Ctrl Pts',(-3.04157977881897,-7.30543567298837,
59.0164463709199));
#74664=CARTESIAN_POINT('Ctrl Pts',(-3.2178655779645,-7.22953280398241,59.0087107096395));
#74665=CARTESIAN_POINT('Ctrl Pts',(-3.39137161991687,-7.14720361649382,
59.0009750483591));
#74666=CARTESIAN_POINT('Ctrl Pts',(-3.56470271607927,-7.06495744135791,
58.9932471869302));
#74667=CARTESIAN_POINT('Ctrl Pts',(-3.7352593116472,-6.97629799864975,58.9855193255014));
#74668=CARTESIAN_POINT('Ctrl Pts',(-3.90252292868786,-6.88144140359166,
58.9777914640725));
#74669=CARTESIAN_POINT('Ctrl Pts',(-4.06965203187759,-6.78666109246258,
58.9700698174106));
#74670=CARTESIAN_POINT('Ctrl Pts',(-4.23349311703626,-6.68569372735895,
58.9623481707487));
#74671=CARTESIAN_POINT('Ctrl Pts',(-4.39354913597794,-6.57880285384412,
58.9546265240868));
#74672=CARTESIAN_POINT('Ctrl Pts',(-4.55350906375469,-6.47197615328962,
58.9469095131895));
#74673=CARTESIAN_POINT('Ctrl Pts',(-4.70968815124361,-6.35923322465589,
58.9391925022922));
#74674=CARTESIAN_POINT('Ctrl Pts',(-4.86161529483965,-6.24088276808507,
58.9314754913948));
#74675=CARTESIAN_POINT('Ctrl Pts',(-5.01348217065545,-6.12257925980236,
58.9237615417485));
#74676=CARTESIAN_POINT('Ctrl Pts',(-5.16110017782105,-5.99867287476642,
58.9160475921022));
#74677=CARTESIAN_POINT('Ctrl Pts',(-5.30402842574628,-5.86951475497553,
58.9083336424558));
#74678=CARTESIAN_POINT('Ctrl Pts',(-5.44695652514239,-5.74035676940402,
58.9006197008257));
#74679=CARTESIAN_POINT('Ctrl Pts',(-5.58519459979148,-5.60594729289418,
58.8929057591956));
#74680=CARTESIAN_POINT('Ctrl Pts',(-5.71833572041561,-5.46667701520941,
58.8851918175655));
#74681=CARTESIAN_POINT('Ctrl Pts',(-5.85148343683082,-5.32739983809605,
58.8774774937879));
#74682=CARTESIAN_POINT('Ctrl Pts',(-5.97953344640783,-5.18326164036616,
58.8697631700103));
#74683=CARTESIAN_POINT('Ctrl Pts',(-6.10211664965986,-5.03468900667598,
58.8620488462326));
#74684=CARTESIAN_POINT('Ctrl Pts',(-6.22472853604888,-4.8860816086046,58.8543327173871));
#74685=CARTESIAN_POINT('Ctrl Pts',(-6.34187083937764,-4.7330379865422,58.8466165885416));
#74686=CARTESIAN_POINT('Ctrl Pts',(-6.45321560781147,-4.5760167524932,58.8389004596961));
#74687=CARTESIAN_POINT('Ctrl Pts',(-6.5646069752631,-4.41892980332006,58.8311811015652));
#74688=CARTESIAN_POINT('Ctrl Pts',(-6.67019576834552,-4.25786222139797,
58.8234617434344));
#74689=CARTESIAN_POINT('Ctrl Pts',(-6.76969809502244,-4.09330046566943,
58.8157423853036));
#74690=CARTESIAN_POINT('Ctrl Pts',(-6.86931999294081,-3.92854095724419,
58.8080137508747));
#74691=CARTESIAN_POINT('Ctrl Pts',(-6.96284063123002,-3.76027919802655,
58.8002851164459));
#74692=CARTESIAN_POINT('Ctrl Pts',(-7.05002224248504,-3.58902596542101,
58.792556482017));
#74693=CARTESIAN_POINT('Ctrl Pts',(-7.13726074137302,-3.41766098687617,
58.7848228045096));
#74694=CARTESIAN_POINT('Ctrl Pts',(-7.21815182366781,-3.24330097270297,
58.7770891270021));
#74695=CARTESIAN_POINT('Ctrl Pts',(-7.2925064651054,-3.0664752495978,58.7693554494947));
#74696=CARTESIAN_POINT('Ctrl Pts',(-7.36697586468091,-2.88937661561139,
58.7616098359142));
#74697=CARTESIAN_POINT('Ctrl Pts',(-7.4348885487445,-2.70980500805425,58.7538642223338));
#74698=CARTESIAN_POINT('Ctrl Pts',(-7.49610545161038,-2.52830458179729,
58.7461186087533));
#74699=CARTESIAN_POINT('Ctrl Pts',(-7.53886040783258,-2.40154150794612,
58.7407089366849));
#74700=CARTESIAN_POINT('Ctrl Pts',(-7.57835031313341,-2.27383784497801,
58.7352992646165));
#74701=CARTESIAN_POINT('Ctrl Pts',(-7.61454271413694,-2.14538114436201,
58.7298895925481));
#74702=CARTESIAN_POINT('Ctrl Pts',(-7.68830077885446,-1.88359365928993,
58.7188649870658));
#74703=CARTESIAN_POINT('Ctrl Pts',(-7.74855677595777,-1.61799285473667,
58.7078403815835));
#74704=CARTESIAN_POINT('Ctrl Pts',(-7.79500466405839,-1.34974934239952,
58.6968157761012));
#74705=CARTESIAN_POINT('Ctrl Pts',(-7.83997609327777,-1.09003260129617,
58.6861416144677));
#74706=CARTESIAN_POINT('Ctrl Pts',(-7.87200351402683,-0.827837999041716,
58.6754674528343));
#74707=CARTESIAN_POINT('Ctrl Pts',(-7.89085187608698,-0.564249651886951,
58.6647932912008));
#74708=CARTESIAN_POINT('Ctrl Pts',(-7.90407283064875,-0.379358808341846,
58.6573060302128));
#74709=CARTESIAN_POINT('Ctrl Pts',(-7.91081033794178,-0.193782654100511,
58.6498187692248));
#74710=CARTESIAN_POINT('Ctrl Pts',(-7.91099605152649,-0.00790396939679502,
58.6423315082368));
#74711=CARTESIAN_POINT('',(-7.90222269547159,0.00311450190333342,56.6423315082368));
#74712=CARTESIAN_POINT('Ctrl Pts',(-7.911,5.93636251267071E-12,58.6423315082368));
#74713=CARTESIAN_POINT('Ctrl Pts',(-7.91099999999835,2.20167589667258,58.5537440725041));
#74714=CARTESIAN_POINT('Ctrl Pts',(-6.94214576672053,4.3861041833918,58.4651566367714));
#74715=CARTESIAN_POINT('Ctrl Pts',(-3.67820201487778,7.34180684107883,58.2879817653059));
#74716=CARTESIAN_POINT('Ctrl Pts',(-1.40868175871199,8.08992666571428,58.1993943295732));
#74717=CARTESIAN_POINT('Ctrl Pts',(2.97309270521766,7.65454228025062,58.0222194581077));
#74718=CARTESIAN_POINT('Ctrl Pts',(5.05102072676007,6.47444880833906,57.933632022375));
#74719=CARTESIAN_POINT('Ctrl Pts',(7.66951518848044,2.93425195367247,57.7564571509096));
#74720=CARTESIAN_POINT('Ctrl Pts',(8.18956872247103,0.601881960094407,57.6678697151769));
#74721=CARTESIAN_POINT('Ctrl Pts',(7.32306689761135,-3.71537198232853,57.4906948437114));
#74722=CARTESIAN_POINT('Ctrl Pts',(5.94329958849896,-5.66643518936826,57.4021074079787));
#74723=CARTESIAN_POINT('Ctrl Pts',(2.16154501637446,-7.92205913233104,57.2249325365133));
#74724=CARTESIAN_POINT('Ctrl Pts',(-0.210816529304378,-8.20894963712989,
57.1363451007805));
#74725=CARTESIAN_POINT('Ctrl Pts',(-4.42123908576754,-6.91982244717625,
56.9591702293151));
#74726=CARTESIAN_POINT('Ctrl Pts',(-6.22631625634422,-5.35390358803243,
56.8705827935824));
#74727=CARTESIAN_POINT('Ctrl Pts',(-7.65317280859621,-2.31334857514119,
56.735440741312));
#74728=CARTESIAN_POINT('Ctrl Pts',(-7.91100000000084,-1.15702837836022,
56.6888861247744));
#74729=CARTESIAN_POINT('Ctrl Pts',(-7.911,5.76594327839075E-12,56.6423315082368));
#74730=CARTESIAN_POINT('',(-7.92132537539791,0.00356088473096691,54.6423315082368));
#74731=CARTESIAN_POINT('Ctrl Pts',(-7.89838609934108,0.00447586357080088,
56.6423315082368));
#74732=CARTESIAN_POINT('Ctrl Pts',(-7.90209458248899,1.1298110327076,56.5972864653267));
#74733=CARTESIAN_POINT('Ctrl Pts',(-7.15272636683917,4.89292271398436,56.4463988884626));
#74734=CARTESIAN_POINT('Ctrl Pts',(-2.58089786760515,8.32742667055543,56.2425900446207));
#74735=CARTESIAN_POINT('Ctrl Pts',(2.82873975620344,7.73373310986697,56.0309049767122));
#74736=CARTESIAN_POINT('Ctrl Pts',(6.19471352977467,5.45236858721805,55.8721411757803));
#74737=CARTESIAN_POINT('Ctrl Pts',(8.02841028037048,1.83220300240068,55.7133773748492));
#74738=CARTESIAN_POINT('Ctrl Pts',(7.93460731480094,-3.62384378458733,55.5016923069402));
#74739=CARTESIAN_POINT('Ctrl Pts',(3.7954711336447,-7.85637192923924,55.2900072390316));
#74740=CARTESIAN_POINT('Ctrl Pts',(-1.64811177619533,-8.05978374552938,
55.0783221711231));
#74741=CARTESIAN_POINT('Ctrl Pts',(-6.24123930469383,-5.89715594175713,
54.8800706831835));
#74742=CARTESIAN_POINT('Ctrl Pts',(-7.90119404608586,-2.2838008882752,54.7347404622217));
#74743=CARTESIAN_POINT('Ctrl Pts',(-7.92132537539791,0.00356088473096691,
54.6423315082368));
#74744=CARTESIAN_POINT('',(-7.90965467482103,-0.00646043864732659,52.6423315082368));
#74745=CARTESIAN_POINT('Ctrl Pts',(-7.92132537539791,0.00356088473096691,
54.6423315082368));
#74746=CARTESIAN_POINT('Ctrl Pts',(-7.92425188641814,0.336076901541994,
54.6288979282673));
#74747=CARTESIAN_POINT('Ctrl Pts',(-7.75596513217767,3.2865552664362,54.5096218143437));
#74748=CARTESIAN_POINT('Ctrl Pts',(-4.02499199464678,8.44364384466607,54.2845031664651));
#74749=CARTESIAN_POINT('Ctrl Pts',(3.38756990960737,8.03314424947189,54.0198968315797));
#74750=CARTESIAN_POINT('Ctrl Pts',(7.14415802802205,4.09553804706829,53.8082117636707));
#74751=CARTESIAN_POINT('Ctrl Pts',(8.25041905810794,0.182663886590385,53.6494479627395));
#74752=CARTESIAN_POINT('Ctrl Pts',(7.32226987266179,-3.76785230220073,53.4906841618077));
#74753=CARTESIAN_POINT('Ctrl Pts',(3.73724118410271,-7.8818311594681,53.2789990938992));
#74754=CARTESIAN_POINT('Ctrl Pts',(-2.15499139441648,-8.45483246728375,
53.0673140259903));
#74755=CARTESIAN_POINT('Ctrl Pts',(-6.45081714418401,-5.10522729313052,
52.8556289580818));
#74756=CARTESIAN_POINT('Ctrl Pts',(-7.77803341798768,-2.21995614957399,
52.7316085411562));
#74757=CARTESIAN_POINT('Ctrl Pts',(-7.91375901553935,-0.457593973212717,
52.6605093912079));
#74758=CARTESIAN_POINT('Ctrl Pts',(-7.90965467482103,-0.00646043864732659,
52.6423315082368));
#74759=CARTESIAN_POINT('',(-7.90557077178582,0.000172428555999323,50.6423513293437));
#74760=CARTESIAN_POINT('Ctrl Pts',(-7.90965467482103,-0.00646043864732659,
52.6423315082368));
#74761=CARTESIAN_POINT('Ctrl Pts',(-7.88986108295124,2.16917596066671,52.5546668572536));
#74762=CARTESIAN_POINT('Ctrl Pts',(-5.85400455890075,6.99988501149608,52.361159672316));
#74763=CARTESIAN_POINT('Ctrl Pts',(2.35754329943507,9.05194297588424,52.0618099534242));
#74764=CARTESIAN_POINT('Ctrl Pts',(7.76450970406415,3.96477304772281,51.7972036185382));
#74765=CARTESIAN_POINT('Ctrl Pts',(8.1031421732418,-1.46680360649821,51.5855185506298));
#74766=CARTESIAN_POINT('Ctrl Pts',(6.42995471675893,-5.17285830448992,51.426754749698));
#74767=CARTESIAN_POINT('Ctrl Pts',(3.17601681014416,-7.59771441211321,51.2679909487665));
#74768=CARTESIAN_POINT('Ctrl Pts',(-2.2159366211452,-8.43681569021935,51.0563058808579));
#74769=CARTESIAN_POINT('Ctrl Pts',(-7.0206882469314,-5.13084566170502,50.847759737257));
#74770=CARTESIAN_POINT('Ctrl Pts',(-7.90577022156873,-1.24184940982428,
50.6921348606333));
#74771=CARTESIAN_POINT('Ctrl Pts',(-7.90532993643697,0.00017238839015414,
50.6423525179641));
#74772=CARTESIAN_POINT('',(-7.911,5.08315611824628E-12,48.6423315082368));
#74773=CARTESIAN_POINT('Ctrl Pts',(-7.91099999799831,0.000173334027146164,
50.6423245339043));
#74774=CARTESIAN_POINT('Ctrl Pts',(-7.91094914875265,2.20179054697439,50.5537394229491));
#74775=CARTESIAN_POINT('Ctrl Pts',(-6.94210293929909,4.3861429662668,50.4651543119939));
#74776=CARTESIAN_POINT('Ctrl Pts',(-3.67820201487841,7.34180684107852,50.2879817653059));
#74777=CARTESIAN_POINT('Ctrl Pts',(-1.40868175871268,8.08992666571416,50.1993943295732));
#74778=CARTESIAN_POINT('Ctrl Pts',(2.973092705217,7.65454228025088,50.0222194581078));
#74779=CARTESIAN_POINT('Ctrl Pts',(5.05102072675951,6.4744488083395,49.933632022375));
#74780=CARTESIAN_POINT('Ctrl Pts',(7.66951518848019,2.93425195367313,49.7564571509096));
#74781=CARTESIAN_POINT('Ctrl Pts',(8.18956872247098,0.601881960095113,49.6678697151769));
#74782=CARTESIAN_POINT('Ctrl Pts',(7.32306689761167,-3.7153719823279,49.4906948437114));
#74783=CARTESIAN_POINT('Ctrl Pts',(5.94329958849945,-5.66643518936775,49.4021074079787));
#74784=CARTESIAN_POINT('Ctrl Pts',(2.16154501637514,-7.92205913233085,49.2249325365133));
#74785=CARTESIAN_POINT('Ctrl Pts',(-0.210816529303669,-8.20894963712991,
49.1363451007806));
#74786=CARTESIAN_POINT('Ctrl Pts',(-4.42123908576694,-6.91982244717663,
48.9591702293151));
#74787=CARTESIAN_POINT('Ctrl Pts',(-6.22631625634376,-5.35390358803297,
48.8705827935824));
#74788=CARTESIAN_POINT('Ctrl Pts',(-7.65317280859601,-2.31334857514185,
48.7354407413121));
#74789=CARTESIAN_POINT('Ctrl Pts',(-7.91100000000074,-1.1570283783609,48.6888861247744));
#74790=CARTESIAN_POINT('Ctrl Pts',(-7.911,5.08315611824628E-12,48.6423315082368));
#74791=CARTESIAN_POINT('',(-7.911,4.91273688396632E-12,46.6423315082368));
#74792=CARTESIAN_POINT('Ctrl Pts',(-7.911,5.08315611824628E-12,48.6423315082368));
#74793=CARTESIAN_POINT('Ctrl Pts',(-7.91099999999859,2.20167589667188,48.5537440725041));
#74794=CARTESIAN_POINT('Ctrl Pts',(-6.94214576672087,4.38610418339135,48.4651566367714));
#74795=CARTESIAN_POINT('Ctrl Pts',(-3.67820201487804,7.34180684107875,48.2879817653059));
#74796=CARTESIAN_POINT('Ctrl Pts',(-1.40868175871209,8.08992666571431,48.1993943295732));
#74797=CARTESIAN_POINT('Ctrl Pts',(2.97309270521786,7.65454228025059,48.0222194581077));
#74798=CARTESIAN_POINT('Ctrl Pts',(5.05102072676038,6.47444880833886,47.933632022375));
#74799=CARTESIAN_POINT('Ctrl Pts',(7.66951518848072,2.93425195367186,47.7564571509096));
#74800=CARTESIAN_POINT('Ctrl Pts',(8.18956872247113,0.601881960093575,47.6678697151768));
#74801=CARTESIAN_POINT('Ctrl Pts',(7.32306689761087,-3.71537198232955,47.4906948437114));
#74802=CARTESIAN_POINT('Ctrl Pts',(5.94329958849809,-5.66643518936924,47.4021074079786));
#74803=CARTESIAN_POINT('Ctrl Pts',(2.16154501637293,-7.9220591323315,47.2249325365132));
#74804=CARTESIAN_POINT('Ctrl Pts',(-0.210816529306149,-8.20894963712988,
47.1363451007805));
#74805=CARTESIAN_POINT('Ctrl Pts',(-4.4212390857693,-6.91982244717518,46.959170229315));
#74806=CARTESIAN_POINT('Ctrl Pts',(-6.22631625634571,-5.35390358803076,
46.8705827935823));
#74807=CARTESIAN_POINT('Ctrl Pts',(-7.65317280859644,-2.31334857513992,
46.735440741312));
#74808=CARTESIAN_POINT('Ctrl Pts',(-7.91100000000072,-1.15702837836002,
46.6888861247744));
#74809=CARTESIAN_POINT('Ctrl Pts',(-7.911,4.91273688396632E-12,46.6423315082368));
#74810=CARTESIAN_POINT('',(-7.911,5.19195797465954E-12,44.6423315082368));
#74811=CARTESIAN_POINT('Ctrl Pts',(-7.911,4.91273688396632E-12,46.6423315082368));
#74812=CARTESIAN_POINT('Ctrl Pts',(-7.91099999999863,2.20167589667171,46.5537440725041));
#74813=CARTESIAN_POINT('Ctrl Pts',(-6.94214576672096,4.3861041833912,46.4651566367714));
#74814=CARTESIAN_POINT('Ctrl Pts',(-3.6782020148782,7.34180684107867,46.2879817653059));
#74815=CARTESIAN_POINT('Ctrl Pts',(-1.40868175871226,8.08992666571427,46.1993943295732));
#74816=CARTESIAN_POINT('Ctrl Pts',(2.97309270521769,7.65454228025065,46.0222194581077));
#74817=CARTESIAN_POINT('Ctrl Pts',(5.05102072676024,6.47444880833897,45.933632022375));
#74818=CARTESIAN_POINT('Ctrl Pts',(7.66951518848065,2.93425195367203,45.7564571509096));
#74819=CARTESIAN_POINT('Ctrl Pts',(8.18956872247112,0.601881960093751,45.6678697151768));
#74820=CARTESIAN_POINT('Ctrl Pts',(7.32306689761095,-3.71537198232939,45.4906948437114));
#74821=CARTESIAN_POINT('Ctrl Pts',(5.94329958849821,-5.66643518936911,45.4021074079786));
#74822=CARTESIAN_POINT('Ctrl Pts',(2.1615450163731,-7.92205913233145,45.2249325365132));
#74823=CARTESIAN_POINT('Ctrl Pts',(-0.210816529305973,-8.20894963712989,
45.1363451007805));
#74824=CARTESIAN_POINT('Ctrl Pts',(-4.42123908576915,-6.91982244717527,
44.959170229315));
#74825=CARTESIAN_POINT('Ctrl Pts',(-6.2263162563456,-5.35390358803089,44.8705827935823));
#74826=CARTESIAN_POINT('Ctrl Pts',(-7.65317280859645,-2.31334857513995,
44.735440741312));
#74827=CARTESIAN_POINT('Ctrl Pts',(-7.91100000000076,-1.15702837835989,
44.6888861247744));
#74828=CARTESIAN_POINT('Ctrl Pts',(-7.911,5.19195797465954E-12,44.6423315082368));
#74829=CARTESIAN_POINT('',(-7.90782562621644,0.00332762781947112,42.6423315082368));
#74830=CARTESIAN_POINT('Ctrl Pts',(-7.911,5.19195797465954E-12,44.6423315082368));
#74831=CARTESIAN_POINT('Ctrl Pts',(-7.91099999999856,2.20167589667199,44.5537440725041));
#74832=CARTESIAN_POINT('Ctrl Pts',(-6.94214576672081,4.38610418339144,44.4651566367714));
#74833=CARTESIAN_POINT('Ctrl Pts',(-3.67820201487794,7.3418068410788,44.2879817653059));
#74834=CARTESIAN_POINT('Ctrl Pts',(-1.40868175871198,8.08992666571432,44.1993943295732));
#74835=CARTESIAN_POINT('Ctrl Pts',(2.97309270521796,7.65454228025055,44.0222194581077));
#74836=CARTESIAN_POINT('Ctrl Pts',(5.05102072676047,6.4744488083388,43.933632022375));
#74837=CARTESIAN_POINT('Ctrl Pts',(7.66951518848076,2.93425195367176,43.7564571509095));
#74838=CARTESIAN_POINT('Ctrl Pts',(8.18956872247114,0.601881960093462,43.6678697151768));
#74839=CARTESIAN_POINT('Ctrl Pts',(7.32306689761082,-3.71537198232965,43.4906948437114));
#74840=CARTESIAN_POINT('Ctrl Pts',(5.94329958849801,-5.66643518936932,43.4021074079786));
#74841=CARTESIAN_POINT('Ctrl Pts',(2.16154501637282,-7.92205913233153,43.2249325365132));
#74842=CARTESIAN_POINT('Ctrl Pts',(-0.210816529306261,-8.20894963712988,
43.1363451007805));
#74843=CARTESIAN_POINT('Ctrl Pts',(-4.42123908576939,-6.91982244717511,
42.959170229315));
#74844=CARTESIAN_POINT('Ctrl Pts',(-6.22631625634579,-5.35390358803068,
42.8705827935823));
#74845=CARTESIAN_POINT('Ctrl Pts',(-7.65317280859647,-2.31334857513982,
42.735440741312));
#74846=CARTESIAN_POINT('Ctrl Pts',(-7.91100000000073,-1.15702837835991,
42.6888861247744));
#74847=CARTESIAN_POINT('Ctrl Pts',(-7.911,5.02153874037958E-12,42.6423315082368));
#74848=CARTESIAN_POINT('',(-7.91845049609821,0.000976995136657901,40.6423315082369));
#74849=CARTESIAN_POINT('Ctrl Pts',(-7.90709240406838,0.00409624883905946,
42.6423315082368));
#74850=CARTESIAN_POINT('Ctrl Pts',(-7.90744323469513,0.885716272102219,
42.6068816380023));
#74851=CARTESIAN_POINT('Ctrl Pts',(-7.54808527225096,3.07967697239749,42.5185105007905));
#74852=CARTESIAN_POINT('Ctrl Pts',(-5.54712628819712,6.08619232436321,42.3772180966016));
#74853=CARTESIAN_POINT('Ctrl Pts',(-0.751839041474361,8.69051046575553,
42.1655330286929));
#74854=CARTESIAN_POINT('Ctrl Pts',(4.9699436811625,7.17132064257916,41.9538479607843));
#74855=CARTESIAN_POINT('Ctrl Pts',(7.82683125453677,2.53319956939885,41.7421628928754));
#74856=CARTESIAN_POINT('Ctrl Pts',(8.23123753638788,-2.87248740689012,41.530477824967));
#74857=CARTESIAN_POINT('Ctrl Pts',(3.55408252280707,-8.65990915799413,41.265871490081));
#74858=CARTESIAN_POINT('Ctrl Pts',(-5.26027638092778,-7.67229640261403,
40.9521822955118));
#74859=CARTESIAN_POINT('Ctrl Pts',(-7.90500472213288,-2.5283709606113,40.7443356348972));
#74860=CARTESIAN_POINT('Ctrl Pts',(-7.91845049609821,0.000976995136657901,
40.6423315082369));
#74861=CARTESIAN_POINT('',(-7.90957060305277,-0.00606182810568165,38.6423315082369));
#74862=CARTESIAN_POINT('Ctrl Pts',(-7.91845049609821,0.000976995136657901,
40.6423315082369));
#74863=CARTESIAN_POINT('Ctrl Pts',(-7.91895645951902,0.0961561605313427,
40.6384931009429));
#74864=CARTESIAN_POINT('Ctrl Pts',(-7.91764356014499,0.191342240229911,
40.6346546936489));
#74865=CARTESIAN_POINT('Ctrl Pts',(-7.87092759740858,1.59814129958058,40.5778950193778));
#74866=CARTESIAN_POINT('Ctrl Pts',(-7.08189078581498,4.20229089874874,40.4720524854235));
#74867=CARTESIAN_POINT('Ctrl Pts',(-4.22061022989196,7.09148996933881,40.3132886844917));
#74868=CARTESIAN_POINT('Ctrl Pts',(-0.325041355772333,8.22840781581323,
40.1545248835606));
#74869=CARTESIAN_POINT('Ctrl Pts',(5.02077049564122,7.13316884209834,39.9428398156514));
#74870=CARTESIAN_POINT('Ctrl Pts',(8.42022621943545,2.28647553367909,39.7311547477432));
#74871=CARTESIAN_POINT('Ctrl Pts',(7.61942872714469,-3.10172426520481,39.5194696798341));
#74872=CARTESIAN_POINT('Ctrl Pts',(4.44800486268501,-7.49798026302581,39.3077846119259));
#74873=CARTESIAN_POINT('Ctrl Pts',(-2.85709022741325,-8.91417773190914,
39.0431782770396));
#74874=CARTESIAN_POINT('Ctrl Pts',(-7.51958970425579,-4.00472737273126,
38.8037201534846));
#74875=CARTESIAN_POINT('Ctrl Pts',(-7.91612429028003,-0.696134925501238,
38.6701045638835));
#74876=CARTESIAN_POINT('Ctrl Pts',(-7.90931586281257,-0.00714213791867646,
38.6423315082369));
#74877=CARTESIAN_POINT('',(-7.90205031402523,0.00258408860188915,36.6423315082368));
#74878=CARTESIAN_POINT('Ctrl Pts',(-7.911,4.22939461230953E-12,38.6423315082369));
#74879=CARTESIAN_POINT('Ctrl Pts',(-7.91099999999882,2.20167589667103,38.5537440725041));
#74880=CARTESIAN_POINT('Ctrl Pts',(-6.94214576672134,4.3861041833906,38.4651566367714));
#74881=CARTESIAN_POINT('Ctrl Pts',(-3.67820201487883,7.34180684107835,38.2879817653059));
#74882=CARTESIAN_POINT('Ctrl Pts',(-1.40868175871296,8.08992666571415,38.1993943295732));
#74883=CARTESIAN_POINT('Ctrl Pts',(2.97309270521703,7.65454228025091,38.0222194581078));
#74884=CARTESIAN_POINT('Ctrl Pts',(5.05102072675969,6.47444880833941,37.933632022375));
#74885=CARTESIAN_POINT('Ctrl Pts',(7.6695151884804,2.93425195367269,37.7564571509096));
#74886=CARTESIAN_POINT('Ctrl Pts',(8.18956872247107,0.601881960094457,37.6678697151768));
#74887=CARTESIAN_POINT('Ctrl Pts',(7.32306689761127,-3.71537198232876,37.4906948437114));
#74888=CARTESIAN_POINT('Ctrl Pts',(5.9432995884987,-5.6664351893686,37.4021074079787));
#74889=CARTESIAN_POINT('Ctrl Pts',(2.16154501637379,-7.92205913233127,37.2249325365132));
#74890=CARTESIAN_POINT('Ctrl Pts',(-0.210816529305264,-8.20894963712991,
37.1363451007805));
#74891=CARTESIAN_POINT('Ctrl Pts',(-4.42123908576855,-6.91982244717565,
36.959170229315));
#74892=CARTESIAN_POINT('Ctrl Pts',(-6.22631625634514,-5.35390358803143,
36.8705827935823));
#74893=CARTESIAN_POINT('Ctrl Pts',(-7.65317280859619,-2.31334857514075,
36.735440741312));
#74894=CARTESIAN_POINT('Ctrl Pts',(-7.91100000000059,-1.15702837836087,
36.6888861247744));
#74895=CARTESIAN_POINT('Ctrl Pts',(-7.911,4.05953048954188E-12,36.6423315082369));
#74896=CARTESIAN_POINT('',(-7.92032460290522,0.00410429619978156,34.6423315082369));
#74897=CARTESIAN_POINT('Ctrl Pts',(-7.89801789798098,0.00374838870705885,
36.6423315082368));
#74898=CARTESIAN_POINT('Ctrl Pts',(-7.90109140379909,1.16454375460544,36.5958734928697));
#74899=CARTESIAN_POINT('Ctrl Pts',(-7.11894075804998,4.96435591288772,36.4435729435483));
#74900=CARTESIAN_POINT('Ctrl Pts',(-2.46977960589945,8.36105405809064,36.2383511272497));
#74901=CARTESIAN_POINT('Ctrl Pts',(2.93147714201178,7.69537963103877,36.0266660593408));
#74902=CARTESIAN_POINT('Ctrl Pts',(6.26677020828368,5.36939213081236,35.8679022584095));
#74903=CARTESIAN_POINT('Ctrl Pts',(8.05209744036919,1.72513010441004,35.7091384574778));
#74904=CARTESIAN_POINT('Ctrl Pts',(7.88564631233398,-3.72918440633894,35.4974533895694));
#74905=CARTESIAN_POINT('Ctrl Pts',(3.69051491642543,-7.90621778123017,35.2857683216604));
#74906=CARTESIAN_POINT('Ctrl Pts',(-1.75529427873059,-8.03712196874263,
35.0740832537519));
#74907=CARTESIAN_POINT('Ctrl Pts',(-6.28668782593535,-5.8293691697886,34.8772447382695));
#74908=CARTESIAN_POINT('Ctrl Pts',(-7.89940260670074,-2.24887738882641,
34.7333274897647));
#74909=CARTESIAN_POINT('Ctrl Pts',(-7.92032460290522,0.00410429619978156,
34.6423315082369));
#74910=CARTESIAN_POINT('',(-7.910692815354,-0.00630498622597453,32.6423315082369));
#74911=CARTESIAN_POINT('Ctrl Pts',(-7.92032460290522,0.00410429619978156,
34.6423315082369));
#74912=CARTESIAN_POINT('Ctrl Pts',(-7.92373815489182,0.371692074705317,
34.6274849558103));
#74913=CARTESIAN_POINT('Ctrl Pts',(-7.73535849790647,3.35749249374558,34.5067958694296));
#74914=CARTESIAN_POINT('Ctrl Pts',(-3.91219481221388,8.49649420640381,34.2802642490941));
#74915=CARTESIAN_POINT('Ctrl Pts',(3.49424336047911,7.9873211780795,34.0156579142083));
#74916=CARTESIAN_POINT('Ctrl Pts',(7.19806303432888,4.00003930652512,33.8039728462998));
#74917=CARTESIAN_POINT('Ctrl Pts',(8.2521199516345,0.072780503715108,33.6452090453681));
#74918=CARTESIAN_POINT('Ctrl Pts',(7.27144578913484,-3.86502564053636,33.4864452444366));
#74919=CARTESIAN_POINT('Ctrl Pts',(3.63195094250934,-7.93089947300516,33.274760176528));
#74920=CARTESIAN_POINT('Ctrl Pts',(-2.26738957999657,-8.42538571491713,
33.0630751086194));
#74921=CARTESIAN_POINT('Ctrl Pts',(-6.51822921065279,-5.01887193528488,
32.8513900407104));
#74922=CARTESIAN_POINT('Ctrl Pts',(-7.79222394496349,-2.14925319637973,
32.7287825962423));
#74923=CARTESIAN_POINT('Ctrl Pts',(-7.91444208827574,-0.422243313346306,
32.6590964187509));
#74924=CARTESIAN_POINT('Ctrl Pts',(-7.910692815354,-0.00630498622597453,
32.6423315082369));
#74925=CARTESIAN_POINT('',(-7.90592497177009,4.79922218070005E-5,30.6423372190962));
#74926=CARTESIAN_POINT('Ctrl Pts',(-7.910692815354,-0.00630498622597453,
32.6423315082369));
#74927=CARTESIAN_POINT('Ctrl Pts',(-7.89077166389797,2.20371561880541,32.5532538847966));
#74928=CARTESIAN_POINT('Ctrl Pts',(-5.79915631276819,7.06805053223478,32.3583337274018));
#74929=CARTESIAN_POINT('Ctrl Pts',(2.47787498205179,9.01974598430914,32.057571036053));
#74930=CARTESIAN_POINT('Ctrl Pts',(7.81661836099797,3.86102494974632,31.7929647011671));
#74931=CARTESIAN_POINT('Ctrl Pts',(8.08289089798158,-1.57457950934242,31.5812796332585));
#74932=CARTESIAN_POINT('Ctrl Pts',(6.36049990923886,-5.25802449618405,31.4225158323268));
#74933=CARTESIAN_POINT('Ctrl Pts',(3.07455978983641,-7.63933434043985,31.2637520313955));
#74934=CARTESIAN_POINT('Ctrl Pts',(-2.32808948167419,-8.40655895507157,
31.0520669634867));
#74935=CARTESIAN_POINT('Ctrl Pts',(-7.05624836198249,-5.05965197045065,
30.8449289678837));
#74936=CARTESIAN_POINT('Ctrl Pts',(-7.90630531642784,-1.20693321518151,
30.6907122392577));
#74937=CARTESIAN_POINT('Ctrl Pts',(-7.90538714644296,4.76034783793698E-5,
30.6423380445861));
#74938=CARTESIAN_POINT('',(-7.911,3.37729844090973E-12,28.6423315082369));
#74939=CARTESIAN_POINT('Ctrl Pts',(-7.91099999982219,5.16604830449524E-5,
30.6423294296068));
#74940=CARTESIAN_POINT('Ctrl Pts',(-7.91098484438918,2.20171006714826,30.5537426867508));
#74941=CARTESIAN_POINT('Ctrl Pts',(-6.94213300243702,4.38611574223799,30.4651559438947));
#74942=CARTESIAN_POINT('Ctrl Pts',(-3.67820201487999,7.34180684107772,30.287981765306));
#74943=CARTESIAN_POINT('Ctrl Pts',(-1.40868175871443,8.08992666571386,30.1993943295733));
#74944=CARTESIAN_POINT('Ctrl Pts',(2.97309270521535,7.65454228025152,30.0222194581078));
#74945=CARTESIAN_POINT('Ctrl Pts',(5.05102072675811,6.47444880834058,29.9336320223751));
#74946=CARTESIAN_POINT('Ctrl Pts',(7.66951518847956,2.93425195367478,29.7564571509097));
#74947=CARTESIAN_POINT('Ctrl Pts',(8.18956872247085,0.601881960096879,29.6678697151769));
#74948=CARTESIAN_POINT('Ctrl Pts',(7.32306689761247,-3.71537198232632,29.4906948437115));
#74949=CARTESIAN_POINT('Ctrl Pts',(5.94329958850067,-5.66643518936647,29.4021074079788));
#74950=CARTESIAN_POINT('Ctrl Pts',(2.16154501637685,-7.92205913233039,29.2249325365134));
#74951=CARTESIAN_POINT('Ctrl Pts',(-0.2108165293019,-8.20894963712995,29.1363451007806));
#74952=CARTESIAN_POINT('Ctrl Pts',(-4.42123908576545,-6.91982244717758,
28.9591702293152));
#74953=CARTESIAN_POINT('Ctrl Pts',(-6.22631625634261,-5.35390358803431,
28.8705827935825));
#74954=CARTESIAN_POINT('Ctrl Pts',(-7.65317280859551,-2.3133485751435,28.7354407413121));
#74955=CARTESIAN_POINT('Ctrl Pts',(-7.91100000000049,-1.15702837836261,
28.6888861247745));
#74956=CARTESIAN_POINT('Ctrl Pts',(-7.911,3.37729844090973E-12,28.6423315082369));
#74957=CARTESIAN_POINT('',(-7.911,3.65596442009064E-12,26.6423315082369));
#74958=CARTESIAN_POINT('Ctrl Pts',(-7.911,3.37729844090973E-12,28.6423315082369));
#74959=CARTESIAN_POINT('Ctrl Pts',(-7.91099999999906,2.20167589667017,28.5537440725042));
#74960=CARTESIAN_POINT('Ctrl Pts',(-6.94214576672181,4.38610418338985,28.4651566367714));
#74961=CARTESIAN_POINT('Ctrl Pts',(-3.67820201487962,7.34180684107795,28.287981765306));
#74962=CARTESIAN_POINT('Ctrl Pts',(-1.40868175871383,8.089926665714,28.1993943295733));
#74963=CARTESIAN_POINT('Ctrl Pts',(2.97309270521621,7.65454228025123,28.0222194581078));
#74964=CARTESIAN_POINT('Ctrl Pts',(5.05102072675899,6.47444880833995,27.9336320223751));
#74965=CARTESIAN_POINT('Ctrl Pts',(7.66951518848008,2.93425195367352,27.7564571509096));
#74966=CARTESIAN_POINT('Ctrl Pts',(8.189568722471,0.60188196009534,27.6678697151769));
#74967=CARTESIAN_POINT('Ctrl Pts',(7.32306689761167,-3.71537198232797,27.4906948437114));
#74968=CARTESIAN_POINT('Ctrl Pts',(5.94329958849931,-5.66643518936795,27.4021074079787));
#74969=CARTESIAN_POINT('Ctrl Pts',(2.16154501637464,-7.92205913233103,27.2249325365133));
#74970=CARTESIAN_POINT('Ctrl Pts',(-0.21081652930438,-8.20894963712993,
27.1363451007805));
#74971=CARTESIAN_POINT('Ctrl Pts',(-4.4212390857678,-6.91982244717613,26.9591702293151));
#74972=CARTESIAN_POINT('Ctrl Pts',(-6.22631625634456,-5.3539035880321,26.8705827935823));
#74973=CARTESIAN_POINT('Ctrl Pts',(-7.653172808596,-2.31334857514144,26.735440741312));
#74974=CARTESIAN_POINT('Ctrl Pts',(-7.91100000000053,-1.15702837836143,
26.6888861247745));
#74975=CARTESIAN_POINT('Ctrl Pts',(-7.911,3.65596442009064E-12,26.6423315082369));
#74976=CARTESIAN_POINT('',(-7.911,3.03701508386212E-12,24.6423315082369));
#74977=CARTESIAN_POINT('Ctrl Pts',(-7.911,3.65596442009064E-12,26.6423315082369));
#74978=CARTESIAN_POINT('Ctrl Pts',(-7.91099999999898,2.2016758966703,26.5537440725042));
#74979=CARTESIAN_POINT('Ctrl Pts',(-6.9421457667218,4.3861041833898,26.4651566367714));
#74980=CARTESIAN_POINT('Ctrl Pts',(-3.67820201487989,7.34180684107777,26.287981765306));
#74981=CARTESIAN_POINT('Ctrl Pts',(-1.40868175871432,8.08992666571388,26.1993943295733));
#74982=CARTESIAN_POINT('Ctrl Pts',(2.97309270521546,7.65454228025148,26.0222194581078));
#74983=CARTESIAN_POINT('Ctrl Pts',(5.0510207267582,6.47444880834052,25.9336320223751));
#74984=CARTESIAN_POINT('Ctrl Pts',(7.6695151884796,2.93425195367468,25.7564571509097));
#74985=CARTESIAN_POINT('Ctrl Pts',(8.18956872247086,0.601881960096767,25.6678697151769));
#74986=CARTESIAN_POINT('Ctrl Pts',(7.32306689761242,-3.71537198232642,25.4906948437115));
#74987=CARTESIAN_POINT('Ctrl Pts',(5.9432995885006,-5.66643518936655,25.4021074079788));
#74988=CARTESIAN_POINT('Ctrl Pts',(2.16154501637674,-7.92205913233042,25.2249325365133));
#74989=CARTESIAN_POINT('Ctrl Pts',(-0.210816529302013,-8.20894963712995,
25.1363451007806));
#74990=CARTESIAN_POINT('Ctrl Pts',(-4.42123908576554,-6.91982244717752,
24.9591702293152));
#74991=CARTESIAN_POINT('Ctrl Pts',(-6.22631625634268,-5.35390358803423,
24.8705827935825));
#74992=CARTESIAN_POINT('Ctrl Pts',(-7.65317280859548,-2.31334857514353,
24.7354407413121));
#74993=CARTESIAN_POINT('Ctrl Pts',(-7.91100000000044,-1.1570283783628,24.6888861247745));
#74994=CARTESIAN_POINT('Ctrl Pts',(-7.911,3.03701508386212E-12,24.6423315082369));
#74995=CARTESIAN_POINT('',(-7.90781319780899,0.00316833650103562,22.6423315082369));
#74996=CARTESIAN_POINT('Ctrl Pts',(-7.911,3.03701508386212E-12,24.6423315082369));
#74997=CARTESIAN_POINT('Ctrl Pts',(-7.91099999999916,2.20167589666983,24.5537440725042));
#74998=CARTESIAN_POINT('Ctrl Pts',(-6.942145766722,4.38610418338955,24.4651566367714));
#74999=CARTESIAN_POINT('Ctrl Pts',(-3.67820201487994,7.3418068410778,24.287981765306));
#75000=CARTESIAN_POINT('Ctrl Pts',(-1.40868175871418,8.08992666571394,24.1993943295733));
#75001=CARTESIAN_POINT('Ctrl Pts',(2.97309270521588,7.65454228025136,24.0222194581078));
#75002=CARTESIAN_POINT('Ctrl Pts',(5.05102072675871,6.47444880834017,23.9336320223751));
#75003=CARTESIAN_POINT('Ctrl Pts',(7.66951518847996,2.93425195367385,23.7564571509096));
#75004=CARTESIAN_POINT('Ctrl Pts',(8.18956872247098,0.601881960095694,23.6678697151769));
#75005=CARTESIAN_POINT('Ctrl Pts',(7.32306689761184,-3.71537198232766,23.4906948437114));
#75006=CARTESIAN_POINT('Ctrl Pts',(5.94329958849956,-5.6664351893677,23.4021074079787));
#75007=CARTESIAN_POINT('Ctrl Pts',(2.16154501637498,-7.92205913233094,23.2249325365133));
#75008=CARTESIAN_POINT('Ctrl Pts',(-0.210816529304027,-8.20894963712994,
23.1363451007805));
#75009=CARTESIAN_POINT('Ctrl Pts',(-4.42123908576751,-6.91982244717632,
22.9591702293151));
#75010=CARTESIAN_POINT('Ctrl Pts',(-6.22631625634433,-5.35390358803237,
22.8705827935824));
#75011=CARTESIAN_POINT('Ctrl Pts',(-7.65317280859584,-2.3133485751419,22.7354407413121));
#75012=CARTESIAN_POINT('Ctrl Pts',(-7.91100000000042,-1.15702837836207,
22.6888861247745));
#75013=CARTESIAN_POINT('Ctrl Pts',(-7.911,2.86604073806984E-12,22.6423315082369));
#75014=CARTESIAN_POINT('',(-7.91783831042937,0.00131071308626149,20.6423315082369));
#75015=CARTESIAN_POINT('Ctrl Pts',(-7.90700995084759,0.0039669291065153,
22.6423315082369));
#75016=CARTESIAN_POINT('Ctrl Pts',(-7.9071452622316,0.920854935814697,22.6054686655453));
#75017=CARTESIAN_POINT('Ctrl Pts',(-7.52681417092178,3.15012136567669,22.5156845558762));
#75018=CARTESIAN_POINT('Ctrl Pts',(-5.46558729494383,6.15952129533179,22.3729791792306));
#75019=CARTESIAN_POINT('Ctrl Pts',(-0.63604468917613,8.69975179261806,22.1612941113216));
#75020=CARTESIAN_POINT('Ctrl Pts',(5.06500030754639,7.10450222303656,21.9496090434132));
#75021=CARTESIAN_POINT('Ctrl Pts',(7.85987075412757,2.42874849949774,21.7379239755043));
#75022=CARTESIAN_POINT('Ctrl Pts',(8.19225603304053,-2.98184445809894,21.5262389075959));
#75023=CARTESIAN_POINT('Ctrl Pts',(3.4384472016591,-8.7064694362903,21.2616325727098));
#75024=CARTESIAN_POINT('Ctrl Pts',(-5.32233815554137,-7.60654421846925,
20.9493563505979));
#75025=CARTESIAN_POINT('Ctrl Pts',(-7.90279857213812,-2.49308479875549,
20.7429226624402));
#75026=CARTESIAN_POINT('Ctrl Pts',(-7.91783831042937,0.00131071308626149,
20.6423315082369));
#75027=CARTESIAN_POINT('',(-7.91053182871032,-0.00597217323526291,18.6423315082369));
#75028=CARTESIAN_POINT('Ctrl Pts',(-7.91783831042937,0.00131071308626149,
20.6423315082369));
#75029=CARTESIAN_POINT('Ctrl Pts',(-7.91862346273972,0.131531090670436,
20.6370801284859));
#75030=CARTESIAN_POINT('Ctrl Pts',(-7.9160226862592,0.261758841428933,20.6318287487348));
#75031=CARTESIAN_POINT('Ctrl Pts',(-7.84894794642525,1.70281325792949,20.5736561020066));
#75032=CARTESIAN_POINT('Ctrl Pts',(-7.02530278880841,4.29622469448372,20.4678135680522));
#75033=CARTESIAN_POINT('Ctrl Pts',(-4.1258017534078,7.14706517316476,20.3090497671206));
#75034=CARTESIAN_POINT('Ctrl Pts',(-0.215438464096084,8.23200664081911,
20.1502859661893));
#75035=CARTESIAN_POINT('Ctrl Pts',(5.11531456458206,7.06567696722413,19.9386008982805));
#75036=CARTESIAN_POINT('Ctrl Pts',(8.44992758816854,2.17414436211242,19.7269158303718));
#75037=CARTESIAN_POINT('Ctrl Pts',(7.57744882651523,-3.20291380260486,19.5152307624632));
#75038=CARTESIAN_POINT('Ctrl Pts',(4.34776317168055,-7.5565475374821,19.3035456945544));
#75039=CARTESIAN_POINT('Ctrl Pts',(-2.97554305665166,-8.87534071017187,
19.0389393596687));
#75040=CARTESIAN_POINT('Ctrl Pts',(-7.5451282943228,-3.9335702533891,18.8008942085703));
#75041=CARTESIAN_POINT('Ctrl Pts',(-7.91699102695292,-0.660678904189338,
18.6686915914265));
#75042=CARTESIAN_POINT('Ctrl Pts',(-7.91045528272066,-0.0069486233530125,
18.6423315082369));
#75043=CARTESIAN_POINT('',(-7.90191996158085,0.00205550962533024,16.6423315082369));
#75044=CARTESIAN_POINT('Ctrl Pts',(-7.911,2.7494673204842E-12,18.6423315082369));
#75045=CARTESIAN_POINT('Ctrl Pts',(-7.91099999999924,2.20167589666962,18.5537440725042));
#75046=CARTESIAN_POINT('Ctrl Pts',(-6.94214576672209,4.38610418338945,18.4651566367715));
#75047=CARTESIAN_POINT('Ctrl Pts',(-3.67820201487994,7.34180684107782,18.287981765306));
#75048=CARTESIAN_POINT('Ctrl Pts',(-1.40868175871409,8.08992666571397,18.1993943295733));
#75049=CARTESIAN_POINT('Ctrl Pts',(2.97309270521611,7.65454228025129,18.0222194581078));
#75050=CARTESIAN_POINT('Ctrl Pts',(5.05102072675898,6.47444880833998,17.9336320223751));
#75051=CARTESIAN_POINT('Ctrl Pts',(7.66951518848015,2.93425195367341,17.7564571509096));
#75052=CARTESIAN_POINT('Ctrl Pts',(8.18956872247104,0.601881960095133,17.6678697151769));
#75053=CARTESIAN_POINT('Ctrl Pts',(7.32306689761153,-3.7153719823283,17.4906948437114));
#75054=CARTESIAN_POINT('Ctrl Pts',(5.94329958849902,-5.66643518936829,17.4021074079787));
#75055=CARTESIAN_POINT('Ctrl Pts',(2.16154501637408,-7.9220591323312,17.2249325365132));
#75056=CARTESIAN_POINT('Ctrl Pts',(-0.210816529305057,-8.20894963712993,
17.1363451007805));
#75057=CARTESIAN_POINT('Ctrl Pts',(-4.42123908576851,-6.9198224471757,16.959170229315));
#75058=CARTESIAN_POINT('Ctrl Pts',(-6.22631625634517,-5.35390358803143,
16.8705827935823));
#75059=CARTESIAN_POINT('Ctrl Pts',(-7.65317280859596,-2.3133485751412,16.735440741312));
#75060=CARTESIAN_POINT('Ctrl Pts',(-7.91100000000034,-1.15702837836198,
16.6888861247745));
#75061=CARTESIAN_POINT('Ctrl Pts',(-7.911,2.35367281220533E-12,16.6423315082369));
#75062=CARTESIAN_POINT('',(-7.91926959559151,0.00460530123625597,14.6423315082369));
#75063=CARTESIAN_POINT('Ctrl Pts',(-7.89772730700726,0.00300462915809097,
16.6423315082369));
#75064=CARTESIAN_POINT('Ctrl Pts',(-7.90010539424252,1.19923649303746,16.5944605204127));
#75065=CARTESIAN_POINT('Ctrl Pts',(-7.08451991690688,5.03575724884286,16.4407469986342));
#75066=CARTESIAN_POINT('Ctrl Pts',(-2.35822015041585,8.39320165289849,16.2341122098785));
#75067=CARTESIAN_POINT('Ctrl Pts',(3.03369317972992,7.6556601015982,16.0224271419698));
#75068=CARTESIAN_POINT('Ctrl Pts',(6.33771636031792,5.28546422124097,15.8636633410383));
#75069=CARTESIAN_POINT('Ctrl Pts',(8.0743562618132,1.61775091520958,15.7048995401067));
#75070=CARTESIAN_POINT('Ctrl Pts',(7.83528719697496,-3.83386340922832,15.4932144721981));
#75071=CARTESIAN_POINT('Ctrl Pts',(3.58490407290031,-7.9546616986963,15.2815294042894));
#75072=CARTESIAN_POINT('Ctrl Pts',(-1.86216543943523,-8.01303484464982,
15.0698443363805));
#75073=CARTESIAN_POINT('Ctrl Pts',(-6.33144359478282,-5.76141497936659,
14.8744187933557));
#75074=CARTESIAN_POINT('Ctrl Pts',(-7.89775500108633,-2.21401943858167,
14.7319145173077));
#75075=CARTESIAN_POINT('Ctrl Pts',(-7.91926959559151,0.00460530123625597,
14.6423315082369));
#75076=CARTESIAN_POINT('',(-7.91171611945518,-0.00610363383936718,12.6423315082369));
#75077=CARTESIAN_POINT('Ctrl Pts',(-7.91926959559151,0.00460530123625597,
14.6423315082369));
#75078=CARTESIAN_POINT('Ctrl Pts',(-7.92317454462533,0.407290861127973,
14.6260719833533));
#75079=CARTESIAN_POINT('Ctrl Pts',(-7.71423377210186,3.42846943275032,14.503969924515));
#75080=CARTESIAN_POINT('Ctrl Pts',(-3.79870386219735,8.54783779767484,14.2760253317233));
#75081=CARTESIAN_POINT('Ctrl Pts',(3.60029715467924,7.94008165336425,14.0114189968371));
#75082=CARTESIAN_POINT('Ctrl Pts',(7.25069154288822,3.90383120149957,13.7997339289286));
#75083=CARTESIAN_POINT('Ctrl Pts',(8.25235742781774,-0.037115784206696,
13.6409701279969));
#75084=CARTESIAN_POINT('Ctrl Pts',(7.21933219681781,-3.96151356154354,13.4822063270656));
#75085=CARTESIAN_POINT('Ctrl Pts',(3.52601661662749,-7.97856133140822,13.2705212591568));
#75086=CARTESIAN_POINT('Ctrl Pts',(-2.37938567029377,-8.39444481693599,
13.0588361912482));
#75087=CARTESIAN_POINT('Ctrl Pts',(-6.58448534345744,-4.93162653768452,
12.8471511233393));
#75088=CARTESIAN_POINT('Ctrl Pts',(-7.80591338107149,-2.07856012442669,
12.7259566513281));
#75089=CARTESIAN_POINT('Ctrl Pts',(-7.91509200919393,-0.386870836674057,
12.6576834462939));
#75090=CARTESIAN_POINT('Ctrl Pts',(-7.91171611945518,-0.00610363383936718,
12.6423315082369));
#75091=CARTESIAN_POINT('',(-7.90558071021525,-0.000276217684555168,10.6423315082369));
#75092=CARTESIAN_POINT('Ctrl Pts',(-7.91171611945518,-0.00610363383936718,
12.6423315082369));
#75093=CARTESIAN_POINT('Ctrl Pts',(-7.89181724590517,2.238293845799,12.5518409123396));
#75094=CARTESIAN_POINT('Ctrl Pts',(-5.74352385136303,7.13599824900525,12.3555077824878));
#75095=CARTESIAN_POINT('Ctrl Pts',(2.59776724179471,8.98594944374683,12.053332118682));
#75096=CARTESIAN_POINT('Ctrl Pts',(7.86734082994195,3.75659214309986,11.7887257837959));
#75097=CARTESIAN_POINT('Ctrl Pts',(8.06120621431038,-1.68207617849999,11.5770407158874));
#75098=CARTESIAN_POINT('Ctrl Pts',(6.28991713969547,-5.34225823726834,11.4182769149557));
#75099=CARTESIAN_POINT('Ctrl Pts',(2.97255753145224,-7.67959952006021,11.2595131140244));
#75100=CARTESIAN_POINT('Ctrl Pts',(-2.43982948211331,-8.37481141268209,
11.0478280461154));
#75101=CARTESIAN_POINT('Ctrl Pts',(-7.09110329026493,-4.9884606133613,10.8421008441866));
#75102=CARTESIAN_POINT('Ctrl Pts',(-7.90683872761096,-1.17212167128525,
10.6892949092345));
#75103=CARTESIAN_POINT('Ctrl Pts',(-7.90548959171866,-0.000280861935244084,
10.6423315082369));
#75104=CARTESIAN_POINT('',(-7.911,1.67199587508549E-12,8.64233150823696));
#75105=CARTESIAN_POINT('Ctrl Pts',(-7.911,1.84185999785313E-12,10.642331508237));
#75106=CARTESIAN_POINT('Ctrl Pts',(-7.91099999999949,2.20167589666864,10.5537440725042));
#75107=CARTESIAN_POINT('Ctrl Pts',(-6.94214576672266,4.3861041833885,10.4651566367715));
#75108=CARTESIAN_POINT('Ctrl Pts',(-3.67820201488105,7.34180684107724,10.287981765306));
#75109=CARTESIAN_POINT('Ctrl Pts',(-1.4086817587154,8.08992666571373,10.1993943295733));
#75110=CARTESIAN_POINT('Ctrl Pts',(2.97309270521472,7.65454228025181,10.0222194581079));
#75111=CARTESIAN_POINT('Ctrl Pts',(5.05102072675773,6.47444880834093,9.93363202237514));
#75112=CARTESIAN_POINT('Ctrl Pts',(7.66951518847951,2.93425195367501,9.75645715090968));
#75113=CARTESIAN_POINT('Ctrl Pts',(8.18956872247089,0.601881960096929,9.66786971517696));
#75114=CARTESIAN_POINT('Ctrl Pts',(7.32306689761239,-3.71537198232655,9.49069484371151));
#75115=CARTESIAN_POINT('Ctrl Pts',(5.94329958850041,-5.6664351893668,9.40210740797877));
#75116=CARTESIAN_POINT('Ctrl Pts',(2.16154501637618,-7.92205913233061,9.22493253651332));
#75117=CARTESIAN_POINT('Ctrl Pts',(-0.210816529302787,-8.20894963712997,
9.13634510078059));
#75118=CARTESIAN_POINT('Ctrl Pts',(-4.42123908576646,-6.91982244717699,
8.95917022931514));
#75119=CARTESIAN_POINT('Ctrl Pts',(-6.22631625634352,-5.35390358803331,
8.87058279358241));
#75120=CARTESIAN_POINT('Ctrl Pts',(-7.65317280859549,-2.31334857514306,
8.73544074131211));
#75121=CARTESIAN_POINT('Ctrl Pts',(-7.91100000000024,-1.15702837836326,
8.68888612477454));
#75122=CARTESIAN_POINT('Ctrl Pts',(-7.911,1.67199587508549E-12,8.64233150823696));
#75123=CARTESIAN_POINT('',(-7.911,1.5004664177809E-12,6.64233150823697));
#75124=CARTESIAN_POINT('Ctrl Pts',(-7.911,1.67199587508549E-12,8.64233150823696));
#75125=CARTESIAN_POINT('Ctrl Pts',(-7.91099999999954,2.20167589666832,8.55374407250424));
#75126=CARTESIAN_POINT('Ctrl Pts',(-6.9421457667229,4.38610418338806,8.46515663677151));
#75127=CARTESIAN_POINT('Ctrl Pts',(-3.67820201488173,7.34180684107685,8.28798176530607));
#75128=CARTESIAN_POINT('Ctrl Pts',(-1.40868175871635,8.08992666571352,8.19939432957335));
#75129=CARTESIAN_POINT('Ctrl Pts',(2.97309270521354,7.65454228025223,8.02221945810791));
#75130=CARTESIAN_POINT('Ctrl Pts',(5.05102072675658,6.47444880834178,7.93363202237519));
#75131=CARTESIAN_POINT('Ctrl Pts',(7.66951518847886,2.9342519536766,7.75645715090975));
#75132=CARTESIAN_POINT('Ctrl Pts',(8.18956872247071,0.601881960098821,7.66786971517703));
#75133=CARTESIAN_POINT('Ctrl Pts',(7.32306689761335,-3.71537198232458,7.49069484371159));
#75134=CARTESIAN_POINT('Ctrl Pts',(5.94329958850202,-5.66643518936506,7.40210740797886));
#75135=CARTESIAN_POINT('Ctrl Pts',(2.16154501637873,-7.92205913232988,7.22493253651342));
#75136=CARTESIAN_POINT('Ctrl Pts',(-0.210816529299954,-8.20894963713,7.1363451007807));
#75137=CARTESIAN_POINT('Ctrl Pts',(-4.42123908576381,-6.91982244717863,
6.95917022931526));
#75138=CARTESIAN_POINT('Ctrl Pts',(-6.22631625634134,-5.35390358803579,
6.87058279358254));
#75139=CARTESIAN_POINT('Ctrl Pts',(-7.65317280859497,-2.31334857514532,
6.7354407413122));
#75140=CARTESIAN_POINT('Ctrl Pts',(-7.91100000000022,-1.15702837836448,
6.68888612477459));
#75141=CARTESIAN_POINT('Ctrl Pts',(-7.911,1.5004664177809E-12,6.64233150823697));
#75142=CARTESIAN_POINT('',(-7.911,1.33004718350094E-12,4.64233150823698));
#75143=CARTESIAN_POINT('Ctrl Pts',(-7.911,1.5004664177809E-12,6.64233150823697));
#75144=CARTESIAN_POINT('Ctrl Pts',(-7.91099999999958,2.20167589666815,6.55374407250425));
#75145=CARTESIAN_POINT('Ctrl Pts',(-6.94214576672299,4.38610418338791,6.46515663677152));
#75146=CARTESIAN_POINT('Ctrl Pts',(-3.67820201488189,7.34180684107677,6.28798176530608));
#75147=CARTESIAN_POINT('Ctrl Pts',(-1.40868175871652,8.08992666571349,6.19939432957336));
#75148=CARTESIAN_POINT('Ctrl Pts',(2.97309270521337,7.65454228025229,6.02221945810792));
#75149=CARTESIAN_POINT('Ctrl Pts',(5.05102072675644,6.47444880834189,5.9336320223752));
#75150=CARTESIAN_POINT('Ctrl Pts',(7.6695151884788,2.93425195367677,5.75645715090976));
#75151=CARTESIAN_POINT('Ctrl Pts',(8.18956872247069,0.601881960098999,5.66786971517704));
#75152=CARTESIAN_POINT('Ctrl Pts',(7.32306689761343,-3.71537198232442,5.4906948437116));
#75153=CARTESIAN_POINT('Ctrl Pts',(5.94329958850214,-5.66643518936493,5.40210740797887));
#75154=CARTESIAN_POINT('Ctrl Pts',(2.1615450163789,-7.92205913232983,5.22493253651343));
#75155=CARTESIAN_POINT('Ctrl Pts',(-0.210816529299777,-8.20894963713001,
5.13634510078071));
#75156=CARTESIAN_POINT('Ctrl Pts',(-4.42123908576366,-6.91982244717873,
4.95917022931527));
#75157=CARTESIAN_POINT('Ctrl Pts',(-6.22631625634122,-5.35390358803592,
4.87058279358255));
#75158=CARTESIAN_POINT('Ctrl Pts',(-7.65317280859492,-2.31334857514548,
4.73544074131221));
#75159=CARTESIAN_POINT('Ctrl Pts',(-7.91100000000019,-1.15702837836465,
4.68888612477459));
#75160=CARTESIAN_POINT('Ctrl Pts',(-7.911,1.33004718350094E-12,4.64233150823698));
#75161=CARTESIAN_POINT('',(-7.9078171476394,0.0030170320035519,2.64233150823698));
#75162=CARTESIAN_POINT('Ctrl Pts',(-7.911,1.33004718350094E-12,4.64233150823698));
#75163=CARTESIAN_POINT('Ctrl Pts',(-7.91099999999963,2.20167589666798,4.55374407250426));
#75164=CARTESIAN_POINT('Ctrl Pts',(-6.94214576672309,4.38610418338776,4.46515663677153));
#75165=CARTESIAN_POINT('Ctrl Pts',(-3.67820201488205,7.34180684107669,4.28798176530609));
#75166=CARTESIAN_POINT('Ctrl Pts',(-1.4086817587167,8.08992666571346,4.19939432957337));
#75167=CARTESIAN_POINT('Ctrl Pts',(2.97309270521321,7.65454228025235,4.02221945810792));
#75168=CARTESIAN_POINT('Ctrl Pts',(5.0510207267563,6.474448808342,3.93363202237521));
#75169=CARTESIAN_POINT('Ctrl Pts',(7.66951518847874,2.93425195367693,3.75645715090976));
#75170=CARTESIAN_POINT('Ctrl Pts',(8.18956872247068,0.601881960099174,3.66786971517705));
#75171=CARTESIAN_POINT('Ctrl Pts',(7.32306689761351,-3.71537198232427,3.4906948437116));
#75172=CARTESIAN_POINT('Ctrl Pts',(5.94329958850226,-5.6664351893648,3.40210740797888));
#75173=CARTESIAN_POINT('Ctrl Pts',(2.16154501637907,-7.92205913232978,3.22493253651343));
#75174=CARTESIAN_POINT('Ctrl Pts',(-0.2108165292996,-8.20894963713001,3.13634510078072));
#75175=CARTESIAN_POINT('Ctrl Pts',(-4.42123908576351,-6.91982244717882,
2.95917022931527));
#75176=CARTESIAN_POINT('Ctrl Pts',(-6.22631625634111,-5.35390358803606,
2.87058279358255));
#75177=CARTESIAN_POINT('Ctrl Pts',(-7.65317280859487,-2.31334857514565,
2.73544074131222));
#75178=CARTESIAN_POINT('Ctrl Pts',(-7.91100000000017,-1.15702837836482,
2.6888861247746));
#75179=CARTESIAN_POINT('Ctrl Pts',(-7.911,1.15962794922098E-12,2.64233150823698));
#75180=CARTESIAN_POINT('',(-7.9226973683943,0.00165221630280203,0.642331508236981));
#75181=CARTESIAN_POINT('Ctrl Pts',(-7.90696476388048,0.00382500824235466,
2.64233150823698));
#75182=CARTESIAN_POINT('Ctrl Pts',(-7.90689714804109,0.955993951285606,
2.60405569308827));
#75183=CARTESIAN_POINT('Ctrl Pts',(-7.50511545360724,3.22058475577076,2.5128586109623));
#75184=CARTESIAN_POINT('Ctrl Pts',(-5.38279128402438,6.23167160317878,2.36874026185943));
#75185=CARTESIAN_POINT('Ctrl Pts',(-0.520794108197176,8.70764732515362,
2.15705519395051));
#75186=CARTESIAN_POINT('Ctrl Pts',(5.16041761571073,7.03604612731708,1.94537012604191));
#75187=CARTESIAN_POINT('Ctrl Pts',(7.8900448895937,2.32430843730864,1.73368505813334));
#75188=CARTESIAN_POINT('Ctrl Pts',(8.15525751620599,-3.09170662911801,1.52199999022448));
#75189=CARTESIAN_POINT('Ctrl Pts',(3.31495225340653,-8.74927398045779,1.25739365533871));
#75190=CARTESIAN_POINT('Ctrl Pts',(-5.37156617111391,-7.54432674623615,
0.946530405683787));
#75191=CARTESIAN_POINT('Ctrl Pts',(-7.91185123215259,-2.45352580665413,
0.741509689983209));
#75192=CARTESIAN_POINT('Ctrl Pts',(-7.9226973683943,0.00165221630280203,
0.642331508236981));
#75193=CARTESIAN_POINT('',(-7.90493147168185,-0.00324651952237742,-1.35766849176302));
#75194=CARTESIAN_POINT('Ctrl Pts',(-7.9226973683943,0.00165221630280203,
0.642331508236981));
#75195=CARTESIAN_POINT('Ctrl Pts',(-7.92342618264295,0.16662974251393,0.635667156028865));
#75196=CARTESIAN_POINT('Ctrl Pts',(-7.84288560960201,2.95119247036142,0.52316026986663));
#75197=CARTESIAN_POINT('Ctrl Pts',(-4.56546138485153,8.16671696405687,0.304810849749407));
#75198=CARTESIAN_POINT('Ctrl Pts',(2.87982575388721,8.23246492026226,0.0402045148638317));
#75199=CARTESIAN_POINT('Ctrl Pts',(6.85552241033558,4.54500061088602,-0.17148055304496));
#75200=CARTESIAN_POINT('Ctrl Pts',(8.70655133397208,-0.576037275883916,
-0.383165620953742));
#75201=CARTESIAN_POINT('Ctrl Pts',(6.33123203588563,-6.00082072304389,-0.594850688862375));
#75202=CARTESIAN_POINT('Ctrl Pts',(1.30771107118631,-8.1300716313903,-0.806535756770927));
#75203=CARTESIAN_POINT('Ctrl Pts',(-2.73589803143749,-7.7859037014987,-0.965299557702622));
#75204=CARTESIAN_POINT('Ctrl Pts',(-6.11165572102573,-5.51896580875037,
-1.12406335863396));
#75205=CARTESIAN_POINT('Ctrl Pts',(-7.70344787938649,-2.55725839949862,
-1.25485300332087));
#75206=CARTESIAN_POINT('Ctrl Pts',(-7.91039240334899,-0.623390115977236,
-1.33272138103054));
#75207=CARTESIAN_POINT('Ctrl Pts',(-7.90493147168185,-0.00324651952237742,
-1.35766849176302));
#75208=CARTESIAN_POINT('',(-7.90837905701166,-0.000918770651100465,-3.357668491763));
#75209=CARTESIAN_POINT('Ctrl Pts',(-7.90493147168185,-0.00324651952237742,
-1.35766849176302));
#75210=CARTESIAN_POINT('Ctrl Pts',(-7.88722343394008,2.00767888308271,-1.43856391498488));
#75211=CARTESIAN_POINT('Ctrl Pts',(-6.10452476405389,6.6637469996248,-1.62530187216105));
#75212=CARTESIAN_POINT('Ctrl Pts',(1.77247152912565,9.19149319484671,-1.91788236329163));
#75213=CARTESIAN_POINT('Ctrl Pts',(7.50118080572254,4.44261861729297,-2.18248869817746));
#75214=CARTESIAN_POINT('Ctrl Pts',(8.1730998889146,-0.93638062620659,-2.39417376608628));
#75215=CARTESIAN_POINT('Ctrl Pts',(6.28922068173262,-6.04763295627693,-2.6058588339948));
#75216=CARTESIAN_POINT('Ctrl Pts',(0.980539725566132,-8.66768713018763,
-2.81754390190352));
#75217=CARTESIAN_POINT('Ctrl Pts',(-4.23486739714097,-7.06245238847923,
-3.02922896981223));
#75218=CARTESIAN_POINT('Ctrl Pts',(-7.10657322087715,-4.19516421302404,
-3.18799277074389));
#75219=CARTESIAN_POINT('Ctrl Pts',(-7.88113996482031,-1.50027602753856,
-3.29747261139401));
#75220=CARTESIAN_POINT('Ctrl Pts',(-7.90817870772519,-0.0915277219815716,
-3.3540311850671));
#75221=CARTESIAN_POINT('Ctrl Pts',(-7.90837905701166,-0.000918770651100465,
-3.357668491763));
#75222=CARTESIAN_POINT('',(-7.911,7.02216063075412E-13,-5.35766849176301));
#75223=CARTESIAN_POINT('Ctrl Pts',(-7.911,6.47815134868779E-13,-3.357668491763));
#75224=CARTESIAN_POINT('Ctrl Pts',(-7.91099999999982,2.20167589666714,-3.44625592749572));
#75225=CARTESIAN_POINT('Ctrl Pts',(-6.9421457667236,4.38610418338687,-3.53484336322843));
#75226=CARTESIAN_POINT('Ctrl Pts',(-3.67820201488321,7.34180684107606,-3.71201823469386));
#75227=CARTESIAN_POINT('Ctrl Pts',(-1.40868175871816,8.08992666571316,-3.80060567042658));
#75228=CARTESIAN_POINT('Ctrl Pts',(2.97309270521153,7.65454228025296,-3.977780541892));
#75229=CARTESIAN_POINT('Ctrl Pts',(5.05102072675473,6.47444880834318,-4.06636797762472));
#75230=CARTESIAN_POINT('Ctrl Pts',(7.66951518847789,2.93425195367902,-4.24354284909015));
#75231=CARTESIAN_POINT('Ctrl Pts',(8.18956872247046,0.601881960101596,-4.33213028482286));
#75232=CARTESIAN_POINT('Ctrl Pts',(7.3230668976147,-3.71537198232182,-4.50930515628829));
#75233=CARTESIAN_POINT('Ctrl Pts',(5.94329958850423,-5.66643518936268,-4.59789259202101));
#75234=CARTESIAN_POINT('Ctrl Pts',(2.16154501638213,-7.9220591323289,-4.77506746348644));
#75235=CARTESIAN_POINT('Ctrl Pts',(-0.210816529296236,-8.20894963713006,
-4.86365489921916));
#75236=CARTESIAN_POINT('Ctrl Pts',(-4.42123908576041,-6.91982244718076,
-5.04082977068459));
#75237=CARTESIAN_POINT('Ctrl Pts',(-6.22631625633858,-5.35390358803894,
-5.1294172064173));
#75238=CARTESIAN_POINT('Ctrl Pts',(-7.65317280859422,-2.31334857514834,
-5.26455925868768));
#75239=CARTESIAN_POINT('Ctrl Pts',(-7.9110000000001,-1.15702837836641,-5.31111387522534));
#75240=CARTESIAN_POINT('Ctrl Pts',(-7.911,7.02216063075412E-13,-5.35766849176301));
#75241=CARTESIAN_POINT('',(-7.911,3.06976666308856E-13,-7.35766849176299));
#75242=CARTESIAN_POINT('Ctrl Pts',(-7.911,7.02216063075412E-13,-5.35766849176301));
#75243=CARTESIAN_POINT('Ctrl Pts',(-7.91099999999981,2.2016758966675,-5.44625592749573));
#75244=CARTESIAN_POINT('Ctrl Pts',(-6.9421457667233,4.3861041833875,-5.53484336322846));
#75245=CARTESIAN_POINT('Ctrl Pts',(-3.67820201488211,7.34180684107671,-5.71201823469391));
#75246=CARTESIAN_POINT('Ctrl Pts',(-1.40868175871657,8.08992666571353,-5.80060567042664));
#75247=CARTESIAN_POINT('Ctrl Pts',(2.97309270521362,7.65454228025224,-5.97778054189209));
#75248=CARTESIAN_POINT('Ctrl Pts',(5.0510207267568,6.47444880834166,-6.06636797762481));
#75249=CARTESIAN_POINT('Ctrl Pts',(7.66951518847909,2.93425195367611,-6.24354284909027));
#75250=CARTESIAN_POINT('Ctrl Pts',(8.1895687224708,0.601881960098109,-6.332130284823));
#75251=CARTESIAN_POINT('Ctrl Pts',(7.32306689761293,-3.71537198232549,-6.50930515628846));
#75252=CARTESIAN_POINT('Ctrl Pts',(5.94329958850123,-5.66643518936595,-6.59789259202118));
#75253=CARTESIAN_POINT('Ctrl Pts',(2.16154501637732,-7.9220591323303,-6.77506746348663));
#75254=CARTESIAN_POINT('Ctrl Pts',(-0.210816529301604,-8.20894963713,-6.86365489921936));
#75255=CARTESIAN_POINT('Ctrl Pts',(-4.42123908576546,-6.91982244717762,
-7.04082977068481));
#75256=CARTESIAN_POINT('Ctrl Pts',(-6.22631625634275,-5.35390358803421,
-7.12941720641755));
#75257=CARTESIAN_POINT('Ctrl Pts',(-7.65317280859512,-2.31334857514423,
-7.26455925868784));
#75258=CARTESIAN_POINT('Ctrl Pts',(-7.91100000000004,-1.15702837836455,
-7.31111387522542));
#75259=CARTESIAN_POINT('Ctrl Pts',(-7.911,3.06976666308856E-13,-7.35766849176299));
#75260=CARTESIAN_POINT('',(-7.90153522810969,-6.13663431064494E-5,-9.35774809978824));
#75261=CARTESIAN_POINT('Ctrl Pts',(-7.911,3.06976666308856E-13,-7.35766849176299));
#75262=CARTESIAN_POINT('Ctrl Pts',(-7.91099999999991,2.20167589666695,-7.44625592749571));
#75263=CARTESIAN_POINT('Ctrl Pts',(-6.94214576672365,4.38610418338686,-7.53484336322843));
#75264=CARTESIAN_POINT('Ctrl Pts',(-3.678202014883,7.34180684107621,-7.71201823469387));
#75265=CARTESIAN_POINT('Ctrl Pts',(-1.40868175871774,8.08992666571328,-7.80060567042659));
#75266=CARTESIAN_POINT('Ctrl Pts',(2.97309270521222,7.65454228025274,-7.97778054189203));
#75267=CARTESIAN_POINT('Ctrl Pts',(5.05102072675546,6.47444880834266,-8.06636797762475));
#75268=CARTESIAN_POINT('Ctrl Pts',(7.66951518847836,2.93425195367792,-8.24354284909019));
#75269=CARTESIAN_POINT('Ctrl Pts',(8.1895687224706,0.601881960100234,-8.33213028482292));
#75270=CARTESIAN_POINT('Ctrl Pts',(7.32306689761399,-3.71537198232332,-8.50930515628836));
#75271=CARTESIAN_POINT('Ctrl Pts',(5.94329958850299,-5.66643518936404,-8.59789259202108));
#75272=CARTESIAN_POINT('Ctrl Pts',(2.16154501638009,-7.9220591323295,-8.77506746348652));
#75273=CARTESIAN_POINT('Ctrl Pts',(-0.210816529298536,-8.20894963713004,
-8.86365489921924));
#75274=CARTESIAN_POINT('Ctrl Pts',(-4.42123908576261,-6.9198224471794,-9.04082977068468));
#75275=CARTESIAN_POINT('Ctrl Pts',(-6.22631625634041,-5.35390358803686,
-9.1294172064174));
#75276=CARTESIAN_POINT('Ctrl Pts',(-7.65316473334085,-2.3133657830805,-9.26455849385518));
#75277=CARTESIAN_POINT('Ctrl Pts',(-7.9109915283976,-1.1570663720484,-9.31111234556023));
#75278=CARTESIAN_POINT('Ctrl Pts',(-7.91099999979124,-5.70254707422617E-5,
-9.35766619726528));
#75279=CARTESIAN_POINT('',(-7.91074476364229,0.00235076547380794,-11.3575320716792));
#75280=CARTESIAN_POINT('Ctrl Pts',(-7.89527219315753,-6.42387880278883E-5,
-9.35780229637968));
#75281=CARTESIAN_POINT('Ctrl Pts',(-7.8943301009396,0.251675616834198,-9.36792465872531));
#75282=CARTESIAN_POINT('Ctrl Pts',(-7.88156223750695,0.50372398062786,-9.37784868590548));
#75283=CARTESIAN_POINT('Ctrl Pts',(-7.85712534419498,0.754793832873867,
-9.38764551474725));
#75284=CARTESIAN_POINT('Ctrl Pts',(-7.83259375277481,1.00683663367482,-9.39748030836408));
#75285=CARTESIAN_POINT('Ctrl Pts',(-7.79630326984454,1.25789283539776,-9.40718691589166));
#75286=CARTESIAN_POINT('Ctrl Pts',(-7.74844328219722,1.50670283778631,-9.41683730437658));
#75287=CARTESIAN_POINT('Ctrl Pts',(-7.70059642379473,1.75544458509165,-9.42648504550785));
#75288=CARTESIAN_POINT('Ctrl Pts',(-7.64118718455143,2.00194106078235,-9.43607659843696));
#75289=CARTESIAN_POINT('Ctrl Pts',(-7.57042400098654,2.24498195752224,-9.44568387099945));
#75290=CARTESIAN_POINT('Ctrl Pts',(-7.49983745088267,2.48741619480164,-9.45526716264815));
#75291=CARTESIAN_POINT('Ctrl Pts',(-7.41795433352572,2.72641195855995,-9.46486609555196));
#75292=CARTESIAN_POINT('Ctrl Pts',(-7.3249890753825,2.96081918184579,-9.47455204041744));
#75293=CARTESIAN_POINT('Ctrl Pts',(-7.23232399455102,3.19446952313566,-9.48420671014908));
#75294=CARTESIAN_POINT('Ctrl Pts',(-7.1286489625597,3.42356094898595,-9.49394783084039));
#75295=CARTESIAN_POINT('Ctrl Pts',(-7.01417259474218,3.64700603454982,-9.50384608407707));
#75296=CARTESIAN_POINT('Ctrl Pts',(-6.90790243038578,3.85443352740454,-9.51303478405383));
#75297=CARTESIAN_POINT('Ctrl Pts',(-6.79232442010998,4.0569958014873,-9.52235889603522));
#75298=CARTESIAN_POINT('Ctrl Pts',(-6.66759430689156,4.25386161900847,-9.53187496484008));
#75299=CARTESIAN_POINT('Ctrl Pts',(-6.53521053392643,4.46280747032571,-9.5419749564113));
#75300=CARTESIAN_POINT('Ctrl Pts',(-6.39251823069767,4.66533634529571,-9.55229118519302));
#75301=CARTESIAN_POINT('Ctrl Pts',(-6.24059578980112,4.86088392314525,-9.56289125685668));
#75302=CARTESIAN_POINT('Ctrl Pts',(-6.16211168653307,4.961905050789,-9.56836732157885));
#75303=CARTESIAN_POINT('Ctrl Pts',(-6.08116370595779,5.06106365602323,-9.57391913890214));
#75304=CARTESIAN_POINT('Ctrl Pts',(-5.99789672225837,5.15828587354442,-9.57955602982518));
#75305=CARTESIAN_POINT('Ctrl Pts',(-5.89101188654535,5.28308420639768,-9.58679176881166));
#75306=CARTESIAN_POINT('Ctrl Pts',(-5.78018816140105,5.40448460888323,-9.59403368896476));
#75307=CARTESIAN_POINT('Ctrl Pts',(-5.66550358296166,5.52218078259242,-9.60114611375309));
#75308=CARTESIAN_POINT('Ctrl Pts',(-5.55081900452227,5.63987695630161,-9.60825853854142));
#75309=CARTESIAN_POINT('Ctrl Pts',(-5.43227295202669,5.75386858884513,-9.61524146796497));
#75310=CARTESIAN_POINT('Ctrl Pts',(-5.30997227108176,5.86379653437864,-9.62195922549235));
#75311=CARTESIAN_POINT('Ctrl Pts',(-5.00007320380716,6.14234418861115,-9.63898142664305));
#75312=CARTESIAN_POINT('Ctrl Pts',(-4.66767152718237,6.39691191112764,-9.65584425758327));
#75313=CARTESIAN_POINT('Ctrl Pts',(-4.31753906619885,6.62407803953151,-9.6726110349599));
#75314=CARTESIAN_POINT('Ctrl Pts',(-4.15333299303393,6.73061502783731,-9.68047436378384));
#75315=CARTESIAN_POINT('Ctrl Pts',(-3.98522730228223,6.83112598164767,-9.68831656612694));
#75316=CARTESIAN_POINT('Ctrl Pts',(-3.81371429539387,6.92526179046604,-9.69614417312065));
#75317=CARTESIAN_POINT('Ctrl Pts',(-3.43607642441284,7.13253030654064,-9.71337902249802));
#75318=CARTESIAN_POINT('Ctrl Pts',(-3.04192208333915,7.30888923791777,-9.73054311454239));
#75319=CARTESIAN_POINT('Ctrl Pts',(-2.63652811821922,7.45258697954143,-9.74770616387365));
#75320=CARTESIAN_POINT('Ctrl Pts',(-2.21996567575453,7.60024354914455,-9.76534204986287));
#75321=CARTESIAN_POINT('Ctrl Pts',(-1.79153720395816,7.71341642853467,-9.78297683489474));
#75322=CARTESIAN_POINT('Ctrl Pts',(-1.35692620791112,7.79024165518569,-9.80068615563215));
#75323=CARTESIAN_POINT('Ctrl Pts',(-0.922315211864013,7.86706688183672,
-9.81839547636956));
#75324=CARTESIAN_POINT('Ctrl Pts',(-0.481522224584858,7.90754687054486,
-9.83617933281251));
#75325=CARTESIAN_POINT('Ctrl Pts',(-0.0401750600089637,7.90982063659286,
-9.85411336162388));
#75326=CARTESIAN_POINT('Ctrl Pts',(0.234138411264575,7.91123386569582,-9.86526001915795));
#75327=CARTESIAN_POINT('Ctrl Pts',(0.508667165951846,7.89788740320303,-9.8764646894644));
#75328=CARTESIAN_POINT('Ctrl Pts',(0.782016690662756,7.87024143589644,-9.88774553324992));
#75329=CARTESIAN_POINT('Ctrl Pts',(1.07532735614229,7.84057664289161,-9.89985015205766));
#75330=CARTESIAN_POINT('Ctrl Pts',(1.36680038013542,7.79420532872234,-9.91185505208351));
#75331=CARTESIAN_POINT('Ctrl Pts',(1.65475865274654,7.73181204052291,-9.92378133788048));
#75332=CARTESIAN_POINT('Ctrl Pts',(1.94829366193426,7.66821041429143,-9.93593859378857));
#75333=CARTESIAN_POINT('Ctrl Pts',(2.23817720578776,7.58796037767743,-9.94801416102178));
#75334=CARTESIAN_POINT('Ctrl Pts',(2.52265930792318,7.49173880834698,-9.9600303941952));
#75335=CARTESIAN_POINT('Ctrl Pts',(2.81244630555269,7.39372294206166,-9.97227070073119));
#75336=CARTESIAN_POINT('Ctrl Pts',(3.09662944828447,7.27913446845292,-9.98444943970486));
#75337=CARTESIAN_POINT('Ctrl Pts',(3.3733735729584,7.14863706445015,-9.9965902397732));
#75338=CARTESIAN_POINT('Ctrl Pts',(3.49882216122815,7.08948236649837,-10.0020936853507));
#75339=CARTESIAN_POINT('Ctrl Pts',(3.62274227244574,7.02705795335948,-10.0075893351489));
#75340=CARTESIAN_POINT('Ctrl Pts',(3.74496311571731,6.9614221281404,-10.0130793900722));
#75341=CARTESIAN_POINT('Ctrl Pts',(4.01459670541344,6.81662175945726,-10.0251910984923));
#75342=CARTESIAN_POINT('Ctrl Pts',(4.27596109957176,6.65619488276075,-10.0372755769009));
#75343=CARTESIAN_POINT('Ctrl Pts',(4.52735890105361,6.48136368121027,-10.0493564565806));
#75344=CARTESIAN_POINT('Ctrl Pts',(4.77553132137262,6.30877552737475,-10.0612823411032));
#75345=CARTESIAN_POINT('Ctrl Pts',(5.01399221247215,6.12214982628365,-10.0732047186465));
#75346=CARTESIAN_POINT('Ctrl Pts',(5.24108658267087,5.92261756599295,-10.0851463225595));
#75347=CARTESIAN_POINT('Ctrl Pts',(5.45855407042944,5.73154378757107,-10.0965817033684));
#75348=CARTESIAN_POINT('Ctrl Pts',(5.66559897180327,5.5286339325247,-10.1080347150264));
#75349=CARTESIAN_POINT('Ctrl Pts',(5.86073602097242,5.31484771193084,-10.1195253206034));
#75350=CARTESIAN_POINT('Ctrl Pts',(6.03811594843458,5.12051565421648,-10.1299703016689));
#75351=CARTESIAN_POINT('Ctrl Pts',(6.20565672467288,4.91719604855102,-10.140446345998));
#75352=CARTESIAN_POINT('Ctrl Pts',(6.36221108407443,4.70558972801577,-10.15096844773));
#75353=CARTESIAN_POINT('Ctrl Pts',(6.4541093630474,4.58137564192243,-10.1571449799202));
#75354=CARTESIAN_POINT('Ctrl Pts',(6.54223146098758,4.45447282317314,-10.1633944540145));
#75355=CARTESIAN_POINT('Ctrl Pts',(6.62632645499383,4.32502182821367,-10.1696981874286));
#75356=CARTESIAN_POINT('Ctrl Pts',(6.76675304746766,4.1088572118852,-10.1802245191522));
#75357=CARTESIAN_POINT('Ctrl Pts',(6.89595142361405,3.88558459180187,-10.1909021487313));
#75358=CARTESIAN_POINT('Ctrl Pts',(7.01370242259043,3.6563945797851,-10.2016440851118));
#75359=CARTESIAN_POINT('Ctrl Pts',(7.13162589123027,3.42686887359518,-10.212401755186));
#75360=CARTESIAN_POINT('Ctrl Pts',(7.23806753818029,3.19140821185823,-10.2232239205799));
#75361=CARTESIAN_POINT('Ctrl Pts',(7.33279275849123,2.95125878677734,-10.2340232074323));
#75362=CARTESIAN_POINT('Ctrl Pts',(7.42753659861487,2.71106215634502,-10.2448246170636));
#75363=CARTESIAN_POINT('Ctrl Pts',(7.51055849952725,2.4661749093005,-10.2556031391583));
#75364=CARTESIAN_POINT('Ctrl Pts',(7.58162270374497,2.2178959806029,-10.2662713483209));
#75365=CARTESIAN_POINT('Ctrl Pts',(7.62886775592555,2.05283466639023,-10.2733638093441));
#75366=CARTESIAN_POINT('Ctrl Pts',(7.67082764334959,1.88627535844677,-10.280407513331));
#75367=CARTESIAN_POINT('Ctrl Pts',(7.70743584663393,1.71861221357824,-10.2873767708844));
#75368=CARTESIAN_POINT('Ctrl Pts',(7.75779321985561,1.48797878160987,-10.2969635157176));
#75369=CARTESIAN_POINT('Ctrl Pts',(7.79821517641293,1.25528979134765,-10.306518869809));
#75370=CARTESIAN_POINT('Ctrl Pts',(7.82861986687105,1.02135642216782,-10.3160211309126));
#75371=CARTESIAN_POINT('Ctrl Pts',(7.85899053714492,0.787684803928398,-10.3255127598186));
#75372=CARTESIAN_POINT('Ctrl Pts',(7.87936616761867,0.552770753253131,-10.3349514144832));
#75373=CARTESIAN_POINT('Ctrl Pts',(7.88961438555434,0.317430649804225,-10.3443154654274));
#75374=CARTESIAN_POINT('Ctrl Pts',(7.89975352869977,0.0845953401234145,
-10.3535798520301));
#75375=CARTESIAN_POINT('Ctrl Pts',(7.89997944780537,-0.148657735369844,
-10.3627712145199));
#75376=CARTESIAN_POINT('Ctrl Pts',(7.89011744535605,-0.381518591673179,
-10.3718686067204));
#75377=CARTESIAN_POINT('Ctrl Pts',(7.88049719641686,-0.608671182370837,
-10.380742988786));
#75378=CARTESIAN_POINT('Ctrl Pts',(7.86127723444699,-0.835451096446619,
-10.3895279512));
#75379=CARTESIAN_POINT('Ctrl Pts',(7.83225512777433,-1.06107863291402,-10.3982040507345));
#75380=CARTESIAN_POINT('Ctrl Pts',(7.81094174289927,-1.22677599518276,-10.4045756436268));
#75381=CARTESIAN_POINT('Ctrl Pts',(7.78434102672255,-1.3918513235166,-10.4108885245285));
#75382=CARTESIAN_POINT('Ctrl Pts',(7.75235981311111,-1.55598334814017,-10.4171349925863));
#75383=CARTESIAN_POINT('Ctrl Pts',(7.70451147451017,-1.80154765926557,-10.4264805766008));
#75384=CARTESIAN_POINT('Ctrl Pts',(7.6452308641868,-2.0448997890504,-10.4360084011818));
#75385=CARTESIAN_POINT('Ctrl Pts',(7.57434027445688,-2.28476855324992,-10.4456958405266));
#75386=CARTESIAN_POINT('Ctrl Pts',(7.50474964876695,-2.52023869742153,-10.4552056353796));
#75387=CARTESIAN_POINT('Ctrl Pts',(7.42397084966019,-2.75235117083653,-10.4648692447628));
#75388=CARTESIAN_POINT('Ctrl Pts',(7.33188551855802,-2.97990113339148,-10.4746652648976));
#75389=CARTESIAN_POINT('Ctrl Pts',(7.29948621963131,-3.05996230241089,-10.4781118961996));
#75390=CARTESIAN_POINT('Ctrl Pts',(7.26568773232178,-3.13945871307449,-10.481574918808));
#75391=CARTESIAN_POINT('Ctrl Pts',(7.23048643752592,-3.21833813255745,-10.4850534004867));
#75392=CARTESIAN_POINT('Ctrl Pts',(7.12906088671286,-3.44561353862609,-10.4950759556881));
#75393=CARTESIAN_POINT('Ctrl Pts',(7.01598568581979,-3.66776528176092,-10.5052268505375));
#75394=CARTESIAN_POINT('Ctrl Pts',(6.89226962542617,-3.88396812093333,-10.5154837856883));
#75395=CARTESIAN_POINT('Ctrl Pts',(6.76749883839721,-4.10201417183093,-10.5258281651261));
#75396=CARTESIAN_POINT('Ctrl Pts',(6.63190555753522,-4.31400874328372,-10.5362804006405));
#75397=CARTESIAN_POINT('Ctrl Pts',(6.48657142848231,-4.51913125145167,-10.5468176176773));
#75398=CARTESIAN_POINT('Ctrl Pts',(6.34223603393456,-4.72284416004361,-10.5572824230768));
#75399=CARTESIAN_POINT('Ctrl Pts',(6.18829390950642,-4.91977849361174,-10.5678310460277));
#75400=CARTESIAN_POINT('Ctrl Pts',(6.02584082373453,-5.10916593628471,-10.5784410803237));
#75401=CARTESIAN_POINT('Ctrl Pts',(5.89406586055627,-5.2627888925128,-10.5870474842713));
#75402=CARTESIAN_POINT('Ctrl Pts',(5.75669172154331,-5.41144668954126,-10.5956942953936));
#75403=CARTESIAN_POINT('Ctrl Pts',(5.61431617445421,-5.55475095918828,-10.6043695550134));
#75404=CARTESIAN_POINT('Ctrl Pts',(5.47569223833987,-5.69427914592128,-10.6128162206094));
#75405=CARTESIAN_POINT('Ctrl Pts',(5.33197229166852,-5.82857841806889,-10.6210847911245));
#75406=CARTESIAN_POINT('Ctrl Pts',(5.18360943099864,-5.95746876589514,-10.6292311772605));
#75407=CARTESIAN_POINT('Ctrl Pts',(5.03423940440251,-6.08723408988433,-10.6374328653939));
#75408=CARTESIAN_POINT('Ctrl Pts',(4.88016296020318,-6.21151743703355,-10.6455107046126));
#75409=CARTESIAN_POINT('Ctrl Pts',(4.72179101045929,-6.33012248003263,-10.6535217520204));
#75410=CARTESIAN_POINT('Ctrl Pts',(4.56340416495973,-6.44873867849039,-10.6615335529113));
#75411=CARTESIAN_POINT('Ctrl Pts',(4.40072067015659,-6.56167615829608,-10.6694785494265));
#75412=CARTESIAN_POINT('Ctrl Pts',(4.23410475342769,-6.66871629373732,-10.6774138147709));
#75413=CARTESIAN_POINT('Ctrl Pts',(4.17235649871686,-6.7083856223181,-10.6803546429661));
#75414=CARTESIAN_POINT('Ctrl Pts',(4.11006770474765,-6.74724470401329,-10.6832941346227));
#75415=CARTESIAN_POINT('Ctrl Pts',(4.04725542485125,-6.78528135193709,-10.6862351948125));
#75416=CARTESIAN_POINT('Ctrl Pts',(3.87322138080132,-6.89066952875857,-10.6943839930963));
#75417=CARTESIAN_POINT('Ctrl Pts',(3.69478956963306,-6.98942936383284,-10.7022845483943));
#75418=CARTESIAN_POINT('Ctrl Pts',(3.51265993024444,-7.0811466382946,-10.7100277923973));
#75419=CARTESIAN_POINT('Ctrl Pts',(3.33081252195456,-7.17272178615231,-10.7177590373415));
#75420=CARTESIAN_POINT('Ctrl Pts',(3.14527940909275,-7.25727642932643,-10.7253334581573));
#75421=CARTESIAN_POINT('Ctrl Pts',(2.95673955098527,-7.33444696701495,-10.7328415644625));
#75422=CARTESIAN_POINT('Ctrl Pts',(2.76867816089919,-7.41142166476359,-10.7403306170313));
#75423=CARTESIAN_POINT('Ctrl Pts',(2.57762584290098,-7.48105002179702,-10.7477536912425));
#75424=CARTESIAN_POINT('Ctrl Pts',(2.38422941042553,-7.54301532450862,-10.7552006093872));
#75425=CARTESIAN_POINT('Ctrl Pts',(2.19140278922616,-7.60479805648838,-10.7626255863934));
#75426=CARTESIAN_POINT('Ctrl Pts',(1.99624632021674,-7.65896323288816,-10.7700742670356));
#75427=CARTESIAN_POINT('Ctrl Pts',(1.79936640593767,-7.70523528352425,-10.7776356820015));
#75428=CARTESIAN_POINT('Ctrl Pts',(1.60460627738134,-7.75100912776554,-10.7851156839926));
#75429=CARTESIAN_POINT('Ctrl Pts',(1.40815992522824,-7.78905940092469,-10.7927060057787));
#75430=CARTESIAN_POINT('Ctrl Pts',(1.21057462420595,-7.81915007567315,-10.8004928331463));
#75431=CARTESIAN_POINT('Ctrl Pts',(1.01088526486274,-7.84956118182142,-10.8083625813529));
#75432=CARTESIAN_POINT('Ctrl Pts',(0.810032963616668,-7.87184288689846,
-10.8164330425456));
#75433=CARTESIAN_POINT('Ctrl Pts',(0.608610756537882,-7.88639032445356,
-10.8247931852765));
#75434=CARTESIAN_POINT('Ctrl Pts',(0.407892972403965,-7.90088688604542,
-10.8331240905344));
#75435=CARTESIAN_POINT('Ctrl Pts',(0.206609450497189,-7.90770392506711,
-10.8417426546984));
#75436=CARTESIAN_POINT('Ctrl Pts',(0.00529705867780233,-7.9072451045433,
-10.8507369161467));
#75437=CARTESIAN_POINT('Ctrl Pts',(-0.113003396465576,-7.90697548042177,
-10.8560223593993));
#75438=CARTESIAN_POINT('Ctrl Pts',(-0.231314782286878,-7.90419347896038,
-10.8614375414497));
#75439=CARTESIAN_POINT('Ctrl Pts',(-0.349536553218215,-7.8989815428797,
-10.8670003279862));
#75440=CARTESIAN_POINT('Ctrl Pts',(-0.540788865619985,-7.8905499754986,
-10.8759994808505));
#75441=CARTESIAN_POINT('Ctrl Pts',(-0.731567465986668,-7.87453744660504,
-10.8846651200071));
#75442=CARTESIAN_POINT('Ctrl Pts',(-0.92139693904322,-7.8513257245296,-10.8930793448849));
#75443=CARTESIAN_POINT('Ctrl Pts',(-1.11247201025147,-7.82796169481906,
-10.9015487811204));
#75444=CARTESIAN_POINT('Ctrl Pts',(-1.3025857572263,-7.79730408631012,-10.9097634928579));
#75445=CARTESIAN_POINT('Ctrl Pts',(-1.49129994133902,-7.75971678844881,
-10.9178072062819));
#75446=CARTESIAN_POINT('Ctrl Pts',(-1.68173556735899,-7.72178662102513,
-10.9259242940811));
#75447=CARTESIAN_POINT('Ctrl Pts',(-1.87074633383907,-7.67680016762974,
-10.9338672496608));
#75448=CARTESIAN_POINT('Ctrl Pts',(-2.0579242866238,-7.62509942081404,-10.9417221114086));
#75449=CARTESIAN_POINT('Ctrl Pts',(-2.14284665708554,-7.60164286565404,
-10.9452858509909));
#75450=CARTESIAN_POINT('Ctrl Pts',(-2.22739229822822,-7.57680375416926,
-10.9488314571277));
#75451=CARTESIAN_POINT('Ctrl Pts',(-2.31152562517164,-7.55061154929731,
-10.9523669649785));
#75452=CARTESIAN_POINT('Ctrl Pts',(-2.55696593603283,-7.47420160404176,
-10.9626810245491));
#75453=CARTESIAN_POINT('Ctrl Pts',(-2.79914206145313,-7.3859435225859,-10.972782972479));
#75454=CARTESIAN_POINT('Ctrl Pts',(-3.0367805974362,-7.28640306318918,-10.9827537554328));
#75455=CARTESIAN_POINT('Ctrl Pts',(-3.275600080173,-7.18636793662114,-10.9927740882785));
#75456=CARTESIAN_POINT('Ctrl Pts',(-3.50983661854676,-7.07493897548322,
-11.0026619492579));
#75457=CARTESIAN_POINT('Ctrl Pts',(-3.73824915610893,-6.95270094964151,
-11.0124994978384));
#75458=CARTESIAN_POINT('Ctrl Pts',(-3.96695335934609,-6.83030683501107,
-11.0223496082303));
#75459=CARTESIAN_POINT('Ctrl Pts',(-4.18981874858459,-6.69707695425021,
-11.0321492776509));
#75460=CARTESIAN_POINT('Ctrl Pts',(-4.4056514551113,-6.55359470301871,-11.0419809807038));
#75461=CARTESIAN_POINT('Ctrl Pts',(-4.62095932884421,-6.41046135252605,
-11.0517887763506));
#75462=CARTESIAN_POINT('Ctrl Pts',(-4.82926896525815,-6.25712627609679,
-11.061628450029));
#75463=CARTESIAN_POINT('Ctrl Pts',(-5.02944413836427,-6.09415180425817,
-11.0715818761527));
#75464=CARTESIAN_POINT('Ctrl Pts',(-5.22851875964976,-5.9320733568811,-11.0814805789007));
#75465=CARTESIAN_POINT('Ctrl Pts',(-5.41954859559745,-5.7604619565193,-11.0914917867233));
#75466=CARTESIAN_POINT('Ctrl Pts',(-5.60145879168493,-5.57984225057532,
-11.1016960310228));
#75467=CARTESIAN_POINT('Ctrl Pts',(-5.70701224620803,-5.47503760340664,
-11.1076170473252));
#75468=CARTESIAN_POINT('Ctrl Pts',(-5.80949597148569,-5.36719935489417,
-11.1136030571689));
#75469=CARTESIAN_POINT('Ctrl Pts',(-5.90870552764936,-5.25642413723177,
-11.1196697935519));
#75470=CARTESIAN_POINT('Ctrl Pts',(-6.07735119198448,-5.06811808187836,
-11.1299825983585));
#75471=CARTESIAN_POINT('Ctrl Pts',(-6.23653446489338,-4.87132781030842,
-11.1405286735911));
#75472=CARTESIAN_POINT('Ctrl Pts',(-6.38605251344742,-4.66719413220943,
-11.1513853009217));
#75473=CARTESIAN_POINT('Ctrl Pts',(-6.47850529064013,-4.54097040442988,
-11.1580983724029));
#75474=CARTESIAN_POINT('Ctrl Pts',(-6.56726317871131,-4.41193812238904,
-11.1649301811789));
#75475=CARTESIAN_POINT('Ctrl Pts',(-6.65228203278622,-4.28035772740498,
-11.1718989979642));
#75476=CARTESIAN_POINT('Ctrl Pts',(-6.73767850690118,-4.14819290447768,
-11.1788987674706));
#75477=CARTESIAN_POINT('Ctrl Pts',(-6.81906013954894,-4.01346262579741,
-11.1859143334325));
#75478=CARTESIAN_POINT('Ctrl Pts',(-6.8961809960879,-3.87630285641968,-11.1928178386192));
#75479=CARTESIAN_POINT('Ctrl Pts',(-6.97324733895214,-3.73924003984289,
-11.1997164639919));
#75480=CARTESIAN_POINT('Ctrl Pts',(-7.04605848385439,-3.59975082466254,
-11.2065031869559));
#75481=CARTESIAN_POINT('Ctrl Pts',(-7.11433735457903,-3.4580120805359,-11.2130504212207));
#75482=CARTESIAN_POINT('Ctrl Pts',(-7.12997611780663,-3.42554788427653,
-11.2145500161228));
#75483=CARTESIAN_POINT('Ctrl Pts',(-7.14537700041407,-3.39296585919192,
-11.216037047336));
#75484=CARTESIAN_POINT('Ctrl Pts',(-7.16053647716106,-3.36026846246956,
-11.2175099818246));
#75485=CARTESIAN_POINT('Ctrl Pts',(-7.26445657857949,-3.13612373503488,
-11.2276071312184));
#75486=CARTESIAN_POINT('Ctrl Pts',(-7.35790650102895,-2.90725336245844,
-11.2376559047231));
#75487=CARTESIAN_POINT('Ctrl Pts',(-7.44069004122439,-2.67462442953598,
-11.2476688324051));
#75488=CARTESIAN_POINT('Ctrl Pts',(-7.52496909473305,-2.43779297440435,
-11.2578626470922));
#75489=CARTESIAN_POINT('Ctrl Pts',(-7.5981933250589,-2.1970652754948,-11.2680193091238));
#75490=CARTESIAN_POINT('Ctrl Pts',(-7.6601147676513,-1.95342728081224,-11.278152039988));
#75491=CARTESIAN_POINT('Ctrl Pts',(-7.67375050021579,-1.89977571200254,
-11.2803833705648));
#75492=CARTESIAN_POINT('Ctrl Pts',(-7.68683796295885,-1.84598290739436,
-11.2826135406588));
#75493=CARTESIAN_POINT('Ctrl Pts',(-7.69937421557069,-1.79205922674744,
-11.2848426914563));
#75494=CARTESIAN_POINT('Ctrl Pts',(-7.75656683562454,-1.54604977921671,
-11.2950124749275));
#75495=CARTESIAN_POINT('Ctrl Pts',(-7.80229081606649,-1.2973175900563,-11.3051610433009));
#75496=CARTESIAN_POINT('Ctrl Pts',(-7.83639807134673,-1.04695990943283,
-11.3153018028891));
#75497=CARTESIAN_POINT('Ctrl Pts',(-7.87018914773473,-0.798923078536818,
-11.3253485562575));
#75498=CARTESIAN_POINT('Ctrl Pts',(-7.89257801450306,-0.549289861374268,
-11.3353876449467));
#75499=CARTESIAN_POINT('Ctrl Pts',(-7.90337060055902,-0.299119670074988,
-11.3454321058796));
#75500=CARTESIAN_POINT('Ctrl Pts',(-7.90766935757047,-0.19947526063231,
-11.3494328798033));
#75501=CARTESIAN_POINT('Ctrl Pts',(-7.91012781524847,-0.0997456492172265,
-11.3534345060231));
#75502=CARTESIAN_POINT('Ctrl Pts',(-7.91073139072936,2.07722496012377E-6,
-11.3574378083492));
#75503=CARTESIAN_POINT('',(-7.91701821474139,0.000346299696071325,-13.3576683701812));
#75504=CARTESIAN_POINT('Ctrl Pts',(-7.9107641172329,0.0057498417356433,
-11.357668491763));
#75505=CARTESIAN_POINT('Ctrl Pts',(-7.91457765203306,0.720360372816585,
-11.3863491342362));
#75506=CARTESIAN_POINT('Ctrl Pts',(-7.48577816839556,4.0661084013071,-11.5208723106634));
#75507=CARTESIAN_POINT('Ctrl Pts',(-3.83963961366753,7.83245821801285,-11.7083167540687));
#75508=CARTESIAN_POINT('Ctrl Pts',(1.61179695439645,8.07554689442854,-11.9200018219771));
#75509=CARTESIAN_POINT('Ctrl Pts',(5.28078975215679,6.34161180548053,-12.0787656229088));
#75510=CARTESIAN_POINT('Ctrl Pts',(7.65342116652072,3.0393371559865,-12.2375294238402));
#75511=CARTESIAN_POINT('Ctrl Pts',(8.39493817415805,-2.35203089183565,-12.449214491749));
#75512=CARTESIAN_POINT('Ctrl Pts',(4.10002393395763,-8.40746607421705,-12.7138208266349));
#75513=CARTESIAN_POINT('Ctrl Pts',(-4.86854992279596,-7.99517047053262,
-13.0313484284978));
#75514=CARTESIAN_POINT('Ctrl Pts',(-7.87876404316446,-2.76416089730763,
-13.2459642558688));
#75515=CARTESIAN_POINT('Ctrl Pts',(-7.92001450609604,-0.0721905216786065,
-13.3547375492854));
#75516=CARTESIAN_POINT('Ctrl Pts',(-7.9200591301389,0.000344913405787141,
-13.3576683087477));
#75517=CARTESIAN_POINT('',(-7.90609173527438,-0.00664493357794552,-15.3576684795722));
#75518=CARTESIAN_POINT('Ctrl Pts',(-7.91099999229989,0.000349043278910089,
-13.357668491763));
#75519=CARTESIAN_POINT('Ctrl Pts',(-7.91099075434638,0.20972551476333,-13.3661379354309));
#75520=CARTESIAN_POINT('Ctrl Pts',(-7.90266499763303,0.41926599422585,-13.3746073790987));
#75521=CARTESIAN_POINT('Ctrl Pts',(-7.88600956288663,0.628310571342361,
-13.3830768227666));
#75522=CARTESIAN_POINT('Ctrl Pts',(-7.8693785523935,0.837048596407084,-13.3915338464742));
#75523=CARTESIAN_POINT('Ctrl Pts',(-7.84444225460933,1.04529190279781,-13.3999908701819));
#75524=CARTESIAN_POINT('Ctrl Pts',(-7.81123946961377,1.25238131108219,-13.4084478938895));
#75525=CARTESIAN_POINT('Ctrl Pts',(-7.77810937884916,1.45901731748252,-13.4168864017758));
#75526=CARTESIAN_POINT('Ctrl Pts',(-7.73674896429563,1.66450420300881,-13.4253249096621));
#75527=CARTESIAN_POINT('Ctrl Pts',(-7.68724859145397,1.8681889875462,-13.4337634175484));
#75528=CARTESIAN_POINT('Ctrl Pts',(-7.63781407341306,2.07160279188426,-13.4421906989283));
#75529=CARTESIAN_POINT('Ctrl Pts',(-7.58026126041488,2.2732190173356,-13.4506179803081));
#75530=CARTESIAN_POINT('Ctrl Pts',(-7.5147317215566,2.47239320356429,-13.459045261688));
#75531=CARTESIAN_POINT('Ctrl Pts',(-7.44933605342673,2.67116049553043,-13.467455326919));
#75532=CARTESIAN_POINT('Ctrl Pts',(-7.37599626340356,2.86749544967156,-13.4758653921499));
#75533=CARTESIAN_POINT('Ctrl Pts',(-7.29490394662192,3.06076745434213,-13.4842754573809));
#75534=CARTESIAN_POINT('Ctrl Pts',(-7.21980856354628,3.23974662036612,-13.492063582018));
#75535=CARTESIAN_POINT('Ctrl Pts',(-7.13806543391911,3.41609904358483,-13.4998517066552));
#75536=CARTESIAN_POINT('Ctrl Pts',(-7.04986516082454,3.58933450853949,-13.5076398312923));
#75537=CARTESIAN_POINT('Ctrl Pts',(-6.96044519053985,3.7649655988411,-13.5155356557517));
#75538=CARTESIAN_POINT('Ctrl Pts',(-6.86446279964864,3.93724411927462,-13.5234314802112));
#75539=CARTESIAN_POINT('Ctrl Pts',(-6.7622093011055,4.10566028405204,-13.5313273046706));
#75540=CARTESIAN_POINT('Ctrl Pts',(-6.65993276105922,4.27411439923354,-13.5392249083519));
#75541=CARTESIAN_POINT('Ctrl Pts',(-6.55138247468514,4.43870413154281,-13.5471225120332));
#75542=CARTESIAN_POINT('Ctrl Pts',(-6.43689370421093,4.59894775363775,-13.5550201157145));
#75543=CARTESIAN_POINT('Ctrl Pts',(-6.32236027950089,4.75925387580551,-13.5629207997106));
#75544=CARTESIAN_POINT('Ctrl Pts',(-6.20188395362811,4.91521023122139,-13.5708214837068));
#75545=CARTESIAN_POINT('Ctrl Pts',(-6.07584113021107,5.06636709688861,-13.5787221677029));
#75546=CARTESIAN_POINT('Ctrl Pts',(-5.94965993959841,5.2176898994258,-13.586631524906));
#75547=CARTESIAN_POINT('Ctrl Pts',(-5.81790026256002,5.36420242302357,-13.594540882109));
#75548=CARTESIAN_POINT('Ctrl Pts',(-5.68097715809304,5.5054899445213,-13.6024502393121));
#75549=CARTESIAN_POINT('Ctrl Pts',(-5.5439725304119,5.64686158778152,-13.6103643057));
#75550=CARTESIAN_POINT('Ctrl Pts',(-5.40179859206367,5.78300178958583,-13.618278372088));
#75551=CARTESIAN_POINT('Ctrl Pts',(-5.2549047719409,5.91353505424908,-13.626192438476));
#75552=CARTESIAN_POINT('Ctrl Pts',(-5.10780592246906,6.04425051276001,-13.6341175510461));
#75553=CARTESIAN_POINT('Ctrl Pts',(-4.95597429147119,6.16934317932718,-13.6420426636161));
#75554=CARTESIAN_POINT('Ctrl Pts',(-4.79989076011748,6.28847912383741,-13.6499677761862));
#75555=CARTESIAN_POINT('Ctrl Pts',(-4.69199044414871,6.37083762729002,-13.6554463948654));
#75556=CARTESIAN_POINT('Ctrl Pts',(-4.58205879117334,6.45035035206467,-13.6609250135446));
#75557=CARTESIAN_POINT('Ctrl Pts',(-4.47026179466765,6.52691967831187,-13.6664036322239));
#75558=CARTESIAN_POINT('Ctrl Pts',(-4.30446367426373,6.64047416339802,-13.674528579296));
#75559=CARTESIAN_POINT('Ctrl Pts',(-4.13419830883315,6.74780213904776,-13.6826535263681));
#75560=CARTESIAN_POINT('Ctrl Pts',(-3.95996164627996,6.84854909889618,-13.6907784734402));
#75561=CARTESIAN_POINT('Ctrl Pts',(-3.78587853744792,6.94920727105576,-13.6988962600454));
#75562=CARTESIAN_POINT('Ctrl Pts',(-3.6078313856262,7.04329583102843,-13.7070140466506));
#75563=CARTESIAN_POINT('Ctrl Pts',(-3.42634505531038,7.13050352793897,-13.7151318332557));
#75564=CARTESIAN_POINT('Ctrl Pts',(-3.24499285480648,7.21764677287693,-13.7232436203061));
#75565=CARTESIAN_POINT('Ctrl Pts',(-3.06020683191874,7.29791915628924,-13.7313554073564));
#75566=CARTESIAN_POINT('Ctrl Pts',(-2.87253689653869,7.37105506545867,-13.7394671944068));
#75567=CARTESIAN_POINT('Ctrl Pts',(-2.68497900404071,7.44414731095852,-13.7475741385504));
#75568=CARTESIAN_POINT('Ctrl Pts',(-2.49454093047948,7.51011146233047,-13.755681082694));
#75569=CARTESIAN_POINT('Ctrl Pts',(-2.30179356405779,7.56872957559339,-13.7637880268376));
#75570=CARTESIAN_POINT('Ctrl Pts',(-2.1091339234749,7.62732100977244,-13.771891281237));
#75571=CARTESIAN_POINT('Ctrl Pts',(-1.91416739244046,7.67857298073169,-13.7799945356364));
#75572=CARTESIAN_POINT('Ctrl Pts',(-1.71748160661575,7.72231687584345,-13.7880977900358));
#75573=CARTESIAN_POINT('Ctrl Pts',(-1.51942509676862,7.76636562678205,-13.7962575168712));
#75574=CARTESIAN_POINT('Ctrl Pts',(-1.31962558725591,7.80280114233388,-13.8044172437067));
#75575=CARTESIAN_POINT('Ctrl Pts',(-1.11869634644107,7.83150301567071,-13.8125769705422));
#75576=CARTESIAN_POINT('Ctrl Pts',(-0.919233156929076,7.85999546991737,
-13.8206771611045));
#75577=CARTESIAN_POINT('Ctrl Pts',(-0.718656991572907,7.88086673495674,
-13.8287773516669));
#75578=CARTESIAN_POINT('Ctrl Pts',(-0.517576039129384,7.89405067400249,
-13.8368775422292));
#75579=CARTESIAN_POINT('Ctrl Pts',(-0.316496285765364,7.90723453443019,
-13.8449776844888));
#75580=CARTESIAN_POINT('Ctrl Pts',(-0.11491207127654,7.91273113943406,-13.8530778267483));
#75581=CARTESIAN_POINT('Ctrl Pts',(0.086564994665258,7.91052637323829,-13.8611779690079));
#75582=CARTESIAN_POINT('Ctrl Pts',(0.28806684418487,7.90832133583551,-13.8692791076613));
#75583=CARTESIAN_POINT('Ctrl Pts',(0.489461198268721,7.89841304197515,-13.8773802463147));
#75584=CARTESIAN_POINT('Ctrl Pts',(0.690137595971672,7.88083949199744,-13.885481384968));
#75585=CARTESIAN_POINT('Ctrl Pts',(0.893365828455263,7.86304247380639,-13.8936855390613));
#75586=CARTESIAN_POINT('Ctrl Pts',(1.0958573836457,7.83738394580421,-13.9018896931545));
#75587=CARTESIAN_POINT('Ctrl Pts',(1.29698467679072,7.80395744146328,-13.9100938472478));
#75588=CARTESIAN_POINT('Ctrl Pts',(1.49577570822341,7.77091921392481,-13.9182027032301));
#75589=CARTESIAN_POINT('Ctrl Pts',(1.6932336908906,7.73029260087103,-13.9263115592124));
#75590=CARTESIAN_POINT('Ctrl Pts',(1.88876369041668,7.68221925759501,-13.9344204151948));
#75591=CARTESIAN_POINT('Ctrl Pts',(2.0877405953304,7.63329845220912,-13.9426722183435));
#75592=CARTESIAN_POINT('Ctrl Pts',(2.28472057268627,7.57666601142176,-13.9509240214922));
#75593=CARTESIAN_POINT('Ctrl Pts',(2.4790932858785,7.5125240418858,-13.9591758246409));
#75594=CARTESIAN_POINT('Ctrl Pts',(2.67346599907072,7.44838207234984,-13.9674276277896));
#75595=CARTESIAN_POINT('Ctrl Pts',(2.86523113133767,7.37673072038818,-13.9756794309383));
#75596=CARTESIAN_POINT('Ctrl Pts',(3.05379994502888,7.29782343550059,-13.983931234087));
#75597=CARTESIAN_POINT('Ctrl Pts',(3.23272021792076,7.22295361652636,-13.9917608154601));
#75598=CARTESIAN_POINT('Ctrl Pts',(3.40910472212366,7.14140820148784,-13.9995903968331));
#75599=CARTESIAN_POINT('Ctrl Pts',(3.582415844458,7.05338342339166,-14.0074199782062));
#75600=CARTESIAN_POINT('Ctrl Pts',(3.75558086419229,6.96543285085584,-14.0152429591823));
#75601=CARTESIAN_POINT('Ctrl Pts',(3.92567734919365,6.87101394949806,-14.0230659401585));
#75602=CARTESIAN_POINT('Ctrl Pts',(4.09218683031946,6.77037132997592,-14.0308889211346));
#75603=CARTESIAN_POINT('Ctrl Pts',(4.25858531953984,6.66979579682047,-14.0387066874674));
#75604=CARTESIAN_POINT('Ctrl Pts',(4.42140126671791,6.56300498893785,-14.0465244538002));
#75605=CARTESIAN_POINT('Ctrl Pts',(4.58013989159596,6.45028988289761,-14.0543422201329));
#75606=CARTESIAN_POINT('Ctrl Pts',(4.73880243453417,6.33762880015463,-14.0621562394833));
#75607=CARTESIAN_POINT('Ctrl Pts',(4.8933912614168,6.21904927851853,-14.0699702588337));
#75608=CARTESIAN_POINT('Ctrl Pts',(5.04343959259385,6.09488622337258,-14.0777842781841));
#75609=CARTESIAN_POINT('Ctrl Pts',(5.19344422153273,5.97075933126398,-14.0855960216669));
#75610=CARTESIAN_POINT('Ctrl Pts',(5.33891071871571,5.84105237002629,-14.0934077651497));
#75611=CARTESIAN_POINT('Ctrl Pts',(5.47940435891093,5.7061413294404,-14.1012195086325));
#75612=CARTESIAN_POINT('Ctrl Pts',(5.61990585709268,5.57122274310982,-14.109031689036));
#75613=CARTESIAN_POINT('Ctrl Pts',(5.75543368421152,5.43109973513091,-14.1168438694394));
#75614=CARTESIAN_POINT('Ctrl Pts',(5.88558874019122,5.28618635514625,-14.1246560498429));
#75615=CARTESIAN_POINT('Ctrl Pts',(5.98576841705805,5.17464727223264,-14.1306690449014));
#75616=CARTESIAN_POINT('Ctrl Pts',(6.08276579425345,5.06027103084489,-14.1366820399599));
#75617=CARTESIAN_POINT('Ctrl Pts',(6.1764146710011,4.94326034230875,-14.1426950350184));
#75618=CARTESIAN_POINT('Ctrl Pts',(6.31097163630591,4.77513656224381,-14.1513346513765));
#75619=CARTESIAN_POINT('Ctrl Pts',(6.43855081732628,4.60165334075478,-14.1599742677346));
#75620=CARTESIAN_POINT('Ctrl Pts',(6.558772299389,4.4233954067851,-14.1686138840926));
#75621=CARTESIAN_POINT('Ctrl Pts',(6.67919284757172,4.24484230830184,-14.1772678061711));
#75622=CARTESIAN_POINT('Ctrl Pts',(6.79223121574276,4.06149888478754,-14.1859217282496));
#75623=CARTESIAN_POINT('Ctrl Pts',(6.89755215429033,3.87397667505173,-14.194575650328));
#75624=CARTESIAN_POINT('Ctrl Pts',(7.00595230436682,3.68097197951481,-14.2034825824632));
#75625=CARTESIAN_POINT('Ctrl Pts',(7.10617684071803,3.48354071662988,-14.2123895145984));
#75626=CARTESIAN_POINT('Ctrl Pts',(7.19791305150503,3.28237241990813,-14.2212964467335));
#75627=CARTESIAN_POINT('Ctrl Pts',(7.28734088338441,3.08626616628856,-14.2299792517318));
#75628=CARTESIAN_POINT('Ctrl Pts',(7.36870235703809,2.88660889449176,-14.2386620567301));
#75629=CARTESIAN_POINT('Ctrl Pts',(7.44175776740229,2.6840570655833,-14.2473448617284));
#75630=CARTESIAN_POINT('Ctrl Pts',(7.51764182011688,2.4736626049171,-14.256363857432));
#75631=CARTESIAN_POINT('Ctrl Pts',(7.58456374204374,2.26014525684741,-14.2653828531356));
#75632=CARTESIAN_POINT('Ctrl Pts',(7.64231217849465,2.04425672713394,-14.2744018488392));
#75633=CARTESIAN_POINT('Ctrl Pts',(7.70006061494556,1.82836819742046,-14.2834208445428));
#75634=CARTESIAN_POINT('Ctrl Pts',(7.74863552531833,1.61010875937359,-14.2924398402464));
#75635=CARTESIAN_POINT('Ctrl Pts',(7.78788463880215,1.39024237193,-14.30145883595));
#75636=CARTESIAN_POINT('Ctrl Pts',(7.82410083849344,1.18736581533357,-14.3097809028816));
#75637=CARTESIAN_POINT('Ctrl Pts',(7.8524074670251,0.982949090818679,-14.3181029698132));
#75638=CARTESIAN_POINT('Ctrl Pts',(7.87268864814392,0.777621019125552,-14.3264250367447));
#75639=CARTESIAN_POINT('Ctrl Pts',(7.89295183701053,0.572475102230492,-14.3347397208357));
#75640=CARTESIAN_POINT('Ctrl Pts',(7.90520375286211,0.366419740936222,-14.3430544049267));
#75641=CARTESIAN_POINT('Ctrl Pts',(7.90937998358545,0.160091459040854,-14.3513690890177));
#75642=CARTESIAN_POINT('Ctrl Pts',(7.91355276382944,-0.046066350597841,
-14.3596769033623));
#75643=CARTESIAN_POINT('Ctrl Pts',(7.90966316409722,-0.252496339491838,
-14.3679847177069));
#75644=CARTESIAN_POINT('Ctrl Pts',(7.89769872063863,-0.458558521917263,
-14.3762925320516));
#75645=CARTESIAN_POINT('Ctrl Pts',(7.88574630764296,-0.664413505115063,
-14.3845919927396));
#75646=CARTESIAN_POINT('Ctrl Pts',(7.86573527478703,-0.869901128927133,
-14.3928914534276));
#75647=CARTESIAN_POINT('Ctrl Pts',(7.83770520431504,-1.07438267402863,-14.4011909141156));
#75648=CARTESIAN_POINT('Ctrl Pts',(7.8096929899418,-1.2787339575004,-14.4094850877677));
#75649=CARTESIAN_POINT('Ctrl Pts',(7.77367196712769,-1.48208015174069,-14.4177792614198));
#75650=CARTESIAN_POINT('Ctrl Pts',(7.72973354910974,-1.68378747464379,-14.4260734350718));
#75651=CARTESIAN_POINT('Ctrl Pts',(7.68582757825155,-1.88534584294121,-14.4343614837338));
#75652=CARTESIAN_POINT('Ctrl Pts',(7.63401594334801,-2.08526747025648,-14.4426495323957));
#75653=CARTESIAN_POINT('Ctrl Pts',(7.57444126841368,-2.28292804778246,-14.4509375810576));
#75654=CARTESIAN_POINT('Ctrl Pts',(7.5521942070119,-2.35674073765073,-14.4540325996656));
#75655=CARTESIAN_POINT('Ctrl Pts',(7.52886509214598,-2.43023822453188,-14.4571276182735));
#75656=CARTESIAN_POINT('Ctrl Pts',(7.50446316936996,-2.50338841164726,-14.4602226368814));
#75657=CARTESIAN_POINT('Ctrl Pts',(7.44057615319467,-2.69490394222084,-14.4683257484961));
#75658=CARTESIAN_POINT('Ctrl Pts',(7.36935875614377,-2.88395744816265,-14.4764288601108));
#75659=CARTESIAN_POINT('Ctrl Pts',(7.29103315278047,-3.06997663917107,-14.4845319717255));
#75660=CARTESIAN_POINT('Ctrl Pts',(7.2126902665228,-3.25603687614518,-14.492636871328));
#75661=CARTESIAN_POINT('Ctrl Pts',(7.12723616953897,-3.43906116901714,-14.5007417709305));
#75662=CARTESIAN_POINT('Ctrl Pts',(7.03494071915571,-3.61849831808237,-14.5088466705329));
#75663=CARTESIAN_POINT('Ctrl Pts',(6.94261334424597,-3.79799753354408,-14.5169543735789));
#75664=CARTESIAN_POINT('Ctrl Pts',(6.84344004211401,-3.97390684716521,-14.5250620766249));
#75665=CARTESIAN_POINT('Ctrl Pts',(6.73773631810158,-4.14570021923137,-14.5331697796709));
#75666=CARTESIAN_POINT('Ctrl Pts',(6.63193750652792,-4.31764813091226,-14.5412847761374));
#75667=CARTESIAN_POINT('Ctrl Pts',(6.51959670117142,-4.48547243041464,-14.549399772604));
#75668=CARTESIAN_POINT('Ctrl Pts',(6.40107313684719,-4.64867547767462,-14.5575147690705));
#75669=CARTESIAN_POINT('Ctrl Pts',(6.28249170862118,-4.81195820162294,-14.565633727326));
#75670=CARTESIAN_POINT('Ctrl Pts',(6.15772169320428,-4.9706149192871,-14.5737526855816));
#75671=CARTESIAN_POINT('Ctrl Pts',(6.02716279811976,-5.12418087160877,-14.5818716438371));
#75672=CARTESIAN_POINT('Ctrl Pts',(5.89646408747138,-5.27791127775948,-14.5899992966878));
#75673=CARTESIAN_POINT('Ctrl Pts',(5.75996432141575,-5.42653978663855,-14.5981269495384));
#75674=CARTESIAN_POINT('Ctrl Pts',(5.6181012176356,-5.56963730492403,-14.6062546023891));
#75675=CARTESIAN_POINT('Ctrl Pts',(5.54402580606425,-5.64435727988145,-14.6104985475304));
#75676=CARTESIAN_POINT('Ctrl Pts',(5.468488653673,-5.71756985211167,-14.6147424926717));
#75677=CARTESIAN_POINT('Ctrl Pts',(5.39155571906165,-5.7892182484558,-14.618986437813));
#75678=CARTESIAN_POINT('Ctrl Pts',(5.24655695785499,-5.92425701650521,-14.62698518102));
#75679=CARTESIAN_POINT('Ctrl Pts',(5.09634720996129,-6.05397053172142,-14.6349839242271));
#75680=CARTESIAN_POINT('Ctrl Pts',(4.94135049965329,-6.17794271902679,-14.6429826674341));
#75681=CARTESIAN_POINT('Ctrl Pts',(4.78648003360986,-6.3018139314303,-14.6509748956935));
#75682=CARTESIAN_POINT('Ctrl Pts',(4.62683063523018,-6.41995292735989,-14.6589671239529));
#75683=CARTESIAN_POINT('Ctrl Pts',(4.46286163144894,-6.53198186299847,-14.6669593522123));
#75684=CARTESIAN_POINT('Ctrl Pts',(4.29899840672196,-6.64393852696015,-14.674946424556));
#75685=CARTESIAN_POINT('Ctrl Pts',(4.13082140589961,-6.74979279877053,-14.6829334968998));
#75686=CARTESIAN_POINT('Ctrl Pts',(3.95882167681481,-6.8492081243879,-14.6909205692436));
#75687=CARTESIAN_POINT('Ctrl Pts',(3.78690378681533,-6.94857614726033,-14.6989038412634));
#75688=CARTESIAN_POINT('Ctrl Pts',(3.61116708319462,-7.04151116391887,-14.7068871132832));
#75689=CARTESIAN_POINT('Ctrl Pts',(3.43213048645932,-7.12772062611299,-14.714870385303));
#75690=CARTESIAN_POINT('Ctrl Pts',(3.25314877500478,-7.21390366002025,-14.7228512099789));
#75691=CARTESIAN_POINT('Ctrl Pts',(3.07086948823391,-7.29336510497759,-14.7308320346547));
#75692=CARTESIAN_POINT('Ctrl Pts',(2.88583533747721,-7.36585876900771,-14.7388128593306));
#75693=CARTESIAN_POINT('Ctrl Pts',(2.69484906990006,-7.4406843850331,-14.7470504085117));
#75694=CARTESIAN_POINT('Ctrl Pts',(2.50092808359502,-7.50808631240983,-14.7552879576927));
#75695=CARTESIAN_POINT('Ctrl Pts',(2.30469117493277,-7.56784775138791,-14.7635255068738));
#75696=CARTESIAN_POINT('Ctrl Pts',(2.11454406535485,-7.62575461999568,-14.7715074210686));
#75697=CARTESIAN_POINT('Ctrl Pts',(1.92222296018322,-7.67648802646134,-14.7794893352633));
#75698=CARTESIAN_POINT('Ctrl Pts',(1.72830597348213,-7.71990151893313,-14.787471249458));
#75699=CARTESIAN_POINT('Ctrl Pts',(1.53434587363534,-7.76332466343313,-14.7954549382546));
#75700=CARTESIAN_POINT('Ctrl Pts',(1.33878951142208,-7.79942457607385,-14.8034386270511));
#75701=CARTESIAN_POINT('Ctrl Pts',(1.1422253876637,-7.82810591163511,-14.8114223158476));
#75702=CARTESIAN_POINT('Ctrl Pts',(0.945587380888185,-7.85679802771708,
-14.8194090054919));
#75703=CARTESIAN_POINT('Ctrl Pts',(0.747941188373335,-7.87806595933183,
-14.8273956951363));
#75704=CARTESIAN_POINT('Ctrl Pts',(0.549881009058251,-7.89186618461547,
-14.8353823847806));
#75705=CARTESIAN_POINT('Ctrl Pts',(0.351715968011602,-7.90567371634266,
-14.8433733029281));
#75706=CARTESIAN_POINT('Ctrl Pts',(0.153136836514974,-7.91200563622896,
-14.8513642210756));
#75707=CARTESIAN_POINT('Ctrl Pts',(-0.0452612227829571,-7.91087052237061,
-14.8593551392232));
#75708=CARTESIAN_POINT('Ctrl Pts',(-0.243893599454,-7.90973406788978,-14.8673554950182));
#75709=CARTESIAN_POINT('Ctrl Pts',(-0.442344142214344,-7.90111296470408,
-14.8753558508133));
#75710=CARTESIAN_POINT('Ctrl Pts',(-0.640020581781527,-7.88506782817346,
-14.8833562066083));
#75711=CARTESIAN_POINT('Ctrl Pts',(-0.837835164343456,-7.86901147875769,
-14.8913621533231));
#75712=CARTESIAN_POINT('Ctrl Pts',(-1.03487423365295,-7.84552078800775,
-14.8993681000379));
#75713=CARTESIAN_POINT('Ctrl Pts',(-1.23055425625879,-7.81470775028749,
-14.9073740467526));
#75714=CARTESIAN_POINT('Ctrl Pts',(-1.42648816563034,-7.78385473392054,
-14.9153903808534));
#75715=CARTESIAN_POINT('Ctrl Pts',(-1.62105917916205,-7.74566045817603,
-14.9234067149541));
#75716=CARTESIAN_POINT('Ctrl Pts',(-1.81369636153397,-7.70028743023002,
-14.9314230490548));
#75717=CARTESIAN_POINT('Ctrl Pts',(-1.85447618584592,-7.69068230579165,
-14.9331200459286));
#75718=CARTESIAN_POINT('Ctrl Pts',(-1.89516941090222,-7.68075565024744,
-14.9348170428024));
#75719=CARTESIAN_POINT('Ctrl Pts',(-1.93577072653057,-7.67050928519791,
-14.9365140396761));
#75720=CARTESIAN_POINT('Ctrl Pts',(-2.12148695064299,-7.62364094612004,
-14.9442763460656));
#75721=CARTESIAN_POINT('Ctrl Pts',(-2.30582851698515,-7.56994078708024,
-14.9520386524551));
#75722=CARTESIAN_POINT('Ctrl Pts',(-2.48824141034103,-7.50949903015268,
-14.9598009588446));
#75723=CARTESIAN_POINT('Ctrl Pts',(-2.67043333221745,-7.4491304912099,-14.9675538621251));
#75724=CARTESIAN_POINT('Ctrl Pts',(-2.85070089537913,-7.38203672085767,
-14.9753067654055));
#75725=CARTESIAN_POINT('Ctrl Pts',(-3.02849949459476,-7.30835903683168,
-14.983059668686));
#75726=CARTESIAN_POINT('Ctrl Pts',(-3.20611877614155,-7.23475565997461,
-14.9908047528242));
#75727=CARTESIAN_POINT('Ctrl Pts',(-3.38127372221828,-7.15458172401382,
-14.9985498369623));
#75728=CARTESIAN_POINT('Ctrl Pts',(-3.55343404572194,-7.06802854286146,
-15.0062949211005));
#75729=CARTESIAN_POINT('Ctrl Pts',(-3.72545560752278,-6.98154512381546,
-15.0140337626792));
#75730=CARTESIAN_POINT('Ctrl Pts',(-3.89448703355623,-6.88869285669213,
-15.0217726042579));
#75731=CARTESIAN_POINT('Ctrl Pts',(-4.06001713331067,-6.78971147231042,
-15.0295114458366));
#75732=CARTESIAN_POINT('Ctrl Pts',(-4.22544730722923,-6.69078984018879,
-15.0372456156957));
#75733=CARTESIAN_POINT('Ctrl Pts',(-4.38738005675412,-6.58574664200628,
-15.0449797855547));
#75734=CARTESIAN_POINT('Ctrl Pts',(-4.54532788920346,-6.4748679816371,-15.0527139554138));
#75735=CARTESIAN_POINT('Ctrl Pts',(-4.7032123081869,-6.36403383723271,-15.0604450201304));
#75736=CARTESIAN_POINT('Ctrl Pts',(-4.85711470327773,-6.2473691027134,-15.0681760848471));
#75737=CARTESIAN_POINT('Ctrl Pts',(-5.00657565793525,-6.12520376651832,
-15.0759071495637));
#75738=CARTESIAN_POINT('Ctrl Pts',(-5.15603444218046,-6.00304020435947,
-15.0836381020129));
#75739=CARTESIAN_POINT('Ctrl Pts',(-5.30105162963631,-5.87537641817403,
-15.0913690544621));
#75740=CARTESIAN_POINT('Ctrl Pts',(-5.44119975803647,-5.74258358172903,
-15.0991000069113));
#75741=CARTESIAN_POINT('Ctrl Pts',(-5.58135376516648,-5.60978517508329,
-15.1068312836473));
#75742=CARTESIAN_POINT('Ctrl Pts',(-5.71663804510143,-5.47185753609265,
-15.1145625603832));
#75743=CARTESIAN_POINT('Ctrl Pts',(-5.84666111061152,-5.32920959032977,
-15.1222938371192));
#75744=CARTESIAN_POINT('Ctrl Pts',(-5.97671343882886,-5.18652954053167,
-15.1300268538394));
#75745=CARTESIAN_POINT('Ctrl Pts',(-6.1015019526909,-5.03912733376445,-15.1377598705596));
#75746=CARTESIAN_POINT('Ctrl Pts',(-6.22067463421474,-4.88744596852358,
-15.1454928872798));
#75747=CARTESIAN_POINT('Ctrl Pts',(-6.33989596504546,-4.73570268310777,
-15.1532290608133));
#75748=CARTESIAN_POINT('Ctrl Pts',(-6.45349667690804,-4.57967704279862,
-15.1609652343468));
#75749=CARTESIAN_POINT('Ctrl Pts',(-6.56116732938121,-4.41984210983387,
-15.1687014078803));
#75750=CARTESIAN_POINT('Ctrl Pts',(-6.66896449115314,-4.25981937634201,
-15.1764466711506));
#75751=CARTESIAN_POINT('Ctrl Pts',(-6.77081747789992,-4.09597870938968,
-15.1841919344208));
#75752=CARTESIAN_POINT('Ctrl Pts',(-6.86646166892844,-3.92881981632353,
-15.1919371976911));
#75753=CARTESIAN_POINT('Ctrl Pts',(-6.96216723914695,-3.76155364985849,
-15.199687431446));
#75754=CARTESIAN_POINT('Ctrl Pts',(-7.05165591067077,-3.59096533211792,
-15.207437665201));
#75755=CARTESIAN_POINT('Ctrl Pts',(-7.13471077295075,-3.41757562993719,
-15.2151878989559));
#75756=CARTESIAN_POINT('Ctrl Pts',(-7.21789071619652,-3.24392480214849,
-15.2229498045949));
#75757=CARTESIAN_POINT('Ctrl Pts',(-7.29461735644497,-3.06746449180773,
-15.2307117102339));
#75758=CARTESIAN_POINT('Ctrl Pts',(-7.36472290601075,-2.88873285675234,
-15.2384736158729));
#75759=CARTESIAN_POINT('Ctrl Pts',(-7.41159305387289,-2.76923906183062,
-15.2436629577616));
#75760=CARTESIAN_POINT('Ctrl Pts',(-7.45550474725539,-2.64873033476617,
-15.2488522996503));
#75761=CARTESIAN_POINT('Ctrl Pts',(-7.49642058529095,-2.52737005767382,
-15.254041641539));
#75762=CARTESIAN_POINT('Ctrl Pts',(-7.57449418564336,-2.29579631441745,
-15.2639436898451));
#75763=CARTESIAN_POINT('Ctrl Pts',(-7.64185984319201,-2.06052492540488,
-15.2738457381511));
#75764=CARTESIAN_POINT('Ctrl Pts',(-7.69822398065782,-1.82243478446414,
-15.2837477864572));
#75765=CARTESIAN_POINT('Ctrl Pts',(-7.75419103741931,-1.58602196894888,
-15.2935800756488));
#75766=CARTESIAN_POINT('Ctrl Pts',(-7.79931102614652,-1.34682987051205,
-15.3034123648404));
#75767=CARTESIAN_POINT('Ctrl Pts',(-7.83334275199692,-1.10574062498276,
-15.313244654032));
#75768=CARTESIAN_POINT('Ctrl Pts',(-7.86686461943143,-0.868263343811501,
-15.3229296372828));
#75769=CARTESIAN_POINT('Ctrl Pts',(-7.88962796807497,-0.628945265185901,
-15.3326146205337));
#75770=CARTESIAN_POINT('Ctrl Pts',(-7.90144738229136,-0.388651855625442,
-15.3422996037846));
#75771=CARTESIAN_POINT('Ctrl Pts',(-7.90769935463835,-0.26154676190137,
-15.3474225520421));
#75772=CARTESIAN_POINT('Ctrl Pts',(-7.91089001490665,-0.134169158847204,
-15.3525455002997));
#75773=CARTESIAN_POINT('Ctrl Pts',(-7.91099720514315,-0.00664982836847595,
-15.3576684485573));
#75774=CARTESIAN_POINT('',(-7.90123025115119,0.00640242758643106,-17.357668491763));
#75775=CARTESIAN_POINT('Ctrl Pts',(-7.90416357127559,-0.00664300961161102,
-15.357668491763));
#75776=CARTESIAN_POINT('Ctrl Pts',(-7.88770305298382,1.76662955928556,-15.4289687423093));
#75777=CARTESIAN_POINT('Ctrl Pts',(-6.84972407068773,4.86972663156239,-15.5531902598329));
#75778=CARTESIAN_POINT('Ctrl Pts',(-3.20850006480543,7.57508514008354,-15.7303330443335));
#75779=CARTESIAN_POINT('Ctrl Pts',(2.16791332744694,8.45152836813056,-15.9420181122425));
#75780=CARTESIAN_POINT('Ctrl Pts',(7.06190333620408,5.12052295862938,-16.153703180151));
#75781=CARTESIAN_POINT('Ctrl Pts',(8.23216325382504,-0.209368643025021,
-16.3653882480596));
#75782=CARTESIAN_POINT('Ctrl Pts',(7.1501053363542,-4.12053083678862,-16.5241520489911));
#75783=CARTESIAN_POINT('Ctrl Pts',(4.30140354181539,-7.02213311397595,-16.6829158499228));
#75784=CARTESIAN_POINT('Ctrl Pts',(-0.884203313355227,-8.67324741747039,
-16.8946009178314));
#75785=CARTESIAN_POINT('Ctrl Pts',(-6.57909573114569,-5.95492941612458,
-17.1195184651114));
#75786=CARTESIAN_POINT('Ctrl Pts',(-7.89072598479452,-1.64495943571458,
-17.2915147454144));
#75787=CARTESIAN_POINT('Ctrl Pts',(-7.90123025115119,0.00640242758643106,
-17.357668491763));
#75788=CARTESIAN_POINT('',(-7.92320976604736,0.000404932896808444,-19.357668491763));
#75789=CARTESIAN_POINT('Ctrl Pts',(-7.90123025115119,0.00640242758643106,
-17.357668491763));
#75790=CARTESIAN_POINT('Ctrl Pts',(-7.90753226153451,0.997133170294752,
-17.3973572793687));
#75791=CARTESIAN_POINT('Ctrl Pts',(-7.27867603918967,4.62157268202392,-17.5428886009288));
#75792=CARTESIAN_POINT('Ctrl Pts',(-2.98788410044997,8.19005518207874,-17.7413411894661));
#75793=CARTESIAN_POINT('Ctrl Pts',(2.42295246631377,7.86165942351676,-17.9530262573749));
#75794=CARTESIAN_POINT('Ctrl Pts',(7.10076568002593,5.07023734257003,-18.1647113252837));
#75795=CARTESIAN_POINT('Ctrl Pts',(8.70021840697434,-0.629629868003249,
-18.3763963931923));
#75796=CARTESIAN_POINT('Ctrl Pts',(6.16354960033092,-5.46104416669315,-18.5880814611009));
#75797=CARTESIAN_POINT('Ctrl Pts',(2.81719811372365,-7.75668585711246,-18.7468452620326));
#75798=CARTESIAN_POINT('Ctrl Pts',(-1.2307231308085,-8.1423428124343,-18.9056090629639));
#75799=CARTESIAN_POINT('Ctrl Pts',(-6.06942212463287,-6.14568924132969,
-19.1092168062076));
#75800=CARTESIAN_POINT('Ctrl Pts',(-7.90917992093008,-2.41623274109057,
-19.2599032824738));
#75801=CARTESIAN_POINT('Ctrl Pts',(-7.92320976604736,0.000404932896808444,
-19.357668491763));
#75802=CARTESIAN_POINT('',(-7.90590625482663,-0.00331516544455179,-21.3576684917629));
#75803=CARTESIAN_POINT('Ctrl Pts',(-7.92320976604736,0.000404932896808444,
-19.357668491763));
#75804=CARTESIAN_POINT('Ctrl Pts',(-7.92436890655183,0.200066624748522,
-19.3657458164281));
#75805=CARTESIAN_POINT('Ctrl Pts',(-7.91747607560175,0.399707638355385,
-19.3738231410933));
#75806=CARTESIAN_POINT('Ctrl Pts',(-7.70314717160521,3.20752212073992,-19.4877429997129));
#75807=CARTESIAN_POINT('Ctrl Pts',(-4.45324040862703,8.23372206639351,-19.6994280676215));
#75808=CARTESIAN_POINT('Ctrl Pts',(2.98773583580864,8.19010927024974,-19.9640344025073));
#75809=CARTESIAN_POINT('Ctrl Pts',(6.91606556959596,4.45470813661777,-20.1757194704162));
#75810=CARTESIAN_POINT('Ctrl Pts',(8.69757176104145,-0.693127271215149,
-20.3874045383246));
#75811=CARTESIAN_POINT('Ctrl Pts',(6.25104031345718,-6.0839731343322,-20.5990896062335));
#75812=CARTESIAN_POINT('Ctrl Pts',(1.19920785351243,-8.14703919165728,-20.8107746741421));
#75813=CARTESIAN_POINT('Ctrl Pts',(-2.83927105800281,-7.74863346384884,
-20.9695384750738));
#75814=CARTESIAN_POINT('Ctrl Pts',(-6.18463760817827,-5.43715767248063,
-21.1283022760051));
#75815=CARTESIAN_POINT('Ctrl Pts',(-7.72004795960938,-2.48666735898332,
-21.257678948235));
#75816=CARTESIAN_POINT('Ctrl Pts',(-7.91116624839655,-0.58820461059737,
-21.3341343534875));
#75817=CARTESIAN_POINT('Ctrl Pts',(-7.90590625482663,-0.00331516544455179,
-21.3576684917629));
#75818=CARTESIAN_POINT('',(-7.90816594433051,-0.00119641522101588,-23.3576684917629));
#75819=CARTESIAN_POINT('Ctrl Pts',(-7.90590625482663,-0.00331516544455179,
-21.3576684917629));
#75820=CARTESIAN_POINT('Ctrl Pts',(-7.88750993085865,2.04227967710652,-21.4399768874419));
#75821=CARTESIAN_POINT('Ctrl Pts',(-6.05345660778066,6.73272226081268,-21.6281278170751));
#75822=CARTESIAN_POINT('Ctrl Pts',(1.89472071635594,9.16709128407982,-21.9221212806628));
#75823=CARTESIAN_POINT('Ctrl Pts',(7.5596726420224,4.34232712133296,-22.1867276155486));
#75824=CARTESIAN_POINT('Ctrl Pts',(8.15990728483216,-1.04513188083783,-22.3984126834575));
#75825=CARTESIAN_POINT('Ctrl Pts',(6.20812811174647,-6.13085029181979,-22.6100977513659));
#75826=CARTESIAN_POINT('Ctrl Pts',(0.86502967669206,-8.67997452520378,-22.8217828192748));
#75827=CARTESIAN_POINT('Ctrl Pts',(-4.32853973836911,-7.00543294876879,
-23.0334678871834));
#75828=CARTESIAN_POINT('Ctrl Pts',(-7.16180808017606,-4.10015679219509,
-23.1922316881149));
#75829=CARTESIAN_POINT('Ctrl Pts',(-7.89088696941476,-1.43010423471138,
-23.3002985563082));
#75830=CARTESIAN_POINT('Ctrl Pts',(-7.90804982156466,-0.0566024631711976,
-23.3554441575241));
#75831=CARTESIAN_POINT('Ctrl Pts',(-7.90816594433051,-0.00119641522101588,
-23.3576684917629));
#75832=CARTESIAN_POINT('',(-7.911,-5.53446177775641E-13,-25.357668491763));
#75833=CARTESIAN_POINT('Ctrl Pts',(-7.911,-7.19979631469414E-13,-23.3576684917629));
#75834=CARTESIAN_POINT('Ctrl Pts',(-7.9110000000002,2.20167589666604,-23.4462559274957));
#75835=CARTESIAN_POINT('Ctrl Pts',(-6.94214576672412,4.38610418338618,-23.5348433632284));
#75836=CARTESIAN_POINT('Ctrl Pts',(-3.67820201488356,7.34180684107597,-23.7120182346938));
#75837=CARTESIAN_POINT('Ctrl Pts',(-1.40868175871822,8.08992666571323,-23.8006056704266));
#75838=CARTESIAN_POINT('Ctrl Pts',(2.97309270521199,7.65454228025286,-23.977780541892));
#75839=CARTESIAN_POINT('Ctrl Pts',(5.05102072675538,6.47444880834276,-24.0663679776247));
#75840=CARTESIAN_POINT('Ctrl Pts',(7.66951518847842,2.93425195367785,-24.2435428490902));
#75841=CARTESIAN_POINT('Ctrl Pts',(8.18956872247065,0.601881960100011,-24.3321302848229));
#75842=CARTESIAN_POINT('Ctrl Pts',(7.32306689761382,-3.71537198232373,-24.5093051562884));
#75843=CARTESIAN_POINT('Ctrl Pts',(5.94329958850262,-5.66643518936447,-24.5978925920211));
#75844=CARTESIAN_POINT('Ctrl Pts',(2.16154501637934,-7.92205913232974,-24.7750674634866));
#75845=CARTESIAN_POINT('Ctrl Pts',(-0.210816529299463,-8.20894963713005,
-24.8636548992193));
#75846=CARTESIAN_POINT('Ctrl Pts',(-4.42123908576359,-6.91982244717881,
-25.0408297706847));
#75847=CARTESIAN_POINT('Ctrl Pts',(-6.22631625634127,-5.35390358803591,
-25.1294172064175));
#75848=CARTESIAN_POINT('Ctrl Pts',(-7.65317280859467,-2.31334857514596,
-25.2645592586878));
#75849=CARTESIAN_POINT('Ctrl Pts',(-7.91099999999992,-1.15702837836586,
-25.3111138752254));
#75850=CARTESIAN_POINT('Ctrl Pts',(-7.911,-5.53446177775641E-13,-25.357668491763));
#75851=CARTESIAN_POINT('',(-7.911,-4.99045249569008E-13,-27.357668491763));
#75852=CARTESIAN_POINT('Ctrl Pts',(-7.911,-5.53446177775641E-13,-25.357668491763));
#75853=CARTESIAN_POINT('Ctrl Pts',(-7.91100000000015,2.20167589666617,-25.4462559274957));
#75854=CARTESIAN_POINT('Ctrl Pts',(-6.94214576672406,4.38610418338626,-25.5348433632284));
#75855=CARTESIAN_POINT('Ctrl Pts',(-3.67820201488354,7.34180684107597,-25.7120182346938));
#75856=CARTESIAN_POINT('Ctrl Pts',(-1.40868175871824,8.08992666571321,-25.8006056704266));
#75857=CARTESIAN_POINT('Ctrl Pts',(2.97309270521189,7.65454228025289,-25.977780541892));
#75858=CARTESIAN_POINT('Ctrl Pts',(5.05102072675527,6.47444880834283,-26.0663679776247));
#75859=CARTESIAN_POINT('Ctrl Pts',(7.66951518847833,2.93425195367804,-26.2435428490902));
#75860=CARTESIAN_POINT('Ctrl Pts',(8.18956872247062,0.601881960100267,-26.3321302848229));
#75861=CARTESIAN_POINT('Ctrl Pts',(7.32306689761396,-3.71537198232343,-26.5093051562884));
#75862=CARTESIAN_POINT('Ctrl Pts',(5.94329958850287,-5.6664351893642,-26.5978925920211));
#75863=CARTESIAN_POINT('Ctrl Pts',(2.16154501637977,-7.92205913232961,-26.7750674634865));
#75864=CARTESIAN_POINT('Ctrl Pts',(-0.210816529298972,-8.20894963713005,
-26.8636548992193));
#75865=CARTESIAN_POINT('Ctrl Pts',(-4.42123908576311,-6.9198224471791,-27.0408297706847));
#75866=CARTESIAN_POINT('Ctrl Pts',(-6.22631625634086,-5.35390358803637,
-27.1294172064174));
#75867=CARTESIAN_POINT('Ctrl Pts',(-7.65317280859458,-2.31334857514636,
-27.2645592586878));
#75868=CARTESIAN_POINT('Ctrl Pts',(-7.91099999999993,-1.15702837836603,
-27.3111138752254));
#75869=CARTESIAN_POINT('Ctrl Pts',(-7.911,-4.99045249569008E-13,-27.357668491763));
#75870=CARTESIAN_POINT('',(-7.90149590314777,-6.97287683065524E-5,-29.3577571379651));
#75871=CARTESIAN_POINT('Ctrl Pts',(-7.911,-4.99045249569008E-13,-27.357668491763));
#75872=CARTESIAN_POINT('Ctrl Pts',(-7.91100000000014,2.2016758966663,-27.4462559274957));
#75873=CARTESIAN_POINT('Ctrl Pts',(-6.94214576672396,4.38610418338645,-27.5348433632284));
#75874=CARTESIAN_POINT('Ctrl Pts',(-3.67820201488322,7.34180684107615,-27.7120182346939));
#75875=CARTESIAN_POINT('Ctrl Pts',(-1.4086817587178,8.08992666571331,-27.8006056704266));
#75876=CARTESIAN_POINT('Ctrl Pts',(2.97309270521246,7.65454228025269,-27.977780541892));
#75877=CARTESIAN_POINT('Ctrl Pts',(5.05102072675582,6.47444880834243,-28.0663679776248));
#75878=CARTESIAN_POINT('Ctrl Pts',(7.66951518847865,2.93425195367728,-28.2435428490902));
#75879=CARTESIAN_POINT('Ctrl Pts',(8.18956872247071,0.601881960099353,-28.3321302848229));
#75880=CARTESIAN_POINT('Ctrl Pts',(7.3230668976135,-3.71537198232438,-28.5093051562884));
#75881=CARTESIAN_POINT('Ctrl Pts',(5.94329958850209,-5.66643518936504,-28.5978925920211));
#75882=CARTESIAN_POINT('Ctrl Pts',(2.16154501637852,-7.92205913232997,-28.7750674634866));
#75883=CARTESIAN_POINT('Ctrl Pts',(-0.210816529300357,-8.20894963713003,
-28.8636548992193));
#75884=CARTESIAN_POINT('Ctrl Pts',(-4.42123908576441,-6.9198224471783,-29.0408297706848));
#75885=CARTESIAN_POINT('Ctrl Pts',(-6.22631625634193,-5.35390358803515,
-29.1294172064175));
#75886=CARTESIAN_POINT('Ctrl Pts',(-7.6531636284135,-2.31336813762078,-29.2645583892041));
#75887=CARTESIAN_POINT('Ctrl Pts',(-7.91099036922816,-1.15707157067501,
-29.311112136258));
#75888=CARTESIAN_POINT('Ctrl Pts',(-7.9109999997302,-6.48282003627523E-5,
-29.3576658833118));
#75889=CARTESIAN_POINT('',(-7.91011762826041,0.00206862855998248,-31.357532306749));
#75890=CARTESIAN_POINT('Ctrl Pts',(-7.89569987159112,-7.27173581417825E-5,
-29.3578127892145));
#75891=CARTESIAN_POINT('Ctrl Pts',(-7.8945841079301,0.255048674726026,-29.3680723344091));
#75892=CARTESIAN_POINT('Ctrl Pts',(-7.88131840855623,0.510468153943764,
-29.3781339197719));
#75893=CARTESIAN_POINT('Ctrl Pts',(-7.85608173587964,0.764857387287981,
-29.3880686173644));
#75894=CARTESIAN_POINT('Ctrl Pts',(-7.83074434981928,1.02026182579864,-29.3980429619033));
#75895=CARTESIAN_POINT('Ctrl Pts',(-7.79334103122647,1.27462730778321,-29.4078894038951));
#75896=CARTESIAN_POINT('Ctrl Pts',(-7.74408245254443,1.52665288736753,-29.4176798696952));
#75897=CARTESIAN_POINT('Ctrl Pts',(-7.69482460245071,1.77867473921754,-29.4274701906835));
#75898=CARTESIAN_POINT('Ctrl Pts',(-7.63371264112704,2.02835647531821,-29.437204537136));
#75899=CARTESIAN_POINT('Ctrl Pts',(-7.56097485512378,2.27444610108197,-29.4469548322165));
#75900=CARTESIAN_POINT('Ctrl Pts',(-7.48841280666463,2.51994116398042,-29.4566815701748));
#75901=CARTESIAN_POINT('Ctrl Pts',(-7.40428182726746,2.76186135706339,-29.4664241797891));
#75902=CARTESIAN_POINT('Ctrl Pts',(-7.30881422844452,2.99901519620115,-29.4762540641735));
#75903=CARTESIAN_POINT('Ctrl Pts',(-7.21365811614968,3.23539526259412,-29.4860518761418));
#75904=CARTESIAN_POINT('Ctrl Pts',(-7.10723999461208,3.46704010152067,-29.4959363942986));
#75905=CARTESIAN_POINT('Ctrl Pts',(-6.98978405375929,3.69282117826146,-29.5059783251252));
#75906=CARTESIAN_POINT('Ctrl Pts',(-6.87400734420874,3.91537433269568,-29.5158766895689));
#75907=CARTESIAN_POINT('Ctrl Pts',(-6.74750682809626,4.13223049888618,-29.5259279978963));
#75908=CARTESIAN_POINT('Ctrl Pts',(-6.61048107240587,4.34235580006046,-29.5361999671321));
#75909=CARTESIAN_POINT('Ctrl Pts',(-6.47370176868633,4.55210317378352,-29.5464534613955));
#75910=CARTESIAN_POINT('Ctrl Pts',(-6.32643606094231,4.75514437299453,-29.556926823528));
#75911=CARTESIAN_POINT('Ctrl Pts',(-6.16979938689121,4.95090743069015,-29.5676874058276));
#75912=CARTESIAN_POINT('Ctrl Pts',(-6.10215945038996,5.0354431939272,-29.5723341152133));
#75913=CARTESIAN_POINT('Ctrl Pts',(-6.03277162499537,5.11862225049764,-29.5770343838391));
#75914=CARTESIAN_POINT('Ctrl Pts',(-5.96172351681003,5.20040060098812,-29.5817936352299));
#75915=CARTESIAN_POINT('Ctrl Pts',(-5.85905843910731,5.31857096360503,-29.588670791094));
#75916=CARTESIAN_POINT('Ctrl Pts',(-5.75283076577076,5.43362924400229,-29.5955541844561));
#75917=CARTESIAN_POINT('Ctrl Pts',(-5.64310303154788,5.54530414778243,-29.6023197989571));
#75918=CARTESIAN_POINT('Ctrl Pts',(-5.53544242143685,5.65487524537421,-29.6089579583078));
#75919=CARTESIAN_POINT('Ctrl Pts',(-5.42441198582704,5.76118885449211,-29.6154827345914));
#75920=CARTESIAN_POINT('Ctrl Pts',(-5.31009505383172,5.86394639032005,-29.6217769891479));
#75921=CARTESIAN_POINT('Ctrl Pts',(-4.99017996486874,6.15151259457539,-29.6393914139866));
#75922=CARTESIAN_POINT('Ctrl Pts',(-4.64623847650883,6.41344155099911,-29.6568267531459));
#75923=CARTESIAN_POINT('Ctrl Pts',(-4.28356735312668,6.64607706485341,-29.6741546816272));
#75924=CARTESIAN_POINT('Ctrl Pts',(-4.10061586087137,6.76343136098351,-29.6828958528123));
#75925=CARTESIAN_POINT('Ctrl Pts',(-3.91289804297522,6.87333210944896,-29.6916096906125));
#75926=CARTESIAN_POINT('Ctrl Pts',(-3.72109217012557,6.97531459386228,-29.7003053960622));
#75927=CARTESIAN_POINT('Ctrl Pts',(-3.33363652617021,7.18132334939974,-29.7178710738207));
#75928=CARTESIAN_POINT('Ctrl Pts',(-2.92950218373761,7.35501904141783,-29.7353627613642));
#75929=CARTESIAN_POINT('Ctrl Pts',(-2.51426387279328,7.49464824607955,-29.7528563019399));
#75930=CARTESIAN_POINT('Ctrl Pts',(-2.09919877920832,7.63421920418384,-29.7703425450557));
#75931=CARTESIAN_POINT('Ctrl Pts',(-1.67303963538504,7.73975436701759,-29.7878306396581));
#75932=CARTESIAN_POINT('Ctrl Pts',(-1.24130498229201,7.80951741044183,-29.8053963341193));
#75933=CARTESIAN_POINT('Ctrl Pts',(-0.834176089700127,7.87530446369241,
-29.8219609107229));
#75934=CARTESIAN_POINT('Ctrl Pts',(-0.422088617451437,7.90928259463422,
-29.8385944939792));
#75935=CARTESIAN_POINT('Ctrl Pts',(-0.00962658081288734,7.90997912443843,
-29.855360605038));
#75936=CARTESIAN_POINT('Ctrl Pts',(0.015301500377193,7.91002122080117,-29.8563739030887));
#75937=CARTESIAN_POINT('Ctrl Pts',(0.0402309621464365,7.90994174037809,
-29.857387685219));
#75938=CARTESIAN_POINT('Ctrl Pts',(0.0651607972488829,7.90974035367802,
-29.8584019654515));
#75939=CARTESIAN_POINT('Ctrl Pts',(0.304397112014934,7.90780776921566,-29.8681353898395));
#75940=CARTESIAN_POINT('Ctrl Pts',(0.543667487189482,7.8946490670781,-29.8779146847761));
#75941=CARTESIAN_POINT('Ctrl Pts',(0.782055855848812,7.87057601841741,-29.8877522426792));
#75942=CARTESIAN_POINT('Ctrl Pts',(1.07669559247589,7.84082256711823,-29.8999111222669));
#75943=CARTESIAN_POINT('Ctrl Pts',(1.36946104408517,7.79417976114013,-29.9119816789554));
#75944=CARTESIAN_POINT('Ctrl Pts',(1.65866474447215,7.73135886840473,-29.9239804189653));
#75945=CARTESIAN_POINT('Ctrl Pts',(1.95397836663951,7.66721077708829,-29.9362326528372));
#75946=CARTESIAN_POINT('Ctrl Pts',(2.24557891627073,7.58619388002973,-29.9484100034761));
#75947=CARTESIAN_POINT('Ctrl Pts',(2.53169299840934,7.48901518069949,-29.9605300455267));
#75948=CARTESIAN_POINT('Ctrl Pts',(2.82371124363093,7.38983113131884,-29.9729001930747));
#75949=CARTESIAN_POINT('Ctrl Pts',(3.11001518622114,7.27381144226102,-29.9852106424252));
#75950=CARTESIAN_POINT('Ctrl Pts',(3.38873034071391,7.14165481546951,-29.9974800788239));
#75951=CARTESIAN_POINT('Ctrl Pts',(3.54067584638536,7.06960776254835,-30.0041689354858));
#75952=CARTESIAN_POINT('Ctrl Pts',(3.6903660414768,6.99276382658616,-30.0108456029372));
#75953=CARTESIAN_POINT('Ctrl Pts',(3.83749696044171,6.91122971103455,-30.0175131086534));
#75954=CARTESIAN_POINT('Ctrl Pts',(4.10723893957669,6.76174941246346,-30.029736958001));
#75955=CARTESIAN_POINT('Ctrl Pts',(4.36838012447758,6.59650743440992,-30.0419300132912));
#75956=CARTESIAN_POINT('Ctrl Pts',(4.6191916329761,6.41676870673628,-30.0541109303471));
#75957=CARTESIAN_POINT('Ctrl Pts',(4.86657260539754,6.23948839970459,-30.0661252399148));
#75958=CARTESIAN_POINT('Ctrl Pts',(5.1039054682342,6.04810464874452,-30.0781277410248));
#75959=CARTESIAN_POINT('Ctrl Pts',(5.32950460302231,5.84378910404561,-30.0901363344138));
#75960=CARTESIAN_POINT('Ctrl Pts',(5.54573629318662,5.64795725567181,-30.1016463007416));
#75961=CARTESIAN_POINT('Ctrl Pts',(5.75118907158626,5.44024461804703,-30.1131618639188));
#75962=CARTESIAN_POINT('Ctrl Pts',(5.94434311403979,5.22165265539691,-30.1246987861385));
#75963=CARTESIAN_POINT('Ctrl Pts',(6.09093752971214,5.05575210975818,-30.1334547425243));
#75964=CARTESIAN_POINT('Ctrl Pts',(6.23044718286647,4.88358435767637,-30.1422230018536));
#75965=CARTESIAN_POINT('Ctrl Pts',(6.36218972045515,4.70557793093048,-30.1510104547341));
#75966=CARTESIAN_POINT('Ctrl Pts',(6.47502102515782,4.55312377494704,-30.1585364959936));
#75967=CARTESIAN_POINT('Ctrl Pts',(6.5822020773836,4.39662647188323,-30.1661748264367));
#75968=CARTESIAN_POINT('Ctrl Pts',(6.68326889010009,4.23635763789733,-30.1738931191833));
#75969=CARTESIAN_POINT('Ctrl Pts',(6.82187292273323,4.01656336420068,-30.1844780626576));
#75970=CARTESIAN_POINT('Ctrl Pts',(6.94897773567381,3.78967367522231,-30.1952133964538));
#75971=CARTESIAN_POINT('Ctrl Pts',(7.06437106698293,3.55693002058069,-30.2060157398447));
#75972=CARTESIAN_POINT('Ctrl Pts',(7.17996231729417,3.32378717136383,-30.2168366110743));
#75973=CARTESIAN_POINT('Ctrl Pts',(7.28380100830786,3.08477018935011,-30.2277247219611));
#75974=CARTESIAN_POINT('Ctrl Pts',(7.37566767430952,2.84117894413984,-30.2385962620053));
#75975=CARTESIAN_POINT('Ctrl Pts',(7.46761138924782,2.59738339798738,-30.2494769200533));
#75976=CARTESIAN_POINT('Ctrl Pts',(7.54756210101163,2.34900604493784,-30.260340979451));
#75977=CARTESIAN_POINT('Ctrl Pts',(7.61530687772506,2.09740160556108,-30.2711044186453));
#75978=CARTESIAN_POINT('Ctrl Pts',(7.64910139818574,1.97188858762782,-30.2764737664197));
#75979=CARTESIAN_POINT('Ctrl Pts',(7.67985864228526,1.84557329561306,-30.2818180746663));
#75980=CARTESIAN_POINT('Ctrl Pts',(7.70755389160994,1.71862844955189,-30.2871269129571));
#75981=CARTESIAN_POINT('Ctrl Pts',(7.75778494272112,1.48838776906388,-30.2967555869726));
#75982=CARTESIAN_POINT('Ctrl Pts',(7.7980703493988,1.2561018325183,-30.306339698528));
#75983=CARTESIAN_POINT('Ctrl Pts',(7.82835458766272,1.02258119335211,-30.3158624553201));
#75984=CARTESIAN_POINT('Ctrl Pts',(7.85870170280127,0.788575712935363,-30.3254049834922));
#75985=CARTESIAN_POINT('Ctrl Pts',(7.87900595604867,0.553329539576292,-30.334885901864));
#75986=CARTESIAN_POINT('Ctrl Pts',(7.8891598651935,0.317662158590311,-30.3442883133212));
#75987=CARTESIAN_POINT('Ctrl Pts',(7.89921463198212,0.0842958243343077,
-30.353598920015));
#75988=CARTESIAN_POINT('Ctrl Pts',(7.89931609340655,-0.149484304558608,
-30.3628325453864));
#75989=CARTESIAN_POINT('Ctrl Pts',(7.88931193660423,-0.382866602834017,
-30.3719727824525));
#75990=CARTESIAN_POINT('Ctrl Pts',(7.87955525618199,-0.610475640304844,
-30.3808869142278));
#75991=CARTESIAN_POINT('Ctrl Pts',(7.8601864526231,-0.837706877758794,-30.3897122209094));
#75992=CARTESIAN_POINT('Ctrl Pts',(7.83102226607746,-1.06378235556531,-30.3984334832386));
#75993=CARTESIAN_POINT('Ctrl Pts',(7.80977207922144,-1.22850994498162,-30.4047881420193));
#75994=CARTESIAN_POINT('Ctrl Pts',(7.78332050071093,-1.39262344223998,-30.411087561994));
#75995=CARTESIAN_POINT('Ctrl Pts',(7.75158330011696,-1.55581053101365,-30.4173258556459));
#75996=CARTESIAN_POINT('Ctrl Pts',(7.70457969503489,-1.79749477951883,-30.4265649279559));
#75997=CARTESIAN_POINT('Ctrl Pts',(7.64648254573122,-2.03708246863251,-30.4359439692));
#75998=CARTESIAN_POINT('Ctrl Pts',(7.57715365975328,-2.27333984897705,-30.4454542601858));
#75999=CARTESIAN_POINT('Ctrl Pts',(7.50910989560062,-2.50521782077371,-30.4547882627121));
#76000=CARTESIAN_POINT('Ctrl Pts',(7.43024698951954,-2.73388696816542,-30.4642486942303));
#76001=CARTESIAN_POINT('Ctrl Pts',(7.34048365772138,-2.95818606679694,-30.4738273114881));
#76002=CARTESIAN_POINT('Ctrl Pts',(7.29244812213151,-3.07821645247063,-30.4789531685722));
#76003=CARTESIAN_POINT('Ctrl Pts',(7.24129187452229,-3.19699555119828,-30.4841128704931));
#76004=CARTESIAN_POINT('Ctrl Pts',(7.18700835380188,-3.31434728423305,-30.4893051539998));
#76005=CARTESIAN_POINT('Ctrl Pts',(7.08428777633514,-3.5364116902273,-30.4991304997605));
#76006=CARTESIAN_POINT('Ctrl Pts',(6.97036643537057,-3.7533632004455,-30.5090725133482));
#76007=CARTESIAN_POINT('Ctrl Pts',(6.84623930951474,-3.9644337130622,-30.5191226350746));
#76008=CARTESIAN_POINT('Ctrl Pts',(6.72111484907999,-4.17720013154452,-30.529253507353));
#76009=CARTESIAN_POINT('Ctrl Pts',(6.585620644126,-4.38399005579828,-30.5394942320004));
#76010=CARTESIAN_POINT('Ctrl Pts',(6.44081709798858,-4.58405060379496,-30.5498360413406));
#76011=CARTESIAN_POINT('Ctrl Pts',(6.29708880068084,-4.78262558824133,-30.5601010568543));
#76012=CARTESIAN_POINT('Ctrl Pts',(6.14418968361826,-4.97457026492628,-30.5704656614117));
#76013=CARTESIAN_POINT('Ctrl Pts',(5.98318592183888,-5.15918983316727,-30.5809212812048));
#76014=CARTESIAN_POINT('Ctrl Pts',(5.86457305787863,-5.29520066602083,-30.5886240267458));
#76015=CARTESIAN_POINT('Ctrl Pts',(5.7415621333112,-5.42723669077786,-30.5963761698626));
#76016=CARTESIAN_POINT('Ctrl Pts',(5.6145860317735,-5.55503702543636,-30.6041742823954));
#76017=CARTESIAN_POINT('Ctrl Pts',(5.47707440897578,-5.6934412700159,-30.6126194236162));
#76018=CARTESIAN_POINT('Ctrl Pts',(5.33451368350287,-5.82666177022762,-30.620869880412));
#76019=CARTESIAN_POINT('Ctrl Pts',(5.18736468424763,-5.95453344434437,-30.6289856878826));
#76020=CARTESIAN_POINT('Ctrl Pts',(5.03910865941913,-6.08336711761884,-30.6371625518772));
#76021=CARTESIAN_POINT('Ctrl Pts',(4.88619485176865,-6.20677180674103,-30.6452027329487));
#76022=CARTESIAN_POINT('Ctrl Pts',(4.72904226888832,-6.32456931573893,-30.6531676313768));
#76023=CARTESIAN_POINT('Ctrl Pts',(4.57154450184332,-6.44262556585327,-30.6611500246292));
#76024=CARTESIAN_POINT('Ctrl Pts',(4.40978902703204,-6.55505063482755,-30.6690568041598));
#76025=CARTESIAN_POINT('Ctrl Pts',(4.24414915186498,-6.66164613483122,-30.6769497757334));
#76026=CARTESIAN_POINT('Ctrl Pts',(4.1790019173349,-6.70357083461492,-30.6800541325178));
#76027=CARTESIAN_POINT('Ctrl Pts',(4.11325330167021,-6.74459349773157,-30.6831563533496));
#76028=CARTESIAN_POINT('Ctrl Pts',(4.04692412666748,-6.78470090112318,-30.6862601985267));
#76029=CARTESIAN_POINT('Ctrl Pts',(3.87255137163058,-6.89013924596139,-30.6944198964985));
#76030=CARTESIAN_POINT('Ctrl Pts',(3.69377325136641,-6.98893125659474,-30.7023236757362));
#76031=CARTESIAN_POINT('Ctrl Pts',(3.51129648404317,-7.08067426001595,-30.7100645035343));
#76032=CARTESIAN_POINT('Ctrl Pts',(3.3227320584461,-7.17547792733447,-30.7180635752452));
#76033=CARTESIAN_POINT('Ctrl Pts',(3.13021895902962,-7.26275441992961,-30.7258886416189));
#76034=CARTESIAN_POINT('Ctrl Pts',(2.93451511514658,-7.34211356730782,-30.733642288336));
#76035=CARTESIAN_POINT('Ctrl Pts',(2.74578128959534,-7.41864632813661,-30.7411197878979));
#76036=CARTESIAN_POINT('Ctrl Pts',(2.55408037837696,-7.48781629011548,-30.7485308644529));
#76037=CARTESIAN_POINT('Ctrl Pts',(2.36006295633384,-7.54931729946368,-30.7559675286102));
#76038=CARTESIAN_POINT('Ctrl Pts',(2.16646713096828,-7.61068466812676,-30.7633880330181));
#76039=CARTESIAN_POINT('Ctrl Pts',(1.97056531729853,-7.66441681384306,-30.7708340139462));
#76040=CARTESIAN_POINT('Ctrl Pts',(1.7729674110032,-7.71024644124962,-30.7783968834934));
#76041=CARTESIAN_POINT('Ctrl Pts',(1.57577205934891,-7.75598270264054,-30.7859443456494));
#76042=CARTESIAN_POINT('Ctrl Pts',(1.37688788298791,-7.79384911456881,-30.7936082206489));
#76043=CARTESIAN_POINT('Ctrl Pts',(1.17687850676287,-7.82360973146476,-30.8014793630427));
#76044=CARTESIAN_POINT('Ctrl Pts',(1.15334442373915,-7.82711151144171,-30.8024055202164));
#76045=CARTESIAN_POINT('Ctrl Pts',(1.12979471031162,-7.8305010950992,-30.803334547013));
#76046=CARTESIAN_POINT('Ctrl Pts',(1.10623024247913,-7.83377811993991,-30.8042665914413));
#76047=CARTESIAN_POINT('Ctrl Pts',(0.905979520921187,-7.8616262595024,-30.8121871000065));
#76048=CARTESIAN_POINT('Ctrl Pts',(0.704667374967774,-7.88134454934293,
-30.8203255296031));
#76049=CARTESIAN_POINT('Ctrl Pts',(0.502870338412337,-7.89333825659674,
-30.8287727118013));
#76050=CARTESIAN_POINT('Ctrl Pts',(0.301909383542035,-7.90528227174832,
-30.8371848957933));
#76051=CARTESIAN_POINT('Ctrl Pts',(0.100467690963634,-7.9095663226281,-30.845903279251));
#76052=CARTESIAN_POINT('Ctrl Pts',(-0.100936048976943,-7.90659976529281,
-30.8550175694211));
#76053=CARTESIAN_POINT('Ctrl Pts',(-0.183832286805069,-7.90537875299944,
-30.858768941495));
#76054=CARTESIAN_POINT('Ctrl Pts',(-0.26672270296442,-7.90292947207764,
-30.8625873834358));
#76055=CARTESIAN_POINT('Ctrl Pts',(-0.349573704434322,-7.89928047876121,
-30.8664791502737));
#76056=CARTESIAN_POINT('Ctrl Pts',(-0.555271224667018,-7.89022097600061,
-30.8761413966397));
#76057=CARTESIAN_POINT('Ctrl Pts',(-0.760421052167959,-7.87245429262813,
-30.885478905345));
#76058=CARTESIAN_POINT('Ctrl Pts',(-0.964441435025923,-7.84640026727707,
-30.8945578142934));
#76059=CARTESIAN_POINT('Ctrl Pts',(-1.17049180476456,-7.82008700640792,
-30.903727057677));
#76060=CARTESIAN_POINT('Ctrl Pts',(-1.37539052845679,-7.78532100936025,
-30.9126325296072));
#76061=CARTESIAN_POINT('Ctrl Pts',(-1.57858110370323,-7.74250281151564,
-30.9213423618969));
#76062=CARTESIAN_POINT('Ctrl Pts',(-1.78447308460689,-7.69911534847875,
-30.9301679908479));
#76063=CARTESIAN_POINT('Ctrl Pts',(-1.98861165089484,-7.64746051126545,
-30.9387927435451));
#76064=CARTESIAN_POINT('Ctrl Pts',(-2.19045516918942,-7.58791701913866,
-30.9472875055138));
#76065=CARTESIAN_POINT('Ctrl Pts',(-2.23095995217108,-7.5759681775462,-30.9489921849255));
#76066=CARTESIAN_POINT('Ctrl Pts',(-2.27137241886445,-7.5637015280104,-30.950691629594));
#76067=CARTESIAN_POINT('Ctrl Pts',(-2.31168834357439,-7.55111993061152,
-30.9523864123576));
#76068=CARTESIAN_POINT('Ctrl Pts',(-2.57166766327819,-7.46998685091454,
-30.9633153064138));
#76069=CARTESIAN_POINT('Ctrl Pts',(-2.82801669922837,-7.37561949093419,
-30.9740590899625));
#76070=CARTESIAN_POINT('Ctrl Pts',(-3.07923169674846,-7.26866601893759,
-30.9846904548434));
#76071=CARTESIAN_POINT('Ctrl Pts',(-3.33250716791111,-7.16083531105857,
-30.9954090185275));
#76072=CARTESIAN_POINT('Ctrl Pts',(-3.58056374531226,-7.04021220390749,
-31.0060133118579));
#76073=CARTESIAN_POINT('Ctrl Pts',(-3.82190987656764,-6.90747907848244,
-31.0165778300476));
#76074=CARTESIAN_POINT('Ctrl Pts',(-4.06373872533062,-6.7744804729225,-31.0271634783789));
#76075=CARTESIAN_POINT('Ctrl Pts',(-4.29883021368951,-6.62932435886097,
-31.0377091923015));
#76076=CARTESIAN_POINT('Ctrl Pts',(-4.5257357913364,-6.47270005511793,-31.048289914918));
#76077=CARTESIAN_POINT('Ctrl Pts',(-4.75199172242079,-6.31652417772732,
-31.0588403441844));
#76078=CARTESIAN_POINT('Ctrl Pts',(-4.97010874902366,-6.14894660191629,
-31.0694255819671));
#76079=CARTESIAN_POINT('Ctrl Pts',(-5.17870111614328,-5.97063918916825,
-31.0801199295073));
#76080=CARTESIAN_POINT('Ctrl Pts',(-5.38620263206032,-5.79326424992492,
-31.0907583500641));
#76081=CARTESIAN_POINT('Ctrl Pts',(-5.58427925653382,-5.60527220954998,
-31.1015047421654));
#76082=CARTESIAN_POINT('Ctrl Pts',(-5.77161221360211,-5.40730016750988,
-31.1124322474445));
#76083=CARTESIAN_POINT('Ctrl Pts',(-5.84246648446754,-5.33242191378447,
-31.1165653184804));
#76084=CARTESIAN_POINT('Ctrl Pts',(-5.91178424954878,-5.2561156581599,-31.1207242987006));
#76085=CARTESIAN_POINT('Ctrl Pts',(-5.97949564096399,-5.17841460947582,
-31.1249131455985));
#76086=CARTESIAN_POINT('Ctrl Pts',(-6.15602892318531,-4.97583686192772,
-31.1358340685944));
#76087=CARTESIAN_POINT('Ctrl Pts',(-6.32164132715477,-4.763781453909,-31.1469580012156));
#76088=CARTESIAN_POINT('Ctrl Pts',(-6.4760637532379,-4.54363763691952,-31.1583550752257));
#76089=CARTESIAN_POINT('Ctrl Pts',(-6.6121491758484,-4.34963495783987,-31.1683987953805));
#76090=CARTESIAN_POINT('Ctrl Pts',(-6.73954516965971,-4.14935043551168,
-31.1786546396211));
#76091=CARTESIAN_POINT('Ctrl Pts',(-6.8580827178115,-3.94370481381216,-31.189170605431));
#76092=CARTESIAN_POINT('Ctrl Pts',(-6.92636458653132,-3.82524557821441,
-31.1952281779732));
#76093=CARTESIAN_POINT('Ctrl Pts',(-6.99151032737667,-3.7049668770132,-31.2012588830443));
#76094=CARTESIAN_POINT('Ctrl Pts',(-7.05325504757299,-3.58291852259966,
-31.2071169359491));
#76095=CARTESIAN_POINT('Ctrl Pts',(-7.09044186461077,-3.50941280727845,
-31.2106450488124));
#76096=CARTESIAN_POINT('Ctrl Pts',(-7.12639444898179,-3.43526600339684,
-31.2141105362931));
#76097=CARTESIAN_POINT('Ctrl Pts',(-7.16105018869253,-3.36049679187304,
-31.2174815505884));
#76098=CARTESIAN_POINT('Ctrl Pts',(-7.26544716940653,-3.13526195347102,
-31.2276363970096));
#76099=CARTESIAN_POINT('Ctrl Pts',(-7.3592402758094,-2.90524691619423,-31.2377407236085));
#76100=CARTESIAN_POINT('Ctrl Pts',(-7.44224561077067,-2.67144349523618,
-31.2478073653404));
#76101=CARTESIAN_POINT('Ctrl Pts',(-7.52689158749378,-2.43301883328608,
-31.2580729792569));
#76102=CARTESIAN_POINT('Ctrl Pts',(-7.60031955403292,-2.19065390436773,
-31.2682994038636));
#76103=CARTESIAN_POINT('Ctrl Pts',(-7.6622941268666,-1.94536481155424,-31.2785002503257));
#76104=CARTESIAN_POINT('Ctrl Pts',(-7.68376815431407,-1.86037278222993,
-31.2820348169536));
#76105=CARTESIAN_POINT('Ctrl Pts',(-7.70386670237713,-1.7750294130185,-31.2855663126582));
#76106=CARTESIAN_POINT('Ctrl Pts',(-7.72257873394354,-1.68937622778368,
-31.2890953036726));
#76107=CARTESIAN_POINT('Ctrl Pts',(-7.77687405767233,-1.4408426891231,-31.299335116965));
#76108=CARTESIAN_POINT('Ctrl Pts',(-7.81949938009848,-1.18970175964949,
-31.3095538421798));
#76109=CARTESIAN_POINT('Ctrl Pts',(-7.8503183535253,-0.937080670013483,
-31.3197653124211));
#76110=CARTESIAN_POINT('Ctrl Pts',(-7.88089443223502,-0.686450572330713,
-31.3298963026237));
#76111=CARTESIAN_POINT('Ctrl Pts',(-7.89984967201503,-0.434362651769033,
-31.3400201517598));
#76112=CARTESIAN_POINT('Ctrl Pts',(-7.90700057737854,-0.181910412584309,
-31.3501503684347));
#76113=CARTESIAN_POINT('Ctrl Pts',(-7.9087176329076,-0.12129228228041,-31.3525828079186));
#76114=CARTESIAN_POINT('Ctrl Pts',(-7.90975385920825,-0.0606531482638515,
-31.3550156145312));
#76115=CARTESIAN_POINT('Ctrl Pts',(-7.91010626430346,-8.17558293495676E-6,
-31.357448975289));
#76116=CARTESIAN_POINT('',(-7.91695845694372,0.000899907545194336,-33.3576681232209));
#76117=CARTESIAN_POINT('Ctrl Pts',(-7.91013619988552,0.00546266007265983,
-31.357668491763));
#76118=CARTESIAN_POINT('Ctrl Pts',(-7.91398572774975,0.755458957314721,
-31.3877621066932));
#76119=CARTESIAN_POINT('Ctrl Pts',(-7.45882838377432,4.13741011254259,-31.5236982555779));
#76120=CARTESIAN_POINT('Ctrl Pts',(-3.73499777086688,7.88289450337639,-31.7125556714397));
#76121=CARTESIAN_POINT('Ctrl Pts',(1.71919252665886,8.05336725367734,-31.9242407393484));
#76122=CARTESIAN_POINT('Ctrl Pts',(5.36476995012875,6.27072755588009,-32.0830045402799));
#76123=CARTESIAN_POINT('Ctrl Pts',(7.69321605282543,2.93715043272905,-32.2417683412114));
#76124=CARTESIAN_POINT('Ctrl Pts',(8.3628728449941,-2.46361402060145,-32.45345340912));
#76125=CARTESIAN_POINT('Ctrl Pts',(3.98770187756028,-8.46131879696375,-32.718059744006));
#76126=CARTESIAN_POINT('Ctrl Pts',(-4.97458638376742,-7.92962921668339,
-33.0355873458691));
#76127=CARTESIAN_POINT('Ctrl Pts',(-7.89551479792441,-2.6937012197221,-33.2487900774767));
#76128=CARTESIAN_POINT('Ctrl Pts',(-7.91988269843863,-0.0366651763938352,
-33.3561502751302));
#76129=CARTESIAN_POINT('Ctrl Pts',(-7.91993966167306,0.000895686316540435,
-33.3576679388293));
#76130=CARTESIAN_POINT('',(-7.9066350512344,-0.00678589508903775,-35.3576684826878));
#76131=CARTESIAN_POINT('Ctrl Pts',(-7.91099994785175,0.000908344479788625,
-33.3576684917629));
#76132=CARTESIAN_POINT('Ctrl Pts',(-7.91097574369575,0.211708411063882,
-33.3661955907321));
#76133=CARTESIAN_POINT('Ctrl Pts',(-7.9025215909712,0.422656322421778,-33.3747226897013));
#76134=CARTESIAN_POINT('Ctrl Pts',(-7.8856278558695,0.633083184688264,-33.3832497886705));
#76135=CARTESIAN_POINT('Ctrl Pts',(-7.8687588186536,0.8432024122853,-33.3917644214021));
#76136=CARTESIAN_POINT('Ctrl Pts',(-7.84347483866858,1.05280185273585,-33.4002790541336));
#76137=CARTESIAN_POINT('Ctrl Pts',(-7.80981823579319,1.26121375027078,-33.4087936868652));
#76138=CARTESIAN_POINT('Ctrl Pts',(-7.77586205415544,1.47148073040437,-33.4173841086817));
#76139=CARTESIAN_POINT('Ctrl Pts',(-7.73338344372194,1.68053865778044,-33.4259745304982));
#76140=CARTESIAN_POINT('Ctrl Pts',(-7.68247971765538,1.88770399899287,-33.4345649523148));
#76141=CARTESIAN_POINT('Ctrl Pts',(-7.63221165482289,2.09228235098158,-33.4430481007402));
#76142=CARTESIAN_POINT('Ctrl Pts',(-7.5737276962571,2.29501483569678,-33.4515312491657));
#76143=CARTESIAN_POINT('Ctrl Pts',(-7.5071733698418,2.49524928516933,-33.4600143975911));
#76144=CARTESIAN_POINT('Ctrl Pts',(-7.43935662741166,2.69928182245006,-33.4686584561032));
#76145=CARTESIAN_POINT('Ctrl Pts',(-7.36316031003098,2.90072034532527,-33.4773025146153));
#76146=CARTESIAN_POINT('Ctrl Pts',(-7.27879312200625,3.09888555565296,-33.4859465731274));
#76147=CARTESIAN_POINT('Ctrl Pts',(-7.19442593398151,3.29705076598066,-33.4945906316394));
#76148=CARTESIAN_POINT('Ctrl Pts',(-7.10188792480581,3.49194237486484,-33.5032346901515));
#76149=CARTESIAN_POINT('Ctrl Pts',(-7.00144247287156,3.6828961835857,-33.5118787486636));
#76150=CARTESIAN_POINT('Ctrl Pts',(-6.90969162978071,3.8573209345741,-33.5197745731229));
#76151=CARTESIAN_POINT('Ctrl Pts',(-6.81142359265998,4.02830602410947,-33.5276703975822));
#76152=CARTESIAN_POINT('Ctrl Pts',(-6.70693643722551,4.19534559089199,-33.5355662220415));
#76153=CARTESIAN_POINT('Ctrl Pts',(-6.6024257369623,4.36242279787988,-33.5434638257227));
#76154=CARTESIAN_POINT('Ctrl Pts',(-6.491693306939,4.52555241994048,-33.5513614294039));
#76155=CARTESIAN_POINT('Ctrl Pts',(-6.37508079460592,4.68425723698504,-33.5592590330851));
#76156=CARTESIAN_POINT('Ctrl Pts',(-6.25842279971076,4.84302395391966,-33.5671597170812));
#76157=CARTESIAN_POINT('Ctrl Pts',(-6.13588035452739,4.99736215080486,-33.5750604010772));
#76158=CARTESIAN_POINT('Ctrl Pts',(-6.00783581806122,5.14682715692112,-33.5829610850732));
#76159=CARTESIAN_POINT('Ctrl Pts',(-5.87965071696043,5.29645624261899,-33.5908704422762));
#76160=CARTESIAN_POINT('Ctrl Pts',(-5.74595168043331,5.44120118966321,-33.5987797994791));
#76161=CARTESIAN_POINT('Ctrl Pts',(-5.60715925335904,5.58065283882362,-33.606689156682));
#76162=CARTESIAN_POINT('Ctrl Pts',(-5.46828419008667,5.72018751667909,-33.6146032230699));
#76163=CARTESIAN_POINT('Ctrl Pts',(-5.32430993930035,5.85442237952135,-33.6225172894578));
#76164=CARTESIAN_POINT('Ctrl Pts',(-5.1756908903522,5.98298794980612,-33.6304313558457));
#76165=CARTESIAN_POINT('Ctrl Pts',(-5.02686440403994,6.11173296749824,-33.6383564684156));
#76166=CARTESIAN_POINT('Ctrl Pts',(-4.87338043208956,6.23479266745573,-33.6462815809855));
#76167=CARTESIAN_POINT('Ctrl Pts',(-4.71572425983158,6.35183955285679,-33.6542066935555));
#76168=CARTESIAN_POINT('Ctrl Pts',(-4.60673677950182,6.43275389282588,-33.6596853122353));
#76169=CARTESIAN_POINT('Ctrl Pts',(-4.49575603825922,6.51079565603233,-33.6651639309152));
#76170=CARTESIAN_POINT('Ctrl Pts',(-4.38294931482201,6.5858694417443,-33.6706425495951));
#76171=CARTESIAN_POINT('Ctrl Pts',(-4.21565374072506,6.69720599773693,-33.6787674966672));
#76172=CARTESIAN_POINT('Ctrl Pts',(-4.04397423338339,6.80225710806551,-33.6868924437393));
#76173=CARTESIAN_POINT('Ctrl Pts',(-3.86841141753026,6.90067490211802,-33.6950173908114));
#76174=CARTESIAN_POINT('Ctrl Pts',(-3.69300332412921,6.99900596116147,-33.7031351774165));
#76175=CARTESIAN_POINT('Ctrl Pts',(-3.51371902384952,7.09071520313219,-33.7112529640217));
#76176=CARTESIAN_POINT('Ctrl Pts',(-3.33108747943779,7.17549839414189,-33.7193707506269));
#76177=CARTESIAN_POINT('Ctrl Pts',(-3.14859091122309,7.26021892504141,-33.7274825376773));
#76178=CARTESIAN_POINT('Ctrl Pts',(-2.96275232132562,7.3380234769545,-33.7355943247276));
#76179=CARTESIAN_POINT('Ctrl Pts',(-2.77412510792397,7.40865378362262,-33.743706111778));
#76180=CARTESIAN_POINT('Ctrl Pts',(-2.58561050891936,7.47924192251838,-33.7518130559216));
#76181=CARTESIAN_POINT('Ctrl Pts',(-2.39431090591447,7.54266424523087,-33.7599200000652));
#76182=CARTESIAN_POINT('Ctrl Pts',(-2.20080003875554,7.59871042936982,-33.7680269442088));
#76183=CARTESIAN_POINT('Ctrl Pts',(-2.00737724493054,7.65473110499669,-33.7761301986082));
#76184=CARTESIAN_POINT('Ctrl Pts',(-1.81174550159248,7.70338224834809,-33.7842334530076));
#76185=CARTESIAN_POINT('Ctrl Pts',(-1.61449463763728,7.7445030870315,-33.792336707407));
#76186=CARTESIAN_POINT('Ctrl Pts',(-1.41586911157071,7.7859105011843,-33.8004964342425));
#76187=CARTESIAN_POINT('Ctrl Pts',(-1.21560212248025,7.81968214425426,-33.8086561610779));
#76188=CARTESIAN_POINT('Ctrl Pts',(-1.01430848775576,7.8457057867133,-33.8168158879134));
#76189=CARTESIAN_POINT('Ctrl Pts',(-0.814483563081723,7.87153955140854,
-33.8249160784758));
#76190=CARTESIAN_POINT('Ctrl Pts',(-0.613647249258924,7.88973798165448,
-33.8330162690381));
#76191=CARTESIAN_POINT('Ctrl Pts',(-0.41240856183088,7.90024304550997,-33.8411164596004));
#76192=CARTESIAN_POINT('Ctrl Pts',(-0.211171074422902,7.91074804672199,
-33.84921660186));
#76193=CARTESIAN_POINT('Ctrl Pts',(-0.00953153840357959,7.9135597564478,
-33.8573167441196));
#76194=CARTESIAN_POINT('Ctrl Pts',(0.191898302812708,7.90867220469894,-33.8654168863791));
#76195=CARTESIAN_POINT('Ctrl Pts',(0.393352921797685,7.90378405173516,-33.8735180250325));
#76196=CARTESIAN_POINT('Ctrl Pts',(0.594597474016501,7.8911947568253,-33.8816191636859));
#76197=CARTESIAN_POINT('Ctrl Pts',(0.795022058686897,7.87095044617874,-33.8897203023393));
#76198=CARTESIAN_POINT('Ctrl Pts',(0.997995276040814,7.85044870547761,-33.8979244564325));
#76199=CARTESIAN_POINT('Ctrl Pts',(1.20012719317032,7.82209596204581,-33.9061286105257));
#76200=CARTESIAN_POINT('Ctrl Pts',(1.40079152651456,7.78599409833099,-33.914332764619));
#76201=CARTESIAN_POINT('Ctrl Pts',(1.59912497581198,7.75031158795511,-33.9224416206013));
#76202=CARTESIAN_POINT('Ctrl Pts',(1.79602444336803,7.70705911654199,-33.9305504765836));
#76203=CARTESIAN_POINT('Ctrl Pts',(1.99089693392044,7.65638624930236,-33.9386593325659));
#76204=CARTESIAN_POINT('Ctrl Pts',(2.18920473894702,7.60482009418108,-33.9469111357146));
#76205=CARTESIAN_POINT('Ctrl Pts',(2.3854131010413,7.5455695796454,-33.9551629388633));
#76206=CARTESIAN_POINT('Ctrl Pts',(2.57891442908054,7.47884492201036,-33.963414742012));
#76207=CARTESIAN_POINT('Ctrl Pts',(2.77241575711979,7.41212026437533,-33.9716665451607));
#76208=CARTESIAN_POINT('Ctrl Pts',(2.96320973631898,7.33792161416906,-33.9799183483094));
#76209=CARTESIAN_POINT('Ctrl Pts',(3.1507110563056,7.25651023837724,-33.988170151458));
#76210=CARTESIAN_POINT('Ctrl Pts',(3.32861845617368,7.1792644558524,-33.9959997328312));
#76211=CARTESIAN_POINT('Ctrl Pts',(3.50390141623488,7.0953774368945,-34.0038293142043));
#76212=CARTESIAN_POINT('Ctrl Pts',(3.67602498412764,7.00505255626747,-34.0116588955775));
#76213=CARTESIAN_POINT('Ctrl Pts',(3.84800345053782,6.91480382020479,-34.0194818765537));
#76214=CARTESIAN_POINT('Ctrl Pts',(4.01682751842343,6.81812819118313,-34.0273048575299));
#76215=CARTESIAN_POINT('Ctrl Pts',(4.18198202198616,6.71527716239506,-34.0351278385061));
#76216=CARTESIAN_POINT('Ctrl Pts',(4.3470264368443,6.61249469205547,-34.042945604839));
#76217=CARTESIAN_POINT('Ctrl Pts',(4.5084058612547,6.50354520522174,-34.0507633711718));
#76218=CARTESIAN_POINT('Ctrl Pts',(4.66562943363786,6.3887262414328,-34.0585811375046));
#76219=CARTESIAN_POINT('Ctrl Pts',(4.8227776502318,6.27396230930038,-34.0663951568551));
#76220=CARTESIAN_POINT('Ctrl Pts',(4.9757736987484,6.15333471093492,-34.0742091762056));
#76221=CARTESIAN_POINT('Ctrl Pts',(5.12415530071364,6.02718453792219,-34.0820231955561));
#76222=CARTESIAN_POINT('Ctrl Pts',(5.2724936858831,5.90107110670354,-34.0898349390389));
#76223=CARTESIAN_POINT('Ctrl Pts',(5.41622003437488,5.7694385334315,-34.0976466825218));
#76224=CARTESIAN_POINT('Ctrl Pts',(5.55490466639366,5.63266856359203,-34.1054584260047));
#76225=CARTESIAN_POINT('Ctrl Pts',(5.69359705521876,5.49589094403571,-34.1132706064082));
#76226=CARTESIAN_POINT('Ctrl Pts',(5.82724690900963,5.35397559648287,-34.1210827868118));
#76227=CARTESIAN_POINT('Ctrl Pts',(5.95546067679407,5.20734184850193,-34.1288949672153));
#76228=CARTESIAN_POINT('Ctrl Pts',(6.05414615411811,5.09447860720291,-34.1349079622734));
#76229=CARTESIAN_POINT('Ctrl Pts',(6.14961183275785,4.97882083627733,-34.1409209573315));
#76230=CARTESIAN_POINT('Ctrl Pts',(6.24169422609106,4.86057344229892,-34.1469339523896));
#76231=CARTESIAN_POINT('Ctrl Pts',(6.3740004302427,4.69067273401156,-34.1555735687475));
#76232=CARTESIAN_POINT('Ctrl Pts',(6.49925809951242,4.51550597958778,-34.1642131851054));
#76233=CARTESIAN_POINT('Ctrl Pts',(6.61709513949074,4.33566291527928,-34.1728528014633));
#76234=CARTESIAN_POINT('Ctrl Pts',(6.73512729736257,4.15552206175378,-34.1815067235416));
#76235=CARTESIAN_POINT('Ctrl Pts',(6.84571413915423,3.97068961318091,-34.1901606456199));
#76236=CARTESIAN_POINT('Ctrl Pts',(6.94852858857239,3.7817815185164,-34.1988145676982));
#76237=CARTESIAN_POINT('Ctrl Pts',(7.05434896865036,3.58735041967443,-34.2077214998334));
#76238=CARTESIAN_POINT('Ctrl Pts',(7.15193551328766,3.38860201701987,-34.2166284319687));
#76239=CARTESIAN_POINT('Ctrl Pts',(7.24098472058632,3.18622994716882,-34.2255353641039));
#76240=CARTESIAN_POINT('Ctrl Pts',(7.3277931626481,2.98895021123961,-34.234218169102));
#76241=CARTESIAN_POINT('Ctrl Pts',(7.40648867438301,2.78822718812726,-34.2429009741001));
#76242=CARTESIAN_POINT('Ctrl Pts',(7.47684031378366,2.58472047273578,-34.2515837790982));
#76243=CARTESIAN_POINT('Ctrl Pts',(7.54991590786283,2.37333415319829,-34.260602774802));
#76244=CARTESIAN_POINT('Ctrl Pts',(7.61398857970821,2.15894456789642,-34.2696217705058));
#76245=CARTESIAN_POINT('Ctrl Pts',(7.66885700350564,1.94230617045371,-34.2786407662096));
#76246=CARTESIAN_POINT('Ctrl Pts',(7.72372542730307,1.72566777301096,-34.2876597619135));
#76247=CARTESIAN_POINT('Ctrl Pts',(7.7693895660935,1.50678083725419,-34.2966787576173));
#76248=CARTESIAN_POINT('Ctrl Pts',(7.80570733587141,1.28641128210356,-34.3056977533211));
#76249=CARTESIAN_POINT('Ctrl Pts',(7.83921870685186,1.08307043929824,-34.3140198202528));
#76250=CARTESIAN_POINT('Ctrl Pts',(7.86480069827297,0.87829489340369,-34.3223418871845));
#76251=CARTESIAN_POINT('Ctrl Pts',(7.88234581788412,0.672714952475907,-34.3306639541162));
#76252=CARTESIAN_POINT('Ctrl Pts',(7.89987537251337,0.467317389789561,-34.3389786382073));
#76253=CARTESIAN_POINT('Ctrl Pts',(7.90938225381209,0.261117145926104,-34.3472933222984));
#76254=CARTESIAN_POINT('Ctrl Pts',(7.91081053168458,0.0547515459911957,
-34.3556080063895));
#76255=CARTESIAN_POINT('Ctrl Pts',(7.91223762948737,-0.151443550854259,
-34.3639158207342));
#76256=CARTESIAN_POINT('Ctrl Pts',(7.90559943770837,-0.357803439669933,
-34.372223635079));
#76257=CARTESIAN_POINT('Ctrl Pts',(7.89089201610962,-0.56368802550476,-34.3805314494238));
#76258=CARTESIAN_POINT('Ctrl Pts',(7.87619938308761,-0.769365590688492,
-34.3888309101119));
#76259=CARTESIAN_POINT('Ctrl Pts',(7.85345373671981,-0.974568515980631,
-34.3971303708));
#76260=CARTESIAN_POINT('Ctrl Pts',(7.82270316128366,-1.17865866579036,-34.4054298314882));
#76261=CARTESIAN_POINT('Ctrl Pts',(7.79197217499952,-1.38261880330231,-34.4137240051404));
#76262=CARTESIAN_POINT('Ctrl Pts',(7.75324647473878,-1.58546729094061,-34.4220181787926));
#76263=CARTESIAN_POINT('Ctrl Pts',(7.70662590542911,-1.78657162010622,-34.4303123524448));
#76264=CARTESIAN_POINT('Ctrl Pts',(7.66003976396481,-1.98752743995822,-34.4386004011068));
#76265=CARTESIAN_POINT('Ctrl Pts',(7.6055704552009,-2.18674138772235,-34.4468884497689));
#76266=CARTESIAN_POINT('Ctrl Pts',(7.54336890415005,-2.38359110920941,-34.455176498431));
#76267=CARTESIAN_POINT('Ctrl Pts',(7.5201408844132,-2.45710099985758,-34.4582715170382));
#76268=CARTESIAN_POINT('Ctrl Pts',(7.49583510457647,-2.5302813062398,-34.4613665356454));
#76269=CARTESIAN_POINT('Ctrl Pts',(7.47046123679272,-2.60310005754241,-34.4644615542527));
#76270=CARTESIAN_POINT('Ctrl Pts',(7.40402955775045,-2.79374785140743,-34.4725646658673));
#76271=CARTESIAN_POINT('Ctrl Pts',(7.33030093350632,-2.98183622350412,-34.4806677774819));
#76272=CARTESIAN_POINT('Ctrl Pts',(7.24950513986053,-3.16679589287591,-34.4887708890966));
#76273=CARTESIAN_POINT('Ctrl Pts',(7.16869151826189,-3.35179637442511,-34.496875788699));
#76274=CARTESIAN_POINT('Ctrl Pts',(7.08080774480915,-3.53366648421667,-34.5049806883014));
#76275=CARTESIAN_POINT('Ctrl Pts',(6.98613099298384,-3.71185866499125,-34.5130855879038));
#76276=CARTESIAN_POINT('Ctrl Pts',(6.891421492952,-3.89011248153413,-34.5211932909497));
#76277=CARTESIAN_POINT('Ctrl Pts',(6.78991447785789,-4.06468555036316,-34.5293009939957));
#76278=CARTESIAN_POINT('Ctrl Pts',(6.681932430106,-4.23505607985275,-34.5374086970416));
#76279=CARTESIAN_POINT('Ctrl Pts',(6.57385324528844,-4.40557986901518,-34.545523693508));
#76280=CARTESIAN_POINT('Ctrl Pts',(6.45928755908311,-4.57189329479687,-34.5536386899745));
#76281=CARTESIAN_POINT('Ctrl Pts',(6.33860120130483,-4.73350354503057,-34.5617536864409));
#76282=CARTESIAN_POINT('Ctrl Pts',(6.21785592373628,-4.89519269433973,-34.5698726446964));
#76283=CARTESIAN_POINT('Ctrl Pts',(6.09098421019588,-5.05217383686884,-34.5779916029519));
#76284=CARTESIAN_POINT('Ctrl Pts',(5.95839192175607,-5.20398757749785,-34.5861105612074));
#76285=CARTESIAN_POINT('Ctrl Pts',(5.82565764019086,-5.35596389551176,-34.594238214058));
#76286=CARTESIAN_POINT('Ctrl Pts',(5.68719075730522,-5.50276151854457,-34.6023658669085));
#76287=CARTESIAN_POINT('Ctrl Pts',(5.54343466601592,-5.64395722021465,-34.6104935197591));
#76288=CARTESIAN_POINT('Ctrl Pts',(5.46837080976693,-5.71768414029212,-34.6147374649008));
#76289=CARTESIAN_POINT('Ctrl Pts',(5.39186541572526,-5.78988432594594,-34.6189814100425));
#76290=CARTESIAN_POINT('Ctrl Pts',(5.31398519266527,-5.86050188739277,-34.6232253551842));
#76291=CARTESIAN_POINT('Ctrl Pts',(5.1672010367998,-5.99359779722687,-34.6312240983912));
#76292=CARTESIAN_POINT('Ctrl Pts',(5.01527727034038,-6.12129953400736,-34.6392228415982));
#76293=CARTESIAN_POINT('Ctrl Pts',(4.85864342064975,-6.24319670609352,-34.6472215848053));
#76294=CARTESIAN_POINT('Ctrl Pts',(4.7021371486678,-6.36499459337029,-34.6552138130646));
#76295=CARTESIAN_POINT('Ctrl Pts',(4.54092870148769,-6.48099713351476,-34.663206041324));
#76296=CARTESIAN_POINT('Ctrl Pts',(4.37548239689503,-6.59083263286679,-34.6711982695834));
#76297=CARTESIAN_POINT('Ctrl Pts',(4.2101428243874,-6.70059727556302,-34.6791853419272));
#76298=CARTESIAN_POINT('Ctrl Pts',(4.04057112114329,-6.80420262255289,-34.6871724142709));
#76299=CARTESIAN_POINT('Ctrl Pts',(3.86726277319624,-6.90131868870367,-34.6951594866147));
#76300=CARTESIAN_POINT('Ctrl Pts',(3.69403688698755,-6.99838854611879,-34.7031427586345));
#76301=CARTESIAN_POINT('Ctrl Pts',(3.51707819126993,-7.0889751142768,-34.7111260306543));
#76302=CARTESIAN_POINT('Ctrl Pts',(3.33690945627348,-7.17279278110226,-34.7191093026741));
#76303=CARTESIAN_POINT('Ctrl Pts',(3.15679595362462,-7.25658475286742,-34.7270901273499));
#76304=CARTESIAN_POINT('Ctrl Pts',(2.97347467648266,-7.33361181932799,-34.7350709520258));
#76305=CARTESIAN_POINT('Ctrl Pts',(2.78749156648602,-7.40363503738328,-34.7430517767017));
#76306=CARTESIAN_POINT('Ctrl Pts',(2.59552581386482,-7.47591073895201,-34.7512893258828));
#76307=CARTESIAN_POINT('Ctrl Pts',(2.40072446071612,-7.54072432977293,-34.7595268750638));
#76308=CARTESIAN_POINT('Ctrl Pts',(2.20370913556884,-7.59786726955732,-34.7677644242449));
#76309=CARTESIAN_POINT('Ctrl Pts',(2.01280776602208,-7.65323689857788,-34.7757463384396));
#76310=CARTESIAN_POINT('Ctrl Pts',(1.81982811947343,-7.70140475138358,-34.7837282526344));
#76311=CARTESIAN_POINT('Ctrl Pts',(1.62535020896077,-7.74223208759794,-34.7917101668291));
#76312=CARTESIAN_POINT('Ctrl Pts',(1.43082906059342,-7.78306850086597,-34.7996938556256));
#76313=CARTESIAN_POINT('Ctrl Pts',(1.23480931164135,-7.81656107490002,-34.8076775444222));
#76314=CARTESIAN_POINT('Ctrl Pts',(1.03788068041415,-7.84262230973946,-34.8156612332187));
#76315=CARTESIAN_POINT('Ctrl Pts',(0.840878029161418,-7.86869334027623,
-34.823647922863));
#76316=CARTESIAN_POINT('Ctrl Pts',(0.642966146148042,-7.88732741907902,
-34.8316346125073));
#76317=CARTESIAN_POINT('Ctrl Pts',(0.444739757187343,-7.89848894082767,
-34.8396213021516));
#76318=CARTESIAN_POINT('Ctrl Pts',(0.246408418496715,-7.90965637197465,
-34.8476122202991));
#76319=CARTESIAN_POINT('Ctrl Pts',(0.0477625754923947,-7.91334333987846,
-34.8556031384466));
#76320=CARTESIAN_POINT('Ctrl Pts',(-0.150602776180313,-7.90956634739268,
-34.8635940565941));
#76321=CARTESIAN_POINT('Ctrl Pts',(-0.349202406596975,-7.90578489410239,
-34.8715944123892));
#76322=CARTESIAN_POINT('Ctrl Pts',(-0.547520549466926,-7.89452187716758,
-34.8795947681842));
#76323=CARTESIAN_POINT('Ctrl Pts',(-0.744965795211754,-7.87584579356176,
-34.8875951239792));
#76324=CARTESIAN_POINT('Ctrl Pts',(-0.942549022385511,-7.85715665847581,
-34.895601070694));
#76325=CARTESIAN_POINT('Ctrl Pts',(-1.13925780523297,-7.83104416842073,
-34.9036070174088));
#76326=CARTESIAN_POINT('Ctrl Pts',(-1.33451015342385,-7.79762807848699,
-34.9116129641235));
#76327=CARTESIAN_POINT('Ctrl Pts',(-1.53001583349051,-7.76416863255358,
-34.9196292982243));
#76328=CARTESIAN_POINT('Ctrl Pts',(-1.72406097825754,-7.72338672726847,
-34.927645632325));
#76329=CARTESIAN_POINT('Ctrl Pts',(-1.91607686706567,-7.67545245829168,
-34.9356619664257));
#76330=CARTESIAN_POINT('Ctrl Pts',(-1.95672516826432,-7.66530513863392,
-34.9373589632995));
#76331=CARTESIAN_POINT('Ctrl Pts',(-1.99728259619836,-7.65483746958424,
-34.9390559601734));
#76332=CARTESIAN_POINT('Ctrl Pts',(-2.03774386542381,-7.64405134329484,
-34.9407529570472));
#76333=CARTESIAN_POINT('Ctrl Pts',(-2.22281949725187,-7.59471405911662,
-34.9485152634367));
#76334=CARTESIAN_POINT('Ctrl Pts',(-2.40642961687235,-7.53856386645909,
-34.9562775698263));
#76335=CARTESIAN_POINT('Ctrl Pts',(-2.58802145964085,-7.47569835697231,
-34.9640398762158));
#76336=CARTESIAN_POINT('Ctrl Pts',(-2.76939332553528,-7.41290900155749,
-34.9717927794963));
#76337=CARTESIAN_POINT('Ctrl Pts',(-2.94875144641187,-7.34342063688923,
-34.9795456827767));
#76338=CARTESIAN_POINT('Ctrl Pts',(-3.1255531471949,-7.26738182043988,-34.9872985860572));
#76339=CARTESIAN_POINT('Ctrl Pts',(-3.3021765357247,-7.19141969246487,-34.9950436701955));
#76340=CARTESIAN_POINT('Ctrl Pts',(-3.47624831006344,-7.1089204044593,-35.0027887543336));
#76341=CARTESIAN_POINT('Ctrl Pts',(-3.64724077777109,-7.02008231497065,
-35.0105338384719));
#76342=CARTESIAN_POINT('Ctrl Pts',(-3.81809542507101,-6.93131582923087,
-35.0182726800506));
#76343=CARTESIAN_POINT('Ctrl Pts',(-3.98587539060148,-6.83622087845153,
-35.0260115216293));
#76344=CARTESIAN_POINT('Ctrl Pts',(-4.15007272156713,-6.73504397949296,
-35.033750363208));
#76345=CARTESIAN_POINT('Ctrl Pts',(-4.31417093125197,-6.6339281581643,-35.0414845330671));
#76346=CARTESIAN_POINT('Ctrl Pts',(-4.47469050846732,-6.52673788722465,
-35.0492187029262));
#76347=CARTESIAN_POINT('Ctrl Pts',(-4.63114781367576,-6.4137657369042,-35.0569528727853));
#76348=CARTESIAN_POINT('Ctrl Pts',(-4.78754230384056,-6.30083894305044,
-35.064683937502));
#76349=CARTESIAN_POINT('Ctrl Pts',(-4.9398774798041,-6.1821351029284,-35.0724150022187));
#76350=CARTESIAN_POINT('Ctrl Pts',(-5.087698360072,-6.05799029356441,-35.0801460669354));
#76351=CARTESIAN_POINT('Ctrl Pts',(-5.23551709374356,-5.93384728698225,
-35.0878770193846));
#76352=CARTESIAN_POINT('Ctrl Pts',(-5.37882138040632,-5.80426369085599,
-35.0956079718338));
#76353=CARTESIAN_POINT('Ctrl Pts',(-5.51718873845376,-5.66961633836708,
-35.103338924283));
#76354=CARTESIAN_POINT('Ctrl Pts',(-5.65556190053407,-5.5349633378867,-35.111070201019));
#76355=CARTESIAN_POINT('Ctrl Pts',(-5.78899746349417,-5.39524640787177,
-35.118801477755));
#76356=CARTESIAN_POINT('Ctrl Pts',(-5.91710942029829,-5.25087965089824,
-35.1265327544909));
#76357=CARTESIAN_POINT('Ctrl Pts',(-6.04525020969944,-5.10648040305787,
-35.1342657712112));
#76358=CARTESIAN_POINT('Ctrl Pts',(-6.16806476860649,-4.95742951284821,
-35.1419987879314));
#76359=CARTESIAN_POINT('Ctrl Pts',(-6.28520700946487,-4.80417462715227,
-35.1497318046516));
#76360=CARTESIAN_POINT('Ctrl Pts',(-6.40239707075277,-4.65085717893059,
-35.1574679781851));
#76361=CARTESIAN_POINT('Ctrl Pts',(-6.5139099852212,-4.49333260282782,-35.1652041517186));
#76362=CARTESIAN_POINT('Ctrl Pts',(-6.61944263944751,-4.33207803981694,
-35.1729403252521));
#76363=CARTESIAN_POINT('Ctrl Pts',(-6.72509929089872,-4.17063400826229,
-35.1806855885224));
#76364=CARTESIAN_POINT('Ctrl Pts',(-6.8247614526579,-4.00545153773251,-35.1884308517927));
#76365=CARTESIAN_POINT('Ctrl Pts',(-6.91817118187755,-3.83703381510237,
-35.196176115063));
#76366=CARTESIAN_POINT('Ctrl Pts',(-7.01164085633237,-3.66850801122551,
-35.2039263488179));
#76367=CARTESIAN_POINT('Ctrl Pts',(-7.09884994372007,-3.49674313833837,
-35.2116765825729));
#76368=CARTESIAN_POINT('Ctrl Pts',(-7.17958848754662,-3.32226280560224,
-35.2194268163279));
#76369=CARTESIAN_POINT('Ctrl Pts',(-7.26044862395376,-3.14751970476409,
-35.2271887219669));
#76370=CARTESIAN_POINT('Ctrl Pts',(-7.33481861693578,-2.9700533062728,-35.2349506276059));
#76371=CARTESIAN_POINT('Ctrl Pts',(-7.40253786009505,-2.79040395460218,
-35.2427125332449));
#76372=CARTESIAN_POINT('Ctrl Pts',(-7.44781260595259,-2.67029660607155,
-35.2479018751334));
#76373=CARTESIAN_POINT('Ctrl Pts',(-7.49011564425207,-2.54921381182251,
-35.2530912170218));
#76374=CARTESIAN_POINT('Ctrl Pts',(-7.52941175312994,-2.42731943753368,
-35.2582805589102));
#76375=CARTESIAN_POINT('Ctrl Pts',(-7.60583955379658,-2.19024459204487,
-35.2683734153981));
#76376=CARTESIAN_POINT('Ctrl Pts',(-7.67108903170758,-1.94948830154461,
-35.278466271886));
#76377=CARTESIAN_POINT('Ctrl Pts',(-7.72486690969569,-1.70597544750463,
-35.2885591283739));
#76378=CARTESIAN_POINT('Ctrl Pts',(-7.77818830022531,-1.46452962489109,
-35.2985663127866));
#76379=CARTESIAN_POINT('Ctrl Pts',(-7.82023202030717,-1.22037366359654,
-35.3085734971994));
#76380=CARTESIAN_POINT('Ctrl Pts',(-7.85075827923368,-0.974430829276153,
-35.3185806816121));
#76381=CARTESIAN_POINT('Ctrl Pts',(-7.8807546520397,-0.732757161860744,
-35.3284141576075));
#76382=CARTESIAN_POINT('Ctrl Pts',(-7.89962993631264,-0.489357991626549,
-35.3382476336029));
#76383=CARTESIAN_POINT('Ctrl Pts',(-7.90720121262665,-0.245132582566322,
-35.3480811095982));
#76384=CARTESIAN_POINT('Ctrl Pts',(-7.90966180182129,-0.165761763477523,
-35.3512768910988));
#76385=CARTESIAN_POINT('Ctrl Pts',(-7.91092883589041,-0.0863038717799649,
-35.3544726725994));
#76386=CARTESIAN_POINT('Ctrl Pts',(-7.91099708577542,-0.00679034998251756,
-35.3576684541));
#76387=CARTESIAN_POINT('',(-7.90050494756768,0.00579114955300497,-37.357668491763));
#76388=CARTESIAN_POINT('Ctrl Pts',(-7.90525032249359,-0.00678448088220818,
-35.357668491763));
#76389=CARTESIAN_POINT('Ctrl Pts',(-7.88783545099137,1.80107895371635,-35.4303817147664));
#76390=CARTESIAN_POINT('Ctrl Pts',(-6.8135975783561,4.939319079492,-35.556016204747));
#76391=CARTESIAN_POINT('Ctrl Pts',(-3.10734150823737,7.61713964008616,-35.7345719617048));
#76392=CARTESIAN_POINT('Ctrl Pts',(2.28026636839026,8.42190983339215,-35.9462570296134));
#76393=CARTESIAN_POINT('Ctrl Pts',(7.12946490356375,5.02602867964289,-36.1579420975222));
#76394=CARTESIAN_POINT('Ctrl Pts',(8.22864524405818,-0.318974158456952,
-36.3696271654307));
#76395=CARTESIAN_POINT('Ctrl Pts',(7.09460005342516,-4.21538026514994,-36.5283909663624));
#76396=CARTESIAN_POINT('Ctrl Pts',(4.20751149604049,-7.07879035645357,-36.6871547672938));
#76397=CARTESIAN_POINT('Ctrl Pts',(-0.999622714554145,-8.66070382201061,
-36.8988398352026));
#76398=CARTESIAN_POINT('Ctrl Pts',(-6.62226577165369,-5.88434235214676,
-37.1223444100256));
#76399=CARTESIAN_POINT('Ctrl Pts',(-7.89111861597513,-1.61068309120649,
-37.2929277178714));
#76400=CARTESIAN_POINT('Ctrl Pts',(-7.90050494756768,0.00579114955300497,
-37.357668491763));
#76401=CARTESIAN_POINT('',(-7.92255110667597,0.00112620878001013,-39.357668491763));
#76402=CARTESIAN_POINT('Ctrl Pts',(-7.90050494756768,0.00579114955300497,
-37.357668491763));
#76403=CARTESIAN_POINT('Ctrl Pts',(-7.90646401672607,1.03203678113555,-37.3987702518258));
#76404=CARTESIAN_POINT('Ctrl Pts',(-7.24737305659377,4.69309146320393,-37.5457145458429));
#76405=CARTESIAN_POINT('Ctrl Pts',(-2.87855582146927,8.22911730782232,-37.7455801068374));
#76406=CARTESIAN_POINT('Ctrl Pts',(2.52742786906601,7.82869694853837,-37.9572651747459));
#76407=CARTESIAN_POINT('Ctrl Pts',(7.16765417016174,4.97523000971477,-38.1689502426547));
#76408=CARTESIAN_POINT('Ctrl Pts',(8.69106246208229,-0.745431002793219,
-38.3806353105634));
#76409=CARTESIAN_POINT('Ctrl Pts',(6.09028077099974,-5.54263720594378,-38.5923203784721));
#76410=CARTESIAN_POINT('Ctrl Pts',(2.71365595713207,-7.79351345955097,-38.7510841794036));
#76411=CARTESIAN_POINT('Ctrl Pts',(-1.33904198433904,-8.12523184063725,
-38.9098479803352));
#76412=CARTESIAN_POINT('Ctrl Pts',(-6.1173318547664,-6.07862255922375,-39.1120427511214));
#76413=CARTESIAN_POINT('Ctrl Pts',(-7.90693077504529,-2.3808942637658,-39.2613162549308));
#76414=CARTESIAN_POINT('Ctrl Pts',(-7.92255110667597,0.00112620878001013,
-39.357668491763));
#76415=CARTESIAN_POINT('',(-7.90690567208597,-0.00336307952236492,-41.357668491763));
#76416=CARTESIAN_POINT('Ctrl Pts',(-7.92255110667597,0.00112620878001013,
-39.357668491763));
#76417=CARTESIAN_POINT('Ctrl Pts',(-7.92408964478569,0.23574538088166,-39.3671587888852));
#76418=CARTESIAN_POINT('Ctrl Pts',(-7.8084390703918,3.08644196615606,-39.4824916199614));
#76419=CARTESIAN_POINT('Ctrl Pts',(-4.34320070494277,8.2922938225927,-39.7036669849931));
#76420=CARTESIAN_POINT('Ctrl Pts',(3.0965349810775,8.14959670132102,-39.9682733198783));
#76421=CARTESIAN_POINT('Ctrl Pts',(6.97477370654661,4.36221495204592,-40.1799583877874));
#76422=CARTESIAN_POINT('Ctrl Pts',(8.68757048396973,-0.808887531523498,
-40.3916434556958));
#76423=CARTESIAN_POINT('Ctrl Pts',(6.16946845661581,-6.16667601407484,-40.6033285236047));
#76424=CARTESIAN_POINT('Ctrl Pts',(1.09061100012035,-8.16228612048976,-40.8150135915134));
#76425=CARTESIAN_POINT('Ctrl Pts',(-2.94220442932188,-7.71013708010145,
-40.9737773924447));
#76426=CARTESIAN_POINT('Ctrl Pts',(-6.25649344662526,-5.35431747772463,
-41.1325411933765));
#76427=CARTESIAN_POINT('Ctrl Pts',(-7.73613906322107,-2.41608628745108,
-41.2605048931491));
#76428=CARTESIAN_POINT('Ctrl Pts',(-7.91192326830252,-0.553012152266311,
-41.3355473259446));
#76429=CARTESIAN_POINT('Ctrl Pts',(-7.90690567208597,-0.00336307952236492,
-41.357668491763));
#76430=CARTESIAN_POINT('',(-7.9079676034592,-0.00146772438904264,-43.357668491763));
#76431=CARTESIAN_POINT('Ctrl Pts',(-7.90690567208597,-0.00336307952236492,
-41.357668491763));
#76432=CARTESIAN_POINT('Ctrl Pts',(-7.88791571362478,2.07687865559345,-41.4413898598989));
#76433=CARTESIAN_POINT('Ctrl Pts',(-6.00161559860685,6.8015463040485,-41.6309537619893));
#76434=CARTESIAN_POINT('Ctrl Pts',(2.0166268162176,9.14104728615705,-41.926360198034));
#76435=CARTESIAN_POINT('Ctrl Pts',(7.61682718247753,4.24127327055065,-42.1909665329198));
#76436=CARTESIAN_POINT('Ctrl Pts',(8.14526619226151,-1.15370108892476,-42.4026516008286));
#76437=CARTESIAN_POINT('Ctrl Pts',(6.1259358175118,-6.2129775721734,-42.614336668737));
#76438=CARTESIAN_POINT('Ctrl Pts',(0.74936559032438,-8.69072409594159,-42.8260217366459));
#76439=CARTESIAN_POINT('Ctrl Pts',(-4.42144418447609,-6.94717053122234,
-43.0377068045546));
#76440=CARTESIAN_POINT('Ctrl Pts',(-7.21577302375009,-4.00442260102508,
-43.1964706054861));
#76441=CARTESIAN_POINT('Ctrl Pts',(-7.90016440029126,-1.35993271260852,
-43.3031245012222));
#76442=CARTESIAN_POINT('Ctrl Pts',(-7.90792716545684,-0.0216761063237722,
-43.3568571299812));
#76443=CARTESIAN_POINT('Ctrl Pts',(-7.9079676034592,-0.00146772438904264,
-43.357668491763));
#76444=CARTESIAN_POINT('',(-7.911,-1.23234755733392E-13,-45.357668491763));
#76445=CARTESIAN_POINT('Ctrl Pts',(-7.911,-1.21014309684142E-13,-43.357668491763));
#76446=CARTESIAN_POINT('Ctrl Pts',(-7.91100000000004,2.20167589666662,-43.4462559274957));
#76447=CARTESIAN_POINT('Ctrl Pts',(-6.94214576672381,4.38610418338667,-43.5348433632284));
#76448=CARTESIAN_POINT('Ctrl Pts',(-3.67820201488307,7.34180684107621,-43.7120182346939));
#76449=CARTESIAN_POINT('Ctrl Pts',(-1.4086817587177,8.08992666571331,-43.8006056704266));
#76450=CARTESIAN_POINT('Ctrl Pts',(2.97309270521244,7.65454228025268,-43.977780541892));
#76451=CARTESIAN_POINT('Ctrl Pts',(5.05102072675574,6.47444880834247,-44.0663679776248));
#76452=CARTESIAN_POINT('Ctrl Pts',(7.66951518847856,2.93425195367744,-44.2435428490902));
#76453=CARTESIAN_POINT('Ctrl Pts',(8.18956872247067,0.601881960099604,-44.3321302848229));
#76454=CARTESIAN_POINT('Ctrl Pts',(7.32306689761364,-3.71537198232405,-44.5093051562884));
#76455=CARTESIAN_POINT('Ctrl Pts',(5.94329958850238,-5.66643518936472,-44.5978925920211));
#76456=CARTESIAN_POINT('Ctrl Pts',(2.16154501637904,-7.92205913232982,-44.7750674634866));
#76457=CARTESIAN_POINT('Ctrl Pts',(-0.210816529299753,-8.20894963713003,
-44.8636548992193));
#76458=CARTESIAN_POINT('Ctrl Pts',(-4.4212390857638,-6.91982244717867,-45.0408297706847));
#76459=CARTESIAN_POINT('Ctrl Pts',(-6.22631625634142,-5.35390358803574,
-45.1294172064175));
#76460=CARTESIAN_POINT('Ctrl Pts',(-7.65317280859476,-2.31334857514569,
-45.2645592586878));
#76461=CARTESIAN_POINT('Ctrl Pts',(-7.91099999999998,-1.15702837836551,
-45.3111138752254));
#76462=CARTESIAN_POINT('Ctrl Pts',(-7.911,-1.23234755733392E-13,-45.357668491763));
#76463=CARTESIAN_POINT('',(-7.911,-1.27675647831893E-14,-47.357668491763));
#76464=CARTESIAN_POINT('Ctrl Pts',(-7.911,-1.23234755733392E-13,-45.357668491763));
#76465=CARTESIAN_POINT('Ctrl Pts',(-7.91100000000004,2.20167589666662,-45.4462559274957));
#76466=CARTESIAN_POINT('Ctrl Pts',(-6.94214576672381,4.38610418338667,-45.5348433632284));
#76467=CARTESIAN_POINT('Ctrl Pts',(-3.67820201488307,7.34180684107621,-45.7120182346939));
#76468=CARTESIAN_POINT('Ctrl Pts',(-1.4086817587177,8.08992666571331,-45.8006056704266));
#76469=CARTESIAN_POINT('Ctrl Pts',(2.97309270521244,7.65454228025268,-45.977780541892));
#76470=CARTESIAN_POINT('Ctrl Pts',(5.05102072675574,6.47444880834247,-46.0663679776248));
#76471=CARTESIAN_POINT('Ctrl Pts',(7.66951518847856,2.93425195367745,-46.2435428490902));
#76472=CARTESIAN_POINT('Ctrl Pts',(8.18956872247067,0.601881960099607,-46.3321302848229));
#76473=CARTESIAN_POINT('Ctrl Pts',(7.32306689761365,-3.71537198232405,-46.5093051562884));
#76474=CARTESIAN_POINT('Ctrl Pts',(5.94329958850238,-5.66643518936472,-46.5978925920211));
#76475=CARTESIAN_POINT('Ctrl Pts',(2.16154501637904,-7.92205913232982,-46.7750674634866));
#76476=CARTESIAN_POINT('Ctrl Pts',(-0.210816529299751,-8.20894963713003,
-46.8636548992193));
#76477=CARTESIAN_POINT('Ctrl Pts',(-4.4212390857638,-6.91982244717867,-47.0408297706847));
#76478=CARTESIAN_POINT('Ctrl Pts',(-6.22631625634141,-5.35390358803574,
-47.1294172064175));
#76479=CARTESIAN_POINT('Ctrl Pts',(-7.65317280859478,-2.31334857514566,
-47.2645592586878));
#76480=CARTESIAN_POINT('Ctrl Pts',(-7.911,-1.15702837836543,-47.3111138752254));
#76481=CARTESIAN_POINT('Ctrl Pts',(-7.911,-1.27675647831893E-14,-47.357668491763));
#76482=CARTESIAN_POINT('',(-7.911,-1.49880108324396E-14,-49.357668491763));
#76483=CARTESIAN_POINT('Ctrl Pts',(-7.911,-1.27675647831893E-14,-47.357668491763));
#76484=CARTESIAN_POINT('Ctrl Pts',(-7.911,2.20167589666671,-47.4462559274957));
#76485=CARTESIAN_POINT('Ctrl Pts',(-6.94214576672376,4.38610418338673,-47.5348433632284));
#76486=CARTESIAN_POINT('Ctrl Pts',(-3.67820201488303,7.34180684107622,-47.7120182346939));
#76487=CARTESIAN_POINT('Ctrl Pts',(-1.40868175871768,8.08992666571331,-47.8006056704266));
#76488=CARTESIAN_POINT('Ctrl Pts',(2.97309270521242,7.65454228025268,-47.977780541892));
#76489=CARTESIAN_POINT('Ctrl Pts',(5.05102072675571,6.47444880834249,-48.0663679776248));
#76490=CARTESIAN_POINT('Ctrl Pts',(7.66951518847853,2.93425195367752,-48.2435428490902));
#76491=CARTESIAN_POINT('Ctrl Pts',(8.18956872247066,0.601881960099707,-48.3321302848229));
#76492=CARTESIAN_POINT('Ctrl Pts',(7.3230668976137,-3.71537198232393,-48.5093051562884));
#76493=CARTESIAN_POINT('Ctrl Pts',(5.94329958850248,-5.6664351893646,-48.5978925920211));
#76494=CARTESIAN_POINT('Ctrl Pts',(2.16154501637922,-7.92205913232976,-48.7750674634866));
#76495=CARTESIAN_POINT('Ctrl Pts',(-0.210816529299534,-8.20894963713003,
-48.8636548992193));
#76496=CARTESIAN_POINT('Ctrl Pts',(-4.42123908576359,-6.9198224471788,-49.0408297706847));
#76497=CARTESIAN_POINT('Ctrl Pts',(-6.22631625634123,-5.35390358803594,
-49.1294172064175));
#76498=CARTESIAN_POINT('Ctrl Pts',(-7.65317280859473,-2.31334857514585,
-49.2645592586878));
#76499=CARTESIAN_POINT('Ctrl Pts',(-7.911,-1.15702837836553,-49.3111138752254));
#76500=CARTESIAN_POINT('Ctrl Pts',(-7.911,-1.49880108324396E-14,-49.357668491763));
#76501=CARTESIAN_POINT('',(-7.90980225400435,0.0042058662603975,-51.357668491763));
#76502=CARTESIAN_POINT('Ctrl Pts',(-7.911,-1.49880108324396E-14,-49.357668491763));
#76503=CARTESIAN_POINT('Ctrl Pts',(-7.91100000000001,2.20167589666673,-49.4462559274957));
#76504=CARTESIAN_POINT('Ctrl Pts',(-6.94214576672374,4.38610418338676,-49.5348433632284));
#76505=CARTESIAN_POINT('Ctrl Pts',(-3.67820201488297,7.34180684107626,-49.7120182346939));
#76506=CARTESIAN_POINT('Ctrl Pts',(-1.40868175871759,8.08992666571333,-49.8006056704266));
#76507=CARTESIAN_POINT('Ctrl Pts',(2.97309270521254,7.65454228025264,-49.977780541892));
#76508=CARTESIAN_POINT('Ctrl Pts',(5.05102072675583,6.4744488083424,-50.0663679776248));
#76509=CARTESIAN_POINT('Ctrl Pts',(7.66951518847861,2.93425195367734,-50.2435428490902));
#76510=CARTESIAN_POINT('Ctrl Pts',(8.18956872247068,0.601881960099496,-50.3321302848229));
#76511=CARTESIAN_POINT('Ctrl Pts',(7.3230668976136,-3.71537198232415,-50.5093051562884));
#76512=CARTESIAN_POINT('Ctrl Pts',(5.9432995885023,-5.6664351893648,-50.5978925920211));
#76513=CARTESIAN_POINT('Ctrl Pts',(2.16154501637893,-7.92205913232985,-50.7750674634866));
#76514=CARTESIAN_POINT('Ctrl Pts',(-0.210816529299864,-8.20894963713003,
-50.8636548992193));
#76515=CARTESIAN_POINT('Ctrl Pts',(-4.4212390857639,-6.91982244717861,-51.0408297706847));
#76516=CARTESIAN_POINT('Ctrl Pts',(-6.22631625634149,-5.35390358803565,
-51.1294172064175));
#76517=CARTESIAN_POINT('Ctrl Pts',(-7.6531728085948,-2.31334857514557,-51.2645592586878));
#76518=CARTESIAN_POINT('Ctrl Pts',(-7.91100000000001,-1.15702837836536,
-51.3111138752254));
#76519=CARTESIAN_POINT('Ctrl Pts',(-7.911,3.99680288865056E-14,-51.357668491763));
#76520=CARTESIAN_POINT('',(-7.91971459369528,0.0014675095212946,-53.357668491763));
#76521=CARTESIAN_POINT('Ctrl Pts',(-7.9095354027183,0.0051429103620837,
-51.357668491763));
#76522=CARTESIAN_POINT('Ctrl Pts',(-7.91338204178412,0.79052735029231,-51.3891750791503));
#76523=CARTESIAN_POINT('Ctrl Pts',(-7.43130218892738,4.20872011440281,-51.5265242004919));
#76524=CARTESIAN_POINT('Ctrl Pts',(-3.62969356886065,7.93193284741365,-51.7167945888108));
#76525=CARTESIAN_POINT('Ctrl Pts',(1.82628321975503,8.02975944020611,-51.9284796567195));
#76526=CARTESIAN_POINT('Ctrl Pts',(5.44779876741806,6.19873126434857,-52.0872434576511));
#76527=CARTESIAN_POINT('Ctrl Pts',(7.73164663510024,2.83444283938916,-52.2460072585824));
#76528=CARTESIAN_POINT('Ctrl Pts',(8.32932445584858,-2.57476025556633,-52.4576923264914));
#76529=CARTESIAN_POINT('Ctrl Pts',(3.87467264772705,-8.51367100141516,-52.7222986613769));
#76530=CARTESIAN_POINT('Ctrl Pts',(-2.0949362231413,-8.07967815626293,-52.9339837292857));
#76531=CARTESIAN_POINT('Ctrl Pts',(-6.49724597062893,-5.24286928254714,
-53.1457736727477));
#76532=CARTESIAN_POINT('Ctrl Pts',(-7.91319423021304,-2.62067617436248,
-53.2517210822554));
#76533=CARTESIAN_POINT('Ctrl Pts',(-7.91971459369528,0.0014675095212946,
-53.357668491763));
#76534=CARTESIAN_POINT('',(-7.90637295173893,-0.00687858255987051,-55.357668491763));
#76535=CARTESIAN_POINT('Ctrl Pts',(-7.91971459369528,0.0014675095212946,
-53.357668491763));
#76536=CARTESIAN_POINT('Ctrl Pts',(-7.92296509383969,1.30864592776983,-53.4104848831869));
#76537=CARTESIAN_POINT('Ctrl Pts',(-7.22881565719418,3.92557064294125,-53.516222541588));
#76538=CARTESIAN_POINT('Ctrl Pts',(-3.5727400178991,7.96013245645519,-53.7278027339433));
#76539=CARTESIAN_POINT('Ctrl Pts',(2.33048199300974,8.40589601261067,-53.9394878018521));
#76540=CARTESIAN_POINT('Ctrl Pts',(6.5678014334901,4.96752769388497,-54.1511728697608));
#76541=CARTESIAN_POINT('Ctrl Pts',(8.15955942910485,1.23465406198757,-54.3099366706923));
#76542=CARTESIAN_POINT('Ctrl Pts',(7.74058036951053,-2.80995397960037,-54.4687004716237));
#76543=CARTESIAN_POINT('Ctrl Pts',(4.71476302133078,-7.33335162650678,-54.6803855395325));
#76544=CARTESIAN_POINT('Ctrl Pts',(-2.51764341483412,-9.0087265231183,-54.9449918744182));
#76545=CARTESIAN_POINT('Ctrl Pts',(-7.44792865863706,-4.20704786616543,
-55.1883932808209));
#76546=CARTESIAN_POINT('Ctrl Pts',(-7.91420801088355,-0.795191286074574,
-55.3259521532691));
#76547=CARTESIAN_POINT('Ctrl Pts',(-7.90637295173893,-0.00687858255987051,
-55.357668491763));
#76548=CARTESIAN_POINT('',(-7.90348210374974,0.00514758300883319,-57.3576685050633));
#76549=CARTESIAN_POINT('Ctrl Pts',(-7.90637295173893,-0.00687858255987051,
-55.357668491763));
#76550=CARTESIAN_POINT('Ctrl Pts',(-7.88806115557395,1.83553527476434,-55.4317946872235));
#76551=CARTESIAN_POINT('Ctrl Pts',(-6.77682717523258,5.00881673632035,-55.5588421496612));
#76552=CARTESIAN_POINT('Ctrl Pts',(-3.00563183108224,7.65784328303544,-55.7388108790758));
#76553=CARTESIAN_POINT('Ctrl Pts',(2.39221485231049,8.39079788323256,-55.9504959469846));
#76554=CARTESIAN_POINT('Ctrl Pts',(7.19576250330689,4.93064285982486,-56.1621810148933));
#76555=CARTESIAN_POINT('Ctrl Pts',(8.22366753122325,-0.42852282073491,-56.373866082802));
#76556=CARTESIAN_POINT('Ctrl Pts',(7.03783755391621,-4.30948274059994,-56.5326298837334));
#76557=CARTESIAN_POINT('Ctrl Pts',(4.11287160034719,-7.13419116803278,-56.6913936846651));
#76558=CARTESIAN_POINT('Ctrl Pts',(-1.11486118009225,-8.64662670095146,
-56.9030787525737));
#76559=CARTESIAN_POINT('Ctrl Pts',(-6.66473466282189,-5.813654756809,-57.1251703549397));
#76560=CARTESIAN_POINT('Ctrl Pts',(-7.89158108502462,-1.57638635919126,
-57.2943406903285));
#76561=CARTESIAN_POINT('Ctrl Pts',(-7.89984496754574,0.00514488164946481,
-57.357668491763));
#76562=CARTESIAN_POINT('Ctrl Pts',(-7.91099832163338,0.00515316542435353,
-57.3576685325485));
#76563=CARTESIAN_POINT('Ctrl Pts',(-7.91085916274685,0.218786073952081,
-57.3662108111025));
#76564=CARTESIAN_POINT('Ctrl Pts',(-7.9020624298758,0.432087522141027,-57.3747530896565));
#76565=CARTESIAN_POINT('Ctrl Pts',(-7.88471273520091,0.644380387163226,
-57.3832953682106));
#76566=CARTESIAN_POINT('Ctrl Pts',(-7.86727553774343,0.857743946324986,
-57.3918807295483));
#76567=CARTESIAN_POINT('Ctrl Pts',(-7.84119897104923,1.0700884923815,-57.400466090886));
#76568=CARTESIAN_POINT('Ctrl Pts',(-7.80663937810051,1.28074299540948,-57.4090514522238));
#76569=CARTESIAN_POINT('Ctrl Pts',(-7.77199163430166,1.49193481302781,-57.4176587121672));
#76570=CARTESIAN_POINT('Ctrl Pts',(-7.72881765076389,1.70142773919554,-57.4262659721107));
#76571=CARTESIAN_POINT('Ctrl Pts',(-7.67732369902306,1.90856538279907,-57.4348732320542));
#76572=CARTESIAN_POINT('Ctrl Pts',(-7.62561836094242,2.11655334118395,-57.4435158254128));
#76573=CARTESIAN_POINT('Ctrl Pts',(-7.56552472331091,2.32216642644666,-57.4521584187715));
#76574=CARTESIAN_POINT('Ctrl Pts',(-7.49729893266142,2.52476329867057,-57.4608010121301));
#76575=CARTESIAN_POINT('Ctrl Pts',(-7.4330625818184,2.71551350676614,-57.4689382378609));
#76576=CARTESIAN_POINT('Ctrl Pts',(-7.36161781954197,2.90358999692527,-57.4770754635918));
#76577=CARTESIAN_POINT('Ctrl Pts',(-7.28321501793959,3.08847859025429,-57.4852126893226));
#76578=CARTESIAN_POINT('Ctrl Pts',(-7.20694901075638,3.2683282193331,-57.49312814264));
#76579=CARTESIAN_POINT('Ctrl Pts',(-7.12391001297988,3.44560427246274,-57.5010435959574));
#76580=CARTESIAN_POINT('Ctrl Pts',(-7.03429161510033,3.61976000222794,-57.5089590492749));
#76581=CARTESIAN_POINT('Ctrl Pts',(-6.94477585168995,3.79371628208886,-57.5168654375078));
#76582=CARTESIAN_POINT('Ctrl Pts',(-6.84869585259342,3.96455905283594,-57.5247718257407));
#76583=CARTESIAN_POINT('Ctrl Pts',(-6.74629377754161,4.13176006891777,-57.5326782139736));
#76584=CARTESIAN_POINT('Ctrl Pts',(-6.64398997877225,4.29880062053368,-57.5405770143677));
#76585=CARTESIAN_POINT('Ctrl Pts',(-6.53537636928849,4.46220608781448,-57.5484758147618));
#76586=CARTESIAN_POINT('Ctrl Pts',(-6.42074178691205,4.62147118413622,-57.5563746151559));
#76587=CARTESIAN_POINT('Ctrl Pts',(-6.30619595984499,4.78061297017407,-57.5642672999393));
#76588=CARTESIAN_POINT('Ctrl Pts',(-6.18563864786141,4.9356204933995,-57.5721599847227));
#76589=CARTESIAN_POINT('Ctrl Pts',(-6.05940306125347,5.0860156843321,-57.5800526695061));
#76590=CARTESIAN_POINT('Ctrl Pts',(-5.93324180565368,5.23632231841267,-57.5879407068583));
#76591=CARTESIAN_POINT('Ctrl Pts',(-5.80140915870419,5.38202176850061,-57.5958287442104));
#76592=CARTESIAN_POINT('Ctrl Pts',(-5.66428000406136,5.52266720304516,-57.6037167815625));
#76593=CARTESIAN_POINT('Ctrl Pts',(-5.5201169483989,5.67052690262347,-57.6120094277968));
#76594=CARTESIAN_POINT('Ctrl Pts',(-5.37009998048853,5.81280016037822,-57.6203020740311));
#76595=CARTESIAN_POINT('Ctrl Pts',(-5.21471123017033,5.94900897510967,-57.6285947202654));
#76596=CARTESIAN_POINT('Ctrl Pts',(-5.06697584815294,6.07850909167075,-57.6364789284648));
#76597=CARTESIAN_POINT('Ctrl Pts',(-4.91438539018964,6.20252752270697,-57.6443631366643));
#76598=CARTESIAN_POINT('Ctrl Pts',(-4.75739045796715,6.32069276507276,-57.6522473448637));
#76599=CARTESIAN_POINT('Ctrl Pts',(-4.60039352230813,6.43885951536341,-57.6601316536747));
#76600=CARTESIAN_POINT('Ctrl Pts',(-4.43899227564785,6.55117272033783,-57.6680159624858));
#76601=CARTESIAN_POINT('Ctrl Pts',(-4.27366866590118,6.65730254187794,-57.6759002712968));
#76602=CARTESIAN_POINT('Ctrl Pts',(-4.10831517529886,6.76345154549302,-57.6837860051305));
#76603=CARTESIAN_POINT('Ctrl Pts',(-3.9390381992495,6.86341475255014,-57.6916717389642));
#76604=CARTESIAN_POINT('Ctrl Pts',(-3.76634699959945,6.9569067320619,-57.6995574727979));
#76605=CARTESIAN_POINT('Ctrl Pts',(-3.59359557855781,7.05043131437636,-57.7074459565683));
#76606=CARTESIAN_POINT('Ctrl Pts',(-3.41742786468763,7.13748000874252,-57.7153344403387));
#76607=CARTESIAN_POINT('Ctrl Pts',(-3.23837615719559,7.21781413341374,-57.7232229241091));
#76608=CARTESIAN_POINT('Ctrl Pts',(-3.05914933812736,7.29822682441304,-57.7311191227729));
#76609=CARTESIAN_POINT('Ctrl Pts',(-2.87703320663395,7.37191168846707,-57.7390153214367));
#76610=CARTESIAN_POINT('Ctrl Pts',(-2.69257938423742,7.43867846190301,-57.7469115201004));
#76611=CARTESIAN_POINT('Ctrl Pts',(-2.50802082035909,7.50548314862637,-57.754812202594));
#76612=CARTESIAN_POINT('Ctrl Pts',(-2.32112224657997,7.56536180751737,-57.7627128850875));
#76613=CARTESIAN_POINT('Ctrl Pts',(-2.13244902244087,7.61817446418044,-57.7706135675811));
#76614=CARTESIAN_POINT('Ctrl Pts',(-1.94354909294622,7.67105057930277,-57.7785237433509));
#76615=CARTESIAN_POINT('Ctrl Pts',(-1.75287058839649,7.71684365430557,-57.7864339191206));
#76616=CARTESIAN_POINT('Ctrl Pts',(-1.56098863082943,7.75546487932356,-57.7943440948904));
#76617=CARTESIAN_POINT('Ctrl Pts',(-1.49309807954772,7.76912961513766,-57.7971428269888));
#76618=CARTESIAN_POINT('Ctrl Pts',(-1.42505692050413,7.78189702095104,-57.7999415590872));
#76619=CARTESIAN_POINT('Ctrl Pts',(-1.35689073356133,7.79376472169743,-57.8027402911856));
#76620=CARTESIAN_POINT('Ctrl Pts',(-1.14764710348681,7.83019393823696,-57.8113313080833));
#76621=CARTESIAN_POINT('Ctrl Pts',(-0.93680763769509,7.85821466188491,-57.819922324981));
#76622=CARTESIAN_POINT('Ctrl Pts',(-0.72504044045087,7.87770508204711,-57.8285133418786));
#76623=CARTESIAN_POINT('Ctrl Pts',(-0.513577331250256,7.89716751485426,
-57.8370920224676));
#76624=CARTESIAN_POINT('Ctrl Pts',(-0.301189396300564,7.90812406632587,
-57.8456707030565));
#76625=CARTESIAN_POINT('Ctrl Pts',(-0.0885520643070004,7.91050437910927,
-57.8542493836455));
#76626=CARTESIAN_POINT('Ctrl Pts',(0.132988948679575,7.91298436181182,-57.8631872760181));
#76627=CARTESIAN_POINT('Ctrl Pts',(0.354800446724125,7.90615438536036,-57.8721251683908));
#76628=CARTESIAN_POINT('Ctrl Pts',(0.576111061264889,7.88999474303299,-57.8810630607634));
#76629=CARTESIAN_POINT('Ctrl Pts',(0.787697048110754,7.87454517286209,-57.8896082124811));
#76630=CARTESIAN_POINT('Ctrl Pts',(0.998824916988692,7.85056819881669,-57.8981533641988));
#76631=CARTESIAN_POINT('Ctrl Pts',(1.20881788092876,7.81809953446149,-57.9066985159165));
#76632=CARTESIAN_POINT('Ctrl Pts',(1.4184905733951,7.7856803897987,-57.9152306349674));
#76633=CARTESIAN_POINT('Ctrl Pts',(1.62703156890904,7.74479542895872,-57.9237627540182));
#76634=CARTESIAN_POINT('Ctrl Pts',(1.83376833298211,7.69553212591254,-57.9322948730691));
#76635=CARTESIAN_POINT('Ctrl Pts',(2.04005942046293,7.64637502314053,-57.940808598847));
#76636=CARTESIAN_POINT('Ctrl Pts',(2.24455379595958,7.58887567644805,-57.9493223246248));
#76637=CARTESIAN_POINT('Ctrl Pts',(2.44658818084193,7.52317268666383,-57.9578360504027));
#76638=CARTESIAN_POINT('Ctrl Pts',(2.47560291817479,7.51373689190204,-57.9590587309742));
#76639=CARTESIAN_POINT('Ctrl Pts',(2.50456693108681,7.50413198676287,-57.9602814115457));
#76640=CARTESIAN_POINT('Ctrl Pts',(2.53347826806922,7.49435846922343,-57.9615040921172));
#76641=CARTESIAN_POINT('Ctrl Pts',(2.72023584712716,7.43122481076774,-57.9694022001719));
#76642=CARTESIAN_POINT('Ctrl Pts',(2.90462196341087,7.36110954243289,-57.9773003082265));
#76643=CARTESIAN_POINT('Ctrl Pts',(3.08608986276696,7.28422750598353,-57.9851984162812));
#76644=CARTESIAN_POINT('Ctrl Pts',(3.26759908676467,7.20732796162994,-57.9930983229267));
#76645=CARTESIAN_POINT('Ctrl Pts',(3.44618845437253,7.12365871143836,-58.0009982295721));
#76646=CARTESIAN_POINT('Ctrl Pts',(3.62133263770538,7.03348213384308,-58.0088981362176));
#76647=CARTESIAN_POINT('Ctrl Pts',(3.79654549278514,6.94327019918943,-58.0168011403132));
#76648=CARTESIAN_POINT('Ctrl Pts',(3.96831016761474,6.84654600880677,-58.0247041444089));
#76649=CARTESIAN_POINT('Ctrl Pts',(4.13612706728578,6.74361726992761,-58.0326071485046));
#76650=CARTESIAN_POINT('Ctrl Pts',(4.30412849990507,6.64057534969614,-58.0405188428135));
#76651=CARTESIAN_POINT('Ctrl Pts',(4.46817319296667,6.53131542959639,-58.0484305371224));
#76652=CARTESIAN_POINT('Ctrl Pts',(4.62779060407383,6.41618852005191,-58.0563422314313));
#76653=CARTESIAN_POINT('Ctrl Pts',(4.78750324303065,6.3009929257195,-58.0642586458621));
#76654=CARTESIAN_POINT('Ctrl Pts',(4.94278306407319,6.1799235724126,-58.0721750602929));
#76655=CARTESIAN_POINT('Ctrl Pts',(5.09319337766763,6.05337114488139,-58.0800914747237));
#76656=CARTESIAN_POINT('Ctrl Pts',(5.24381364271843,5.92664206811761,-58.0880189393459));
#76657=CARTESIAN_POINT('Ctrl Pts',(5.38955056562051,5.79441485351669,-58.095946403968));
#76658=CARTESIAN_POINT('Ctrl Pts',(5.53000404279176,5.65711731243987,-58.1038738685901));
#76659=CARTESIAN_POINT('Ctrl Pts',(5.62682346950656,5.56247338133801,-58.1093385434096));
#76660=CARTESIAN_POINT('Ctrl Pts',(5.72113309984425,5.46542086394359,-58.1148032182291));
#76661=CARTESIAN_POINT('Ctrl Pts',(5.81281330100186,5.36610869510634,-58.1202678930487));
#76662=CARTESIAN_POINT('Ctrl Pts',(5.94910954444989,5.21846639752973,-58.1283919442633));
#76663=CARTESIAN_POINT('Ctrl Pts',(6.07989121708775,5.0655052690018,-58.1365159954779));
#76664=CARTESIAN_POINT('Ctrl Pts',(6.20473593274536,4.90766472009841,-58.1446400466925));
#76665=CARTESIAN_POINT('Ctrl Pts',(6.32947055221235,4.74996336525756,-58.1527569335903));
#76666=CARTESIAN_POINT('Ctrl Pts',(6.4482784550839,4.58739141945296,-58.1608738204881));
#76667=CARTESIAN_POINT('Ctrl Pts',(6.56077587581787,4.42042315930119,-58.1689907073859));
#76668=CARTESIAN_POINT('Ctrl Pts',(6.67319011625287,4.25357835504472,-58.1771015926787));
#76669=CARTESIAN_POINT('Ctrl Pts',(6.77930299951989,4.08234398301251,-58.1852124779716));
#76670=CARTESIAN_POINT('Ctrl Pts',(6.87877229876129,3.90722569885518,-58.1933233632644));
#76671=CARTESIAN_POINT('Ctrl Pts',(6.97818220307628,3.73221198100805,-58.2014294054003));
#76672=CARTESIAN_POINT('Ctrl Pts',(7.07095627605335,3.55331925393053,-58.2095354475361));
#76673=CARTESIAN_POINT('Ctrl Pts',(7.15679642731891,3.37108082043658,-58.2176414896719));
#76674=CARTESIAN_POINT('Ctrl Pts',(7.24259752190372,3.18892530418136,-58.2257438436141));
#76675=CARTESIAN_POINT('Ctrl Pts',(7.32147085031128,3.00342740715577,-58.2338461975563));
#76676=CARTESIAN_POINT('Ctrl Pts',(7.3931647158307,2.81514413211755,-58.2419485514985));
#76677=CARTESIAN_POINT('Ctrl Pts',(7.46537122377707,2.62551454949265,-58.2501088408074));
#76678=CARTESIAN_POINT('Ctrl Pts',(7.53029503972041,2.43305989051288,-58.2582691301163));
#76679=CARTESIAN_POINT('Ctrl Pts',(7.58772835729282,2.2383698032127,-58.2664294194251));
#76680=CARTESIAN_POINT('Ctrl Pts',(7.64473244252684,2.04513474732919,-58.2745287221811));
#76681=CARTESIAN_POINT('Ctrl Pts',(7.69435753628214,1.84969787995055,-58.2826280249371));
#76682=CARTESIAN_POINT('Ctrl Pts',(7.73645038245148,1.65265134855068,-58.290727327693));
#76683=CARTESIAN_POINT('Ctrl Pts',(7.77854301549651,1.45560581483591,-58.2988265894406));
#76684=CARTESIAN_POINT('Ctrl Pts',(7.81310341012868,1.25695094704828,-58.3069258511882));
#76685=CARTESIAN_POINT('Ctrl Pts',(7.84002929200141,1.05728979024667,-58.3150251129358));
#76686=CARTESIAN_POINT('Ctrl Pts',(7.86695851597118,0.857603851082755,-58.3231253799808));
#76687=CARTESIAN_POINT('Ctrl Pts',(7.88625129500784,0.656911691738669,-58.3312256470258));
#76688=CARTESIAN_POINT('Ctrl Pts',(7.8978570906672,0.455822745590702,-58.3393259140708));
#76689=CARTESIAN_POINT('Ctrl Pts',(7.90961408817888,0.252113985857309,-58.3475317124742));
#76690=CARTESIAN_POINT('Ctrl Pts',(7.9134823826409,0.0479983655472201,-58.3557375108776));
#76691=CARTESIAN_POINT('Ctrl Pts',(7.90946392466752,-0.155889141325008,
-58.363943309281));
#76692=CARTESIAN_POINT('Ctrl Pts',(7.90549335173915,-0.357347068864224,
-58.3720513251449));
#76693=CARTESIAN_POINT('Ctrl Pts',(7.89382300183199,-0.558581968020428,
-58.3801593410087));
#76694=CARTESIAN_POINT('Ctrl Pts',(7.87450716322381,-0.758984806393986,
-58.3882673568725));
#76695=CARTESIAN_POINT('Ctrl Pts',(7.85484190156595,-0.96301292722977,-58.3965220465457));
#76696=CARTESIAN_POINT('Ctrl Pts',(7.82725193743623,-1.16617824928713,-58.4047767362189));
#76697=CARTESIAN_POINT('Ctrl Pts',(7.79184931729559,-1.36784692731325,-58.4130314258921));
#76698=CARTESIAN_POINT('Ctrl Pts',(7.75644669715494,-1.56951560533937,-58.4212861155654));
#76699=CARTESIAN_POINT('Ctrl Pts',(7.71323152042349,-1.76968730392838,-58.4295408052386));
#76700=CARTESIAN_POINT('Ctrl Pts',(7.66236985097129,-1.96774217491169,-58.4377954949118));
#76701=CARTESIAN_POINT('Ctrl Pts',(7.61414229894411,-2.15553981697616,-58.4456226755759));
#76702=CARTESIAN_POINT('Ctrl Pts',(7.55894713824618,-2.34179431903526,-58.4534498562401));
#76703=CARTESIAN_POINT('Ctrl Pts',(7.49690066953181,-2.52594563503917,-58.4612770369042));
#76704=CARTESIAN_POINT('Ctrl Pts',(7.43490653106102,-2.70994163707567,-58.4690976160924));
#76705=CARTESIAN_POINT('Ctrl Pts',(7.36607270179688,-2.8918376534716,-58.4769181952806));
#76706=CARTESIAN_POINT('Ctrl Pts',(7.29056612145986,-3.07108557819898,-58.4847387744688));
#76707=CARTESIAN_POINT('Ctrl Pts',(7.21510988267937,-3.25021399520272,-58.4925541395402));
#76708=CARTESIAN_POINT('Ctrl Pts',(7.13298988893582,-3.42669751336263,-58.5003695046116));
#76709=CARTESIAN_POINT('Ctrl Pts',(7.04442238528958,-3.60000475800118,-58.508184869683));
#76710=CARTESIAN_POINT('Ctrl Pts',(6.95589726898374,-3.77322905988,-58.5159964944149));
#76711=CARTESIAN_POINT('Ctrl Pts',(6.86093094902157,-3.94327980316541,-58.5238081191467));
#76712=CARTESIAN_POINT('Ctrl Pts',(6.7597871872997,-4.10964696566735,-58.5316197438785));
#76713=CARTESIAN_POINT('Ctrl Pts',(6.65867285555185,-4.27596572003035,-58.5394290956485));
#76714=CARTESIAN_POINT('Ctrl Pts',(6.55138484618283,-4.43860272842584,-58.5472384474184));
#76715=CARTESIAN_POINT('Ctrl Pts',(6.43823220753763,-4.59707374770355,-58.5550477991884));
#76716=CARTESIAN_POINT('Ctrl Pts',(6.3250730511939,-4.75555389506118,-58.5628576007843));
#76717=CARTESIAN_POINT('Ctrl Pts',(6.20604879017585,-4.9098672834239,-58.5706674023803));
#76718=CARTESIAN_POINT('Ctrl Pts',(6.08151128181401,-5.05955942046033,-58.5784772039763));
#76719=CARTESIAN_POINT('Ctrl Pts',(5.98539707458308,-5.17508719413442,-58.5845045679319));
#76720=CARTESIAN_POINT('Ctrl Pts',(5.88599991776427,-5.28786298909097,-58.5905319318876));
#76721=CARTESIAN_POINT('Ctrl Pts',(5.78349774602666,-5.3976916197301,-58.5965592958433));
#76722=CARTESIAN_POINT('Ctrl Pts',(5.63624585190805,-5.55546850987703,-58.6052180466187));
#76723=CARTESIAN_POINT('Ctrl Pts',(5.48265750959305,-5.70708495534743,-58.6138767973941));
#76724=CARTESIAN_POINT('Ctrl Pts',(5.32325943148045,-5.85207911986454,-58.6225355481695));
#76725=CARTESIAN_POINT('Ctrl Pts',(5.16358670029539,-5.99732311859072,-58.6312092185257));
#76726=CARTESIAN_POINT('Ctrl Pts',(4.99808438945357,-6.13592187420624,-58.6398828888818));
#76727=CARTESIAN_POINT('Ctrl Pts',(4.82731218949133,-6.26745387100603,-58.648556559238));
#76728=CARTESIAN_POINT('Ctrl Pts',(4.65213878395515,-6.40237576005756,-58.6574537706994));
#76729=CARTESIAN_POINT('Ctrl Pts',(4.47142045450506,-6.52986163258815,-58.6663509821608));
#76730=CARTESIAN_POINT('Ctrl Pts',(4.28579100704396,-6.64950497736043,-58.6752481936222));
#76731=CARTESIAN_POINT('Ctrl Pts',(4.10420815118273,-6.76654018123396,-58.6839514521216));
#76732=CARTESIAN_POINT('Ctrl Pts',(3.91792627144628,-6.87607113708023,-58.6926547106211));
#76733=CARTESIAN_POINT('Ctrl Pts',(3.72756326656371,-6.97776419018047,-58.7013579691205));
#76734=CARTESIAN_POINT('Ctrl Pts',(3.53083687456925,-7.08285660264607,-58.7103521570629));
#76735=CARTESIAN_POINT('Ctrl Pts',(3.329752063795,-7.1795779754511,-58.7193463450053));
#76736=CARTESIAN_POINT('Ctrl Pts',(3.12501450883253,-7.26761345419431,-58.7283405329477));
#76737=CARTESIAN_POINT('Ctrl Pts',(2.92027695387007,-7.35564893293752,-58.73733472089));
#76738=CARTESIAN_POINT('Ctrl Pts',(2.71188690799654,-7.43499844067692,-58.7463289088324));
#76739=CARTESIAN_POINT('Ctrl Pts',(2.5005704045462,-7.50540263089913,-58.7553230967748));
#76740=CARTESIAN_POINT('Ctrl Pts',(2.30602259325594,-7.5702200062094,-58.7636035649349));
#76741=CARTESIAN_POINT('Ctrl Pts',(2.10882647462805,-7.62751117665964,-58.7718840330949));
#76742=CARTESIAN_POINT('Ctrl Pts',(1.90958123564917,-7.67707108892816,-58.780164501255));
#76743=CARTESIAN_POINT('Ctrl Pts',(1.71051044070642,-7.72658761029224,-58.7884377196646));
#76744=CARTESIAN_POINT('Ctrl Pts',(1.50939439240345,-7.76838630330906,-58.7967109380741));
#76745=CARTESIAN_POINT('Ctrl Pts',(1.3068474972431,-7.80231187654976,-58.8049841564836));
#76746=CARTESIAN_POINT('Ctrl Pts',(1.10446218895956,-7.83621038481166,-58.8132507747251));
#76747=CARTESIAN_POINT('Ctrl Pts',(0.900648604277325,-7.86224825325279,
-58.8215173929667));
#76748=CARTESIAN_POINT('Ctrl Pts',(0.696032189003861,-7.88032107162332,
-58.8297840112083));
#76749=CARTESIAN_POINT('Ctrl Pts',(0.491605623434067,-7.89837712145059,
-58.8380429594151));
#76750=CARTESIAN_POINT('Ctrl Pts',(0.286378010497993,-7.90848284528599,
-58.8463019076219));
#76751=CARTESIAN_POINT('Ctrl Pts',(0.0809811801980997,-7.91058550604528,
-58.8545608558286));
#76752=CARTESIAN_POINT('Ctrl Pts',(-0.124296303540743,-7.91268694504605,
-58.8628150051441));
#76753=CARTESIAN_POINT('Ctrl Pts',(-0.329742510875407,-7.90679459287275,
-58.8710691544595));
#76754=CARTESIAN_POINT('Ctrl Pts',(-0.534723027352655,-7.89290772048038,
-58.879323303775));
#76755=CARTESIAN_POINT('Ctrl Pts',(-0.739574435034937,-7.87902959485767,
-58.8875722541414));
#76756=CARTESIAN_POINT('Ctrl Pts',(-0.943960440065985,-7.8571670181748,
-58.8958212045077));
#76757=CARTESIAN_POINT('Ctrl Pts',(-1.14724860916018,-7.8273713102663,-58.9040701548741));
#76758=CARTESIAN_POINT('Ctrl Pts',(-1.22953323205989,-7.81531094984196,
-58.9074090691515));
#76759=CARTESIAN_POINT('Ctrl Pts',(-1.31163802229569,-7.80195143964422,
-58.9107479834289));
#76760=CARTESIAN_POINT('Ctrl Pts',(-1.39352124695277,-7.78729860312876,
-58.9140868977063));
#76761=CARTESIAN_POINT('Ctrl Pts',(-1.593574597164,-7.75149946298389,-58.9222443803904));
#76762=CARTESIAN_POINT('Ctrl Pts',(-1.79221772401568,-7.70799244489013,
-58.9304018630746));
#76763=CARTESIAN_POINT('Ctrl Pts',(-1.98884540888124,-7.65691941576846,
-58.9385593457587));
#76764=CARTESIAN_POINT('Ctrl Pts',(-2.1855319194016,-7.60583110698573,-58.9467192689398));
#76765=CARTESIAN_POINT('Ctrl Pts',(-2.38020148346095,-7.54717235000572,
-58.9548791921208));
#76766=CARTESIAN_POINT('Ctrl Pts',(-2.57226312296309,-7.48113516962795,
-58.9630391153019));
#76767=CARTESIAN_POINT('Ctrl Pts',(-2.76440328367153,-7.41507099104753,
-58.9712023745318));
#76768=CARTESIAN_POINT('Ctrl Pts',(-2.95393309825705,-7.34162247254659,
-58.9793656337617));
#76769=CARTESIAN_POINT('Ctrl Pts',(-3.14028006557105,-7.26103037521378,
-58.9875288929916));
#76770=CARTESIAN_POINT('Ctrl Pts',(-3.32680413727205,-7.1803616830525,-58.9956999105931));
#76771=CARTESIAN_POINT('Ctrl Pts',(-3.51013903017709,-7.09253596794178,
-59.0038709281946));
#76772=CARTESIAN_POINT('Ctrl Pts',(-3.68973410881148,-6.99784132474245,
-59.0120419457962));
#76773=CARTESIAN_POINT('Ctrl Pts',(-3.86942144382874,-6.9030980377533,-59.0202171607762));
#76774=CARTESIAN_POINT('Ctrl Pts',(-4.0453648593851,-6.80147893396333,-59.0283923757563));
#76775=CARTESIAN_POINT('Ctrl Pts',(-4.21704044198085,-6.69331688407907,
-59.0365675907364));
#76776=CARTESIAN_POINT('Ctrl Pts',(-4.38889848638682,-6.58503987641735,
-59.044751494573));
#76777=CARTESIAN_POINT('Ctrl Pts',(-4.55647937343348,-6.47020619796347,
-59.0529353984097));
#76778=CARTESIAN_POINT('Ctrl Pts',(-4.71928897235881,-6.34919149147138,
-59.0611193022464));
#76779=CARTESIAN_POINT('Ctrl Pts',(-4.79708330211563,-6.29136776335945,
-59.0650297677102));
#76780=CARTESIAN_POINT('Ctrl Pts',(-4.87378875650194,-6.23213340341129,
-59.068940233174));
#76781=CARTESIAN_POINT('Ctrl Pts',(-4.94935420446545,-6.17153254538451,
-59.0728506986378));
#76782=CARTESIAN_POINT('Ctrl Pts',(-5.1009359491697,-6.04996926431046,-59.0806949607123));
#76783=CARTESIAN_POINT('Ctrl Pts',(-5.24821928464149,-5.92267130269681,
-59.0885392227869));
#76784=CARTESIAN_POINT('Ctrl Pts',(-5.39074057696754,-5.78997729113299,
-59.0963834848614));
#76785=CARTESIAN_POINT('Ctrl Pts',(-5.53313583457969,-5.6574006238025,-59.1042208100825));
#76786=CARTESIAN_POINT('Ctrl Pts',(-5.67077718123352,-5.51943764764221,
-59.1120581353035));
#76787=CARTESIAN_POINT('Ctrl Pts',(-5.80323284396378,-5.37646813054258,
-59.1198954605245));
#76788=CARTESIAN_POINT('Ctrl Pts',(-5.93559695283294,-5.23359743452043,
-59.1277273685564));
#76789=CARTESIAN_POINT('Ctrl Pts',(-6.06278228019247,-5.08572734678121,
-59.1355592765882));
#76790=CARTESIAN_POINT('Ctrl Pts',(-6.18439267908374,-4.93327560459534,
-59.1433911846201));
#76791=CARTESIAN_POINT('Ctrl Pts',(-6.30594249857902,-4.78089980521159,
-59.15121919124));
#76792=CARTESIAN_POINT('Ctrl Pts',(-6.42192270412385,-4.62394717177293,
-59.1590471978599));
#76793=CARTESIAN_POINT('Ctrl Pts',(-6.53197621747703,-4.46286989439694,
-59.1668752044799));
#76794=CARTESIAN_POINT('Ctrl Pts',(-6.64374089025095,-4.29928811814352,
-59.1748249243179));
#76795=CARTESIAN_POINT('Ctrl Pts',(-6.74939279949715,-4.13145264848913,
-59.1827746441559));
#76796=CARTESIAN_POINT('Ctrl Pts',(-6.84860216557749,-3.95986986877693,
-59.190724363994));
#76797=CARTESIAN_POINT('Ctrl Pts',(-6.9462700263592,-3.79095312529222,-59.198550561873));
#76798=CARTESIAN_POINT('Ctrl Pts',(-7.03769392991793,-3.61840499634442,
-59.206376759752));
#76799=CARTESIAN_POINT('Ctrl Pts',(-7.12260440071309,-3.44273547501729,
-59.214202957631));
#76800=CARTESIAN_POINT('Ctrl Pts',(-7.20752447139024,-3.26704609269235,
-59.2220300403311));
#76801=CARTESIAN_POINT('Ctrl Pts',(-7.28592948924982,-3.08823493065946,
-59.2298571230312));
#76802=CARTESIAN_POINT('Ctrl Pts',(-7.35759718539343,-2.90683412968312,
-59.2376842057313));
#76803=CARTESIAN_POINT('Ctrl Pts',(-7.42928551732976,-2.72538109667577,
-59.2455135421394));
#76804=CARTESIAN_POINT('Ctrl Pts',(-7.49423253421238,-2.54133726544852,
-59.2533428785474));
#76805=CARTESIAN_POINT('Ctrl Pts',(-7.55226505272291,-2.3552523375257,-59.2611722149555));
#76806=CARTESIAN_POINT('Ctrl Pts',(-7.61186909651773,-2.16412821473829,
-59.2692135704252));
#76807=CARTESIAN_POINT('Ctrl Pts',(-7.66417875621187,-1.97085127087421,
-59.277254925895));
#76808=CARTESIAN_POINT('Ctrl Pts',(-7.70906204074682,-1.77603025084496,
-59.2852962813648));
#76809=CARTESIAN_POINT('Ctrl Pts',(-7.7528314978707,-1.58604392583883,-59.2931380818725));
#76810=CARTESIAN_POINT('Ctrl Pts',(-7.78953877974173,-1.39458960276944,
-59.3009798823802));
#76811=CARTESIAN_POINT('Ctrl Pts',(-7.81911395936368,-1.20223869946197,
-59.3088216828878));
#76812=CARTESIAN_POINT('Ctrl Pts',(-7.84981806476796,-1.00254549437397,
-59.3169628158387));
#76813=CARTESIAN_POINT('Ctrl Pts',(-7.87283483272258,-0.801886345405845,
-59.3251039487895));
#76814=CARTESIAN_POINT('Ctrl Pts',(-7.88814537586744,-0.600902262586137,
-59.3332450817403));
#76815=CARTESIAN_POINT('Ctrl Pts',(-7.9034559190123,-0.399918179766429,
-59.3413862146912));
#76816=CARTESIAN_POINT('Ctrl Pts',(-7.91106028968049,-0.198609580813962,
-59.349527347642));
#76817=CARTESIAN_POINT('Ctrl Pts',(-7.91099963985057,0.00238710789585057,
-59.3576684805928));
#76818=CARTESIAN_POINT('Origin',(0.,0.,-63.6971797838103));
#76819=CARTESIAN_POINT('',(-6.76699852120032,-0.00296022942052201,59.3028202161897));
#76820=CARTESIAN_POINT('Ctrl Pts',(3.09908550384712,6.01564277861017,58.6513967904261));
#76821=CARTESIAN_POINT('Ctrl Pts',(2.93373232018322,6.10082796552483,58.6601462383254));
#76822=CARTESIAN_POINT('Ctrl Pts',(2.76486502144422,6.17919158180192,58.6688956862247));
#76823=CARTESIAN_POINT('Ctrl Pts',(2.59305716434349,6.2504674659138,58.677645134124));
#76824=CARTESIAN_POINT('Ctrl Pts',(2.42125069459275,6.32174277447228,58.6863945113714));
#76825=CARTESIAN_POINT('Ctrl Pts',(2.24650397871046,6.3859303555783,58.6951438886188));
#76826=CARTESIAN_POINT('Ctrl Pts',(2.06941053323754,6.44281220003544,58.7038932658663));
#76827=CARTESIAN_POINT('Ctrl Pts',(1.89231845896675,6.49969360406687,58.7126425753688));
#76828=CARTESIAN_POINT('Ctrl Pts',(1.71287996431505,6.5492692970088,58.7213918848715));
#76829=CARTESIAN_POINT('Ctrl Pts',(1.53170449173513,6.59137090065477,58.730141194374));
#76830=CARTESIAN_POINT('Ctrl Pts',(1.35053036178176,6.63347219230082,58.7388904390386));
#76831=CARTESIAN_POINT('Ctrl Pts',(1.16761955878847,6.66809944062454,58.7476396837032));
#76832=CARTESIAN_POINT('Ctrl Pts',(0.983593309310479,6.69513503985392,58.7563889283678));
#76833=CARTESIAN_POINT('Ctrl Pts',(0.799568362460015,6.72217044771214,58.765138111101));
#76834=CARTESIAN_POINT('Ctrl Pts',(0.614428268438671,6.74161427235976,58.7738872938342));
#76835=CARTESIAN_POINT('Ctrl Pts',(0.428801816330387,6.75340047696801,58.7826364765673));
#76836=CARTESIAN_POINT('Ctrl Pts',(0.243176616522917,6.76518660206241,58.7913856002755));
#76837=CARTESIAN_POINT('Ctrl Pts',(0.0570653511656112,6.76931519233997,
58.8001347239836));
#76838=CARTESIAN_POINT('Ctrl Pts',(-0.128899900799864,6.76577222610795,
58.8088838476917));
#76839=CARTESIAN_POINT('Ctrl Pts',(-0.314863959941901,6.76222928260134,
58.817632915281));
#76840=CARTESIAN_POINT('Ctrl Pts',(-0.500681721080607,6.75101488651277,
58.8263819828702));
#76841=CARTESIAN_POINT('Ctrl Pts',(-0.685722110173271,6.73216712415991,
58.8351310504595));
#76842=CARTESIAN_POINT('Ctrl Pts',(-0.870761373827518,6.71331947644146,
58.8438800648359));
#76843=CARTESIAN_POINT('Ctrl Pts',(-1.05502298984327,6.68683858439999,58.8526290792122));
#76844=CARTESIAN_POINT('Ctrl Pts',(-1.23788117676037,6.6528143813143,58.8613780935886));
#76845=CARTESIAN_POINT('Ctrl Pts',(-1.43009641451765,6.61704912302383,58.8705748044761));
#76846=CARTESIAN_POINT('Ctrl Pts',(-1.62076048992662,6.57294837083173,58.8797715153636));
#76847=CARTESIAN_POINT('Ctrl Pts',(-1.80915798961093,6.5206776004206,58.8889682262512));
#76848=CARTESIAN_POINT('Ctrl Pts',(-1.98840443002967,6.47094578577423,58.8977182239577));
#76849=CARTESIAN_POINT('Ctrl Pts',(-2.16559895952141,6.41381888474493,58.9064682216642));
#76850=CARTESIAN_POINT('Ctrl Pts',(-2.34013966242265,6.34949095285255,58.9152182193707));
#76851=CARTESIAN_POINT('Ctrl Pts',(-2.5146768255395,6.28516432556711,58.9239680396223));
#76852=CARTESIAN_POINT('Ctrl Pts',(-2.68656000078769,6.21363705879692,58.9327178598738));
#76853=CARTESIAN_POINT('Ctrl Pts',(-2.85520533840808,6.13515211510897,58.9414676801254));
#76854=CARTESIAN_POINT('Ctrl Pts',(-3.02384747998247,6.05666865881161,58.9502173345567));
#76855=CARTESIAN_POINT('Ctrl Pts',(-3.18925164684457,5.97122791039887,58.9589669889879));
#76856=CARTESIAN_POINT('Ctrl Pts',(-3.35085601829078,5.87912008251954,58.9677166434192));
#76857=CARTESIAN_POINT('Ctrl Pts',(-3.51245754191336,5.78701387778224,58.9764661436623));
#76858=CARTESIAN_POINT('Ctrl Pts',(-3.67025915510852,5.68824097061037,58.9852156439055));
#76859=CARTESIAN_POINT('Ctrl Pts',(-3.82372487928749,5.58313684656913,58.9939651441486));
#76860=CARTESIAN_POINT('Ctrl Pts',(-3.97718810300705,5.4780344350184,59.0027145018337));
#76861=CARTESIAN_POINT('Ctrl Pts',(-4.12631534262926,5.36660117496452,59.0114638595189));
#76862=CARTESIAN_POINT('Ctrl Pts',(-4.27060009886119,5.24921554097437,59.020213217204));
#76863=CARTESIAN_POINT('Ctrl Pts',(-4.41488269594112,5.13183166360378,59.0289624439592));
#76864=CARTESIAN_POINT('Ctrl Pts',(-4.55432273234992,5.00849577139558,59.0377116707143));
#76865=CARTESIAN_POINT('Ctrl Pts',(-4.68844662480115,4.8796267527743,59.0464608974695));
#76866=CARTESIAN_POINT('Ctrl Pts',(-4.82256868835062,4.75075949139979,59.055210004921));
#76867=CARTESIAN_POINT('Ctrl Pts',(-4.95137454637762,4.61635945312632,59.0639591123725));
#76868=CARTESIAN_POINT('Ctrl Pts',(-5.07442674460975,4.47688309134707,59.072708219824));
#76869=CARTESIAN_POINT('Ctrl Pts',(-5.19747742838423,4.33740844616489,59.0814572195963));
#76870=CARTESIAN_POINT('Ctrl Pts',(-5.314774404508,4.1928578173619,59.0902062193687));
#76871=CARTESIAN_POINT('Ctrl Pts',(-5.42591931531016,4.04372211999591,59.098955219141));
#76872=CARTESIAN_POINT('Ctrl Pts',(-5.53707636462847,3.89457013500993,59.1077051744216));
#76873=CARTESIAN_POINT('Ctrl Pts',(-5.64207983273339,3.74083230916619,59.1164551297022));
#76874=CARTESIAN_POINT('Ctrl Pts',(-5.74057303468619,3.58303087252034,59.1252050849828));
#76875=CARTESIAN_POINT('Ctrl Pts',(-5.83906243363648,3.4252355288763,59.1339547024116));
#76876=CARTESIAN_POINT('Ctrl Pts',(-5.9310419176832,3.26337713157185,59.1427043198404));
#76877=CARTESIAN_POINT('Ctrl Pts',(-6.01619906699561,3.0980054529134,59.1514539372692));
#76878=CARTESIAN_POINT('Ctrl Pts',(-6.10135338095297,2.93263928039775,59.1602032633746));
#76879=CARTESIAN_POINT('Ctrl Pts',(-6.17968568352761,2.76376031540399,59.16895258948));
#76880=CARTESIAN_POINT('Ctrl Pts',(-6.25092992694816,2.59194213831711,59.1777019155854));
#76881=CARTESIAN_POINT('Ctrl Pts',(-6.32217217691038,2.42012876880992,59.1864509968792));
#76882=CARTESIAN_POINT('Ctrl Pts',(-6.38632665483789,2.24537661647845,59.195200078173));
#76883=CARTESIAN_POINT('Ctrl Pts',(-6.44317547869293,2.06827917621634,59.2039491594668));
#76884=CARTESIAN_POINT('Ctrl Pts',(-6.50002944235881,1.8911657242361,59.2126990317817));
#76885=CARTESIAN_POINT('Ctrl Pts',(-6.54957634250346,1.71170683289395,59.2214489040967));
#76886=CARTESIAN_POINT('Ctrl Pts',(-6.59164787708347,1.53051209225571,59.2301987764117));
#76887=CARTESIAN_POINT('Ctrl Pts',(-6.63371649074966,1.34932993148241,59.2389480412464));
#76888=CARTESIAN_POINT('Ctrl Pts',(-6.66831071257086,1.16641244174219,59.2476973060812));
#76889=CARTESIAN_POINT('Ctrl Pts',(-6.69531304840301,0.982380875162206,
59.256446570916));
#76890=CARTESIAN_POINT('Ctrl Pts',(-6.72231677033018,0.798339861798014,
59.2651962848717));
#76891=CARTESIAN_POINT('Ctrl Pts',(-6.7417277847787,0.613184940732301,59.2739459988273));
#76892=CARTESIAN_POINT('Ctrl Pts',(-6.75348015835505,0.427545027692672,
59.282695712783));
#76893=CARTESIAN_POINT('Ctrl Pts',(-6.76249038365204,0.285219953550303,
59.2894038805852));
#76894=CARTESIAN_POINT('Ctrl Pts',(-6.76699999999987,0.142609995762151,
59.2961120483875));
#76895=CARTESIAN_POINT('Ctrl Pts',(-6.767,6.12589398735536E-12,59.3028202161897));
#76896=CARTESIAN_POINT('',(3.93017071637407,-5.50872463825845,59.9999950688108));
#76897=CARTESIAN_POINT('Ctrl Pts',(-6.7669966225104,-0.00676098608203946,
59.3028202161897));
#76898=CARTESIAN_POINT('Ctrl Pts',(-6.76676245139478,-0.241140280658097,
59.3138571345979));
#76899=CARTESIAN_POINT('Ctrl Pts',(-6.75434836748514,-0.474955858725596,
59.3248940530061));
#76900=CARTESIAN_POINT('Ctrl Pts',(-6.72994860126805,-0.707163930280838,
59.3359309714143));
#76901=CARTESIAN_POINT('Ctrl Pts',(-6.70469071231455,-0.947538597532459,
59.3473560505344));
#76902=CARTESIAN_POINT('Ctrl Pts',(-6.66658916004148,-1.18619120591911,
59.3587811296546));
#76903=CARTESIAN_POINT('Ctrl Pts',(-6.61590677114137,-1.42199388028421,
59.3702062087747));
#76904=CARTESIAN_POINT('Ctrl Pts',(-6.58607853721709,-1.56077142182427,
59.3769302393501));
#76905=CARTESIAN_POINT('Ctrl Pts',(-6.55189355796116,-1.69856235289583,
59.3836542699255));
#76906=CARTESIAN_POINT('Ctrl Pts',(-6.51341303837284,-1.83514021032582,
59.390378300501));
#76907=CARTESIAN_POINT('Ctrl Pts',(-6.46732120164663,-1.99873270783956,
59.3984323216717));
#76908=CARTESIAN_POINT('Ctrl Pts',(-6.4149747861413,-2.16089713411304,59.4064863428424));
#76909=CARTESIAN_POINT('Ctrl Pts',(-6.35647389237976,-2.32110505050818,
59.4145403640131));
#76910=CARTESIAN_POINT('Ctrl Pts',(-6.29804717134514,-2.48110984080951,
59.422584173567));
#76911=CARTESIAN_POINT('Ctrl Pts',(-6.23348162378241,-2.63916270946047,
59.4306279831208));
#76912=CARTESIAN_POINT('Ctrl Pts',(-6.16292816805098,-2.79474603415836,
59.4386717926746));
#76913=CARTESIAN_POINT('Ctrl Pts',(-6.09244856921295,-2.9501664908449,59.4467071817935));
#76914=CARTESIAN_POINT('Ctrl Pts',(-6.01599368843736,-3.10312220959545,
59.4547425709124));
#76915=CARTESIAN_POINT('Ctrl Pts',(-5.9337639612522,-3.25311147244368,59.4627779600313));
#76916=CARTESIAN_POINT('Ctrl Pts',(-5.85160216824035,-3.40297682150881,
59.4708067107052));
#76917=CARTESIAN_POINT('Ctrl Pts',(-5.76367520277198,-3.549880265369,59.4788354613792));
#76918=CARTESIAN_POINT('Ctrl Pts',(-5.6702311985322,-3.69334092052062,59.4868642120531));
#76919=CARTESIAN_POINT('Ctrl Pts',(-5.57684379896657,-3.83671467289336,
59.4948880992281));
#76920=CARTESIAN_POINT('Ctrl Pts',(-5.47794621688296,-3.97664947481862,
59.5029119864031));
#76921=CARTESIAN_POINT('Ctrl Pts',(-5.37383196588725,-4.11268999590394,
59.5109358735781));
#76922=CARTESIAN_POINT('Ctrl Pts',(-5.26734063065929,-4.25183652576834,
59.5191429581109));
#76923=CARTESIAN_POINT('Ctrl Pts',(-5.15539175069455,-4.38690846339147,
59.5273500426437));
#76924=CARTESIAN_POINT('Ctrl Pts',(-5.03834590325707,-4.51745055967774,
59.5355571271764));
#76925=CARTESIAN_POINT('Ctrl Pts',(-4.92395316522499,-4.64503362349048,
59.5435781795376));
#76926=CARTESIAN_POINT('Ctrl Pts',(-4.80469231569053,-4.76828971445624,
59.5515992318988));
#76927=CARTESIAN_POINT('Ctrl Pts',(-4.68093990593028,-4.8868282757909,59.5596202842601));
#76928=CARTESIAN_POINT('Ctrl Pts',(-4.55717567703545,-5.00537815830478,
59.5676421026823));
#76929=CARTESIAN_POINT('Ctrl Pts',(-4.42891930459848,-5.11920935457248,
59.5756639211046));
#76930=CARTESIAN_POINT('Ctrl Pts',(-4.29658302598711,-5.22796932860164,
59.5836857395269));
#76931=CARTESIAN_POINT('Ctrl Pts',(-4.16420771428784,-5.33676138179813,
59.5917099240149));
#76932=CARTESIAN_POINT('Ctrl Pts',(-4.02775039091781,-5.44047899770564,
59.5997341085029));
#76933=CARTESIAN_POINT('Ctrl Pts',(-3.88765492987487,-5.53881107695682,
59.607758292991));
#76934=CARTESIAN_POINT('Ctrl Pts',(-3.74194723076937,-5.64108234905435,
59.6161039271054));
#76935=CARTESIAN_POINT('Ctrl Pts',(-3.59230424695664,-5.73752741084,59.6244495612198));
#76936=CARTESIAN_POINT('Ctrl Pts',(-3.43925576289736,-5.82784769853994,
59.6327951953342));
#76937=CARTESIAN_POINT('Ctrl Pts',(-3.29184412045361,-5.91484145112546,
59.6408334561481));
#76938=CARTESIAN_POINT('Ctrl Pts',(-3.14127371831896,-5.99615343455977,
59.648871716962));
#76939=CARTESIAN_POINT('Ctrl Pts',(-2.98803986133646,-6.07156543134177,
59.6569099777759));
#76940=CARTESIAN_POINT('Ctrl Pts',(-2.8346906192944,-6.14703421334025,59.6649542913983));
#76941=CARTESIAN_POINT('Ctrl Pts',(-2.67867426953415,-6.21659401200429,
59.6729986050208));
#76942=CARTESIAN_POINT('Ctrl Pts',(-2.52050341237357,-6.28007575975109,
59.6810429186433));
#76943=CARTESIAN_POINT('Ctrl Pts',(-2.36210941707737,-6.34364706381118,
59.6890985807099));
#76944=CARTESIAN_POINT('Ctrl Pts',(-2.20155520008267,-6.40112308495481,
59.6971542427765));
#76945=CARTESIAN_POINT('Ctrl Pts',(-2.03936627375364,-6.4523851560083,59.7052099048432));
#76946=CARTESIAN_POINT('Ctrl Pts',(-2.02127295671169,-6.4581038010773,59.7061085706834));
#76947=CARTESIAN_POINT('Ctrl Pts',(-2.00315930335778,-6.46374516653992,
59.7070072365237));
#76948=CARTESIAN_POINT('Ctrl Pts',(-1.98502604839923,-6.46930912750168,
59.7079059023639));
#76949=CARTESIAN_POINT('Ctrl Pts',(-1.8179755959339,-6.52056645544894,59.716184754427));
#76950=CARTESIAN_POINT('Ctrl Pts',(-1.64870852544739,-6.56541988083409,
59.7244636064902));
#76951=CARTESIAN_POINT('Ctrl Pts',(-1.47775383359712,-6.60367568913624,
59.7327424585533));
#76952=CARTESIAN_POINT('Ctrl Pts',(-1.30700296077214,-6.64188588733272,
59.7410114402377));
#76953=CARTESIAN_POINT('Ctrl Pts',(-1.13456881615889,-6.67351405838662,
59.749280421922));
#76954=CARTESIAN_POINT('Ctrl Pts',(-0.960996955664091,-6.69841577174815,
59.7575494036064));
#76955=CARTESIAN_POINT('Ctrl Pts',(-0.787598457064301,-6.7232926135193,
59.7658101263118));
#76956=CARTESIAN_POINT('Ctrl Pts',(-0.613064854139222,-6.74145633030057,
59.7740708490173));
#76957=CARTESIAN_POINT('Ctrl Pts',(-0.437953487104271,-6.75281317253285,
59.7823315717228));
#76958=CARTESIAN_POINT('Ctrl Pts',(-0.262983158915239,-6.7641608676952,
59.7905856410463));
#76959=CARTESIAN_POINT('Ctrl Pts',(-0.0874363452809178,-6.7687125879057,
59.79883971037));
#76960=CARTESIAN_POINT('Ctrl Pts',(0.0881227175283366,-6.76642619014317,
59.8070937796936));
#76961=CARTESIAN_POINT('Ctrl Pts',(0.263568487755914,-6.76414126784936,
59.8153425224632));
#76962=CARTESIAN_POINT('Ctrl Pts',(0.439026138577658,-6.7550270268809,59.8235912652328));
#76963=CARTESIAN_POINT('Ctrl Pts',(0.613929548963045,-6.73909337440208,
59.8318400080024));
#76964=CARTESIAN_POINT('Ctrl Pts',(0.788771168558378,-6.72316535104721,
59.8400858366131));
#76965=CARTESIAN_POINT('Ctrl Pts',(0.963058585888288,-6.70042274672029,
59.8483316652238));
#76966=CARTESIAN_POINT('Ctrl Pts',(1.13622860175855,-6.6709274890787,59.8565774938345));
#76967=CARTESIAN_POINT('Ctrl Pts',(1.30936777225028,-6.64143748518951,59.8648218536822));
#76968=CARTESIAN_POINT('Ctrl Pts',(1.48138958922909,-6.60519728369291,59.87306621353));
#76969=CARTESIAN_POINT('Ctrl Pts',(1.65173875488613,-6.56232032787239,59.8813105733777));
#76970=CARTESIAN_POINT('Ctrl Pts',(1.82208741484256,-6.51944349933693,59.8895549087511));
#76971=CARTESIAN_POINT('Ctrl Pts',(1.99076309056789,-6.4699300429887,59.8977992441246));
#76972=CARTESIAN_POINT('Ctrl Pts',(2.15722329153252,-6.41394392479928,59.906043579498));
#76973=CARTESIAN_POINT('Ctrl Pts',(2.32377430564038,-6.35792726312055,59.9142924126072));
#76974=CARTESIAN_POINT('Ctrl Pts',(2.48810709374139,-6.29543099531484,59.9225412457165));
#76975=CARTESIAN_POINT('Ctrl Pts',(2.64969617231629,-6.22666838641761,59.9307900788258));
#76976=CARTESIAN_POINT('Ctrl Pts',(2.81132951822863,-6.15788693999967,59.9390411717033));
#76977=CARTESIAN_POINT('Ctrl Pts',(2.97021733406415,-6.08283587684997,59.9472922645809));
#76978=CARTESIAN_POINT('Ctrl Pts',(3.12585648725734,-6.00177558902957,59.9555433574585));
#76979=CARTESIAN_POINT('Ctrl Pts',(3.28164598528946,-5.92063699831645,59.9638024207549));
#76980=CARTESIAN_POINT('Ctrl Pts',(3.43418024003722,-5.83347775498091,59.9720614840512));
#76981=CARTESIAN_POINT('Ctrl Pts',(3.58298213321032,-5.74060345548233,59.9803205473475));
#76982=CARTESIAN_POINT('Ctrl Pts',(3.70113944056089,-5.66685589141029,59.9868787211686));
#76983=CARTESIAN_POINT('Ctrl Pts',(3.81694387682903,-5.5895057333956,59.9934368949897));
#76984=CARTESIAN_POINT('Ctrl Pts',(3.93017071637407,-5.50872463825845,59.9999950688108));
#76985=CARTESIAN_POINT('',(-3.9288823673735,-5.5096435767971,60.));
#76986=CARTESIAN_POINT('Origin',(0.,0.,60.));
#76987=CARTESIAN_POINT('',(-6.767,6.12589399508461E-12,59.6971797838098));
#76988=CARTESIAN_POINT('Ctrl Pts',(-6.76699999999828,4.8251696278534E-6,
59.6972856394408));
#76989=CARTESIAN_POINT('Ctrl Pts',(-6.76700012330983,-0.172931943421076,
59.7054271911032));
#76990=CARTESIAN_POINT('Ctrl Pts',(-6.76036657910632,-0.346010060321547,
59.7135687427657));
#76991=CARTESIAN_POINT('Ctrl Pts',(-6.74709290135145,-0.518677530391343,
59.7217102944281));
#76992=CARTESIAN_POINT('Ctrl Pts',(-6.73382589159082,-0.691258261448973,
59.7298477562053));
#76993=CARTESIAN_POINT('Ctrl Pts',(-6.71392541802703,-0.863428392473532,
59.7379852179824));
#76994=CARTESIAN_POINT('Ctrl Pts',(-6.68743708328302,-1.03463725871978,
59.7461226797596));
#76995=CARTESIAN_POINT('Ctrl Pts',(-6.66095324210352,-1.2058170805548,59.754258761072));
#76996=CARTESIAN_POINT('Ctrl Pts',(-6.62788381370195,-1.37603559988613,
59.7623948423845));
#76997=CARTESIAN_POINT('Ctrl Pts',(-6.58832614279841,-1.54474840544311,
59.770530923697));
#76998=CARTESIAN_POINT('Ctrl Pts',(-6.54877357131926,-1.71343946204029,
59.778665956178));
#76999=CARTESIAN_POINT('Ctrl Pts',(-6.50273450992899,-1.88062483587207,
59.786800988659));
#77000=CARTESIAN_POINT('Ctrl Pts',(-6.45035713046092,-2.04577171001849,
59.79493602114));
#77001=CARTESIAN_POINT('Ctrl Pts',(-6.39795895982377,-2.21098413911664,
59.8030742828173));
#77002=CARTESIAN_POINT('Ctrl Pts',(-6.33921755402332,-2.37415610228029,
59.8112125444945));
#77003=CARTESIAN_POINT('Ctrl Pts',(-6.27433070659144,-2.53477083467593,
59.8193508061717));
#77004=CARTESIAN_POINT('Ctrl Pts',(-6.21616619078512,-2.6787457465556,59.8266459371373));
#77005=CARTESIAN_POINT('Ctrl Pts',(-6.15306435077641,-2.8206659006872,59.8339410681029));
#77006=CARTESIAN_POINT('Ctrl Pts',(-6.08520006302406,-2.9601738450591,59.8412361990685));
#77007=CARTESIAN_POINT('Ctrl Pts',(-6.00156606930072,-3.13209941785128,
59.8502265083695));
#77008=CARTESIAN_POINT('Ctrl Pts',(-5.91066731636849,-3.30042675591245,
59.8592168176706));
#77009=CARTESIAN_POINT('Ctrl Pts',(-5.8128322377742,-3.46457362102366,59.8682071269716));
#77010=CARTESIAN_POINT('Ctrl Pts',(-5.71495502541899,-3.62879117780161,
59.877201308049));
#77011=CARTESIAN_POINT('Ctrl Pts',(-5.61013564670481,-3.78882445698208,
59.8861954891264));
#77012=CARTESIAN_POINT('Ctrl Pts',(-5.49874687476357,-3.94411863504103,
59.8951896702038));
#77013=CARTESIAN_POINT('Ctrl Pts',(-5.38731626860201,-4.09947113684972,
59.9041872292208));
#77014=CARTESIAN_POINT('Ctrl Pts',(-5.26931148017941,-4.25008078234281,
59.9131847882379));
#77015=CARTESIAN_POINT('Ctrl Pts',(-5.1451475288827,-4.39542329088249,59.9221823472549));
#77016=CARTESIAN_POINT('Ctrl Pts',(-5.02099117538933,-4.54075690566689,
59.9311793556961));
#77017=CARTESIAN_POINT('Ctrl Pts',(-4.89067657261529,-4.68082384439261,
59.9401763641372));
#77018=CARTESIAN_POINT('Ctrl Pts',(-4.75465817488559,-4.81513391714017,
59.9491733725783));
#77019=CARTESIAN_POINT('Ctrl Pts',(-4.61867977633247,-4.94940449308137,
59.9581677352528));
#77020=CARTESIAN_POINT('Ctrl Pts',(-4.47700110815396,-5.07792141547894,
59.9671620979274));
#77021=CARTESIAN_POINT('Ctrl Pts',(-4.3301132284925,-5.20023157450073,59.9761564606019));
#77022=CARTESIAN_POINT('Ctrl Pts',(-4.20031611473255,-5.30831064583825,
59.9841043070679));
#77023=CARTESIAN_POINT('Ctrl Pts',(-4.06645208522247,-5.41154372129691,
59.992052153534));
#77024=CARTESIAN_POINT('Ctrl Pts',(-3.9288823673735,-5.5096435767971,60.));
#77025=CARTESIAN_POINT('Ctrl Pts',(3.0990855038472,6.01564277861012,59.0457563580462));
#77026=CARTESIAN_POINT('Ctrl Pts',(2.93373232018322,6.10082796552483,59.0545058059455));
#77027=CARTESIAN_POINT('Ctrl Pts',(2.76486502144412,6.17919158180197,59.0632552538448));
#77028=CARTESIAN_POINT('Ctrl Pts',(2.59305716434331,6.25046746591388,59.0720047017441));
#77029=CARTESIAN_POINT('Ctrl Pts',(2.42125069459259,6.32174277447234,59.0807540789916));
#77030=CARTESIAN_POINT('Ctrl Pts',(2.24650397871033,6.38593035557835,59.089503456239));
#77031=CARTESIAN_POINT('Ctrl Pts',(2.06941053323744,6.44281220003548,59.0982528334864));
#77032=CARTESIAN_POINT('Ctrl Pts',(1.89231845896655,6.49969360406694,59.107002142989));
#77033=CARTESIAN_POINT('Ctrl Pts',(1.71287996431475,6.54926929700888,59.1157514524916));
#77034=CARTESIAN_POINT('Ctrl Pts',(1.53170449173474,6.59137090065486,59.1245007619942));
#77035=CARTESIAN_POINT('Ctrl Pts',(1.35053036178139,6.6334721923009,59.1332500066587));
#77036=CARTESIAN_POINT('Ctrl Pts',(1.16761955878813,6.6680994406246,59.1419992513233));
#77037=CARTESIAN_POINT('Ctrl Pts',(0.983593309310163,6.69513503985396,59.1507484959879));
#77038=CARTESIAN_POINT('Ctrl Pts',(0.7995683624596,6.72217044771219,59.1594976787211));
#77039=CARTESIAN_POINT('Ctrl Pts',(0.614428268438157,6.74161427235981,59.1682468614543));
#77040=CARTESIAN_POINT('Ctrl Pts',(0.428801816329773,6.75340047696805,59.1769960441875));
#77041=CARTESIAN_POINT('Ctrl Pts',(0.243176616522205,6.76518660206244,59.1857451678956));
#77042=CARTESIAN_POINT('Ctrl Pts',(0.0570653511647989,6.76931519233997,
59.1944942916037));
#77043=CARTESIAN_POINT('Ctrl Pts',(-0.128899900800774,6.76577222610794,
59.2032434153119));
#77044=CARTESIAN_POINT('Ctrl Pts',(-0.314863959942781,6.76222928260129,
59.2119924829011));
#77045=CARTESIAN_POINT('Ctrl Pts',(-0.500681721081455,6.75101488651271,
59.2207415504904));
#77046=CARTESIAN_POINT('Ctrl Pts',(-0.685722110174087,6.73216712415983,
59.2294906180797));
#77047=CARTESIAN_POINT('Ctrl Pts',(-0.870761373828302,6.71331947644136,
59.238239632456));
#77048=CARTESIAN_POINT('Ctrl Pts',(-1.05502298984402,6.68683858439987,59.2469886468324));
#77049=CARTESIAN_POINT('Ctrl Pts',(-1.23788117676109,6.65281438131417,59.2557376612087));
#77050=CARTESIAN_POINT('Ctrl Pts',(-1.43009641451833,6.61704912302368,59.2649343720963));
#77051=CARTESIAN_POINT('Ctrl Pts',(-1.62076048992727,6.57294837083157,59.2741310829838));
#77052=CARTESIAN_POINT('Ctrl Pts',(-1.80915798961154,6.52067760042043,59.2833277938713));
#77053=CARTESIAN_POINT('Ctrl Pts',(-1.98840443003037,6.47094578577401,59.2920777915778));
#77054=CARTESIAN_POINT('Ctrl Pts',(-2.1655989595222,6.41381888474466,59.3008277892843));
#77055=CARTESIAN_POINT('Ctrl Pts',(-2.34013966242353,6.34949095285223,59.3095777869908));
#77056=CARTESIAN_POINT('Ctrl Pts',(-2.51467682554033,6.28516432556677,59.3183276072424));
#77057=CARTESIAN_POINT('Ctrl Pts',(-2.68656000078849,6.21363705879657,59.327077427494));
#77058=CARTESIAN_POINT('Ctrl Pts',(-2.85520533840885,6.13515211510861,59.3358272477456));
#77059=CARTESIAN_POINT('Ctrl Pts',(-3.0238474799832,6.05666865881125,59.3445769021768));
#77060=CARTESIAN_POINT('Ctrl Pts',(-3.18925164684526,5.9712279103985,59.3533265566081));
#77061=CARTESIAN_POINT('Ctrl Pts',(-3.35085601829143,5.87912008251916,59.3620762110393));
#77062=CARTESIAN_POINT('Ctrl Pts',(-3.51245754191409,5.7870138777818,59.3708257112825));
#77063=CARTESIAN_POINT('Ctrl Pts',(-3.67025915510932,5.68824097060985,59.3795752115256));
#77064=CARTESIAN_POINT('Ctrl Pts',(-3.82372487928835,5.58313684656854,59.3883247117687));
#77065=CARTESIAN_POINT('Ctrl Pts',(-3.97718810300798,5.47803443501773,59.3970740694539));
#77066=CARTESIAN_POINT('Ctrl Pts',(-4.12631534263025,5.36660117496376,59.405823427139));
#77067=CARTESIAN_POINT('Ctrl Pts',(-4.27060009886224,5.24921554097352,59.4145727848241));
#77068=CARTESIAN_POINT('Ctrl Pts',(-4.41488269594212,5.13183166360292,59.4233220115793));
#77069=CARTESIAN_POINT('Ctrl Pts',(-4.55432273235087,5.00849577139472,59.4320712383345));
#77070=CARTESIAN_POINT('Ctrl Pts',(-4.68844662480206,4.87962675277343,59.4408204650896));
#77071=CARTESIAN_POINT('Ctrl Pts',(-4.82256868835157,4.75075949139883,59.4495695725411));
#77072=CARTESIAN_POINT('Ctrl Pts',(-4.95137454637862,4.61635945312526,59.4583186799926));
#77073=CARTESIAN_POINT('Ctrl Pts',(-5.07442674461078,4.47688309134591,59.4670677874441));
#77074=CARTESIAN_POINT('Ctrl Pts',(-5.19747742838537,4.33740844616353,59.4758167872165));
#77075=CARTESIAN_POINT('Ctrl Pts',(-5.31477440450924,4.19285781736032,59.4845657869889));
#77076=CARTESIAN_POINT('Ctrl Pts',(-5.42591931531149,4.04372211999411,59.4933147867612));
#77077=CARTESIAN_POINT('Ctrl Pts',(-5.53707636462981,3.89457013500802,59.5020647420418));
#77078=CARTESIAN_POINT('Ctrl Pts',(-5.64207983273473,3.74083230916417,59.5108146973224));
#77079=CARTESIAN_POINT('Ctrl Pts',(-5.74057303468752,3.58303087251819,59.519564652603));
#77080=CARTESIAN_POINT('Ctrl Pts',(-5.83906243363768,3.42523552887426,59.5283142700318));
#77081=CARTESIAN_POINT('Ctrl Pts',(-5.93104191768426,3.26337713156991,59.5370638874606));
#77082=CARTESIAN_POINT('Ctrl Pts',(-6.01619906699655,3.09800545291158,59.5458135048894));
#77083=CARTESIAN_POINT('Ctrl Pts',(-6.10135338095373,2.93263928039616,59.5545628309948));
#77084=CARTESIAN_POINT('Ctrl Pts',(-6.17968568352821,2.76376031540263,59.5633121571001));
#77085=CARTESIAN_POINT('Ctrl Pts',(-6.25092992694862,2.59194213831601,59.5720614832055));
#77086=CARTESIAN_POINT('Ctrl Pts',(-6.32217217691089,2.42012876880859,59.5808105644993));
#77087=CARTESIAN_POINT('Ctrl Pts',(-6.38632665483844,2.2453766164769,59.5895596457932));
#77088=CARTESIAN_POINT('Ctrl Pts',(-6.44317547869351,2.06827917621455,59.598308727087));
#77089=CARTESIAN_POINT('Ctrl Pts',(-6.50002944235937,1.89116572423421,59.6070585994019));
#77090=CARTESIAN_POINT('Ctrl Pts',(-6.54957634250399,1.71170683289195,59.6158084717169));
#77091=CARTESIAN_POINT('Ctrl Pts',(-6.59164787708396,1.5305120922536,59.6245583440318));
#77092=CARTESIAN_POINT('Ctrl Pts',(-6.63371649075008,1.34932993148032,59.6333076088666));
#77093=CARTESIAN_POINT('Ctrl Pts',(-6.66831071257123,1.16641244174011,59.6420568737014));
#77094=CARTESIAN_POINT('Ctrl Pts',(-6.69531304840331,0.982380875160149,
59.6508061385362));
#77095=CARTESIAN_POINT('Ctrl Pts',(-6.72231677033042,0.798339861795978,
59.6595558524919));
#77096=CARTESIAN_POINT('Ctrl Pts',(-6.74172778477889,0.61318494073029,59.6683055664475));
#77097=CARTESIAN_POINT('Ctrl Pts',(-6.75348015835517,0.427545027690687,
59.6770552804032));
#77098=CARTESIAN_POINT('Ctrl Pts',(-6.76249038365208,0.285219953548977,
59.6837634482054));
#77099=CARTESIAN_POINT('Ctrl Pts',(-6.76699999999987,0.142609995761487,
59.6904716160076));
#77100=CARTESIAN_POINT('Ctrl Pts',(-6.767,6.12589398735536E-12,59.6971797838098));
#77101=CARTESIAN_POINT('Ctrl Pts',(-2.92312393079455,6.09699903205172,-60.6636842274549));
#77102=CARTESIAN_POINT('Ctrl Pts',(-3.93696870157765,5.61092651139488,-60.6107538653005));
#77103=CARTESIAN_POINT('Ctrl Pts',(-5.71385275345024,4.12729922236996,-60.5049022361689));
#77104=CARTESIAN_POINT('Ctrl Pts',(-6.99683237773153,0.880191322515334,
-60.3461293400603));
#77105=CARTESIAN_POINT('Ctrl Pts',(-6.55662514285608,-2.55525940431229,
-60.1873655391287));
#77106=CARTESIAN_POINT('Ctrl Pts',(-3.87957147477697,-6.36386071307339,
-59.9756804712201));
#77107=CARTESIAN_POINT('Ctrl Pts',(2.33603082002131,-7.64687216116862,-59.7110741363342));
#77108=CARTESIAN_POINT('Ctrl Pts',(7.70057569811667,-2.15972995654168,-59.3935465344711));
#77109=CARTESIAN_POINT('Ctrl Pts',(6.26959392394697,4.02615150262351,-59.1289401995852));
#77110=CARTESIAN_POINT('Ctrl Pts',(2.40708136811262,6.61358385766357,-58.9172551316766));
#77111=CARTESIAN_POINT('Ctrl Pts',(-1.05041112263128,6.97500520632018,-58.758491330745));
#77112=CARTESIAN_POINT('Ctrl Pts',(-4.24145056983912,5.61648152126252,-58.5997275298136));
#77113=CARTESIAN_POINT('Ctrl Pts',(-7.18314404472123,1.99726048125854,-58.3880424619048));
#77114=CARTESIAN_POINT('Ctrl Pts',(-6.80569859354872,-3.04864719331499,
-58.1763573939962));
#77115=CARTESIAN_POINT('Ctrl Pts',(-3.35804436576745,-6.17750544855752,
-57.9646723260874));
#77116=CARTESIAN_POINT('Ctrl Pts',(1.11993342530363,-7.36667282618036,-57.7529872581789));
#77117=CARTESIAN_POINT('Ctrl Pts',(6.71700196989707,-4.34658677302633,-57.4883809232929));
#77118=CARTESIAN_POINT('Ctrl Pts',(7.27905940725944,3.30630186467041,-57.17085332143));
#77119=CARTESIAN_POINT('Ctrl Pts',(2.20588712983283,7.11743132022739,-56.9062469865439));
#77120=CARTESIAN_POINT('Ctrl Pts',(-2.41771698918159,6.61000287796941,-56.6945619186354));
#77121=CARTESIAN_POINT('Ctrl Pts',(-5.29460658627333,4.66012616950757,-56.5357981177038));
#77122=CARTESIAN_POINT('Ctrl Pts',(-6.86186273884577,1.56597944961906,-56.3770343167724));
#77123=CARTESIAN_POINT('Ctrl Pts',(-6.78168957233196,-3.09729046827898,
-56.1653492488635));
#77124=CARTESIAN_POINT('Ctrl Pts',(-3.24397994606998,-6.7148219785863,-55.953664180955));
#77125=CARTESIAN_POINT('Ctrl Pts',(1.40863712635378,-6.88867756320579,-55.7419791130463));
#77126=CARTESIAN_POINT('Ctrl Pts',(5.60038102276455,-4.91503719715207,-55.5302940451375));
#77127=CARTESIAN_POINT('Ctrl Pts',(7.93799707766255,0.999673053673553,-55.2656877102517));
#77128=CARTESIAN_POINT('Ctrl Pts',(3.44015086769524,7.21676185626268,-54.9481601083886));
#77129=CARTESIAN_POINT('Ctrl Pts',(-2.8953477620337,6.86590885072102,-54.6835537735029));
#77130=CARTESIAN_POINT('Ctrl Pts',(-6.1060944895583,3.50044640710944,-54.4718687055941));
#77131=CARTESIAN_POINT('Ctrl Pts',(-7.05161310117804,0.156122379568802,
-54.3131049046626));
#77132=CARTESIAN_POINT('Ctrl Pts',(-6.25832624994688,-3.22037419800652,
-54.1543411037311));
#77133=CARTESIAN_POINT('Ctrl Pts',(-3.19421094982843,-6.73658192074147,
-53.9426560358224));
#77134=CARTESIAN_POINT('Ctrl Pts',(1.84186590314193,-7.22632474479682,-53.7309709679136));
#77135=CARTESIAN_POINT('Ctrl Pts',(5.5134977225823,-4.36342534981377,-53.5192859000051));
#77136=CARTESIAN_POINT('Ctrl Pts',(7.44970212626647,-0.154258536351977,
-53.3076008320962));
#77137=CARTESIAN_POINT('Ctrl Pts',(5.42959217157294,5.87628054081612,-53.0429944972106));
#77138=CARTESIAN_POINT('Ctrl Pts',(-2.01498652368906,7.73667364412597,-52.7254668953474));
#77139=CARTESIAN_POINT('Ctrl Pts',(-6.63630755816859,3.38868188023253,-52.4608605604616));
#77140=CARTESIAN_POINT('Ctrl Pts',(-6.92573590590944,-1.25367347471575,
-52.2491754925529));
#77141=CARTESIAN_POINT('Ctrl Pts',(-5.49566665660641,-4.42122941071933,
-52.0904116916214));
#77142=CARTESIAN_POINT('Ctrl Pts',(-2.71453384249522,-6.49374802783983,
-51.9316478906898));
#77143=CARTESIAN_POINT('Ctrl Pts',(1.8939556401918,-7.21092584926551,-51.7199628227812));
#77144=CARTESIAN_POINT('Ctrl Pts',(6.06237564429645,-4.3427918283758,-51.5082777548724));
#77145=CARTESIAN_POINT('Ctrl Pts',(7.0280343009548,0.211829618358026,-51.2965926869638));
#77146=CARTESIAN_POINT('Ctrl Pts',(5.7990414182339,4.67899306415061,-51.084907619055));
#77147=CARTESIAN_POINT('Ctrl Pts',(0.370283363009991,7.9921232707625,-50.8203012841692));
#77148=CARTESIAN_POINT('Ctrl Pts',(-6.5234529958798,4.62178004425476,-50.5027736823062));
#77149=CARTESIAN_POINT('Ctrl Pts',(-7.25943048449507,-1.68059868276578,
-50.2381673474203));
#77150=CARTESIAN_POINT('Ctrl Pts',(-4.49156266215061,-5.41879874803109,
-50.0264822795117));
#77151=CARTESIAN_POINT('Ctrl Pts',(-1.3577735496372,-6.92142127677832,-49.86771847858));
#77152=CARTESIAN_POINT('Ctrl Pts',(2.10458729961294,-6.71626158881723,-49.7089546776486));
#77153=CARTESIAN_POINT('Ctrl Pts',(6.09231344885727,-4.29746860506485,-49.4972696097399));
#77154=CARTESIAN_POINT('Ctrl Pts',(7.43469033521331,0.58104985727342,-49.2855845418312));
#77155=CARTESIAN_POINT('Ctrl Pts',(5.24069490095294,4.68756385319076,-49.0738994739225));
#77156=CARTESIAN_POINT('Ctrl Pts',(1.42390403077878,7.31398350940805,-48.8622144060138));
#77157=CARTESIAN_POINT('Ctrl Pts',(-4.86299012607282,6.35314655723462,-48.5976080711279));
#77158=CARTESIAN_POINT('Ctrl Pts',(-7.96710335872743,-0.664495175513357,
-48.280080469265));
#77159=CARTESIAN_POINT('Ctrl Pts',(-4.47196403319157,-5.96030876528817,
-48.015474134379));
#77160=CARTESIAN_POINT('Ctrl Pts',(0.0528141213109033,-7.03809105427595,
-47.8037890664705));
#77161=CARTESIAN_POINT('Ctrl Pts',(3.41802194588758,-6.16982556318776,-47.6450252655387));
#77162=CARTESIAN_POINT('Ctrl Pts',(5.93494174663343,-3.7833746702093,-47.4862614646075));
#77163=CARTESIAN_POINT('Ctrl Pts',(7.42841097714051,0.635003878211527,-47.2745763966986));
#77164=CARTESIAN_POINT('Ctrl Pts',(5.31407594064479,5.23190560065949,-47.06289132879));
#77165=CARTESIAN_POINT('Ctrl Pts',(0.991198393882503,6.96101024755598,-46.8512062608813));
#77166=CARTESIAN_POINT('Ctrl Pts',(-3.62020483763898,6.51275474728599,-46.6395211929726));
#77167=CARTESIAN_POINT('Ctrl Pts',(-7.81155787921683,1.7293662549123,-46.3749148580867));
#77168=CARTESIAN_POINT('Ctrl Pts',(-5.66768900817763,-5.63858059031783,
-46.0573872562237));
#77169=CARTESIAN_POINT('Ctrl Pts',(0.416498227822971,-7.43977634865123,
-45.7927809213378));
#77170=CARTESIAN_POINT('Ctrl Pts',(4.5723780380445,-5.35078256864332,-45.5810958534292));
#77171=CARTESIAN_POINT('Ctrl Pts',(6.58797943991901,-2.51955321474632,-45.4223320524976));
#77172=CARTESIAN_POINT('Ctrl Pts',(6.97697150051971,0.926998442312364,-45.2635682515661));
#77173=CARTESIAN_POINT('Ctrl Pts',(5.27452955658915,5.26914201054712,-45.0518831836575));
#77174=CARTESIAN_POINT('Ctrl Pts',(0.696828925394616,7.42473358214861,-44.8401981157487));
#77175=CARTESIAN_POINT('Ctrl Pts',(-3.72397799269562,5.96406956972614,-44.6285130478401));
#77176=CARTESIAN_POINT('Ctrl Pts',(-6.96348714803389,2.65173607358044,-44.4168279799313));
#77177=CARTESIAN_POINT('Ctrl Pts',(-7.09013851937479,-3.70689626507969,
-44.1522216450455));
#77178=CARTESIAN_POINT('Ctrl Pts',(-0.705509311452106,-7.96357623046209,
-43.8346940431824));
#77179=CARTESIAN_POINT('Ctrl Pts',(5.10928337137563,-5.42392536109363,-43.5700877082966));
#77180=CARTESIAN_POINT('Ctrl Pts',(6.94377013876049,-1.14959613767053,-43.3584026403879));
#77181=CARTESIAN_POINT('Ctrl Pts',(6.66280533293569,2.31444304275086,-43.1996388394564));
#77182=CARTESIAN_POINT('Ctrl Pts',(4.74111534605175,5.20185377596739,-43.0408750385248));
#77183=CARTESIAN_POINT('Ctrl Pts',(0.642595000024069,7.4277581568458,-42.8291899706162));
#77184=CARTESIAN_POINT('Ctrl Pts',(-4.24779877571826,6.12931031015385,-42.6175049027075));
#77185=CARTESIAN_POINT('Ctrl Pts',(-6.68957363577079,2.16511951037697,-42.4058198347988));
#77186=CARTESIAN_POINT('Ctrl Pts',(-7.03521870122052,-2.45510799981555,
-42.1941347668902));
#77187=CARTESIAN_POINT('Ctrl Pts',(-3.03766568752031,-7.40160329353348,
-41.9295284320042));
#77188=CARTESIAN_POINT('Ctrl Pts',(4.58812924676499,-6.54716425499665,-41.6120008301413));
#77189=CARTESIAN_POINT('Ctrl Pts',(7.40165051643521,-0.859832846711758,
-41.3473944952554));
#77190=CARTESIAN_POINT('Ctrl Pts',(6.05287482910103,3.59168780978024,-41.1357094273467));
#77191=CARTESIAN_POINT('Ctrl Pts',(3.6073452975506,6.06107922790767,-40.9769456264152));
#77192=CARTESIAN_POINT('Ctrl Pts',(0.277812056168763,7.03280014592772,-40.8181818254836));
#77193=CARTESIAN_POINT('Ctrl Pts',(-4.29124033042278,6.09670205908065,-40.606496757575));
#77194=CARTESIAN_POINT('Ctrl Pts',(-7.19674686893622,1.95424507716112,-40.3948116896662));
#77195=CARTESIAN_POINT('Ctrl Pts',(-6.51230720008338,-2.65103618503351,
-40.1831266217576));
#77196=CARTESIAN_POINT('Ctrl Pts',(-3.80169893709803,-6.40850549320421,
-39.9714415538489));
#77197=CARTESIAN_POINT('Ctrl Pts',(2.44194806796726,-7.61892602519113,-39.706835218963));
#77198=CARTESIAN_POINT('Ctrl Pts',(7.72619583474277,-2.05479626487146,-39.3893076171001));
#77199=CARTESIAN_POINT('Ctrl Pts',(6.21661117867084,4.10822204182721,-39.1247012822141));
#77200=CARTESIAN_POINT('Ctrl Pts',(2.31824809444377,6.64554292682674,-38.9130162143055));
#77201=CARTESIAN_POINT('Ctrl Pts',(-1.14289969095182,6.96012943839095,-38.7542524133739));
#77202=CARTESIAN_POINT('Ctrl Pts',(-4.31601150658888,5.55963147214867,-38.5954886124424));
#77203=CARTESIAN_POINT('Ctrl Pts',(-7.20898655868447,1.90132384599566,-38.3838035445337));
#77204=CARTESIAN_POINT('Ctrl Pts',(-6.76455528773798,-3.13895381875682,
-38.172118476625));
#77205=CARTESIAN_POINT('Ctrl Pts',(-3.27546111720417,-6.2216952988955,-37.9604334087163));
#77206=CARTESIAN_POINT('Ctrl Pts',(1.217916036499,-7.35109093895588,-37.7487483408077));
#77207=CARTESIAN_POINT('Ctrl Pts',(6.77429797690968,-4.25676297954459,-37.4841420059218));
#77208=CARTESIAN_POINT('Ctrl Pts',(7.23437967918326,3.40294584505053,-37.1666144040588));
#77209=CARTESIAN_POINT('Ctrl Pts',(2.11091462183016,7.14617256656133,-36.9020080691729));
#77210=CARTESIAN_POINT('Ctrl Pts',(-2.50552638293833,6.5772222529035,-36.6903230012642));
#77211=CARTESIAN_POINT('Ctrl Pts',(-5.35619325413247,4.58920639404244,-36.5315592003327));
#77212=CARTESIAN_POINT('Ctrl Pts',(-6.88210809687881,1.47446450414678,-36.3727953994011));
#77213=CARTESIAN_POINT('Ctrl Pts',(-6.73984272261571,-3.18732484146961,
-36.1611103314925));
#77214=CARTESIAN_POINT('Ctrl Pts',(-3.15427412249773,-6.75742510704284,
-35.9494252635838));
#77215=CARTESIAN_POINT('Ctrl Pts',(1.50024575056515,-6.86930859770662,-35.7377401956751));
#77216=CARTESIAN_POINT('Ctrl Pts',(5.66533577993045,-4.8400235500874,-35.5260551277664));
#77217=CARTESIAN_POINT('Ctrl Pts',(7.92398104023708,1.1052911914726,-35.2614487928805));
#77218=CARTESIAN_POINT('Ctrl Pts',(3.34374339023025,7.26193293188651,-34.9439211910175));
#77219=CARTESIAN_POINT('Ctrl Pts',(-2.98652130102637,6.82674398306001,-34.6793148561316));
#77220=CARTESIAN_POINT('Ctrl Pts',(-6.15216696733666,3.41882386584927,-34.467629788223));
#77221=CARTESIAN_POINT('Ctrl Pts',(-7.05306685073663,0.0622053194999262,
-34.3088659872914));
#77222=CARTESIAN_POINT('Ctrl Pts',(-6.21488702937856,-3.3034280139237,-34.15010218636));
#77223=CARTESIAN_POINT('Ctrl Pts',(-3.10421963643972,-6.77852048897011,
-33.9384171184512));
#77224=CARTESIAN_POINT('Ctrl Pts',(1.93793235897052,-7.20115667717395,-33.7267320505425));
#77225=CARTESIAN_POINT('Ctrl Pts',(5.57111465182142,-4.28961763550966,-33.5150469826339));
#77226=CARTESIAN_POINT('Ctrl Pts',(7.45109575912954,-0.0550404673175772,
-33.3033619147252));
#77227=CARTESIAN_POINT('Ctrl Pts',(5.35085890249345,5.94806297458176,-33.0387555798393));
#77228=CARTESIAN_POINT('Ctrl Pts',(-2.11783372013389,7.70915495374104,-32.7212279779763));
#77229=CARTESIAN_POINT('Ctrl Pts',(-6.68084470050438,3.30000863324214,-32.4566216430904));
#77230=CARTESIAN_POINT('Ctrl Pts',(-6.90842719020237,-1.34578927673002,
-32.2449365751818));
#77231=CARTESIAN_POINT('Ctrl Pts',(-5.43630380155726,-4.49402074760545,
-32.0861727742502));
#77232=CARTESIAN_POINT('Ctrl Pts',(-2.62781877401236,-6.5293204793502,-31.9274089733187));
#77233=CARTESIAN_POINT('Ctrl Pts',(1.9898124172897,-7.1850654913261,-31.71572390541));
#77234=CARTESIAN_POINT('Ctrl Pts',(6.11966913731047,-4.26167677880455,-31.5040388375013));
#77235=CARTESIAN_POINT('Ctrl Pts',(7.02459028872639,0.305400062451879,-31.2923537695926));
#77236=CARTESIAN_POINT('Ctrl Pts',(5.73621913850456,4.755801452943,-31.0806687016839));
#77237=CARTESIAN_POINT('Ctrl Pts',(0.263822956621364,7.99634551476757,-30.8160623667981));
#77238=CARTESIAN_POINT('Ctrl Pts',(-6.58442076827012,4.53450029367066,-30.498534764935));
#77239=CARTESIAN_POINT('Ctrl Pts',(-7.23640700599555,-1.77712029286393,
-30.2339284300492));
#77240=CARTESIAN_POINT('Ctrl Pts',(-4.41900465028644,-5.47813042199944,
-30.0222433621405));
#77241=CARTESIAN_POINT('Ctrl Pts',(-1.26548364847116,-6.93888842958194,
-29.863479561209));
#77242=CARTESIAN_POINT('Ctrl Pts',(2.19383817480087,-6.68764020368173,-29.7047157602774));
#77243=CARTESIAN_POINT('Ctrl Pts',(6.14900073797299,-4.21595890575949,-29.4930306923688));
#77244=CARTESIAN_POINT('Ctrl Pts',(7.42629352233101,0.680002821564867,-29.28134562446));
#77245=CARTESIAN_POINT('Ctrl Pts',(5.17780799600353,4.75693622819738,-29.0696605565514));
#77246=CARTESIAN_POINT('Ctrl Pts',(1.32638068810365,7.33229648438925,-28.8579754886427));
#77247=CARTESIAN_POINT('Ctrl Pts',(-4.9471609732356,6.28782493783651,-28.5933691537568));
#77248=CARTESIAN_POINT('Ctrl Pts',(-7.95754813273417,-0.770530649711755,
-28.2758415518938));
#77249=CARTESIAN_POINT('Ctrl Pts',(-4.39219670953444,-6.0193314376669,-28.0112352170079));
#77250=CARTESIAN_POINT('Ctrl Pts',(0.146532586535858,-7.03676368942229,
-27.7995501490993));
#77251=CARTESIAN_POINT('Ctrl Pts',(3.4998797126913,-6.12376220141065,-27.6407863481677));
#77252=CARTESIAN_POINT('Ctrl Pts',(5.9847970280502,-3.7040062046594,-27.4820225472362));
#77253=CARTESIAN_POINT('Ctrl Pts',(7.41929623919157,0.733868439001849,-27.2703374793275));
#77254=CARTESIAN_POINT('Ctrl Pts',(5.24393377056136,5.30220689214575,-27.0586524114188));
#77255=CARTESIAN_POINT('Ctrl Pts',(0.898413807847284,6.97359237068558,-26.8469673435102));
#77256=CARTESIAN_POINT('Ctrl Pts',(-3.70661131342256,6.46396859800302,-26.6352822756014));
#77257=CARTESIAN_POINT('Ctrl Pts',(-7.83389444007708,1.62518984912946,-26.3706759407156));
#77258=CARTESIAN_POINT('Ctrl Pts',(-5.59209997235955,-5.71355473116891,
-26.0531483388526));
#77259=CARTESIAN_POINT('Ctrl Pts',(0.515533510984028,-7.43357034612457,
-25.7885420039666));
#77260=CARTESIAN_POINT('Ctrl Pts',(4.64322661531511,-5.28941978089454,-25.576856936058));
#77261=CARTESIAN_POINT('Ctrl Pts',(6.62094706514696,-2.43160059698462,-25.4180931351265));
#77262=CARTESIAN_POINT('Ctrl Pts',(6.96400842882034,1.01982549214703,-25.259329334195));
#77263=CARTESIAN_POINT('Ctrl Pts',(5.20389503224099,5.3389133785877,-25.0476442662863));
#77264=CARTESIAN_POINT('Ctrl Pts',(0.597895242178444,7.43335459913841,-24.8359591983776));
#77265=CARTESIAN_POINT('Ctrl Pts',(-3.80306866895886,5.91395017072331,-24.6242741304689));
#77266=CARTESIAN_POINT('Ctrl Pts',(-6.99818169797508,2.55877126505823,-24.4125890625602));
#77267=CARTESIAN_POINT('Ctrl Pts',(-7.04014674245482,-3.8009838185247,-24.1479827276743));
#77268=CARTESIAN_POINT('Ctrl Pts',(-0.599399329136246,-7.97226506152157,
-23.8304551258113));
#77269=CARTESIAN_POINT('Ctrl Pts',(5.18105835187421,-5.35540635677676,-23.5658487909255));
#77270=CARTESIAN_POINT('Ctrl Pts',(6.95846310331139,-1.05702708552953,-23.3541637230168));
#77271=CARTESIAN_POINT('Ctrl Pts',(6.63139413153894,2.40296345684338,-23.1953999220853));
#77272=CARTESIAN_POINT('Ctrl Pts',(4.6714241668463,5.26452786909883,-23.0366361211537));
#77273=CARTESIAN_POINT('Ctrl Pts',(0.543625848766956,7.43565669643223,-22.824951053245));
#77274=CARTESIAN_POINT('Ctrl Pts',(-4.32904344307952,6.07220076949717,-22.6132659853364));
#77275=CARTESIAN_POINT('Ctrl Pts',(-6.71781241570783,2.07584543499186,-22.4015809174276));
#77276=CARTESIAN_POINT('Ctrl Pts',(-7.00190130512566,-2.54857520549042,
-22.189895849519));
#77277=CARTESIAN_POINT('Ctrl Pts',(-2.93883245980067,-7.44139825014128,
-21.9252895146331));
#77278=CARTESIAN_POINT('Ctrl Pts',(4.67490811358557,-6.48548563304697,-21.6077619127701));
#77279=CARTESIAN_POINT('Ctrl Pts',(7.41244423136772,-0.761192097038367,
-21.3431555778842));
#77280=CARTESIAN_POINT('Ctrl Pts',(6.00450920570145,3.67197279651351,-21.1314705099755));
#77281=CARTESIAN_POINT('Ctrl Pts',(3.52631272330616,6.10857921944075,-20.972706709044));
#77282=CARTESIAN_POINT('Ctrl Pts',(0.184134731243384,7.03587605290655,-20.8139429081125));
#77283=CARTESIAN_POINT('Ctrl Pts',(-4.37204691618338,6.03901691778854,-20.6022578402038));
#77284=CARTESIAN_POINT('Ctrl Pts',(-7.22213255654739,1.85823589805217,-20.3905727722951));
#77285=CARTESIAN_POINT('Ctrl Pts',(-6.47642708112463,-2.73752263652566,
-20.1788877043864));
#77286=CARTESIAN_POINT('Ctrl Pts',(-3.71602260761794,-6.45856280022372,
-19.9672026364777));
#77287=CARTESIAN_POINT('Ctrl Pts',(2.54318941299879,-7.58573211717858,-19.7025963015919));
#77288=CARTESIAN_POINT('Ctrl Pts',(7.75287357221985,-1.95172773206238,-19.3850686997289));
#77289=CARTESIAN_POINT('Ctrl Pts',(6.16135257878985,4.19064163244365,-19.120462364843));
#77290=CARTESIAN_POINT('Ctrl Pts',(2.2295467787481,6.67582475661716,-18.9087772969343));
#77291=CARTESIAN_POINT('Ctrl Pts',(-1.23548331867775,6.94429279855072,-18.7500134960028));
#77292=CARTESIAN_POINT('Ctrl Pts',(-4.38966396424912,5.50166408571866,-18.5912496950713));
#77293=CARTESIAN_POINT('Ctrl Pts',(-7.23366643236317,1.80515636883538,-18.3795646271625));
#77294=CARTESIAN_POINT('Ctrl Pts',(-6.72215541861812,-3.22875608324548,
-18.1678795592539));
#77295=CARTESIAN_POINT('Ctrl Pts',(-3.19231911765856,-6.26476149375589,
-17.9561944913452));
#77296=CARTESIAN_POINT('Ctrl Pts',(1.31569927410357,-7.33422067331522,-17.7445094234365));
#77297=CARTESIAN_POINT('Ctrl Pts',(6.83038273611529,-4.1661752030084,-17.4799030885506));
#77298=CARTESIAN_POINT('Ctrl Pts',(7.18842268592018,3.49898114534428,-17.1623754866876));
#77299=CARTESIAN_POINT('Ctrl Pts',(2.01556502657803,7.17364903764925,-16.8977691518017));
#77300=CARTESIAN_POINT('Ctrl Pts',(-2.59289018175187,6.54327406770214,-16.686084083893));
#77301=CARTESIAN_POINT('Ctrl Pts',(-5.41683075771138,4.51747341387265,-16.5273202829615));
#77302=CARTESIAN_POINT('Ctrl Pts',(-6.90113265742603,1.38268777231947,-16.36855648203));
#77303=CARTESIAN_POINT('Ctrl Pts',(-6.69680090920865,-3.27679373062556,
-16.1568714141213));
#77304=CARTESIAN_POINT('Ctrl Pts',(-3.06400879141773,-6.79883000546907,
-15.9451863462126));
#77305=CARTESIAN_POINT('Ctrl Pts',(1.59158827167064,-6.84872139133249,-15.7335012783039));
#77306=CARTESIAN_POINT('Ctrl Pts',(5.72928589328394,-4.76415161574215,-15.5218162103953));
#77307=CARTESIAN_POINT('Ctrl Pts',(7.90855975212633,1.21071333974291,-15.2572098755094));
#77308=CARTESIAN_POINT('Ctrl Pts',(3.24674295129907,7.30581617446789,-14.9396822736464));
#77309=CARTESIAN_POINT('Ctrl Pts',(-3.07716522097081,6.78636847618651,-14.6750759387605));
#77310=CARTESIAN_POINT('Ctrl Pts',(-6.19714842559212,3.33659503249492,-14.4633908708518));
#77311=CARTESIAN_POINT('Ctrl Pts',(-7.05326982105232,-0.0317227704806144,
-14.3046270699203));
#77312=CARTESIAN_POINT('Ctrl Pts',(-6.1703456687824,-3.3858960053215,-14.1458632689888));
#77313=CARTESIAN_POINT('Ctrl Pts',(-3.01367782577689,-6.81925696341364,
-13.9341782010801));
#77314=CARTESIAN_POINT('Ctrl Pts',(2.03365514493514,-7.17471156692939,-13.7224931331714));
#77315=CARTESIAN_POINT('Ctrl Pts',(5.62774360737277,-4.21504920639009,-13.5108080652627));
#77316=CARTESIAN_POINT('Ctrl Pts',(7.45116802533417,0.0441873624320021,
-13.299122997354));
#77317=CARTESIAN_POINT('Ctrl Pts',(5.27117671963474,6.01879058734929,-13.0345166624682));
#77318=CARTESIAN_POINT('Ctrl Pts',(-2.22030534292114,7.68026913272724,-12.7169890606051));
#77319=CARTESIAN_POINT('Ctrl Pts',(-6.72419707133592,3.21075016741692,-12.4523827257193));
#77320=CARTESIAN_POINT('Ctrl Pts',(-6.88989334381324,-1.43766641839012,
-12.2406976578106));
#77321=CARTESIAN_POINT('Ctrl Pts',(-5.37597688010952,-4.56601512122575,
-12.081933856879));
#77322=CARTESIAN_POINT('Ctrl Pts',(-2.54063769187477,-6.56373503043344,
-11.9231700559475));
#77323=CARTESIAN_POINT('Ctrl Pts',(2.08531632387576,-7.15793094406632,-11.7114849880388));
#77324=CARTESIAN_POINT('Ctrl Pts',(6.17587737688397,-4.17980596952113,-11.4997999201302));
#77325=CARTESIAN_POINT('Ctrl Pts',(7.01990054562355,0.398916347332255,-11.2881148522215));
#77326=CARTESIAN_POINT('Ctrl Pts',(5.67237960581295,4.83176645465385,-11.0764297843128));
#77327=CARTESIAN_POINT('Ctrl Pts',(0.157315764243724,7.9991496982057,-10.8118234494269));
#77328=CARTESIAN_POINT('Ctrl Pts',(-6.64422086882444,4.44641640123863,-10.4942958475639));
#77329=CARTESIAN_POINT('Ctrl Pts',(-7.21210023334577,-1.87332675097102,
-10.229689512678));
#77330=CARTESIAN_POINT('Ctrl Pts',(-4.34566297840795,-5.53649061209207,
-10.0180044447693));
#77331=CARTESIAN_POINT('Ctrl Pts',(-1.17296932823043,-6.95512504975756,
-9.85924064383781));
#77332=CARTESIAN_POINT('Ctrl Pts',(2.28269999784015,-6.65783284192195,-9.70047684290628));
#77333=CARTESIAN_POINT('Ctrl Pts',(6.20459757202321,-4.13370155428382,-9.48879177499759));
#77334=CARTESIAN_POINT('Ctrl Pts',(7.41657974109306,0.778835195121069,-9.27710670708891));
#77335=CARTESIAN_POINT('Ctrl Pts',(5.11400286593109,4.82546501488344,-9.06542163918021));
#77336=CARTESIAN_POINT('Ctrl Pts',(1.2286221269591,7.3493091603161,-8.85373657127153));
#77337=CARTESIAN_POINT('Ctrl Pts',(-5.03045449789125,6.22138824448616,-8.58913023638566));
#77338=CARTESIAN_POINT('Ctrl Pts',(-7.94658172644672,-0.876429479098477,
-8.27160263452264));
#77339=CARTESIAN_POINT('Ctrl Pts',(-4.31165047994483,-6.07728665034922,
-8.00699629963675));
#77340=CARTESIAN_POINT('Ctrl Pts',(0.240225065879416,-7.03418843488154,
-7.7953112317281));
#77341=CARTESIAN_POINT('Ctrl Pts',(3.58111681579404,-6.07661286033268,-7.63654743079656));
#77342=CARTESIAN_POINT('Ctrl Pts',(6.03359097405248,-3.62398087590763,-7.47778362986505));
#77343=CARTESIAN_POINT('Ctrl Pts',(7.40886577377939,0.832602856610925,-7.26609856195636));
#77344=CARTESIAN_POINT('Ctrl Pts',(5.17286164869607,5.37156789777357,-7.05441349404767));
#77345=CARTESIAN_POINT('Ctrl Pts',(0.805469898391115,6.98493780685348,-6.84272842613898));
#77346=CARTESIAN_POINT('Ctrl Pts',(-3.79236046403696,6.41403613766814,-6.63104335823029));
#77347=CARTESIAN_POINT('Ctrl Pts',(-7.85484174916773,1.52072523455442,-6.36643702334443));
#77348=CARTESIAN_POINT('Ctrl Pts',(-5.51551924154778,-5.78751563845428,
-6.04890942148139));
#77349=CARTESIAN_POINT('Ctrl Pts',(0.614477370300083,-7.42604608457251,
-5.78430308659554));
#77350=CARTESIAN_POINT('Ctrl Pts',(4.71325176917766,-5.22711897523551,-5.57261801868683));
#77351=CARTESIAN_POINT('Ctrl Pts',(6.65274054142896,-2.3432167619946,-5.41385421775533));
#77352=CARTESIAN_POINT('Ctrl Pts',(6.94981036898054,1.11247168640414,-5.25509041682382));
#77353=CARTESIAN_POINT('Ctrl Pts',(5.13233765828268,5.40773795397972,-5.04340534891511));
#77354=CARTESIAN_POINT('Ctrl Pts',(0.498855525711081,7.44065739044357,-4.83172028100644));
#77355=CARTESIAN_POINT('Ctrl Pts',(-3.88148491049595,5.86278200618377,-4.62003521309773));
#77356=CARTESIAN_POINT('Ctrl Pts',(-7.03163520948331,2.46535267365039,-4.40835014518906));
#77357=CARTESIAN_POINT('Ctrl Pts',(-6.98890645635959,-3.89439728104558,
-4.14374381030317));
#77358=CARTESIAN_POINT('Ctrl Pts',(-0.493183084648223,-7.9795401550328,
-3.82621620844016));
#77359=CARTESIAN_POINT('Ctrl Pts',(5.25191458918605,-5.28593754317327,-3.56160987355429));
#77360=CARTESIAN_POINT('Ctrl Pts',(6.97192198309366,-0.964270705111193,
-3.3499248056456));
#77361=CARTESIAN_POINT('Ctrl Pts',(6.59880710436197,2.4910580020008,-3.19116100471409));
#77362=CARTESIAN_POINT('Ctrl Pts',(4.60090423538341,5.32626785654532,-3.03239720378256));
#77363=CARTESIAN_POINT('Ctrl Pts',(0.444561041262034,7.44223775212194,-2.82071213587389));
#77364=CARTESIAN_POINT('Ctrl Pts',(-4.40952184136037,6.01401219799929,-2.60902706796518));
#77365=CARTESIAN_POINT('Ctrl Pts',(-6.74485818788436,1.98620579880015,-2.3973420000565));
#77366=CARTESIAN_POINT('Ctrl Pts',(-6.96734613170004,-2.64159645294223,
-2.18565693214781));
#77367=CARTESIAN_POINT('Ctrl Pts',(-2.83946969726026,-7.47986078096427,
-1.92105059726195));
#77368=CARTESIAN_POINT('Ctrl Pts',(4.7608431875892,-6.4226794151087,-1.60352299539891));
#77369=CARTESIAN_POINT('Ctrl Pts',(7.42194841553578,-0.662378202151734,
-1.33891666051305));
#77370=CARTESIAN_POINT('Ctrl Pts',(5.9550441596121,3.75155376618664,-1.12723159260437));
#77371=CARTESIAN_POINT('Ctrl Pts',(3.44473025469408,6.15511117604201,-0.968467791672837));
#77372=CARTESIAN_POINT('Ctrl Pts',(0.0902840996684676,7.03748939660186,
-0.809703990741332));
#77373=CARTESIAN_POINT('Ctrl Pts',(-4.45175724995302,5.98075099950192,-0.598018922832637));
#77374=CARTESIAN_POINT('Ctrl Pts',(-7.24685279529469,1.76095730151135,-0.386333854923946));
#77375=CARTESIAN_POINT('Ctrl Pts',(-6.43867929370588,-2.8224249160729,-0.174648787015262));
#77376=CARTESIAN_POINT('Ctrl Pts',(-3.63136500170378,-6.51004176743807,
0.0370362808934363));
#77377=CARTESIAN_POINT('Ctrl Pts',(2.64750335128596,-7.54575664707182,0.30164261577929));
#77378=CARTESIAN_POINT('Ctrl Pts',(7.7722224652204,-1.85774493315581,0.61917021764233));
#77379=CARTESIAN_POINT('Ctrl Pts',(5.78168950601745,5.51640505597175,0.936697819505367));
#77380=CARTESIAN_POINT('Ctrl Pts',(-1.50915260430786,7.85303608732375,1.25422542136839));
#77381=CARTESIAN_POINT('Ctrl Pts',(-6.41397970440127,3.79846283921743,1.51883175625427));
#77382=CARTESIAN_POINT('Ctrl Pts',(-6.98435547543984,-0.800907015052163,
1.73051682416294));
#77383=CARTESIAN_POINT('Ctrl Pts',(-5.37638526453188,-5.1683969992388,1.94220189207163));
#77384=CARTESIAN_POINT('Ctrl Pts',(-0.837541475616295,-7.40851195633607,
2.15388695998032));
#77385=CARTESIAN_POINT('Ctrl Pts',(3.61930145044134,-6.03614655527597,2.365572027889));
#77386=CARTESIAN_POINT('Ctrl Pts',(6.0740939213309,-3.58565798032842,2.52433582882053));
#77387=CARTESIAN_POINT('Ctrl Pts',(7.03395291651438,-0.245383316014028,
2.68309962975204));
#77388=CARTESIAN_POINT('Ctrl Pts',(6.08050492620003,4.30714789716092,2.89478469766074));
#77389=CARTESIAN_POINT('Ctrl Pts',(0.882264463901975,7.94594539005975,3.15939103254659));
#77390=CARTESIAN_POINT('Ctrl Pts',(-6.21766375310328,5.03503355675137,3.47691863440964));
#77391=CARTESIAN_POINT('Ctrl Pts',(-7.35021948757106,-1.22319966630272,
3.74152496929548));
#77392=CARTESIAN_POINT('Ctrl Pts',(-4.82923170259673,-5.11044485465725,
3.95321003720419));
#77393=CARTESIAN_POINT('Ctrl Pts',(-0.784305848368582,-7.4160022871715,
4.16489510511287));
#77394=CARTESIAN_POINT('Ctrl Pts',(4.12912677557379,-6.207644428425,4.37658017302156));
#77395=CARTESIAN_POINT('Ctrl Pts',(6.65614737669631,-2.28760817504574,4.58826524093025));
#77396=CARTESIAN_POINT('Ctrl Pts',(6.95598832049435,1.16784059488296,4.74702904186177));
#77397=CARTESIAN_POINT('Ctrl Pts',(5.53969319297264,4.34157960410871,4.90579284279328));
#77398=CARTESIAN_POINT('Ctrl Pts',(1.87864408485616,7.21071695220868,5.11747791070198));
#77399=CARTESIAN_POINT('Ctrl Pts',(-4.44151621939306,6.6474975978659,5.38208424558783));
#77400=CARTESIAN_POINT('Ctrl Pts',(-7.99926348658972,-0.151417668957308,
5.69961184745087));
#77401=CARTESIAN_POINT('Ctrl Pts',(-4.83594761117343,-5.66881541653162,
5.96421818233674));
#77402=CARTESIAN_POINT('Ctrl Pts',(-0.404092264403739,-7.01960450483423,
6.17590325024542));
#77403=CARTESIAN_POINT('Ctrl Pts',(4.17525112536443,-6.17895762063777,6.38758831815411));
#77404=CARTESIAN_POINT('Ctrl Pts',(7.156391420427,-2.090593565277,6.5992733860628));
#77405=CARTESIAN_POINT('Ctrl Pts',(6.56560655093786,2.53579731763451,6.81095845397148));
#77406=CARTESIAN_POINT('Ctrl Pts',(4.56997778699433,5.37260872683312,6.96972225490302));
#77407=CARTESIAN_POINT('Ctrl Pts',(1.4427462000845,6.88883142652401,7.12848605583452));
#77408=CARTESIAN_POINT('Ctrl Pts',(-3.20579129558015,6.72656264803865,7.34017112374322));
#77409=CARTESIAN_POINT('Ctrl Pts',(-7.67862993198306,2.22596768550027,7.60477745862907));
#77410=CARTESIAN_POINT('Ctrl Pts',(-6.02267558443041,-5.2667374102175,7.92230506049211));
#77411=CARTESIAN_POINT('Ctrl Pts',(-0.0496813718136637,-7.45113341886978,
8.18691139537797));
#77412=CARTESIAN_POINT('Ctrl Pts',(4.21089851742052,-5.63084998901683,8.39859646328667));
#77413=CARTESIAN_POINT('Ctrl Pts',(7.1732101275522,-2.03894477191619,8.61028153119536));
#77414=CARTESIAN_POINT('Ctrl Pts',(6.82147720567854,3.00864891656105,8.82196659910403));
#77415=CARTESIAN_POINT('Ctrl Pts',(3.39044470865432,6.16784744531429,9.03365166701273));
#77416=CARTESIAN_POINT('Ctrl Pts',(0.0369233981766486,7.05324451337045,
9.19241546794424));
#77417=CARTESIAN_POINT('Ctrl Pts',(-3.33202473910315,6.19960693574218,9.35117926887578));
#77418=CARTESIAN_POINT('Ctrl Pts',(-6.78409772386992,3.08216822459523,9.56286433678446));
#77419=CARTESIAN_POINT('Ctrl Pts',(-7.30820813198778,-3.24135522065651,
9.82747067167031));
#77420=CARTESIAN_POINT('Ctrl Pts',(-1.21654428380106,-7.90766489866231,
10.1449982735333));
#77421=CARTESIAN_POINT('Ctrl Pts',(4.75992590661602,-5.73279712080287,10.4096046084192));
#77422=CARTESIAN_POINT('Ctrl Pts',(6.84754599281427,-1.5966376542311,10.6212896763279));
#77423=CARTESIAN_POINT('Ctrl Pts',(6.80108736415966,3.05899493007411,10.8329747442366));
#77424=CARTESIAN_POINT('Ctrl Pts',(3.28173063850979,6.69438298776749,11.0446598121453));
#77425=CARTESIAN_POINT('Ctrl Pts',(-1.37759893649087,6.90215028822854,11.2563448800539));
#77426=CARTESIAN_POINT('Ctrl Pts',(-4.51347815651237,5.42016018521777,11.4151086809855));
#77427=CARTESIAN_POINT('Ctrl Pts',(-6.54136045533796,2.59771407453355,11.573872481917));
#77428=CARTESIAN_POINT('Ctrl Pts',(-7.17513323814465,-2.01027508232136,
11.7855575498257));
#77429=CARTESIAN_POINT('Ctrl Pts',(-3.50428048372235,-7.1858408038537,12.0501638847115));
#77430=CARTESIAN_POINT('Ctrl Pts',(4.16113777706602,-6.8334527542274,12.3676914865746));
#77431=CARTESIAN_POINT('Ctrl Pts',(7.3332485659688,-1.32110670821003,12.6322978214604));
#77432=CARTESIAN_POINT('Ctrl Pts',(6.26711360556603,3.18769900987276,12.8439828893691));
#77433=CARTESIAN_POINT('Ctrl Pts',(3.23371169900418,6.71977291021621,13.0556679572778));
#77434=CARTESIAN_POINT('Ctrl Pts',(-1.79982222873307,7.23499547447016,13.2673530251865));
#77435=CARTESIAN_POINT('Ctrl Pts',(-5.49842592883326,4.39371935110196,13.4790380930952));
#77436=CARTESIAN_POINT('Ctrl Pts',(-6.94337994338588,1.24060326636724,13.6378018940267));
#77437=CARTESIAN_POINT('Ctrl Pts',(-6.67746686908588,-2.22462384055129,
13.7965656949582));
#77438=CARTESIAN_POINT('Ctrl Pts',(-4.19518348608569,-6.15826098909458,
14.0082507628669));
#77439=CARTESIAN_POINT('Ctrl Pts',(1.94601072151856,-7.7543105456682,14.2728570977528));
#77440=CARTESIAN_POINT('Ctrl Pts',(7.58385486765223,-2.54878196210885,14.5903846996158));
#77441=CARTESIAN_POINT('Ctrl Pts',(6.46130100527587,3.71125946061199,14.8549910345017));
#77442=CARTESIAN_POINT('Ctrl Pts',(2.74229720123972,6.47440684408134,15.0666761024104));
#77443=CARTESIAN_POINT('Ctrl Pts',(-1.85291024787358,7.22350073928682,15.278361170319));
#77444=CARTESIAN_POINT('Ctrl Pts',(-6.03579160453311,4.3764985179128,15.4900462382278));
#77445=CARTESIAN_POINT('Ctrl Pts',(-7.03600990966135,-0.178946869939357,
15.7017313061364));
#77446=CARTESIAN_POINT('Ctrl Pts',(-6.11117763952622,-3.52180768368873,
15.860495107068));
#77447=CARTESIAN_POINT('Ctrl Pts',(-3.67639914473557,-6.00180009232866,
16.0192589079995));
#77448=CARTESIAN_POINT('Ctrl Pts',(0.755726421246436,-7.41300347146555,
16.2309439759082));
#77449=CARTESIAN_POINT('Ctrl Pts',(6.482036887681,-4.67968883085927,16.495550310794));
#77450=CARTESIAN_POINT('Ctrl Pts',(7.44356313702867,2.933344843187,16.8130779126571));
#77451=CARTESIAN_POINT('Ctrl Pts',(2.55373727311784,7.00002024315999,17.0776842475429));
#77452=CARTESIAN_POINT('Ctrl Pts',(-2.07089157952434,6.71934118708596,17.2893693154516));
#77453=CARTESIAN_POINT('Ctrl Pts',(-6.06900715527003,4.33351952417816,17.5010543833603));
#77454=CARTESIAN_POINT('Ctrl Pts',(-7.43605551059056,-0.538143116708798,
17.712739451269));
#77455=CARTESIAN_POINT('Ctrl Pts',(-5.26797085158183,-4.66754116618141,
17.9244245191776));
#77456=CARTESIAN_POINT('Ctrl Pts',(-2.40785237543088,-6.62962053520908,
18.0831883201092));
#77457=CARTESIAN_POINT('Ctrl Pts',(1.05189606637116,-6.9592405968785,18.2419521210407));
#77458=CARTESIAN_POINT('Ctrl Pts',(5.35158471534051,-5.18500568237527,18.4536371889494));
#77459=CARTESIAN_POINT('Ctrl Pts',(7.97270485365884,0.593520920752225,18.7182435238353));
#77460=CARTESIAN_POINT('Ctrl Pts',(3.80617374547976,7.03734222297062,19.0357711256983));
#77461=CARTESIAN_POINT('Ctrl Pts',(-2.55361055168965,7.00006647218875,19.3003774605842));
#77462=CARTESIAN_POINT('Ctrl Pts',(-5.91114442013924,3.80742820902396,19.5120625284928));
#77463=CARTESIAN_POINT('Ctrl Pts',(-7.43379342875041,-0.592414192789416,
19.7237475964015));
#77464=CARTESIAN_POINT('Ctrl Pts',(-5.3427489512837,-5.19995703964968,19.9354326643102));
#77465=CARTESIAN_POINT('Ctrl Pts',(-1.02496003552201,-6.96325458077588,
20.1471177322189));
#77466=CARTESIAN_POINT('Ctrl Pts',(2.42671806721124,-6.6227381742754,20.3058815331504));
#77467=CARTESIAN_POINT('Ctrl Pts',(5.28599472059724,-4.64712543767729,20.4646453340819));
#77468=CARTESIAN_POINT('Ctrl Pts',(7.43318820353908,-0.521014416784694,
20.6763304019907));
#77469=CARTESIAN_POINT('Ctrl Pts',(5.7176764398638,5.58788563733667,20.9409367368765));
#77470=CARTESIAN_POINT('Ctrl Pts',(-1.61941318767134,7.83509062306115,21.2584643387396));
#77471=CARTESIAN_POINT('Ctrl Pts',(-6.46123381947619,3.71137642860669,21.5230706736254));
#77472=CARTESIAN_POINT('Ctrl Pts',(-6.97425290871281,-0.893271676437503,
21.7347557415341));
#77473=CARTESIAN_POINT('Ctrl Pts',(-5.30607199686021,-5.2400228321342,21.9464408094428));
#77474=CARTESIAN_POINT('Ctrl Pts',(-0.739338760625791,-7.41875311408065,
22.1581258773514));
#77475=CARTESIAN_POINT('Ctrl Pts',(3.69959238591993,-5.98752650174991,22.3698109452601));
#77476=CARTESIAN_POINT('Ctrl Pts',(6.12117994620704,-3.5043940373318,22.5285747461917));
#77477=CARTESIAN_POINT('Ctrl Pts',(7.03665373271079,-0.151721012440911,
22.6873385471232));
#77478=CARTESIAN_POINT('Ctrl Pts',(6.02256833025328,4.38775724022655,22.8990236150319));
#77479=CARTESIAN_POINT('Ctrl Pts',(0.776397834368402,7.95697782890683,23.1636299499177));
#77480=CARTESIAN_POINT('Ctrl Pts',(-6.2841755041135,4.95179587397182,23.4811575517808));
#77481=CARTESIAN_POINT('Ctrl Pts',(-7.33327248069457,-1.32097395456858,
23.7457638866666));
#77482=CARTESIAN_POINT('Ctrl Pts',(-4.76075272415858,-5.17429912374916,
23.9574489545753));
#77483=CARTESIAN_POINT('Ctrl Pts',(-0.685478317186439,-7.42579011242699,
24.169134022484));
#77484=CARTESIAN_POINT('Ctrl Pts',(4.21142387439496,-6.1521076486698,24.3808190903927));
#77485=CARTESIAN_POINT('Ctrl Pts',(6.68602078785581,-2.19876862254172,24.5925041583014));
#77486=CARTESIAN_POINT('Ctrl Pts',(6.93981963119231,1.26036700577737,24.7512679592329));
#77487=CARTESIAN_POINT('Ctrl Pts',(5.48138722818666,4.41496422118694,24.9100317601644));
#77488=CARTESIAN_POINT('Ctrl Pts',(1.78245547991169,7.23509470248057,25.1217168280731));
#77489=CARTESIAN_POINT('Ctrl Pts',(-4.5296441244476,6.5877624329345,25.3863231629589));
#77490=CARTESIAN_POINT('Ctrl Pts',(-7.99653786750668,-0.257926884050681,
25.703850764822));
#77491=CARTESIAN_POINT('Ctrl Pts',(-4.76002968637034,-5.73271095116737,
25.9684570997079));
#77492=CARTESIAN_POINT('Ctrl Pts',(-0.310579469273625,-7.02436319646701,
26.1801421676165));
#77493=CARTESIAN_POINT('Ctrl Pts',(4.2571633622848,-6.1228097654567,26.3918272355252));
#77494=CARTESIAN_POINT('Ctrl Pts',(7.1835963760093,-1.9951096905261,26.6035123034339));
#77495=CARTESIAN_POINT('Ctrl Pts',(6.53125629229405,2.62300375056602,26.8151973713426));
#77496=CARTESIAN_POINT('Ctrl Pts',(4.49802791353949,5.43298871632856,26.9739611722741));
#77497=CARTESIAN_POINT('Ctrl Pts',(1.35088274939726,6.90743301213046,27.1327249732057));
#77498=CARTESIAN_POINT('Ctrl Pts',(-3.29508170266839,6.68327610266628,27.3444100411143));
#77499=CARTESIAN_POINT('Ctrl Pts',(-7.70759130112504,2.12351738908524,27.6090163760003));
#77500=CARTESIAN_POINT('Ctrl Pts',(-5.95200674357977,-5.34647172145942,
27.9265439778632));
#77501=CARTESIAN_POINT('Ctrl Pts',(0.049546484282045,-7.45113431704577,
28.1911503127491));
#77502=CARTESIAN_POINT('Ctrl Pts',(4.28550868087525,-5.57427603090819,28.4028353806578));
#77503=CARTESIAN_POINT('Ctrl Pts',(7.19972581056599,-1.94324151093504,28.6145204485665));
#77504=CARTESIAN_POINT('Ctrl Pts',(6.78080750212263,3.09922073912179,28.8262055164751));
#77505=CARTESIAN_POINT('Ctrl Pts',(3.30800958166722,6.21244960049673,29.0378905843839));
#77506=CARTESIAN_POINT('Ctrl Pts',(-0.0570048159302318,7.05311079976029,
29.1966543853154));
#77507=CARTESIAN_POINT('Ctrl Pts',(-3.41428671659465,6.15468612006932,29.3554181862469));
#77508=CARTESIAN_POINT('Ctrl Pts',(-6.82454005487817,2.99155409964336,29.5671032541556));
#77509=CARTESIAN_POINT('Ctrl Pts',(-7.26439642334094,-3.33838798995519,
29.8317095890415));
#77510=CARTESIAN_POINT('Ctrl Pts',(-1.11113353487349,-7.92316391422415,
30.1492371909045));
#77511=CARTESIAN_POINT('Ctrl Pts',(4.83584497311704,-5.66890296801239,30.4138435257904));
#77512=CARTESIAN_POINT('Ctrl Pts',(6.86820054380616,-1.50531033766313,30.6255285936991));
#77513=CARTESIAN_POINT('Ctrl Pts',(6.75974903295088,3.14929076597755,30.8372136616077));
#77514=CARTESIAN_POINT('Ctrl Pts',(3.19229350999306,6.73749075819042,31.0488987295164));
#77515=CARTESIAN_POINT('Ctrl Pts',(-1.46938967088129,6.88319340322654,31.2605837974251));
#77516=CARTESIAN_POINT('Ctrl Pts',(-4.58525582745349,5.35957558949753,31.4193475983566));
#77517=CARTESIAN_POINT('Ctrl Pts',(-6.57537304786625,2.51037533071907,31.5781113992881));
#77518=CARTESIAN_POINT('Ctrl Pts',(-7.14772707930367,-2.10564491107097,
31.7897964671968));
#77519=CARTESIAN_POINT('Ctrl Pts',(-3.40827909532261,-7.23186859499761,
32.0544028020827));
#77520=CARTESIAN_POINT('Ctrl Pts',(4.25176688234156,-6.77743480398061,32.3719304039457));
#77521=CARTESIAN_POINT('Ctrl Pts',(7.35019092621592,-1.22333593625597,32.6365367388316));
#77522=CARTESIAN_POINT('Ctrl Pts',(6.22410872607908,3.27087274111372,32.8482218067403));
#77523=CARTESIAN_POINT('Ctrl Pts',(3.14394072191596,6.76223898233638,33.059906874649));
#77524=CARTESIAN_POINT('Ctrl Pts',(-1.89600787713411,7.21038651533262,33.2715919425577));
#77525=CARTESIAN_POINT('Ctrl Pts',(-5.55644760618287,4.32010965495771,33.4832770104663));
#77526=CARTESIAN_POINT('Ctrl Pts',(-6.95928484424909,1.14803134074789,33.6420408113979));
#77527=CARTESIAN_POINT('Ctrl Pts',(-6.64725045028281,-2.3133474600465,33.8008046123294));
#77528=CARTESIAN_POINT('Ctrl Pts',(-4.11280466208001,-6.21358034496234,
34.0124896802381));
#77529=CARTESIAN_POINT('Ctrl Pts',(2.04909889679104,-7.72770881167863,34.2770960151239));
#77530=CARTESIAN_POINT('Ctrl Pts',(7.61712341562411,-2.44756511969248,34.594623616987));
#77531=CARTESIAN_POINT('Ctrl Pts',(6.41130688418545,3.79697267590346,34.8592299518729));
#77532=CARTESIAN_POINT('Ctrl Pts',(2.65583722899417,6.51035072294137,35.0709150197815));
#77533=CARTESIAN_POINT('Ctrl Pts',(-1.94893811868904,7.19818584968968,35.2826000876902));
#77534=CARTESIAN_POINT('Ctrl Pts',(-6.0935363118243,4.29573448750313,35.4942851555989));
#77535=CARTESIAN_POINT('Ctrl Pts',(-7.03300307526989,-0.272626437379933,
35.7059702235076));
#77536=CARTESIAN_POINT('Ctrl Pts',(-6.06373740921473,-3.60287525940376,
35.8647340244391));
#77537=CARTESIAN_POINT('Ctrl Pts',(-3.59614984158672,-6.05022489966651,
36.0234978253707));
#77538=CARTESIAN_POINT('Ctrl Pts',(0.854375102710567,-7.40228249093471,
36.2351828932793));
#77539=CARTESIAN_POINT('Ctrl Pts',(6.54377947812764,-4.59295546555386,36.4997892281652));
#77540=CARTESIAN_POINT('Ctrl Pts',(7.4038410646272,3.03220738633166,36.8173168300282));
#77541=CARTESIAN_POINT('Ctrl Pts',(2.46029465899688,7.03340654702068,37.0819231649141));
#77542=CARTESIAN_POINT('Ctrl Pts',(-2.16018645213729,6.6911682398978,37.2936082328227));
#77543=CARTESIAN_POINT('Ctrl Pts',(-6.12617658509613,4.2523169878751,37.5052933007315));
#77544=CARTESIAN_POINT('Ctrl Pts',(-7.42822994676136,-0.637118064947822,
37.7169783686402));
#77545=CARTESIAN_POINT('Ctrl Pts',(-5.20534816136745,-4.73727853836591,
37.9286634365488));
#77546=CARTESIAN_POINT('Ctrl Pts',(-2.3193551460399,-6.66109699743759,38.0874272374804));
#77547=CARTESIAN_POINT('Ctrl Pts',(1.1444759270142,-6.9446158909024,38.2461910384118));
#77548=CARTESIAN_POINT('Ctrl Pts',(5.4201566233756,-5.11328124297969,38.4578761063206));
#77549=CARTESIAN_POINT('Ctrl Pts',(7.96409426376987,0.69963728082014,38.7224824412064));
#77550=CARTESIAN_POINT('Ctrl Pts',(3.712123078394,7.0874033605291,39.0400100430695));
#77551=CARTESIAN_POINT('Ctrl Pts',(-2.64660091651398,6.96544047806516,39.3046163779553));
#77552=CARTESIAN_POINT('Ctrl Pts',(-5.96132212199443,3.72837450914394,39.516301445864));
#77553=CARTESIAN_POINT('Ctrl Pts',(-7.42524536156241,-0.691354205706398,
39.7279865137728));
#77554=CARTESIAN_POINT('Ctrl Pts',(-5.27302968365255,-5.27064298980338,
39.9396715816813));
#77555=CARTESIAN_POINT('Ctrl Pts',(-0.932142569072262,-6.97628609376343,
40.1513566495901));
#77556=CARTESIAN_POINT('Ctrl Pts',(2.51469496931212,-6.58983540872235,40.3101204505215));
#77557=CARTESIAN_POINT('Ctrl Pts',(5.34740973093818,-4.57632212471511,40.4688842514532));
#77558=CARTESIAN_POINT('Ctrl Pts',(7.43946722675043,-0.421983736459396,
40.6805693193617));
#77559=CARTESIAN_POINT('Ctrl Pts',(5.64275805398072,5.66352993380997,40.9451756542477));
#77560=CARTESIAN_POINT('Ctrl Pts',(-1.7236060347068,7.81283088138394,41.2627032561106));
#77561=CARTESIAN_POINT('Ctrl Pts',(-6.51008366618329,3.62500594814068,41.5273095909966));
#77562=CARTESIAN_POINT('Ctrl Pts',(-6.96173920250525,-0.986065514515229,
41.7389946589052));
#77563=CARTESIAN_POINT('Ctrl Pts',(-5.23582244289624,-5.31021681888934,
41.950679726814));
#77564=CARTESIAN_POINT('Ctrl Pts',(-0.64048094734282,-7.42794074604368,
42.1623647947226));
#77565=CARTESIAN_POINT('Ctrl Pts',(3.77899759003504,-5.93772975518615,42.3740498626313));
#77566=CARTESIAN_POINT('Ctrl Pts',(6.16730365221708,-3.42257025699746,42.5328136635628));
#77567=CARTESIAN_POINT('Ctrl Pts',(7.03805019928911,-0.0580035514068519,
42.6915774644943));
#77568=CARTESIAN_POINT('Ctrl Pts',(5.96360448931232,4.4675680617965,42.903262532403));
#77569=CARTESIAN_POINT('Ctrl Pts',(0.670369434414901,7.96661123617363,43.1678688672888));
#77570=CARTESIAN_POINT('Ctrl Pts',(-6.34955916802911,4.86767321373177,43.485396469152));
#77571=CARTESIAN_POINT('Ctrl Pts',(-7.3150314182536,-1.41851077356636,43.7500028040378));
#77572=CARTESIAN_POINT('Ctrl Pts',(-4.69142673684704,-5.23723716241792,
43.9616878719465));
#77573=CARTESIAN_POINT('Ctrl Pts',(-0.58653157107381,-7.43425988470175,
44.1733729398552));
#77574=CARTESIAN_POINT('Ctrl Pts',(4.29297534917504,-6.09548047507495,44.3850580077638));
#77575=CARTESIAN_POINT('Ctrl Pts',(6.71470797317736,-2.10953887521942,44.5967430756726));
#77576=CARTESIAN_POINT('Ctrl Pts',(6.9224205318893,1.35266976103254,44.755506876604));
#77577=CARTESIAN_POINT('Ctrl Pts',(5.42210907004846,4.48756596076176,44.9142706775357));
#77578=CARTESIAN_POINT('Ctrl Pts',(1.68595087211227,7.25818934366925,45.1259557454442));
#77579=CARTESIAN_POINT('Ctrl Pts',(-4.61696880509652,6.52685903170057,45.3905620803302));
#77580=CARTESIAN_POINT('Ctrl Pts',(-7.99239412183842,-0.364390374716451,
45.7080896821931));
#77581=CARTESIAN_POINT('Ctrl Pts',(-4.6832676396441,-5.79558984748086,45.972696017079));
#77582=CARTESIAN_POINT('Ctrl Pts',(-0.217011590012495,-7.02787620070355,
46.1843810849877));
#77583=CARTESIAN_POINT('Ctrl Pts',(4.33832063441401,-6.0655760971378,46.3960661528965));
#77584=CARTESIAN_POINT('Ctrl Pts',(7.20952740566221,-1.89927200728346,46.607751220805));
#77585=CARTESIAN_POINT('Ctrl Pts',(6.49574778867412,2.70974502436097,46.8194362887139));
#77586=CARTESIAN_POINT('Ctrl Pts',(4.42528036686922,5.49240522697806,46.9782000896452));
#77587=CARTESIAN_POINT('Ctrl Pts',(1.25877973477203,6.92480964352208,47.1369638905769));
#77588=CARTESIAN_POINT('Ctrl Pts',(-3.38378776442068,6.63880435448184,47.3486489584854));
#77589=CARTESIAN_POINT('Ctrl Pts',(-7.73518581709401,2.02069051117516,47.6132552933714));
#77590=CARTESIAN_POINT('Ctrl Pts',(-5.88028238222423,-5.42525789703002,
47.9307828952344));
#77591=CARTESIAN_POINT('Ctrl Pts',(0.148765553839371,-7.44981384161723,
48.1953892301203));
#77592=CARTESIAN_POINT('Ctrl Pts',(4.35935885831631,-5.51671353860559,48.407074298029));
#77593=CARTESIAN_POINT('Ctrl Pts',(7.22496470440797,-1.84719363825532,48.6187593659376));
#77594=CARTESIAN_POINT('Ctrl Pts',(6.73893529979263,3.18924295027096,48.8304444338464));
#77595=CARTESIAN_POINT('Ctrl Pts',(3.2249878169521,6.25595004868359,49.042129501755));
#77596=CARTESIAN_POINT('Ctrl Pts',(-0.150922920881917,7.05172629748821,
49.2008933026865));
#77597=CARTESIAN_POINT('Ctrl Pts',(-3.495943209325,6.1086738410938,49.359657103618));
#77598=CARTESIAN_POINT('Ctrl Pts',(-6.86377213163642,2.90040945673224,49.5713421715268));
#77599=CARTESIAN_POINT('Ctrl Pts',(-7.2192964569405,-3.43482873426469,49.8359485064125));
#77600=CARTESIAN_POINT('Ctrl Pts',(-1.00552573910145,-7.93725784714026,
50.1534761082757));
#77601=CARTESIAN_POINT('Ctrl Pts',(4.91090645773264,-5.6040035000133,50.4180824431614));
#77602=CARTESIAN_POINT('Ctrl Pts',(6.88763709785911,-1.41371607149604,50.6297675110702));
#77603=CARTESIAN_POINT('Ctrl Pts',(6.71721193744111,3.23902811112609,50.8414525789789));
#77604=CARTESIAN_POINT('Ctrl Pts',(3.10229026467322,6.7794037115615,51.0531376468875));
#77605=CARTESIAN_POINT('Ctrl Pts',(-1.56091982579034,6.86301586247476,51.2648227147963));
#77606=CARTESIAN_POINT('Ctrl Pts',(-4.65622035563679,5.29804053424458,51.4235865157277));
#77607=CARTESIAN_POINT('Ctrl Pts',(-6.60821957306057,2.42259140051073,51.5823503166593));
#77608=CARTESIAN_POINT('Ctrl Pts',(-7.11905335270188,-2.20064132775103,
51.794035384568));
#77609=CARTESIAN_POINT('Ctrl Pts',(-3.31167328750886,-7.27661389680405,
52.0586417194539));
#77610=CARTESIAN_POINT('Ctrl Pts',(4.34164198524954,-6.72021495310217,52.3761693213169));
#77611=CARTESIAN_POINT('Ctrl Pts',(7.36582981413719,-1.12534821957666,52.6407756562027));
#77612=CARTESIAN_POINT('Ctrl Pts',(6.18000007184479,3.35346642033527,52.8524607241115));
#77613=CARTESIAN_POINT('Ctrl Pts',(3.0536122031964,6.80350584881866,53.0641457920201));
#77614=CARTESIAN_POINT('Ctrl Pts',(-1.99185729091034,7.18449887601852,53.2758308599288));
#77615=CARTESIAN_POINT('Ctrl Pts',(-5.61348391010628,4.24573383726985,53.4875159278375));
#77616=CARTESIAN_POINT('Ctrl Pts',(-6.97395559726895,1.05525582368896,53.646279728769));
#77617=CARTESIAN_POINT('Ctrl Pts',(-6.61585521413192,-2.40166083161287,
53.8050435297005));
#77618=CARTESIAN_POINT('Ctrl Pts',(-4.02969648644615,-6.26779779800259,
54.0167285976093));
#77619=CARTESIAN_POINT('Ctrl Pts',(2.15182370290406,-7.69973664706345,54.281334932495));
#77620=CARTESIAN_POINT('Ctrl Pts',(7.64904112730664,-2.34591424651271,54.5988625343582));
#77621=CARTESIAN_POINT('Ctrl Pts',(6.36017583535967,3.88201256989678,54.8634688692439));
#77622=CARTESIAN_POINT('Ctrl Pts',(2.5689062153214,6.54514002756553,55.0751539371527));
#77623=CARTESIAN_POINT('Ctrl Pts',(-2.04462021559947,7.17159454156269,55.2868390050613));
#77624=CARTESIAN_POINT('Ctrl Pts',(-6.15020070906691,4.21420845931486,55.49852407297));
#77625=CARTESIAN_POINT('Ctrl Pts',(-7.02874863621731,-0.366257412569875,
55.7102091408788));
#77626=CARTESIAN_POINT('Ctrl Pts',(-6.01522263894987,-3.68330441628207,
55.8689729418102));
#77627=CARTESIAN_POINT('Ctrl Pts',(-3.51526135293355,-6.09757583857006,
56.0277367427418));
#77628=CARTESIAN_POINT('Ctrl Pts',(0.952869138907655,-7.39025080980567,
56.2394218106504));
#77629=CARTESIAN_POINT('Ctrl Pts',(6.60436808219333,-4.50540343472597,56.5040281455363));
#77630=CARTESIAN_POINT('Ctrl Pts',(7.36279468941762,3.13052494009091,56.8215557473994));
#77631=CARTESIAN_POINT('Ctrl Pts',(2.36643471902825,7.06555773634852,57.0861620822851));
#77632=CARTESIAN_POINT('Ctrl Pts',(-2.24912350964978,6.66179247408394,57.297847150194));
#77633=CARTESIAN_POINT('Ctrl Pts',(-6.18219453733946,4.17040210987243,57.5095322181025));
#77634=CARTESIAN_POINT('Ctrl Pts',(-7.41921937995394,-0.736064935536567,
57.7212172860114));
#77635=CARTESIAN_POINT('Ctrl Pts',(-5.14163886745774,-4.80607088708851,
57.9329023539199));
#77636=CARTESIAN_POINT('Ctrl Pts',(-2.23078681769651,-6.69161051830819,
58.0916661548515));
#77637=CARTESIAN_POINT('Ctrl Pts',(1.23747337014818,-6.92836140896512,58.250429955783));
#77638=CARTESIAN_POINT('Ctrl Pts',(5.48642653137197,-5.0415104690091,58.4621150236917));
#77639=CARTESIAN_POINT('Ctrl Pts',(7.95684541214289,0.807409843183617,58.7267213585775));
#77640=CARTESIAN_POINT('Ctrl Pts',(3.61256597258128,7.13309616752026,59.0442489604406));
#77641=CARTESIAN_POINT('Ctrl Pts',(-2.73097502532573,6.93480882320121,59.3088552953264));
#77642=CARTESIAN_POINT('Ctrl Pts',(-6.02140560873619,3.6416148042235,59.5205403632351));
#77643=CARTESIAN_POINT('Ctrl Pts',(-7.04413462746363,0.332516821336018,
59.6793041641666));
#77644=CARTESIAN_POINT('Ctrl Pts',(-6.33691269983105,-3.08643256639824,
59.8380746593449));
#77645=CARTESIAN_POINT('Ctrl Pts',(-4.84078143417837,-4.8527243283379,59.9439238875458));
#77646=CARTESIAN_POINT('Ctrl Pts',(-3.92534899164063,-5.50542332685364,
59.9968518487696));
#77647=CARTESIAN_POINT('Ctrl Pts',(-3.09289325614769,6.45110082070439,-60.4369614153577));
#77648=CARTESIAN_POINT('Ctrl Pts',(-4.16562014990033,5.93679815796041,-60.3840310532033));
#77649=CARTESIAN_POINT('Ctrl Pts',(-6.04570215501001,4.36700469538412,-60.2781794240718));
#77650=CARTESIAN_POINT('Ctrl Pts',(-7.40319472859208,0.93131111440289,-60.1194065279632));
#77651=CARTESIAN_POINT('Ctrl Pts',(-6.93742111779479,-2.70366387687074,
-59.9606427270316));
#77652=CARTESIAN_POINT('Ctrl Pts',(-4.10488940433561,-6.73346130664272,
-59.7489576591229));
#77653=CARTESIAN_POINT('Ctrl Pts',(2.47170292483413,-8.09098755230349,-59.4843513242371));
#77654=CARTESIAN_POINT('Ctrl Pts',(8.14781008572697,-2.28516285174072,-59.166823722374));
#77655=CARTESIAN_POINT('Ctrl Pts',(6.63371968662535,4.25998251374448,-58.9022173874882));
#77656=CARTESIAN_POINT('Ctrl Pts',(2.54687994990649,6.99768788344637,-58.6905323195795));
#77657=CARTESIAN_POINT('Ctrl Pts',(-1.11141694785635,7.38009987772104,-58.5317685186479));
#77658=CARTESIAN_POINT('Ctrl Pts',(-4.48778573003331,5.94267579194522,-58.3730047177166));
#77659=CARTESIAN_POINT('Ctrl Pts',(-7.60032701309895,2.11325746684096,-58.1613196498077));
#77660=CARTESIAN_POINT('Ctrl Pts',(-7.20096026774904,-3.22570666445012,
-57.9496345818991));
#77661=CARTESIAN_POINT('Ctrl Pts',(-3.55307302003504,-6.5362828925506,-57.7379495139904));
#77662=CARTESIAN_POINT('Ctrl Pts',(1.18497697000321,-7.79451478752187,-57.5262644460818));
#77663=CARTESIAN_POINT('Ctrl Pts',(7.10711231753246,-4.59902803843737,-57.2616581111957));
#77664=CARTESIAN_POINT('Ctrl Pts',(7.70181295244941,3.49832541559333,-56.944130509333));
#77665=CARTESIAN_POINT('Ctrl Pts',(2.33400074345349,7.53079782198634,-56.6795241744469));
#77666=CARTESIAN_POINT('Ctrl Pts',(-2.55813326706307,6.99389892744948,-56.4678391065383));
#77667=CARTESIAN_POINT('Ctrl Pts',(-5.60210698976003,4.93077719032846,-56.3090753056067));
#77668=CARTESIAN_POINT('Ctrl Pts',(-7.26038631684579,1.65692847571967,-56.1503115046752));
#77669=CARTESIAN_POINT('Ctrl Pts',(-7.17555684949993,-3.27717504576235,
-55.9386264367666));
#77670=CARTESIAN_POINT('Ctrl Pts',(-3.43238396175318,-7.1048057165866,-55.7269413688578));
#77671=CARTESIAN_POINT('Ctrl Pts',(1.49044801780787,-7.28875849380132,-55.5152563009492));
#77672=CARTESIAN_POINT('Ctrl Pts',(5.92564020795954,-5.20049295229579,-55.3035712330405));
#77673=CARTESIAN_POINT('Ctrl Pts',(8.39902043501333,1.05773211100905,-55.0389648981546));
#77674=CARTESIAN_POINT('Ctrl Pts',(3.63994810713719,7.6358972814368,-54.7214372962916));
#77675=CARTESIAN_POINT('Ctrl Pts',(-3.06350390178714,7.26466741899136,-54.4568309614057));
#77676=CARTESIAN_POINT('Ctrl Pts',(-6.46072452460837,3.70374549364738,-54.245145893497));
#77677=CARTESIAN_POINT('Ctrl Pts',(-7.46115700940049,0.165189662269874,
-54.0863820925655));
#77678=CARTESIAN_POINT('Ctrl Pts',(-6.62179760813936,-3.40740723797466,
-53.9276182916339));
#77679=CARTESIAN_POINT('Ctrl Pts',(-3.37972447947155,-7.12782943365753,
-53.7159332237254));
#77680=CARTESIAN_POINT('Ctrl Pts',(1.9488378753097,-7.64601556384835,-53.5042481558165));
#77681=CARTESIAN_POINT('Ctrl Pts',(5.83371089549533,-4.61684456685773,-53.292563087908));
#77682=CARTESIAN_POINT('Ctrl Pts',(7.88236626709611,-0.16321757068143,-53.0808780199992));
#77683=CARTESIAN_POINT('Ctrl Pts',(5.74493227405618,6.21756343083984,-52.8162716851135));
#77684=CARTESIAN_POINT('Ctrl Pts',(-2.13201300317532,8.18600452989546,-52.4987440832501));
#77685=CARTESIAN_POINT('Ctrl Pts',(-7.02173133206871,3.58548990146649,-52.2341377483646));
#77686=CARTESIAN_POINT('Ctrl Pts',(-7.32796911262751,-1.32648438012215,
-52.0224526804557));
#77687=CARTESIAN_POINT('Ctrl Pts',(-5.81484423605366,-4.67800577465704,
-51.8636888795243));
#77688=CARTESIAN_POINT('Ctrl Pts',(-2.87218866315881,-6.87089222281699,
-51.7049250785927));
#77689=CARTESIAN_POINT('Ctrl Pts',(2.00395288249048,-7.62972233055806,-51.4932400106842));
#77690=CARTESIAN_POINT('Ctrl Pts',(6.4144665742518,-4.59501269081789,-51.2815549427753));
#77691=CARTESIAN_POINT('Ctrl Pts',(7.43620879853939,0.224132268622218,-51.0698698748668));
#77692=CARTESIAN_POINT('Ctrl Pts',(6.13583841096293,4.95073983734211,-50.8581848069579));
#77693=CARTESIAN_POINT('Ctrl Pts',(0.391788697102781,8.45629017163187,-50.5935784720722));
#77694=CARTESIAN_POINT('Ctrl Pts',(-6.90232239734956,4.89020399705925,-50.276050870209));
#77695=CARTESIAN_POINT('Ctrl Pts',(-7.68104402021101,-1.77820456993238,
-50.0114445353233));
#77696=CARTESIAN_POINT('Ctrl Pts',(-4.75242384388133,-5.73351198956874,
-49.7997594674145));
#77697=CARTESIAN_POINT('Ctrl Pts',(-1.43663038395558,-7.32340389826851,
-49.6409956664831));
#77698=CARTESIAN_POINT('Ctrl Pts',(2.22681761706147,-7.10632893656609,-49.4822318655515));
#77699=CARTESIAN_POINT('Ctrl Pts',(6.44614310799523,-4.54705718327047,-49.2705467976428));
#77700=CARTESIAN_POINT('Ctrl Pts',(7.86648262055552,0.614796097461046,-49.0588617297342));
#77701=CARTESIAN_POINT('Ctrl Pts',(5.54506421911325,4.95980840106012,-48.8471766618254));
#77702=CARTESIAN_POINT('Ctrl Pts',(1.50660159420562,7.73876537820023,-48.6354915939168));
#77703=CARTESIAN_POINT('Ctrl Pts',(-5.14542308904248,6.72212489357063,-48.3708852590308));
#77704=CARTESIAN_POINT('Ctrl Pts',(-8.42981715200117,-0.703087756710445,
-48.0533576571679));
#77705=CARTESIAN_POINT('Ctrl Pts',(-4.73168696485318,-6.30647185037608,
-47.7887513222819));
#77706=CARTESIAN_POINT('Ctrl Pts',(0.0558814622644325,-7.4468496284399,
-47.5770662543734));
#77707=CARTESIAN_POINT('Ctrl Pts',(3.61653398079731,-6.5281569744467,-47.4183024534417));
#77708=CARTESIAN_POINT('Ctrl Pts',(6.27963156485163,-4.00310567735237,-47.2595386525103));
#77709=CARTESIAN_POINT('Ctrl Pts',(7.85983856963731,0.671883662495001,-47.0478535846016));
#77710=CARTESIAN_POINT('Ctrl Pts',(5.62270708618466,5.53576445343586,-46.8361685166929));
#77711=CARTESIAN_POINT('Ctrl Pts',(1.04876525953824,7.36529211910175,-46.6244834487842));
#77712=CARTESIAN_POINT('Ctrl Pts',(-3.83045925978348,6.89100281538415,-46.4127983808755));
#77713=CARTESIAN_POINT('Ctrl Pts',(-8.26523789501724,1.8298044673638,-46.1481920459897));
#77714=CARTESIAN_POINT('Ctrl Pts',(-5.99685730962747,-5.96605833174442,
-45.8306644441266));
#77715=CARTESIAN_POINT('Ctrl Pts',(0.440687630948982,-7.87186401971451,
-45.5660581092408));
#77716=CARTESIAN_POINT('Ctrl Pts',(4.83793281887333,-5.66154556340304,-45.354373041332));
#77717=CARTESIAN_POINT('Ctrl Pts',(6.97059641115693,-2.6658839415933,-45.1956092404006));
#77718=CARTESIAN_POINT('Ctrl Pts',(7.38218037044503,0.980836700245129,-45.036845439469));
#77719=CARTESIAN_POINT('Ctrl Pts',(5.58086392542702,5.57516348124011,-44.8251603715604));
#77720=CARTESIAN_POINT('Ctrl Pts',(0.737299387595404,7.85594759873095,-44.6134753036517));
#77721=CARTESIAN_POINT('Ctrl Pts',(-3.94025935688594,6.31045107498579,-44.4017902357429));
#77722=CARTESIAN_POINT('Ctrl Pts',(-7.36791287311896,2.80574372254866,-44.1901051678343));
#77723=CARTESIAN_POINT('Ctrl Pts',(-7.50191990859716,-3.92218555591228,
-43.9254988329484));
#77724=CARTESIAN_POINT('Ctrl Pts',(-0.746483913511334,-8.4260851750192,
-43.6079712310853));
#77725=CARTESIAN_POINT('Ctrl Pts',(5.40602056471108,-5.7389363462987,-43.3433648961995));
#77726=CARTESIAN_POINT('Ctrl Pts',(7.34705073847908,-1.21636243473493,-43.1316798282908));
#77727=CARTESIAN_POINT('Ctrl Pts',(7.04976804581042,2.4488613716479,-42.9729160273593));
#77728=CARTESIAN_POINT('Ctrl Pts',(5.01647005997232,5.50396727749474,-42.8141522264277));
#77729=CARTESIAN_POINT('Ctrl Pts',(0.679915661826589,7.85914783481573,-42.6024671585192));
#77730=CARTESIAN_POINT('Ctrl Pts',(-4.49450262730389,6.48528867469395,-42.3907820906104));
#77731=CARTESIAN_POINT('Ctrl Pts',(-7.07809099936217,2.29086542033022,-42.1790970227017));
#77732=CARTESIAN_POINT('Ctrl Pts',(-7.44381045473222,-2.59769587452286,
-41.9674119547931));
#77733=CARTESIAN_POINT('Ctrl Pts',(-3.21408737425887,-7.83147394815582,
-41.7028056199072));
#77734=CARTESIAN_POINT('Ctrl Pts',(4.85459882701441,-6.92741076005743,-41.3852780180441));
#77735=CARTESIAN_POINT('Ctrl Pts',(7.83152391367127,-0.909770258110416,
-41.1206716831583));
#77736=CARTESIAN_POINT('Ctrl Pts',(6.40441397027651,3.80028601867642,-40.9089866152495));
#77737=CARTESIAN_POINT('Ctrl Pts',(3.81685286273701,6.41309486453266,-40.7502228143181));
#77738=CARTESIAN_POINT('Ctrl Pts',(0.293946837473347,7.44125143447466,-40.5914590133865));
#77739=CARTESIAN_POINT('Ctrl Pts',(-4.54046718260951,6.45078660012343,-40.3797739454779));
#77740=CARTESIAN_POINT('Ctrl Pts',(-7.61471986276085,2.06774381213691,-40.1680888775692));
#77741=CARTESIAN_POINT('Ctrl Pts',(-6.89052927551469,-2.8050031858434,-39.9564038096605));
#77742=CARTESIAN_POINT('Ctrl Pts',(-4.02249418185155,-6.78069896835596,
-39.7447187417518));
#77743=CARTESIAN_POINT('Ctrl Pts',(2.58377163955079,-8.06141835936246,-39.4801124068659));
#77744=CARTESIAN_POINT('Ctrl Pts',(8.17491818981989,-2.17413481632614,-39.162584805003));
#77745=CARTESIAN_POINT('Ctrl Pts',(6.57765980704569,4.34681954947786,-38.897978470117));
#77746=CARTESIAN_POINT('Ctrl Pts',(2.45288741330638,7.03150307289015,-38.6862934022084));
#77747=CARTESIAN_POINT('Ctrl Pts',(-1.20927707147813,7.36436015426162,-38.5275296012768));
#77748=CARTESIAN_POINT('Ctrl Pts',(-4.56667702027796,5.88252400307868,-38.3687658003453));
#77749=CARTESIAN_POINT('Ctrl Pts',(-7.62767040977012,2.01174901928726,-38.1570807324367));
#77750=CARTESIAN_POINT('Ctrl Pts',(-7.15742743914158,-3.32125812221487,
-37.9453956645279));
#77751=CARTESIAN_POINT('Ctrl Pts',(-3.46569349778444,-6.5830392030377,-37.7337105966193));
#77752=CARTESIAN_POINT('Ctrl Pts',(1.28865021977318,-7.77802793473847,-37.5220255287106));
#77753=CARTESIAN_POINT('Ctrl Pts',(7.16773596466101,-4.50398745456938,-37.2574191938247));
#77754=CARTESIAN_POINT('Ctrl Pts',(7.65453831308241,3.60058228948636,-36.9398915919617));
#77755=CARTESIAN_POINT('Ctrl Pts',(2.2335124177871,7.56120830373943,-36.6752852570758));
#77756=CARTESIAN_POINT('Ctrl Pts',(-2.65104245880669,6.95921446774165,-36.4636001891671));
#77757=CARTESIAN_POINT('Ctrl Pts',(-5.66727049093198,4.85573853290007,-36.3048363882356));
#77758=CARTESIAN_POINT('Ctrl Pts',(-7.28180748570867,1.56009852105847,-36.1460725873041));
#77759=CARTESIAN_POINT('Ctrl Pts',(-7.13127961653182,-3.3724384393972,-35.9343875193954));
#77760=CARTESIAN_POINT('Ctrl Pts',(-3.33746819925646,-7.14988315148624,
-35.7227024514867));
#77761=CARTESIAN_POINT('Ctrl Pts',(1.58737709188624,-7.26826461663796,-35.511017383578));
#77762=CARTESIAN_POINT('Ctrl Pts',(5.99436741048307,-5.12112265920587,-35.2993323156693));
#77763=CARTESIAN_POINT('Ctrl Pts',(8.38419037352516,1.16948434384604,-35.0347259807835));
#77764=CARTESIAN_POINT('Ctrl Pts',(3.53794147178642,7.68369180485678,-34.7171983789205));
#77765=CARTESIAN_POINT('Ctrl Pts',(-3.15997262174759,7.22322793235497,-34.4525920440345));
#77766=CARTESIAN_POINT('Ctrl Pts',(-6.50947280185845,3.61738247470258,-34.2409069761259));
#77767=CARTESIAN_POINT('Ctrl Pts',(-7.46269518989241,0.0658180828906648,
-34.0821431751943));
#77768=CARTESIAN_POINT('Ctrl Pts',(-6.57583552253201,-3.49528465721146,
-33.9233793742629));
#77769=CARTESIAN_POINT('Ctrl Pts',(-3.28450664646774,-7.17220371196996,
-33.7116943063541));
#77770=CARTESIAN_POINT('Ctrl Pts',(2.05048368315385,-7.6193857840429,-33.5000092384455));
#77771=CARTESIAN_POINT('Ctrl Pts',(5.89467410338615,-4.53875024474639,-33.2883241705368));
#77772=CARTESIAN_POINT('Ctrl Pts',(7.88384083943231,-0.0582371100955341,
-33.0766391026281));
#77773=CARTESIAN_POINT('Ctrl Pts',(5.66162633057394,6.29351484807696,-32.8120327677422));
#77774=CARTESIAN_POINT('Ctrl Pts',(-2.24083336379937,8.15688760775168,-32.4945051658792));
#77775=CARTESIAN_POINT('Ctrl Pts',(-7.06885510459415,3.49166668558162,-32.2298988309934));
#77776=CARTESIAN_POINT('Ctrl Pts',(-7.30965514053794,-1.42395008789908,
-32.0182137630846));
#77777=CARTESIAN_POINT('Ctrl Pts',(-5.75203370239377,-4.75502469013619,
-31.8594499621531));
#77778=CARTESIAN_POINT('Ctrl Pts',(-2.78043735296234,-6.90853065279322,
-31.7006861612216));
#77779=CARTESIAN_POINT('Ctrl Pts',(2.10537683387303,-7.60236005356738,-31.4890010933129));
#77780=CARTESIAN_POINT('Ctrl Pts',(6.47508756137363,-4.50918663768756,-31.2773160254043));
#77781=CARTESIAN_POINT('Ctrl Pts',(7.43256476481124,0.323137101247964,-31.0656309574955));
#77782=CARTESIAN_POINT('Ctrl Pts',(6.06936753599808,5.03200910725189,-30.8539458895869));
#77783=CARTESIAN_POINT('Ctrl Pts',(0.279145278362542,8.46075763531737,-30.589339554701));
#77784=CARTESIAN_POINT('Ctrl Pts',(-6.96683105881335,4.79785520912865,-30.271811952838));
#77785=CARTESIAN_POINT('Ctrl Pts',(-7.65668338307411,-1.88033196651658,
-30.0072056179521));
#77786=CARTESIAN_POINT('Ctrl Pts',(-4.67565180448538,-5.79628953121159,
-29.7955205500434));
#77787=CARTESIAN_POINT('Ctrl Pts',(-1.33898046568837,-7.34188550917158,
-29.6367567491119));
#77788=CARTESIAN_POINT('Ctrl Pts',(2.32125200866079,-7.07604527731557,-29.4779929481804));
#77789=CARTESIAN_POINT('Ctrl Pts',(6.50612268408102,-4.46081355992071,-29.2663078802717));
#77790=CARTESIAN_POINT('Ctrl Pts',(7.85759813719054,0.719496056538602,-29.054622812363));
#77791=CARTESIAN_POINT('Ctrl Pts',(5.47852496562181,5.03320978803537,-28.8429377444543));
#77792=CARTESIAN_POINT('Ctrl Pts',(1.40341428637399,7.75814193498001,-28.6312526765456));
#77793=CARTESIAN_POINT('Ctrl Pts',(-5.23448241451663,6.65300952217338,-28.3666463416597));
#77794=CARTESIAN_POINT('Ctrl Pts',(-8.41970697715564,-0.815281564029267,
-28.0491187397968));
#77795=CARTESIAN_POINT('Ctrl Pts',(-4.6472869109242,-6.36892244422085,-27.7845124049108));
#77796=CARTESIAN_POINT('Ctrl Pts',(0.15504291279928,-7.44544517282956,-27.5728273370022));
#77797=CARTESIAN_POINT('Ctrl Pts',(3.70314588672555,-6.47941834263744,-27.4140635360706));
#77798=CARTESIAN_POINT('Ctrl Pts',(6.33238234358283,-3.91912764643002,-27.2552997351391));
#77799=CARTESIAN_POINT('Ctrl Pts',(7.85019446552089,0.776490083768835,-27.0436146672305));
#77800=CARTESIAN_POINT('Ctrl Pts',(5.54849119593889,5.61014870654456,-26.8319295993218));
#77801=CARTESIAN_POINT('Ctrl Pts',(0.950591926071428,7.37860498735393,-26.6202445314131));
#77802=CARTESIAN_POINT('Ctrl Pts',(-3.92188405481974,6.8393832618917,-26.4085594635044));
#77803=CARTESIAN_POINT('Ctrl Pts',(-8.28887171968077,1.719577699521,-26.1439531286185));
#77804=CARTESIAN_POINT('Ctrl Pts',(-5.9168782103298,-6.04538682417708,-25.8264255267555));
#77805=CARTESIAN_POINT('Ctrl Pts',(0.545474689815221,-7.86529758468923,
-25.5618191918696));
#77806=CARTESIAN_POINT('Ctrl Pts',(4.91289614305521,-5.5966189448607,-25.3501341239609));
#77807=CARTESIAN_POINT('Ctrl Pts',(7.00547873163074,-2.5728232076744,-25.1913703230294));
#77808=CARTESIAN_POINT('Ctrl Pts',(7.3684644288746,1.0790549637259,-25.0326065220979));
#77809=CARTESIAN_POINT('Ctrl Pts',(5.50612708594302,5.64898703398499,-24.8209214541893));
#77810=CARTESIAN_POINT('Ctrl Pts',(0.632619829400307,7.86506930753982,-24.6092363862805));
#77811=CARTESIAN_POINT('Ctrl Pts',(-4.0239434650627,6.25742083923526,-24.3975513183718));
#77812=CARTESIAN_POINT('Ctrl Pts',(-7.40462241471851,2.707379699625,-24.1858662504631));
#77813=CARTESIAN_POINT('Ctrl Pts',(-7.44902470697067,-4.02173753058972,
-23.9212599155773));
#77814=CARTESIAN_POINT('Ctrl Pts',(-0.634211270789191,-8.43527863640637,
-23.6037323137142));
#77815=CARTESIAN_POINT('Ctrl Pts',(5.48196409580995,-5.66643789211513,-23.3391259788284));
#77816=CARTESIAN_POINT('Ctrl Pts',(7.3625970416972,-1.1184171529497,-23.1274409109197));
#77817=CARTESIAN_POINT('Ctrl Pts',(7.01653254322224,2.54252287839892,-22.9686771099882));
#77818=CARTESIAN_POINT('Ctrl Pts',(4.94273135327337,5.5702813594737,-22.8099133090567));
#77819=CARTESIAN_POINT('Ctrl Pts',(0.57519857567604,7.86750510614556,-22.598228241148));
#77820=CARTESIAN_POINT('Ctrl Pts',(-4.58046582617219,6.42486232352286,-22.3865431732393));
#77821=CARTESIAN_POINT('Ctrl Pts',(-7.10796983245198,2.19640648111162,-22.1748581053306));
#77822=CARTESIAN_POINT('Ctrl Pts',(-7.40855804938307,-2.696591472844,-21.9631730374219));
#77823=CARTESIAN_POINT('Ctrl Pts',(-3.10951410581919,-7.87358011807365,
-21.698566702536));
#77824=CARTESIAN_POINT('Ctrl Pts',(4.94641764083134,-6.86214996428105,-21.3810391006731));
#77825=CARTESIAN_POINT('Ctrl Pts',(7.84294450647332,-0.805400646465767,
-21.1164327657871));
#77826=CARTESIAN_POINT('Ctrl Pts',(6.35323936598892,3.88523380054131,-20.9047476978785));
#77827=CARTESIAN_POINT('Ctrl Pts',(3.73111407493928,6.46335356274661,-20.7459838969469));
#77828=CARTESIAN_POINT('Ctrl Pts',(0.194828916586261,7.44450598411966,-20.5872200960154));
#77829=CARTESIAN_POINT('Ctrl Pts',(-4.62596685695389,6.38975121855693,-20.3755350281067));
#77830=CARTESIAN_POINT('Ctrl Pts',(-7.64157990149821,1.96615860753231,-20.163849960198));
#77831=CARTESIAN_POINT('Ctrl Pts',(-6.85256530936594,-2.89651260142109,
-19.9521648922894));
#77832=CARTESIAN_POINT('Ctrl Pts',(-3.93184193858918,-6.83366350594211,
-19.7404798243806));
#77833=CARTESIAN_POINT('Ctrl Pts',(2.69089288404973,-8.02629661404211,-19.4758734894948));
#77834=CARTESIAN_POINT('Ctrl Pts',(8.20314531815434,-2.06508026455434,-19.1583458876318));
#77835=CARTESIAN_POINT('Ctrl Pts',(6.51919189567336,4.43402590884787,-18.8937395527459));
#77836=CARTESIAN_POINT('Ctrl Pts',(2.35903449854064,7.0635436121762,-18.6820544848372));
#77837=CARTESIAN_POINT('Ctrl Pts',(-1.30723777536977,7.34760375332838,-18.5232906839057));
#77838=CARTESIAN_POINT('Ctrl Pts',(-4.64460706874297,5.82118998412822,-18.3645268829742));
#77839=CARTESIAN_POINT('Ctrl Pts',(-7.65378364228116,1.90999632298988,-18.1528418150655));
#77840=CARTESIAN_POINT('Ctrl Pts',(-7.11256506848367,-3.41627592672793,
-17.9411567471568));
#77841=CARTESIAN_POINT('Ctrl Pts',(-3.37772277338639,-6.62860659833298,
-17.7294716792481));
#77842=CARTESIAN_POINT('Ctrl Pts',(1.39211251672382,-7.76017787703827,-17.5177866113394));
#77843=CARTESIAN_POINT('Ctrl Pts',(7.227078017077,-4.40813851700414,-17.2531802764535));
#77844=CARTESIAN_POINT('Ctrl Pts',(7.6059122274626,3.70219513234312,-16.9356526745905));
#77845=CARTESIAN_POINT('Ctrl Pts',(2.13262510438074,7.59028055457192,-16.6710463397047));
#77846=CARTESIAN_POINT('Ctrl Pts',(-2.74348017632364,6.92329463828742,-16.459361271796));
#77847=CARTESIAN_POINT('Ctrl Pts',(-5.73142970221724,4.77983944142699,-16.3005974708645));
#77848=CARTESIAN_POINT('Ctrl Pts',(-7.3019369555535,1.46299157600233,-16.1418336699329));
#77849=CARTESIAN_POINT('Ctrl Pts',(-7.08573801871702,-3.46710350678975,
-15.9301486020242));
#77850=CARTESIAN_POINT('Ctrl Pts',(-3.24196043414937,-7.19369276549707,
-15.7184635341156));
#77851=CARTESIAN_POINT('Ctrl Pts',(1.68402460811039,-7.24648174555041,-15.5067784662069));
#77852=CARTESIAN_POINT('Ctrl Pts',(6.06203162144491,-5.04084423118742,-15.2950933982982));
#77853=CARTESIAN_POINT('Ctrl Pts',(8.36787344713815,1.28102920446546,-15.0304870634123));
#77854=CARTESIAN_POINT('Ctrl Pts',(3.43530743692631,7.73012370040796,-14.7129594615493));
#77855=CARTESIAN_POINT('Ctrl Pts',(-3.25588096342051,7.18050749494654,-14.4483531266634));
#77856=CARTESIAN_POINT('Ctrl Pts',(-6.55706669530387,3.53037795140363,-14.2366680587547));
#77857=CARTESIAN_POINT('Ctrl Pts',(-7.46290994832736,-0.033565166995917,
-14.0779042578232));
#77858=CARTESIAN_POINT('Ctrl Pts',(-6.52870728675789,-3.58254222838565,
-13.9191404568917));
#77859=CARTESIAN_POINT('Ctrl Pts',(-3.18870634438395,-7.21530608123946,
-13.707455388983));
#77860=CARTESIAN_POINT('Ctrl Pts',(2.15176586145997,-7.59140479347599,-13.4957703210743));
#77861=CARTESIAN_POINT('Ctrl Pts',(5.95459195800815,-4.45985102698973,-13.2840852531656));
#77862=CARTESIAN_POINT('Ctrl Pts',(7.88391730271688,0.046753678088791,-13.0724001852569));
#77863=CARTESIAN_POINT('Ctrl Pts',(5.57731636225459,6.36835018237381,-12.8077938503711));
#77864=CARTESIAN_POINT('Ctrl Pts',(-2.34925633818179,8.1263241547038,-12.4902662485081));
#77865=CARTESIAN_POINT('Ctrl Pts',(-7.11472529640173,3.39722426249561,-12.2256599136221));
#77866=CARTESIAN_POINT('Ctrl Pts',(-7.2900448845705,-1.52116327439485,-12.0139748457135));
#77867=CARTESIAN_POINT('Ctrl Pts',(-5.68820311124292,-4.83120035628055,
-11.855211044782));
#77868=CARTESIAN_POINT('Ctrl Pts',(-2.68819296394879,-6.94494393374836,
-11.6964472438505));
#77869=CARTESIAN_POINT('Ctrl Pts',(2.20642742071403,-7.57364958483073,-11.4847621759418));
#77870=CARTESIAN_POINT('Ctrl Pts',(6.53456026565597,-4.42256093179789,-11.2730771080331));
#77871=CARTESIAN_POINT('Ctrl Pts',(7.42760265059398,0.422084629198934,-11.0613920401244));
#77872=CARTESIAN_POINT('Ctrl Pts',(6.00182032800683,5.11238600780666,-10.8497069722157));
#77873=CARTESIAN_POINT('Ctrl Pts',(0.166452356394491,8.46372468024947,-10.5851006373298));
#77874=CARTESIAN_POINT('Ctrl Pts',(-7.03010423234284,4.7046555763631,-10.2675730354668));
#77875=CARTESIAN_POINT('Ctrl Pts',(-7.63096492057063,-1.98212590769799,
-10.0029667005809));
#77876=CARTESIAN_POINT('Ctrl Pts',(-4.59805059163296,-5.85803916709372,
-9.79128163267221));
#77877=CARTESIAN_POINT('Ctrl Pts',(-1.24109309452522,-7.3590651205164,-9.6325178317407));
#77878=CARTESIAN_POINT('Ctrl Pts',(2.41527475272299,-7.04450676223615,-9.47375403080917));
#77879=CARTESIAN_POINT('Ctrl Pts',(6.56494847360213,-4.37377886222366,-9.26206896290048));
#77880=CARTESIAN_POINT('Ctrl Pts',(7.84732019852157,0.824068421206676,-9.0503838949918));
#77881=CARTESIAN_POINT('Ctrl Pts',(5.41101415828665,5.105718592729,-8.83869882708312));
#77882=CARTESIAN_POINT('Ctrl Pts',(1.29997809904393,7.77614267387747,-8.62701375917442));
#77883=CARTESIAN_POINT('Ctrl Pts',(-5.32261346430697,6.58271431550789,-8.36240742428857));
#77884=CARTESIAN_POINT('Ctrl Pts',(-8.40810366342223,-0.927330790472802,
-8.04487982242553));
#77885=CARTESIAN_POINT('Ctrl Pts',(-4.5620627137284,-6.43024358239611,-7.78027348753966));
#77886=CARTESIAN_POINT('Ctrl Pts',(0.254176868243534,-7.44272035253782,
-7.56858841963099));
#77887=CARTESIAN_POINT('Ctrl Pts',(3.78910108201798,-6.42953065997176,-7.40982461869945));
#77888=CARTESIAN_POINT('Ctrl Pts',(6.38401014661282,-3.83445460297475,-7.25106081776795));
#77889=CARTESIAN_POINT('Ctrl Pts',(7.8391582190614,0.88095880339981,-7.03937574985924));
#77890=CARTESIAN_POINT('Ctrl Pts',(5.47329134412917,5.68353806382972,-6.82769068195057));
#77891=CARTESIAN_POINT('Ctrl Pts',(0.852250015990716,7.39060934428252,-6.61600561404187));
#77892=CARTESIAN_POINT('Ctrl Pts',(-4.01261334852559,6.78655082184165,-6.40432054613319));
#77893=CARTESIAN_POINT('Ctrl Pts',(-8.31103560754686,1.60904598428258,-6.13971421124732));
#77894=CARTESIAN_POINT('Ctrl Pts',(-5.83584982033124,-6.12364323641863,
-5.82218660938429));
#77895=CARTESIAN_POINT('Ctrl Pts',(0.650165015118219,-7.85733632873061,
-5.55758027449843));
#77896=CARTESIAN_POINT('Ctrl Pts',(4.98698822100662,-5.53069983016105,-5.34589520658973));
#77897=CARTESIAN_POINT('Ctrl Pts',(7.03911871088246,-2.47930621227326,-5.18713140565822));
#77898=CARTESIAN_POINT('Ctrl Pts',(7.353441773466,1.17708186789058,-5.02836760472671));
#77899=CARTESIAN_POINT('Ctrl Pts',(5.43041379954702,5.72180880621457,-4.816682536818));
#77900=CARTESIAN_POINT('Ctrl Pts',(0.527828079749971,7.87279623069239,-4.60499746890933));
#77901=CARTESIAN_POINT('Ctrl Pts',(-4.10691396866242,6.20328092769522,-4.39331240100062));
#77902=CARTESIAN_POINT('Ctrl Pts',(-7.44001884079827,2.60853553899251,-4.18162733309195));
#77903=CARTESIAN_POINT('Ctrl Pts',(-7.39480848519591,-4.1205762644595,-3.91702099820607));
#77904=CARTESIAN_POINT('Ctrl Pts',(-0.521826194395602,-8.44297625313128,
-3.59949339634306));
#77905=CARTESIAN_POINT('Ctrl Pts',(5.55693552491327,-5.59293446557778,-3.33488706145718));
#77906=CARTESIAN_POINT('Ctrl Pts',(7.37683758691506,-1.02027366322683,-3.1232019935485));
#77907=CARTESIAN_POINT('Ctrl Pts',(6.98205292519039,2.63573378257931,-2.96443819261698));
#77908=CARTESIAN_POINT('Ctrl Pts',(4.86811576200549,5.63560708473504,-2.80567439168545));
#77909=CARTESIAN_POINT('Ctrl Pts',(0.470380277749741,7.87446837668858,-2.59398932377678));
#77910=CARTESIAN_POINT('Ctrl Pts',(-4.66561825254938,6.36329427350808,-2.38230425586808));
#77911=CARTESIAN_POINT('Ctrl Pts',(-7.13658637022202,2.10156075002914,-2.17061918795939));
#77912=CARTESIAN_POINT('Ctrl Pts',(-7.37199597901472,-2.79501521255998,
-1.9589341200507));
#77913=CARTESIAN_POINT('Ctrl Pts',(-3.00438054821123,-7.914276477521,-1.69432778516484));
#77914=CARTESIAN_POINT('Ctrl Pts',(5.03734365599351,-6.79569608394466,-1.37680018330181));
#77915=CARTESIAN_POINT('Ctrl Pts',(7.85300067508422,-0.700847833672291,
-1.11219384841594));
#77916=CARTESIAN_POINT('Ctrl Pts',(6.30090148669033,3.96943667741106,-0.900508780507268));
#77917=CARTESIAN_POINT('Ctrl Pts',(3.64479345598366,6.51258800445165,-0.741744979575735));
#77918=CARTESIAN_POINT('Ctrl Pts',(0.0955276237381259,7.44621302766392,
-0.582981178644231));
#77919=CARTESIAN_POINT('Ctrl Pts',(-4.71030661113408,6.32810132960302,-0.371296110735536));
#77920=CARTESIAN_POINT('Ctrl Pts',(-7.66773584340214,1.86323026021221,-0.159611042826847));
#77921=CARTESIAN_POINT('Ctrl Pts',(-6.81262520422293,-2.98634583944321,
0.0520740250818385));
#77922=CARTESIAN_POINT('Ctrl Pts',(-3.84226758436661,-6.88813227096892,
0.263759092990537));
#77923=CARTESIAN_POINT('Ctrl Pts',(2.80126517201592,-7.98399944675405,0.528365427876391));
#77924=CARTESIAN_POINT('Ctrl Pts',(8.22361795704757,-1.96563912835421,0.845893029739429));
#77925=CARTESIAN_POINT('Ctrl Pts',(6.11747873359508,5.83678708112643,1.16342063160247));
#77926=CARTESIAN_POINT('Ctrl Pts',(-1.59680123828806,8.30912507639158,1.4809482334655));
#77927=CARTESIAN_POINT('Ctrl Pts',(-6.78649111104133,4.01907013773023,1.74555456835137));
#77928=CARTESIAN_POINT('Ctrl Pts',(-7.38999319219831,-0.847422129305244,
1.95723963626005));
#77929=CARTESIAN_POINT('Ctrl Pts',(-5.68863521383442,-5.46856739655706,
2.16892470416873));
#77930=CARTESIAN_POINT('Ctrl Pts',(-0.886184247744874,-7.83878385259253,
2.38060977207743));
#77931=CARTESIAN_POINT('Ctrl Pts',(3.82950340562284,-6.3867141509991,2.59229483998611));
#77932=CARTESIAN_POINT('Ctrl Pts',(6.42686542591582,-3.79390598851325,2.75105864091764));
#77933=CARTESIAN_POINT('Ctrl Pts',(7.44247115572417,-0.259634699464653,
2.90982244184915));
#77934=CARTESIAN_POINT('Ctrl Pts',(6.43364876941854,4.55729862973626,3.12150750975785));
#77935=CARTESIAN_POINT('Ctrl Pts',(0.933504659789757,8.40743036986156,3.38611384464369));
#77936=CARTESIAN_POINT('Ctrl Pts',(-6.57877351294465,5.32745846595636,3.70364144650676));
#77937=CARTESIAN_POINT('Ctrl Pts',(-7.77710587116025,-1.2942407124703,3.96824778139258));
#77938=CARTESIAN_POINT('Ctrl Pts',(-5.10970404230305,-5.40724950467182,
4.1799328493013));
#77939=CARTESIAN_POINT('Ctrl Pts',(-0.829856799302938,-7.84670920720481,
4.39161791720997));
#77940=CARTESIAN_POINT('Ctrl Pts',(4.36893838930713,-6.56817228546896,4.60330298511867));
#77941=CARTESIAN_POINT('Ctrl Pts',(7.04272340848429,-2.4204679872681,4.81498805302735));
#77942=CARTESIAN_POINT('Ctrl Pts',(7.3599785283304,1.23566649436854,4.97375185395888));
#77943=CARTESIAN_POINT('Ctrl Pts',(5.8614277476127,4.59373006293499,5.13251565489037));
#77944=CARTESIAN_POINT('Ctrl Pts',(1.98775206194297,7.62950130116858,5.34420072279909));
#77945=CARTESIAN_POINT('Ctrl Pts',(-4.69947080153288,7.03357126740298,5.60880705768493));
#77946=CARTESIAN_POINT('Ctrl Pts',(-8.46384507724044,-0.160211711261087,
5.92633465954799));
#77947=CARTESIAN_POINT('Ctrl Pts',(-5.11680999772523,-5.99804913757792,
6.19094099443383));
#77948=CARTESIAN_POINT('Ctrl Pts',(-0.427561153418098,-7.42728941633418,
6.40262606234254));
#77949=CARTESIAN_POINT('Ctrl Pts',(4.41774155119458,-6.53781940394695,6.61431113025119));
#77950=CARTESIAN_POINT('Ctrl Pts',(7.57202064866731,-2.21201115398199,6.82599619815993));
#77951=CARTESIAN_POINT('Ctrl Pts',(6.94692414850596,2.68307147023272,7.03768126606858));
#77952=CARTESIAN_POINT('Ctrl Pts',(4.83539316593233,5.68463934220696,7.19644506700012));
#77953=CARTESIAN_POINT('Ctrl Pts',(1.5265380798821,7.28892129320051,7.35520886793162));
#77954=CARTESIAN_POINT('Ctrl Pts',(-3.39197738907421,7.11722826117605,7.56689393584032));
#77955=CARTESIAN_POINT('Ctrl Pts',(-8.12458975238406,2.3552475385514,7.83150027072619));
#77956=CARTESIAN_POINT('Ctrl Pts',(-6.37246081249254,-5.57261922642259,
8.14902787258922));
#77957=CARTESIAN_POINT('Ctrl Pts',(-0.052566768797828,-7.88388068637668,
8.41363420747508));
#77958=CARTESIAN_POINT('Ctrl Pts',(4.45545927411695,-5.95787875222696,8.62531927538377));
#77959=CARTESIAN_POINT('Ctrl Pts',(7.58981615343419,-2.15736269963801,8.83700434329246));
#77960=CARTESIAN_POINT('Ctrl Pts',(7.21765527083583,3.18338536594938,9.04868941120114));
#77961=CARTESIAN_POINT('Ctrl Pts',(3.58735511151804,6.52606397135328,9.26037447910983));
#77962=CARTESIAN_POINT('Ctrl Pts',(0.0390678369844106,7.46288317082481,
9.41913828004134));
#77963=CARTESIAN_POINT('Ctrl Pts',(-3.52554222430388,6.55966799091853,9.57790208097286));
#77964=CARTESIAN_POINT('Ctrl Pts',(-7.17810486177338,3.26117453171754,9.78958714888157));
#77965=CARTESIAN_POINT('Ctrl Pts',(-7.73265457814575,-3.42960679741785,
10.0541934837674));
#77966=CARTESIAN_POINT('Ctrl Pts',(-1.28719879835849,-8.36692662233385,
10.3717210856304));
#77967=CARTESIAN_POINT('Ctrl Pts',(5.03637310113398,-6.06574677419579,10.6363274205163));
#77968=CARTESIAN_POINT('Ctrl Pts',(7.24523808218346,-1.68936724894143,10.848012488425));
#77969=CARTESIAN_POINT('Ctrl Pts',(7.19608122716862,3.236655377538,11.0596975563337));
#77970=CARTESIAN_POINT('Ctrl Pts',(3.47232714063519,7.08317966912418,11.2713826242423));
#77971=CARTESIAN_POINT('Ctrl Pts',(-1.45760719053445,7.30301368836414,11.483067692151));
#77972=CARTESIAN_POINT('Ctrl Pts',(-4.77561214732757,5.73495249636615,11.6418314930825));
#77973=CARTESIAN_POINT('Ctrl Pts',(-6.92126988705709,2.74858423137024,11.8005952940141));
#77974=CARTESIAN_POINT('Ctrl Pts',(-7.59185095453138,-2.12702793050032,
12.0122803619227));
#77975=CARTESIAN_POINT('Ctrl Pts',(-3.70780224593713,-7.60318039473171,
12.2768866968086));
#77976=CARTESIAN_POINT('Ctrl Pts',(4.40280852720821,-7.23032633584101,12.5944142986716));
#77977=CARTESIAN_POINT('Ctrl Pts',(7.75914931159707,-1.39783400403488,12.8590206335575));
#77978=CARTESIAN_POINT('Ctrl Pts',(6.63109531620007,3.37283433876996,13.0707057014662));
#77979=CARTESIAN_POINT('Ctrl Pts',(3.42151935496463,7.11004418865015,13.2823907693749));
#77980=CARTESIAN_POINT('Ctrl Pts',(-1.90435238645548,7.65518987255624,13.4940758372836));
#77981=CARTESIAN_POINT('Ctrl Pts',(-5.81776376141959,4.64889798453833,13.7057609051923));
#77982=CARTESIAN_POINT('Ctrl Pts',(-7.34663788131966,1.31265507961464,13.8645247061238));
#77983=CARTESIAN_POINT('Ctrl Pts',(-7.06528109532774,-2.35382564571477,
14.0232885070553));
#77984=CARTESIAN_POINT('Ctrl Pts',(-4.43883154447283,-6.51592075249081,
14.234973574964));
#77985=CARTESIAN_POINT('Ctrl Pts',(2.05903122121148,-8.20466574821215,14.4995799098498));
#77986=CARTESIAN_POINT('Ctrl Pts',(8.02431033753216,-2.696810237482,14.8171075117129));
#77987=CARTESIAN_POINT('Ctrl Pts',(6.83656074059215,3.92680215731425,15.0817138465987));
#77988=CARTESIAN_POINT('Ctrl Pts',(2.90156446352231,6.85042774090353,15.2933989145075));
#77989=CARTESIAN_POINT('Ctrl Pts',(-1.96052365399983,7.64302754561716,15.5050839824161));
#77990=CARTESIAN_POINT('Ctrl Pts',(-6.38633858541117,4.63067699901154,15.7167690503248));
#77991=CARTESIAN_POINT('Ctrl Pts',(-7.44464761501319,-0.189339754436876,
15.9284541182335));
#77992=CARTESIAN_POINT('Ctrl Pts',(-6.46610289399227,-3.72634739142553,
16.087217919165));
#77993=CARTESIAN_POINT('Ctrl Pts',(-3.88991722241724,-6.35037291260615,
16.2459817200965));
#77994=CARTESIAN_POINT('Ctrl Pts',(0.799617534905987,-7.84353622614305,
16.4576667880052));
#77995=CARTESIAN_POINT('Ctrl Pts',(6.85850092252447,-4.95147601282085,16.7222731228911));
#77996=CARTESIAN_POINT('Ctrl Pts',(7.87587073736038,3.10370777915764,17.0398007247542));
#77997=CARTESIAN_POINT('Ctrl Pts',(2.70205334327046,7.40656773901479,17.30440705964));
#77998=CARTESIAN_POINT('Ctrl Pts',(-2.19116491540037,7.10958739188392,17.5160921275487));
#77999=CARTESIAN_POINT('Ctrl Pts',(-6.42148323042302,4.58520186931298,17.7277771954574));
#78000=CARTESIAN_POINT('Ctrl Pts',(-7.86792708265074,-0.569397417255415,
17.9394622633661));
#78001=CARTESIAN_POINT('Ctrl Pts',(-5.57392430365033,-4.93862283551883,
18.1511473312747));
#78002=CARTESIAN_POINT('Ctrl Pts',(-2.54769573582305,-7.01465593988385,
18.3099111322063));
#78003=CARTESIAN_POINT('Ctrl Pts',(1.11298813422668,-7.36341969057114,18.4686749331378));
#78004=CARTESIAN_POINT('Ctrl Pts',(5.6623942972133,-5.48614067955183,18.6803600010465));
#78005=CARTESIAN_POINT('Ctrl Pts',(8.43574397081144,0.627991455935019,18.9449663359324));
#78006=CARTESIAN_POINT('Ctrl Pts',(4.02722887835911,7.44605730647597,19.2624939377953));
#78007=CARTESIAN_POINT('Ctrl Pts',(-2.70191926211008,7.40661665293494,19.5271002726813));
#78008=CARTESIAN_POINT('Ctrl Pts',(-6.25445213614084,4.02855619869448,19.7387853405899));
#78009=CARTESIAN_POINT('Ctrl Pts',(-7.86553362351802,-0.62682045137493,
19.9504704084987));
#78010=CARTESIAN_POINT('Ctrl Pts',(-5.6530453692469,-5.50196038243845,20.1621554764072));
#78011=CARTESIAN_POINT('Ctrl Pts',(-1.08448771134512,-7.36766679880903,
20.373840544316));
#78012=CARTESIAN_POINT('Ctrl Pts',(2.56765711011421,-7.00737386487682,20.5326043452475));
#78013=CARTESIAN_POINT('Ctrl Pts',(5.59299496375529,-4.91702140140031,20.6913681461791));
#78014=CARTESIAN_POINT('Ctrl Pts',(7.86489324800924,-0.551273915912889,
20.9030532140877));
#78015=CARTESIAN_POINT('Ctrl Pts',(6.04974791365749,5.9124191149653,21.1676595489736));
#78016=CARTESIAN_POINT('Ctrl Pts',(-1.71346554085533,8.29013737463471,21.4851871508366));
#78017=CARTESIAN_POINT('Ctrl Pts',(-6.83648965277288,3.92692591858082,21.7497934857225));
#78018=CARTESIAN_POINT('Ctrl Pts',(-7.37930388813884,-0.94515114971917,
21.9614785536312));
#78019=CARTESIAN_POINT('Ctrl Pts',(-5.61423828898686,-5.54435311785144,
22.1731636215399));
#78020=CARTESIAN_POINT('Ctrl Pts',(-0.782278110981478,-7.84961979676501,
22.3848486894485));
#78021=CARTESIAN_POINT('Ctrl Pts',(3.91445748172455,-6.33527033978052,22.5965337573573));
#78022=CARTESIAN_POINT('Ctrl Pts',(6.47668611509837,-3.70792239451836,22.7552975582887));
#78023=CARTESIAN_POINT('Ctrl Pts',(7.44532883004716,-0.160532672340616,
22.9140613592203));
#78024=CARTESIAN_POINT('Ctrl Pts',(6.37234732920244,4.64258960591542,23.1257464271289));
#78025=CARTESIAN_POINT('Ctrl Pts',(0.821489503303927,8.41910355119662,23.3903527620148));
#78026=CARTESIAN_POINT('Ctrl Pts',(-6.64914813647221,5.23938650122914,23.7078803638778));
#78027=CARTESIAN_POINT('Ctrl Pts',(-7.75917461524326,-1.39769354032214,
23.9724866987637));
#78028=CARTESIAN_POINT('Ctrl Pts',(-5.03724793862302,-5.47481230492465,
24.1841717666724));
#78029=CARTESIAN_POINT('Ctrl Pts',(-0.725289558244549,-7.85706549022317,
24.3958568345811));
#78030=CARTESIAN_POINT('Ctrl Pts',(4.45601514279779,-6.50941003807893,24.6075419024897));
#78031=CARTESIAN_POINT('Ctrl Pts',(7.07433180898348,-2.32646880717035,24.8192269703985));
#78032=CARTESIAN_POINT('Ctrl Pts',(7.34287079315154,1.33356665838692,24.97799077133));
#78033=CARTESIAN_POINT('Ctrl Pts',(5.79973548633705,4.67137671516041,25.1367545722615));
#78034=CARTESIAN_POINT('Ctrl Pts',(1.88597701080095,7.65529486353575,25.3484396401702));
#78035=CARTESIAN_POINT('Ctrl Pts',(-4.79271700308801,6.97036680083047,25.613045975056));
#78036=CARTESIAN_POINT('Ctrl Pts',(-8.46096115952763,-0.27290677342026,
25.9305735769191));
#78037=CARTESIAN_POINT('Ctrl Pts',(-5.03648290821302,-6.06565559999674,
26.1951799118049));
#78038=CARTESIAN_POINT('Ctrl Pts',(-0.328617317895261,-7.43232448347727,
26.4068649797136));
#78039=CARTESIAN_POINT('Ctrl Pts',(4.50441109075738,-6.47841059106454,26.6185500476223));
#78040=CARTESIAN_POINT('Ctrl Pts',(7.60080561490422,-2.11098176238599,26.830235115531));
#78041=CARTESIAN_POINT('Ctrl Pts',(6.91057889396949,2.77534268236474,27.0419201834397));
#78042=CARTESIAN_POINT('Ctrl Pts',(4.75926458443607,5.74852608349403,27.2006839843712));
#78043=CARTESIAN_POINT('Ctrl Pts',(1.42933937950413,7.30860322254663,27.3594477853027));
#78044=CARTESIAN_POINT('Ctrl Pts',(-3.48645360850935,7.07142771784166,27.5711328532114));
#78045=CARTESIAN_POINT('Ctrl Pts',(-8.15523314124773,2.24684712913524,27.8357391880973));
#78046=CARTESIAN_POINT('Ctrl Pts',(-6.29768766347067,-5.65698435063977,
28.1532667899603));
#78047=CARTESIAN_POINT('Ctrl Pts',(0.0524240472627744,-7.88388163671697,
28.4178731248462));
#78048=CARTESIAN_POINT('Ctrl Pts',(4.53440265005737,-5.89801908919164,28.6295581927548));
#78049=CARTESIAN_POINT('Ctrl Pts',(7.61787181549885,-2.05610118028825,28.8412432606637));
#78050=CARTESIAN_POINT('Ctrl Pts',(7.17462355037663,3.27921742296345,29.0529283285722));
#78051=CARTESIAN_POINT('Ctrl Pts',(3.5001323134553,6.57325653254444,29.264613396481));
#78052=CARTESIAN_POINT('Ctrl Pts',(-0.0603155442375287,7.46274169138947,
29.4233771974124));
#78053=CARTESIAN_POINT('Ctrl Pts',(-3.61258181668668,6.5121382620584,29.582140998344));
#78054=CARTESIAN_POINT('Ctrl Pts',(-7.22089600433169,3.16529771547212,29.7938260662526));
#78055=CARTESIAN_POINT('Ctrl Pts',(-7.68629837108023,-3.53227504032997,
30.0584324011386));
#78056=CARTESIAN_POINT('Ctrl Pts',(-1.17566599913336,-8.38332579043041,
30.3759600030015));
#78057=CARTESIAN_POINT('Ctrl Pts',(5.1167013986517,-5.99814177387708,30.6405663378874));
#78058=CARTESIAN_POINT('Ctrl Pts',(7.26709220913254,-1.59273582030463,30.8522514057961));
#78059=CARTESIAN_POINT('Ctrl Pts',(7.15234204646914,3.33219541912908,31.0639364737048));
#78060=CARTESIAN_POINT('Ctrl Pts',(3.3776956784777,7.12879105460941,31.2756215416134));
#78061=CARTESIAN_POINT('Ctrl Pts',(-1.55472895139519,7.28295582452796,31.4873066095222));
#78062=CARTESIAN_POINT('Ctrl Pts',(-4.85155852512464,5.67084926572459,31.6460704104537));
#78063=CARTESIAN_POINT('Ctrl Pts',(-6.95725786448992,2.65617302399775,31.8048342113852));
#78064=CARTESIAN_POINT('Ctrl Pts',(-7.56285309954371,-2.22793665252618,
32.0165192792939));
#78065=CARTESIAN_POINT('Ctrl Pts',(-3.60622528451092,-7.65188139003492,
32.2811256141798));
#78066=CARTESIAN_POINT('Ctrl Pts',(4.49870119380519,-7.17105497251761,32.5986532160427));
#78067=CARTESIAN_POINT('Ctrl Pts',(7.77707565101753,-1.29438489671535,32.8632595509287));
#78068=CARTESIAN_POINT('Ctrl Pts',(6.58559279735529,3.46083863777819,33.0749446188373));
#78069=CARTESIAN_POINT('Ctrl Pts',(3.32653465496305,7.15497660724926,33.2866296867461));
#78070=CARTESIAN_POINT('Ctrl Pts',(-2.00612430934377,7.62915167316433,33.4983147546547));
#78071=CARTESIAN_POINT('Ctrl Pts',(-5.87915522440015,4.5710131810946,33.7099998225634));
#78072=CARTESIAN_POINT('Ctrl Pts',(-7.36346650774268,1.21470675746504,33.8687636234949));
#78073=CARTESIAN_POINT('Ctrl Pts',(-7.03330976597137,-2.44770215964113,
34.0275274244265));
#78074=CARTESIAN_POINT('Ctrl Pts',(-4.35166831935865,-6.57445294843889,
34.2392124923351));
#78075=CARTESIAN_POINT('Ctrl Pts',(2.16810655624256,-8.17651903749918,34.503818827221));
#78076=CARTESIAN_POINT('Ctrl Pts',(8.05951105775482,-2.58971491866223,34.821346429084));
#78077=CARTESIAN_POINT('Ctrl Pts',(6.78366305865034,4.01749342864384,35.08595276397));
#78078=CARTESIAN_POINT('Ctrl Pts',(2.81008306505412,6.88845917000401,35.2976378318785));
#78079=CARTESIAN_POINT('Ctrl Pts',(-2.0621286358887,7.61624241670414,35.5093228997874));
#78080=CARTESIAN_POINT('Ctrl Pts',(-6.44743699245361,4.54522235154967,35.7210079676959));
#78081=CARTESIAN_POINT('Ctrl Pts',(-7.44146614955639,-0.288460048080047,
35.9326930356047));
#78082=CARTESIAN_POINT('Ctrl Pts',(-6.41590742781489,-3.81212321351088,
36.0914568365361));
#78083=CARTESIAN_POINT('Ctrl Pts',(-3.80500719656959,-6.40161013811945,
36.2502206374678));
#78084=CARTESIAN_POINT('Ctrl Pts',(0.903995539004252,-7.83219259201457,
36.4619057053764));
#78085=CARTESIAN_POINT('Ctrl Pts',(6.92382940196311,-4.85970534315815,36.7265120402622));
#78086=CARTESIAN_POINT('Ctrl Pts',(7.83384168462113,3.2083120656049,37.0440396421253));
#78087=CARTESIAN_POINT('Ctrl Pts',(2.60318376473262,7.44189305415814,37.3086459770111));
#78088=CARTESIAN_POINT('Ctrl Pts',(-2.28564585970917,7.07977821498037,37.5203310449198));
#78089=CARTESIAN_POINT('Ctrl Pts',(-6.48197294900942,4.4992832483924,37.7320161128285));
#78090=CARTESIAN_POINT('Ctrl Pts',(-7.85964702536755,-0.67412063706526,
37.9437011807372));
#78091=CARTESIAN_POINT('Ctrl Pts',(-5.50766460996938,-5.01241041799476,
38.1553862486459));
#78092=CARTESIAN_POINT('Ctrl Pts',(-2.45405876029574,-7.04796049352537,
38.3141500495774));
#78093=CARTESIAN_POINT('Ctrl Pts',(1.21094485225064,-7.34794561025246,38.4729138505089));
#78094=CARTESIAN_POINT('Ctrl Pts',(5.73494872765964,-5.41025062488443,38.6845989184177));
#78095=CARTESIAN_POINT('Ctrl Pts',(8.42663329468905,0.740270846816575,38.9492052533034));
#78096=CARTESIAN_POINT('Ctrl Pts',(3.92771593232857,7.49902589707133,39.2667328551665));
#78097=CARTESIAN_POINT('Ctrl Pts',(-2.80031032559594,7.36997964874085,39.5313391900524));
#78098=CARTESIAN_POINT('Ctrl Pts',(-6.30754406085944,3.94491121441702,39.7430242579611));
#78099=CARTESIAN_POINT('Ctrl Pts',(-7.85648910129288,-0.731506706887516,
39.9547093258698));
#78100=CARTESIAN_POINT('Ctrl Pts',(-5.57927694280141,-5.57675163443824,
40.1663943937784));
#78101=CARTESIAN_POINT('Ctrl Pts',(-0.986279587833537,-7.38145515660392,
40.3780794616871));
#78102=CARTESIAN_POINT('Ctrl Pts',(2.66074353875926,-6.97256017100103,40.5368432626186));
#78103=CARTESIAN_POINT('Ctrl Pts',(5.65797683787586,-4.84210597038945,40.6956070635502));
#78104=CARTESIAN_POINT('Ctrl Pts',(7.87153694461785,-0.446491727206108,
40.9072921314589));
#78105=CARTESIAN_POINT('Ctrl Pts',(5.9704784143324,5.99245668434905,41.1718984663447));
#78106=CARTESIAN_POINT('Ctrl Pts',(-1.82370970482655,8.26658483066225,41.4894260682078));
#78107=CARTESIAN_POINT('Ctrl Pts',(-6.8881766031114,3.83553920939982,41.7540324030937));
#78108=CARTESIAN_POINT('Ctrl Pts',(-7.36606341032977,-1.04333427256905,
41.9657174710023));
#78109=CARTESIAN_POINT('Ctrl Pts',(-5.53990877821464,-5.61862383417993,
42.177402538911));
#78110=CARTESIAN_POINT('Ctrl Pts',(-0.677678829097026,-7.85934102843741,
42.3890876068197));
#78111=CARTESIAN_POINT('Ctrl Pts',(3.99847438491617,-6.28258149549219,42.6007726747284));
#78112=CARTESIAN_POINT('Ctrl Pts',(6.52548859581569,-3.62134644892725,42.7595364756599));
#78113=CARTESIAN_POINT('Ctrl Pts',(7.44680640067528,-0.0613722843181,42.9183002765914));
#78114=CARTESIAN_POINT('Ctrl Pts',(6.30995898361038,4.72703568403096,43.1299853445001));
#78115=CARTESIAN_POINT('Ctrl Pts',(0.709303181088316,8.42929644793126,43.394591679386));
#78116=CARTESIAN_POINT('Ctrl Pts',(-6.71832915581128,5.15037816128001,43.712119281249));
#78117=CARTESIAN_POINT('Ctrl Pts',(-7.73987414754349,-1.50089510715489,
43.9767256161348));
#78118=CARTESIAN_POINT('Ctrl Pts',(-4.96389563344953,-5.54140566188194,
44.1884106840436));
#78119=CARTESIAN_POINT('Ctrl Pts',(-0.620596178485482,-7.86602717031948,
44.4000957519522));
#78120=CARTESIAN_POINT('Ctrl Pts',(4.54230296786022,-6.44949406890597,44.6117808198609));
#78121=CARTESIAN_POINT('Ctrl Pts',(7.10468508996624,-2.23205677050182,44.8234658877696));
#78122=CARTESIAN_POINT('Ctrl Pts',(7.32446118816338,1.43123017728363,44.9822296887011));
#78123=CARTESIAN_POINT('Ctrl Pts',(5.73701456861917,4.74819502188697,45.1409934896327));
#78124=CARTESIAN_POINT('Ctrl Pts',(1.78386760397576,7.67973079635173,45.3526785575413));
#78125=CARTESIAN_POINT('Ctrl Pts',(-4.88511333053378,6.90592624907402,45.6172848924272));
#78126=CARTESIAN_POINT('Ctrl Pts',(-8.45657675320892,-0.385553455566417,
45.9348124942902));
#78127=CARTESIAN_POINT('Ctrl Pts',(-4.95526267182601,-6.13218637972633,
46.1994188291761));
#78128=CARTESIAN_POINT('Ctrl Pts',(-0.229615199062717,-7.43604151613453,
46.4111038970848));
#78129=CARTESIAN_POINT('Ctrl Pts',(4.59028181864933,-6.41785290313922,46.6227889649935));
#78130=CARTESIAN_POINT('Ctrl Pts',(7.62824266808339,-2.00957801379248,46.8344740329021));
#78131=CARTESIAN_POINT('Ctrl Pts',(6.87300812585219,2.8671217198266,47.0461591008109));
#78132=CARTESIAN_POINT('Ctrl Pts',(4.6822920024229,5.81139338896664,47.2049229017423));
#78133=CARTESIAN_POINT('Ctrl Pts',(1.33188720178281,7.326989054731,47.3636867026739));
#78134=CARTESIAN_POINT('Ctrl Pts',(-3.58031154497339,7.02437313743209,47.5753717705826));
#78135=CARTESIAN_POINT('Ctrl Pts',(-8.1844302927773,2.13804826710671,47.8399781054684));
#78136=CARTESIAN_POINT('Ctrl Pts',(-6.22179769137573,-5.74034627331874,
48.1575057073316));
#78137=CARTESIAN_POINT('Ctrl Pts',(0.157405566479999,-7.8824844706561,48.4221120422172));
#78138=CARTESIAN_POINT('Ctrl Pts',(4.61254190148167,-5.83711347982825,48.6337971101261));
#78139=CARTESIAN_POINT('Ctrl Pts',(7.64457653497177,-1.95447503486593,48.8454821780346));
#78140=CARTESIAN_POINT('Ctrl Pts',(7.13031949236453,3.37446794820925,49.0571672459435));
#78141=CARTESIAN_POINT('Ctrl Pts',(3.41228880689173,6.61928340175076,49.2688523138521));
#78142=CARTESIAN_POINT('Ctrl Pts',(-0.159688229184292,7.46127677993111,
49.4276161147836));
#78143=CARTESIAN_POINT('Ctrl Pts',(-3.6989807589367,6.46345367983997,49.5863799157152));
#78144=CARTESIAN_POINT('Ctrl Pts',(-7.26240660343833,3.06885956982117,49.7980649836238));
#78145=CARTESIAN_POINT('Ctrl Pts',(-7.63857908676835,-3.63431687459858,
50.0626713185097));
#78146=CARTESIAN_POINT('Ctrl Pts',(-1.06392470896808,-8.39823827142704,
50.3801989203728));
#78147=CARTESIAN_POINT('Ctrl Pts',(5.19612230760402,-5.92947307160712,50.6448052552585));
#78148=CARTESIAN_POINT('Ctrl Pts',(7.28765760026079,-1.49582193815768,50.8564903231673));
#78149=CARTESIAN_POINT('Ctrl Pts',(7.10733447958075,3.42714453391363,51.068175391076));
#78150=CARTESIAN_POINT('Ctrl Pts',(3.28246522055953,7.17313823040342,51.2798604589846));
#78151=CARTESIAN_POINT('Ctrl Pts',(-1.65157499882752,7.26160641164148,51.4915455268934));
#78152=CARTESIAN_POINT('Ctrl Pts',(-4.92664453442159,5.60574037471812,51.6503093278248));
#78153=CARTESIAN_POINT('Ctrl Pts',(-6.99201205167683,2.56329077467563,51.8090731287563));
#78154=CARTESIAN_POINT('Ctrl Pts',(-7.53251405893683,-2.3284502754392,52.0207581966651));
#78155=CARTESIAN_POINT('Ctrl Pts',(-3.50400880017233,-7.69922541152626,
52.2853645315508));
#78156=CARTESIAN_POINT('Ctrl Pts',(4.59379606705064,-7.11051190452267,52.602892133414));
#78157=CARTESIAN_POINT('Ctrl Pts',(7.7936228149868,-1.19070624494491,52.8674984682998));
#78158=CARTESIAN_POINT('Ctrl Pts',(6.53892239868291,3.5482291964793,53.0791835362085));
#78159=CARTESIAN_POINT('Ctrl Pts',(3.23096003240178,7.1986401726906,53.2908686041172));
#78160=CARTESIAN_POINT('Ctrl Pts',(-2.10754046975733,7.60176053035004,53.5025536720258));
#78161=CARTESIAN_POINT('Ctrl Pts',(-5.93950408539159,4.49231776126522,53.7142387399347));
#78162=CARTESIAN_POINT('Ctrl Pts',(-7.37898930942744,1.11654301968292,53.873002540866));
#78163=CARTESIAN_POINT('Ctrl Pts',(-7.00009115585931,-2.54114459924067,
54.0317663417977));
#78164=CARTESIAN_POINT('Ctrl Pts',(-4.26373338329906,-6.63181924519665,
54.2434514097062));
#78165=CARTESIAN_POINT('Ctrl Pts',(2.27679741834353,-8.14692230422807,54.5080577445922));
#78166=CARTESIAN_POINT('Ctrl Pts',(8.09328248775631,-2.48216036142054,54.8255853464552));
#78167=CARTESIAN_POINT('Ctrl Pts',(6.72956241843219,4.10747227349011,55.090191681341));
#78168=CARTESIAN_POINT('Ctrl Pts',(2.71810326799314,6.92526896945336,55.3018767492498));
#78169=CARTESIAN_POINT('Ctrl Pts',(-2.16336776199988,7.58810673736746,55.5135618171584));
#78170=CARTESIAN_POINT('Ctrl Pts',(-6.50739234715102,4.45896145096741,55.7252468850672));
#78171=CARTESIAN_POINT('Ctrl Pts',(-7.43696462099792,-0.387528927329647,
55.9369319529758));
#78172=CARTESIAN_POINT('Ctrl Pts',(-6.36457501450357,-3.89722353864109,
56.0956957539074));
#78173=CARTESIAN_POINT('Ctrl Pts',(-3.71942086257268,-6.4517111270184,56.2544595548388));
#78174=CARTESIAN_POINT('Ctrl Pts',(1.0082099163406,-7.81946213435861,56.4661446227476));
#78175=CARTESIAN_POINT('Ctrl Pts',(6.98793687374695,-4.7670684614793,56.7307509576334));
#78176=CARTESIAN_POINT('Ctrl Pts',(7.79041141615472,3.3123397107483,57.0482785594965));
#78177=CARTESIAN_POINT('Ctrl Pts',(2.50387262287746,7.47591152173031,57.3128848943822));
#78178=CARTESIAN_POINT('Ctrl Pts',(-2.37974820771574,7.04869636209595,57.524569962291));
#78179=CARTESIAN_POINT('Ctrl Pts',(-6.54124431444534,4.41261091435839,57.7362550301996));
#78180=CARTESIAN_POINT('Ctrl Pts',(-7.85011314244894,-0.778814148529765,
57.9479400981084));
#78181=CARTESIAN_POINT('Ctrl Pts',(-5.440255204774,-5.08519809189294,58.1596251660171));
#78182=CARTESIAN_POINT('Ctrl Pts',(-2.36034655652782,-7.08024618005674,
58.3183889669485));
#78183=CARTESIAN_POINT('Ctrl Pts',(1.30934340514053,-7.33074709976975,58.4771527678801));
#78184=CARTESIAN_POINT('Ctrl Pts',(5.80506746240374,-5.33431154462047,58.6888378357887));
#78185=CARTESIAN_POINT('Ctrl Pts',(8.41896344392571,0.854302628986389,58.9534441706747));
#78186=CARTESIAN_POINT('Ctrl Pts',(3.82237674437087,7.54737245299685,59.2709717725376));
#78187=CARTESIAN_POINT('Ctrl Pts',(-2.88958471775843,7.33756896722465,59.5355781074236));
#78188=CARTESIAN_POINT('Ctrl Pts',(-6.37111707909232,3.85311267538591,59.7472631753321));
#78189=CARTESIAN_POINT('Ctrl Pts',(-7.45324420054764,0.351828748494111,
59.9060269762639));
#78190=CARTESIAN_POINT('Ctrl Pts',(-6.70494820545435,-3.26568653815952,
60.0647974714419));
#78191=CARTESIAN_POINT('Ctrl Pts',(-5.12192455972379,-5.13456107383707,
60.1706466996429));
#78192=CARTESIAN_POINT('Ctrl Pts',(-4.15332558991753,-5.82516755464222,
60.2235746608667));
#78193=CARTESIAN_POINT('Ctrl Pts',(-3.26266258150082,6.80520260935705,-60.2102386032606));
#78194=CARTESIAN_POINT('Ctrl Pts',(-4.39427159822301,6.26266980452596,-60.1573082411063));
#78195=CARTESIAN_POINT('Ctrl Pts',(-6.37755155656977,4.60671016839827,-60.0514566119747));
#78196=CARTESIAN_POINT('Ctrl Pts',(-7.80955707945264,0.982430906290448,
-59.892683715866));
#78197=CARTESIAN_POINT('Ctrl Pts',(-7.31821709273351,-2.8520683494292,-59.7339199149344));
#78198=CARTESIAN_POINT('Ctrl Pts',(-4.33020733389426,-7.10306190021205,
-59.5222348470259));
#78199=CARTESIAN_POINT('Ctrl Pts',(2.60737502964694,-8.53510294343834,-59.2576285121399));
#78200=CARTESIAN_POINT('Ctrl Pts',(8.59504447333725,-2.41059574693977,-58.9401009102769));
#78201=CARTESIAN_POINT('Ctrl Pts',(6.99784544930374,4.49381352486545,-58.675494575391));
#78202=CARTESIAN_POINT('Ctrl Pts',(2.68667853170036,7.38179190922916,-58.4638095074824));
#78203=CARTESIAN_POINT('Ctrl Pts',(-1.17242277308143,7.78519454912189,-58.3050457065508));
#78204=CARTESIAN_POINT('Ctrl Pts',(-4.73412089022752,6.26887006262792,-58.1462819056193));
#78205=CARTESIAN_POINT('Ctrl Pts',(-8.01750998147662,2.22925445242337,-57.9345968377106));
#78206=CARTESIAN_POINT('Ctrl Pts',(-7.59622194194939,-3.40276613558523,
-57.7229117698019));
#78207=CARTESIAN_POINT('Ctrl Pts',(-3.74810167430262,-6.89506033654368,
-57.5112267018932));
#78208=CARTESIAN_POINT('Ctrl Pts',(1.25002051470277,-8.22235674886337,-57.2995416339846));
#78209=CARTESIAN_POINT('Ctrl Pts',(7.49722266516787,-4.85146930384844,-57.0349352990986));
#78210=CARTESIAN_POINT('Ctrl Pts',(8.12456649763937,3.69034896651629,-56.7174076972357));
#78211=CARTESIAN_POINT('Ctrl Pts',(2.46211435707413,7.94416432374526,-56.4528013623498));
#78212=CARTESIAN_POINT('Ctrl Pts',(-2.69854954494453,7.37779497692955,-56.2411162944411));
#78213=CARTESIAN_POINT('Ctrl Pts',(-5.90960739324672,5.20142821114934,-56.0823524935096));
#78214=CARTESIAN_POINT('Ctrl Pts',(-7.6589098948458,1.74787750182028,-55.9235886925781));
#78215=CARTESIAN_POINT('Ctrl Pts',(-7.56942412666791,-3.45705962324571,
-55.7119036246693));
#78216=CARTESIAN_POINT('Ctrl Pts',(-3.62078797743637,-7.49478945458689,
-55.5002185567607));
#78217=CARTESIAN_POINT('Ctrl Pts',(1.57225890926194,-7.68883942439684,-55.288533488852));
#78218=CARTESIAN_POINT('Ctrl Pts',(6.25089939315454,-5.48594870743951,-55.0768484209433));
#78219=CARTESIAN_POINT('Ctrl Pts',(8.86004379236408,1.11579116834456,-54.8122420860574));
#78220=CARTESIAN_POINT('Ctrl Pts',(3.83974534657913,8.05503270661092,-54.4947144841945));
#78221=CARTESIAN_POINT('Ctrl Pts',(-3.23166004154058,7.6634259872617,-54.2301081493085));
#78222=CARTESIAN_POINT('Ctrl Pts',(-6.81535455965847,3.90704458018533,-54.0184230813999));
#78223=CARTESIAN_POINT('Ctrl Pts',(-7.87070091762291,0.174256944970944,
-53.8596592804683));
#78224=CARTESIAN_POINT('Ctrl Pts',(-6.98526896633185,-3.59444027794282,
-53.7008954795368));
#78225=CARTESIAN_POINT('Ctrl Pts',(-3.56523800911463,-7.51907694657359,
-53.4892104116282));
#78226=CARTESIAN_POINT('Ctrl Pts',(2.05580984747745,-8.06570638289985,-53.2775253437196));
#78227=CARTESIAN_POINT('Ctrl Pts',(6.1539240684084,-4.8702637839017,-53.0658402758107));
#78228=CARTESIAN_POINT('Ctrl Pts',(8.31503040792571,-0.172176605010883,
-52.8541552079022));
#78229=CARTESIAN_POINT('Ctrl Pts',(6.06027237653944,6.55884632086358,-52.5895488730162));
#78230=CARTESIAN_POINT('Ctrl Pts',(-2.24903948266158,8.63533541566494,-52.2720212711532));
#78231=CARTESIAN_POINT('Ctrl Pts',(-7.40715510596884,3.78229792270048,-52.0074149362673));
#78232=CARTESIAN_POINT('Ctrl Pts',(-7.73020231934559,-1.39929528552856,
-51.7957298683586));
#78233=CARTESIAN_POINT('Ctrl Pts',(-6.13402181550093,-4.93478213859474,
-51.6369660674271));
#78234=CARTESIAN_POINT('Ctrl Pts',(-3.02984348382236,-7.24803641779415,
-51.4782022664956));
#78235=CARTESIAN_POINT('Ctrl Pts',(2.11395012478913,-8.04851881185056,-51.2665171985869));
#78236=CARTESIAN_POINT('Ctrl Pts',(6.76655750420719,-4.84723355326002,-51.0548321306782));
#78237=CARTESIAN_POINT('Ctrl Pts',(7.84438329612395,0.236434918886423,-50.8431470627695));
#78238=CARTESIAN_POINT('Ctrl Pts',(6.47263540369198,5.22248661053359,-50.6314619948608));
#78239=CARTESIAN_POINT('Ctrl Pts',(0.413294031195558,8.92045707250124,-50.366855659975));
#78240=CARTESIAN_POINT('Ctrl Pts',(-7.28119179881932,5.15862794986372,-50.0493280581119));
#78241=CARTESIAN_POINT('Ctrl Pts',(-8.10265755592695,-1.87581045709897,
-49.7847217232261));
#78242=CARTESIAN_POINT('Ctrl Pts',(-5.01328502561204,-6.04822523110639,
-49.5730366553175));
#78243=CARTESIAN_POINT('Ctrl Pts',(-1.51548721827395,-7.72538651975872,
-49.4142728543859));
#78244=CARTESIAN_POINT('Ctrl Pts',(2.34904793451002,-7.49639628431493,-49.2555090534543));
#78245=CARTESIAN_POINT('Ctrl Pts',(6.7999727671332,-4.7966457614761,-49.0438239855458));
#78246=CARTESIAN_POINT('Ctrl Pts',(8.29827490589769,0.648542337648683,-48.8321389176368));
#78247=CARTESIAN_POINT('Ctrl Pts',(5.84943353727355,5.23205294892948,-48.6204538497284));
#78248=CARTESIAN_POINT('Ctrl Pts',(1.58929915763245,8.16354724699242,-48.4087687818195));
#78249=CARTESIAN_POINT('Ctrl Pts',(-5.42785605201213,7.09110322990665,-48.1441624469338));
#78250=CARTESIAN_POINT('Ctrl Pts',(-8.89253094527492,-0.741680337907531,
-47.8266348450706));
#78251=CARTESIAN_POINT('Ctrl Pts',(-4.99140989651476,-6.65263493546399,
-47.5620285101848));
#78252=CARTESIAN_POINT('Ctrl Pts',(0.0589488032179521,-7.85560820260387,
-47.3503434422762));
#78253=CARTESIAN_POINT('Ctrl Pts',(3.81504601570707,-6.88648838570566,-47.1915796413446));
#78254=CARTESIAN_POINT('Ctrl Pts',(6.62432138306982,-4.22283668449543,-47.0328158404131));
#78255=CARTESIAN_POINT('Ctrl Pts',(8.29126616213413,0.708763446778455,-46.8211307725044));
#78256=CARTESIAN_POINT('Ctrl Pts',(5.93133823172453,5.83962330621226,-46.6094457045957));
#78257=CARTESIAN_POINT('Ctrl Pts',(1.106332125194,7.76957399064748,-46.3977606366871));
#78258=CARTESIAN_POINT('Ctrl Pts',(-4.04071368192798,7.26925088348232,-46.1860755687783));
#78259=CARTESIAN_POINT('Ctrl Pts',(-8.71891791081765,1.93024267981529,-45.9214692338925));
#78260=CARTESIAN_POINT('Ctrl Pts',(-6.3260256110773,-6.29353607317102,-45.6039416320294));
#78261=CARTESIAN_POINT('Ctrl Pts',(0.464877034074995,-8.30395169077777,
-45.3393352971436));
#78262=CARTESIAN_POINT('Ctrl Pts',(5.10348759970218,-5.97230855816275,-45.1276502292349));
#78263=CARTESIAN_POINT('Ctrl Pts',(7.35321338239484,-2.8122146684403,-44.9688864283033));
#78264=CARTESIAN_POINT('Ctrl Pts',(7.78738924037035,1.03467495817789,-44.8101226273719));
#78265=CARTESIAN_POINT('Ctrl Pts',(5.8871982942649,5.8811849519331,-44.5984375594632));
#78266=CARTESIAN_POINT('Ctrl Pts',(0.777769849796183,8.28716161531329,-44.3867524915545));
#78267=CARTESIAN_POINT('Ctrl Pts',(-4.15654072107625,6.65683258024544,-44.1750674236458));
#78268=CARTESIAN_POINT('Ctrl Pts',(-7.77233859820406,2.95975137151687,-43.9633823557371));
#78269=CARTESIAN_POINT('Ctrl Pts',(-7.91370129781951,-4.13747484674488,
-43.6987760208512));
#78270=CARTESIAN_POINT('Ctrl Pts',(-0.78745851557057,-8.88859411957631,
-43.3812484189883));
#78271=CARTESIAN_POINT('Ctrl Pts',(5.70275775804652,-6.05394733150377,-43.1166420841023));
#78272=CARTESIAN_POINT('Ctrl Pts',(7.75033133819768,-1.28312873179931,-42.9049570161937));
#78273=CARTESIAN_POINT('Ctrl Pts',(7.43673075868515,2.58327970054494,-42.7461932152622));
#78274=CARTESIAN_POINT('Ctrl Pts',(5.29182477389289,5.8060807790221,-42.5874294143306));
#78275=CARTESIAN_POINT('Ctrl Pts',(0.717236323629105,8.29053751278568,-42.375744346422));
#78276=CARTESIAN_POINT('Ctrl Pts',(-4.74120647888952,6.84126703923405,-42.1640592785132));
#78277=CARTESIAN_POINT('Ctrl Pts',(-7.46660836295353,2.41661133028347,-41.9523742106046));
#78278=CARTESIAN_POINT('Ctrl Pts',(-7.85240220824392,-2.74028374923017,
-41.7406891426959));
#78279=CARTESIAN_POINT('Ctrl Pts',(-3.39050906099741,-8.26134460277815,
-41.47608280781));
#78280=CARTESIAN_POINT('Ctrl Pts',(5.12106840726382,-7.30765726511821,-41.1585552059471));
#78281=CARTESIAN_POINT('Ctrl Pts',(8.26139731090733,-0.959707669509055,
-40.8939488710611));
#78282=CARTESIAN_POINT('Ctrl Pts',(6.75595311145198,4.00888422757258,-40.6822638031524));
#78283=CARTESIAN_POINT('Ctrl Pts',(4.02636042792342,6.76511050115767,-40.5235000022209));
#78284=CARTESIAN_POINT('Ctrl Pts',(0.310081618777929,7.84970272302158,-40.3647362012893));
#78285=CARTESIAN_POINT('Ctrl Pts',(-4.78969403479622,6.80487114116623,-40.1530511333807));
#78286=CARTESIAN_POINT('Ctrl Pts',(-8.0326928565855,2.18124254711268,-39.9413660654719));
#78287=CARTESIAN_POINT('Ctrl Pts',(-7.26875135094599,-2.95897018665329,
-39.7296809975633));
#78288=CARTESIAN_POINT('Ctrl Pts',(-4.24328942660509,-7.15289244350772,
-39.5179959296546));
#78289=CARTESIAN_POINT('Ctrl Pts',(2.72559521113433,-8.5039106935338,-39.2533895947687));
#78290=CARTESIAN_POINT('Ctrl Pts',(8.62364054489699,-2.29347336778082,-38.9358619929058));
#78291=CARTESIAN_POINT('Ctrl Pts',(6.93870843542055,4.58541705712851,-38.6712556580198));
#78292=CARTESIAN_POINT('Ctrl Pts',(2.58752673216899,7.41746321895357,-38.4595705901112));
#78293=CARTESIAN_POINT('Ctrl Pts',(-1.27565445200444,7.76859087013229,-38.3008067891796));
#78294=CARTESIAN_POINT('Ctrl Pts',(-4.81734253396703,6.20541653400868,-38.1420429882481));
#78295=CARTESIAN_POINT('Ctrl Pts',(-8.04635426085578,2.12217419257887,-37.9303579203395));
#78296=CARTESIAN_POINT('Ctrl Pts',(-7.55029959054519,-3.50356242567293,
-37.7186728524307));
#78297=CARTESIAN_POINT('Ctrl Pts',(-3.6559258783647,-6.9443831071799,-37.5069877845221));
#78298=CARTESIAN_POINT('Ctrl Pts',(1.35938440304736,-8.20496493052104,-37.2953027166133));
#78299=CARTESIAN_POINT('Ctrl Pts',(7.56117395241235,-4.75121192959417,-37.0306963817275));
#78300=CARTESIAN_POINT('Ctrl Pts',(8.07469694698156,3.79821873392218,-36.7131687798645));
#78301=CARTESIAN_POINT('Ctrl Pts',(2.35611021374405,7.97624404091755,-36.4485624449786));
#78302=CARTESIAN_POINT('Ctrl Pts',(-2.79655853467506,7.34120668257979,-36.23687737707));
#78303=CARTESIAN_POINT('Ctrl Pts',(-5.97834772773149,5.12227067175771,-36.0781135761384));
#78304=CARTESIAN_POINT('Ctrl Pts',(-7.68150687453854,1.64573253797016,-35.9193497752069));
#78305=CARTESIAN_POINT('Ctrl Pts',(-7.52271651044792,-3.55755203732478,
-35.7076647072982));
#78306=CARTESIAN_POINT('Ctrl Pts',(-3.52066227601521,-7.54234119592964,
-35.4959796393895));
#78307=CARTESIAN_POINT('Ctrl Pts',(1.67450843320736,-7.66722063556932,-35.2842945714808));
#78308=CARTESIAN_POINT('Ctrl Pts',(6.32339904103569,-5.40222176832433,-35.0726095035722));
#78309=CARTESIAN_POINT('Ctrl Pts',(8.84439970681327,1.23367749621947,-34.8080031686863));
#78310=CARTESIAN_POINT('Ctrl Pts',(3.73213955334257,8.10545067782704,-34.4904755668233));
#78311=CARTESIAN_POINT('Ctrl Pts',(-3.33342394246881,7.61971188164993,-34.2258692319374));
#78312=CARTESIAN_POINT('Ctrl Pts',(-6.86677863638025,3.8159410835559,-34.0141841640287));
#78313=CARTESIAN_POINT('Ctrl Pts',(-7.87232352904819,0.0694308462814094,
-33.8554203630972));
#78314=CARTESIAN_POINT('Ctrl Pts',(-6.93678401568545,-3.68714130049925,
-33.6966565621657));
#78315=CARTESIAN_POINT('Ctrl Pts',(-3.46479365649576,-7.56588693496979,
-33.484971494257));
#78316=CARTESIAN_POINT('Ctrl Pts',(2.16303500733719,-8.03761489091188,-33.2732864263483));
#78317=CARTESIAN_POINT('Ctrl Pts',(6.21823355495086,-4.78788285398311,-33.0616013584396));
#78318=CARTESIAN_POINT('Ctrl Pts',(8.31658591973511,-0.0614337528735027,
-32.8499162905309));
#78319=CARTESIAN_POINT('Ctrl Pts',(5.97239375865441,6.63896672157217,-32.585309955645));
#78320=CARTESIAN_POINT('Ctrl Pts',(-2.36383300746484,8.60462026176232,-32.267782353782));
#78321=CARTESIAN_POINT('Ctrl Pts',(-7.45686550868394,3.68332473792107,-32.0031760188961));
#78322=CARTESIAN_POINT('Ctrl Pts',(-7.71088309087349,-1.50211089906813,
-31.7914909509875));
#78323=CARTESIAN_POINT('Ctrl Pts',(-6.0677636032303,-5.01602863266695,-31.6327271500559));
#78324=CARTESIAN_POINT('Ctrl Pts',(-2.93305593191232,-7.28774082623624,
-31.4739633491245));
#78325=CARTESIAN_POINT('Ctrl Pts',(2.22094125045637,-8.01965461580867,-31.2622782812157));
#78326=CARTESIAN_POINT('Ctrl Pts',(6.83050598543679,-4.75669649657056,-31.0505932133071));
#78327=CARTESIAN_POINT('Ctrl Pts',(7.84053924089609,0.340874140044041,-30.8389081453983));
#78328=CARTESIAN_POINT('Ctrl Pts',(6.40251593349158,5.30821676156078,-30.6272230774897));
#78329=CARTESIAN_POINT('Ctrl Pts',(0.294467600103715,8.92516975586717,-30.3626167426038));
#78330=CARTESIAN_POINT('Ctrl Pts',(-7.34924134935658,5.06121012458663,-30.0450891407408));
#78331=CARTESIAN_POINT('Ctrl Pts',(-8.07695976015268,-1.98354364016924,
-29.7804828058548));
#78332=CARTESIAN_POINT('Ctrl Pts',(-4.93229895868432,-6.11444864042372,
-29.5687977379463));
#78333=CARTESIAN_POINT('Ctrl Pts',(-1.4124772829056,-7.74488258876122,-29.4100339370147));
#78334=CARTESIAN_POINT('Ctrl Pts',(2.44866584252073,-7.46445035094941,-29.2512701360832));
#78335=CARTESIAN_POINT('Ctrl Pts',(6.86324463018906,-4.70566821408192,-29.0395850681745));
#78336=CARTESIAN_POINT('Ctrl Pts',(8.28890275205008,0.758989291512339,-28.8279000002658));
#78337=CARTESIAN_POINT('Ctrl Pts',(5.7792419352401,5.30948334787337,-28.6162149323571));
#78338=CARTESIAN_POINT('Ctrl Pts',(1.48044788464432,8.18398738557075,-28.4045298644485));
#78339=CARTESIAN_POINT('Ctrl Pts',(-5.52180385579767,7.01819410651025,-28.1399235295625));
#78340=CARTESIAN_POINT('Ctrl Pts',(-8.8818658215771,-0.860032478346779,
-27.8223959276996));
#78341=CARTESIAN_POINT('Ctrl Pts',(-4.90237711231396,-6.7185134507748,-27.5577895928137));
#78342=CARTESIAN_POINT('Ctrl Pts',(0.163553239062703,-7.85412665623684,
-27.346104524905));
#78343=CARTESIAN_POINT('Ctrl Pts',(3.90641206075979,-6.83507448386419,-27.1873407239735));
#78344=CARTESIAN_POINT('Ctrl Pts',(6.67996765911546,-4.13424908820067,-27.0285769230419));
#78345=CARTESIAN_POINT('Ctrl Pts',(8.28109269185019,0.819111728535833,-26.8168918551333));
#78346=CARTESIAN_POINT('Ctrl Pts',(5.85304862131644,5.91809052094336,-26.6052067872245));
#78347=CARTESIAN_POINT('Ctrl Pts',(1.00277004429556,7.78361760402229,-26.3935217193159));
#78348=CARTESIAN_POINT('Ctrl Pts',(-4.13715679621693,7.21479792578039,-26.1818366514072));
#78349=CARTESIAN_POINT('Ctrl Pts',(-8.74384899928446,1.81396554991253,-25.9172303165214));
#78350=CARTESIAN_POINT('Ctrl Pts',(-6.24165644830004,-6.37721891718524,
-25.5997027146583));
#78351=CARTESIAN_POINT('Ctrl Pts',(0.57541586864642,-8.2970248232539,-25.3350963797725));
#78352=CARTESIAN_POINT('Ctrl Pts',(5.18256567079529,-5.90381810882687,-25.1234113118638));
#78353=CARTESIAN_POINT('Ctrl Pts',(7.39001039811455,-2.71404581836418,-24.9646475109322));
#78354=CARTESIAN_POINT('Ctrl Pts',(7.77292042892884,1.13828443530474,-24.8058837100007));
#78355=CARTESIAN_POINT('Ctrl Pts',(5.80835913964507,5.9590606893823,-24.5941986420921));
#78356=CARTESIAN_POINT('Ctrl Pts',(0.667344416622147,8.29678401594118,-24.3825135741833));
#78357=CARTESIAN_POINT('Ctrl Pts',(-4.24481826116653,6.60089150774721,-24.1708285062747));
#78358=CARTESIAN_POINT('Ctrl Pts',(-7.81106313146197,2.85598813419176,-23.959143438366));
#78359=CARTESIAN_POINT('Ctrl Pts',(-7.8579026714865,-4.24249124265474,-23.6945371034801));
#78360=CARTESIAN_POINT('Ctrl Pts',(-0.66902321244215,-8.89829221129115,
-23.377009501617));
#78361=CARTESIAN_POINT('Ctrl Pts',(5.7828698397457,-5.97746942745352,-23.1124031667312));
#78362=CARTESIAN_POINT('Ctrl Pts',(7.766730980083,-1.17980722036984,-22.9007180988225));
#78363=CARTESIAN_POINT('Ctrl Pts',(7.40167095490554,2.68208229995444,-22.741954297891));
#78364=CARTESIAN_POINT('Ctrl Pts',(5.21403853970046,5.87603484984857,-22.5831904969595));
#78365=CARTESIAN_POINT('Ctrl Pts',(0.606771302585118,8.29935351585887,-22.3715054290508));
#78366=CARTESIAN_POINT('Ctrl Pts',(-4.83188820926486,6.77752387754858,-22.1598203611421));
#78367=CARTESIAN_POINT('Ctrl Pts',(-7.49812724919615,2.31696752723136,-21.9481352932334));
#78368=CARTESIAN_POINT('Ctrl Pts',(-7.81521479364046,-2.84460774019756,
-21.7364502253247));
#78369=CARTESIAN_POINT('Ctrl Pts',(-3.28019575183774,-8.30576198600601,
-21.4718438904388));
#78370=CARTESIAN_POINT('Ctrl Pts',(5.21792716807712,-7.23881429551514,-21.1543162885758));
#78371=CARTESIAN_POINT('Ctrl Pts',(8.27344478157893,-0.849609195893172,
-20.88970995369));
#78372=CARTESIAN_POINT('Ctrl Pts',(6.70196952627641,4.09849480456911,-20.6780248857812));
#78373=CARTESIAN_POINT('Ctrl Pts',(3.93591542657239,6.81812790605245,-20.5192610848498));
#78374=CARTESIAN_POINT('Ctrl Pts',(0.205523101929143,7.8531359153328,-20.3604972839182));
#78375=CARTESIAN_POINT('Ctrl Pts',(-4.87988679772441,6.74048551932531,-20.1488122160095));
#78376=CARTESIAN_POINT('Ctrl Pts',(-8.06102724644903,2.07408131701245,-19.9371271481009));
#78377=CARTESIAN_POINT('Ctrl Pts',(-7.22870353760725,-3.05550256631652,
-19.7254420801922));
#78378=CARTESIAN_POINT('Ctrl Pts',(-4.14766126956044,-7.20876421166052,
-19.5137570122835));
#78379=CARTESIAN_POINT('Ctrl Pts',(2.83859635510066,-8.46686111090562,-19.2491506773976));
#78380=CARTESIAN_POINT('Ctrl Pts',(8.65341706408883,-2.17843279704631,-18.9316230755346));
#78381=CARTESIAN_POINT('Ctrl Pts',(6.87703121255687,4.67741018525212,-18.6670167406487));
#78382=CARTESIAN_POINT('Ctrl Pts',(2.48852221833318,7.45126246773523,-18.45533167274));
#78383=CARTESIAN_POINT('Ctrl Pts',(-1.37899223206182,7.75091470810606,-18.2965678718085));
#78384=CARTESIAN_POINT('Ctrl Pts',(-4.89955017323679,6.14071588253778,-18.137804070877));
#78385=CARTESIAN_POINT('Ctrl Pts',(-8.07390085219916,2.01483627714438,-17.9261190029683));
#78386=CARTESIAN_POINT('Ctrl Pts',(-7.5029747183492,-3.6037957702104,-17.7144339350596));
#78387=CARTESIAN_POINT('Ctrl Pts',(-3.56312642911424,-6.99245170291008,
-17.5027488671509));
#78388=CARTESIAN_POINT('Ctrl Pts',(1.46852575934409,-8.18613508076134,-17.2910637992423));
#78389=CARTESIAN_POINT('Ctrl Pts',(7.62377329803872,-4.6501018309999,-17.0264574643564));
#78390=CARTESIAN_POINT('Ctrl Pts',(8.02340176900499,3.90540911934195,-16.7089298624934));
#78391=CARTESIAN_POINT('Ctrl Pts',(2.24968518218346,8.00691207149459,-16.4443235276075));
#78392=CARTESIAN_POINT('Ctrl Pts',(-2.89407017089541,7.30331520887269,-16.2326384596988));
#78393=CARTESIAN_POINT('Ctrl Pts',(-6.04602864672309,5.04220546898135,-16.0738746587673));
#78394=CARTESIAN_POINT('Ctrl Pts',(-7.70274125368099,1.54329537968519,-15.9151108578358));
#78395=CARTESIAN_POINT('Ctrl Pts',(-7.47467512822539,-3.65741328295393,
-15.703425789927));
#78396=CARTESIAN_POINT('Ctrl Pts',(-3.419912076881,-7.58855552552508,-15.4917407220184));
#78397=CARTESIAN_POINT('Ctrl Pts',(1.77646094455016,-7.64424209976831,-15.2800556541097));
#78398=CARTESIAN_POINT('Ctrl Pts',(6.39477734960587,-5.31753684663269,-15.068370586201));
#78399=CARTESIAN_POINT('Ctrl Pts',(8.82718714214999,1.35134506918803,-14.8037642513151));
#78400=CARTESIAN_POINT('Ctrl Pts',(3.62387192255354,8.154431226348,-14.4862366494521));
#78401=CARTESIAN_POINT('Ctrl Pts',(-3.4345967058702,7.57464651370659,-14.2216303145662));
#78402=CARTESIAN_POINT('Ctrl Pts',(-6.91698496501562,3.72416087031233,-14.0099452466575));
#78403=CARTESIAN_POINT('Ctrl Pts',(-7.87255007560244,-0.0354075635112222,
-13.851181445726));
#78404=CARTESIAN_POINT('Ctrl Pts',(-6.88706890473335,-3.7791884514498,-13.6924176447945));
#78405=CARTESIAN_POINT('Ctrl Pts',(-3.36373486299103,-7.61135519906527,
-13.4807325768858));
#78406=CARTESIAN_POINT('Ctrl Pts',(2.26987657798482,-8.00809802002258,-13.2690475089771));
#78407=CARTESIAN_POINT('Ctrl Pts',(6.2814403086435,-4.70465284758939,-13.0573624410685));
#78408=CARTESIAN_POINT('Ctrl Pts',(8.31666658009959,0.0493199937455939,
-12.8456773731598));
#78409=CARTESIAN_POINT('Ctrl Pts',(5.88345600487443,6.71790977739831,-12.5810710382739));
#78410=CARTESIAN_POINT('Ctrl Pts',(-2.47820733344243,8.57237917668041,-12.2635434364109));
#78411=CARTESIAN_POINT('Ctrl Pts',(-7.50525352146753,3.5836983575743,-11.998937101525));
#78412=CARTESIAN_POINT('Ctrl Pts',(-7.69019642532775,-1.60466013039959,
-11.7872520336163));
#78413=CARTESIAN_POINT('Ctrl Pts',(-6.00042934237632,-5.09638559133537,
-11.6284882326848));
#78414=CARTESIAN_POINT('Ctrl Pts',(-2.83574823602284,-7.32615283706326,
-11.4697244317533));
#78415=CARTESIAN_POINT('Ctrl Pts',(2.3275385175523,-7.98936822559517,-11.2580393638446));
#78416=CARTESIAN_POINT('Ctrl Pts',(6.89324315442797,-4.66531589407465,-11.0463542959359));
#78417=CARTESIAN_POINT('Ctrl Pts',(7.83530475556439,0.445252911065612,-10.8346692280272));
#78418=CARTESIAN_POINT('Ctrl Pts',(6.33126105020073,5.39300556095946,-10.6229841601185));
#78419=CARTESIAN_POINT('Ctrl Pts',(0.175588948545246,8.92829966229325,-10.3583778252327));
#78420=CARTESIAN_POINT('Ctrl Pts',(-7.41598759586123,4.96289475148757,-10.0408502233696));
#78421=CARTESIAN_POINT('Ctrl Pts',(-8.04982960779548,-2.09092506442495,
-9.7762438884838));
#78422=CARTESIAN_POINT('Ctrl Pts',(-4.85043820485799,-6.17958772209538,
-9.56455882057513));
#78423=CARTESIAN_POINT('Ctrl Pts',(-1.30921686082002,-7.76300519127524,
-9.40579501964359));
#78424=CARTESIAN_POINT('Ctrl Pts',(2.54784950760582,-7.43118068255035,-9.24703121871208));
#78425=CARTESIAN_POINT('Ctrl Pts',(6.92529937518107,-4.61385617016351,-9.03534615080339));
#78426=CARTESIAN_POINT('Ctrl Pts',(8.27806065595005,0.86930164729228,-8.8236610828947));
#78427=CARTESIAN_POINT('Ctrl Pts',(5.7080254506422,5.38597217057458,-8.61197601498602));
#78428=CARTESIAN_POINT('Ctrl Pts',(1.37133407112876,8.20297618743883,-8.40029094707731));
#78429=CARTESIAN_POINT('Ctrl Pts',(-5.6147724307227,6.94404038652962,-8.13568461219148));
#78430=CARTESIAN_POINT('Ctrl Pts',(-8.86962560039774,-0.978232101847115,
-7.81815701032842));
#78431=CARTESIAN_POINT('Ctrl Pts',(-4.81247494751196,-6.78320051444302,
-7.55355067544256));
#78432=CARTESIAN_POINT('Ctrl Pts',(0.268128670607651,-7.85125227019408,
-7.34186560753389));
#78433=CARTESIAN_POINT('Ctrl Pts',(3.99708534824191,-6.78244845961086,-7.18310180660235));
#78434=CARTESIAN_POINT('Ctrl Pts',(6.73442931917313,-4.04492833004187,-7.02433800567085));
#78435=CARTESIAN_POINT('Ctrl Pts',(8.26945066434343,0.929314750188685,-6.81265293776215));
#78436=CARTESIAN_POINT('Ctrl Pts',(5.77372103956225,5.99550822988587,-6.60096786985345));
#78437=CARTESIAN_POINT('Ctrl Pts',(0.899030133590318,7.79628088171154,-6.38928280194479));
#78438=CARTESIAN_POINT('Ctrl Pts',(-4.23286623301421,7.15906550601515,-6.17759773403607));
#78439=CARTESIAN_POINT('Ctrl Pts',(-8.76722946592603,1.69736673401073,-5.91299139915023));
#78440=CARTESIAN_POINT('Ctrl Pts',(-6.15618039911467,-6.45977083438301,
-5.59546379728718));
#78441=CARTESIAN_POINT('Ctrl Pts',(0.685852659936336,-8.28862657288868,
-5.33085746240133));
#78442=CARTESIAN_POINT('Ctrl Pts',(5.26072467283561,-5.8342806850866,-5.11917239449263));
#78443=CARTESIAN_POINT('Ctrl Pts',(7.42549688033595,-2.61539566255192,-4.96040859356112));
#78444=CARTESIAN_POINT('Ctrl Pts',(7.75707317795147,1.24169204937703,-4.80164479262961));
#78445=CARTESIAN_POINT('Ctrl Pts',(5.72848994081137,6.03587965844944,-4.58995972472091));
#78446=CARTESIAN_POINT('Ctrl Pts',(0.556800633788882,8.30493507094121,-4.37827465681223));
#78447=CARTESIAN_POINT('Ctrl Pts',(-4.33234302682892,6.54377984920668,-4.16658958890353));
#78448=CARTESIAN_POINT('Ctrl Pts',(-7.8484024721132,2.75171840433465,-3.95490452099485));
#78449=CARTESIAN_POINT('Ctrl Pts',(-7.80071051403226,-4.34675524787344,
-3.69029818610897));
#78450=CARTESIAN_POINT('Ctrl Pts',(-0.550469304142969,-8.90641235122975,
-3.37277058424596));
#78451=CARTESIAN_POINT('Ctrl Pts',(5.86195646064047,-5.89993138798228,-3.10816424936009));
#78452=CARTESIAN_POINT('Ctrl Pts',(7.78175319073645,-1.07627662134248,-2.8964791814514));
#78453=CARTESIAN_POINT('Ctrl Pts',(7.3652987460188,2.78040956315781,-2.73771538051989));
#78454=CARTESIAN_POINT('Ctrl Pts',(5.13532728862757,5.94494631292473,-2.57895157958836));
#78455=CARTESIAN_POINT('Ctrl Pts',(0.496199514237444,8.30669900125524,-2.36726651167968));
#78456=CARTESIAN_POINT('Ctrl Pts',(-4.92171466373837,6.71257634901686,-2.15558144377098));
#78457=CARTESIAN_POINT('Ctrl Pts',(-7.52831455255968,2.21691570125815,-1.9438963758623));
#78458=CARTESIAN_POINT('Ctrl Pts',(-7.77664582632939,-2.94843397217774,
-1.73221130795361));
#78459=CARTESIAN_POINT('Ctrl Pts',(-3.16929139916222,-8.34869217407772,
-1.46760497306774));
#78460=CARTESIAN_POINT('Ctrl Pts',(5.31384412439784,-7.16871275278065,-1.15007737120471));
#78461=CARTESIAN_POINT('Ctrl Pts',(8.28405293463262,-0.739317465192835,
-0.885471036318848));
#78462=CARTESIAN_POINT('Ctrl Pts',(6.64675881376857,4.18731958863545,-0.673785968410167));
#78463=CARTESIAN_POINT('Ctrl Pts',(3.84485665727322,6.8700648328613,-0.515022167478636));
#78464=CARTESIAN_POINT('Ctrl Pts',(0.100771147807785,7.85493665872597,-0.356258366547131));
#78465=CARTESIAN_POINT('Ctrl Pts',(-4.96885597231511,6.67545165970414,-0.144573298638437));
#78466=CARTESIAN_POINT('Ctrl Pts',(-8.08861889150961,1.96550321891304,0.0671117692702526));
#78467=CARTESIAN_POINT('Ctrl Pts',(-7.18657111473999,-3.15026676281351,
0.278796837178939));
#78468=CARTESIAN_POINT('Ctrl Pts',(-4.05317016702944,-7.26622277449979,
0.490481905087635));
#78469=CARTESIAN_POINT('Ctrl Pts',(2.9550269927459,-8.42224224643628,0.755088239973491));
#78470=CARTESIAN_POINT('Ctrl Pts',(8.67501344887474,-2.07353332355263,1.07261584183653));
#78471=CARTESIAN_POINT('Ctrl Pts',(6.45326796117271,6.15716910628112,1.39014344369957));
#78472=CARTESIAN_POINT('Ctrl Pts',(-1.68444987226829,8.76521406545941,1.70767104556259));
#78473=CARTESIAN_POINT('Ctrl Pts',(-7.15900251768137,4.23967743624303,1.97227738044847));
#78474=CARTESIAN_POINT('Ctrl Pts',(-7.79563090895679,-0.893937243558322,
2.18396244835714));
#78475=CARTESIAN_POINT('Ctrl Pts',(-6.00088516313695,-5.76873779387534,
2.39564751626584));
#78476=CARTESIAN_POINT('Ctrl Pts',(-0.934827019873464,-8.26905574884899,
2.60733258417452));
#78477=CARTESIAN_POINT('Ctrl Pts',(4.03970536080434,-6.73728174672223,2.81901765208321));
#78478=CARTESIAN_POINT('Ctrl Pts',(6.77963693050073,-4.00215399669808,2.97778145301474));
#78479=CARTESIAN_POINT('Ctrl Pts',(7.85098939493397,-0.273886082915279,
3.13654525394624));
#78480=CARTESIAN_POINT('Ctrl Pts',(6.78679261263705,4.80744936231159,3.34823032185494));
#78481=CARTESIAN_POINT('Ctrl Pts',(0.984744855677549,8.86891534966339,3.6128366567408));
#78482=CARTESIAN_POINT('Ctrl Pts',(-6.93988327278603,5.61988337516134,3.93036425860384));
#78483=CARTESIAN_POINT('Ctrl Pts',(-8.20399225474943,-1.36528175863787,
4.19497059348969));
#78484=CARTESIAN_POINT('Ctrl Pts',(-5.39017638200938,-5.7040541546864,4.40665566139839));
#78485=CARTESIAN_POINT('Ctrl Pts',(-0.875407750237295,-8.27741612723811,
4.61834072930707));
#78486=CARTESIAN_POINT('Ctrl Pts',(4.60875000304047,-6.92870014251292,4.83002579721577));
#78487=CARTESIAN_POINT('Ctrl Pts',(7.42929944027226,-2.55332779949047,5.04171086512445));
#78488=CARTESIAN_POINT('Ctrl Pts',(7.76396873616646,1.30349239385412,5.20047466605597));
#78489=CARTESIAN_POINT('Ctrl Pts',(6.18316230225275,4.84588052176129,5.35923846698748));
#78490=CARTESIAN_POINT('Ctrl Pts',(2.09686003902976,8.04828565012845,5.57092353489619));
#78491=CARTESIAN_POINT('Ctrl Pts',(-4.95742538367269,7.41964493694006,5.83552986978204));
#78492=CARTESIAN_POINT('Ctrl Pts',(-8.92842666789117,-0.169005753564876,
6.15305747164507));
#78493=CARTESIAN_POINT('Ctrl Pts',(-5.39767238427704,-6.32728285862421,
6.41766380653094));
#78494=CARTESIAN_POINT('Ctrl Pts',(-0.451030042432455,-7.83497432783414,
6.62934887443963));
#78495=CARTESIAN_POINT('Ctrl Pts',(4.66023197702472,-6.89668118725614,6.84103394234832));
#78496=CARTESIAN_POINT('Ctrl Pts',(7.98764987690763,-2.33342874268697,7.05271901025701));
#78497=CARTESIAN_POINT('Ctrl Pts',(7.32824174607405,2.83034562283092,7.26440407816568));
#78498=CARTESIAN_POINT('Ctrl Pts',(5.10080854487034,5.9966699575808,7.42316787909722));
#78499=CARTESIAN_POINT('Ctrl Pts',(1.6103299596797,7.68901115987702,7.58193168002873));
#78500=CARTESIAN_POINT('Ctrl Pts',(-3.57816348256826,7.50789387431347,7.79361674793741));
#78501=CARTESIAN_POINT('Ctrl Pts',(-8.57054957278509,2.48452739160254,8.05822308282328));
#78502=CARTESIAN_POINT('Ctrl Pts',(-6.72224604055467,-5.87850104262768,
8.37575068468631));
#78503=CARTESIAN_POINT('Ctrl Pts',(-0.0554521657819921,-8.31662795388359,
8.64035701957219));
#78504=CARTESIAN_POINT('Ctrl Pts',(4.70002003081336,-6.28490751543709,8.85204208748085));
#78505=CARTESIAN_POINT('Ctrl Pts',(8.00642217931619,-2.27578062735984,9.06372715538958));
#78506=CARTESIAN_POINT('Ctrl Pts',(7.61383333599314,3.35812181533772,9.27541222329822));
#78507=CARTESIAN_POINT('Ctrl Pts',(3.78426551438176,6.88428049739225,9.48709729120694));
#78508=CARTESIAN_POINT('Ctrl Pts',(0.0412122757921709,7.87252182827916,
9.64586109213845));
#78509=CARTESIAN_POINT('Ctrl Pts',(-3.71905970950459,6.91972904609487,9.80462489306996));
#78510=CARTESIAN_POINT('Ctrl Pts',(-7.57211199967683,3.44018083883985,10.0163099609787));
#78511=CARTESIAN_POINT('Ctrl Pts',(-8.15710102430372,-3.61785837417917,
10.2809162958645));
#78512=CARTESIAN_POINT('Ctrl Pts',(-1.35785331291593,-8.82618834600539,
10.5984438977276));
#78513=CARTESIAN_POINT('Ctrl Pts',(5.31282029565194,-6.39869642758869,10.8630502326134));
#78514=CARTESIAN_POINT('Ctrl Pts',(7.64293017155263,-1.78209684365176,11.0747353005222));
#78515=CARTESIAN_POINT('Ctrl Pts',(7.59107509017759,3.41431582500192,11.2864203684308));
#78516=CARTESIAN_POINT('Ctrl Pts',(3.66292364276056,7.47197635048085,11.4981054363395));
#78517=CARTESIAN_POINT('Ctrl Pts',(-1.53761544457804,7.70387708849976,11.7097905042482));
#78518=CARTESIAN_POINT('Ctrl Pts',(-5.03774613814279,6.04974480751453,11.8685543051797));
#78519=CARTESIAN_POINT('Ctrl Pts',(-7.3011793187762,2.89945438820694,12.0273181061112));
#78520=CARTESIAN_POINT('Ctrl Pts',(-8.00856867091811,-2.2437807786793,12.2390031740199));
#78521=CARTESIAN_POINT('Ctrl Pts',(-3.91132400815189,-8.02051998560973,
12.5036095089058));
#78522=CARTESIAN_POINT('Ctrl Pts',(4.64447927735037,-7.62719991745463,12.8211371107688));
#78523=CARTESIAN_POINT('Ctrl Pts',(8.18505005722536,-1.47456129985973,13.0857434456547));
#78524=CARTESIAN_POINT('Ctrl Pts',(6.99507702683413,3.55796966766715,13.2974285135634));
#78525=CARTESIAN_POINT('Ctrl Pts',(3.60932701092508,7.50031546708409,13.5091135814721));
#78526=CARTESIAN_POINT('Ctrl Pts',(-2.0088825441779,8.07538427064232,13.7207986493808));
#78527=CARTESIAN_POINT('Ctrl Pts',(-6.13710159400592,4.90407661797473,13.9324837172894));
#78528=CARTESIAN_POINT('Ctrl Pts',(-7.74989581925343,1.38470689286203,14.091247518221));
#78529=CARTESIAN_POINT('Ctrl Pts',(-7.45309532156961,-2.48302745087824,
14.2500113191525));
#78530=CARTESIAN_POINT('Ctrl Pts',(-4.68247960285998,-6.87358051588703,
14.4616963870612));
#78531=CARTESIAN_POINT('Ctrl Pts',(2.1720517209044,-8.6550209507561,14.726302721947));
#78532=CARTESIAN_POINT('Ctrl Pts',(8.46476580741211,-2.84483851285514,15.0438303238101));
#78533=CARTESIAN_POINT('Ctrl Pts',(7.21182047590841,4.14234485401649,15.3084366586959));
#78534=CARTESIAN_POINT('Ctrl Pts',(3.06083172580491,7.22644863772574,15.5201217266046));
#78535=CARTESIAN_POINT('Ctrl Pts',(-2.06813706012608,8.06255435194748,15.7318067945133));
#78536=CARTESIAN_POINT('Ctrl Pts',(-6.73688556628923,4.8848554801103,15.943491862422));
#78537=CARTESIAN_POINT('Ctrl Pts',(-7.85328532036503,-0.199732638934405,
16.1551769303307));
#78538=CARTESIAN_POINT('Ctrl Pts',(-6.82102814845832,-3.93088709916232,
16.3139407312622));
#78539=CARTESIAN_POINT('Ctrl Pts',(-4.1034353000989,-6.69894573288364,16.4727045321937));
#78540=CARTESIAN_POINT('Ctrl Pts',(0.843508648565539,-8.27406898082055,
16.6843896001024));
#78541=CARTESIAN_POINT('Ctrl Pts',(7.23496495736793,-5.22326319478244,16.9489959349882));
#78542=CARTESIAN_POINT('Ctrl Pts',(8.30817833769211,3.27407071512828,17.2665235368513));
#78543=CARTESIAN_POINT('Ctrl Pts',(2.85036941342305,7.81311523486957,17.5311298717372));
#78544=CARTESIAN_POINT('Ctrl Pts',(-2.31143825127639,7.49983359668189,17.7428149396458));
#78545=CARTESIAN_POINT('Ctrl Pts',(-6.77395930557603,4.83688421444779,17.9545000075546));
#78546=CARTESIAN_POINT('Ctrl Pts',(-8.29979865471094,-0.600651717802035,
18.1661850754632));
#78547=CARTESIAN_POINT('Ctrl Pts',(-5.87987775571883,-5.20970450485624,
18.377870143372));
#78548=CARTESIAN_POINT('Ctrl Pts',(-2.68753909621523,-7.39969134455864,
18.5366339443034));
#78549=CARTESIAN_POINT('Ctrl Pts',(1.17408020208218,-7.7675987842638,18.695397745235));
#78550=CARTESIAN_POINT('Ctrl Pts',(5.9732038790861,-5.7872756767284,18.9070828131436));
#78551=CARTESIAN_POINT('Ctrl Pts',(8.89878308796401,0.662461991117818,19.1716891480295));
#78552=CARTESIAN_POINT('Ctrl Pts',(4.24828401123849,7.85477238998132,19.4892167498925));
#78553=CARTESIAN_POINT('Ctrl Pts',(-2.85022797253053,7.81316683368111,19.7538230847783));
#78554=CARTESIAN_POINT('Ctrl Pts',(-6.59775985214242,4.24968418836499,19.9655081526871));
#78555=CARTESIAN_POINT('Ctrl Pts',(-8.29727381828563,-0.661226709960443,
20.1771932205958));
#78556=CARTESIAN_POINT('Ctrl Pts',(-5.96334178721012,-5.80396372522722,
20.3888782885045));
#78557=CARTESIAN_POINT('Ctrl Pts',(-1.14401538716822,-7.77207901684218,
20.6005633564131));
#78558=CARTESIAN_POINT('Ctrl Pts',(2.7085961530172,-7.39200955547825,20.7593271573447));
#78559=CARTESIAN_POINT('Ctrl Pts',(5.89999520691335,-5.18691736512331,20.9180909582762));
#78560=CARTESIAN_POINT('Ctrl Pts',(8.2965982924794,-0.581533415041086,21.1297760261849));
#78561=CARTESIAN_POINT('Ctrl Pts',(6.38181938745116,6.23695259259394,21.3943823610707));
#78562=CARTESIAN_POINT('Ctrl Pts',(-1.80751789403929,8.74518412620829,21.7119099629338));
#78563=CARTESIAN_POINT('Ctrl Pts',(-7.2117454860696,4.14247540855493,21.9765162978196));
#78564=CARTESIAN_POINT('Ctrl Pts',(-7.78435486756486,-0.997030623000835,
22.1882013657284));
#78565=CARTESIAN_POINT('Ctrl Pts',(-5.92240458111352,-5.84868340356868,
22.399886433637));
#78566=CARTESIAN_POINT('Ctrl Pts',(-0.825217461337168,-8.28048647944938,
22.6115715015457));
#78567=CARTESIAN_POINT('Ctrl Pts',(4.12932257752919,-6.68301417781114,22.8232565694544));
#78568=CARTESIAN_POINT('Ctrl Pts',(6.83219228398968,-3.91145075170492,22.982020370386));
#78569=CARTESIAN_POINT('Ctrl Pts',(7.85400392738354,-0.169344332240322,
23.1407841713174));
#78570=CARTESIAN_POINT('Ctrl Pts',(6.7221263281516,4.89742197160429,23.3524692392262));
#78571=CARTESIAN_POINT('Ctrl Pts',(0.866581172239455,8.88122927348642,23.617075574112));
#78572=CARTESIAN_POINT('Ctrl Pts',(-7.01412076883092,5.52697712848645,23.934603175975));
#78573=CARTESIAN_POINT('Ctrl Pts',(-8.18507674979193,-1.47441312607569,
24.1992095108609));
#78574=CARTESIAN_POINT('Ctrl Pts',(-5.31374315308747,-5.77532548610016,
24.4108945787696));
#78575=CARTESIAN_POINT('Ctrl Pts',(-0.765100799302659,-8.28834086801934,
24.6225796466782));
#78576=CARTESIAN_POINT('Ctrl Pts',(4.70060641120063,-6.86671242748808,24.834264714587));
#78577=CARTESIAN_POINT('Ctrl Pts',(7.46264283011114,-2.45416899179898,25.0459497824956));
#78578=CARTESIAN_POINT('Ctrl Pts',(7.74592195511079,1.40676631099648,25.2047135834272));
#78579=CARTESIAN_POINT('Ctrl Pts',(6.11808374448742,4.92778920913389,25.3634773843586));
#78580=CARTESIAN_POINT('Ctrl Pts',(1.98949854169024,8.07549502459095,25.5751624522674));
#78581=CARTESIAN_POINT('Ctrl Pts',(-5.05578988172845,7.35297116872643,25.8397687871532));
#78582=CARTESIAN_POINT('Ctrl Pts',(-8.92538445154858,-0.287886662789833,
26.1572963890163));
#78583=CARTESIAN_POINT('Ctrl Pts',(-5.31293613005572,-6.39860024882612,
26.4219027239021));
#78584=CARTESIAN_POINT('Ctrl Pts',(-0.346655166516884,-7.84028577048752,
26.6335877918108));
#78585=CARTESIAN_POINT('Ctrl Pts',(4.75165881922995,-6.83401141667239,26.8452728597195));
#78586=CARTESIAN_POINT('Ctrl Pts',(8.01801485379917,-2.22685383424587,27.0569579276282));
#78587=CARTESIAN_POINT('Ctrl Pts',(7.28990149564492,2.92768161416345,27.2686429955369));
#78588=CARTESIAN_POINT('Ctrl Pts',(5.02050125533267,6.06406345065949,27.4274067964684));
#78589=CARTESIAN_POINT('Ctrl Pts',(1.507796009611,7.70977343296281,27.5861705973999));
#78590=CARTESIAN_POINT('Ctrl Pts',(-3.67782551435031,7.45957933301706,27.7978556653086));
#78591=CARTESIAN_POINT('Ctrl Pts',(-8.60287498137043,2.37017686918522,28.0624620001945));
#78592=CARTESIAN_POINT('Ctrl Pts',(-6.64336858336157,-5.96749697982012,
28.3799896020575));
#78593=CARTESIAN_POINT('Ctrl Pts',(0.0553016102434953,-8.31662895638818,
28.6445959369434));
#78594=CARTESIAN_POINT('Ctrl Pts',(4.78329661923949,-6.22176214747512,28.856281004852));
#78595=CARTESIAN_POINT('Ctrl Pts',(8.03601782043171,-2.16896084964146,29.0679660727609));
#78596=CARTESIAN_POINT('Ctrl Pts',(7.56843959863063,3.4592141068051,29.2796511406694));
#78597=CARTESIAN_POINT('Ctrl Pts',(3.69225504524338,6.93406346459216,29.4913362085781));
#78598=CARTESIAN_POINT('Ctrl Pts',(-0.0636262725448295,7.87237258301866,
29.6501000095096));
#78599=CARTESIAN_POINT('Ctrl Pts',(-3.81087691677871,6.86959040404745,29.8088638104412));
#78600=CARTESIAN_POINT('Ctrl Pts',(-7.61725195378524,3.33904133130091,30.0205488783499));
#78601=CARTESIAN_POINT('Ctrl Pts',(-8.1082003188195,-3.72616209070479,30.2851552132357));
#78602=CARTESIAN_POINT('Ctrl Pts',(-1.24019846339322,-8.84348766663666,
30.6026828150987));
#78603=CARTESIAN_POINT('Ctrl Pts',(5.39755782418636,-6.32738057974178,30.8672891499846));
#78604=CARTESIAN_POINT('Ctrl Pts',(7.66598387445893,-1.68016130294613,31.0789742178933));
#78605=CARTESIAN_POINT('Ctrl Pts',(7.54493505998739,3.51510007228062,31.290659285802));
#78606=CARTESIAN_POINT('Ctrl Pts',(3.56309784696235,7.52009135102838,31.5023443537107));
#78607=CARTESIAN_POINT('Ctrl Pts',(-1.64006823190909,7.68271824582937,31.7140294216193));
#78608=CARTESIAN_POINT('Ctrl Pts',(-5.1178612227958,5.98212294195165,31.8727932225509));
#78609=CARTESIAN_POINT('Ctrl Pts',(-7.33914268111359,2.80197071727642,32.0315570234824));
#78610=CARTESIAN_POINT('Ctrl Pts',(-7.97797911978374,-2.35022839398137,
32.2432420913911));
#78611=CARTESIAN_POINT('Ctrl Pts',(-3.80417147369922,-8.07189418507224,
32.5078484262769));
#78612=CARTESIAN_POINT('Ctrl Pts',(4.74563550526883,-7.5646751410546,32.82537602814));
#78613=CARTESIAN_POINT('Ctrl Pts',(8.20396037581917,-1.36543385717473,33.0899823630259));
#78614=CARTESIAN_POINT('Ctrl Pts',(6.9470768686315,3.65080453444267,33.3016674309345));
#78615=CARTESIAN_POINT('Ctrl Pts',(3.50912858801016,7.54771423216215,33.5133524988433));
#78616=CARTESIAN_POINT('Ctrl Pts',(-2.11624074155345,8.04791683099602,33.7250375667519));
#78617=CARTESIAN_POINT('Ctrl Pts',(-6.20186284261742,4.8219167072315,33.9367226346606));
#78618=CARTESIAN_POINT('Ctrl Pts',(-7.76764817123625,1.2813821741822,34.0954864355922));
#78619=CARTESIAN_POINT('Ctrl Pts',(-7.41936908165992,-2.58205685923576,
34.2542502365237));
#78620=CARTESIAN_POINT('Ctrl Pts',(-4.5905319766373,-6.93532555191544,34.4659353044323));
#78621=CARTESIAN_POINT('Ctrl Pts',(2.2871142156941,-8.62532926331976,34.7305416393182));
#78622=CARTESIAN_POINT('Ctrl Pts',(8.50189869988551,-2.73186471763199,35.0480692411812));
#78623=CARTESIAN_POINT('Ctrl Pts',(7.15601923311525,4.23801418138421,35.3126755760671));
#78624=CARTESIAN_POINT('Ctrl Pts',(2.96432890111406,7.26656761706666,35.5243606439757));
#78625=CARTESIAN_POINT('Ctrl Pts',(-2.17531915308836,8.03429898371857,35.7360457118845));
#78626=CARTESIAN_POINT('Ctrl Pts',(-6.80133767308289,4.79471021559624,35.9477307797929));
#78627=CARTESIAN_POINT('Ctrl Pts',(-7.84992922384292,-0.304293658780176,
36.1594158477019));
#78628=CARTESIAN_POINT('Ctrl Pts',(-6.76807744641505,-4.02137116761797,
36.3181796486333));
#78629=CARTESIAN_POINT('Ctrl Pts',(-4.01386455155247,-6.75299537657241,
36.4769434495648));
#78630=CARTESIAN_POINT('Ctrl Pts',(0.953615975297951,-8.26210269309442,
36.6886285174736));
#78631=CARTESIAN_POINT('Ctrl Pts',(7.30387932579855,-5.12645522076245,36.9532348523594));
#78632=CARTESIAN_POINT('Ctrl Pts',(8.26384230461509,3.38441674487815,37.2707624542225));
#78633=CARTESIAN_POINT('Ctrl Pts',(2.74607287046835,7.85037956129559,37.5353687891083));
#78634=CARTESIAN_POINT('Ctrl Pts',(-2.41110526728106,7.46838819006294,37.747053857017));
#78635=CARTESIAN_POINT('Ctrl Pts',(-6.83776931292273,4.74624950890969,37.9587389249257));
#78636=CARTESIAN_POINT('Ctrl Pts',(-8.2910641039737,-0.711123209182693,
38.1704239928344));
#78637=CARTESIAN_POINT('Ctrl Pts',(-5.80998105857133,-5.2875422976236,38.3821090607431));
#78638=CARTESIAN_POINT('Ctrl Pts',(-2.58876237455158,-7.43482398961316,
38.5408728616746));
#78639=CARTESIAN_POINT('Ctrl Pts',(1.27741377748707,-7.75127532960252,38.6996366626061));
#78640=CARTESIAN_POINT('Ctrl Pts',(6.04974083194368,-5.70722000678919,38.9113217305148));
#78641=CARTESIAN_POINT('Ctrl Pts',(8.88917232560822,0.78090441281303,39.1759280654007));
#78642=CARTESIAN_POINT('Ctrl Pts',(4.14330878626316,7.91064843361354,39.4934556672637));
#78643=CARTESIAN_POINT('Ctrl Pts',(-2.95401973467792,7.77451881941656,39.7580620021495));
#78644=CARTESIAN_POINT('Ctrl Pts',(-6.65376599972446,4.16144791969008,39.9697470700583));
#78645=CARTESIAN_POINT('Ctrl Pts',(-8.28773284102336,-0.771659208068619,
40.1814321379668));
#78646=CARTESIAN_POINT('Ctrl Pts',(-5.88552420195028,-5.88286027907313,
40.3931172058756));
#78647=CARTESIAN_POINT('Ctrl Pts',(-1.04041660659482,-7.7866242194444,40.6048022737843));
#78648=CARTESIAN_POINT('Ctrl Pts',(2.80679210820641,-7.35528493327974,40.7635660747157));
#78649=CARTESIAN_POINT('Ctrl Pts',(5.96854394481355,-5.10788981606378,40.9223298756474));
#78650=CARTESIAN_POINT('Ctrl Pts',(8.30360666248527,-0.470999717952826,
41.134014943556));
#78651=CARTESIAN_POINT('Ctrl Pts',(6.29819877468409,6.32138343488813,41.3986212784418));
#78652=CARTESIAN_POINT('Ctrl Pts',(-1.92381337494631,8.72033877994056,41.7161488803048));
#78653=CARTESIAN_POINT('Ctrl Pts',(-7.26626954003949,4.04607247065895,41.9807552151907));
#78654=CARTESIAN_POINT('Ctrl Pts',(-7.7703876181543,-1.10060303062287,42.1924402830995));
#78655=CARTESIAN_POINT('Ctrl Pts',(-5.84399511353304,-5.92703084947052,
42.4041253510082));
#78656=CARTESIAN_POINT('Ctrl Pts',(-0.71487671085122,-8.29074131083116,
42.6158104189167));
#78657=CARTESIAN_POINT('Ctrl Pts',(4.21795117979728,-6.62743323579823,42.8274954868256));
#78658=CARTESIAN_POINT('Ctrl Pts',(6.88367353941432,-3.82012264085702,42.9862592877569));
#78659=CARTESIAN_POINT('Ctrl Pts',(7.85556260206146,-0.0647410172293493,
43.1450230886886));
#78660=CARTESIAN_POINT('Ctrl Pts',(6.65631347790844,4.98650330626542,43.3567081565972));
#78661=CARTESIAN_POINT('Ctrl Pts',(0.748236927761726,8.8919816596889,43.621314491483));
#78662=CARTESIAN_POINT('Ctrl Pts',(-7.08709914359345,5.43308310882824,43.938842093346));
#78663=CARTESIAN_POINT('Ctrl Pts',(-8.1647168768334,-1.58327944074342,44.2034484282321));
#78664=CARTESIAN_POINT('Ctrl Pts',(-5.236364530052,-5.84557416134595,44.4151334961406));
#78665=CARTESIAN_POINT('Ctrl Pts',(-0.654660785897164,-8.29779445593723,
44.6268185640494));
#78666=CARTESIAN_POINT('Ctrl Pts',(4.79163058654542,-6.80350766273701,44.8385036319579));
#78667=CARTESIAN_POINT('Ctrl Pts',(7.49466220675512,-2.3545746657842,45.0501886998668));
#78668=CARTESIAN_POINT('Ctrl Pts',(7.72650184443749,1.50979059353471,45.2089525007983));
#78669=CARTESIAN_POINT('Ctrl Pts',(6.05192006718989,5.00882408301219,45.3677163017298));
#78670=CARTESIAN_POINT('Ctrl Pts',(1.88178433583927,8.10127224903418,45.5794013696383));
#78671=CARTESIAN_POINT('Ctrl Pts',(-5.15325785597106,7.28499346644748,45.8440077045244));
#78672=CARTESIAN_POINT('Ctrl Pts',(-8.92075938457942,-0.4067165364164,46.1615353063873));
#78673=CARTESIAN_POINT('Ctrl Pts',(-5.22725770400791,-6.4687829119718,46.4261416412733));
#78674=CARTESIAN_POINT('Ctrl Pts',(-0.242218808112939,-7.84420683156551,
46.637826709182));
#78675=CARTESIAN_POINT('Ctrl Pts',(4.84224300288465,-6.77012970914063,46.8495117770905));
#78676=CARTESIAN_POINT('Ctrl Pts',(8.04695793050456,-2.1198840203015,47.0611968449994));
#78677=CARTESIAN_POINT('Ctrl Pts',(7.25026846303026,3.02449841529221,47.272881912908));
#78678=CARTESIAN_POINT('Ctrl Pts',(4.93930363797658,6.13038155095525,47.4316457138395));
#78679=CARTESIAN_POINT('Ctrl Pts',(1.4049946687936,7.72916846593991,47.5904095147711));
#78680=CARTESIAN_POINT('Ctrl Pts',(-3.77683532552611,7.40994192038234,47.8020945826797));
#78681=CARTESIAN_POINT('Ctrl Pts',(-8.63367476846056,2.25540602303826,48.0667009175657));
#78682=CARTESIAN_POINT('Ctrl Pts',(-6.56331300052723,-6.05543464960746,
48.3842285194284));
#78683=CARTESIAN_POINT('Ctrl Pts',(0.166045579120638,-8.31515509969495,
48.6488348543146));
#78684=CARTESIAN_POINT('Ctrl Pts',(4.86572494464703,-6.15751342105094,48.860519922223));
#78685=CARTESIAN_POINT('Ctrl Pts',(8.06418836553557,-2.06175643147653,49.072204990132));
#78686=CARTESIAN_POINT('Ctrl Pts',(7.52170368493643,3.55969294614753,49.2838900580404));
#78687=CARTESIAN_POINT('Ctrl Pts',(3.59958979683137,6.98261675481792,49.4955751259492));
#78688=CARTESIAN_POINT('Ctrl Pts',(-0.168453537486675,7.870827262374,49.6543389268806));
#78689=CARTESIAN_POINT('Ctrl Pts',(-3.90201830854838,6.81823351858615,49.8131027278124));
#78690=CARTESIAN_POINT('Ctrl Pts',(-7.66104107524026,3.2373096829101,50.0247877957208));
#78691=CARTESIAN_POINT('Ctrl Pts',(-8.0578617165962,-3.83380501493248,50.2893941306069));
#78692=CARTESIAN_POINT('Ctrl Pts',(-1.12232367883472,-8.85921869571382,
50.6069217324699));
#78693=CARTESIAN_POINT('Ctrl Pts',(5.4813381574754,-6.25494264320094,50.8715280673556));
#78694=CARTESIAN_POINT('Ctrl Pts',(7.68767810266248,-1.57792780481932,51.0832131352645));
#78695=CARTESIAN_POINT('Ctrl Pts',(7.49745702172037,3.61526095670117,51.294898203173));
#78696=CARTESIAN_POINT('Ctrl Pts',(3.46264017644585,7.56687274924533,51.5065832710818));
#78697=CARTESIAN_POINT('Ctrl Pts',(-1.7422301718647,7.66019696080821,51.7182683389905));
#78698=CARTESIAN_POINT('Ctrl Pts',(-5.1970687132064,5.91344021519166,51.8770321399219));
#78699=CARTESIAN_POINT('Ctrl Pts',(-7.3758045302931,2.70399014884053,52.0357959408536));
#78700=CARTESIAN_POINT('Ctrl Pts',(-7.94597476517177,-2.45625922312734,
52.247481008762));
#78701=CARTESIAN_POINT('Ctrl Pts',(-3.69634431283579,-8.12183692624851,
52.5120873436481));
#78702=CARTESIAN_POINT('Ctrl Pts',(4.84595014885174,-7.50080885594317,52.829614945511));
#78703=CARTESIAN_POINT('Ctrl Pts',(8.22141581583643,-1.25606427031315,53.094221280397));
#78704=CARTESIAN_POINT('Ctrl Pts',(6.89784472552101,3.74299197262333,53.3059063483056));
#78705=CARTESIAN_POINT('Ctrl Pts',(3.40830786160718,7.59377449656253,53.5175914162142));
#78706=CARTESIAN_POINT('Ctrl Pts',(-2.22322364860433,8.01902218468158,53.729276484123));
#78707=CARTESIAN_POINT('Ctrl Pts',(-6.26552426067689,4.73890168526058,53.9409615520318));
#78708=CARTESIAN_POINT('Ctrl Pts',(-7.78402302158592,1.17783021567688,54.0997253529632));
#78709=CARTESIAN_POINT('Ctrl Pts',(-7.38432709758672,-2.68062836686848,
54.2584891538947));
#78710=CARTESIAN_POINT('Ctrl Pts',(-4.49777028015197,-6.9958406923907,54.4701742218034));
#78711=CARTESIAN_POINT('Ctrl Pts',(2.40177113378299,-8.5941079613927,54.7347805566892));
#78712=CARTESIAN_POINT('Ctrl Pts',(8.53752384820599,-2.61840647632836,55.0523081585523));
#78713=CARTESIAN_POINT('Ctrl Pts',(7.09894900150471,4.33293197708344,55.3169144934381));
#78714=CARTESIAN_POINT('Ctrl Pts',(2.86730032066488,7.3053979113412,55.5285995613469));
#78715=CARTESIAN_POINT('Ctrl Pts',(-2.28211530840029,8.00461893317224,55.7402846292555));
#78716=CARTESIAN_POINT('Ctrl Pts',(-6.86458398523512,4.70371444261994,55.9519696971641));
#78717=CARTESIAN_POINT('Ctrl Pts',(-7.84518060577856,-0.408800442089421,
56.163654765073));
#78718=CARTESIAN_POINT('Ctrl Pts',(-6.71392739005728,-4.1111426610001,56.3224185660044));
#78719=CARTESIAN_POINT('Ctrl Pts',(-3.92358037221183,-6.80584641546676,
56.4811823669359));
#78720=CARTESIAN_POINT('Ctrl Pts',(1.06355069377355,-8.24867345891154,56.6928674348446));
#78721=CARTESIAN_POINT('Ctrl Pts',(7.37150566530056,-5.02873348823263,56.9574737697305));
#78722=CARTESIAN_POINT('Ctrl Pts',(8.21802814289185,3.4941544814057,57.2750013715935));
#78723=CARTESIAN_POINT('Ctrl Pts',(2.64131052672665,7.8862653071121,57.5396077064795));
#78724=CARTESIAN_POINT('Ctrl Pts',(-2.51037290578171,7.43560025010796,57.7512927743881));
#78725=CARTESIAN_POINT('Ctrl Pts',(-6.90029409155121,4.65481971884436,57.9629778422968));
#78726=CARTESIAN_POINT('Ctrl Pts',(-8.28100690494395,-0.821563361522968,
58.1746629102055));
#78727=CARTESIAN_POINT('Ctrl Pts',(-5.73887154209026,-5.36432529669737,
58.3863479781142));
#78728=CARTESIAN_POINT('Ctrl Pts',(-2.48990629535911,-7.46888184180529,
58.5451117790458));
#78729=CARTESIAN_POINT('Ctrl Pts',(1.38121344013289,-7.73313279057438,58.7038755799772));
#78730=CARTESIAN_POINT('Ctrl Pts',(6.1237083934355,-5.62711262023186,58.9155606478858));
#78731=CARTESIAN_POINT('Ctrl Pts',(8.88108147570853,0.901195414789174,59.1801669827717));
#78732=CARTESIAN_POINT('Ctrl Pts',(4.03218751616045,7.96164873847342,59.4976945846348));
#78733=CARTESIAN_POINT('Ctrl Pts',(-3.04819441019116,7.74032911124811,59.7623009195206));
#78734=CARTESIAN_POINT('Ctrl Pts',(-6.72082854944846,4.06461054654832,59.9739859874293));
#78735=CARTESIAN_POINT('Ctrl Pts',(-7.86235377363163,0.371140675652209,
60.1327497883608));
#78736=CARTESIAN_POINT('Ctrl Pts',(-7.07298371107766,-3.44494050992081,
60.291520283539));
#78737=CARTESIAN_POINT('Ctrl Pts',(-5.4030676852692,-5.41639781933624,60.39736951174));
#78738=CARTESIAN_POINT('Ctrl Pts',(-4.38130218819444,-6.1449117824308,60.4502974729639));
#78739=CARTESIAN_POINT('Ctrl Pts',(-3.43243190685397,7.15930439800971,-59.9835157911635));
#78740=CARTESIAN_POINT('Ctrl Pts',(-4.6229230465457,6.5885414510915,-59.9305854290092));
#78741=CARTESIAN_POINT('Ctrl Pts',(-6.70940095812955,4.84641564141242,-59.8247337998776));
#78742=CARTESIAN_POINT('Ctrl Pts',(-8.21591943031317,1.033550698178,-59.6659609037689));
#78743=CARTESIAN_POINT('Ctrl Pts',(-7.69901306767222,-3.00047282198764,
-59.5071971028374));
#78744=CARTESIAN_POINT('Ctrl Pts',(-4.55552526345291,-7.47266249378137,
-59.2955120349288));
#78745=CARTESIAN_POINT('Ctrl Pts',(2.74304713445976,-8.9792183345732,-59.0309057000428));
#78746=CARTESIAN_POINT('Ctrl Pts',(9.04227886094756,-2.5360286421388,-58.7133780981799));
#78747=CARTESIAN_POINT('Ctrl Pts',(7.36197121198212,4.72764453598642,-58.4487717632939));
#78748=CARTESIAN_POINT('Ctrl Pts',(2.82647711349423,7.76589593501196,-58.2370866953853));
#78749=CARTESIAN_POINT('Ctrl Pts',(-1.2334285983065,8.19028922052275,-58.0783228944537));
#78750=CARTESIAN_POINT('Ctrl Pts',(-4.98045605042172,6.59506433331062,-57.9195590935222));
#78751=CARTESIAN_POINT('Ctrl Pts',(-8.43469294985433,2.3452514380058,-57.7078740256135));
#78752=CARTESIAN_POINT('Ctrl Pts',(-7.99148361614971,-3.57982560672035,
-57.4961889577049));
#78753=CARTESIAN_POINT('Ctrl Pts',(-3.9431303285702,-7.25383778053677,-57.2845038897961));
#78754=CARTESIAN_POINT('Ctrl Pts',(1.31506405940233,-8.65019871020488,-57.0728188218875));
#78755=CARTESIAN_POINT('Ctrl Pts',(7.8873330128033,-5.10391056925949,-56.8082124870015));
#78756=CARTESIAN_POINT('Ctrl Pts',(8.54732004282932,3.88237251743919,-56.4906848851387));
#78757=CARTESIAN_POINT('Ctrl Pts',(2.5902279706948,8.35753082550421,-56.2260785502526));
#78758=CARTESIAN_POINT('Ctrl Pts',(-2.83896582282601,7.76169102640962,-56.0143934823441));
#78759=CARTESIAN_POINT('Ctrl Pts',(-6.2171077967334,5.47207923197023,-55.8556296814125));
#78760=CARTESIAN_POINT('Ctrl Pts',(-8.05743347284584,1.83882652792089,-55.696865880481));
#78761=CARTESIAN_POINT('Ctrl Pts',(-7.96329140383586,-3.63694420072908,
-55.4851808125723));
#78762=CARTESIAN_POINT('Ctrl Pts',(-3.80919199311957,-7.88477319258719,
-55.2734957446636));
#78763=CARTESIAN_POINT('Ctrl Pts',(1.65406980071603,-8.08892035499237,-55.0618106767549));
#78764=CARTESIAN_POINT('Ctrl Pts',(6.57615857834954,-5.77140446258325,-54.8501256088461));
#78765=CARTESIAN_POINT('Ctrl Pts',(9.32106714971483,1.17385022568006,-54.5855192739605));
#78766=CARTESIAN_POINT('Ctrl Pts',(4.03954258602107,8.47416813178503,-54.2679916720972));
#78767=CARTESIAN_POINT('Ctrl Pts',(-3.39981618129403,8.06218455553205,-54.0033853372115));
#78768=CARTESIAN_POINT('Ctrl Pts',(-7.16998459470855,4.11034366672326,-53.7917002693027));
#78769=CARTESIAN_POINT('Ctrl Pts',(-8.28024482584534,0.183324227672024,
-53.6329364683713));
#78770=CARTESIAN_POINT('Ctrl Pts',(-7.34874032452431,-3.78147331791097,
-53.4741726674397));
#78771=CARTESIAN_POINT('Ctrl Pts',(-3.75075153875775,-7.91032445948964,
-53.2624875995311));
#78772=CARTESIAN_POINT('Ctrl Pts',(2.16278181964522,-8.48539720195137,-53.0508025316223));
#78773=CARTESIAN_POINT('Ctrl Pts',(6.47413724132143,-5.12368300094565,-52.8391174637137));
#78774=CARTESIAN_POINT('Ctrl Pts',(8.74769454875537,-0.181135639340342,
-52.6274323958049));
#78775=CARTESIAN_POINT('Ctrl Pts',(6.37561247902266,6.9001292108873,-52.3628260609192));
#78776=CARTESIAN_POINT('Ctrl Pts',(-2.3660659621478,9.08466630143443,-52.045298459056));
#78777=CARTESIAN_POINT('Ctrl Pts',(-7.79257887986899,3.97910594393446,-51.7806921241703));
#78778=CARTESIAN_POINT('Ctrl Pts',(-8.13243552606366,-1.47210619093496,
-51.5690070562615));
#78779=CARTESIAN_POINT('Ctrl Pts',(-6.45319939494819,-5.19155850253244,
-51.41024325533));
#78780=CARTESIAN_POINT('Ctrl Pts',(-3.18749830448594,-7.62518061277131,
-51.2514794543985));
#78781=CARTESIAN_POINT('Ctrl Pts',(2.22394736708779,-8.46731529314309,-51.0397943864898));
#78782=CARTESIAN_POINT('Ctrl Pts',(7.11864843416257,-5.09945441570212,-50.8281093185811));
#78783=CARTESIAN_POINT('Ctrl Pts',(8.25255779370852,0.248737569150617,-50.6164242506724));
#78784=CARTESIAN_POINT('Ctrl Pts',(6.80943239642104,5.49423338372509,-50.4047391827638));
#78785=CARTESIAN_POINT('Ctrl Pts',(0.434799365288336,9.38462397337061,-50.1401328478779));
#78786=CARTESIAN_POINT('Ctrl Pts',(-7.66006120028907,5.42705190266821,-49.8226052460149));
#78787=CARTESIAN_POINT('Ctrl Pts',(-8.52427109164289,-1.97341634426556,
-49.557998911129));
#78788=CARTESIAN_POINT('Ctrl Pts',(-5.27414620734275,-6.36293847264405,
-49.3463138432203));
#78789=CARTESIAN_POINT('Ctrl Pts',(-1.59434405259234,-8.1273691412489,-49.1875500422887));
#78790=CARTESIAN_POINT('Ctrl Pts',(2.47127825195855,-7.88646363206378,-49.0287862413573));
#78791=CARTESIAN_POINT('Ctrl Pts',(7.15380242627116,-5.04623433968172,-48.8171011734485));
#78792=CARTESIAN_POINT('Ctrl Pts',(8.73006719123986,0.682288577836312,-48.6054161055399));
#78793=CARTESIAN_POINT('Ctrl Pts',(6.15380285543387,5.50429749679883,-48.3937310376312));
#78794=CARTESIAN_POINT('Ctrl Pts',(1.67199672105926,8.5883291157846,-48.1820459697225));
#78795=CARTESIAN_POINT('Ctrl Pts',(-5.71028901498176,7.46008156624264,-47.9174396348366));
#78796=CARTESIAN_POINT('Ctrl Pts',(-9.35524473854869,-0.780272919104606,
-47.5999120329737));
#78797=CARTESIAN_POINT('Ctrl Pts',(-5.25113282817633,-6.99879802055191,
-47.3353056980877));
#78798=CARTESIAN_POINT('Ctrl Pts',(0.0620161441714672,-8.26436677676782,
-47.1236206301791));
#78799=CARTESIAN_POINT('Ctrl Pts',(4.0135580506168,-7.24481979696462,-46.9648568292474));
#78800=CARTESIAN_POINT('Ctrl Pts',(6.96901120128802,-4.44256769163848,-46.8060930283161));
#78801=CARTESIAN_POINT('Ctrl Pts',(8.72269375463095,0.745643231061926,-46.5944079604073));
#78802=CARTESIAN_POINT('Ctrl Pts',(6.23996937726438,6.14348215898863,-46.3827228924987));
#78803=CARTESIAN_POINT('Ctrl Pts',(1.16389899084976,8.17385586219323,-46.17103782459));
#78804=CARTESIAN_POINT('Ctrl Pts',(-4.25096810407249,7.64749895158049,-45.9593527566812));
#78805=CARTESIAN_POINT('Ctrl Pts',(-9.17259792661805,2.03068089226677,-45.6947464217955));
#78806=CARTESIAN_POINT('Ctrl Pts',(-6.65519391252716,-6.6210138145976,-45.3772188199323));
#78807=CARTESIAN_POINT('Ctrl Pts',(0.489066437201014,-8.73603936184105,
-45.1126124850466));
#78808=CARTESIAN_POINT('Ctrl Pts',(5.36904238053102,-6.28307155292245,-44.9009274171378));
#78809=CARTESIAN_POINT('Ctrl Pts',(7.73583035363276,-2.95854539528728,-44.7421636162063));
#78810=CARTESIAN_POINT('Ctrl Pts',(8.19259811029568,1.08851321611066,-44.5833998152748));
#78811=CARTESIAN_POINT('Ctrl Pts',(6.19353266310277,6.18720642262607,-44.3717147473661));
#78812=CARTESIAN_POINT('Ctrl Pts',(0.818240311996971,8.71837563189565,-44.1600296794574));
#78813=CARTESIAN_POINT('Ctrl Pts',(-4.37282208526656,7.00321408550508,-43.9483446115487));
#78814=CARTESIAN_POINT('Ctrl Pts',(-8.17676432328914,3.11375902048511,-43.73665954364));
#78815=CARTESIAN_POINT('Ctrl Pts',(-8.32548268704189,-4.35276413757749,
-43.4720532087542));
#78816=CARTESIAN_POINT('Ctrl Pts',(-0.828433117629804,-9.35110306413339,
-43.1545256068911));
#78817=CARTESIAN_POINT('Ctrl Pts',(5.99949495138197,-6.36895831670886,-42.8899192720053));
#78818=CARTESIAN_POINT('Ctrl Pts',(8.15361193791628,-1.3498950288637,-42.6782342040966));
#78819=CARTESIAN_POINT('Ctrl Pts',(7.82369347155987,2.71769802944199,-42.5194704031651));
#78820=CARTESIAN_POINT('Ctrl Pts',(5.56717948781346,6.10819428054944,-42.3607066022336));
#78821=CARTESIAN_POINT('Ctrl Pts',(0.754556985431625,8.72192719075563,-42.1490215343248));
#78822=CARTESIAN_POINT('Ctrl Pts',(-4.98791033047516,7.19724540377413,-41.9373364664162));
#78823=CARTESIAN_POINT('Ctrl Pts',(-7.85512572654492,2.54235724023673,-41.7256513985074));
#78824=CARTESIAN_POINT('Ctrl Pts',(-8.26099396175561,-2.88287162393748,
-41.5139663305988));
#78825=CARTESIAN_POINT('Ctrl Pts',(-3.56693074773598,-8.69121525740047,
-41.2493599957129));
#78826=CARTESIAN_POINT('Ctrl Pts',(5.38753798751325,-7.687903770179,-40.9318323938499));
#78827=CARTESIAN_POINT('Ctrl Pts',(8.69127070814338,-1.0096450809077,-40.667226058964));
#78828=CARTESIAN_POINT('Ctrl Pts',(7.10749225262746,4.21748243646874,-40.4555409910554));
#78829=CARTESIAN_POINT('Ctrl Pts',(4.23586799310983,7.11712613778268,-40.2967771901239));
#78830=CARTESIAN_POINT('Ctrl Pts',(0.326216400082517,8.25815401156851,-40.1380133891923));
#78831=CARTESIAN_POINT('Ctrl Pts',(-5.03892088698296,7.15895568220903,-39.9263283212837));
#78832=CARTESIAN_POINT('Ctrl Pts',(-8.45066585041011,2.29474128208847,-39.7146432533749));
#78833=CARTESIAN_POINT('Ctrl Pts',(-7.64697342637731,-3.11293718746318,
-39.5029581854663));
#78834=CARTESIAN_POINT('Ctrl Pts',(-4.46408467135861,-7.52508591865946,
-39.2912731175575));
#78835=CARTESIAN_POINT('Ctrl Pts',(2.86741878271786,-8.94640302770514,-39.0266667826717));
#78836=CARTESIAN_POINT('Ctrl Pts',(9.07236289997408,-2.41281191923549,-38.7091391808087));
#78837=CARTESIAN_POINT('Ctrl Pts',(7.29975706379542,4.82401456477915,-38.4445328459229));
#78838=CARTESIAN_POINT('Ctrl Pts',(2.72216605103158,7.80342336501699,-38.2328477780141));
#78839=CARTESIAN_POINT('Ctrl Pts',(-1.34203183253074,8.17282158600294,-38.0740839770826));
#78840=CARTESIAN_POINT('Ctrl Pts',(-5.06800804765613,6.52830906493869,-37.915320176151));
#78841=CARTESIAN_POINT('Ctrl Pts',(-8.46503811194142,2.23259936587045,-37.7036351082425));
#78842=CARTESIAN_POINT('Ctrl Pts',(-7.94317174194882,-3.68586672913096,
-37.4919500403336));
#78843=CARTESIAN_POINT('Ctrl Pts',(-3.84615825894495,-7.3057270113221,-37.2802649724251));
#78844=CARTESIAN_POINT('Ctrl Pts',(1.43011858632153,-8.6319019263036,-37.0685799045163));
#78845=CARTESIAN_POINT('Ctrl Pts',(7.95461194016368,-4.99843640461897,-36.8039735696305));
#78846=CARTESIAN_POINT('Ctrl Pts',(8.49485558088072,3.99585517835802,-36.4864459677674));
#78847=CARTESIAN_POINT('Ctrl Pts',(2.47870800970099,8.39127977809564,-36.2218396328816));
#78848=CARTESIAN_POINT('Ctrl Pts',(-2.94207461054343,7.72319889741794,-36.0101545649728));
#78849=CARTESIAN_POINT('Ctrl Pts',(-6.289424964531,5.38880281061534,-35.8513907640414));
#78850=CARTESIAN_POINT('Ctrl Pts',(-8.08120626336839,1.73136655488185,-35.6926269631098));
#78851=CARTESIAN_POINT('Ctrl Pts',(-7.91415340436405,-3.74266563525237,
-35.4809418952012));
#78852=CARTESIAN_POINT('Ctrl Pts',(-3.70385635277393,-7.93479924037305,
-35.2692568272924));
#78853=CARTESIAN_POINT('Ctrl Pts',(1.76163977452845,-8.06617665450065,-35.0575717593838));
#78854=CARTESIAN_POINT('Ctrl Pts',(6.65243067158831,-5.68332087744279,-34.8458866914751));
#78855=CARTESIAN_POINT('Ctrl Pts',(9.30460904010135,1.29787064859291,-34.5812803565892));
#78856=CARTESIAN_POINT('Ctrl Pts',(3.92633763489875,8.52720955079729,-34.2637527547262));
#78857=CARTESIAN_POINT('Ctrl Pts',(-3.50687526319002,8.0161958309449,-33.9991464198403));
#78858=CARTESIAN_POINT('Ctrl Pts',(-7.22408447090204,4.01449969240922,-33.7874613519316));
#78859=CARTESIAN_POINT('Ctrl Pts',(-8.28195186820398,0.0730436096721498,
-33.6286975510001));
#78860=CARTESIAN_POINT('Ctrl Pts',(-7.2977325088389,-3.87899794378701,-33.4699337500686));
#78861=CARTESIAN_POINT('Ctrl Pts',(-3.64508066652378,-7.95957015796966,
-33.25824868216));
#78862=CARTESIAN_POINT('Ctrl Pts',(2.27558633152054,-8.45584399778082,-33.0465636142511));
#78863=CARTESIAN_POINT('Ctrl Pts',(6.54179300651556,-5.03701546321985,-32.8348785463426));
#78864=CARTESIAN_POINT('Ctrl Pts',(8.7493310000379,-0.0646303956514614,
-32.6231934784338));
#78865=CARTESIAN_POINT('Ctrl Pts',(6.28316118673488,6.98441859506738,-32.358587143548));
#78866=CARTESIAN_POINT('Ctrl Pts',(-2.48683265113032,9.05235291577295,-32.0410595416849));
#78867=CARTESIAN_POINT('Ctrl Pts',(-7.84487591277371,3.87498279026055,-31.7764532067991));
#78868=CARTESIAN_POINT('Ctrl Pts',(-8.11211104120906,-1.58027171023717,
-31.5647681388904));
#78869=CARTESIAN_POINT('Ctrl Pts',(-6.38349350406684,-5.27703257519772,
-31.4060043379588));
#78870=CARTESIAN_POINT('Ctrl Pts',(-3.08567451086231,-7.66695099967925,
-31.2472405370274));
#78871=CARTESIAN_POINT('Ctrl Pts',(2.3365056670397,-8.43694917804998,-31.0355554691186));
#78872=CARTESIAN_POINT('Ctrl Pts',(7.18592440949995,-5.00420635545355,-30.82387040121));
#78873=CARTESIAN_POINT('Ctrl Pts',(8.24851371698094,0.35861117884011,-30.6121853333012));
#78874=CARTESIAN_POINT('Ctrl Pts',(6.73566433098507,5.58442441586969,-30.4005002653926));
#78875=CARTESIAN_POINT('Ctrl Pts',(0.309789921844893,9.38958187641696,-30.1358939305067));
#78876=CARTESIAN_POINT('Ctrl Pts',(-7.73165163989981,5.32456504004463,-29.8183663286437));
#78877=CARTESIAN_POINT('Ctrl Pts',(-8.49723613723125,-2.0867553138219,-29.5537599937579));
#78878=CARTESIAN_POINT('Ctrl Pts',(-5.18894611288327,-6.43260774963586,
-29.3420749258491));
#78879=CARTESIAN_POINT('Ctrl Pts',(-1.48597410012283,-8.14787966835088,
-29.1833111249176));
#78880=CARTESIAN_POINT('Ctrl Pts',(2.57607967638066,-7.85285542458324,-29.0245473239861));
#78881=CARTESIAN_POINT('Ctrl Pts',(7.22036657629709,-4.95052286824314,-28.8128622560774));
#78882=CARTESIAN_POINT('Ctrl Pts',(8.72020736690963,0.798482526486089,-28.6011771881687));
#78883=CARTESIAN_POINT('Ctrl Pts',(6.07995890485837,5.58575690771135,-28.3894921202601));
#78884=CARTESIAN_POINT('Ctrl Pts',(1.55748148291466,8.60983283616151,-28.1778070523513));
#78885=CARTESIAN_POINT('Ctrl Pts',(-5.80912529707869,7.38337869084711,-27.9132007174655));
#78886=CARTESIAN_POINT('Ctrl Pts',(-9.34402466599859,-0.904783392664291,
-27.5956731156025));
#78887=CARTESIAN_POINT('Ctrl Pts',(-5.1574673137037,-7.06810445732873,-27.3310667807166));
#78888=CARTESIAN_POINT('Ctrl Pts',(0.172063565326116,-8.26280813964411,
-27.1193817128079));
#78889=CARTESIAN_POINT('Ctrl Pts',(4.10967823479405,-7.19073062509099,-26.9606179118764));
#78890=CARTESIAN_POINT('Ctrl Pts',(7.02755297464808,-4.34937052997129,-26.8018541109449));
#78891=CARTESIAN_POINT('Ctrl Pts',(8.71199091817952,0.861733373302816,-26.5901690430362));
#78892=CARTESIAN_POINT('Ctrl Pts',(6.15760604669396,6.22603233534218,-26.3784839751275));
#78893=CARTESIAN_POINT('Ctrl Pts',(1.05494816251971,8.18863022069064,-26.1667989072188));
#78894=CARTESIAN_POINT('Ctrl Pts',(-4.35242953761413,7.59021258966908,-25.9551138393102));
#78895=CARTESIAN_POINT('Ctrl Pts',(-9.19882627888814,1.90835340030406,-25.6905075044242));
#78896=CARTESIAN_POINT('Ctrl Pts',(-6.5664346862703,-6.7090510101934,-25.3729799025613));
#78897=CARTESIAN_POINT('Ctrl Pts',(0.605357047477619,-8.72875206181856,
-25.1083735676753));
#78898=CARTESIAN_POINT('Ctrl Pts',(5.45223519853537,-6.21101727279304,-24.8966884997667));
#78899=CARTESIAN_POINT('Ctrl Pts',(7.77454206459834,-2.85526842905397,-24.7379246988352));
#78900=CARTESIAN_POINT('Ctrl Pts',(8.1773764289831,1.19751390688361,-24.5791608979036));
#78901=CARTESIAN_POINT('Ctrl Pts',(6.11059119334711,6.26913434477958,-24.367475829995));
#78902=CARTESIAN_POINT('Ctrl Pts',(0.702069003843994,8.72849872434259,-24.1557907620863));
#78903=CARTESIAN_POINT('Ctrl Pts',(-4.46569305727037,6.94436217625916,-23.9441056941776));
#78904=CARTESIAN_POINT('Ctrl Pts',(-8.21750384820542,3.00459656875853,-23.7324206262689));
#78905=CARTESIAN_POINT('Ctrl Pts',(-8.26678063600234,-4.46324495471978,
-23.467814291383));
#78906=CARTESIAN_POINT('Ctrl Pts',(-0.703835154095096,-9.36130578617593,
-23.15028668952));
#78907=CARTESIAN_POINT('Ctrl Pts',(6.08377558368143,-6.2885009627919,-22.8856803546341));
#78908=CARTESIAN_POINT('Ctrl Pts',(8.17086491846883,-1.24119728778999,-22.6739952867254));
#78909=CARTESIAN_POINT('Ctrl Pts',(7.78680936658882,2.82164172150997,-22.5152314857939));
#78910=CARTESIAN_POINT('Ctrl Pts',(5.48534572612754,6.18178834022344,-22.3564676848624));
#78911=CARTESIAN_POINT('Ctrl Pts',(0.638344029494194,8.73120192557217,-22.1447826169537));
#78912=CARTESIAN_POINT('Ctrl Pts',(-5.08331059235753,7.13018543157429,-21.933097549045));
#78913=CARTESIAN_POINT('Ctrl Pts',(-7.8882846659403,2.43752857335111,-21.7214124811363));
#78914=CARTESIAN_POINT('Ctrl Pts',(-8.22187153789785,-2.99262400755114,
-21.5097274132277));
#78915=CARTESIAN_POINT('Ctrl Pts',(-3.45087739785627,-8.73794385393837,
-21.2451210783418));
#78916=CARTESIAN_POINT('Ctrl Pts',(5.4894366953229,-7.61547862674922,-20.9275934764787));
#78917=CARTESIAN_POINT('Ctrl Pts',(8.70394505668451,-0.893817745320576,
-20.6629871415929));
#78918=CARTESIAN_POINT('Ctrl Pts',(7.0506996865639,4.3117558085969,-20.4513020736842));
#78919=CARTESIAN_POINT('Ctrl Pts',(4.14071677820549,7.17290224935829,-20.2925382727527));
#78920=CARTESIAN_POINT('Ctrl Pts',(0.216217287272026,8.26176584654593,-20.1337744718212));
#78921=CARTESIAN_POINT('Ctrl Pts',(-5.13380673849493,7.09121982009368,-19.9220894039125));
#78922=CARTESIAN_POINT('Ctrl Pts',(-8.48047459139985,2.1820040264926,-19.7104043360038));
#78923=CARTESIAN_POINT('Ctrl Pts',(-7.60484176584855,-3.21449253121196,
-19.4987192680951));
#78924=CARTESIAN_POINT('Ctrl Pts',(-4.36348060053169,-7.58386491737891,
-19.2870342001864));
#78925=CARTESIAN_POINT('Ctrl Pts',(2.9862998261516,-8.90742560776914,-19.0224278653005));
#78926=CARTESIAN_POINT('Ctrl Pts',(9.10368881002332,-2.29178532953828,-18.7049002634375));
#78927=CARTESIAN_POINT('Ctrl Pts',(7.23487052944038,4.92079446165636,-18.4402939285516));
#78928=CARTESIAN_POINT('Ctrl Pts',(2.61800993812571,7.83898132329426,-18.2286088606429));
#78929=CARTESIAN_POINT('Ctrl Pts',(-1.45074668875384,8.15422566288372,-18.0698450597114));
#78930=CARTESIAN_POINT('Ctrl Pts',(-5.15449327773064,6.46024178094735,-17.9110812587799));
#78931=CARTESIAN_POINT('Ctrl Pts',(-8.49401806211714,2.11967623129888,-17.6993961908712));
#78932=CARTESIAN_POINT('Ctrl Pts',(-7.89338436821475,-3.79131561369287,
-17.4877111229625));
#78933=CARTESIAN_POINT('Ctrl Pts',(-3.74853008484207,-7.35629680748716,
-17.2760260550539));
#78934=CARTESIAN_POINT('Ctrl Pts',(1.54493900196434,-8.61209228448443,-17.0643409871452));
#78935=CARTESIAN_POINT('Ctrl Pts',(8.02046857900044,-4.89206514499563,-16.7997346522593));
#78936=CARTESIAN_POINT('Ctrl Pts',(8.44089131054738,4.10862310634076,-16.4822070503963));
#78937=CARTESIAN_POINT('Ctrl Pts',(2.36674525998617,8.42354358841728,-16.2176007155104));
#78938=CARTESIAN_POINT('Ctrl Pts',(-3.04466016546718,7.68333577945795,-16.0059156476017));
#78939=CARTESIAN_POINT('Ctrl Pts',(-6.36062759122894,5.3045714965357,-15.8471518466702));
#78940=CARTESIAN_POINT('Ctrl Pts',(-8.10354555180846,1.62359918336805,-15.6883880457387));
#78941=CARTESIAN_POINT('Ctrl Pts',(-7.86361223773377,-3.84772305911811,
-15.4767029778299));
#78942=CARTESIAN_POINT('Ctrl Pts',(-3.59786371961263,-7.98341828555309,
-15.2650179099214));
#78943=CARTESIAN_POINT('Ctrl Pts',(1.86889728098991,-8.04200245398623,-15.0533328420126));
#78944=CARTESIAN_POINT('Ctrl Pts',(6.72752307776684,-5.59422946207796,-14.841647774104));
#78945=CARTESIAN_POINT('Ctrl Pts',(9.28650083716182,1.42166093391058,-14.577041439218));
#78946=CARTESIAN_POINT('Ctrl Pts',(3.81243640818078,8.57873875228808,-14.2595138373551));
#78947=CARTESIAN_POINT('Ctrl Pts',(-3.61331244831989,7.96878553246661,-13.9949075024691));
#78948=CARTESIAN_POINT('Ctrl Pts',(-7.27690323472737,3.91794378922106,-13.7832224345605));
#78949=CARTESIAN_POINT('Ctrl Pts',(-8.28219020287749,-0.0372499600265304,
-13.624458633629));
#78950=CARTESIAN_POINT('Ctrl Pts',(-7.24543052270881,-3.97583467451395,
-13.4656948326974));
#78951=CARTESIAN_POINT('Ctrl Pts',(-3.5387633815981,-8.00740431689109,-13.2540097647887));
#78952=CARTESIAN_POINT('Ctrl Pts',(2.38798729450963,-8.42479124656918,-13.0423246968801));
#78953=CARTESIAN_POINT('Ctrl Pts',(6.60828865927887,-4.94945466818906,-12.8306396289714));
#78954=CARTESIAN_POINT('Ctrl Pts',(8.74941585748231,0.0518863094023924,
-12.6189545610627));
#78955=CARTESIAN_POINT('Ctrl Pts',(6.18959564749428,7.06746937242281,-12.3543482261768));
#78956=CARTESIAN_POINT('Ctrl Pts',(-2.60715832870307,9.018434198657,-12.0368206243138));
#78957=CARTESIAN_POINT('Ctrl Pts',(-7.89578174653336,3.77017245265299,-11.7722142894279));
#78958=CARTESIAN_POINT('Ctrl Pts',(-8.09034796608499,-1.68815698640432,
-11.5605292215192));
#78959=CARTESIAN_POINT('Ctrl Pts',(-6.31265557350973,-5.36157082639018,
-11.4017654205877));
#78960=CARTESIAN_POINT('Ctrl Pts',(-2.98330350809687,-7.70736174037816,
-11.2430016196562));
#78961=CARTESIAN_POINT('Ctrl Pts',(2.44864961439056,-8.40508686635958,-11.0313165517475));
#78962=CARTESIAN_POINT('Ctrl Pts',(7.25192604319999,-4.90807085635143,-10.8196314838388));
#78963=CARTESIAN_POINT('Ctrl Pts',(8.24300686053481,0.4684211929323,-10.6079464159301));
#78964=CARTESIAN_POINT('Ctrl Pts',(6.66070177239462,5.67362511411226,-10.3962613480214));
#78965=CARTESIAN_POINT('Ctrl Pts',(0.184725540696012,9.39287464433703,-10.1316550131356));
#78966=CARTESIAN_POINT('Ctrl Pts',(-7.80187095937965,5.22113392661204,-9.81412741127258));
#78967=CARTESIAN_POINT('Ctrl Pts',(-8.46869429502031,-2.19972422115192,
-9.54952107638669));
#78968=CARTESIAN_POINT('Ctrl Pts',(-5.10282581808303,-6.50113627709704,
-9.33783600847803));
#78969=CARTESIAN_POINT('Ctrl Pts',(-1.3773406271148,-8.16694526203408,-9.17907220754648));
#78970=CARTESIAN_POINT('Ctrl Pts',(2.68042426248865,-7.81785460286454,-9.02030840661499));
#78971=CARTESIAN_POINT('Ctrl Pts',(7.28565027676,-4.85393347810338,-8.80862333870625));
#78972=CARTESIAN_POINT('Ctrl Pts',(8.70880111337855,0.914534873377897,-8.59693827079764));
#78973=CARTESIAN_POINT('Ctrl Pts',(6.00503674299778,5.66622574842014,-8.38525320288888));
#78974=CARTESIAN_POINT('Ctrl Pts',(1.44269004321358,8.6298097010002,-8.17356813498026));
#78975=CARTESIAN_POINT('Ctrl Pts',(-5.90693139713842,7.30536645755135,-7.90896180009433));
#78976=CARTESIAN_POINT('Ctrl Pts',(-9.33114753737324,-1.02913341322142,
-7.59143419823135));
#78977=CARTESIAN_POINT('Ctrl Pts',(-5.06288718129553,-7.13615744648993,
-7.32682786334546));
#78978=CARTESIAN_POINT('Ctrl Pts',(0.282080472971771,-8.25978418785034,
-7.11514279543679));
#78979=CARTESIAN_POINT('Ctrl Pts',(4.20506961446584,-7.13536625924996,-6.95637899450525));
#78980=CARTESIAN_POINT('Ctrl Pts',(7.08484849173346,-4.25540205710899,-6.79761519357375));
#78981=CARTESIAN_POINT('Ctrl Pts',(8.69974310962545,0.977670696977567,-6.58593012566506));
#78982=CARTESIAN_POINT('Ctrl Pts',(6.07415073499534,6.30747839594202,-6.37424505775635));
#78983=CARTESIAN_POINT('Ctrl Pts',(0.945810251189927,8.20195241914058,-6.16255998984768));
#78984=CARTESIAN_POINT('Ctrl Pts',(-4.45311911750285,7.53158019018864,-5.95087492193897));
#78985=CARTESIAN_POINT('Ctrl Pts',(-9.22342332430518,1.7856874837389,-5.68626858705313));
#78986=CARTESIAN_POINT('Ctrl Pts',(-6.47651097789812,-6.79589843234738,
-5.36874098519009));
#78987=CARTESIAN_POINT('Ctrl Pts',(0.72154030475446,-8.71991681704676,-5.10413465030423));
#78988=CARTESIAN_POINT('Ctrl Pts',(5.5344611246646,-6.13786154001214,-4.89244958239554));
#78989=CARTESIAN_POINT('Ctrl Pts',(7.81187504978943,-2.75148511283057,-4.73368578146402));
#78990=CARTESIAN_POINT('Ctrl Pts',(8.16070458243695,1.30630223086348,-4.57492198053251));
#78991=CARTESIAN_POINT('Ctrl Pts',(6.02656608207569,6.3499505106843,-4.36323691262381));
#78992=CARTESIAN_POINT('Ctrl Pts',(0.585773187827785,8.73707391119004,-4.15155184471514));
#78993=CARTESIAN_POINT('Ctrl Pts',(-4.55777208499541,6.88427877071814,-3.93986677680643));
#78994=CARTESIAN_POINT('Ctrl Pts',(-8.25678610342815,2.89490126967677,-3.72818170889775));
#78995=CARTESIAN_POINT('Ctrl Pts',(-8.20661254286858,-4.57293423128735,
-3.46357537401188));
#78996=CARTESIAN_POINT('Ctrl Pts',(-0.579112413890349,-9.36984844932824,
-3.14604777214886));
#78997=CARTESIAN_POINT('Ctrl Pts',(6.1669773963677,-6.20692831038676,-2.88144143726299));
#78998=CARTESIAN_POINT('Ctrl Pts',(8.18666879455784,-1.13227957945813,-2.6697563693543));
#78999=CARTESIAN_POINT('Ctrl Pts',(7.74854456684722,2.92508534373634,-2.51099256842279));
#79000=CARTESIAN_POINT('Ctrl Pts',(5.40253881524966,6.25428554111442,-2.35222876749126));
#79001=CARTESIAN_POINT('Ctrl Pts',(0.522018750725154,8.73892962582191,-2.14054369958259));
#79002=CARTESIAN_POINT('Ctrl Pts',(-5.17781107492739,7.06185842452563,-1.92885863167389));
#79003=CARTESIAN_POINT('Ctrl Pts',(-7.92004273489733,2.33227065248713,-1.7171735637652));
#79004=CARTESIAN_POINT('Ctrl Pts',(-8.18129567364406,-3.10185273179549,
-1.50548849585651));
#79005=CARTESIAN_POINT('Ctrl Pts',(-3.3342022501132,-8.78310787063445,-1.24088216097064));
#79006=CARTESIAN_POINT('Ctrl Pts',(5.59034459280216,-7.54172942161662,-0.923354559107611));
#79007=CARTESIAN_POINT('Ctrl Pts',(8.71510519418105,-0.777787096713387,
-0.658748224221747));
#79008=CARTESIAN_POINT('Ctrl Pts',(6.9926161408468,4.40520249985987,-0.447063156313067));
#79009=CARTESIAN_POINT('Ctrl Pts',(4.0449198585628,7.22754166127095,-0.288299355381536));
#79010=CARTESIAN_POINT('Ctrl Pts',(0.106014671877446,8.26366028978802,-0.129535554450031));
#79011=CARTESIAN_POINT('Ctrl Pts',(-5.22740533349617,7.02280198980525,0.0821495134586626));
#79012=CARTESIAN_POINT('Ctrl Pts',(-8.50950193961704,2.06777617761388,0.293834581367354));
#79013=CARTESIAN_POINT('Ctrl Pts',(-7.56051702525706,-3.31418768618381,
0.505519649276039));
#79014=CARTESIAN_POINT('Ctrl Pts',(-4.26407274969228,-7.64431327803062,
0.717204717184737));
#79015=CARTESIAN_POINT('Ctrl Pts',(3.10878881347585,-8.86048504611851,0.98181105207059));
#79016=CARTESIAN_POINT('Ctrl Pts',(9.12640894070192,-2.18142751875103,1.29933865393363));
#79017=CARTESIAN_POINT('Ctrl Pts',(6.78905718875035,6.47755113143582,1.61686625579666));
#79018=CARTESIAN_POINT('Ctrl Pts',(-1.77209850624849,9.22130305452722,1.93439385765969));
#79019=CARTESIAN_POINT('Ctrl Pts',(-7.53151392432143,4.46028473475584,2.19900019254556));
#79020=CARTESIAN_POINT('Ctrl Pts',(-8.20126862571526,-0.940452357811408,
2.41068526045425));
#79021=CARTESIAN_POINT('Ctrl Pts',(-6.31313511243949,-6.06890819119358,
2.62237032836292));
#79022=CARTESIAN_POINT('Ctrl Pts',(-0.98346979200203,-8.69932764510544,
2.83405539627164));
#79023=CARTESIAN_POINT('Ctrl Pts',(4.24990731598581,-7.08784934244536,3.04574046418029));
#79024=CARTESIAN_POINT('Ctrl Pts',(7.13240843508565,-4.21040200488291,3.20450426511184));
#79025=CARTESIAN_POINT('Ctrl Pts',(8.25950763414373,-0.288137466365907,
3.36326806604334));
#79026=CARTESIAN_POINT('Ctrl Pts',(7.13993645585559,5.05760009488693,3.57495313395204));
#79027=CARTESIAN_POINT('Ctrl Pts',(1.03598505156533,9.33040032946519,3.83955946883789));
#79028=CARTESIAN_POINT('Ctrl Pts',(-7.3009930326274,5.91230828436634,4.15708707070094));
#79029=CARTESIAN_POINT('Ctrl Pts',(-8.63087863833863,-1.43632280480546,
4.42169340558678));
#79030=CARTESIAN_POINT('Ctrl Pts',(-5.67064872171571,-6.00085880470096,
4.63337847349549));
#79031=CARTESIAN_POINT('Ctrl Pts',(-0.920958701171648,-8.70812304727144,
4.84506354140417));
#79032=CARTESIAN_POINT('Ctrl Pts',(4.84856161677379,-7.28922799955687,5.05674860931286));
#79033=CARTESIAN_POINT('Ctrl Pts',(7.81587547206024,-2.68618761171285,5.26843367722155));
#79034=CARTESIAN_POINT('Ctrl Pts',(8.16795894400251,1.37131829333971,5.42719747815307));
#79035=CARTESIAN_POINT('Ctrl Pts',(6.50489685689283,5.09803098058757,5.58596127908458));
#79036=CARTESIAN_POINT('Ctrl Pts',(2.20596801611654,8.46706999908836,5.79764634699328));
#79037=CARTESIAN_POINT('Ctrl Pts',(-5.21537996581248,7.80571860647714,6.06225268187913));
#79038=CARTESIAN_POINT('Ctrl Pts',(-9.39300825854191,-0.177799795868655,
6.37978028374218));
#79039=CARTESIAN_POINT('Ctrl Pts',(-5.67853477082882,-6.65651657967052,
6.64438661862803));
#79040=CARTESIAN_POINT('Ctrl Pts',(-0.474498931446816,-8.2426592393341,
6.85607168653673));
#79041=CARTESIAN_POINT('Ctrl Pts',(4.90272240285487,-7.25554297056533,7.06775675444541));
#79042=CARTESIAN_POINT('Ctrl Pts',(8.40327910514793,-2.45484633139196,7.27944182235409));
#79043=CARTESIAN_POINT('Ctrl Pts',(7.70955934364213,2.97761977542913,7.49112689026279));
#79044=CARTESIAN_POINT('Ctrl Pts',(5.36622392380833,6.30870057295464,7.64989069119431));
#79045=CARTESIAN_POINT('Ctrl Pts',(1.6941218394773,8.08910102655353,7.80865449212583));
#79046=CARTESIAN_POINT('Ctrl Pts',(-3.76434957606231,7.89855948745089,8.02033956003451));
#79047=CARTESIAN_POINT('Ctrl Pts',(-9.01650939318612,2.61380724465366,8.28494589492038));
#79048=CARTESIAN_POINT('Ctrl Pts',(-7.07203126861679,-6.18438285883276,
8.6024734967834));
#79049=CARTESIAN_POINT('Ctrl Pts',(-0.0583375627661657,-8.7493752213905,
8.86707983166928));
#79050=CARTESIAN_POINT('Ctrl Pts',(4.94458078750979,-6.61193627864721,9.07876489957795));
#79051=CARTESIAN_POINT('Ctrl Pts',(8.42302820519816,-2.39419855508166,9.29044996748667));
#79052=CARTESIAN_POINT('Ctrl Pts',(8.01001140115047,3.53285826472605,9.50213503539534));
#79053=CARTESIAN_POINT('Ctrl Pts',(3.98117591724546,7.24249702343123,9.71382010330402));
#79054=CARTESIAN_POINT('Ctrl Pts',(0.0433567145999381,8.28216048573352,
9.87258390423556));
#79055=CARTESIAN_POINT('Ctrl Pts',(-3.91257719470531,7.2797901012712,10.0313477051671));
#79056=CARTESIAN_POINT('Ctrl Pts',(-7.9661191375803,3.61918714596217,10.2430327730758));
#79057=CARTESIAN_POINT('Ctrl Pts',(-8.58154747046168,-3.80610995094048,
10.5076391079616));
#79058=CARTESIAN_POINT('Ctrl Pts',(-1.42850782747337,-9.28545006967693,
10.8251667098247));
#79059=CARTESIAN_POINT('Ctrl Pts',(5.58926749016992,-6.7316460809816,11.0897730447105));
#79060=CARTESIAN_POINT('Ctrl Pts',(8.0406222609218,-1.8748264383621,11.3014581126192));
#79061=CARTESIAN_POINT('Ctrl Pts',(7.98606895318656,3.59197627246583,11.5131431805279));
#79062=CARTESIAN_POINT('Ctrl Pts',(3.85352014488595,7.86077303183749,11.7248282484366));
#79063=CARTESIAN_POINT('Ctrl Pts',(-1.61762369862161,8.1047404886354,11.9365133163453));
#79064=CARTESIAN_POINT('Ctrl Pts',(-5.299880128958,6.36453711866289,12.0952771172768));
#79065=CARTESIAN_POINT('Ctrl Pts',(-7.68108875049532,3.05032454504364,12.2540409182083));
#79066=CARTESIAN_POINT('Ctrl Pts',(-8.42528638730484,-2.36053362685826,
12.465725986117));
#79067=CARTESIAN_POINT('Ctrl Pts',(-4.11484577036667,-8.43785957648776,
12.7303323210029));
#79068=CARTESIAN_POINT('Ctrl Pts',(4.88615002749256,-8.02407349906823,13.0478599228659));
#79069=CARTESIAN_POINT('Ctrl Pts',(8.61095080285362,-1.55128859568458,13.3124662577518));
#79070=CARTESIAN_POINT('Ctrl Pts',(7.35905873746818,3.74310499656434,13.5241513256605));
#79071=CARTESIAN_POINT('Ctrl Pts',(3.79713466688552,7.89058674551804,13.7358363935691));
#79072=CARTESIAN_POINT('Ctrl Pts',(-2.11341270190033,8.4955786687284,13.9475214614779));
#79073=CARTESIAN_POINT('Ctrl Pts',(-6.45643942659223,5.15925525141111,14.1592065293865));
#79074=CARTESIAN_POINT('Ctrl Pts',(-8.15315375718723,1.45675870610943,14.3179703303181));
#79075=CARTESIAN_POINT('Ctrl Pts',(-7.84090954781147,-2.61222925604173,
14.4767341312496));
#79076=CARTESIAN_POINT('Ctrl Pts',(-4.92612766124713,-7.23124027928325,
14.6884191991583));
#79077=CARTESIAN_POINT('Ctrl Pts',(2.28507222059734,-9.10537615330006,14.9530255340441));
#79078=CARTESIAN_POINT('Ctrl Pts',(8.90522127729204,-2.99286678822828,15.2705531359072));
#79079=CARTESIAN_POINT('Ctrl Pts',(7.58708021122468,4.35788755071873,15.535159470793));
#79080=CARTESIAN_POINT('Ctrl Pts',(3.22009898808751,7.60246953454795,15.7468445387017));
#79081=CARTESIAN_POINT('Ctrl Pts',(-2.17575046625231,8.48208115827781,15.9585296066104));
#79082=CARTESIAN_POINT('Ctrl Pts',(-7.08743254716731,5.13903396120905,16.1702146745191));
#79083=CARTESIAN_POINT('Ctrl Pts',(-8.26192302571686,-0.210125523431927,
16.3818997424278));
#79084=CARTESIAN_POINT('Ctrl Pts',(-7.17595340292437,-4.13542680689911,
16.5406635433593));
#79085=CARTESIAN_POINT('Ctrl Pts',(-4.31695337778056,-7.04751855316114,
16.6994273442908));
#79086=CARTESIAN_POINT('Ctrl Pts',(0.887399762225084,-8.70460173549805,
16.9111124121995));
#79087=CARTESIAN_POINT('Ctrl Pts',(7.6114289922114,-5.49505037674401,17.1757187470854));
#79088=CARTESIAN_POINT('Ctrl Pts',(8.74048593802383,3.44443365109889,17.4932463489484));
#79089=CARTESIAN_POINT('Ctrl Pts',(2.99868548357566,8.21966273072438,17.7578526838342));
#79090=CARTESIAN_POINT('Ctrl Pts',(-2.43171158715242,7.89007980147984,17.9695377517429));
#79091=CARTESIAN_POINT('Ctrl Pts',(-7.12643538072904,5.08856655958259,18.1812228196516));
#79092=CARTESIAN_POINT('Ctrl Pts',(-8.7316702267711,-0.631906018348646,
18.3929078875603));
#79093=CARTESIAN_POINT('Ctrl Pts',(-6.18583120778734,-5.48078617419366,
18.604592955469));
#79094=CARTESIAN_POINT('Ctrl Pts',(-2.82738245660738,-7.7847267492334,18.7633567564005));
#79095=CARTESIAN_POINT('Ctrl Pts',(1.23517226993769,-8.17177787795647,18.922120557332));
#79096=CARTESIAN_POINT('Ctrl Pts',(6.28401346095891,-6.08841067390496,19.1338056252407));
#79097=CARTESIAN_POINT('Ctrl Pts',(9.36182220511659,0.696932526300606,19.3984119601266));
#79098=CARTESIAN_POINT('Ctrl Pts',(4.46933914411785,8.26348747348669,19.7159395619896));
#79099=CARTESIAN_POINT('Ctrl Pts',(-2.99853668295097,8.21971701442728,19.9805458968755));
#79100=CARTESIAN_POINT('Ctrl Pts',(-6.94106756814404,4.47081217803551,20.1922309647842));
#79101=CARTESIAN_POINT('Ctrl Pts',(-8.72901401305323,-0.695632968545975,
20.4039160326929));
#79102=CARTESIAN_POINT('Ctrl Pts',(-6.27363820517334,-6.10596706801597,
20.6156011006015));
#79103=CARTESIAN_POINT('Ctrl Pts',(-1.20354306299133,-8.17649123487534,
20.8272861685103));
#79104=CARTESIAN_POINT('Ctrl Pts',(2.84953519592018,-7.77664524607966,20.9860499694417));
#79105=CARTESIAN_POINT('Ctrl Pts',(6.2069954500714,-5.45681332884632,21.1448137703733));
#79106=CARTESIAN_POINT('Ctrl Pts',(8.72830333694957,-0.611792914169276,
21.356498838282));
#79107=CARTESIAN_POINT('Ctrl Pts',(6.71389086124484,6.56148607022255,21.6211051731678));
#79108=CARTESIAN_POINT('Ctrl Pts',(-1.90157024722326,9.20023087778187,21.9386327750308));
#79109=CARTESIAN_POINT('Ctrl Pts',(-7.58700131936631,4.35802489852905,22.2032391099167));
#79110=CARTESIAN_POINT('Ctrl Pts',(-8.18940584699088,-1.04891009628249,
22.4149241778254));
#79111=CARTESIAN_POINT('Ctrl Pts',(-6.23057087324017,-6.15301368928593,
22.6266092457341));
#79112=CARTESIAN_POINT('Ctrl Pts',(-0.868156811692852,-8.71135316213372,
22.8382943136427));
#79113=CARTESIAN_POINT('Ctrl Pts',(4.34418767333381,-7.03075801584175,23.0499793815515));
#79114=CARTESIAN_POINT('Ctrl Pts',(7.18769845288102,-4.11497910889147,23.208743182483));
#79115=CARTESIAN_POINT('Ctrl Pts',(8.26267902471989,-0.178155992140028,
23.3675069834145));
#79116=CARTESIAN_POINT('Ctrl Pts',(7.07190532710078,5.15225433729316,23.5791920513232));
#79117=CARTESIAN_POINT('Ctrl Pts',(0.911672841174965,9.34335499577618,23.8437983862091));
#79118=CARTESIAN_POINT('Ctrl Pts',(-7.37909340118962,5.81456775574379,24.1613259880721));
#79119=CARTESIAN_POINT('Ctrl Pts',(-8.6109788843406,-1.55113271182926,24.425932322958));
#79120=CARTESIAN_POINT('Ctrl Pts',(-5.59023836755192,-6.07583866727565,
24.6376173908666));
#79121=CARTESIAN_POINT('Ctrl Pts',(-0.804912040360767,-8.71961624581554,
24.8493024587754));
#79122=CARTESIAN_POINT('Ctrl Pts',(4.94519767960346,-7.22401481689722,25.060987526684));
#79123=CARTESIAN_POINT('Ctrl Pts',(7.85095385123881,-2.5818691764276,25.2726725945928));
#79124=CARTESIAN_POINT('Ctrl Pts',(8.14897311707001,1.47996596360603,25.4314363955242));
#79125=CARTESIAN_POINT('Ctrl Pts',(6.4364320026378,5.18420170310737,25.5902001964558));
#79126=CARTESIAN_POINT('Ctrl Pts',(2.09302007257951,8.49569518564614,25.8018852643645));
#79127=CARTESIAN_POINT('Ctrl Pts',(-5.31886276036888,7.73557553662241,26.0664915992503));
#79128=CARTESIAN_POINT('Ctrl Pts',(-9.38980774356954,-0.302866552159413,
26.3840192011134));
#79129=CARTESIAN_POINT('Ctrl Pts',(-5.58938935189839,-6.7315448976555,26.6486255359992));
#79130=CARTESIAN_POINT('Ctrl Pts',(-0.36469301513852,-8.24824705749777,
26.8603106039079));
#79131=CARTESIAN_POINT('Ctrl Pts',(4.99890654770252,-7.18961224228023,27.0719956718166));
#79132=CARTESIAN_POINT('Ctrl Pts',(8.43522409269409,-2.34272590610575,27.2836807397253));
#79133=CARTESIAN_POINT('Ctrl Pts',(7.66922409732036,3.08002054596217,27.495365807634));
#79134=CARTESIAN_POINT('Ctrl Pts',(5.28173792622925,6.37960081782495,27.6541296085655));
#79135=CARTESIAN_POINT('Ctrl Pts',(1.58625263971785,8.11094364337897,27.812893409497));
#79136=CARTESIAN_POINT('Ctrl Pts',(-3.86919742019125,7.84773094819247,28.0245784774057));
#79137=CARTESIAN_POINT('Ctrl Pts',(-9.05051682149315,2.49350660923522,28.2891848122916));
#79138=CARTESIAN_POINT('Ctrl Pts',(-6.98904950325245,-6.27800960900046,
28.6067124141546));
#79139=CARTESIAN_POINT('Ctrl Pts',(0.0581791732242141,-8.74937627605938,
28.8713187490405));
#79140=CARTESIAN_POINT('Ctrl Pts',(5.03219058842161,-6.54550520575857,29.0830038169491));
#79141=CARTESIAN_POINT('Ctrl Pts',(8.45416382536456,-2.28182051899467,29.2946888848579));
#79142=CARTESIAN_POINT('Ctrl Pts',(7.96225564688464,3.63921079064677,29.5063739527665));
#79143=CARTESIAN_POINT('Ctrl Pts',(3.88437777703145,7.29487039663986,29.7180590206752));
#79144=CARTESIAN_POINT('Ctrl Pts',(-0.0669370008521218,8.28200347464785,
29.8768228216067));
#79145=CARTESIAN_POINT('Ctrl Pts',(-4.00917201687075,7.22704254603652,30.0355866225382));
#79146=CARTESIAN_POINT('Ctrl Pts',(-8.01360790323876,3.51278494712968,30.2472716904469));
#79147=CARTESIAN_POINT('Ctrl Pts',(-8.53010226655877,-3.92004914107959,
30.5118780253328));
#79148=CARTESIAN_POINT('Ctrl Pts',(-1.30473092765309,-9.30364954284291,
30.8294056271958));
#79149=CARTESIAN_POINT('Ctrl Pts',(5.67841424972103,-6.65661938560647,31.0940119620817));
#79150=CARTESIAN_POINT('Ctrl Pts',(8.06487553978532,-1.76758678558764,31.3056970299904));
#79151=CARTESIAN_POINT('Ctrl Pts',(7.93752807350566,3.69800472543214,31.5173820978991));
#79152=CARTESIAN_POINT('Ctrl Pts',(3.74850001544698,7.91139164744737,31.7290671658077));
#79153=CARTESIAN_POINT('Ctrl Pts',(-1.725407512423,8.08248066713078,31.9407522337164));
#79154=CARTESIAN_POINT('Ctrl Pts',(-5.38416392046695,6.29339661817871,32.0995160346479));
#79155=CARTESIAN_POINT('Ctrl Pts',(-7.72102749773726,2.94776841055509,32.2582798355795));
#79156=CARTESIAN_POINT('Ctrl Pts',(-8.39310514002376,-2.47252013543657,
32.4699649034881));
#79157=CARTESIAN_POINT('Ctrl Pts',(-4.00211766288754,-8.49190698010957,
32.734571238374));
#79158=CARTESIAN_POINT('Ctrl Pts',(4.99256981673248,-7.95829530959158,33.052098840237));
#79159=CARTESIAN_POINT('Ctrl Pts',(8.63084510062077,-1.43648281763411,33.316705175123));
#79160=CARTESIAN_POINT('Ctrl Pts',(7.30856093990772,3.84077043110713,33.5283902430316));
#79161=CARTESIAN_POINT('Ctrl Pts',(3.69172252105726,7.94045185707503,33.7400753109404));
#79162=CARTESIAN_POINT('Ctrl Pts',(-2.2263571737631,8.46668198882771,33.9517603788489));
#79163=CARTESIAN_POINT('Ctrl Pts',(-6.52457046083469,5.07282023336842,34.1634454467577));
#79164=CARTESIAN_POINT('Ctrl Pts',(-8.17182983472982,1.34805759089933,34.3222092476892));
#79165=CARTESIAN_POINT('Ctrl Pts',(-7.80542839734849,-2.71641155883038,
34.4809730486207));
#79166=CARTESIAN_POINT('Ctrl Pts',(-4.82939563391592,-7.29619815539201,
34.6926581165294));
#79167=CARTESIAN_POINT('Ctrl Pts',(2.40612187514562,-9.0741394891403,34.9572644514153));
#79168=CARTESIAN_POINT('Ctrl Pts',(8.94428634201623,-2.87401451660175,35.2747920532783));
#79169=CARTESIAN_POINT('Ctrl Pts',(7.52837540758014,4.45853493412458,35.5393983881642));
#79170=CARTESIAN_POINT('Ctrl Pts',(3.11857473717401,7.64467606412931,35.7510834560729));
#79171=CARTESIAN_POINT('Ctrl Pts',(-2.28850967028801,8.45235555073301,35.9627685239815));
#79172=CARTESIAN_POINT('Ctrl Pts',(-7.15523835371221,5.04419807964279,36.1744535918902));
#79173=CARTESIAN_POINT('Ctrl Pts',(-8.25839229812943,-0.320127269480299,
36.3861386597989));
#79174=CARTESIAN_POINT('Ctrl Pts',(-7.12024746501521,-4.23061912172507,
36.5449024607304));
#79175=CARTESIAN_POINT('Ctrl Pts',(-4.22272190653533,-7.10438061502535,
36.703666261662));
#79176=CARTESIAN_POINT('Ctrl Pts',(1.00323641159163,-8.69201279417427,36.9153513295706));
#79177=CARTESIAN_POINT('Ctrl Pts',(7.68392924963401,-5.39320509836674,37.1799576644565));
#79178=CARTESIAN_POINT('Ctrl Pts',(8.69384292460902,3.56052142415137,37.4974852663195));
#79179=CARTESIAN_POINT('Ctrl Pts',(2.8889619762041,8.25886606843306,37.7620916012054));
#79180=CARTESIAN_POINT('Ctrl Pts',(-2.53656467485294,7.8569981651455,37.973776669114));
#79181=CARTESIAN_POINT('Ctrl Pts',(-7.19356567683603,4.99321576942699,38.1854617370228));
#79182=CARTESIAN_POINT('Ctrl Pts',(-8.72248118257988,-0.748125781300136,
38.3971468049315));
#79183=CARTESIAN_POINT('Ctrl Pts',(-6.11229750717327,-5.56267417725245,
38.6088318728402));
#79184=CARTESIAN_POINT('Ctrl Pts',(-2.72346598880742,-7.82168748570094,
38.7675956737716));
#79185=CARTESIAN_POINT('Ctrl Pts',(1.34388270272352,-8.15460504895256,38.9263594747032));
#79186=CARTESIAN_POINT('Ctrl Pts',(6.36453293622773,-6.00418938869395,39.1380445426119));
#79187=CARTESIAN_POINT('Ctrl Pts',(9.35171135652741,0.821537978809482,39.4026508774977));
#79188=CARTESIAN_POINT('Ctrl Pts',(4.35890164019773,8.32227097015575,39.7201784793608));
#79189=CARTESIAN_POINT('Ctrl Pts',(-3.10772914375988,8.17905799009226,39.9847848142466));
#79190=CARTESIAN_POINT('Ctrl Pts',(-6.99998793858948,4.37798462496313,40.1964698821553));
#79191=CARTESIAN_POINT('Ctrl Pts',(-8.71897658075383,-0.811811709249727,
40.408154950064));
#79192=CARTESIAN_POINT('Ctrl Pts',(-6.19177146109914,-6.18896892370799,
40.6198400179727));
#79193=CARTESIAN_POINT('Ctrl Pts',(-1.09455362535609,-8.19179328228488,
40.8315250858814));
#79194=CARTESIAN_POINT('Ctrl Pts',(2.95284067765355,-7.73800969555844,40.9902888868129));
#79195=CARTESIAN_POINT('Ctrl Pts',(6.27911105175123,-5.3736736617381,41.1490526877445));
#79196=CARTESIAN_POINT('Ctrl Pts',(8.73567638035269,-0.495507708699551,
41.3607377556531));
#79197=CARTESIAN_POINT('Ctrl Pts',(6.62591913503577,6.65031018542722,41.625344090539));
#79198=CARTESIAN_POINT('Ctrl Pts',(-2.02391704506606,9.17409272921886,41.9428716924019));
#79199=CARTESIAN_POINT('Ctrl Pts',(-7.64436247696758,4.25660573191808,42.2074780272879));
#79200=CARTESIAN_POINT('Ctrl Pts',(-8.17471182597883,-1.15787178867669,
42.4191630951966));
#79201=CARTESIAN_POINT('Ctrl Pts',(-6.14808144885145,-6.23543786476111,
42.6308481631052));
#79202=CARTESIAN_POINT('Ctrl Pts',(-0.75207459260542,-8.72214159322487,
42.842533231014));
#79203=CARTESIAN_POINT('Ctrl Pts',(4.4374279746784,-6.97228497610427,43.0542182989226));
#79204=CARTESIAN_POINT('Ctrl Pts',(7.24185848301294,-4.01889883278679,43.2129820998541));
#79205=CARTESIAN_POINT('Ctrl Pts',(8.26431880344762,-0.0681097501406032,
43.3717459007857));
#79206=CARTESIAN_POINT('Ctrl Pts',(7.00266797220651,5.24597092849989,43.5834309686943));
#79207=CARTESIAN_POINT('Ctrl Pts',(0.787170674435132,9.35466687144652,43.8480373035802));
#79208=CARTESIAN_POINT('Ctrl Pts',(-7.45586913137561,5.71578805637648,44.1655649054432));
#79209=CARTESIAN_POINT('Ctrl Pts',(-8.58955960612328,-1.66566377433196,
44.4301712403291));
#79210=CARTESIAN_POINT('Ctrl Pts',(-5.50883342665449,-6.14974266080996,
44.6418563082378));
#79211=CARTESIAN_POINT('Ctrl Pts',(-0.68872539330883,-8.72956174155499,
44.8535413761465));
#79212=CARTESIAN_POINT('Ctrl Pts',(5.04095820523059,-7.15752125656805,45.0652264440551));
#79213=CARTESIAN_POINT('Ctrl Pts',(7.884639323544,-2.47709256106658,45.2769115119639));
#79214=CARTESIAN_POINT('Ctrl Pts',(8.12854250071157,1.5883510097858,45.4356753128953));
#79215=CARTESIAN_POINT('Ctrl Pts',(6.3668255657606,5.26945314413741,45.594439113827));
#79216=CARTESIAN_POINT('Ctrl Pts',(1.97970106770277,8.52281370171664,45.8061241817355));
#79217=CARTESIAN_POINT('Ctrl Pts',(-5.42140238140834,7.66406068382094,46.0707305166215));
#79218=CARTESIAN_POINT('Ctrl Pts',(-9.38494201594991,-0.427879617266375,
46.3882581184846));
#79219=CARTESIAN_POINT('Ctrl Pts',(-5.49925273618984,-6.80537944421727,
46.6528644533703));
#79220=CARTESIAN_POINT('Ctrl Pts',(-0.25482241716316,-8.25237214699649,
46.864549521279));
#79221=CARTESIAN_POINT('Ctrl Pts',(5.09420418711999,-7.12240651514204,47.0762345891877));
#79222=CARTESIAN_POINT('Ctrl Pts',(8.46567319292571,-2.23019002681052,47.2879196570964));
#79223=CARTESIAN_POINT('Ctrl Pts',(7.62752880020834,3.18187511075783,47.4996047250052));
#79224=CARTESIAN_POINT('Ctrl Pts',(5.19631527353026,6.44936971294384,47.6583685259366));
#79225=CARTESIAN_POINT('Ctrl Pts',(1.47810213580437,8.13134787714882,47.8171323268681));
#79226=CARTESIAN_POINT('Ctrl Pts',(-3.97335910607881,7.79551070333261,48.0288173947768));
#79227=CARTESIAN_POINT('Ctrl Pts',(-9.08291924414386,2.3727637789698,48.2934237296627));
#79228=CARTESIAN_POINT('Ctrl Pts',(-6.90482830967873,-6.37052302589617,
48.6109513315257));
#79229=CARTESIAN_POINT('Ctrl Pts',(0.174685591761263,-8.74782572873383,
48.8755576664116));
#79230=CARTESIAN_POINT('Ctrl Pts',(5.11890798781239,-6.4779133622736,49.0872427343203));
#79231=CARTESIAN_POINT('Ctrl Pts',(8.48380019609937,-2.16903782808714,49.298927802229));
#79232=CARTESIAN_POINT('Ctrl Pts',(7.91308787750832,3.74491794408583,49.5106128701377));
#79233=CARTESIAN_POINT('Ctrl Pts',(3.786890786771,7.34595010788508,49.7222979380464));
#79234=CARTESIAN_POINT('Ctrl Pts',(-0.177218845789058,8.28037774481689,
49.8810617389778));
#79235=CARTESIAN_POINT('Ctrl Pts',(-4.10505585816007,7.17301335733233,50.0398255399094));
#79236=CARTESIAN_POINT('Ctrl Pts',(-8.05967554704219,3.40575979599903,50.251510607818));
#79237=CARTESIAN_POINT('Ctrl Pts',(-8.47714434642404,-4.03329315526637,
50.5161169427039));
#79238=CARTESIAN_POINT('Ctrl Pts',(-1.18072264870137,-9.32019912000061,
50.833644544567));
#79239=CARTESIAN_POINT('Ctrl Pts',(5.76655400734678,-6.58041221479475,51.0982508794527));
#79240=CARTESIAN_POINT('Ctrl Pts',(8.08769860506414,-1.66003367148095,51.3099359473616));
#79241=CARTESIAN_POINT('Ctrl Pts',(7.88757956386002,3.80337737948872,51.5216210152701));
#79242=CARTESIAN_POINT('Ctrl Pts',(3.64281513233217,7.96060726808723,51.7333060831789));
#79243=CARTESIAN_POINT('Ctrl Pts',(-1.83288534490189,8.05878750997495,51.9449911510876));
#79244=CARTESIAN_POINT('Ctrl Pts',(-5.46749289199121,6.22114005566518,52.1037549520191));
#79245=CARTESIAN_POINT('Ctrl Pts',(-7.75959700890935,2.84468952300543,52.2625187529506));
#79246=CARTESIAN_POINT('Ctrl Pts',(-8.35943547140671,-2.58406817081551,
52.4742038208594));
#79247=CARTESIAN_POINT('Ctrl Pts',(-3.88867982549927,-8.54444844097074,
52.7388101557451));
#79248=CARTESIAN_POINT('Ctrl Pts',(5.09810423065285,-7.89110580736366,53.0563377576083));
#79249=CARTESIAN_POINT('Ctrl Pts',(8.64920881668602,-1.32142229568139,53.320944092494));
#79250=CARTESIAN_POINT('Ctrl Pts',(7.25676705235914,3.93775474876736,53.5326291604028));
#79251=CARTESIAN_POINT('Ctrl Pts',(3.58565569081256,7.98890882043448,53.7443142283114));
#79252=CARTESIAN_POINT('Ctrl Pts',(-2.33890682745132,8.43628383901313,53.9559992962201));
#79253=CARTESIAN_POINT('Ctrl Pts',(-6.5915444359622,4.98548560925594,54.1676843641289));
#79254=CARTESIAN_POINT('Ctrl Pts',(-8.1890567337444,1.23911741167084,54.3264481650602));
#79255=CARTESIAN_POINT('Ctrl Pts',(-7.76856303931412,-2.82011213449629,
54.485211965992));
#79256=CARTESIAN_POINT('Ctrl Pts',(-4.73180717700486,-7.35986213958475,
54.6968970339004));
#79257=CARTESIAN_POINT('Ctrl Pts',(2.52674484922246,-9.04129361855733,54.9615033687864));
#79258=CARTESIAN_POINT('Ctrl Pts',(8.98176520865567,-2.75465259123618,55.2790309706494));
#79259=CARTESIAN_POINT('Ctrl Pts',(7.46833558457723,4.55839168067677,55.5436373055353));
#79260=CARTESIAN_POINT('Ctrl Pts',(3.0164973733366,7.68552685322903,55.7553223734439));
#79261=CARTESIAN_POINT('Ctrl Pts',(-2.40086285480069,8.42113112897703,55.9670074413527));
#79262=CARTESIAN_POINT('Ctrl Pts',(-7.22177562331924,4.94846743427247,56.1786925092613));
#79263=CARTESIAN_POINT('Ctrl Pts',(-8.25339659055917,-0.430071956849194,
56.3903775771701));
#79264=CARTESIAN_POINT('Ctrl Pts',(-7.06327976561099,-4.3250617833591,56.5491413781016));
#79265=CARTESIAN_POINT('Ctrl Pts',(-4.12773988185095,-7.15998170391512,
56.7079051790331));
#79266=CARTESIAN_POINT('Ctrl Pts',(1.11889147120648,-8.67788478346445,56.9195902469418));
#79267=CARTESIAN_POINT('Ctrl Pts',(7.7550744568542,-5.29039851498598,57.1841965818276));
#79268=CARTESIAN_POINT('Ctrl Pts',(8.64564486962893,3.67596925206309,57.5017241836908));
#79269=CARTESIAN_POINT('Ctrl Pts',(2.77874843057585,8.29661909249389,57.7663305185765));
#79270=CARTESIAN_POINT('Ctrl Pts',(-2.64099760384767,7.82250413811996,57.9780155864852));
#79271=CARTESIAN_POINT('Ctrl Pts',(-7.25934386865709,4.89702852333033,58.189700654394));
#79272=CARTESIAN_POINT('Ctrl Pts',(-8.71190066743893,-0.86431257451617,
58.4013857223026));
#79273=CARTESIAN_POINT('Ctrl Pts',(-6.03748787940653,-5.6434525015018,58.6130707902113));
#79274=CARTESIAN_POINT('Ctrl Pts',(-2.61946603419042,-7.85751750355384,
58.7718345911428));
#79275=CARTESIAN_POINT('Ctrl Pts',(1.45308347512525,-8.13551848137901,58.9305983920743));
#79276=CARTESIAN_POINT('Ctrl Pts',(6.44234932446726,-5.91991369584324,59.1422834599831));
#79277=CARTESIAN_POINT('Ctrl Pts',(9.34319950749135,0.948088200591955,59.4068897948688));
#79278=CARTESIAN_POINT('Ctrl Pts',(4.24199828795001,8.37592502394999,59.7244173967321));
#79279=CARTESIAN_POINT('Ctrl Pts',(-3.20680410262386,8.14308925527156,59.9890237316177));
#79280=CARTESIAN_POINT('Ctrl Pts',(-7.07054001980459,4.27610841771073,60.2007087995265));
#79281=CARTESIAN_POINT('Ctrl Pts',(-8.27146334671563,0.390452602810304,
60.359472600458));
#79282=CARTESIAN_POINT('Ctrl Pts',(-7.44101921670096,-3.62419448168208,
60.5182430956361));
#79283=CARTESIAN_POINT('Ctrl Pts',(-5.68421081081461,-5.69823456483541,
60.6240923238372));
#79284=CARTESIAN_POINT('Ctrl Pts',(-4.60927878647134,-6.46465601021938,
60.6770202850609));
#79285=CARTESIAN_POINT('Ctrl Pts',(-3.42485771374982,7.13737126555386,59.9999999999999));
#79286=CARTESIAN_POINT('Ctrl Pts',(-3.60849199590157,7.03465838837373,59.9999999999999));
#79287=CARTESIAN_POINT('Ctrl Pts',(-3.78755911055656,6.92445885384906,60.));
#79288=CARTESIAN_POINT('Ctrl Pts',(-3.96154458364211,6.80675795931572,60.));
#79289=CARTESIAN_POINT('Ctrl Pts',(-4.13247087319123,6.69112659755657,60.));
#79290=CARTESIAN_POINT('Ctrl Pts',(-4.2984929941888,6.56825460060961,60.));
#79291=CARTESIAN_POINT('Ctrl Pts',(-4.45931652738607,6.43861171335742,60.));
#79292=CARTESIAN_POINT('Ctrl Pts',(-4.62009538315812,6.30900484142145,60.));
#79293=CARTESIAN_POINT('Ctrl Pts',(-4.77567893444557,6.17263015411101,60.));
#79294=CARTESIAN_POINT('Ctrl Pts',(-4.92573131027231,6.02992581332935,60.));
#79295=CARTESIAN_POINT('Ctrl Pts',(-4.96262713058505,5.99483677401014,60.));
#79296=CARTESIAN_POINT('Ctrl Pts',(-4.99918832229332,5.95936492333879,60.));
#79297=CARTESIAN_POINT('Ctrl Pts',(-5.03540946333644,5.9235165595251,60.));
#79298=CARTESIAN_POINT('Ctrl Pts',(-5.06052699232729,5.89865753268521,60.));
#79299=CARTESIAN_POINT('Ctrl Pts',(-5.08548260315889,5.87361570900131,60.));
#79300=CARTESIAN_POINT('Ctrl Pts',(-5.11025822621535,5.84840998085388,60.0000000000001));
#79301=CARTESIAN_POINT('Ctrl Pts',(-5.25368359056449,5.70249475058922,60.0000000000001));
#79302=CARTESIAN_POINT('Ctrl Pts',(-5.39120059555047,5.55097235209628,60.));
#79303=CARTESIAN_POINT('Ctrl Pts',(-5.52252818805357,5.39430470386248,60.));
#79304=CARTESIAN_POINT('Ctrl Pts',(-5.65352735584239,5.2380288508838,60.0000000000001));
#79305=CARTESIAN_POINT('Ctrl Pts',(-5.77836838570734,5.076632761517,60.));
#79306=CARTESIAN_POINT('Ctrl Pts',(-5.89672849428091,4.91054798451264,60.));
#79307=CARTESIAN_POINT('Ctrl Pts',(-6.00771815129665,4.75480554174704,60.));
#79308=CARTESIAN_POINT('Ctrl Pts',(-6.11300877241676,4.5949394925689,60.));
#79309=CARTESIAN_POINT('Ctrl Pts',(-6.21229482069967,4.43129207005651,60.));
#79310=CARTESIAN_POINT('Ctrl Pts',(-6.23475787616974,4.39426752136105,60.));
#79311=CARTESIAN_POINT('Ctrl Pts',(-6.25691341041412,4.35704937873796,60.));
#79312=CARTESIAN_POINT('Ctrl Pts',(-6.27875759151048,4.31964155207945,60.));
#79313=CARTESIAN_POINT('Ctrl Pts',(-6.2951680303997,4.29153892600024,60.));
#79314=CARTESIAN_POINT('Ctrl Pts',(-6.31140442788322,4.26332614950814,60.));
#79315=CARTESIAN_POINT('Ctrl Pts',(-6.32745245424683,4.23502760248424,60.));
#79316=CARTESIAN_POINT('Ctrl Pts',(-6.38414409403106,4.13505948192255,60.));
#79317=CARTESIAN_POINT('Ctrl Pts',(-6.43851755582811,4.03396718679547,60.));
#79318=CARTESIAN_POINT('Ctrl Pts',(-6.4905241514475,3.93183211822126,60.));
#79319=CARTESIAN_POINT('Ctrl Pts',(-6.58454597607521,3.74718389444401,60.));
#79320=CARTESIAN_POINT('Ctrl Pts',(-6.67083516273044,3.55912849623771,59.9999999999999));
#79321=CARTESIAN_POINT('Ctrl Pts',(-6.74928129002232,3.36812873857614,59.9999999999999));
#79322=CARTESIAN_POINT('Ctrl Pts',(-6.82527147153296,3.18310869036922,59.9999999999999));
#79323=CARTESIAN_POINT('Ctrl Pts',(-6.89390186093913,2.99532499045739,59.9999999999999));
#79324=CARTESIAN_POINT('Ctrl Pts',(-6.95502099206733,2.80518508079014,59.9999999999999));
#79325=CARTESIAN_POINT('Ctrl Pts',(-7.01575663887716,2.61623818012524,59.9999999999999));
#79326=CARTESIAN_POINT('Ctrl Pts',(-7.069075069887,2.42496390511742,60.));
#79327=CARTESIAN_POINT('Ctrl Pts',(-7.11477647237383,2.23175902296667,60.));
#79328=CARTESIAN_POINT('Ctrl Pts',(-7.1597701772088,2.04154596675526,59.9999999999999));
#79329=CARTESIAN_POINT('Ctrl Pts',(-7.19738093165887,1.84946105664228,59.9999999999999));
#79330=CARTESIAN_POINT('Ctrl Pts',(-7.22736781049597,1.65588890955698,60.));
#79331=CARTESIAN_POINT('Ctrl Pts',(-7.23119593616582,1.63117748462834,60.));
#79332=CARTESIAN_POINT('Ctrl Pts',(-7.23489974672764,1.60644183693712,60.));
#79333=CARTESIAN_POINT('Ctrl Pts',(-7.23847868072504,1.58168278120198,60.));
#79334=CARTESIAN_POINT('Ctrl Pts',(-7.24275065143607,1.55212929935218,60.));
#79335=CARTESIAN_POINT('Ctrl Pts',(-7.24684510735891,1.52253890325882,59.9999999999999));
#79336=CARTESIAN_POINT('Ctrl Pts',(-7.25075778712086,1.49293926291434,59.9999999999999));
#79337=CARTESIAN_POINT('Ctrl Pts',(-7.27632909266145,1.29949091211867,60.));
#79338=CARTESIAN_POINT('Ctrl Pts',(-7.29417366705118,1.10543161726051,59.9999999999999));
#79339=CARTESIAN_POINT('Ctrl Pts',(-7.30417158068525,0.911143029985696,
60.));
#79340=CARTESIAN_POINT('Ctrl Pts',(-7.31396241695766,0.720878559093373,
60.));
#79341=CARTESIAN_POINT('Ctrl Pts',(-7.31622819308078,0.530393618398438,
60.));
#79342=CARTESIAN_POINT('Ctrl Pts',(-7.31080782602039,0.340046611414723,
60.));
#79343=CARTESIAN_POINT('Ctrl Pts',(-7.30524905362152,0.144839224749122,
60.));
#79344=CARTESIAN_POINT('Ctrl Pts',(-7.29160651157262,-0.0502238645111097,
60.));
#79345=CARTESIAN_POINT('Ctrl Pts',(-7.27000990910251,-0.244634982193785,
60.));
#79346=CARTESIAN_POINT('Ctrl Pts',(-7.24855927055549,-0.437732142763655,
60.));
#79347=CARTESIAN_POINT('Ctrl Pts',(-7.21926140690079,-0.630186811838858,
60.));
#79348=CARTESIAN_POINT('Ctrl Pts',(-7.18219679971437,-0.821480864997494,
60.));
#79349=CARTESIAN_POINT('Ctrl Pts',(-7.16291568882707,-0.92099255906403,
60.));
#79350=CARTESIAN_POINT('Ctrl Pts',(-7.14153207281526,-1.02018977269293,
60.0000000000001));
#79351=CARTESIAN_POINT('Ctrl Pts',(-7.11805266783406,-1.11899638281762,
60.0000000000001));
#79352=CARTESIAN_POINT('Ctrl Pts',(-7.10912968526417,-1.15654629775968,
60.0000000000001));
#79353=CARTESIAN_POINT('Ctrl Pts',(-7.09990398456901,-1.1940397736015,60.0000000000001));
#79354=CARTESIAN_POINT('Ctrl Pts',(-7.09037582080005,-1.23147253281501,
60.0000000000001));
#79355=CARTESIAN_POINT('Ctrl Pts',(-7.08335466798265,-1.25905613960301,
60.));
#79356=CARTESIAN_POINT('Ctrl Pts',(-7.07616842942188,-1.28660971580694,
60.));
#79357=CARTESIAN_POINT('Ctrl Pts',(-7.06882369474851,-1.31410786163049,
60.));
#79358=CARTESIAN_POINT('Ctrl Pts',(-7.01922252390528,-1.49981099312826,
60.));
#79359=CARTESIAN_POINT('Ctrl Pts',(-6.96234315275086,-1.68320568927462,
60.));
#79360=CARTESIAN_POINT('Ctrl Pts',(-6.89834858945776,-1.86382382254377,
60.));
#79361=CARTESIAN_POINT('Ctrl Pts',(-6.83476009194915,-2.04329587651797,
60.));
#79362=CARTESIAN_POINT('Ctrl Pts',(-6.76414607432457,-2.22002716239884,
60.));
#79363=CARTESIAN_POINT('Ctrl Pts',(-6.68661966823323,-2.39353830166946,
60.0000000000001));
#79364=CARTESIAN_POINT('Ctrl Pts',(-6.60956772599301,-2.56598754774135,
60.0000000000001));
#79365=CARTESIAN_POINT('Ctrl Pts',(-6.52568743586049,-2.73525657050835,
60.));
#79366=CARTESIAN_POINT('Ctrl Pts',(-6.43504829728646,-2.90084515405146,
60.));
#79367=CARTESIAN_POINT('Ctrl Pts',(-6.401950884911,-2.96131079527905,60.));
#79368=CARTESIAN_POINT('Ctrl Pts',(-6.36795187632475,-3.02128535832417,
60.));
#79369=CARTESIAN_POINT('Ctrl Pts',(-6.3330533832055,-3.08074324429221,60.));
#79370=CARTESIAN_POINT('Ctrl Pts',(-6.2364595051223,-3.24531389691768,60.));
#79371=CARTESIAN_POINT('Ctrl Pts',(-6.13297666239597,-3.40592940627831,
60.));
#79372=CARTESIAN_POINT('Ctrl Pts',(-6.02288068162145,-3.56221579876367,
60.));
#79373=CARTESIAN_POINT('Ctrl Pts',(-6.01281665044061,-3.57650216159043,
60.));
#79374=CARTESIAN_POINT('Ctrl Pts',(-6.00269734068414,-3.59075231937767,
60.));
#79375=CARTESIAN_POINT('Ctrl Pts',(-5.9925229520943,-3.60496596753975,60.));
#79376=CARTESIAN_POINT('Ctrl Pts',(-5.97091601107585,-3.6351509221228,60.));
#79377=CARTESIAN_POINT('Ctrl Pts',(-5.94906067036394,-3.66517122529426,
60.));
#79378=CARTESIAN_POINT('Ctrl Pts',(-5.92695881890567,-3.69502390954886,
60.));
#79379=CARTESIAN_POINT('Ctrl Pts',(-5.90764738480234,-3.72110761325478,
60.));
#79380=CARTESIAN_POINT('Ctrl Pts',(-5.88814412064115,-3.74706799764837,
60.));
#79381=CARTESIAN_POINT('Ctrl Pts',(-5.86847065476455,-3.77287665540249,
60.));
#79382=CARTESIAN_POINT('Ctrl Pts',(-5.75525480403238,-3.92139899316552,
60.));
#79383=CARTESIAN_POINT('Ctrl Pts',(-5.63630504801428,-4.06503978380686,
59.9999999999999));
#79384=CARTESIAN_POINT('Ctrl Pts',(-5.51195816007129,-4.20352564428108,
60.));
#79385=CARTESIAN_POINT('Ctrl Pts',(-5.38717446497607,-4.34249797944989,
60.));
#79386=CARTESIAN_POINT('Ctrl Pts',(-5.25695511161658,-4.47627956078094,
59.9999999999999));
#79387=CARTESIAN_POINT('Ctrl Pts',(-5.12160437608111,-4.60455649665402,
59.9999999999999));
#79388=CARTESIAN_POINT('Ctrl Pts',(-4.98709347465071,-4.73203749044954,
59.9999999999999));
#79389=CARTESIAN_POINT('Ctrl Pts',(-4.84751410863532,-4.85408231728632,
60.));
#79390=CARTESIAN_POINT('Ctrl Pts',(-4.70313771916586,-4.97033965601283,
60.));
#79391=CARTESIAN_POINT('Ctrl Pts',(-4.56146741367584,-5.08441795339487,
60.));
#79392=CARTESIAN_POINT('Ctrl Pts',(-4.41517767953588,-5.19292392882823,
60.));
#79393=CARTESIAN_POINT('Ctrl Pts',(-4.26450693334287,-5.29547942882985,
60.));
#79394=CARTESIAN_POINT('Ctrl Pts',(-4.1549207018082,-5.37007035674584,60.));
#79395=CARTESIAN_POINT('Ctrl Pts',(-4.04301652795845,-5.44151256479602,
60.));
#79396=CARTESIAN_POINT('Ctrl Pts',(-3.9288823673735,-5.5096435767971,60.));
#79397=CARTESIAN_POINT('Ctrl Pts',(-3.93301173192423,-5.51252654933308,
-60.));
#79398=CARTESIAN_POINT('Ctrl Pts',(-4.08952080384978,-5.42059770583385,
-60.));
#79399=CARTESIAN_POINT('Ctrl Pts',(-4.24181965717463,-5.32232120961294,
-60.));
#79400=CARTESIAN_POINT('Ctrl Pts',(-4.38947572522641,-5.21781239717533,
-60.));
#79401=CARTESIAN_POINT('Ctrl Pts',(-4.53705291796563,-5.11335941153411,
-60.));
#79402=CARTESIAN_POINT('Ctrl Pts',(-4.67999341387791,-5.00268139404814,
-60.));
#79403=CARTESIAN_POINT('Ctrl Pts',(-4.81813643652202,-4.88627279397718,
-60.));
#79404=CARTESIAN_POINT('Ctrl Pts',(-4.95837547651839,-4.7680979487421,-60.));
#79405=CARTESIAN_POINT('Ctrl Pts',(-5.09367081531429,-4.64401689247806,
-60.));
#79406=CARTESIAN_POINT('Ctrl Pts',(-5.22383156481562,-4.51449705972283,
-60.));
#79407=CARTESIAN_POINT('Ctrl Pts',(-5.35596904369448,-4.38301023108473,
-60.));
#79408=CARTESIAN_POINT('Ctrl Pts',(-5.48281531429085,-4.24591770621096,
-60.));
#79409=CARTESIAN_POINT('Ctrl Pts',(-5.6041399810699,-4.1036642545346,-60.));
#79410=CARTESIAN_POINT('Ctrl Pts',(-5.70214434390653,-3.98875391302721,
-60.));
#79411=CARTESIAN_POINT('Ctrl Pts',(-5.79654527992217,-3.87047499888056,
-60.));
#79412=CARTESIAN_POINT('Ctrl Pts',(-5.88720352206258,-3.74904468981495,
-60.));
#79413=CARTESIAN_POINT('Ctrl Pts',(-5.90038741125276,-3.73138580187213,
-60.));
#79414=CARTESIAN_POINT('Ctrl Pts',(-5.91349113483187,-3.71366150064713,
-60.));
#79415=CARTESIAN_POINT('Ctrl Pts',(-5.92650729286421,-3.6958821765402,-60.));
#79416=CARTESIAN_POINT('Ctrl Pts',(-6.03764306928045,-3.54407709059468,
-60.));
#79417=CARTESIAN_POINT('Ctrl Pts',(-6.14253987674664,-3.38807418550578,
-60.));
#79418=CARTESIAN_POINT('Ctrl Pts',(-6.24102436169895,-3.22837952733627,
-60.));
#79419=CARTESIAN_POINT('Ctrl Pts',(-6.34131022385272,-3.06576389824877,
-60.));
#79420=CARTESIAN_POINT('Ctrl Pts',(-6.43494756756259,-2.89931974799542,
-60.));
#79421=CARTESIAN_POINT('Ctrl Pts',(-6.52172278078293,-2.72953725844725,
-60.));
#79422=CARTESIAN_POINT('Ctrl Pts',(-6.54759921289344,-2.6789079957661,-60.));
#79423=CARTESIAN_POINT('Ctrl Pts',(-6.57286520629013,-2.62798160952088,
-60.));
#79424=CARTESIAN_POINT('Ctrl Pts',(-6.59751447498585,-2.57677045843014,
-60.));
#79425=CARTESIAN_POINT('Ctrl Pts',(-6.68040386452845,-2.40456003287614,
-60.));
#79426=CARTESIAN_POINT('Ctrl Pts',(-6.75632263423444,-2.22913159646629,
-60.));
#79427=CARTESIAN_POINT('Ctrl Pts',(-6.82519899342782,-2.05090247570647,
-60.));
#79428=CARTESIAN_POINT('Ctrl Pts',(-6.89423580505223,-1.87225815739493,
-60.));
#79429=CARTESIAN_POINT('Ctrl Pts',(-6.95619763361968,-1.69079948329051,
-60.));
#79430=CARTESIAN_POINT('Ctrl Pts',(-7.01096564304006,-1.50692333508897,
-60.));
#79431=CARTESIAN_POINT('Ctrl Pts',(-7.02583863164074,-1.45698929722488,
-60.));
#79432=CARTESIAN_POINT('Ctrl Pts',(-7.04018082205761,-1.40687687506854,
-60.));
#79433=CARTESIAN_POINT('Ctrl Pts',(-7.05398920151378,-1.35659381192878,
-60.));
#79434=CARTESIAN_POINT('Ctrl Pts',(-7.06130669006673,-1.32994725719725,
-60.));
#79435=CARTESIAN_POINT('Ctrl Pts',(-7.06847426548418,-1.30325278069041,
-60.));
#79436=CARTESIAN_POINT('Ctrl Pts',(-7.07549144748142,-1.27651152744079,
-60.));
#79437=CARTESIAN_POINT('Ctrl Pts',(-7.08197914199504,-1.25178805838116,
-60.));
#79438=CARTESIAN_POINT('Ctrl Pts',(-7.08833643947356,-1.22703150330183,
-60.));
#79439=CARTESIAN_POINT('Ctrl Pts',(-7.09456102669435,-1.20225171368677,
-60.));
#79440=CARTESIAN_POINT('Ctrl Pts',(-7.14220708680675,-1.01257498434034,
-60.));
#79441=CARTESIAN_POINT('Ctrl Pts',(-7.18212278214278,-0.821380786189583,
-60.));
#79442=CARTESIAN_POINT('Ctrl Pts',(-7.2142837787498,-0.629129382873918,
-60.));
#79443=CARTESIAN_POINT('Ctrl Pts',(-7.24659626634971,-0.435972399537559,
-60.));
#79444=CARTESIAN_POINT('Ctrl Pts',(-7.27108109768127,-0.241747604229979,
-60.));
#79445=CARTESIAN_POINT('Ctrl Pts',(-7.28766818194827,-0.0468948140504708,
-60.));
#79446=CARTESIAN_POINT('Ctrl Pts',(-7.30418370687894,0.147117350005538,
-60.));
#79447=CARTESIAN_POINT('Ctrl Pts',(-7.31286968915527,0.341752756646404,
-60.));
#79448=CARTESIAN_POINT('Ctrl Pts',(-7.31360856011759,0.536594313533747,
-60.));
#79449=CARTESIAN_POINT('Ctrl Pts',(-7.31409810186552,0.665687323263242,
-60.));
#79450=CARTESIAN_POINT('Ctrl Pts',(-7.31109804508312,0.794871162698884,
-60.));
#79451=CARTESIAN_POINT('Ctrl Pts',(-7.30456172141964,0.924026543564304,
-60.));
#79452=CARTESIAN_POINT('Ctrl Pts',(-7.29714775632053,1.07052380034001,-60.));
#79453=CARTESIAN_POINT('Ctrl Pts',(-7.28518443291222,1.21698458021077,-60.));
#79454=CARTESIAN_POINT('Ctrl Pts',(-7.26874210131775,1.36321456224292,-60.));
#79455=CARTESIAN_POINT('Ctrl Pts',(-7.26405275890041,1.40491925926174,-60.));
#79456=CARTESIAN_POINT('Ctrl Pts',(-7.25899899522214,1.44660517619321,-60.));
#79457=CARTESIAN_POINT('Ctrl Pts',(-7.25358219346459,1.4882677788116,-60.));
#79458=CARTESIAN_POINT('Ctrl Pts',(-7.24901532725683,1.52339321639291,-60.));
#79459=CARTESIAN_POINT('Ctrl Pts',(-7.2441894596039,1.55850797715054,-60.));
#79460=CARTESIAN_POINT('Ctrl Pts',(-7.2391110333888,1.59357215124191,-60.));
#79461=CARTESIAN_POINT('Ctrl Pts',(-7.2112095232227,1.78621911871558,-60.));
#79462=CARTESIAN_POINT('Ctrl Pts',(-7.17566576866628,1.97753353254058,-60.));
#79463=CARTESIAN_POINT('Ctrl Pts',(-7.13276029827355,2.16706682927203,-60.));
#79464=CARTESIAN_POINT('Ctrl Pts',(-7.08881801138619,2.36118022375171,-60.));
#79465=CARTESIAN_POINT('Ctrl Pts',(-7.03715395035248,2.55342602264969,-60.));
#79466=CARTESIAN_POINT('Ctrl Pts',(-6.9780154261089,2.74333156236495,-60.));
#79467=CARTESIAN_POINT('Ctrl Pts',(-6.91852012664441,2.93438277813066,-60.));
#79468=CARTESIAN_POINT('Ctrl Pts',(-6.85145977804132,3.12306613872702,-60.));
#79469=CARTESIAN_POINT('Ctrl Pts',(-6.77703309916436,3.30889912524294,-60.));
#79470=CARTESIAN_POINT('Ctrl Pts',(-6.70296831599029,3.49382850890717,-60.));
#79471=CARTESIAN_POINT('Ctrl Pts',(-6.62160844992583,3.67593589277402,-60.));
#79472=CARTESIAN_POINT('Ctrl Pts',(-6.53309963579732,3.85473369085425,-60.));
#79473=CARTESIAN_POINT('Ctrl Pts',(-6.46222636298705,3.99790570424058,-60.));
#79474=CARTESIAN_POINT('Ctrl Pts',(-6.38676821807548,4.13895553781842,-60.));
#79475=CARTESIAN_POINT('Ctrl Pts',(-6.30677843138628,4.27762247763241,-60.));
#79476=CARTESIAN_POINT('Ctrl Pts',(-6.29320342493038,4.30115553955328,-60.));
#79477=CARTESIAN_POINT('Ctrl Pts',(-6.2795014627675,4.32461364165953,-60.));
#79478=CARTESIAN_POINT('Ctrl Pts',(-6.2656767166826,4.34798939028162,-60.));
#79479=CARTESIAN_POINT('Ctrl Pts',(-6.24175455611388,4.38843848124628,-60.));
#79480=CARTESIAN_POINT('Ctrl Pts',(-6.21746139506088,4.42864682897115,-60.));
#79481=CARTESIAN_POINT('Ctrl Pts',(-6.19280011122744,4.46860844401354,-60.));
#79482=CARTESIAN_POINT('Ctrl Pts',(-6.08720463490951,4.63971736937743,-60.));
#79483=CARTESIAN_POINT('Ctrl Pts',(-5.97486400026855,4.80630398343347,-60.));
#79484=CARTESIAN_POINT('Ctrl Pts',(-5.85618687666969,4.96812701738046,-60.));
#79485=CARTESIAN_POINT('Ctrl Pts',(-5.73620135676387,5.13173412439543,-60.));
#79486=CARTESIAN_POINT('Ctrl Pts',(-5.60973852475551,5.29047255139371,-60.));
#79487=CARTESIAN_POINT('Ctrl Pts',(-5.47717146481258,5.44407198105424,-60.));
#79488=CARTESIAN_POINT('Ctrl Pts',(-5.40441740036826,5.52836881021334,-60.));
#79489=CARTESIAN_POINT('Ctrl Pts',(-5.32982396086839,5.61111740341094,-60.));
#79490=CARTESIAN_POINT('Ctrl Pts',(-5.25344719017398,5.69226956964437,-60.));
#79491=CARTESIAN_POINT('Ctrl Pts',(-5.20079500682673,5.74821378798068,-60.));
#79492=CARTESIAN_POINT('Ctrl Pts',(-5.14729523733269,5.80339927185339,-60.));
#79493=CARTESIAN_POINT('Ctrl Pts',(-5.09296524201554,5.85780942633472,-60.));
#79494=CARTESIAN_POINT('Ctrl Pts',(-5.06656807641211,5.88424553865109,-60.));
#79495=CARTESIAN_POINT('Ctrl Pts',(-5.03997397463221,5.91049937778292,-60.));
#79496=CARTESIAN_POINT('Ctrl Pts',(-5.01320308796063,5.93655167337536,-60.));
#79497=CARTESIAN_POINT('Ctrl Pts',(-4.86528754035126,6.08049683351553,-60.));
#79498=CARTESIAN_POINT('Ctrl Pts',(-4.71185216667681,6.21841958267782,-60.));
#79499=CARTESIAN_POINT('Ctrl Pts',(-4.55329863095189,6.35005394068721,-60.));
#79500=CARTESIAN_POINT('Ctrl Pts',(-4.39412852588249,6.48220018705946,-60.));
#79501=CARTESIAN_POINT('Ctrl Pts',(-4.22979994004088,6.60800956229862,-60.));
#79502=CARTESIAN_POINT('Ctrl Pts',(-4.06067591285683,6.72718329191288,-60.));
#79503=CARTESIAN_POINT('Ctrl Pts',(-3.89230921701461,6.84582336583042,-60.));
#79504=CARTESIAN_POINT('Ctrl Pts',(-3.71918944625603,6.95788757299026,-60.));
#79505=CARTESIAN_POINT('Ctrl Pts',(-3.54163890299614,7.06304431300309,-60.));
#79506=CARTESIAN_POINT('Ctrl Pts',(-3.50154405698965,7.08679103447151,-60.));
#79507=CARTESIAN_POINT('Ctrl Pts',(-3.46122313234071,7.11018533926288,-60.));
#79508=CARTESIAN_POINT('Ctrl Pts',(-3.4206796250969,7.13322310757535,-60.));
#79509=CARTESIAN_POINT('Ctrl Pts',(4.59493373696683,-6.44781750921883,-60.6643731623753));
#79510=CARTESIAN_POINT('Ctrl Pts',(5.66758804391333,-5.68341533656089,-60.6114196764411));
#79511=CARTESIAN_POINT('Ctrl Pts',(7.420231908041,-3.6147783613617,-60.5055449235297));
#79512=CARTESIAN_POINT('Ctrl Pts',(8.24850409473424,0.389368816384953,-60.3467489036408));
#79513=CARTESIAN_POINT('Ctrl Pts',(7.05091419264973,4.26423914542533,-60.1879851027094));
#79514=CARTESIAN_POINT('Ctrl Pts',(3.1979029178683,8.12048633360201,-59.9763000348008));
#79515=CARTESIAN_POINT('Ctrl Pts',(-4.23022369577523,8.35267581578188,-59.7116936999148));
#79516=CARTESIAN_POINT('Ctrl Pts',(-9.31726541786132,0.94545657484609,-59.3941660980519));
#79517=CARTESIAN_POINT('Ctrl Pts',(-6.42446717770634,-5.90348168320496,
-59.1295597631658));
#79518=CARTESIAN_POINT('Ctrl Pts',(-1.4490501247666,-8.11293657404488,-58.9178746952573));
#79519=CARTESIAN_POINT('Ctrl Pts',(2.61219513444578,-7.83570724861456,-58.7591108943257));
#79520=CARTESIAN_POINT('Ctrl Pts',(6.02072951395808,-5.62778786725318,-58.6003470933942));
#79521=CARTESIAN_POINT('Ctrl Pts',(8.68771888553699,-0.861913486306708,
-58.3886620254857));
#79522=CARTESIAN_POINT('Ctrl Pts',(7.23919397520838,4.88343575175983,-58.1769769575768));
#79523=CARTESIAN_POINT('Ctrl Pts',(2.63366693853143,7.8007910704191,-57.9652918896683));
#79524=CARTESIAN_POINT('Ctrl Pts',(-2.77103540777255,8.27359001524915,-57.7536068217594));
#79525=CARTESIAN_POINT('Ctrl Pts',(-8.62164699515589,3.66576579702773,-57.4890004868736));
#79526=CARTESIAN_POINT('Ctrl Pts',(-7.73354855495184,-5.27571385914043,
-57.1714728850106));
#79527=CARTESIAN_POINT('Ctrl Pts',(-1.1157857437006,-8.65379742007332,-56.9068665501247));
#79528=CARTESIAN_POINT('Ctrl Pts',(4.11628243882215,-7.14010761184303,-56.695181482216));
#79529=CARTESIAN_POINT('Ctrl Pts',(7.04367409087663,-4.31305663032169,-56.5364176812845));
#79530=CARTESIAN_POINT('Ctrl Pts',(8.23048748680303,-0.42887819825834,-56.3776538803531));
#79531=CARTESIAN_POINT('Ctrl Pts',(7.20173000873569,4.93473188277679,-56.1659688124443));
#79532=CARTESIAN_POINT('Ctrl Pts',(2.39419873589606,8.39775644139713,-55.9542837445356));
#79533=CARTESIAN_POINT('Ctrl Pts',(-3.00812442644778,7.66419399588113,-55.742598676627));
#79534=CARTESIAN_POINT('Ctrl Pts',(-7.44760558900325,4.54573886957917,-55.5309136087182));
#79535=CARTESIAN_POINT('Ctrl Pts',(-8.95683435881455,-2.74700645169454,
-55.2663072738324));
#79536=CARTESIAN_POINT('Ctrl Pts',(-2.51973131736528,-9.01619753462101,
-54.9487796719692));
#79537=CARTESIAN_POINT('Ctrl Pts',(4.718673013345,-7.33943323573433,-54.6841733370835));
#79538=CARTESIAN_POINT('Ctrl Pts',(7.74699969690703,-2.8122842977038,-54.4724882691748));
#79539=CARTESIAN_POINT('Ctrl Pts',(8.16632621930467,1.23567797082505,-54.3137244682434));
#79540=CARTESIAN_POINT('Ctrl Pts',(6.57324816560372,4.97164730573518,-54.1549606673117));
#79541=CARTESIAN_POINT('Ctrl Pts',(2.33241468102429,8.41286709177905,-53.943275599403));
#79542=CARTESIAN_POINT('Ctrl Pts',(-3.57570292077998,7.96673386021558,-53.7315905314943));
#79543=CARTESIAN_POINT('Ctrl Pts',(-7.23662431142663,3.92682465094442,-53.5199054635857));
#79544=CARTESIAN_POINT('Ctrl Pts',(-8.62520104969994,-1.31775439966483,
-53.3082203956771));
#79545=CARTESIAN_POINT('Ctrl Pts',(-5.08395332956645,-7.86920232075575,
-53.0436140607911));
#79546=CARTESIAN_POINT('Ctrl Pts',(3.87788594583802,-8.52073145927405,-52.7260864589282));
#79547=CARTESIAN_POINT('Ctrl Pts',(8.3362320335911,-2.5768955255669,-52.4614801240423));
#79548=CARTESIAN_POINT('Ctrl Pts',(7.73805855367662,2.8367934663068,-52.2497950561336));
#79549=CARTESIAN_POINT('Ctrl Pts',(5.45231667204648,6.20387192351473,-52.0910312552021));
#79550=CARTESIAN_POINT('Ctrl Pts',(1.82779777155195,8.0364185862005,-51.9322674542705));
#79551=CARTESIAN_POINT('Ctrl Pts',(-3.63270370379316,7.93851086500441,-51.7205823863618));
#79552=CARTESIAN_POINT('Ctrl Pts',(-7.86568586511065,3.79282027538551,-51.5088973184531));
#79553=CARTESIAN_POINT('Ctrl Pts',(-8.06524943223459,-1.65542588568015,
-51.2972122505444));
#79554=CARTESIAN_POINT('Ctrl Pts',(-5.75054767799861,-6.56214684434599,
-51.0855271826359));
#79555=CARTESIAN_POINT('Ctrl Pts',(1.17744529526638,-9.29432887296655,-50.8209208477498));
#79556=CARTESIAN_POINT('Ctrl Pts',(8.45361418193282,-4.02209786974241,-50.5033932458868));
#79557=CARTESIAN_POINT('Ctrl Pts',(8.03730415832691,3.39630636628952,-50.238786911001));
#79558=CARTESIAN_POINT('Ctrl Pts',(4.09366137959014,7.15310309306182,-50.0271018430924));
#79559=CARTESIAN_POINT('Ctrl Pts',(0.176726936200001,8.25739374897774,-49.8683380421608));
#79560=CARTESIAN_POINT('Ctrl Pts',(-3.77637944480456,7.32555981991549,-49.7095742412292));
#79561=CARTESIAN_POINT('Ctrl Pts',(-7.89112337486653,3.73452310690604,-49.4978891733208));
#79562=CARTESIAN_POINT('Ctrl Pts',(-8.46025155684443,-2.1630171901463,-49.2862041054118));
#79563=CARTESIAN_POINT('Ctrl Pts',(-5.10469934135701,-6.45993249976306,
-49.0745190375033));
#79564=CARTESIAN_POINT('Ctrl Pts',(-0.174200713771704,-8.72354422898261,
-48.8628339695944));
#79565=CARTESIAN_POINT('Ctrl Pts',(6.88566245154638,-6.35284024870503,-48.5982276347087));
#79566=CARTESIAN_POINT('Ctrl Pts',(9.05770761919772,2.36617765518383,-48.2807000328456));
#79567=CARTESIAN_POINT('Ctrl Pts',(3.96233018059051,7.77387256180204,-48.0160936979597));
#79568=CARTESIAN_POINT('Ctrl Pts',(-1.47399934069216,8.10877754623701,-47.804408630051));
#79569=CARTESIAN_POINT('Ctrl Pts',(-5.1818917662573,6.43146807956242,-47.6456448291196));
#79570=CARTESIAN_POINT('Ctrl Pts',(-7.6063569291163,3.17304312186065,-47.486881028188));
#79571=CARTESIAN_POINT('Ctrl Pts',(-8.44217486912475,-2.22399964759411,
-47.2751959602793));
#79572=CARTESIAN_POINT('Ctrl Pts',(-5.08006411145565,-7.10263672120833,
-47.0635108923708));
#79573=CARTESIAN_POINT('Ctrl Pts',(0.254115101922676,-8.22946588680703,
-46.8518258244619));
#79574=CARTESIAN_POINT('Ctrl Pts',(5.48398835986514,-6.78648962811834,-46.6401407565533));
#79575=CARTESIAN_POINT('Ctrl Pts',(9.35889206087632,-0.426691943992846,
-46.3755344216674));
#79576=CARTESIAN_POINT('Ctrl Pts',(5.40635409573626,7.64278741051195,-46.0580068198043));
#79577=CARTESIAN_POINT('Ctrl Pts',(-1.97420597526809,8.49915677196114,-45.7934004849185));
#79578=CARTESIAN_POINT('Ctrl Pts',(-6.3491530516771,5.2548266267402,-45.5817154170098));
#79579=CARTESIAN_POINT('Ctrl Pts',(-8.1059799567344,1.58394219485922,-45.4229516160784));
#79580=CARTESIAN_POINT('Ctrl Pts',(-7.86275378607339,-2.47021684997314,
-45.2641878151467));
#79581=CARTESIAN_POINT('Ctrl Pts',(-5.02696592541148,-7.13765399400476,
-45.0525027472383));
#79582=CARTESIAN_POINT('Ctrl Pts',(0.686813685647454,-8.70533093748678,
-44.8408176793293));
#79583=CARTESIAN_POINT('Ctrl Pts',(5.4935424570323,-6.13267270771309,-44.6291326114208));
#79584=CARTESIAN_POINT('Ctrl Pts',(8.5657174085411,-1.66104036095169,-44.417447543512));
#79585=CARTESIAN_POINT('Ctrl Pts',(7.43517373916352,5.69992263900624,-44.1528412086262));
#79586=CARTESIAN_POINT('Ctrl Pts',(-0.784985710407776,9.32870095164485,
-43.8353136067632));
#79587=CARTESIAN_POINT('Ctrl Pts',(-6.98323053873475,5.23140959111778,-43.5707072718773));
#79588=CARTESIAN_POINT('Ctrl Pts',(-8.24137938270553,-0.067920696662337,
-43.3590222039687));
#79589=CARTESIAN_POINT('Ctrl Pts',(-7.22175712406885,-4.00774350184691,
-43.2002584030371));
#79590=CARTESIAN_POINT('Ctrl Pts',(-4.42511092475034,-6.95293187727002,
-43.0414946021055));
#79591=CARTESIAN_POINT('Ctrl Pts',(0.74998704541379,-8.69793138539803,-42.8298095341971));
#79592=CARTESIAN_POINT('Ctrl Pts',(6.13101610681114,-6.21813004592047,-42.6181244662881));
#79593=CARTESIAN_POINT('Ctrl Pts',(8.15202112896183,-1.15465786279127,-42.4064393983796));
#79594=CARTESIAN_POINT('Ctrl Pts',(7.62314388033113,4.24479059359405,-42.1947543304707));
#79595=CARTESIAN_POINT('Ctrl Pts',(2.01829922153478,9.14862803236388,-41.9301479955849));
#79596=CARTESIAN_POINT('Ctrl Pts',(-6.60752745019684,6.63185079790396,-41.6126203937219));
#79597=CARTESIAN_POINT('Ctrl Pts',(-8.71142860376982,-0.49413231889662,
-41.348014058836));
#79598=CARTESIAN_POINT('Ctrl Pts',(-6.26168200844734,-5.35875785754551,
-41.1363289909274));
#79599=CARTESIAN_POINT('Ctrl Pts',(-2.94464442381838,-7.71653116062592,
-40.9775651899958));
#79600=CARTESIAN_POINT('Ctrl Pts',(1.09151545285383,-8.16905517195739,-40.8188013890643));
#79601=CARTESIAN_POINT('Ctrl Pts',(6.17458484789321,-6.17179008955651,-40.6071163211557));
#79602=CARTESIAN_POINT('Ctrl Pts',(8.69477515810992,-0.809558348651662,
-40.3954312532469));
#79603=CARTESIAN_POINT('Ctrl Pts',(6.98055794413596,4.36583257302729,-40.1837461853383));
#79604=CARTESIAN_POINT('Ctrl Pts',(3.09910296317843,8.15635522934804,-39.9720611174295));
#79605=CARTESIAN_POINT('Ctrl Pts',(-4.34680255725139,8.29917069052533,-39.7074547825437));
#79606=CARTESIAN_POINT('Ctrl Pts',(-9.32575364040251,0.819257620827232,
-39.3899271806806));
#79607=CARTESIAN_POINT('Ctrl Pts',(-6.34686678583791,-5.9875234504747,-39.1253208457948));
#79608=CARTESIAN_POINT('Ctrl Pts',(-1.34015246294474,-8.13197016268393,
-38.9136357778861));
#79609=CARTESIAN_POINT('Ctrl Pts',(2.71590641448793,-7.79997668479713,-38.7548719769546));
#79610=CARTESIAN_POINT('Ctrl Pts',(6.09533149127371,-5.54723376087484,-38.5961081760231));
#79611=CARTESIAN_POINT('Ctrl Pts',(8.69827003214864,-0.746049194896171,
-38.3844231081144));
#79612=CARTESIAN_POINT('Ctrl Pts',(7.17359836511665,4.97935600915946,-38.1727380402057));
#79613=CARTESIAN_POINT('Ctrl Pts',(2.52952388592635,7.83518935174345,-37.961052972297));
#79614=CARTESIAN_POINT('Ctrl Pts',(-2.8809430316479,8.23594178294709,-37.7493679043883));
#79615=CARTESIAN_POINT('Ctrl Pts',(-8.66971126591377,3.55063841976205,-37.4847615695025));
#79616=CARTESIAN_POINT('Ctrl Pts',(-7.66260082678378,-5.37823508040855,
-37.1672339676394));
#79617=CARTESIAN_POINT('Ctrl Pts',(-1.00045170994875,-8.66788621540555,
-36.9026276327536));
#79618=CARTESIAN_POINT('Ctrl Pts',(4.21100082016462,-7.08466085591197,-36.6909425648448));
#79619=CARTESIAN_POINT('Ctrl Pts',(7.10048366399641,-4.21887611490971,-36.5321787639134));
#79620=CARTESIAN_POINT('Ctrl Pts',(8.23546932769645,-0.319238686367667,
-36.3734149629817));
#79621=CARTESIAN_POINT('Ctrl Pts',(7.13537742784409,5.03019680684496,-36.1617298950732));
#79622=CARTESIAN_POINT('Ctrl Pts',(2.28215741217129,8.42889419295488,-35.9500448271644));
#79623=CARTESIAN_POINT('Ctrl Pts',(-3.10991845228071,7.62345659706342,-35.7383597592558));
#79624=CARTESIAN_POINT('Ctrl Pts',(-7.50747875837207,4.44615929722344,-35.5266746913471));
#79625=CARTESIAN_POINT('Ctrl Pts',(-8.91945952295018,-2.86603706198215,
-35.2620683564612));
#79626=CARTESIAN_POINT('Ctrl Pts',(-2.39944315868245,-9.04895223432061,
-34.9445407545982));
#79627=CARTESIAN_POINT('Ctrl Pts',(4.81599059219255,-7.27594596482617,-34.6799344197123));
#79628=CARTESIAN_POINT('Ctrl Pts',(7.78376272709339,-2.70887156562104,-34.4682493518036));
#79629=CARTESIAN_POINT('Ctrl Pts',(8.1491471373085,1.3443157628072,-34.3094855508721));
#79630=CARTESIAN_POINT('Ctrl Pts',(6.50646009136296,5.05873951353536,-34.1507217499406));
#79631=CARTESIAN_POINT('Ctrl Pts',(2.22017743346687,8.44318086489356,-33.9390366820319));
#79632=CARTESIAN_POINT('Ctrl Pts',(-3.68147533938544,7.91841139973504,-33.7273516141232));
#79633=CARTESIAN_POINT('Ctrl Pts',(-7.28827443373505,3.83010953442713,-33.5156665462146));
#79634=CARTESIAN_POINT('Ctrl Pts',(-8.60688830613688,-1.43249554602399,
-33.3039814783058));
#79635=CARTESIAN_POINT('Ctrl Pts',(-4.97871184944764,-7.93620532385422,
-33.03937514342));
#79636=CARTESIAN_POINT('Ctrl Pts',(3.99100891174753,-8.4683358387062,-32.7218475415569));
#79637=CARTESIAN_POINT('Ctrl Pts',(8.3698082446935,-2.46565711610875,-32.4572412066711));
#79638=CARTESIAN_POINT('Ctrl Pts',(7.69959610060171,2.93958623590426,-32.2455561387624));
#79639=CARTESIAN_POINT('Ctrl Pts',(5.36921899827152,6.27592792216698,-32.0867923378309));
#79640=CARTESIAN_POINT('Ctrl Pts',(1.72061826725716,8.06004597782691,-31.9280285368993));
#79641=CARTESIAN_POINT('Ctrl Pts',(-3.73809523544606,7.88943185306239,-31.7163434689907));
#79642=CARTESIAN_POINT('Ctrl Pts',(-7.91549573176501,3.68774010613095,-31.5046584010819));
#79643=CARTESIAN_POINT('Ctrl Pts',(-8.04248971735526,-1.76268046264216,
-31.2929733331733));
#79644=CARTESIAN_POINT('Ctrl Pts',(-5.66265257150908,-6.63814248552081,
-31.0812882652646));
#79645=CARTESIAN_POINT('Ctrl Pts',(1.30110936217168,-9.2778252327726,-30.8166819303787));
#79646=CARTESIAN_POINT('Ctrl Pts',(8.50642510580062,-3.90916818903571,-30.4991543285157));
#79647=CARTESIAN_POINT('Ctrl Pts',(7.99136438532443,3.50303444575207,-30.2345479936298));
#79648=CARTESIAN_POINT('Ctrl Pts',(3.99804368483144,7.20698231195957,-30.0228629257211));
#79649=CARTESIAN_POINT('Ctrl Pts',(0.0667512025953981,8.25901496624065,
-29.8640991247897));
#79650=CARTESIAN_POINT('Ctrl Pts',(-3.87359583864445,7.2746218915583,-29.7053353238581));
#79651=CARTESIAN_POINT('Ctrl Pts',(-7.94015466836669,3.62910936674481,-29.4936502559494));
#79652=CARTESIAN_POINT('Ctrl Pts',(-8.43069744832558,-2.27548682807728,
-29.2819651880407));
#79653=CARTESIAN_POINT('Ctrl Pts',(-5.0182226450366,-6.52733672733278,-29.070280120132));
#79654=CARTESIAN_POINT('Ctrl Pts',(-0.0580176842298914,-8.72509047242555,
-28.8585950522234));
#79655=CARTESIAN_POINT('Ctrl Pts',(6.96964987081364,-6.26058362299151,-28.5939887173375));
#79656=CARTESIAN_POINT('Ctrl Pts',(9.02539513654387,2.48658533736819,-28.2764611154745));
#79657=CARTESIAN_POINT('Ctrl Pts',(3.85845761819846,7.82594785797371,-28.0118547805886));
#79658=CARTESIAN_POINT('Ctrl Pts',(-1.58184964927522,8.08842994887182,-27.8001697126799));
#79659=CARTESIAN_POINT('Ctrl Pts',(-5.26707730973789,6.36189284324087,-27.6414059117484));
#79660=CARTESIAN_POINT('Ctrl Pts',(-7.64793649183002,3.07147127664212,-27.4826421108169));
#79661=CARTESIAN_POINT('Ctrl Pts',(-8.41181028701722,-2.33622315899216,
-27.2709570429082));
#79662=CARTESIAN_POINT('Ctrl Pts',(-4.98503099143786,-7.16965590418124,
-27.0592719749995));
#79663=CARTESIAN_POINT('Ctrl Pts',(0.363680730071077,-8.22535224739468,
-26.8475869070908));
#79664=CARTESIAN_POINT('Ctrl Pts',(5.57387478172201,-6.71286002545695,-26.6359018391822));
#79665=CARTESIAN_POINT('Ctrl Pts',(9.36374428260679,-0.302025879935631,
-26.3712955042962));
#79666=CARTESIAN_POINT('Ctrl Pts',(5.30409909579721,7.7141037582293,-26.0537679024333));
#79667=CARTESIAN_POINT('Ctrl Pts',(-2.08721043851178,8.47211352925138,-25.7891615675473));
#79668=CARTESIAN_POINT('Ctrl Pts',(-6.41856628069534,5.16981181969319,-25.5774764996387));
#79669=CARTESIAN_POINT('Ctrl Pts',(-8.12635386345765,1.47585799503287,-25.4187126987071));
#79670=CARTESIAN_POINT('Ctrl Pts',(-7.82916181514927,-2.57470263496797,
-25.2599488977757));
#79671=CARTESIAN_POINT('Ctrl Pts',(-4.93147120402558,-7.20396298694315,
-25.0482638298669));
#79672=CARTESIAN_POINT('Ctrl Pts',(0.80267783129953,-8.69541304764167,-24.8365787619583));
#79673=CARTESIAN_POINT('Ctrl Pts',(5.57472144074746,-6.05897385084444,-24.6248936940496));
#79674=CARTESIAN_POINT('Ctrl Pts',(8.5870772328764,-1.54682720441233,-24.4132086261409));
#79675=CARTESIAN_POINT('Ctrl Pts',(7.35861111677501,5.7984281537566,-24.148602291255));
#79676=CARTESIAN_POINT('Ctrl Pts',(-0.909142294207787,9.31742047455447,
-23.831074689392));
#79677=CARTESIAN_POINT('Ctrl Pts',(-7.05227571023749,5.13795313076632,-23.5664683545061));
#79678=CARTESIAN_POINT('Ctrl Pts',(-8.23974415554159,-0.177661481296447,
-23.3547832865974));
#79679=CARTESIAN_POINT('Ctrl Pts',(-7.16774742692252,-4.10355708617308,
-23.1960194856659));
#79680=CARTESIAN_POINT('Ctrl Pts',(-4.33212943221437,-7.01124261232236,
-23.0372556847344));
#79681=CARTESIAN_POINT('Ctrl Pts',(0.865747052963905,-8.68717289995225,
-22.8255706168257));
#79682=CARTESIAN_POINT('Ctrl Pts',(6.21327656379671,-6.13593465673581,-22.613885548917));
#79683=CARTESIAN_POINT('Ctrl Pts',(8.16667436351112,-1.04599861735849,-22.4022004810083));
#79684=CARTESIAN_POINT('Ctrl Pts',(7.56594194114363,4.34592824917043,-22.1905154130997));
#79685=CARTESIAN_POINT('Ctrl Pts',(1.89629202393501,9.17469362879016,-21.9259090782138));
#79686=CARTESIAN_POINT('Ctrl Pts',(-6.69525499167751,6.54327323341937,-21.6083814763508));
#79687=CARTESIAN_POINT('Ctrl Pts',(-8.70407602585803,-0.610094749395952,
-21.3437751414648));
#79688=CARTESIAN_POINT('Ctrl Pts',(-6.18976657936131,-5.44166675236,-21.1320900735562));
#79689=CARTESIAN_POINT('Ctrl Pts',(-2.84162568899887,-7.75505946974343,
-20.9733262726247));
#79690=CARTESIAN_POINT('Ctrl Pts',(1.200202366515,-8.15379559872055,-20.8145624716932));
#79691=CARTESIAN_POINT('Ctrl Pts',(6.25622435294957,-6.0890186236323,-20.6028774037845));
#79692=CARTESIAN_POINT('Ctrl Pts',(8.7047847293251,-0.693702087401876,-20.3911923358758));
#79693=CARTESIAN_POINT('Ctrl Pts',(6.92180112003964,4.458402462964,-20.1795072679671));
#79694=CARTESIAN_POINT('Ctrl Pts',(2.99021358987876,8.19690139568593,-19.9678222000584));
#79695=CARTESIAN_POINT('Ctrl Pts',(-4.4569335177732,8.24055036028256,-19.7032158651726));
#79696=CARTESIAN_POINT('Ctrl Pts',(-9.33583642412451,0.694998037950466,
-19.3856882633095));
#79697=CARTESIAN_POINT('Ctrl Pts',(-6.2665708099483,-6.07151096112495,-19.1210819284237));
#79698=CARTESIAN_POINT('Ctrl Pts',(-1.23174377969414,-8.14909532475251,
-18.909396860515));
#79699=CARTESIAN_POINT('Ctrl Pts',(2.81953443944885,-7.76311854092135,-18.7506330595834));
#79700=CARTESIAN_POINT('Ctrl Pts',(6.16866108305093,-5.46557305584287,-18.5918692586519));
#79701=CARTESIAN_POINT('Ctrl Pts',(8.70743357014198,-0.630152025265054,
-18.3801841907432));
#79702=CARTESIAN_POINT('Ctrl Pts',(7.10665440379958,5.07444213238395,-18.1684991228345));
#79703=CARTESIAN_POINT('Ctrl Pts',(2.42496184085793,7.86817916277512,-17.9568140549259));
#79704=CARTESIAN_POINT('Ctrl Pts',(-2.99036197747448,8.1968472626595,-17.7451289870171));
#79705=CARTESIAN_POINT('Ctrl Pts',(-8.71622481146367,3.43487287366311,-17.4805226521313));
#79706=CARTESIAN_POINT('Ctrl Pts',(-7.59030180965086,-5.47979766498507,
-17.1629950502683));
#79707=CARTESIAN_POINT('Ctrl Pts',(-0.884936590487096,-8.68044021337483,
-16.8983887153824));
#79708=CARTESIAN_POINT('Ctrl Pts',(4.30497073139276,-7.02795662711218,-16.6867036474737));
#79709=CARTESIAN_POINT('Ctrl Pts',(7.15603497791545,-4.12394802713198,-16.5279398465422));
#79710=CARTESIAN_POINT('Ctrl Pts',(8.23899025497878,-0.209542274176545,
-16.3691760456107));
#79711=CARTESIAN_POINT('Ctrl Pts',(7.06775983111587,5.12476945072128,-16.157490977702));
#79712=CARTESIAN_POINT('Ctrl Pts',(2.16971119591914,8.45853729058758,-15.9458059097933));
#79713=CARTESIAN_POINT('Ctrl Pts',(-3.21116090047537,7.5813672209176,-15.7341208418846));
#79714=CARTESIAN_POINT('Ctrl Pts',(-7.56602061402016,4.34579128259928,-15.5224357739759));
#79715=CARTESIAN_POINT('Ctrl Pts',(-8.88050289184019,-2.984559433186,-15.2578294390901));
#79716=CARTESIAN_POINT('Ctrl Pts',(-2.27872950387278,-9.08010219430069,
-14.940301837227));
#79717=CARTESIAN_POINT('Ctrl Pts',(4.91245411866735,-7.21116839348148,-14.6756955023412));
#79718=CARTESIAN_POINT('Ctrl Pts',(7.81914539187849,-2.60497844355453,-14.4640104344325));
#79719=CARTESIAN_POINT('Ctrl Pts',(8.13052289929572,1.45271515434484,-14.305246633501));
#79720=CARTESIAN_POINT('Ctrl Pts',(6.43851816967762,5.14493461231858,-14.1464828325695));
#79721=CARTESIAN_POINT('Ctrl Pts',(2.10754646363905,8.47199733575168,-13.9347977646608));
#79722=CARTESIAN_POINT('Ctrl Pts',(-3.78659489079374,7.86868469967962,-13.7231126967521));
#79723=CARTESIAN_POINT('Ctrl Pts',(-7.33863206363579,3.7327151916162,-13.5114276288434));
#79724=CARTESIAN_POINT('Ctrl Pts',(-8.58704922933571,-1.54698265557786,
-13.2997425609347));
#79725=CARTESIAN_POINT('Ctrl Pts',(-4.87258745156184,-8.00180093160806,
-13.0351362260488));
#79726=CARTESIAN_POINT('Ctrl Pts',(4.10342411775835,-8.41443845545048,-12.7176086241858));
#79727=CARTESIAN_POINT('Ctrl Pts',(8.40190016589835,-2.35398145052911,-12.4530022892999));
#79728=CARTESIAN_POINT('Ctrl Pts',(7.65976821207041,3.04185770345587,-12.2413172213913));
#79729=CARTESIAN_POINT('Ctrl Pts',(5.28516915482317,6.34687095666369,-12.0825534204597));
#79730=CARTESIAN_POINT('Ctrl Pts',(1.6131336309578,8.08224401233811,-11.9237896195282));
#79731=CARTESIAN_POINT('Ctrl Pts',(-3.84282385859219,7.8389537404691,-11.7121045516196));
#79732=CARTESIAN_POINT('Ctrl Pts',(-7.9639018756391,3.58200595827936,-11.5004194837108));
#79733=CARTESIAN_POINT('Ctrl Pts',(-8.01830375876113,-1.86962244835244,
-11.2887344158021));
#79734=CARTESIAN_POINT('Ctrl Pts',(-5.57375325824777,-6.71296092792641,
-11.0770493478935));
#79735=CARTESIAN_POINT('Ctrl Pts',(1.42454269218899,-9.25967627621681,-10.8124430130076));
#79736=CARTESIAN_POINT('Ctrl Pts',(8.55772751231042,-3.79554526198939,-10.4949154111446));
#79737=CARTESIAN_POINT('Ctrl Pts',(7.94400743510141,3.60914130205669,-10.2303090762587));
#79738=CARTESIAN_POINT('Ctrl Pts',(3.90171698267865,7.2595834548406,-10.01862400835));
#79739=CARTESIAN_POINT('Ctrl Pts',(-0.0432363685727964,8.25917154150874,
-9.85986020741853));
#79740=CARTESIAN_POINT('Ctrl Pts',(-3.97012529449484,7.22239389207724,-9.701096406487));
#79741=CARTESIAN_POINT('Ctrl Pts',(-7.98777786610472,3.5230520454781,-9.48941133857833));
#79742=CARTESIAN_POINT('Ctrl Pts',(-8.39964825188414,-2.38755293440294,
-9.27772627066964));
#79743=CARTESIAN_POINT('Ctrl Pts',(-4.93085602423302,-6.59358340626946,
-9.06604120276094));
#79744=CARTESIAN_POINT('Ctrl Pts',(0.0581756340859371,-8.72508942070459,
-8.85435613485225));
#79745=CARTESIAN_POINT('Ctrl Pts',(7.05240130226248,-6.16721675426193,-8.58974979996641));
#79746=CARTESIAN_POINT('Ctrl Pts',(8.99148210312331,2.60655205203753,-8.27222219810335));
#79747=CARTESIAN_POINT('Ctrl Pts',(3.75390080240723,7.87663531165635,-8.00761586321752));
#79748=CARTESIAN_POINT('Ctrl Pts',(-1.68941943488566,8.06664796081758,-7.7959307953088));
#79749=CARTESIAN_POINT('Ctrl Pts',(-5.35132879720302,6.29118939786795,-7.63716699437731));
#79750=CARTESIAN_POINT('Ctrl Pts',(-7.68815978033691,2.96935474106919,-7.47840319344575));
#79751=CARTESIAN_POINT('Ctrl Pts',(-8.37995396641292,-2.44803236789822,
-7.26671812553711));
#79752=CARTESIAN_POINT('Ctrl Pts',(-4.88911383309103,-7.23540363053417,
-7.05503305762839));
#79753=CARTESIAN_POINT('Ctrl Pts',(0.473181863587134,-8.21977993570431,
-6.84334798971971));
#79754=CARTESIAN_POINT('Ctrl Pts',(5.66277274055247,-6.63803997368177,-6.63166292181101));
#79755=CARTESIAN_POINT('Ctrl Pts',(9.36693595117432,-0.177306255126965,
-6.36705658692516));
#79756=CARTESIAN_POINT('Ctrl Pts',(5.20090347451901,7.7840520978901,-6.04952898506212));
#79757=CARTESIAN_POINT('Ctrl Pts',(-2.1998447589334,8.44356785368252,-5.78492265017626));
#79758=CARTESIAN_POINT('Ctrl Pts',(-6.48684125011734,5.08388020592419,-5.57323758226758));
#79759=CARTESIAN_POINT('Ctrl Pts',(-8.14528665446643,1.36751206783572,-5.41447378133604));
#79760=CARTESIAN_POINT('Ctrl Pts',(-7.79418143112824,-2.67873182434494,
-5.25570998040454));
#79761=CARTESIAN_POINT('Ctrl Pts',(-4.83510194401677,-7.26899444274413,
-5.04402491249584));
#79762=CARTESIAN_POINT('Ctrl Pts',(0.918399634047416,-8.68395311899561,
-4.83233984458715));
#79763=CARTESIAN_POINT('Ctrl Pts',(5.6549118079481,-5.9842005118547,-4.62065477667849));
#79764=CARTESIAN_POINT('Ctrl Pts',(8.60691424489449,-1.43233971771471,-4.40896970876977));
#79765=CARTESIAN_POINT('Ctrl Pts',(7.28074351218162,5.89590534512943,-4.14436337388392));
#79766=CARTESIAN_POINT('Ctrl Pts',(-1.03313762282123,9.30448772696622,-3.82683577202088));
#79767=CARTESIAN_POINT('Ctrl Pts',(-7.12007029059323,5.04358539856761,-3.56222943713502));
#79768=CARTESIAN_POINT('Ctrl Pts',(-8.23664763540929,-0.287370601108435,
-3.35054436922633));
#79769=CARTESIAN_POINT('Ctrl Pts',(-7.1124667608933,-4.19864329744608,-3.19178056829482));
#79770=CARTESIAN_POINT('Ctrl Pts',(-4.23837940774058,-7.06830933872544,
-3.0330167673633));
#79771=CARTESIAN_POINT('Ctrl Pts',(0.981352895278001,-8.67487531489779,
-2.8213316994546));
#79772=CARTESIAN_POINT('Ctrl Pts',(6.29443638452256,-6.05264830836724,-2.60964663154593));
#79773=CARTESIAN_POINT('Ctrl Pts',(8.17987790832939,-0.937157174411471,
-2.39796156363723));
#79774=CARTESIAN_POINT('Ctrl Pts',(7.50740159707945,4.44630291769865,-2.18627649572855));
#79775=CARTESIAN_POINT('Ctrl Pts',(1.77394145444216,9.19911577626299,-1.92167016084267));
#79776=CARTESIAN_POINT('Ctrl Pts',(-6.78178271222209,6.45356424815529,-1.60414255897965));
#79777=CARTESIAN_POINT('Ctrl Pts',(-8.69520103819224,-0.725998020850346,
-1.33953622409378));
#79778=CARTESIAN_POINT('Ctrl Pts',(-6.11672416772516,-5.52354273279491,
-1.1278511561851));
#79779=CARTESIAN_POINT('Ctrl Pts',(-2.73816693432726,-7.79236061590932,
-0.969087355253568));
#79780=CARTESIAN_POINT('Ctrl Pts',(1.30879556680406,-8.13681396711638,-0.81032355432205));
#79781=CARTESIAN_POINT('Ctrl Pts',(6.33648257904002,-6.00579725335872,-0.598638486413376));
#79782=CARTESIAN_POINT('Ctrl Pts',(8.71377174908705,-0.576514988363227,
-0.386953418504678));
#79783=CARTESIAN_POINT('Ctrl Pts',(6.86120775183791,4.54876981752662,-0.175268350595999));
#79784=CARTESIAN_POINT('Ctrl Pts',(2.88221401723271,8.23929217159093,0.0364167173126955));
#79785=CARTESIAN_POINT('Ctrl Pts',(-4.56924755978218,8.17348969005498,0.301023052198559));
#79786=CARTESIAN_POINT('Ctrl Pts',(-9.33928858972985,0.5826915139453,0.618550654061595));
#79787=CARTESIAN_POINT('Ctrl Pts',(-5.56239871442755,-7.52472998215995,
0.936078255924624));
#79788=CARTESIAN_POINT('Ctrl Pts',(3.31770137076159,-8.75652982581897,1.25360585778766));
#79789=CARTESIAN_POINT('Ctrl Pts',(8.16202073879245,-3.0942706070242,1.51821219267352));
#79790=CARTESIAN_POINT('Ctrl Pts',(7.89658816915579,2.32623600553997,1.72989726058221));
#79791=CARTESIAN_POINT('Ctrl Pts',(5.16469719276892,7.04188117863399,1.9415823284909));
#79792=CARTESIAN_POINT('Ctrl Pts',(-0.521226007064963,8.71486864918164,
2.1532673963996));
#79793=CARTESIAN_POINT('Ctrl Pts',(-5.38725527740725,6.23683958004327,2.36495246430828));
#79794=CARTESIAN_POINT('Ctrl Pts',(-7.72719108742934,2.9170121746353,2.5237162652398));
#79795=CARTESIAN_POINT('Ctrl Pts',(-8.16387417419938,-1.12915779804422,
2.68248006617132));
#79796=CARTESIAN_POINT('Ctrl Pts',(-6.14991068781707,-6.18968438231958,
2.89416513408));
#79797=CARTESIAN_POINT('Ctrl Pts',(0.57753512490799,-9.34384939092878,3.15877146896587));
#79798=CARTESIAN_POINT('Ctrl Pts',(8.18381619041701,-4.56023594897756,3.47629907082889));
#79799=CARTESIAN_POINT('Ctrl Pts',(8.23387562737699,2.88686344128947,3.74090540571477));
#79800=CARTESIAN_POINT('Ctrl Pts',(4.54511755749296,6.86517097771756,3.95259047362344));
#79801=CARTESIAN_POINT('Ctrl Pts',(-0.584144307352823,8.71282137839226,
4.16427554153215));
#79802=CARTESIAN_POINT('Ctrl Pts',(-6.00983956524825,6.33232529439785,4.37596060944082));
#79803=CARTESIAN_POINT('Ctrl Pts',(-8.13805209380252,1.30267610342289,4.58764567734951));
#79804=CARTESIAN_POINT('Ctrl Pts',(-7.7901918458369,-2.74384765777136,4.74640947828103));
#79805=CARTESIAN_POINT('Ctrl Pts',(-5.51909885455878,-6.12082461486054,
4.90517327921254));
#79806=CARTESIAN_POINT('Ctrl Pts',(-0.71953763145969,-8.69571274896694,
5.11685834712126));
#79807=CARTESIAN_POINT('Ctrl Pts',(6.45853407846523,-6.77703495389075,5.38146468200709));
#79808=CARTESIAN_POINT('Ctrl Pts',(9.19782165965666,1.78073093027871,5.69899228387014));
#79809=CARTESIAN_POINT('Ctrl Pts',(4.44075853215298,7.51067463980576,5.963598618756));
#79810=CARTESIAN_POINT('Ctrl Pts',(-0.943184956415734,8.17918611230628,
6.1752836866647));
#79811=CARTESIAN_POINT('Ctrl Pts',(-6.05729059692325,6.28997061083414,6.38696875457337));
#79812=CARTESIAN_POINT('Ctrl Pts',(-8.67559507725891,0.974956959624878,
6.59865382248207));
#79813=CARTESIAN_POINT('Ctrl Pts',(-7.06518294672293,-4.24359026031473,
6.81033889039075));
#79814=CARTESIAN_POINT('Ctrl Pts',(-4.19339752672706,-7.11556049246613,
6.96910269132226));
#79815=CARTESIAN_POINT('Ctrl Pts',(-0.281297496662247,-8.23685735403881,
7.12786649225378));
#79816=CARTESIAN_POINT('Ctrl Pts',(5.04883403253763,-7.11634948376184,7.33955156016249));
#79817=CARTESIAN_POINT('Ctrl Pts',(9.30524690078142,-1.02627682884742,7.60415789504834));
#79818=CARTESIAN_POINT('Ctrl Pts',(5.89053541961087,7.28508881838927,7.92168549691137));
#79819=CARTESIAN_POINT('Ctrl Pts',(-1.43868554204972,8.60585578048106,8.18629183179724));
#79820=CARTESIAN_POINT('Ctrl Pts',(-5.98836845278024,5.65049790205964,8.39797689970593));
#79821=CARTESIAN_POINT('Ctrl Pts',(-8.68462793494931,0.911996382211341,
8.60966196761461));
#79822=CARTESIAN_POINT('Ctrl Pts',(-7.26542736414225,-4.84046032623451,
8.82134703552331));
#79823=CARTESIAN_POINT('Ctrl Pts',(-2.67298415987235,-7.79615444096457,
9.03303210343198));
#79824=CARTESIAN_POINT('Ctrl Pts',(1.37351751756126,-8.14427612280999,9.19179590436352));
#79825=CARTESIAN_POINT('Ctrl Pts',(5.08866181120061,-6.48309095431802,9.35055970529502));
#79826=CARTESIAN_POINT('Ctrl Pts',(8.44518758549035,-2.19361840642918,9.56224477320372));
#79827=CARTESIAN_POINT('Ctrl Pts',(7.7802151635707,5.20664152974954,9.82685110808959));
#79828=CARTESIAN_POINT('Ctrl Pts',(-0.184212794636262,9.36680267052184,
10.1443787099526));
#79829=CARTESIAN_POINT('Ctrl Pts',(-6.64221354075295,5.65787672919185,10.4089850448385));
#79830=CARTESIAN_POINT('Ctrl Pts',(-8.2201265957422,0.467120987666701,10.6206701127472));
#79831=CARTESIAN_POINT('Ctrl Pts',(-7.23179673954533,-4.89444743437479,
10.8323551806559));
#79832=CARTESIAN_POINT('Ctrl Pts',(-2.44185285290457,-8.38175671313248,
11.0440402485646));
#79833=CARTESIAN_POINT('Ctrl Pts',(2.97502269802595,-7.68596827553516,11.2557253164733));
#79834=CARTESIAN_POINT('Ctrl Pts',(6.29513342006344,-5.34668861625921,11.4144891174048));
#79835=CARTESIAN_POINT('Ctrl Pts',(8.06789143937566,-1.68347113820463,11.5732529183363));
#79836=CARTESIAN_POINT('Ctrl Pts',(7.87386528083567,3.75970751607194,11.784937986245));
#79837=CARTESIAN_POINT('Ctrl Pts',(2.59992159168183,8.99340156602993,12.0495443211308));
#79838=CARTESIAN_POINT('Ctrl Pts',(-6.1724150737335,7.04785206852052,12.3670719229939));
#79839=CARTESIAN_POINT('Ctrl Pts',(-8.72512994398167,0.0517422876257268,
12.6316782578797));
#79840=CARTESIAN_POINT('Ctrl Pts',(-6.58994591167402,-4.93571637640952,
12.8433633257884));
#79841=CARTESIAN_POINT('Ctrl Pts',(-2.38135891453366,-8.40140639953382,
13.0550483936971));
#79842=CARTESIAN_POINT('Ctrl Pts',(3.52894077140471,-7.98517801838488,13.2667334616058));
#79843=CARTESIAN_POINT('Ctrl Pts',(7.22531924878866,-3.9647988775456,13.4784185295145));
#79844=CARTESIAN_POINT('Ctrl Pts',(8.25920117616535,-0.0371465646322164,
13.637182330446));
#79845=CARTESIAN_POINT('Ctrl Pts',(7.25670460142574,3.90706868104012,13.7959461313775));
#79846=CARTESIAN_POINT('Ctrl Pts',(3.60328291092042,7.94666642882579,14.0076311992862));
#79847=CARTESIAN_POINT('Ctrl Pts',(-3.80185415876567,8.55492659034786,14.2722375341721));
#79848=CARTESIAN_POINT('Ctrl Pts',(-9.26072412706714,1.41771480367452,14.5897651360351));
#79849=CARTESIAN_POINT('Ctrl Pts',(-6.70884936900753,-5.57870145711901,
14.854371470921));
#79850=CARTESIAN_POINT('Ctrl Pts',(-1.86370974865146,-8.01968012079831,
15.0660565388297));
#79851=CARTESIAN_POINT('Ctrl Pts',(3.58787706353087,-7.96125856551249,15.2777416067384));
#79852=CARTESIAN_POINT('Ctrl Pts',(7.8417850655293,-3.83704286390198,15.489426674647));
#79853=CARTESIAN_POINT('Ctrl Pts',(8.08105239231934,1.61909252944133,15.7011117425558));
#79854=CARTESIAN_POINT('Ctrl Pts',(6.34297228097692,5.28984750048557,15.8598755434872));
#79855=CARTESIAN_POINT('Ctrl Pts',(3.03620904660201,7.66200900391343,16.0186393444188));
#79856=CARTESIAN_POINT('Ctrl Pts',(-2.36017584191269,8.40016220452973,16.2303244123274));
#79857=CARTESIAN_POINT('Ctrl Pts',(-8.41746177427002,4.09721872609548,16.4949307472134));
#79858=CARTESIAN_POINT('Ctrl Pts',(-7.99820601778327,-4.87848615036436,
16.8124583490763));
#79859=CARTESIAN_POINT('Ctrl Pts',(-1.54065068654177,-8.58818754253497,
17.0770646839623));
#79860=CARTESIAN_POINT('Ctrl Pts',(3.73812522137653,-7.33587779999464,17.2887497518709));
#79861=CARTESIAN_POINT('Ctrl Pts',(7.87147455696352,-3.78079198965415,17.5004348197796));
#79862=CARTESIAN_POINT('Ctrl Pts',(8.47044106094497,2.11379260724371,17.7121198876883));
#79863=CARTESIAN_POINT('Ctrl Pts',(5.14018585653609,6.44230996976773,17.923804955597));
#79864=CARTESIAN_POINT('Ctrl Pts',(1.44671982465644,8.13159182968389,18.0825687565285));
#79865=CARTESIAN_POINT('Ctrl Pts',(-2.61074308009303,7.81722251956952,18.24133255746));
#79866=CARTESIAN_POINT('Ctrl Pts',(-7.21478856708646,4.9071357225367,18.4530176253687));
#79867=CARTESIAN_POINT('Ctrl Pts',(-9.07841953461377,-2.28542397911376,
18.7176239602546));
#79868=CARTESIAN_POINT('Ctrl Pts',(-2.97801069914672,-8.88270110371666,
19.0351515621176));
#79869=CARTESIAN_POINT('Ctrl Pts',(4.35136880768079,-7.56281424492468,19.2997578970034));
#79870=CARTESIAN_POINT('Ctrl Pts',(7.58373286757206,-3.20557000554551,19.5114429649122));
#79871=CARTESIAN_POINT('Ctrl Pts',(8.45693518308693,2.17594739803703,19.7231280328208));
#79872=CARTESIAN_POINT('Ctrl Pts',(5.11955673730547,7.07153659163915,19.9348131007296));
#79873=CARTESIAN_POINT('Ctrl Pts',(-0.215617128995803,8.23883351209298,
20.1464981686382));
#79874=CARTESIAN_POINT('Ctrl Pts',(-4.12922331496766,7.15299229349241,20.3052619695698));
#79875=CARTESIAN_POINT('Ctrl Pts',(-7.0311289305844,4.29978758919758,20.4640257705013));
#79876=CARTESIAN_POINT('Ctrl Pts',(-8.6797853573168,-0.8913367590688,20.67571083841));
#79877=CARTESIAN_POINT('Ctrl Pts',(-5.47419956556276,-7.5943402035435,20.9403171732958));
#79878=CARTESIAN_POINT('Ctrl Pts',(3.44129873439396,-8.71368978348783,21.2578447751588));
#79879=CARTESIAN_POINT('Ctrl Pts',(8.19904993880632,-2.98431732640053,21.5224511100447));
#79880=CARTESIAN_POINT('Ctrl Pts',(7.8663890100263,2.43076268074111,21.7341361779534));
#79881=CARTESIAN_POINT('Ctrl Pts',(5.06920075424374,7.11039404555973,21.9458212458621));
#79882=CARTESIAN_POINT('Ctrl Pts',(-0.636572166304518,8.70696656881521,
22.1575063137708));
#79883=CARTESIAN_POINT('Ctrl Pts',(-5.47011995174442,6.16462943734903,22.3691913816794));
#79884=CARTESIAN_POINT('Ctrl Pts',(-7.76519537751747,2.8138096390156,22.527955182611));
#79885=CARTESIAN_POINT('Ctrl Pts',(-8.14818489938332,-1.23775207379351,
22.6867189835425));
#79886=CARTESIAN_POINT('Ctrl Pts',(-6.06688873660663,-6.27104585573993,
22.8984040514512));
#79887=CARTESIAN_POINT('Ctrl Pts',(0.701881505993874,-9.33532143861735,
23.163010386337));
#79888=CARTESIAN_POINT('Ctrl Pts',(8.24383438190629,-4.45085624412889,23.4805379882001));
#79889=CARTESIAN_POINT('Ctrl Pts',(8.19469437259043,2.99625665514973,23.7451443230859));
#79890=CARTESIAN_POINT('Ctrl Pts',(4.45329755143643,6.92508658325054,23.9568293909947));
#79891=CARTESIAN_POINT('Ctrl Pts',(-0.700120258078465,8.70427087091072,
24.1685144589033));
#79892=CARTESIAN_POINT('Ctrl Pts',(-6.09362991369378,6.25173299400388,24.3801995268121));
#79893=CARTESIAN_POINT('Ctrl Pts',(-8.15467833577869,1.19418994564688,24.5918845947207));
#79894=CARTESIAN_POINT('Ctrl Pts',(-7.75296212610164,-2.84734300829175,
24.7506483956523));
#79895=CARTESIAN_POINT('Ctrl Pts',(-5.43710132964985,-6.19377723863542,
24.9094121965837));
#79896=CARTESIAN_POINT('Ctrl Pts',(-0.60367674685806,-8.70452350519323,
25.1210972644925));
#79897=CARTESIAN_POINT('Ctrl Pts',(6.54820811350255,-6.69042857468967,25.3857035993782));
#79898=CARTESIAN_POINT('Ctrl Pts',(9.1732929286674,1.90305634889304,25.7032312012414));
#79899=CARTESIAN_POINT('Ctrl Pts',(4.34034841940176,7.56914429786426,25.9678375361272));
#79900=CARTESIAN_POINT('Ctrl Pts',(-1.05201992362399,8.16590089013109,26.1795226040359));
#79901=CARTESIAN_POINT('Ctrl Pts',(-6.14051426705278,6.208750623602,26.3912076719445));
#79902=CARTESIAN_POINT('Ctrl Pts',(-8.68780888576682,0.859341444230168,
26.6028927398533));
#79903=CARTESIAN_POINT('Ctrl Pts',(-7.00804646742056,-4.33729790270126,
26.8145778077619));
#79904=CARTESIAN_POINT('Ctrl Pts',(-4.09827092580945,-7.17077118267629,
26.9733416086935));
#79905=CARTESIAN_POINT('Ctrl Pts',(-0.171585965343747,-8.23987291207912,
27.132105409625));
#79906=CARTESIAN_POINT('Ctrl Pts',(5.14315163742236,-7.04848539060961,27.3437904775337));
#79907=CARTESIAN_POINT('Ctrl Pts',(9.31808828596101,-0.902271968865942,
27.6083968124195));
#79908=CARTESIAN_POINT('Ctrl Pts',(5.79300080182397,7.3628845116753,27.9259244142826));
#79909=CARTESIAN_POINT('Ctrl Pts',(-1.55315835309708,8.58593436580423,28.1905307491684));
#79910=CARTESIAN_POINT('Ctrl Pts',(-6.06308265180774,5.57025242017754,28.4022158170771));
#79911=CARTESIAN_POINT('Ctrl Pts',(-8.69600252795008,0.796266163945025,
28.6139008849858));
#79912=CARTESIAN_POINT('Ctrl Pts',(-7.20032487283164,-4.93678161144116,
28.8255859528945));
#79913=CARTESIAN_POINT('Ctrl Pts',(-2.56892920494273,-7.83105811026166,
29.0372710208032));
#79914=CARTESIAN_POINT('Ctrl Pts',(1.48184945465475,-8.12526344984419,29.1960348217347));
#79915=CARTESIAN_POINT('Ctrl Pts',(5.17454306032357,-6.41475264274277,29.3547986226662));
#79916=CARTESIAN_POINT('Ctrl Pts',(8.47365020358878,-2.08096306896043,29.5664836905749));
#79917=CARTESIAN_POINT('Ctrl Pts',(7.71019075313911,5.30978554755018,29.8310900254608));
#79918=CARTESIAN_POINT('Ctrl Pts',(-0.308930032296374,9.36351904239792,
30.1486176273238));
#79919=CARTESIAN_POINT('Ctrl Pts',(-6.71696802439972,5.56892362695756,30.4132239622097));
#79920=CARTESIAN_POINT('Ctrl Pts',(-8.22561816670618,0.357615775237553,
30.6249090301183));
#79921=CARTESIAN_POINT('Ctrl Pts',(-7.16597830778628,-4.99031608841498,
30.8365940980271));
#79922=CARTESIAN_POINT('Ctrl Pts',(-2.33002018555819,-8.41353058402189,
31.0482791659357));
#79923=CARTESIAN_POINT('Ctrl Pts',(3.07710954772786,-7.64566970366785,31.2599642338444));
#79924=CARTESIAN_POINT('Ctrl Pts',(6.36577472448202,-5.26238501943575,31.4187280347759));
#79925=CARTESIAN_POINT('Ctrl Pts',(8.08959410633424,-1.57588532117043,31.5774918357075));
#79926=CARTESIAN_POINT('Ctrl Pts',(7.82310074732932,3.86422692970949,31.7891769036162));
#79927=CARTESIAN_POINT('Ctrl Pts',(2.47992990429178,9.02722613434294,32.053783238502));
#79928=CARTESIAN_POINT('Ctrl Pts',(-6.2657209013968,6.96503181672575,32.371310840365));
#79929=CARTESIAN_POINT('Ctrl Pts',(-8.72504532207758,-0.0644509998803956,
32.6359171752509));
#79930=CARTESIAN_POINT('Ctrl Pts',(-6.52363483210948,-5.02303412734111,
32.8476022431596));
#79931=CARTESIAN_POINT('Ctrl Pts',(-2.26926994495205,-8.43237295705634,
33.0592873110683));
#79932=CARTESIAN_POINT('Ctrl Pts',(3.63496294949945,-7.93747663361272,33.270972378977));
#79933=CARTESIAN_POINT('Ctrl Pts',(7.27747605933994,-3.86823093830196,33.4826574468857));
#79934=CARTESIAN_POINT('Ctrl Pts',(8.25896350304176,0.072840861189232,33.6414212478171));
#79935=CARTESIAN_POINT('Ctrl Pts',(7.20403244760854,4.00335657224304,33.8001850487487));
#79936=CARTESIAN_POINT('Ctrl Pts',(3.49714116543082,7.99394512967198,34.0118701166574));
#79937=CARTESIAN_POINT('Ctrl Pts',(-3.9154392277668,8.50354041940355,34.2764764515432));
#79938=CARTESIAN_POINT('Ctrl Pts',(-9.27878206673691,1.29426812531432,34.5940040534063));
#79939=CARTESIAN_POINT('Ctrl Pts',(-6.63396539819317,-5.66754557981407,
34.8586103882921));
#79940=CARTESIAN_POINT('Ctrl Pts',(-1.75674995881094,-8.04378722054254,
35.0702954562009));
#79941=CARTESIAN_POINT('Ctrl Pts',(3.69357549100292,-7.91277447310475,35.2819805241094));
#79942=CARTESIAN_POINT('Ctrl Pts',(7.89218594411954,-3.73227704984803,35.4936655920182));
#79943=CARTESIAN_POINT('Ctrl Pts',(8.05877511145054,1.72656076909226,35.7053506599269));
#79944=CARTESIAN_POINT('Ctrl Pts',(6.27196729271126,5.37384501216737,35.8641144608584));
#79945=CARTESIAN_POINT('Ctrl Pts',(2.93390824027782,7.70176147308837,36.0228782617899));
#79946=CARTESIAN_POINT('Ctrl Pts',(-2.47182781457673,8.36798794945601,36.2345633296987));
#79947=CARTESIAN_POINT('Ctrl Pts',(-8.47127625499191,3.9847638101116,36.4991696645844));
#79948=CARTESIAN_POINT('Ctrl Pts',(-7.93253217842265,-4.98456215333826,
36.8166972664475));
#79949=CARTESIAN_POINT('Ctrl Pts',(-1.42614898002516,-8.60794219836928,
37.0813036013334));
#79950=CARTESIAN_POINT('Ctrl Pts',(3.83548240717228,-7.28544837133703,37.2929886692421));
#79951=CARTESIAN_POINT('Ctrl Pts',(7.92112373497429,-3.67563580148848,37.5046737371507));
#79952=CARTESIAN_POINT('Ctrl Pts',(8.44154155094658,2.22640229900672,37.7163588050595));
#79953=CARTESIAN_POINT('Ctrl Pts',(5.05394068509545,6.51018831815488,37.9280438729681));
#79954=CARTESIAN_POINT('Ctrl Pts',(1.33830673024671,8.15013613575943,38.0868076738997));
#79955=CARTESIAN_POINT('Ctrl Pts',(-2.71461008497256,7.78176326016691,38.2455714748312));
#79956=CARTESIAN_POINT('Ctrl Pts',(-7.27949499470204,4.81062445938832,38.4572565427398));
#79957=CARTESIAN_POINT('Ctrl Pts',(-9.04718057646558,-2.40611463309362,
38.7218628776258));
#79958=CARTESIAN_POINT('Ctrl Pts',(-2.85945963599839,-8.9215703333157,39.0393904794887));
#79959=CARTESIAN_POINT('Ctrl Pts',(4.45169362994984,-7.5041984001464,39.3039968143747));
#79960=CARTESIAN_POINT('Ctrl Pts',(7.6257475824808,-3.10429655082013,39.5156818822832));
#79961=CARTESIAN_POINT('Ctrl Pts',(8.42720918276421,2.28837172677223,39.7273669501921));
#79962=CARTESIAN_POINT('Ctrl Pts',(5.02493426218586,7.13908443808384,39.9390520181006));
#79963=CARTESIAN_POINT('Ctrl Pts',(-0.325310915258221,8.23523170255197,
40.1507370860094));
#79964=CARTESIAN_POINT('Ctrl Pts',(-4.22411041690589,7.09737100068912,40.3095008869408));
#79965=CARTESIAN_POINT('Ctrl Pts',(-7.08776385648449,4.20577589339118,40.4682646878724));
#79966=CARTESIAN_POINT('Ctrl Pts',(-8.66714618919647,-1.00684259060368,
40.6799497557811));
#79967=CARTESIAN_POINT('Ctrl Pts',(-5.37258369985886,-7.66656431517888,
40.944556090667));
#79968=CARTESIAN_POINT('Ctrl Pts',(3.55702995286921,-8.66709089236948,41.2620836925299));
#79969=CARTESIAN_POINT('Ctrl Pts',(8.23806376983713,-2.87486958448408,41.5266900274159));
#79970=CARTESIAN_POINT('Ctrl Pts',(7.83332211050503,2.53530037278001,41.7383750953245));
#79971=CARTESIAN_POINT('Ctrl Pts',(4.9740652966121,7.17726787816896,41.9500601632332));
#79972=CARTESIAN_POINT('Ctrl Pts',(-0.752462547816077,8.69771757804969,
42.1617452311419));
#79973=CARTESIAN_POINT('Ctrl Pts',(-5.55172656596247,6.09123965405151,42.3734302990506));
#79974=CARTESIAN_POINT('Ctrl Pts',(-7.80197710260423,2.71015446535334,42.5321940999822));
#79975=CARTESIAN_POINT('Ctrl Pts',(-8.1309798082442,-1.34614810056075,42.6909579009136));
#79976=CARTESIAN_POINT('Ctrl Pts',(-5.98284204359866,-6.35127988270911,
42.9026429688224));
#79977=CARTESIAN_POINT('Ctrl Pts',(0.826133620683909,-9.3251470364568,43.1672493037082));
#79978=CARTESIAN_POINT('Ctrl Pts',(8.30237349258994,-4.34068209061006,43.4847769055712));
#79979=CARTESIAN_POINT('Ctrl Pts',(8.15406792911807,3.10511610266412,43.7493832404571));
#79980=CARTESIAN_POINT('Ctrl Pts',(4.36068436308684,6.98377513617638,43.9610683083658));
#79981=CARTESIAN_POINT('Ctrl Pts',(-0.815969107408102,8.69417587731647,
44.1727533762745));
#79982=CARTESIAN_POINT('Ctrl Pts',(-6.17634116129579,6.17003248068141,44.3844384441832));
#79983=CARTESIAN_POINT('Ctrl Pts',(-8.16985776599225,1.08549181008368,44.5961235120918));
#79984=CARTESIAN_POINT('Ctrl Pts',(-7.71435786793978,-2.95033330676227,
44.7548873130234));
#79985=CARTESIAN_POINT('Ctrl Pts',(-5.35413943147089,-6.26563151638265,
44.9136511139549));
#79986=CARTESIAN_POINT('Ctrl Pts',(-0.487708926553712,-8.71179057772378,
45.1253361818636));
#79987=CARTESIAN_POINT('Ctrl Pts',(6.63672096915272,-6.60263574554677,45.3899425167495));
#79988=CARTESIAN_POINT('Ctrl Pts',(9.14713737891418,2.0250442942005,45.7074701186125));
#79989=CARTESIAN_POINT('Ctrl Pts',(4.23916861421562,7.62627164897394,45.9720764534983));
#79990=CARTESIAN_POINT('Ctrl Pts',(-1.16066833514873,8.15116754109057,46.183761521407));
#79991=CARTESIAN_POINT('Ctrl Pts',(-6.2226489802212,6.12642958328167,46.3954465893157));
#79992=CARTESIAN_POINT('Ctrl Pts',(-8.69848201415944,0.743573535518887,
46.6071316572243));
#79993=CARTESIAN_POINT('Ctrl Pts',(-6.94966718953088,-4.43023637530331,
46.8188167251331));
#79994=CARTESIAN_POINT('Ctrl Pts',(-4.00241754418439,-7.22471021824686,
46.9775805260645));
#79995=CARTESIAN_POINT('Ctrl Pts',(-0.0618440048273914,-8.24142722286535,
47.1363443269962));
#79996=CARTESIAN_POINT('Ctrl Pts',(5.23655716281452,-6.97937132897605,47.3480293949047));
#79997=CARTESIAN_POINT('Ctrl Pts',(9.32927721475058,-0.778107101303471,
47.6126357297907));
#79998=CARTESIAN_POINT('Ctrl Pts',(5.69443886140186,7.43937448149761,47.9301633316538));
#79999=CARTESIAN_POINT('Ctrl Pts',(-1.66735572920219,8.56449033369709,48.1947696665395));
#80000=CARTESIAN_POINT('Ctrl Pts',(-6.13672163238016,5.48901911764058,48.4064547344483));
#80001=CARTESIAN_POINT('Ctrl Pts',(-8.70583498418567,0.68039473696197,48.6181398023569));
#80002=CARTESIAN_POINT('Ctrl Pts',(-7.13394548613349,-5.03222741479912,
48.8298248702656));
#80003=CARTESIAN_POINT('Ctrl Pts',(-2.46441867975,-7.8645730308264,49.0415099381744));
#80004=CARTESIAN_POINT('Ctrl Pts',(1.58991860266646,-8.10480985418721,49.2002737391058));
#80005=CARTESIAN_POINT('Ctrl Pts',(5.25950666332379,-6.34527674803642,49.3590375400374));
#80006=CARTESIAN_POINT('Ctrl Pts',(8.5006101165834,-1.96793869645312,49.570722607946));
#80007=CARTESIAN_POINT('Ctrl Pts',(7.63879902841993,5.4119879355161,49.835328942832));
#80008=CARTESIAN_POINT('Ctrl Pts',(-0.433592484742793,9.35857490109356,
50.1528565446949));
#80009=CARTESIAN_POINT('Ctrl Pts',(-6.79053133046797,5.47898293970952,50.4174628795808));
#80010=CARTESIAN_POINT('Ctrl Pts',(-8.22965101821615,0.248047143734746,
50.6291479474895));
#80011=CARTESIAN_POINT('Ctrl Pts',(-7.09888907160326,-5.08529976688182,
50.8408330153982));
#80012=CARTESIAN_POINT('Ctrl Pts',(-2.21777431573672,-8.44381241133431,
51.0525180833069));
#80013=CARTESIAN_POINT('Ctrl Pts',(3.17865070718642,-7.60401525958635,51.2642031512156));
#80014=CARTESIAN_POINT('Ctrl Pts',(6.43528713144793,-5.1771481987163,51.422966952147));
#80015=CARTESIAN_POINT('Ctrl Pts',(8.10986217614476,-1.46802003887728,51.5817307530786));
#80016=CARTESIAN_POINT('Ctrl Pts',(7.77094887625473,3.96806106684268,51.7934158209873));
#80017=CARTESIAN_POINT('Ctrl Pts',(2.35949842961515,9.05944982714925,52.0580221558731));
#80018=CARTESIAN_POINT('Ctrl Pts',(-6.35791557494276,6.88097639612989,52.3755497577362));
#80019=CARTESIAN_POINT('Ctrl Pts',(-8.72341341312283,-0.180632857834922,
52.640156092622));
#80020=CARTESIAN_POINT('Ctrl Pts',(-6.45616686025931,-5.10946110039852,
52.8518411605307));
#80021=CARTESIAN_POINT('Ctrl Pts',(-2.15677854662195,-8.46184412985793,
53.0635262284394));
#80022=CARTESIAN_POINT('Ctrl Pts',(3.74034050916199,-7.888367627318,53.2752112963481));
#80023=CARTESIAN_POINT('Ctrl Pts',(7.32834229169904,-3.77097701331254,53.4868963642568));
#80024=CARTESIAN_POINT('Ctrl Pts',(8.25726119895179,0.182815371261993,53.6456601651883));
#80025=CARTESIAN_POINT('Ctrl Pts',(7.15008273743028,4.09893451068573,53.8044239661198));
#80026=CARTESIAN_POINT('Ctrl Pts',(3.39037924938521,8.0398062025158,54.0161090340285));
#80027=CARTESIAN_POINT('Ctrl Pts',(-4.02832995383727,8.45064622842747,54.2807153689144));
#80028=CARTESIAN_POINT('Ctrl Pts',(-9.29519449327465,1.17059194815611,54.5982429707774));
#80029=CARTESIAN_POINT('Ctrl Pts',(-6.55790501479776,-5.75538466973715,
54.8628493056633));
#80030=CARTESIAN_POINT('Ctrl Pts',(-1.64947856894098,-8.06646779092916,
55.074534373572));
#80031=CARTESIAN_POINT('Ctrl Pts',(3.79861874928655,-7.86288728353405,55.2862194414806));
#80032=CARTESIAN_POINT('Ctrl Pts',(7.94118755034809,-3.62684906824275,55.4979045093893));
#80033=CARTESIAN_POINT('Ctrl Pts',(8.03506830749714,1.83372246351997,55.709589577298));
#80034=CARTESIAN_POINT('Ctrl Pts',(6.19985085699822,5.45689028163728,55.8683533782295));
#80035=CARTESIAN_POINT('Ctrl Pts',(2.83108565350718,7.74014675877405,56.0271171791611));
#80036=CARTESIAN_POINT('Ctrl Pts',(-2.58303822757656,8.33433267444918,56.2388022470697));
#80037=CARTESIAN_POINT('Ctrl Pts',(-8.52359509037462,3.8715961450888,56.5034085819557));
#80038=CARTESIAN_POINT('Ctrl Pts',(-7.86543999841054,-5.08974355141217,
56.8209361838186));
#80039=CARTESIAN_POINT('Ctrl Pts',(-1.31141381205942,-8.62618819555302,
57.0855425187045));
#80040=CARTESIAN_POINT('Ctrl Pts',(3.93218530965132,-7.2337031704381,57.2972275866132));
#80041=CARTESIAN_POINT('Ctrl Pts',(7.96930150902302,-3.56988901935955,57.5089126545219));
#80042=CARTESIAN_POINT('Ctrl Pts',(8.41128061848056,2.3387416807266,57.7205977224305));
#80043=CARTESIAN_POINT('Ctrl Pts',(4.96663170753987,6.57675829270832,57.9322827903394));
#80044=CARTESIAN_POINT('Ctrl Pts',(1.23000494800474,8.16755528504679,58.0910465912707));
#80045=CARTESIAN_POINT('Ctrl Pts',(-2.81863160931247,7.74433999573533,58.2498103922024));
#80046=CARTESIAN_POINT('Ctrl Pts',(-7.3415364539406,4.71452192664591,58.4614954601109));
#80047=CARTESIAN_POINT('Ctrl Pts',(-9.01718004225608,-2.52898934108735,
58.7261017949969));
#80048=CARTESIAN_POINT('Ctrl Pts',(-2.73543320839727,-8.95429455413672,
59.0436293968599));
#80049=CARTESIAN_POINT('Ctrl Pts',(4.54288040872128,-7.45192048792684,59.3082357317457));
#80050=CARTESIAN_POINT('Ctrl Pts',(7.67764277639221,-2.99214435473956,59.5199207996544));
#80051=CARTESIAN_POINT('Ctrl Pts',(8.19311435259575,1.03068185261496,59.678684600586));
#80052=CARTESIAN_POINT('Ctrl Pts',(6.69025189752799,4.83429374004656,59.8375130498614));
#80053=CARTESIAN_POINT('Ctrl Pts',(4.60790684111087,6.57207682948263,59.9434202321596));
#80054=CARTESIAN_POINT('Ctrl Pts',(3.41916591565856,7.14122334375564,59.9964061474807));
#80055=CARTESIAN_POINT('Ctrl Pts',(4.37098981058075,-6.1335693280065,-60.4415856688784));
#80056=CARTESIAN_POINT('Ctrl Pts',(5.39136601496843,-5.40642193064725,-60.3886321829441));
#80057=CARTESIAN_POINT('Ctrl Pts',(7.05859103065204,-3.43860440421756,-60.2827574300326));
#80058=CARTESIAN_POINT('Ctrl Pts',(7.8464956002649,0.370392094075909,-60.1239614101439));
#80059=CARTESIAN_POINT('Ctrl Pts',(6.70727280426418,4.05641232746857,-59.9651976092124));
#80060=CARTESIAN_POINT('Ctrl Pts',(3.04204627735459,7.72471705861125,-59.7535125413037));
#80061=CARTESIAN_POINT('Ctrl Pts',(-4.02405469353209,7.94559028961535,-59.4889062064178));
#80062=CARTESIAN_POINT('Ctrl Pts',(-8.86316855372843,0.89937772589701,-59.1713786045548));
#80063=CARTESIAN_POINT('Ctrl Pts',(-6.11135702485761,-5.6157628730622,-58.906772269669));
#80064=CARTESIAN_POINT('Ctrl Pts',(-1.3784275667397,-7.71753525273869,-58.6950872017603));
#80065=CARTESIAN_POINT('Ctrl Pts',(2.48488421585976,-7.45381729160668,-58.5363234008287));
#80066=CARTESIAN_POINT('Ctrl Pts',(5.7272963799356,-5.35350558506947,-58.3775595998972));
#80067=CARTESIAN_POINT('Ctrl Pts',(8.26430431855175,-0.819906288515342,
-58.1658745319886));
#80068=CARTESIAN_POINT('Ctrl Pts',(6.88637636880123,4.64543106244188,-57.9541894640798));
#80069=CARTESIAN_POINT('Ctrl Pts',(2.50530954563564,7.42060282805745,-57.7425043961712));
#80070=CARTESIAN_POINT('Ctrl Pts',(-2.63598306863222,7.87035890477309,-57.5308193282625));
#80071=CARTESIAN_POINT('Ctrl Pts',(-8.20145258310699,3.48710685812043,-57.2662129933766));
#80072=CARTESIAN_POINT('Ctrl Pts',(-7.35663752044499,-5.01859065699272,
-56.9486853915136));
#80073=CARTESIAN_POINT('Ctrl Pts',(-1.06140553829354,-8.23203608828134,
-56.6840790566278));
#80074=CARTESIAN_POINT('Ctrl Pts',(3.91566660751038,-6.7921191913466,-56.472393988719));
#80075=CARTESIAN_POINT('Ctrl Pts',(6.70038556434063,-4.10285058779559,-56.3136301877875));
#80076=CARTESIAN_POINT('Ctrl Pts',(7.82935707026716,-0.407975901695247,
-56.154866386856));
#80077=CARTESIAN_POINT('Ctrl Pts',(6.85073828888755,4.69422716676729,-55.9431813189473));
#80078=CARTESIAN_POINT('Ctrl Pts',(2.27751233819034,7.98847381449242,-55.7314962510387));
#80079=CARTESIAN_POINT('Ctrl Pts',(-2.86151704673791,7.2906631041924,-55.5198111831299));
#80080=CARTESIAN_POINT('Ctrl Pts',(-7.08463059670744,4.32419256030661,-55.3081261152213));
#80081=CARTESIAN_POINT('Ctrl Pts',(-8.52030387347526,-2.61312521513784,
-55.0435197803354));
#80082=CARTESIAN_POINT('Ctrl Pts',(-2.39692682072872,-8.57677385790295,
-54.7259921784723));
#80083=CARTESIAN_POINT('Ctrl Pts',(4.48869838858835,-6.98173025450676,-54.4613858435864));
#80084=CARTESIAN_POINT('Ctrl Pts',(7.36943309221841,-2.67522160566258,-54.2497007756778));
#80085=CARTESIAN_POINT('Ctrl Pts',(7.76832283941139,1.17545456122282,-54.0909369747463));
#80086=CARTESIAN_POINT('Ctrl Pts',(6.25288685299758,4.72934343760845,-53.9321731738148));
#80087=CARTESIAN_POINT('Ctrl Pts',(2.21873946141778,8.00284801499922,-53.720488105906));
#80088=CARTESIAN_POINT('Ctrl Pts',(-3.40143338883267,7.5784580409641,-53.5088030379974));
#80089=CARTESIAN_POINT('Ctrl Pts',(-6.88393194308128,3.73544245026433,-53.2971179700887));
#80090=CARTESIAN_POINT('Ctrl Pts',(-8.20483342319923,-1.25353081970317,
-53.08543290218));
#80091=CARTESIAN_POINT('Ctrl Pts',(-4.83617598709369,-7.48567990974514,
-52.8208265672942));
#80092=CARTESIAN_POINT('Ctrl Pts',(3.68888887765348,-8.10545538177222,-52.503298965431));
#80093=CARTESIAN_POINT('Ctrl Pts',(7.92994793033033,-2.4513050089426,-52.2386926305453));
#80094=CARTESIAN_POINT('Ctrl Pts',(7.36092771473285,2.69853626749654,-52.0270075626365));
#80095=CARTESIAN_POINT('Ctrl Pts',(5.18658635397621,5.90151295233514,-51.8682437617051));
#80096=CARTESIAN_POINT('Ctrl Pts',(1.73871613664041,7.64474653273967,-51.7094799607735));
#80097=CARTESIAN_POINT('Ctrl Pts',(-3.45565611673432,7.55161055380676,-51.4977948928649));
#80098=CARTESIAN_POINT('Ctrl Pts',(-7.48233483608931,3.6079690646464,-51.2861098249562));
#80099=CARTESIAN_POINT('Ctrl Pts',(-7.67217224580976,-1.57474516341014,
-51.0744247570474));
#80100=CARTESIAN_POINT('Ctrl Pts',(-5.47028243379752,-6.24232657838186,
-50.8627396891388));
#80101=CARTESIAN_POINT('Ctrl Pts',(1.12005997969442,-8.84134987042121,-50.5981333542529));
#80102=CARTESIAN_POINT('Ctrl Pts',(8.04160920853718,-3.8260723249102,-50.2806057523899));
#80103=CARTESIAN_POINT('Ctrl Pts',(7.64558894461407,3.23078010923851,-50.015999417504));
#80104=CARTESIAN_POINT('Ctrl Pts',(3.8941480339976,6.80448130998449,-49.8043143495953));
#80105=CARTESIAN_POINT('Ctrl Pts',(0.168113770862944,7.85495199818969,-49.6455505486638));
#80106=CARTESIAN_POINT('Ctrl Pts',(-3.59232951311789,6.96853298928954,-49.4867867477323));
#80107=CARTESIAN_POINT('Ctrl Pts',(-7.50653259438449,3.55251313339772,-49.2751016798236));
#80108=CARTESIAN_POINT('Ctrl Pts',(-8.04792309678225,-2.05759791967763,
-49.0634166119149));
#80109=CARTESIAN_POINT('Ctrl Pts',(-4.85591089761415,-6.14509386856656,
-48.8517315440062));
#80110=CARTESIAN_POINT('Ctrl Pts',(-0.165710669289473,-8.29838363723738,
-48.6400464760975));
#80111=CARTESIAN_POINT('Ctrl Pts',(6.55007496031395,-6.04322098748476,-48.3754401412117));
#80112=CARTESIAN_POINT('Ctrl Pts',(8.61626085969852,2.25085692479618,-48.0579125393486));
#80113=CARTESIAN_POINT('Ctrl Pts',(3.76921754196017,7.39499625054909,-47.7933062044627));
#80114=CARTESIAN_POINT('Ctrl Pts',(-1.40216082924845,7.71357892404924,-47.581621136554));
#80115=CARTESIAN_POINT('Ctrl Pts',(-4.92934118453569,6.11801672278348,-47.4228573356226));
#80116=CARTESIAN_POINT('Ctrl Pts',(-7.23564485061669,3.01839807669211,-47.264093534691));
#80117=CARTESIAN_POINT('Ctrl Pts',(-8.0307274151131,-2.1156082665917,-47.0524084667824));
#80118=CARTESIAN_POINT('Ctrl Pts',(-4.83247631834833,-6.75647452473442,
-46.8407233988736));
#80119=CARTESIAN_POINT('Ctrl Pts',(0.241730258758975,-7.82838526013267,
-46.629038330965));
#80120=CARTESIAN_POINT('Ctrl Pts',(5.21671445432797,-6.45573553661324,-46.4173532630562));
#80121=CARTESIAN_POINT('Ctrl Pts',(8.90276643323724,-0.405896199208848,
-46.1527469281705));
#80122=CARTESIAN_POINT('Ctrl Pts',(5.142863862158,7.27029981455958,-45.8352193263073));
#80123=CARTESIAN_POINT('Ctrl Pts',(-1.87798882331211,8.08493218300378,-45.5706129914216));
#80124=CARTESIAN_POINT('Ctrl Pts',(-6.03971349389217,4.99872140855163,-45.3589279235128));
#80125=CARTESIAN_POINT('Ctrl Pts',(-7.71091768105629,1.50674538319905,-45.2001641225813));
#80126=CARTESIAN_POINT('Ctrl Pts',(-7.47954565819725,-2.34982554683893,
-45.0414003216498));
#80127=CARTESIAN_POINT('Ctrl Pts',(-4.78196598600291,-6.78978515582278,
-44.8297152537411));
#80128=CARTESIAN_POINT('Ctrl Pts',(0.65334035126103,-8.28105800946939,-44.6180301858325));
#80129=CARTESIAN_POINT('Ctrl Pts',(5.22580291212903,-5.83378378264447,-44.4063451179237));
#80130=CARTESIAN_POINT('Ctrl Pts',(8.14824884455549,-1.58008600521795,-44.1946600500151));
#80131=CARTESIAN_POINT('Ctrl Pts',(7.07280463966759,5.42212471439058,-43.9300537151291));
#80132=CARTESIAN_POINT('Ctrl Pts',(-0.746727752358712,8.87404675230713,
-43.6125261132662));
#80133=CARTESIAN_POINT('Ctrl Pts',(-6.64288785802943,4.97644565226029,-43.3479197783803));
#80134=CARTESIAN_POINT('Ctrl Pts',(-7.83971812631999,-0.0646104361960217,
-43.1362347104716));
#80135=CARTESIAN_POINT('Ctrl Pts',(-6.86978933990756,-3.81241754784422,
-42.9774709095401));
#80136=CARTESIAN_POINT('Ctrl Pts',(-4.20944367644864,-6.61406586665424,
-42.8187071086085));
#80137=CARTESIAN_POINT('Ctrl Pts',(0.713434822181756,-8.27401909038279,
-42.6070220406999));
#80138=CARTESIAN_POINT('Ctrl Pts',(5.83220791973128,-5.91507617464108,-42.3953369727912));
#80139=CARTESIAN_POINT('Ctrl Pts',(7.7547149382516,-1.09838314149463,-42.1836519048825));
#80140=CARTESIAN_POINT('Ctrl Pts',(7.25161365384919,4.03791164242033,-41.9719668369739));
#80141=CARTESIAN_POINT('Ctrl Pts',(1.91993309088656,8.7027500720075,-41.7073605020879));
#80142=CARTESIAN_POINT('Ctrl Pts',(-6.28549546331617,6.30863336063426,-41.389832900225));
#80143=CARTESIAN_POINT('Ctrl Pts',(-8.28685849294037,-0.470049723154454,
-41.125226565339));
#80144=CARTESIAN_POINT('Ctrl Pts',(-5.9565055390961,-5.0975873284656,-40.9135414974304));
#80145=CARTESIAN_POINT('Ctrl Pts',(-2.80113087785069,-7.34044950523941,
-40.7547776964988));
#80146=CARTESIAN_POINT('Ctrl Pts',(1.03831811199606,-7.77091879071807,-40.5960138955673));
#80147=CARTESIAN_POINT('Ctrl Pts',(5.87365324500275,-5.87099469519337,-40.3843288276587));
#80148=CARTESIAN_POINT('Ctrl Pts',(8.27101668858417,-0.770102790506085,
-40.1726437597499));
#80149=CARTESIAN_POINT('Ctrl Pts',(6.64034551804669,4.15305438202045,-39.9609586918413));
#80150=CARTESIAN_POINT('Ctrl Pts',(2.94806154983591,7.75883780698274,-39.7492736239326));
#80151=CARTESIAN_POINT('Ctrl Pts',(-4.13495183477746,7.8946928511107,-39.4846672890467));
#80152=CARTESIAN_POINT('Ctrl Pts',(-8.87124308458381,0.779329347900915,
-39.1671396871837));
#80153=CARTESIAN_POINT('Ctrl Pts',(-6.03753865411047,-5.69570868499937,
-38.9025333522978));
#80154=CARTESIAN_POINT('Ctrl Pts',(-1.27483726544981,-7.73564119871364,
-38.6908482843891));
#80155=CARTESIAN_POINT('Ctrl Pts',(2.58354090478207,-7.41982813326131,-38.5320844834576));
#80156=CARTESIAN_POINT('Ctrl Pts',(5.7982624702782,-5.27687745540841,-38.3733206825261));
#80157=CARTESIAN_POINT('Ctrl Pts',(8.27434123245942,-0.709688891234698,
-38.1616356146175));
#80158=CARTESIAN_POINT('Ctrl Pts',(6.82397770110707,4.73667644087881,-37.9499505467087));
#80159=CARTESIAN_POINT('Ctrl Pts',(2.40624212751001,7.45332463554742,-37.7382654788));
#80160=CARTESIAN_POINT('Ctrl Pts',(-2.74053410931411,7.83454553961946,-37.5265804108914));
#80161=CARTESIAN_POINT('Ctrl Pts',(-8.2471743387975,3.37759045989717,-37.2619740760054));
#80162=CARTESIAN_POINT('Ctrl Pts',(-7.28914758159962,-5.11611528720145,
-36.9444464741425));
#80163=CARTESIAN_POINT('Ctrl Pts',(-0.951692555430078,-8.24543823603053,
-36.6798401392565));
#80164=CARTESIAN_POINT('Ctrl Pts',(4.00576868589115,-6.73937475169243,-36.4681550713479));
#80165=CARTESIAN_POINT('Ctrl Pts',(6.75442640137216,-4.01326016129843,-36.3093912704164));
#80166=CARTESIAN_POINT('Ctrl Pts',(7.83409611048614,-0.303679905986814,
-36.1506274694848));
#80167=CARTESIAN_POINT('Ctrl Pts',(6.78761954298498,4.78503940351681,-35.9389424015762));
#80168=CARTESIAN_POINT('Ctrl Pts',(2.17093158808615,8.0180940011098,-35.7272573336675));
#80169=CARTESIAN_POINT('Ctrl Pts',(-2.95834992293678,7.25191112966243,-35.5155722657588));
#80170=CARTESIAN_POINT('Ctrl Pts',(-7.14158571907033,4.22946621145696,-35.3038871978501));
#80171=CARTESIAN_POINT('Ctrl Pts',(-8.48475058019903,-2.72635461397087,
-35.0392808629642));
#80172=CARTESIAN_POINT('Ctrl Pts',(-2.28250116281199,-8.60793218723506,
-34.7217532611012));
#80173=CARTESIAN_POINT('Ctrl Pts',(4.58127298702289,-6.92133717157529,-34.4571469262153));
#80174=CARTESIAN_POINT('Ctrl Pts',(7.40440439747531,-2.57684891432614,-34.2454618583067));
#80175=CARTESIAN_POINT('Ctrl Pts',(7.7519810167304,1.27879765798563,-34.0866980573751));
#80176=CARTESIAN_POINT('Ctrl Pts',(6.18935383844591,4.81219102033048,-33.9279342564436));
#80177=CARTESIAN_POINT('Ctrl Pts',(2.11197233624808,8.03168438152565,-33.7162491885349));
#80178=CARTESIAN_POINT('Ctrl Pts',(-3.50205076232064,7.53249067897944,-33.5045641206263));
#80179=CARTESIAN_POINT('Ctrl Pts',(-6.93306478617521,3.64344095186944,-33.2928790527176));
#80180=CARTESIAN_POINT('Ctrl Pts',(-8.18741319037323,-1.36267981080949,
-33.0811939848088));
#80181=CARTESIAN_POINT('Ctrl Pts',(-4.73606367566928,-7.54941737813681,
-32.8165876499231));
#80182=CARTESIAN_POINT('Ctrl Pts',(3.7964985537964,-8.0556133738715,-32.4990600480599));
#80183=CARTESIAN_POINT('Ctrl Pts',(7.96188773294944,-2.34548804136043,-32.2344537131741));
#80184=CARTESIAN_POINT('Ctrl Pts',(7.32433981159772,2.7963192115458,-32.0227686452654));
#80185=CARTESIAN_POINT('Ctrl Pts',(5.10753862311752,5.97005714773156,-31.8640048443339));
#80186=CARTESIAN_POINT('Ctrl Pts',(1.63676025479456,7.66722239288512,-31.7052410434024));
#80187=CARTESIAN_POINT('Ctrl Pts',(-3.5559111666103,7.50492351251473,-31.4935559754937));
#80188=CARTESIAN_POINT('Ctrl Pts',(-7.52971711232564,3.50801020225614,-31.281870907585));
#80189=CARTESIAN_POINT('Ctrl Pts',(-7.65052177432877,-1.67677245909613,
-31.0701858396763));
#80190=CARTESIAN_POINT('Ctrl Pts',(-5.38667108337155,-6.31461840939378,
-30.8585007717676));
#80191=CARTESIAN_POINT('Ctrl Pts',(1.23769701372374,-8.8256505704411,-30.5938944368818));
#80192=CARTESIAN_POINT('Ctrl Pts',(8.09184627904301,-3.71864651380223,-30.2763668350187));
#80193=CARTESIAN_POINT('Ctrl Pts',(7.60188814473553,3.33230656740715,-30.0117605001329));
#80194=CARTESIAN_POINT('Ctrl Pts',(3.803190472164,6.85573460987635,-29.8000754322242));
#80195=CARTESIAN_POINT('Ctrl Pts',(0.0634979399251427,7.85649420196077,
-29.6413116312926));
#80196=CARTESIAN_POINT('Ctrl Pts',(-3.68480785801259,6.92007762985091,-29.4825478303612));
#80197=CARTESIAN_POINT('Ctrl Pts',(-7.55317424289503,3.45223695739262,-29.2708627624524));
#80198=CARTESIAN_POINT('Ctrl Pts',(-8.01980937097215,-2.16458610917884,
-29.0591776945438));
#80199=CARTESIAN_POINT('Ctrl Pts',(-4.77364882810306,-6.20921300689647,
-28.8474926266351));
#80200=CARTESIAN_POINT('Ctrl Pts',(-0.0551900682622783,-8.299854521198,
-28.6358075587264));
#80201=CARTESIAN_POINT('Ctrl Pts',(6.62996907301482,-5.95546068580551,-28.3712012238405));
#80202=CARTESIAN_POINT('Ctrl Pts',(8.58552319501832,2.36539628098087,-28.0536736219775));
#80203=CARTESIAN_POINT('Ctrl Pts',(3.67040743112835,7.44453354574839,-27.7890672870916));
#80204=CARTESIAN_POINT('Ctrl Pts',(-1.50475482230041,7.69422301037469,-27.577382219183));
#80205=CARTESIAN_POINT('Ctrl Pts',(-5.010375028303,6.0518323844581,-27.4186184182514));
#80206=CARTESIAN_POINT('Ctrl Pts',(-7.27519794438339,2.92177655266003,-27.2598546173199));
#80207=CARTESIAN_POINT('Ctrl Pts',(-8.00184271587865,-2.22236232506314,
-27.0481695494112));
#80208=CARTESIAN_POINT('Ctrl Pts',(-4.74207484075496,-6.82022738443972,
-26.8364844815025));
#80209=CARTESIAN_POINT('Ctrl Pts',(0.345955971607388,-7.82447210773809,
-26.6247994135939));
#80210=CARTESIAN_POINT('Ctrl Pts',(5.3022200691065,-6.38569443016573,-26.4131143456851));
#80211=CARTESIAN_POINT('Ctrl Pts',(8.90738217156051,-0.287306002502551,
-26.1485080107993));
#80212=CARTESIAN_POINT('Ctrl Pts',(5.0455924784123,7.33814040749187,-25.8309804089362));
#80213=CARTESIAN_POINT('Ctrl Pts',(-1.98548577227016,8.05920695058564,-25.5663740740504));
#80214=CARTESIAN_POINT('Ctrl Pts',(-6.1057437206868,4.91784998001252,-25.3546890061417));
#80215=CARTESIAN_POINT('Ctrl Pts',(-7.73029862184605,1.40392889809396,-25.1959252052102));
#80216=CARTESIAN_POINT('Ctrl Pts',(-7.44759086384508,-2.44921899355802,
-25.0371614042787));
#80217=CARTESIAN_POINT('Ctrl Pts',(-4.69112540417169,-6.85286243812432,
-24.8254763363699));
#80218=CARTESIAN_POINT('Ctrl Pts',(0.763557609887108,-8.27162348920492,
-24.6137912684613));
#80219=CARTESIAN_POINT('Ctrl Pts',(5.30302546439297,-5.76367679724166,-24.4021062005526));
#80220=CARTESIAN_POINT('Ctrl Pts',(8.16856765215318,-1.47143927121796,-24.190421132644));
#80221=CARTESIAN_POINT('Ctrl Pts',(6.99997346048449,5.51582935213016,-23.925814797758));
#80222=CARTESIAN_POINT('Ctrl Pts',(-0.864833299418169,8.86331605340198,
-23.6082871958951));
#80223=CARTESIAN_POINT('Ctrl Pts',(-6.708567965379,4.88754399245119,-23.3436808610091));
#80224=CARTESIAN_POINT('Ctrl Pts',(-7.83816259545043,-0.169002768904056,
-23.1319957931005));
#80225=CARTESIAN_POINT('Ctrl Pts',(-6.81841192090368,-3.90356145214814,
-22.9732319921689));
#80226=CARTESIAN_POINT('Ctrl Pts',(-4.12099383588237,-6.66953470327981,
-22.8144681912375));
#80227=CARTESIAN_POINT('Ctrl Pts',(0.823553018099068,-8.26378494274268,
-22.6027831233287));
#80228=CARTESIAN_POINT('Ctrl Pts',(5.91045923735201,-5.83688675360274,-22.3910980554201));
#80229=CARTESIAN_POINT('Ctrl Pts',(7.768654016065,-0.995019636861024,-22.1794129875113));
#80230=CARTESIAN_POINT('Ctrl Pts',(7.19719957354974,4.1341201379714,-21.9677279196027));
#80231=CARTESIAN_POINT('Ctrl Pts',(1.80387217509234,8.72754530582543,-21.7031215847168));
#80232=CARTESIAN_POINT('Ctrl Pts',(-6.36894741537249,6.22437281326372,-21.3855939828538));
#80233=CARTESIAN_POINT('Ctrl Pts',(-8.27986425864372,-0.580360476505481,
-21.1209876479679));
#80234=CARTESIAN_POINT('Ctrl Pts',(-5.88809506230738,-5.17645548091035,
-20.9093025800592));
#80235=CARTESIAN_POINT('Ctrl Pts',(-2.70313298147792,-7.377100054782,-20.7505387791277));
#80236=CARTESIAN_POINT('Ctrl Pts',(1.14170793638774,-7.7564029254303,-20.5917749781962));
#80237=CARTESIAN_POINT('Ctrl Pts',(5.9513138741151,-5.79225727374789,-20.3800899102875));
#80238=CARTESIAN_POINT('Ctrl Pts',(8.280538421931,-0.659893032019098,-20.1684048423788));
#80239=CARTESIAN_POINT('Ctrl Pts',(6.58445233348109,4.24111268032075,-19.9567197744701));
#80240=CARTESIAN_POINT('Ctrl Pts',(2.84447913310934,7.79740786915694,-19.7450347065614));
#80241=CARTESIAN_POINT('Ctrl Pts',(-4.23971532731654,7.83892950807863,-19.4804283716756));
#80242=CARTESIAN_POINT('Ctrl Pts',(-8.88083446226933,0.661125821645083,
-19.1629007698126));
#80243=CARTESIAN_POINT('Ctrl Pts',(-5.96115607439654,-5.77560288462947,
-18.8982944349267));
#80244=CARTESIAN_POINT('Ctrl Pts',(-1.17171211131436,-7.75193172937009,
-18.686609367018));
#80245=CARTESIAN_POINT('Ctrl Pts',(2.68211839623764,-7.38476634988415,-18.5278455660865));
#80246=CARTESIAN_POINT('Ctrl Pts',(5.86801818751382,-5.19919665954668,-18.3690817651549));
#80247=CARTESIAN_POINT('Ctrl Pts',(8.28305816582356,-0.599440218123851,
-18.1573966972463));
#80248=CARTESIAN_POINT('Ctrl Pts',(6.76029639696928,4.82712833845422,-17.9457116293376));
#80249=CARTESIAN_POINT('Ctrl Pts',(2.30677613741518,7.48470661755781,-17.7340265614289));
#80250=CARTESIAN_POINT('Ctrl Pts',(-2.84462028871749,7.79735637441958,-17.5223414935202));
#80251=CARTESIAN_POINT('Ctrl Pts',(-8.29142094719077,3.26746699536407,-17.2577351586343));
#80252=CARTESIAN_POINT('Ctrl Pts',(-7.22037221174813,-5.21272800192871,
-16.9402075567713));
#80253=CARTESIAN_POINT('Ctrl Pts',(-0.841807312456317,-8.25738038804991,
-16.6756012218854));
#80254=CARTESIAN_POINT('Ctrl Pts',(4.09515877244995,-6.68543412480008,-16.4639161539767));
#80255=CARTESIAN_POINT('Ctrl Pts',(6.80727030315708,-3.92295859697418,-16.3051523530452));
#80256=CARTESIAN_POINT('Ctrl Pts',(7.83744543784448,-0.199329783135814,
-16.1463885521137));
#80257=CARTESIAN_POINT('Ctrl Pts',(6.72329743449899,4.87500284725866,-15.934703484205));
#80258=CARTESIAN_POINT('Ctrl Pts',(2.06396567875818,8.0462923789589,-15.7230184162963));
#80259=CARTESIAN_POINT('Ctrl Pts',(-3.05465810381368,7.21187306931196,-15.5113333483876));
#80260=CARTESIAN_POINT('Ctrl Pts',(-7.19727441213497,4.13398984675969,-15.299648280479));
#80261=CARTESIAN_POINT('Ctrl Pts',(-8.44769258385265,-2.83910054383924,
-15.0350419455931));
#80262=CARTESIAN_POINT('Ctrl Pts',(-2.1676707462325,-8.63756398727118,-14.7175143437301));
#80263=CARTESIAN_POINT('Ctrl Pts',(4.6730351571543,-6.85971667375965,-14.4529080088442));
#80264=CARTESIAN_POINT('Ctrl Pts',(7.43806261239201,-2.47801924583956,-14.2412229409355));
#80265=CARTESIAN_POINT('Ctrl Pts',(7.73426447080314,1.38191397325961,-14.082459140004));
#80266=CARTESIAN_POINT('Ctrl Pts',(6.12472321167347,4.89418521656284,-13.9236953390725));
#80267=CARTESIAN_POINT('Ctrl Pts',(2.00483067770523,8.05909642002457,-13.7120102711638));
#80268=CARTESIAN_POINT('Ctrl Pts',(-3.60204708749114,7.48518751603995,-13.5003252032551));
#80269=CARTESIAN_POINT('Ctrl Pts',(-6.98096812924419,3.55079333072749,-13.2886401353464));
#80270=CARTESIAN_POINT('Ctrl Pts',(-8.16854101342506,-1.4715871461377,-13.0769550674377));
#80271=CARTESIAN_POINT('Ctrl Pts',(-4.63511147736421,-7.61181604360706,
-12.8123487325518));
#80272=CARTESIAN_POINT('Ctrl Pts',(3.90343496423354,-8.00434279490049,-12.4948211306888));
#80273=CARTESIAN_POINT('Ctrl Pts',(7.99241558571472,-2.23925512826935,-12.2302147958029));
#80274=CARTESIAN_POINT('Ctrl Pts',(7.28645302042453,2.89360626031973,-12.0185297278943));
#80275=CARTESIAN_POINT('Ctrl Pts',(5.02758512861158,6.03754262166171,-11.8597659269627));
#80276=CARTESIAN_POINT('Ctrl Pts',(1.53451411220522,7.68833855869245,-11.7010021260312));
#80277=CARTESIAN_POINT('Ctrl Pts',(-3.65553561624384,7.45690555873499,-11.4893170581226));
#80278=CARTESIAN_POINT('Ctrl Pts',(-7.57576407921462,3.40742923431496,-11.2776319902138));
#80279=CARTESIAN_POINT('Ctrl Pts',(-7.62751457017181,-1.77850239833385,
-11.0659469223052));
#80280=CARTESIAN_POINT('Ctrl Pts',(-5.3021044683393,-6.38579041493706,-10.8542618543965));
#80281=CARTESIAN_POINT('Ctrl Pts',(1.35511455632098,-8.8083861421122,-10.5896555195106));
#80282=CARTESIAN_POINT('Ctrl Pts',(8.14064835301168,-3.61056124319814,-10.2721279176476));
#80283=CARTESIAN_POINT('Ctrl Pts',(7.55683923680033,3.4332420790575,-10.0075215827617));
#80284=CARTESIAN_POINT('Ctrl Pts',(3.71155845792856,6.90577212352062,-9.79583651485306));
#80285=CARTESIAN_POINT('Ctrl Pts',(-0.0411291516472582,7.85664314619816,
-9.63707271392151));
#80286=CARTESIAN_POINT('Ctrl Pts',(-3.77663274431041,6.87039507366472,-9.47830891299001));
#80287=CARTESIAN_POINT('Ctrl Pts',(-7.59847642220299,3.35134856658408,-9.26662384508131));
#80288=CARTESIAN_POINT('Ctrl Pts',(-7.99027342354806,-2.27119043405084,
-9.05493877717264));
#80289=CARTESIAN_POINT('Ctrl Pts',(-4.69054020648244,-6.27223101220251,
-8.84325370926394));
#80290=CARTESIAN_POINT('Ctrl Pts',(0.0553403200935083,-8.29985352073492,
-8.63156864135525));
#80291=CARTESIAN_POINT('Ctrl Pts',(6.70868743640794,-5.86664425117891,-8.36696230646939));
#80292=CARTESIAN_POINT('Ctrl Pts',(8.55326298583737,2.47951616114584,-8.04943470460635));
#80293=CARTESIAN_POINT('Ctrl Pts',(3.57094641545068,7.49275063793162,-7.78482836972049));
#80294=CARTESIAN_POINT('Ctrl Pts',(-1.60708196426699,7.67350261411015,-7.57314330181181));
#80295=CARTESIAN_POINT('Ctrl Pts',(-5.09052033927314,5.98457482276319,-7.41437950088028));
#80296=CARTESIAN_POINT('Ctrl Pts',(-7.31346086486846,2.82463688492333,-7.25561569994876));
#80297=CARTESIAN_POINT('Ctrl Pts',(-7.97153898121459,-2.32872227296088,
-7.04393063204009));
#80298=CARTESIAN_POINT('Ctrl Pts',(-4.65083241033187,-6.8827707546837,-6.83224556413139));
#80299=CARTESIAN_POINT('Ctrl Pts',(0.450120333107332,-7.81917137457972,
-6.6205604962227));
#80300=CARTESIAN_POINT('Ctrl Pts',(5.38678539571902,-6.31452089368896,-6.40887542831401));
#80301=CARTESIAN_POINT('Ctrl Pts',(8.91041828733191,-0.168664855442598,
-6.14426909342813));
#80302=CARTESIAN_POINT('Ctrl Pts',(4.94742631652087,7.40467966516704,-5.82674149156514));
#80303=CARTESIAN_POINT('Ctrl Pts',(-2.09263061810849,8.0320525095882,-5.56213515667924));
#80304=CARTESIAN_POINT('Ctrl Pts',(-6.1706911634019,4.83610642728852,-5.35045008877058));
#80305=CARTESIAN_POINT('Ctrl Pts',(-7.74830868277893,1.30086344146143,-5.19168628783903));
#80306=CARTESIAN_POINT('Ctrl Pts',(-7.41431532367873,-2.54817809782355,
-5.03292248690753));
#80307=CARTESIAN_POINT('Ctrl Pts',(-4.59945290622839,-6.91472444679411,
-4.82123741899884));
#80308=CARTESIAN_POINT('Ctrl Pts',(0.873639462994944,-8.26072208469958,
-4.60955235109015));
#80309=CARTESIAN_POINT('Ctrl Pts',(5.37930758248336,-5.69254769690278,-4.39786728318148));
#80310=CARTESIAN_POINT('Ctrl Pts',(8.18743786494988,-1.36253157712688,-4.18618221527277));
#80311=CARTESIAN_POINT('Ctrl Pts',(6.92590090019624,5.60855578403209,-3.92157588038692));
#80312=CARTESIAN_POINT('Ctrl Pts',(-0.98278545040757,8.85101361093665,-3.60404827852388));
#80313=CARTESIAN_POINT('Ctrl Pts',(-6.77305843181678,4.79777547357795,-3.33944194363801));
#80314=CARTESIAN_POINT('Ctrl Pts',(-7.83521699085168,-0.273364980042835,
-3.12775687572932));
#80315=CARTESIAN_POINT('Ctrl Pts',(-6.76582547640464,-3.99401343348083,
-2.96899307479781));
#80316=CARTESIAN_POINT('Ctrl Pts',(-4.03181291942652,-6.72382016067921,
-2.81022927386629));
#80317=CARTESIAN_POINT('Ctrl Pts',(0.933524562352959,-8.25208670680614,
-2.59854420595759));
#80318=CARTESIAN_POINT('Ctrl Pts',(5.98766356057595,-5.75765954361041,-2.38685913804893));
#80319=CARTESIAN_POINT('Ctrl Pts',(7.78121405787801,-0.891482814498843,
-2.17517407014022));
#80320=CARTESIAN_POINT('Ctrl Pts',(7.14151231839871,4.2296028322805,-1.96348900223155));
#80321=CARTESIAN_POINT('Ctrl Pts',(1.68748462236888,8.75077718769076,-1.69888266734567));
#80322=CARTESIAN_POINT('Ctrl Pts',(-6.45125802233304,6.13903598732601,-1.38135506548265));
#80323=CARTESIAN_POINT('Ctrl Pts',(-8.27142181248957,-0.690614954054182,
-1.11674873059677));
#80324=CARTESIAN_POINT('Ctrl Pts',(-5.81861252887425,-5.2543410602677,-0.905063662688093));
#80325=CARTESIAN_POINT('Ctrl Pts',(-2.60471651056193,-7.41258324978489,
-0.746299861756561));
#80326=CARTESIAN_POINT('Ctrl Pts',(1.24500861472902,-7.740248929974,-0.587536060825044));
#80327=CARTESIAN_POINT('Ctrl Pts',(6.02766054384712,-5.71309187500411,-0.375850992916369));
#80328=CARTESIAN_POINT('Ctrl Pts',(8.28908744005743,-0.548417296970164,
-0.164165925007672));
#80329=CARTESIAN_POINT('Ctrl Pts',(6.52681211271625,4.32707578852068,0.0475191429010087));
#80330=CARTESIAN_POINT('Ctrl Pts',(2.74174315069786,7.83773263990448,0.259204210809702));
#80331=CARTESIAN_POINT('Ctrl Pts',(-4.34655550419588,7.77513718308878,0.523810545695566));
#80332=CARTESIAN_POINT('Ctrl Pts',(-8.88411837919809,0.554292796363548,
0.841338147558601));
#80333=CARTESIAN_POINT('Ctrl Pts',(-5.29130331250487,-7.15799616755843,
1.15886574942163));
#80334=CARTESIAN_POINT('Ctrl Pts',(3.1560060963405,-8.32976161044042,1.47639335128466));
#80335=CARTESIAN_POINT('Ctrl Pts',(7.76422719570322,-2.94346470889751,1.74099968617053));
#80336=CARTESIAN_POINT('Ctrl Pts',(7.51173105023254,2.21286191690165,1.95268475407922));
#80337=CARTESIAN_POINT('Ctrl Pts',(4.91298462537403,6.698680033512,2.1643698219879));
#80338=CARTESIAN_POINT('Ctrl Pts',(-0.495822942463844,8.29013088037915,
2.37605488989661));
#80339=CARTESIAN_POINT('Ctrl Pts',(-5.12469586560105,5.93287385958993,2.58773995780528));
#80340=CARTESIAN_POINT('Ctrl Pts',(-7.35058989770351,2.77484534544985,2.74650375873681));
#80341=CARTESIAN_POINT('Ctrl Pts',(-7.76599029997037,-1.07412587695898,
2.90526755966833));
#80342=CARTESIAN_POINT('Ctrl Pts',(-5.85018163290799,-5.8880168713139,3.116952627577));
#80343=CARTESIAN_POINT('Ctrl Pts',(0.5493877149772,-8.88845689999296,3.38155896246287));
#80344=CARTESIAN_POINT('Ctrl Pts',(7.78496039936211,-4.33798309352451,3.6990865643259));
#80345=CARTESIAN_POINT('Ctrl Pts',(7.83258008256155,2.7461659751253,3.96369289921177));
#80346=CARTESIAN_POINT('Ctrl Pts',(4.32360152919418,6.53058218230311,4.17537796712045));
#80347=CARTESIAN_POINT('Ctrl Pts',(-0.555674784775465,8.28818338771179,
4.38706303502915));
#80348=CARTESIAN_POINT('Ctrl Pts',(-5.7169371761748,6.02370587336679,4.59874810293782));
#80349=CARTESIAN_POINT('Ctrl Pts',(-7.74142671390708,1.23918739648874,4.81043317084652));
#80350=CARTESIAN_POINT('Ctrl Pts',(-7.41052017936217,-2.61012037179468,
4.96919697177804));
#80351=CARTESIAN_POINT('Ctrl Pts',(-5.25011376394542,-5.82251313194528,
5.12796077270955));
#80352=CARTESIAN_POINT('Ctrl Pts',(-0.684469425562928,-8.27190858394483,
5.33964584061826));
#80353=CARTESIAN_POINT('Ctrl Pts',(6.14376360232249,-6.44674165616213,5.60425217550411));
#80354=CARTESIAN_POINT('Ctrl Pts',(8.74954614262611,1.69394319857397,5.92177977736714));
#80355=CARTESIAN_POINT('Ctrl Pts',(4.22432866422699,7.14462584238486,6.18638611225301));
#80356=CARTESIAN_POINT('Ctrl Pts',(-0.897216819650257,7.78055597801422,
6.3980711801617));
#80357=CARTESIAN_POINT('Ctrl Pts',(-5.76207558030114,5.98341543592307,6.60975624807037));
#80358=CARTESIAN_POINT('Ctrl Pts',(-8.25277139000861,0.92744034630844,6.82144131597908));
#80359=CARTESIAN_POINT('Ctrl Pts',(-6.72084614008006,-4.03676980995147,
7.03312638388776));
#80360=CARTESIAN_POINT('Ctrl Pts',(-3.9890233266215,-6.76876842835001,7.19189018481927));
#80361=CARTESIAN_POINT('Ctrl Pts',(-0.267587861335669,-7.83541648839507,
7.3506539857508));
#80362=CARTESIAN_POINT('Ctrl Pts',(4.80276830414162,-6.76951896646725,7.56233905365949));
#80363=CARTESIAN_POINT('Ctrl Pts',(8.85173578479164,-0.976259031907224,
7.82694538854534));
#80364=CARTESIAN_POINT('Ctrl Pts',(5.60344757332302,6.93003442860875,8.14447299040839));
#80365=CARTESIAN_POINT('Ctrl Pts',(-1.3685681241356,8.18643098706431,8.40907932529423));
#80366=CARTESIAN_POINT('Ctrl Pts',(-5.69651250430969,5.37510879774223,8.62076439320295));
#80367=CARTESIAN_POINT('Ctrl Pts',(-8.26136401205398,0.867548287337313,
8.83244946111161));
#80368=CARTESIAN_POINT('Ctrl Pts',(-6.91133121739989,-4.6045501362241,9.04413452902033));
#80369=CARTESIAN_POINT('Ctrl Pts',(-2.54271055807657,-7.4161921746593,9.25581959692898));
#80370=CARTESIAN_POINT('Ctrl Pts',(1.30657620274551,-7.74734740154486,9.41458339786053));
#80371=CARTESIAN_POINT('Ctrl Pts',(4.84065499080121,-6.16712364629238,9.57334719879202));
#80372=CARTESIAN_POINT('Ctrl Pts',(8.03359330030085,-2.08670772021527,9.78503226670073));
#80373=CARTESIAN_POINT('Ctrl Pts',(7.40102973205109,4.95288471535275,10.0496386015866));
#80374=CARTESIAN_POINT('Ctrl Pts',(-0.175234789971888,8.91029150239721,
10.3671662034496));
#80375=CARTESIAN_POINT('Ctrl Pts',(-6.31849105303928,5.38212800194741,10.6317725383355));
#80376=CARTESIAN_POINT('Ctrl Pts',(-7.81950113939896,0.444354846942566,
10.8434576062442));
#80377=CARTESIAN_POINT('Ctrl Pts',(-6.87933965324438,-4.65590606714548,
11.0551426741529));
#80378=CARTESIAN_POINT('Ctrl Pts',(-2.32284392985198,-7.97325386721565,
11.2668277420615));
#80379=CARTESIAN_POINT('Ctrl Pts',(2.83002860187081,-7.31137616774212,11.4785128099703));
#80380=CARTESIAN_POINT('Ctrl Pts',(5.98832662459847,-5.08610630747561,11.6372766109017));
#80381=CARTESIAN_POINT('Ctrl Pts',(7.67468548908019,-1.60142357055152,11.7960404118333));
#80382=CARTESIAN_POINT('Ctrl Pts',(7.49011561048965,3.57647012650109,12.007725479742));
#80383=CARTESIAN_POINT('Ctrl Pts',(2.47320885046191,8.55508889961241,12.2723318146278));
#80384=CARTESIAN_POINT('Ctrl Pts',(-5.87158921942888,6.70435991930579,12.5898594164909));
#80385=CARTESIAN_POINT('Ctrl Pts',(-8.29989206902337,0.049220516537637,
12.8544657513767));
#80386=CARTESIAN_POINT('Ctrl Pts',(-6.26877079868885,-4.69516367899656,
13.0661508192854));
#80387=CARTESIAN_POINT('Ctrl Pts',(-2.26529829299243,-7.99194588411035,
13.2778358871941));
#80388=CARTESIAN_POINT('Ctrl Pts',(3.35695029285333,-7.59600328362433,13.4895209551028));
#80389=CARTESIAN_POINT('Ctrl Pts',(6.87317785685779,-3.77156592168745,13.7012060230115));
#80390=CARTESIAN_POINT('Ctrl Pts',(7.85667133654639,-0.035336147331286,
13.859969823943));
#80391=CARTESIAN_POINT('Ctrl Pts',(6.90303357718645,3.71664932982005,14.0187336248745));
#80392=CARTESIAN_POINT('Ctrl Pts',(3.42766920914769,7.55936863877645,14.2304186927832));
#80393=CARTESIAN_POINT('Ctrl Pts',(-3.6165626623917,8.13798393997374,14.4950250276691));
#80394=CARTESIAN_POINT('Ctrl Pts',(-8.8093829237094,1.348619439562,14.8125526295321));
#80395=CARTESIAN_POINT('Ctrl Pts',(-6.38187924163906,-5.3068115061515,15.077158964418));
#80396=CARTESIAN_POINT('Ctrl Pts',(-1.77287786670344,-7.6288238522603,15.2888440323267));
#80397=CARTESIAN_POINT('Ctrl Pts',(3.41301419869038,-7.57324959646258,15.5005291002354));
#80398=CARTESIAN_POINT('Ctrl Pts',(7.45959889311056,-3.6500363706987,15.712214168144));
#80399=CARTESIAN_POINT('Ctrl Pts',(7.68720501482482,1.54018259102167,15.9238992360527));
#80400=CARTESIAN_POINT('Ctrl Pts',(6.03383395627602,5.03203546508849,16.0826630369842));
#80401=CARTESIAN_POINT('Ctrl Pts',(2.88823290284334,7.28858460248274,16.2414268379158));
#80402=CARTESIAN_POINT('Ctrl Pts',(-2.24514762273551,7.99076232761187,16.4531119058244));
#80403=CARTESIAN_POINT('Ctrl Pts',(-8.00721876580877,3.89753200561023,16.7177182407104));
#80404=CARTESIAN_POINT('Ctrl Pts',(-7.60839633559909,-4.64072269045992,
17.0352458425733));
#80405=CARTESIAN_POINT('Ctrl Pts',(-1.46556377916027,-8.16962384849504,
17.2998521774592));
#80406=CARTESIAN_POINT('Ctrl Pts',(3.5559396911123,-6.97834810053455,17.5115372453679));
#80407=CARTESIAN_POINT('Ctrl Pts',(7.48784140366001,-3.59652700315428,17.7232223132766));
#80408=CARTESIAN_POINT('Ctrl Pts',(8.05761599360032,2.01077240213722,17.9349073811853));
#80409=CARTESIAN_POINT('Ctrl Pts',(4.88966790155371,6.1283302102734,18.146592449094));
#80410=CARTESIAN_POINT('Ctrl Pts',(1.376210838791,7.7352813045818,18.3053562500255));
#80411=CARTESIAN_POINT('Ctrl Pts',(-2.48350293048252,7.43623345537914,18.464120050957));
#80412=CARTESIAN_POINT('Ctrl Pts',(-6.86316041045839,4.66797596443816,18.6758051188657));
#80413=CARTESIAN_POINT('Ctrl Pts',(-8.63596333560425,-2.17403895189931,
18.9404114537515));
#80414=CARTESIAN_POINT('Ctrl Pts',(-2.83287097636486,-8.44978366117008,
19.2579390556146));
#80415=CARTESIAN_POINT('Ctrl Pts',(4.13929553922285,-7.19422431229763,19.5225453905004));
#80416=CARTESIAN_POINT('Ctrl Pts',(7.21412342111526,-3.04933969311035,19.7342304584091));
#80417=CARTESIAN_POINT('Ctrl Pts',(8.04476835359511,2.06989794622304,19.9459155263178));
#80418=CARTESIAN_POINT('Ctrl Pts',(4.87004418658415,6.72689012651754,20.1576005942265));
#80419=CARTESIAN_POINT('Ctrl Pts',(-0.205108566907885,7.83729633415856,
20.3692856621352));
#80420=CARTESIAN_POINT('Ctrl Pts',(-3.92797678237034,6.80437591046944,20.5280494630667));
#80421=CARTESIAN_POINT('Ctrl Pts',(-6.68845181927522,4.09022824177934,20.6868132639982));
#80422=CARTESIAN_POINT('Ctrl Pts',(-8.25675744780296,-0.847895555128566,
20.8984983319069));
#80423=CARTESIAN_POINT('Ctrl Pts',(-5.20740273785928,-7.224213785874,21.1631046667928));
#80424=CARTESIAN_POINT('Ctrl Pts',(3.27357967802362,-8.28900946922719,21.4806322686558));
#80425=CARTESIAN_POINT('Ctrl Pts',(7.7994516984316,-2.83887023664659,21.7452386035417));
#80426=CARTESIAN_POINT('Ctrl Pts',(7.48300371173338,2.31229426095535,21.9569236714504));
#80427=CARTESIAN_POINT('Ctrl Pts',(4.82214241009197,6.76385377928702,22.1686087393591));
#80428=CARTESIAN_POINT('Ctrl Pts',(-0.605547459853415,8.28261392480565,
22.3802938072677));
#80429=CARTESIAN_POINT('Ctrl Pts',(-5.20352195274805,5.86418303269119,22.5919788751764));
#80430=CARTESIAN_POINT('Ctrl Pts',(-7.38674196740523,2.67667260620213,22.750742676108));
#80431=CARTESIAN_POINT('Ctrl Pts',(-7.75106567552916,-1.17742757834563,
22.9095064770395));
#80432=CARTESIAN_POINT('Ctrl Pts',(-5.77120593411264,-5.96541301925682,
23.1211915449482));
#80433=CARTESIAN_POINT('Ctrl Pts',(0.667673809145736,-8.88034457568269,
23.385797879834));
#80434=CARTESIAN_POINT('Ctrl Pts',(7.84205347588213,-4.23393424260604,23.7033254816971));
#80435=CARTESIAN_POINT('Ctrl Pts',(7.79530841005407,2.85022767666477,23.9679318165829));
#80436=CARTESIAN_POINT('Ctrl Pts',(4.23625656757878,6.5875776726129,24.1796168844917));
#80437=CARTESIAN_POINT('Ctrl Pts',(-0.665998399415621,8.2800496075059,24.3913019524002));
#80438=CARTESIAN_POINT('Ctrl Pts',(-5.79664382272207,5.9470414111572,24.6029870203091));
#80439=CARTESIAN_POINT('Ctrl Pts',(-7.75724264040923,1.13598854371463,24.8146720882177));
#80440=CARTESIAN_POINT('Ctrl Pts',(-7.37510492967002,-2.70857165498245,
24.9734358891492));
#80441=CARTESIAN_POINT('Ctrl Pts',(-5.17211256384402,-5.89191025352067,
25.1321996900807));
#80442=CARTESIAN_POINT('Ctrl Pts',(-0.57425526905304,-8.28028992911609,
25.3438847579894));
#80443=CARTESIAN_POINT('Ctrl Pts',(6.22906718140751,-6.36435622414303,25.6084910928752));
#80444=CARTESIAN_POINT('Ctrl Pts',(8.72621287182006,1.81030682620079,25.9260186947383));
#80445=CARTESIAN_POINT('Ctrl Pts',(4.12881225314493,7.20024585656392,26.1906250296241));
#80446=CARTESIAN_POINT('Ctrl Pts',(-1.00074748188264,7.76791823956505,26.4023100975329));
#80447=CARTESIAN_POINT('Ctrl Pts',(-5.84124316681254,5.90615387853627,26.6139951654415));
#80448=CARTESIAN_POINT('Ctrl Pts',(-8.26438993242782,0.817459600412216,
26.8256802333502));
#80449=CARTESIAN_POINT('Ctrl Pts',(-6.6664943293382,-4.12591040990177,27.0373653012589));
#80450=CARTESIAN_POINT('Ctrl Pts',(-3.89853292411994,-6.82128830745126,
27.1961291021904));
#80451=CARTESIAN_POINT('Ctrl Pts',(-0.163223356220313,-7.83828507676261,
27.354892903122));
#80452=CARTESIAN_POINT('Ctrl Pts',(4.89248913876279,-6.70496237508786,27.5665779710306));
#80453=CARTESIAN_POINT('Ctrl Pts',(8.86395131759078,-0.8582978140814,27.8311843059165));
#80454=CARTESIAN_POINT('Ctrl Pts',(5.51066651380619,7.00403858234108,28.1487119077796));
#80455=CARTESIAN_POINT('Ctrl Pts',(-1.47746185782562,8.167480485153,28.4133182426654));
#80456=CARTESIAN_POINT('Ctrl Pts',(-5.76758534699895,5.29877425110231,28.6250033105741));
#80457=CARTESIAN_POINT('Ctrl Pts',(-8.27218423992927,0.757458428859326,
28.8366883784828));
#80458=CARTESIAN_POINT('Ctrl Pts',(-6.84940163528804,-4.69617699751986,
29.0483734463915));
#80459=CARTESIAN_POINT('Ctrl Pts',(-2.44372694399771,-7.44939473895791,
29.2600585143002));
#80460=CARTESIAN_POINT('Ctrl Pts',(1.40962835111201,-7.72926135187306,29.4188223152317));
#80461=CARTESIAN_POINT('Ctrl Pts',(4.92235063350798,-6.10211594853941,29.5775861161632));
#80462=CARTESIAN_POINT('Ctrl Pts',(8.06066873181136,-1.97954288164058,29.7892711840719));
#80463=CARTESIAN_POINT('Ctrl Pts',(7.33441811107692,5.05100178877253,30.0538775189577));
#80464=CARTESIAN_POINT('Ctrl Pts',(-0.293873666226079,8.90716790891514,
30.3714051208208));
#80465=CARTESIAN_POINT('Ctrl Pts',(-6.38960221699068,5.29751021946285,30.6360114557066));
#80466=CARTESIAN_POINT('Ctrl Pts',(-7.82472506690299,0.340186605324074,
30.8476965236154));
#80467=CARTESIAN_POINT('Ctrl Pts',(-6.81672902357357,-4.74710235722308,
31.059381591524));
#80468=CARTESIAN_POINT('Ctrl Pts',(-2.21646166681117,-8.00347917052808,
31.2710666594327));
#80469=CARTESIAN_POINT('Ctrl Pts',(2.92714003054094,-7.27304163299227,31.4827517273414));
#80470=CARTESIAN_POINT('Ctrl Pts',(6.05552507391138,-5.00591142680821,31.6415155282729));
#80471=CARTESIAN_POINT('Ctrl Pts',(7.69533043013239,-1.49908117848691,31.8002793292044));
#80472=CARTESIAN_POINT('Ctrl Pts',(7.44182519513283,3.67589556289904,32.0119643971131));
#80473=CARTESIAN_POINT('Ctrl Pts',(2.35906521467522,8.5872649552221,32.276570731999));
#80474=CARTESIAN_POINT('Ctrl Pts',(-5.96034758795615,6.62557608967355,32.594098333862));
#80475=CARTESIAN_POINT('Ctrl Pts',(-8.29981157134884,-0.0613098425100343,
32.8587046687479));
#80476=CARTESIAN_POINT('Ctrl Pts',(-6.20569153145733,-4.77822581252294,
33.0703897366566));
#80477=CARTESIAN_POINT('Ctrl Pts',(-2.15867221915416,-8.02140322020008,
33.2820748045652));
#80478=CARTESIAN_POINT('Ctrl Pts',(3.45780525326754,-7.55062672789463,33.493759872474));
#80479=CARTESIAN_POINT('Ctrl Pts',(6.92279269365902,-3.67970442756689,33.7054449403826));
#80480=CARTESIAN_POINT('Ctrl Pts',(7.85644524693097,0.0692908059781572,
33.8642087413142));
#80481=CARTESIAN_POINT('Ctrl Pts',(6.85292851347593,3.80824442464031,34.0229725422456));
#80482=CARTESIAN_POINT('Ctrl Pts',(3.32670050871143,7.60434311098562,34.2346576101544));
#80483=CARTESIAN_POINT('Ctrl Pts',(-3.72461192004342,8.08910218400948,34.4992639450402));
#80484=CARTESIAN_POINT('Ctrl Pts',(-8.82656077105497,1.23118919918194,34.8167915469033));
#80485=CARTESIAN_POINT('Ctrl Pts',(-6.31064490135422,-5.39132562044787,
35.0813978817891));
#80486=CARTESIAN_POINT('Ctrl Pts',(-1.67113099105788,-7.65175604092209,
35.2930829496978));
#80487=CARTESIAN_POINT('Ctrl Pts',(3.51356118716118,-7.52712848002853,35.5047680176065));
#80488=CARTESIAN_POINT('Ctrl Pts',(7.50754337705162,-3.55037654273579,35.7164530855152));
#80489=CARTESIAN_POINT('Ctrl Pts',(7.66601346490072,1.64241313608831,35.9281381534239));
#80490=CARTESIAN_POINT('Ctrl Pts',(5.9662895480264,5.11193917832848,36.0869019543554));
#80491=CARTESIAN_POINT('Ctrl Pts',(2.79091794518469,7.32639965002328,36.2456657552869));
#80492=CARTESIAN_POINT('Ctrl Pts',(-2.35135799763592,7.96015615369499,36.4573508231956));
#80493=CARTESIAN_POINT('Ctrl Pts',(-8.0584104826783,3.79055782055054,36.7219571580814));
#80494=CARTESIAN_POINT('Ctrl Pts',(-7.5459232513068,-4.74162885248265,37.0394847599445));
#80495=CARTESIAN_POINT('Ctrl Pts',(-1.35664255828353,-8.18841571891282,
37.3040910948304));
#80496=CARTESIAN_POINT('Ctrl Pts',(3.6485519661657,-6.93037645797473,37.515776162739));
#80497=CARTESIAN_POINT('Ctrl Pts',(7.53507082275758,-3.4964958267972,37.7274612306477));
#80498=CARTESIAN_POINT('Ctrl Pts',(8.03012496305131,2.11789381964731,37.9391462985564));
#80499=CARTESIAN_POINT('Ctrl Pts',(4.80762607306203,6.19290036212831,38.1508313664651));
#80500=CARTESIAN_POINT('Ctrl Pts',(1.27308148848372,7.75292181422578,38.3095951673966));
#80501=CARTESIAN_POINT('Ctrl Pts',(-2.58230775465909,7.4025023788475,38.4683589683282));
#80502=CARTESIAN_POINT('Ctrl Pts',(-6.92471323188677,4.57616838418209,38.6800440362368));
#80503=CARTESIAN_POINT('Ctrl Pts',(-8.60624687491617,-2.28884748864364,
38.9446503711227));
#80504=CARTESIAN_POINT('Ctrl Pts',(-2.72009775291531,-8.48675851570514,
39.2621779729857));
#80505=CARTESIAN_POINT('Ctrl Pts',(4.23473081663686,-7.13846523612135,39.5267843078716));
#80506=CARTESIAN_POINT('Ctrl Pts',(7.25409045900377,-2.95300201687236,39.7384693757802));
#80507=CARTESIAN_POINT('Ctrl Pts',(8.01649111349595,2.17684303476906,39.950154443689));
#80508=CARTESIAN_POINT('Ctrl Pts',(4.78003334023127,6.79114588414926,40.1618395115976));
#80509=CARTESIAN_POINT('Ctrl Pts',(-0.309456191810431,7.8338700665115,40.3735245795064));
#80510=CARTESIAN_POINT('Ctrl Pts',(-4.01823935838767,6.75146544037091,40.5322883804379));
#80511=CARTESIAN_POINT('Ctrl Pts',(-6.74232652089295,4.00079840710311,40.6910521813694));
#80512=CARTESIAN_POINT('Ctrl Pts',(-8.24473427658207,-0.957771962842544,
40.9027372492781));
#80513=CARTESIAN_POINT('Ctrl Pts',(-5.11073933877439,-7.29291790090763,
41.167343584164));
#80514=CARTESIAN_POINT('Ctrl Pts',(3.38367048796323,-8.24468167476436,41.4848711860269));
#80515=CARTESIAN_POINT('Ctrl Pts',(7.83656410693827,-2.7347566645924,41.7494775209129));
#80516=CARTESIAN_POINT('Ctrl Pts',(7.45154839830587,2.41173708491767,41.9611625888215));
#80517=CARTESIAN_POINT('Ctrl Pts',(4.73164358252729,6.82746837258959,42.1728476567303));
#80518=CARTESIAN_POINT('Ctrl Pts',(-0.715789675678205,8.27381570339301,
42.3845327246388));
#80519=CARTESIAN_POINT('Ctrl Pts',(-5.28115129402745,5.79437005749779,42.5962177925476));
#80520=CARTESIAN_POINT('Ctrl Pts',(-7.42173105642654,2.57806928919524,42.7549815934791));
#80521=CARTESIAN_POINT('Ctrl Pts',(-7.73469911131649,-1.28054069283851,
42.9137453944107));
#80522=CARTESIAN_POINT('Ctrl Pts',(-5.69125543650362,-6.04173666926352,
43.1254304623193));
#80523=CARTESIAN_POINT('Ctrl Pts',(0.785870231192877,-8.87066604477925,
43.3900367972052));
#80524=CARTESIAN_POINT('Ctrl Pts',(7.89773955776408,-4.12912966217305,43.7075643990682));
#80525=CARTESIAN_POINT('Ctrl Pts',(7.7566619832233,2.95378162610321,43.9721707339541));
#80526=CARTESIAN_POINT('Ctrl Pts',(4.14815708110641,6.64340591334962,44.1838558018628));
#80527=CARTESIAN_POINT('Ctrl Pts',(-0.776201107218263,8.27044661502238,
44.3955408697715));
#80528=CARTESIAN_POINT('Ctrl Pts',(-5.87532396071409,5.86932274714715,44.6072259376801));
#80529=CARTESIAN_POINT('Ctrl Pts',(-7.77168226861542,1.03258804434432,44.8189110055888));
#80530=CARTESIAN_POINT('Ctrl Pts',(-7.33838213262225,-2.80654250091254,
44.9776748065203));
#80531=CARTESIAN_POINT('Ctrl Pts',(-5.09319399126717,-5.96026255931195,
45.1364386074519));
#80532=CARTESIAN_POINT('Ctrl Pts',(-0.463939388580697,-8.28720282531922,
45.3481236753605));
#80533=CARTESIAN_POINT('Ctrl Pts',(6.31326617366714,-6.28084216635835,45.6127300102465));
#80534=CARTESIAN_POINT('Ctrl Pts',(8.70133206874304,1.92634942800435,45.9302576121094));
#80535=CARTESIAN_POINT('Ctrl Pts',(4.03256366223554,7.25458898399512,46.1948639469953));
#80536=CARTESIAN_POINT('Ctrl Pts',(-1.10410068062192,7.75390295181156,46.4065490149041));
#80537=CARTESIAN_POINT('Ctrl Pts',(-5.91937486901007,5.82784493023922,46.6182340828126));
#80538=CARTESIAN_POINT('Ctrl Pts',(-8.2745428830734,0.70733388841374,46.8299191507214));
#80539=CARTESIAN_POINT('Ctrl Pts',(-6.61096029045708,-4.21431932720265,
47.0416042186301));
#80540=CARTESIAN_POINT('Ctrl Pts',(-3.80735116212366,-6.87259850872246,
47.2003680195615));
#80541=CARTESIAN_POINT('Ctrl Pts',(-0.0588299049391507,-7.83976363488727,
47.3591318204932));
#80542=CARTESIAN_POINT('Ctrl Pts',(4.98134234603678,-6.63921673511537,47.5708168884017));
#80543=CARTESIAN_POINT('Ctrl Pts',(8.87459492999746,-0.740184386986363,
47.8354232232877));
#80544=CARTESIAN_POINT('Ctrl Pts',(5.41690820042068,7.07680064983623,48.1529508251507));
#80545=CARTESIAN_POINT('Ctrl Pts',(-1.58609358048459,8.14708157382943,48.4175571600365));
#80546=CARTESIAN_POINT('Ctrl Pts',(-5.83763537430491,5.22150002736057,48.6292422279453));
#80547=CARTESIAN_POINT('Ctrl Pts',(-8.28153749037398,0.647234243773531,
48.8409272958538));
#80548=CARTESIAN_POINT('Ctrl Pts',(-6.78625739001722,-4.78697104544792,
49.0526123637627));
#80549=CARTESIAN_POINT('Ctrl Pts',(-2.3443099628472,-7.48127623816482,49.2642974316713));
#80550=CARTESIAN_POINT('Ctrl Pts',(1.51243051798487,-7.70980460596024,49.4230612326029));
#80551=CARTESIAN_POINT('Ctrl Pts',(5.00317335353904,-6.03602611020303,49.5818250335343));
#80552=CARTESIAN_POINT('Ctrl Pts',(8.08631469576634,-1.87202699373947,49.7935101014431));
#80553=CARTESIAN_POINT('Ctrl Pts',(7.26650581480223,5.14822312470218,50.0581164363288));
#80554=CARTESIAN_POINT('Ctrl Pts',(-0.412460427341156,8.90246473091509,
50.375644038192));
#80555=CARTESIAN_POINT('Ctrl Pts',(-6.45958025795135,5.21195298403308,50.6402503730777));
#80556=CARTESIAN_POINT('Ctrl Pts',(-7.82856136876646,0.235958035496164,
50.8519354409865));
#80557=CARTESIAN_POINT('Ctrl Pts',(-6.75290952485123,-4.83745680290527,
51.0636205088951));
#80558=CARTESIAN_POINT('Ctrl Pts',(-2.10968633960191,-8.03228514819943,
51.2753055768039));
#80559=CARTESIAN_POINT('Ctrl Pts',(3.02373236434919,-7.23341730736144,51.4869906447125));
#80560=CARTESIAN_POINT('Ctrl Pts',(6.12164964500423,-4.924828804908,51.645754445644));
#80561=CARTESIAN_POINT('Ctrl Pts',(7.7146106921978,-1.39647294150067,51.8045182465756));
#80562=CARTESIAN_POINT('Ctrl Pts',(7.39221505707234,3.77466912120921,52.0162033144842));
#80563=CARTESIAN_POINT('Ctrl Pts',(2.24450322557626,8.61791815741794,52.2808096493702));
#80564=CARTESIAN_POINT('Ctrl Pts',(-6.04804895683927,6.54561728983433,52.5983372512331));
#80565=CARTESIAN_POINT('Ctrl Pts',(-8.29825919696842,-0.171829329049749,
52.8629435861191));
#80566=CARTESIAN_POINT('Ctrl Pts',(-6.14151175556086,-4.86044058214065,
53.0746286540277));
#80567=CARTESIAN_POINT('Ctrl Pts',(-2.05166332979347,-8.04943805234253,
53.2863137219364));
#80568=CARTESIAN_POINT('Ctrl Pts',(3.55804701210798,-7.50391115408883,53.4979987898451));
#80569=CARTESIAN_POINT('Ctrl Pts',(6.97117985135743,-3.58719038068351,53.7096838577538));
#80570=CARTESIAN_POINT('Ctrl Pts',(7.85482590827286,0.173905473015555,53.8684476586853));
#80571=CARTESIAN_POINT('Ctrl Pts',(6.8016081578469,3.89916416776701,54.0272114596168));
#80572=CARTESIAN_POINT('Ctrl Pts',(3.22514186305803,7.64796904632611,54.2388965275255));
#80573=CARTESIAN_POINT('Ctrl Pts',(-3.83200067505273,8.03878590459606,54.5035028624114));
#80574=CARTESIAN_POINT('Ctrl Pts',(-8.84217330287154,1.11354064511878,54.8210304642744));
#80575=CARTESIAN_POINT('Ctrl Pts',(-6.23829148347237,-5.4748836843946,55.0856367991602));
#80576=CARTESIAN_POINT('Ctrl Pts',(-1.56908770187694,-7.67333122518657,
55.297321867069));
#80577=CARTESIAN_POINT('Ctrl Pts',(3.61348493751562,-7.47967264937361,55.5090069349776));
#80578=CARTESIAN_POINT('Ctrl Pts',(7.55415678516325,-3.45008681937387,55.7206920028864));
#80579=CARTESIAN_POINT('Ctrl Pts',(7.64346206275794,1.74435207606906,55.932377070795));
#80580=CARTESIAN_POINT('Ctrl Pts',(5.89768786109866,5.19093705891806,56.0911408717265));
#80581=CARTESIAN_POINT('Ctrl Pts',(2.69310663716597,7.36291414668697,56.2499046726581));
#80582=CARTESIAN_POINT('Ctrl Pts',(-2.45714833322707,7.92814114052003,56.4615897405667));
#80583=CARTESIAN_POINT('Ctrl Pts',(-8.10817944768413,3.68290562380125,56.7261960754527));
#80584=CARTESIAN_POINT('Ctrl Pts',(-7.4821009522292,-4.84168401008916,57.0437236773156));
#80585=CARTESIAN_POINT('Ctrl Pts',(-1.24749925420084,-8.2057724583871,57.3083300122015));
#80586=CARTESIAN_POINT('Ctrl Pts',(3.74054184579962,-6.8811531701488,57.5200150801102));
#80587=CARTESIAN_POINT('Ctrl Pts',(7.58090054991324,-3.39590284033723,57.7317001480188));
#80588=CARTESIAN_POINT('Ctrl Pts',(8.00133886187132,2.22475810125255,57.9433852159276));
#80589=CARTESIAN_POINT('Ctrl Pts',(4.72457228532241,6.25622590654754,58.1550702838363));
#80590=CARTESIAN_POINT('Ctrl Pts',(1.17005802530752,7.76949200400492,58.3138340847677));
#80591=CARTESIAN_POINT('Ctrl Pts',(-2.68125956745956,7.36690301727387,58.4725978856994));
#80592=CARTESIAN_POINT('Ctrl Pts',(-6.98373096787359,4.4847496139812,58.6842829536079));
#80593=CARTESIAN_POINT('Ctrl Pts',(-8.57770848092659,-2.40573363485677,
58.9488892884939));
#80594=CARTESIAN_POINT('Ctrl Pts',(-2.60211601861391,-8.51788785161202,
59.2664168903568));
#80595=CARTESIAN_POINT('Ctrl Pts',(4.32147341265364,-7.08873519980074,59.5310232252428));
#80596=CARTESIAN_POINT('Ctrl Pts',(7.3034564296118,-2.84631579801383,59.7427082931514));
#80597=CARTESIAN_POINT('Ctrl Pts',(7.79380539571414,0.98044936741639,59.901472094083));
#80598=CARTESIAN_POINT('Ctrl Pts',(6.36418815772075,4.59868409180725,60.0603005433583));
#80599=CARTESIAN_POINT('Ctrl Pts',(4.38333064273928,6.25177260444803,60.1662077256567));
#80600=CARTESIAN_POINT('Ctrl Pts',(3.25252554956235,6.7931805456771,60.2191936409778));
#80601=CARTESIAN_POINT('Ctrl Pts',(4.14704588419467,-5.81932114679417,-60.2187981753814));
#80602=CARTESIAN_POINT('Ctrl Pts',(5.11514398602353,-5.1294285247336,-60.165844689447));
#80603=CARTESIAN_POINT('Ctrl Pts',(6.69695015326308,-3.2624304470734,-60.0599699365356));
#80604=CARTESIAN_POINT('Ctrl Pts',(7.44448710579558,0.351415371766862,-59.901173916647));
#80605=CARTESIAN_POINT('Ctrl Pts',(6.36363141587864,3.84858550951182,-59.7424101157154));
#80606=CARTESIAN_POINT('Ctrl Pts',(2.88618963684088,7.3289477836205,-59.5307250478067));
#80607=CARTESIAN_POINT('Ctrl Pts',(-3.81788569128896,7.53850476344882,-59.2661187129209));
#80608=CARTESIAN_POINT('Ctrl Pts',(-8.40907168959556,0.853298876947923,
-58.9485911110578));
#80609=CARTESIAN_POINT('Ctrl Pts',(-5.79824687200889,-5.32804406291944,
-58.683984776172));
#80610=CARTESIAN_POINT('Ctrl Pts',(-1.30780500871279,-7.32213393143249,
-58.4722997082633));
#80611=CARTESIAN_POINT('Ctrl Pts',(2.35757329727375,-7.07192733459881,-58.3135359073319));
#80612=CARTESIAN_POINT('Ctrl Pts',(5.4338632459131,-5.07922330288575,-58.1547721064002));
#80613=CARTESIAN_POINT('Ctrl Pts',(7.84088975156651,-0.777899090723996,
-57.9430870384916));
#80614=CARTESIAN_POINT('Ctrl Pts',(6.5335587623941,4.40742637312395,-57.7314019705828));
#80615=CARTESIAN_POINT('Ctrl Pts',(2.37695215273987,7.04041458569579,-57.5197169026742));
#80616=CARTESIAN_POINT('Ctrl Pts',(-2.50093072949188,7.46712779429702,-57.3080318347655));
#80617=CARTESIAN_POINT('Ctrl Pts',(-7.78125817105807,3.30844791921314,-57.0434254998796));
#80618=CARTESIAN_POINT('Ctrl Pts',(-6.97972648593816,-4.76146745484501,
-56.7258978980166));
#80619=CARTESIAN_POINT('Ctrl Pts',(-1.00702533288646,-7.81027475648936,
-56.4612915631308));
#80620=CARTESIAN_POINT('Ctrl Pts',(3.7150507761986,-6.44413077085018,-56.249606495222));
#80621=CARTESIAN_POINT('Ctrl Pts',(6.35709703780464,-3.89264454526949,-56.0908426942905));
#80622=CARTESIAN_POINT('Ctrl Pts',(7.42822665373128,-0.387073605132157,
-55.9320788933591));
#80623=CARTESIAN_POINT('Ctrl Pts',(6.49974656903945,4.45372245075779,-55.7203938254502));
#80624=CARTESIAN_POINT('Ctrl Pts',(2.16082594048462,7.57919118758771,-55.5087087575417));
#80625=CARTESIAN_POINT('Ctrl Pts',(-2.71490966702803,6.91713221250367,-55.2970236896329));
#80626=CARTESIAN_POINT('Ctrl Pts',(-6.72165560441165,4.10264625103405,-55.0853386217243));
#80627=CARTESIAN_POINT('Ctrl Pts',(-8.08377338813595,-2.47924397858112,
-54.8207322868384));
#80628=CARTESIAN_POINT('Ctrl Pts',(-2.27412232409216,-8.13735018118491,
-54.5032046849754));
#80629=CARTESIAN_POINT('Ctrl Pts',(4.25872376383168,-6.62402727327916,-54.2385983500895));
#80630=CARTESIAN_POINT('Ctrl Pts',(6.9918664875298,-2.53815891362137,-54.0269132821809));
#80631=CARTESIAN_POINT('Ctrl Pts',(7.37031945951809,1.11523115162059,-53.8681494812492));
#80632=CARTESIAN_POINT('Ctrl Pts',(5.93252554039144,4.48703956948173,-53.7093856803178));
#80633=CARTESIAN_POINT('Ctrl Pts',(2.10506424181126,7.5928289382194,-53.497700612409));
#80634=CARTESIAN_POINT('Ctrl Pts',(-3.22716385688535,7.19018222171262,-53.2860155445004));
#80635=CARTESIAN_POINT('Ctrl Pts',(-6.53123957473593,3.54406024958424,-53.0743304765917));
#80636=CARTESIAN_POINT('Ctrl Pts',(-7.78446579669849,-1.1893072397415,-52.862645408683));
#80637=CARTESIAN_POINT('Ctrl Pts',(-4.58839864462092,-7.10215749873455,
-52.5980390737971));
#80638=CARTESIAN_POINT('Ctrl Pts',(3.49989180946896,-7.69017930427037,-52.2805114719342));
#80639=CARTESIAN_POINT('Ctrl Pts',(7.52366382706956,-2.32571449231829,-52.0159051370482));
#80640=CARTESIAN_POINT('Ctrl Pts',(6.98379687578907,2.56027906868629,-51.8042200691396));
#80641=CARTESIAN_POINT('Ctrl Pts',(4.92085603590594,5.59915398115555,-51.6454562682081));
#80642=CARTESIAN_POINT('Ctrl Pts',(1.64963450172886,7.25307447927886,-51.4866924672765));
#80643=CARTESIAN_POINT('Ctrl Pts',(-3.27860852967551,7.1647102426091,-51.275007399368));
#80644=CARTESIAN_POINT('Ctrl Pts',(-7.09898380706795,3.4231178539073,-51.0633223314591));
#80645=CARTESIAN_POINT('Ctrl Pts',(-7.27909505938493,-1.49406444114012,
-50.8516372635505));
#80646=CARTESIAN_POINT('Ctrl Pts',(-5.19001718959643,-5.92250631241772,
-50.6399521956417));
#80647=CARTESIAN_POINT('Ctrl Pts',(1.06267466412245,-8.38837086787587,-50.3753458607559));
#80648=CARTESIAN_POINT('Ctrl Pts',(7.62960423514155,-3.63004678007801,-50.0578182588929));
#80649=CARTESIAN_POINT('Ctrl Pts',(7.2538737309012,3.06525385218751,-49.793211924007));
#80650=CARTESIAN_POINT('Ctrl Pts',(3.69463468840507,6.45585952690713,-49.5815268560984));
#80651=CARTESIAN_POINT('Ctrl Pts',(0.159500605525881,7.45251024740165,-49.4227630551668));
#80652=CARTESIAN_POINT('Ctrl Pts',(-3.4082795814312,6.61150615866358,-49.2639992542353));
#80653=CARTESIAN_POINT('Ctrl Pts',(-7.12194181390246,3.3705031598894,-49.0523141863267));
#80654=CARTESIAN_POINT('Ctrl Pts',(-7.63559463672009,-1.95217864920896,
-48.8406291184179));
#80655=CARTESIAN_POINT('Ctrl Pts',(-4.60712245387128,-5.83025523737004,
-48.6289440505092));
#80656=CARTESIAN_POINT('Ctrl Pts',(-0.157220624807248,-7.87322304549216,
-48.4172589826005));
#80657=CARTESIAN_POINT('Ctrl Pts',(6.21448746908153,-5.73360172626448,-48.1526526477148));
#80658=CARTESIAN_POINT('Ctrl Pts',(8.17481410019929,2.13553619440853,-47.8351250458516));
#80659=CARTESIAN_POINT('Ctrl Pts',(3.57610490332985,7.01611993929612,-47.5705187109658));
#80660=CARTESIAN_POINT('Ctrl Pts',(-1.33032231780475,7.31838030186149,-47.3588336430571));
#80661=CARTESIAN_POINT('Ctrl Pts',(-4.67679060281408,5.80456536600457,-47.2000698421256));
#80662=CARTESIAN_POINT('Ctrl Pts',(-6.86493277211707,2.86375303152355,-47.041306041194));
#80663=CARTESIAN_POINT('Ctrl Pts',(-7.61927996110144,-2.00721688558928,
-46.8296209732854));
#80664=CARTESIAN_POINT('Ctrl Pts',(-4.58488852524102,-6.41031232826053,
-46.6179359053767));
#80665=CARTESIAN_POINT('Ctrl Pts',(0.229345415595273,-7.4273046334583,-46.406250837468));
#80666=CARTESIAN_POINT('Ctrl Pts',(4.94944054879081,-6.12498144510814,-46.1945657695593));
#80667=CARTESIAN_POINT('Ctrl Pts',(8.44664080559815,-0.385100454424842,
-45.9299594346735));
#80668=CARTESIAN_POINT('Ctrl Pts',(4.87937362857974,6.89781221860719,-45.6124318328105));
#80669=CARTESIAN_POINT('Ctrl Pts',(-1.78177167135614,7.67070759404643,-45.3478254979245));
#80670=CARTESIAN_POINT('Ctrl Pts',(-5.73027393610722,4.74261619036305,-45.1361404300159));
#80671=CARTESIAN_POINT('Ctrl Pts',(-7.31585540537817,1.4295485715389,-44.9773766290843));
#80672=CARTESIAN_POINT('Ctrl Pts',(-7.09633753032112,-2.22943424370471,
-44.8186128281528));
#80673=CARTESIAN_POINT('Ctrl Pts',(-4.53696604659435,-6.4419163176408,-44.6069277602442));
#80674=CARTESIAN_POINT('Ctrl Pts',(0.61986701687461,-7.856785081452,-44.3952426923354));
#80675=CARTESIAN_POINT('Ctrl Pts',(4.95806336722576,-5.53489485757584,-44.1835576244268));
#80676=CARTESIAN_POINT('Ctrl Pts',(7.7307802805699,-1.4991316494842,-43.971872556518));
#80677=CARTESIAN_POINT('Ctrl Pts',(6.71043554017164,5.14432678977491,-43.7072662216322));
#80678=CARTESIAN_POINT('Ctrl Pts',(-0.708469794309639,8.41939255296942,
-43.3897386197692));
#80679=CARTESIAN_POINT('Ctrl Pts',(-6.3025451773241,4.72148171340279,-43.1251322848833));
#80680=CARTESIAN_POINT('Ctrl Pts',(-7.43805686993446,-0.0613001757296944,
-42.9134472169747));
#80681=CARTESIAN_POINT('Ctrl Pts',(-6.51782155574628,-3.61709159384154,
-42.7546834160431));
#80682=CARTESIAN_POINT('Ctrl Pts',(-3.99377642814695,-6.27519985603844,
-42.5959196151115));
#80683=CARTESIAN_POINT('Ctrl Pts',(0.676882598949729,-7.85010679536756,
-42.384234547203));
#80684=CARTESIAN_POINT('Ctrl Pts',(5.53339973265141,-5.61202230336168,-42.1725494792941));
#80685=CARTESIAN_POINT('Ctrl Pts',(7.35740874754137,-1.04210842019799,-41.9608644113856));
#80686=CARTESIAN_POINT('Ctrl Pts',(6.88008342736724,3.83103269124661,-41.7491793434768));
#80687=CARTESIAN_POINT('Ctrl Pts',(1.82156696023834,8.25687211165112,-41.484573008591));
#80688=CARTESIAN_POINT('Ctrl Pts',(-5.96346347643551,5.98541592336455,-41.1670454067279));
#80689=CARTESIAN_POINT('Ctrl Pts',(-7.8622883821109,-0.445967127412303,
-40.9024390718421));
#80690=CARTESIAN_POINT('Ctrl Pts',(-5.6513290697449,-4.83641679938568,-40.6907540039334));
#80691=CARTESIAN_POINT('Ctrl Pts',(-2.65761733188299,-6.96436784985291,
-40.5319902030019));
#80692=CARTESIAN_POINT('Ctrl Pts',(0.985120771138287,-7.37278240947874,
-40.3732264020704));
#80693=CARTESIAN_POINT('Ctrl Pts',(5.57272164211232,-5.57019930083024,-40.1615413341616));
#80694=CARTESIAN_POINT('Ctrl Pts',(7.84725821905841,-0.7306472323605,-39.949856266253));
#80695=CARTESIAN_POINT('Ctrl Pts',(6.30013309195742,3.94027619101359,-39.7381711983442));
#80696=CARTESIAN_POINT('Ctrl Pts',(2.79702013649338,7.36132038461744,-39.5264861304356));
#80697=CARTESIAN_POINT('Ctrl Pts',(-3.92310111230352,7.49021501169607,-39.2618797955497));
#80698=CARTESIAN_POINT('Ctrl Pts',(-8.4167325287651,0.739401074974589,-38.9443521936867));
#80699=CARTESIAN_POINT('Ctrl Pts',(-5.72821052238303,-5.40389391952402,
-38.6797458588009));
#80700=CARTESIAN_POINT('Ctrl Pts',(-1.20952206795488,-7.33931223474337,
-38.4680607908921));
#80701=CARTESIAN_POINT('Ctrl Pts',(2.45117539507621,-7.0396795817255,-38.3092969899607));
#80702=CARTESIAN_POINT('Ctrl Pts',(5.50119344928266,-5.00652114994202,-38.150533189029));
#80703=CARTESIAN_POINT('Ctrl Pts',(7.85041243277023,-0.673328587573193,
-37.9388481211205));
#80704=CARTESIAN_POINT('Ctrl Pts',(6.47435703709748,4.49399687259815,-37.7271630532117));
#80705=CARTESIAN_POINT('Ctrl Pts',(2.2829603690937,7.07145991935139,-37.5154779853031));
#80706=CARTESIAN_POINT('Ctrl Pts',(-2.60012518698035,7.43314929629184,-37.3037929173943));
#80707=CARTESIAN_POINT('Ctrl Pts',(-7.82463741168122,3.2045425000323,-37.0391865825085));
#80708=CARTESIAN_POINT('Ctrl Pts',(-6.91569433641548,-4.85399549399435,
-36.7216589806454));
#80709=CARTESIAN_POINT('Ctrl Pts',(-0.902933400911396,-7.82299025665549,
-36.4570526457596));
#80710=CARTESIAN_POINT('Ctrl Pts',(3.80053655161767,-6.39408864747288,-36.2453675778509));
#80711=CARTESIAN_POINT('Ctrl Pts',(6.40836913874791,-3.80764420768715,-36.0866037769195));
#80712=CARTESIAN_POINT('Ctrl Pts',(7.43272289327584,-0.288121125605982,
-35.9278399759878));
#80713=CARTESIAN_POINT('Ctrl Pts',(6.43986165812585,4.53988200018871,-35.7161549080792));
#80714=CARTESIAN_POINT('Ctrl Pts',(2.05970576400102,7.60729380926465,-35.5044698401705));
#80715=CARTESIAN_POINT('Ctrl Pts',(-2.80678139359286,6.88036566226147,-35.2927847722618));
#80716=CARTESIAN_POINT('Ctrl Pts',(-6.77569267976859,4.01277312569048,-35.0810997043531));
#80717=CARTESIAN_POINT('Ctrl Pts',(-8.05004163744785,-2.58667216595958,
-34.8164933694672));
#80718=CARTESIAN_POINT('Ctrl Pts',(-2.16555916694153,-8.16691214014953,
-34.4989657676043));
#80719=CARTESIAN_POINT('Ctrl Pts',(4.34655538185322,-6.56672837832442,-34.2343594327183));
#80720=CARTESIAN_POINT('Ctrl Pts',(7.02504606785724,-2.44482626303123,-34.0226743648097));
#80721=CARTESIAN_POINT('Ctrl Pts',(7.3548148961523,1.21327955316404,-33.8639105638781));
#80722=CARTESIAN_POINT('Ctrl Pts',(5.87224758552886,4.56564252712561,-33.7051467629467));
#80723=CARTESIAN_POINT('Ctrl Pts',(2.00376723902932,7.62018789815773,-33.4934616950379));
#80724=CARTESIAN_POINT('Ctrl Pts',(-3.32262618525587,7.14656995822387,-33.2817766271293));
#80725=CARTESIAN_POINT('Ctrl Pts',(-6.57785513861537,3.45677236931173,-33.0700915592206));
#80726=CARTESIAN_POINT('Ctrl Pts',(-7.76793807460959,-1.29286407559497,
-32.8584064913119));
#80727=CARTESIAN_POINT('Ctrl Pts',(-4.4934155018909,-7.1626294324194,-32.5938001564261));
#80728=CARTESIAN_POINT('Ctrl Pts',(3.60198819584529,-7.6428909090368,-32.2762725545629));
#80729=CARTESIAN_POINT('Ctrl Pts',(7.55396722120535,-2.22531896661211,-32.0116662196771));
#80730=CARTESIAN_POINT('Ctrl Pts',(6.94908352259376,2.65305218718735,-31.7999811517684));
#80731=CARTESIAN_POINT('Ctrl Pts',(4.84585824796351,5.66418637329614,-31.6412173508369));
#80732=CARTESIAN_POINT('Ctrl Pts',(1.55290224233197,7.27439880794334,-31.4824535499054));
#80733=CARTESIAN_POINT('Ctrl Pts',(-3.37372709777454,7.12041517196706,-31.2707684819967));
#80734=CARTESIAN_POINT('Ctrl Pts',(-7.14393849288627,3.32828029838134,-31.059083414088));
#80735=CARTESIAN_POINT('Ctrl Pts',(-7.25855383130227,-1.59086445555011,
-30.8473983461793));
#80736=CARTESIAN_POINT('Ctrl Pts',(-5.11068959523401,-5.99109433326673,
-30.6357132782707));
#80737=CARTESIAN_POINT('Ctrl Pts',(1.1742846652758,-8.37347590810965,-30.3711069433848));
#80738=CARTESIAN_POINT('Ctrl Pts',(7.67726745228539,-3.52812483856874,-30.0535793415218));
#80739=CARTESIAN_POINT('Ctrl Pts',(7.21241190414664,3.16157868906219,-29.7889730066358));
#80740=CARTESIAN_POINT('Ctrl Pts',(3.60833725949656,6.50448690779315,-29.5772879387272));
#80741=CARTESIAN_POINT('Ctrl Pts',(0.0602446772548879,7.45397343768087,
-29.4185241377956));
#80742=CARTESIAN_POINT('Ctrl Pts',(-3.49601987738074,6.56553336814352,-29.2597603368642));
#80743=CARTESIAN_POINT('Ctrl Pts',(-7.16619381742337,3.2753645480404,-29.0480752689555));
#80744=CARTESIAN_POINT('Ctrl Pts',(-7.60892129361871,-2.05368539028039,
-28.8363902010468));
#80745=CARTESIAN_POINT('Ctrl Pts',(-4.52907501116952,-5.89108928646016,
-28.6247051331381));
#80746=CARTESIAN_POINT('Ctrl Pts',(-0.0523624522946749,-7.87461856997043,
-28.4130200652294));
#80747=CARTESIAN_POINT('Ctrl Pts',(6.290288275216,-5.65033774861951,-28.1484137303435));
#80748=CARTESIAN_POINT('Ctrl Pts',(8.14565125349276,2.24420722459355,-27.8308861284805));
#80749=CARTESIAN_POINT('Ctrl Pts',(3.48235724405825,7.06311923352307,-27.5662797935946));
#80750=CARTESIAN_POINT('Ctrl Pts',(-1.42765999532561,7.30001607187756,-27.354594725686));
#80751=CARTESIAN_POINT('Ctrl Pts',(-4.7536727468681,5.74177192567531,-27.1958309247544));
#80752=CARTESIAN_POINT('Ctrl Pts',(-6.90245939693678,2.77208182867794,-27.0370671238229));
#80753=CARTESIAN_POINT('Ctrl Pts',(-7.59187514474007,-2.1085014911341,-26.8253820559143));
#80754=CARTESIAN_POINT('Ctrl Pts',(-4.49911869007206,-6.47079886469823,
-26.6136969880055));
#80755=CARTESIAN_POINT('Ctrl Pts',(0.32823121314369,-7.42359196808149,-26.4020119200969));
#80756=CARTESIAN_POINT('Ctrl Pts',(5.030565356491,-6.05852883487454,-26.1903268521881));
#80757=CARTESIAN_POINT('Ctrl Pts',(8.45102006051422,-0.272586125069461,
-25.9257205173023));
#80758=CARTESIAN_POINT('Ctrl Pts',(4.78708586102741,6.96217705675442,-25.6081929154392));
#80759=CARTESIAN_POINT('Ctrl Pts',(-1.88376110602854,7.6463003719199,-25.3435865805534));
#80760=CARTESIAN_POINT('Ctrl Pts',(-5.79292116067826,4.66588814033186,-25.1319015126447));
#80761=CARTESIAN_POINT('Ctrl Pts',(-7.33424338023445,1.33199980115504,-24.9731377117132));
#80762=CARTESIAN_POINT('Ctrl Pts',(-7.0660199125409,-2.32373535214808,-24.8143739107817));
#80763=CARTESIAN_POINT('Ctrl Pts',(-4.45077960431779,-6.5017618893055,-24.602688842873));
#80764=CARTESIAN_POINT('Ctrl Pts',(0.724437388474664,-7.84783393076815,
-24.3910037749643));
#80765=CARTESIAN_POINT('Ctrl Pts',(5.03132948803849,-5.4683797436389,-24.1793187070556));
#80766=CARTESIAN_POINT('Ctrl Pts',(7.75005807142993,-1.39605133802358,-23.9676336391469));
#80767=CARTESIAN_POINT('Ctrl Pts',(6.64133580419396,5.23323055050373,-23.7030273042611));
#80768=CARTESIAN_POINT('Ctrl Pts',(-0.820524304628543,8.40921163224948,
-23.385499702398));
#80769=CARTESIAN_POINT('Ctrl Pts',(-6.36486022052054,4.63713485413607,-23.1208933675121));
#80770=CARTESIAN_POINT('Ctrl Pts',(-7.43658103535925,-0.160344056511672,
-22.9092082996035));
#80771=CARTESIAN_POINT('Ctrl Pts',(-6.46907641488485,-3.70356581812319,
-22.7504444986719));
#80772=CARTESIAN_POINT('Ctrl Pts',(-3.90985823955037,-6.3278267942373,-22.5916806977405));
#80773=CARTESIAN_POINT('Ctrl Pts',(0.781358983234233,-7.84039698553307,
-22.3799956298317));
#80774=CARTESIAN_POINT('Ctrl Pts',(5.60764191090731,-5.53783885046969,-22.168310561923));
#80775=CARTESIAN_POINT('Ctrl Pts',(7.37063366861889,-0.944040656363546,
-21.9566254940144));
#80776=CARTESIAN_POINT('Ctrl Pts',(6.82845720595584,3.92231202677236,-21.7449404261057));
#80777=CARTESIAN_POINT('Ctrl Pts',(1.71145232624966,8.28039698286071,-21.4803340912198));
#80778=CARTESIAN_POINT('Ctrl Pts',(-6.04263983906747,5.90547239310807,-21.1628064893568));
#80779=CARTESIAN_POINT('Ctrl Pts',(-7.85565249142942,-0.550626203615014,
-20.8982001544709));
#80780=CARTESIAN_POINT('Ctrl Pts',(-5.58642354525344,-4.9112442094607,-20.6865150865622));
#80781=CARTESIAN_POINT('Ctrl Pts',(-2.56464027395697,-6.99914063982059,
-20.5277512856307));
#80782=CARTESIAN_POINT('Ctrl Pts',(1.0832135062605,-7.35901025214003,-20.3689874846992));
#80783=CARTESIAN_POINT('Ctrl Pts',(5.64640339528061,-5.49549592386352,-20.1573024167905));
#80784=CARTESIAN_POINT('Ctrl Pts',(7.85629211453692,-0.626083976636307,
-19.9456173488818));
#80785=CARTESIAN_POINT('Ctrl Pts',(6.24710354692251,4.0238228976775,-19.7339322809731));
#80786=CARTESIAN_POINT('Ctrl Pts',(2.69874467633993,7.39791434262794,-19.5222472130645));
#80787=CARTESIAN_POINT('Ctrl Pts',(-4.02249713685988,7.43730865587472,-19.2576408781786));
#80788=CARTESIAN_POINT('Ctrl Pts',(-8.42583250041413,0.627253605339702,
-18.9401132763156));
#80789=CARTESIAN_POINT('Ctrl Pts',(-5.65574133884476,-5.47969480813399,
-18.6755069414297));
#80790=CARTESIAN_POINT('Ctrl Pts',(-1.11168044293459,-7.35476813398764,
-18.463821873521));
#80791=CARTESIAN_POINT('Ctrl Pts',(2.54470235302645,-7.00641415884697,-18.3050580725895));
#80792=CARTESIAN_POINT('Ctrl Pts',(5.56737529197671,-4.93282026325047,-18.146294271658));
#80793=CARTESIAN_POINT('Ctrl Pts',(7.85868276150516,-0.568728410982657,
-17.9346092037493));
#80794=CARTESIAN_POINT('Ctrl Pts',(6.41393839013896,4.57981454452449,-17.7229241358406));
#80795=CARTESIAN_POINT('Ctrl Pts',(2.18859043397245,7.10123407234051,-17.5112390679319));
#80796=CARTESIAN_POINT('Ctrl Pts',(-2.69887859996051,7.39786548617967,-17.2995540000232));
#80797=CARTESIAN_POINT('Ctrl Pts',(-7.86661708291787,3.10006111706502,-17.0349476651374));
#80798=CARTESIAN_POINT('Ctrl Pts',(-6.85044261384541,-4.94565833887236,
-16.7174200632743));
#80799=CARTESIAN_POINT('Ctrl Pts',(-0.798678034425534,-7.83432056272497,
-16.4528137283885));
#80800=CARTESIAN_POINT('Ctrl Pts',(3.88534681350714,-6.34291162248799,-16.2411286604798));
#80801=CARTESIAN_POINT('Ctrl Pts',(6.45850562839871,-3.72196916681638,-16.0823648595482));
#80802=CARTESIAN_POINT('Ctrl Pts',(7.43590062071016,-0.189117292095101,
-15.9236010586167));
#80803=CARTESIAN_POINT('Ctrl Pts',(6.37883503788212,4.62523624379607,-15.7119159907081));
#80804=CARTESIAN_POINT('Ctrl Pts',(1.9582201615972,7.6340474673302,-15.5002309227993));
#80805=CARTESIAN_POINT('Ctrl Pts',(-2.898155307152,6.84237891770634,-15.2885458548907));
#80806=CARTESIAN_POINT('Ctrl Pts',(-6.82852821024978,3.9221884109201,-15.076860786982));
#80807=CARTESIAN_POINT('Ctrl Pts',(-8.01488227586511,-2.69364165449249,
-14.8122544520961));
#80808=CARTESIAN_POINT('Ctrl Pts',(-2.05661198859221,-8.19502578024167,
-14.4947268502331));
#80809=CARTESIAN_POINT('Ctrl Pts',(4.43361619564124,-6.50826495403781,-14.2301205153472));
#80810=CARTESIAN_POINT('Ctrl Pts',(7.05697983290556,-2.35106004812461,-14.0184354474385));
#80811=CARTESIAN_POINT('Ctrl Pts',(7.33800604231056,1.31111279217438,-13.859671646507));
#80812=CARTESIAN_POINT('Ctrl Pts',(5.81092825366935,4.64343582080709,-13.7009078455755));
#80813=CARTESIAN_POINT('Ctrl Pts',(1.90211489177139,7.64619550429748,-13.4892227776668));
#80814=CARTESIAN_POINT('Ctrl Pts',(-3.41749928418853,7.10169033240024,-13.2775377097581));
#80815=CARTESIAN_POINT('Ctrl Pts',(-6.62330419485259,3.36887146983878,-13.0658526418494));
#80816=CARTESIAN_POINT('Ctrl Pts',(-7.7500327975144,-1.39619163669753,-12.8541675739407));
#80817=CARTESIAN_POINT('Ctrl Pts',(-4.3976355031666,-7.22183115560607,-12.5895612390549));
#80818=CARTESIAN_POINT('Ctrl Pts',(3.70344581070873,-7.59424713435049,-12.2720336371918));
#80819=CARTESIAN_POINT('Ctrl Pts',(7.58293100553107,-2.12452880600961,-12.007427302306));
#80820=CARTESIAN_POINT('Ctrl Pts',(6.91313782877864,2.74535481718361,-11.7957422343973));
#80821=CARTESIAN_POINT('Ctrl Pts',(4.77000110240001,5.7282142866597,-11.6369784334658));
#80822=CARTESIAN_POINT('Ctrl Pts',(1.45589459345264,7.29443310504678,-11.4782146325342));
#80823=CARTESIAN_POINT('Ctrl Pts',(-3.46824737389549,7.07485737700085,-11.2665295646256));
#80824=CARTESIAN_POINT('Ctrl Pts',(-7.18762628279014,3.23285251035057,-11.0548444967169));
#80825=CARTESIAN_POINT('Ctrl Pts',(-7.23672538158249,-1.68738234831527,
-10.8431594288082));
#80826=CARTESIAN_POINT('Ctrl Pts',(-5.03045567843081,-6.05861990194769,
-10.6314743608995));
#80827=CARTESIAN_POINT('Ctrl Pts',(1.28568642045295,-8.3570960080076,-10.3668680260136));
#80828=CARTESIAN_POINT('Ctrl Pts',(7.72356919371295,-3.42557722440691,-10.0493404241506));
#80829=CARTESIAN_POINT('Ctrl Pts',(7.16967103849924,3.25734285605831,-9.78473408926473));
#80830=CARTESIAN_POINT('Ctrl Pts',(3.52139993317844,6.55196079220062,-9.57304902135602));
#80831=CARTESIAN_POINT('Ctrl Pts',(-0.0390219347217104,7.45411475088761,
-9.41428522042451));
#80832=CARTESIAN_POINT('Ctrl Pts',(-3.583140194126,6.51839625525219,-9.255521419493));
#80833=CARTESIAN_POINT('Ctrl Pts',(-7.20917497830124,3.17964508769009,-9.0438363515843));
#80834=CARTESIAN_POINT('Ctrl Pts',(-7.58089859521199,-2.15482793369875,
-8.83215128367564));
#80835=CARTESIAN_POINT('Ctrl Pts',(-4.45022438873187,-5.95087861813555,
-8.62046621576692));
#80836=CARTESIAN_POINT('Ctrl Pts',(0.0525050061010802,-7.87461762076525,
-8.40878114785824));
#80837=CARTESIAN_POINT('Ctrl Pts',(6.36497357055341,-5.5660717480959,-8.14417481297238));
#80838=CARTESIAN_POINT('Ctrl Pts',(8.11504386855144,2.35248027025413,-7.82664721110936));
#80839=CARTESIAN_POINT('Ctrl Pts',(3.38799202849415,7.10886596420688,-7.56204087622348));
#80840=CARTESIAN_POINT('Ctrl Pts',(-1.52474449364832,7.2803572674027,-7.3503558083148));
#80841=CARTESIAN_POINT('Ctrl Pts',(-4.82971188134325,5.67796024765845,-7.19159200738328));
#80842=CARTESIAN_POINT('Ctrl Pts',(-6.93876194940002,2.67991902877748,-7.03282820645175));
#80843=CARTESIAN_POINT('Ctrl Pts',(-7.56312399601624,-2.20941217802357,
-6.82114313854308));
#80844=CARTESIAN_POINT('Ctrl Pts',(-4.41255098757272,-6.53013787883321,
-6.60945807063438));
#80845=CARTESIAN_POINT('Ctrl Pts',(0.427058802627542,-7.41856281345515,
-6.39777300272569));
#80846=CARTESIAN_POINT('Ctrl Pts',(5.11079805088555,-5.99100181369613,-6.186087934817));
#80847=CARTESIAN_POINT('Ctrl Pts',(8.45390062348955,-0.160023455758246,
-5.92148159993113));
#80848=CARTESIAN_POINT('Ctrl Pts',(4.6939491585227,7.02530723244401,-5.60395399806812));
#80849=CARTESIAN_POINT('Ctrl Pts',(-1.98541647728356,7.62053716549387,-5.33934766318224));
#80850=CARTESIAN_POINT('Ctrl Pts',(-5.85454107668646,4.58833264865286,-5.12766259527357));
#80851=CARTESIAN_POINT('Ctrl Pts',(-7.35133071109141,1.23421481508714,-4.96889879434203));
#80852=CARTESIAN_POINT('Ctrl Pts',(-7.03444921622923,-2.41762437130216,
-4.81013499341053));
#80853=CARTESIAN_POINT('Ctrl Pts',(-4.36380386843999,-6.56045445084411,
-4.59844992550183));
#80854=CARTESIAN_POINT('Ctrl Pts',(0.82887929194248,-7.83749105040353,-4.38676485759314));
#80855=CARTESIAN_POINT('Ctrl Pts',(5.10370335701861,-5.40089488195087,-4.17507978968447));
#80856=CARTESIAN_POINT('Ctrl Pts',(7.7679614850053,-1.29272343653906,-3.96339472177576));
#80857=CARTESIAN_POINT('Ctrl Pts',(6.57105828821083,5.32120622293475,-3.69878838688992));
#80858=CARTESIAN_POINT('Ctrl Pts',(-0.932433277993894,8.39753949490707,
-3.38126078502686));
#80859=CARTESIAN_POINT('Ctrl Pts',(-6.42604657304033,4.55196554858829,-3.11665445014101));
#80860=CARTESIAN_POINT('Ctrl Pts',(-7.43378634629405,-0.259359358977234,
-2.90496938223232));
#80861=CARTESIAN_POINT('Ctrl Pts',(-6.41918419191598,-3.78938356951557,
-2.7462055813008));
#80862=CARTESIAN_POINT('Ctrl Pts',(-3.82524643111245,-6.37933098263298,
-2.58744178036929));
#80863=CARTESIAN_POINT('Ctrl Pts',(0.885696229427913,-7.82929809871447,
-2.37575671246058));
#80864=CARTESIAN_POINT('Ctrl Pts',(5.68089073662934,-5.4626707788536,-2.16407164455192));
#80865=CARTESIAN_POINT('Ctrl Pts',(7.38255020742661,-0.845808454586203,
-1.95238657664321));
#80866=CARTESIAN_POINT('Ctrl Pts',(6.775623039718,4.01290274686232,-1.74070150873454));
#80867=CARTESIAN_POINT('Ctrl Pts',(1.6010277902956,8.30243859911855,-1.47609517384866));
#80868=CARTESIAN_POINT('Ctrl Pts',(-6.12073333244397,5.82450772649672,-1.15856757198564));
#80869=CARTESIAN_POINT('Ctrl Pts',(-7.84764258678692,-0.655231887258009,
-0.893961237099761));
#80870=CARTESIAN_POINT('Ctrl Pts',(-5.52050089002332,-4.98513938774051,
-0.682276169191086));
#80871=CARTESIAN_POINT('Ctrl Pts',(-2.47126608679663,-7.03280588366045,
-0.523512368259554));
#80872=CARTESIAN_POINT('Ctrl Pts',(1.18122166265399,-7.34368389283164,-0.364748567328037));
#80873=CARTESIAN_POINT('Ctrl Pts',(5.71883850865417,-5.42038649664947,-0.153063499419362));
#80874=CARTESIAN_POINT('Ctrl Pts',(7.86440313102783,-0.520319605577109,
0.0586215684893359));
#80875=CARTESIAN_POINT('Ctrl Pts',(6.19241647359457,4.10538175951475,0.270306636398015));
#80876=CARTESIAN_POINT('Ctrl Pts',(2.601272284163,7.43617310821803,0.48199170430671));
#80877=CARTESIAN_POINT('Ctrl Pts',(-4.12386344860959,7.37678467612258,0.74659803919257));
#80878=CARTESIAN_POINT('Ctrl Pts',(-8.42894816866634,0.525894078781797,
1.06412564105561));
#80879=CARTESIAN_POINT('Ctrl Pts',(-5.02020791058217,-6.79126235295692,
1.38165324291864));
#80880=CARTESIAN_POINT('Ctrl Pts',(2.99431082191942,-7.90299339506185,1.69918084478167));
#80881=CARTESIAN_POINT('Ctrl Pts',(7.36643365261397,-2.79265881077084,1.96378717966754));
#80882=CARTESIAN_POINT('Ctrl Pts',(7.12687393130928,2.09948782826333,2.17547224757623));
#80883=CARTESIAN_POINT('Ctrl Pts',(4.66127205797912,6.35547888838997,2.38715731548491));
#80884=CARTESIAN_POINT('Ctrl Pts',(-0.470419877862721,7.86539311157671,
2.59884238339361));
#80885=CARTESIAN_POINT('Ctrl Pts',(-4.86213645379484,5.62890813913654,2.81052745130229));
#80886=CARTESIAN_POINT('Ctrl Pts',(-6.97398870797767,2.63267851626443,2.96929125223381));
#80887=CARTESIAN_POINT('Ctrl Pts',(-7.36810642574136,-1.01909395587376,
3.12805505316534));
#80888=CARTESIAN_POINT('Ctrl Pts',(-5.55045257799891,-5.58634936030821,
3.339740121074));
#80889=CARTESIAN_POINT('Ctrl Pts',(0.521240305046402,-8.43306440905713,
3.60434645595989));
#80890=CARTESIAN_POINT('Ctrl Pts',(7.3861046083072,-4.11573023807145,3.9218740578229));
#80891=CARTESIAN_POINT('Ctrl Pts',(7.43128453774611,2.60546850896112,4.18648039270878));
#80892=CARTESIAN_POINT('Ctrl Pts',(4.10208550089539,6.19599338688865,4.39816546061746));
#80893=CARTESIAN_POINT('Ctrl Pts',(-0.5272052621981,7.86354539703132,4.60985052852616));
#80894=CARTESIAN_POINT('Ctrl Pts',(-5.42403478710137,5.71508645233573,4.82153559643483));
#80895=CARTESIAN_POINT('Ctrl Pts',(-7.34480133401163,1.17569868955459,5.03322066434353));
#80896=CARTESIAN_POINT('Ctrl Pts',(-7.03084851288744,-2.476393085818,5.19198446527505));
#80897=CARTESIAN_POINT('Ctrl Pts',(-4.98112867333205,-5.52420164903002,
5.35074826620655));
#80898=CARTESIAN_POINT('Ctrl Pts',(-0.649401219666167,-7.84810441892272,
5.56243333411527));
#80899=CARTESIAN_POINT('Ctrl Pts',(5.82899312617974,-6.11644835843352,5.8270396690011));
#80900=CARTESIAN_POINT('Ctrl Pts',(8.30127062559556,1.60715546686924,6.14456727086416));
#80901=CARTESIAN_POINT('Ctrl Pts',(4.00789879630099,6.77857704496396,6.40917360575001));
#80902=CARTESIAN_POINT('Ctrl Pts',(-0.85124868288478,7.38192584372215,6.62085867365872));
#80903=CARTESIAN_POINT('Ctrl Pts',(-5.46686056367904,5.67686026101199,6.83254374156738));
#80904=CARTESIAN_POINT('Ctrl Pts',(-7.82994770275829,0.879923732992005,
7.04422880947609));
#80905=CARTESIAN_POINT('Ctrl Pts',(-6.37650933343722,-3.82994935958821,
7.25591387738476));
#80906=CARTESIAN_POINT('Ctrl Pts',(-3.78464912651592,-6.42197636423389,
7.41467767831628));
#80907=CARTESIAN_POINT('Ctrl Pts',(-0.253878226009082,-7.43397562275133,
7.5734414792478));
#80908=CARTESIAN_POINT('Ctrl Pts',(4.5567025757456,-6.42268844917267,7.78512654715649));
#80909=CARTESIAN_POINT('Ctrl Pts',(8.39822466880191,-0.926241234967016,
8.04973288204236));
#80910=CARTESIAN_POINT('Ctrl Pts',(5.31635972703513,6.57498003882823,8.36726048390539));
#80911=CARTESIAN_POINT('Ctrl Pts',(-1.29845070622145,7.76700619364757,8.63186681879125));
#80912=CARTESIAN_POINT('Ctrl Pts',(-5.40465655583919,5.09971969342482,8.84355188669994));
#80913=CARTESIAN_POINT('Ctrl Pts',(-7.83810008915857,0.823100192463282,
9.05523695460863));
#80914=CARTESIAN_POINT('Ctrl Pts',(-6.55723507065759,-4.36863994621369,
9.26692202251733));
#80915=CARTESIAN_POINT('Ctrl Pts',(-2.41243695628078,-7.03622990835402,
9.47860709042599));
#80916=CARTESIAN_POINT('Ctrl Pts',(1.23963488792975,-7.35041868027973,9.63737089135754));
#80917=CARTESIAN_POINT('Ctrl Pts',(4.59264817040183,-5.85115633826675,9.79613469228902));
#80918=CARTESIAN_POINT('Ctrl Pts',(7.62199901511133,-1.97979703400137,10.0078197601977));
#80919=CARTESIAN_POINT('Ctrl Pts',(7.0218443005315,4.69912790095596,10.2724260950835));
#80920=CARTESIAN_POINT('Ctrl Pts',(-0.166256785307518,8.4537803342726,10.5899536969466));
#80921=CARTESIAN_POINT('Ctrl Pts',(-5.99476856532561,5.10637927470297,10.8545600318324));
#80922=CARTESIAN_POINT('Ctrl Pts',(-7.41887568305574,0.421588706218421,
11.0662450997412));
#80923=CARTESIAN_POINT('Ctrl Pts',(-6.52688256694344,-4.41736469991614,
11.2779301676499));
#80924=CARTESIAN_POINT('Ctrl Pts',(-2.20383500679938,-7.56475102129884,
11.4896152355585));
#80925=CARTESIAN_POINT('Ctrl Pts',(2.68503450571567,-6.93678405994906,11.7013003034672));
#80926=CARTESIAN_POINT('Ctrl Pts',(5.68151982913352,-4.82552399869201,11.8600641043987));
#80927=CARTESIAN_POINT('Ctrl Pts',(7.28147953878471,-1.5193760028984,12.0188279053302));
#80928=CARTESIAN_POINT('Ctrl Pts',(7.10636594014363,3.39323273693023,12.230512973239));
#80929=CARTESIAN_POINT('Ctrl Pts',(2.34649610924198,8.1167762331949,12.4951193081248));
#80930=CARTESIAN_POINT('Ctrl Pts',(-5.57076336512423,6.36086777009108,12.8126469099879));
#80931=CARTESIAN_POINT('Ctrl Pts',(-7.8746541940651,0.0466987454495366,
13.0772532448737));
#80932=CARTESIAN_POINT('Ctrl Pts',(-5.94759568570367,-4.45461098158359,
13.2889383127824));
#80933=CARTESIAN_POINT('Ctrl Pts',(-2.14923767145121,-7.58248536868689,
13.5006233806911));
#80934=CARTESIAN_POINT('Ctrl Pts',(3.18495981430195,-7.20682854886377,13.7123084485998));
#80935=CARTESIAN_POINT('Ctrl Pts',(6.52103646492693,-3.57833296582929,13.9239935165085));
#80936=CARTESIAN_POINT('Ctrl Pts',(7.45414149692743,-0.0335257300303479,
14.08275731744));
#80937=CARTESIAN_POINT('Ctrl Pts',(6.54936255294715,3.52622997859995,14.2415211183715));
#80938=CARTESIAN_POINT('Ctrl Pts',(3.25205550737496,7.17207084872711,14.4532061862802));
#80939=CARTESIAN_POINT('Ctrl Pts',(-3.43127116601776,7.72104128959961,14.7178125211661));
#80940=CARTESIAN_POINT('Ctrl Pts',(-8.35804172035165,1.27952407544949,15.0353401230291));
#80941=CARTESIAN_POINT('Ctrl Pts',(-6.05490911427058,-5.03492155518401,
15.299946457915));
#80942=CARTESIAN_POINT('Ctrl Pts',(-1.6820459847554,-7.23796758372227,15.5116315258236));
#80943=CARTESIAN_POINT('Ctrl Pts',(3.23815133384991,-7.18524062741268,15.7233165937323));
#80944=CARTESIAN_POINT('Ctrl Pts',(7.07741272069182,-3.46302987749542,15.935001661641));
#80945=CARTESIAN_POINT('Ctrl Pts',(7.29335763733033,1.46127265260201,16.1466867295497));
#80946=CARTESIAN_POINT('Ctrl Pts',(5.72469563157511,4.7742234296914,16.3054505304812));
#80947=CARTESIAN_POINT('Ctrl Pts',(2.74025675908468,6.91516020105205,16.4642143314127));
#80948=CARTESIAN_POINT('Ctrl Pts',(-2.13011940355835,7.58136245069402,16.6758993993214));
#80949=CARTESIAN_POINT('Ctrl Pts',(-7.5969757573475,3.69784528512499,16.9405057342073));
#80950=CARTESIAN_POINT('Ctrl Pts',(-7.21858665341493,-4.40295923055548,
17.2580333360703));
#80951=CARTESIAN_POINT('Ctrl Pts',(-1.39047687177878,-7.75106015445512,
17.5226396709562));
#80952=CARTESIAN_POINT('Ctrl Pts',(3.37375416084809,-6.62081840107444,17.7343247388649));
#80953=CARTESIAN_POINT('Ctrl Pts',(7.10420825035649,-3.41226201665443,17.9460098067736));
#80954=CARTESIAN_POINT('Ctrl Pts',(7.64479092625569,1.90775219703075,18.1576948746822));
#80955=CARTESIAN_POINT('Ctrl Pts',(4.63914994657131,5.81435045077905,18.3693799425909));
#80956=CARTESIAN_POINT('Ctrl Pts',(1.30570185292558,7.3389707794797,18.5281437435225));
#80957=CARTESIAN_POINT('Ctrl Pts',(-2.356262780872,7.05524439118878,18.6869075444539));
#80958=CARTESIAN_POINT('Ctrl Pts',(-6.5115322538303,4.42881620633961,18.8985926123627));
#80959=CARTESIAN_POINT('Ctrl Pts',(-8.19350713659474,-2.06265392468485,
19.1631989472485));
#80960=CARTESIAN_POINT('Ctrl Pts',(-2.687731253583,-8.01686621862352,19.4807265491116));
#80961=CARTESIAN_POINT('Ctrl Pts',(3.92722227076492,-6.82563437967056,19.7453328839974));
#80962=CARTESIAN_POINT('Ctrl Pts',(6.84451397465846,-2.89310938067519,19.9570179519061));
#80963=CARTESIAN_POINT('Ctrl Pts',(7.63260152410329,1.96384849440906,20.1687030198148));
#80964=CARTESIAN_POINT('Ctrl Pts',(4.62053163586282,6.38224366139593,20.3803880877235));
#80965=CARTESIAN_POINT('Ctrl Pts',(-0.194600004819961,7.43575915622415,
20.5920731556322));
#80966=CARTESIAN_POINT('Ctrl Pts',(-3.72673024977302,6.45575952744647,20.7508369565637));
#80967=CARTESIAN_POINT('Ctrl Pts',(-6.34577470796605,3.88066889436112,20.9096007574952));
#80968=CARTESIAN_POINT('Ctrl Pts',(-7.83372953828914,-0.804454351188343,
21.1212858254039));
#80969=CARTESIAN_POINT('Ctrl Pts',(-4.9406059101558,-6.85408736820449,21.3858921602898));
#80970=CARTESIAN_POINT('Ctrl Pts',(3.10586062165327,-7.86432915496657,21.7034197621528));
#80971=CARTESIAN_POINT('Ctrl Pts',(7.39985345805689,-2.69342314689265,21.9680260970386));
#80972=CARTESIAN_POINT('Ctrl Pts',(7.09961841344044,2.19382584116961,22.1797111649474));
#80973=CARTESIAN_POINT('Ctrl Pts',(4.5750840659402,6.41731351301429,22.391396232856));
#80974=CARTESIAN_POINT('Ctrl Pts',(-0.574522753402311,7.85826128079608,
22.6030813007648));
#80975=CARTESIAN_POINT('Ctrl Pts',(-4.93692395375169,5.56373662803334,22.8147663686734));
#80976=CARTESIAN_POINT('Ctrl Pts',(-7.00828855729298,2.53953557338866,22.973530169605));
#80977=CARTESIAN_POINT('Ctrl Pts',(-7.35394645167502,-1.11710308289776,
23.1322939705364));
#80978=CARTESIAN_POINT('Ctrl Pts',(-5.47552313161862,-5.65978018277373,
23.3439790384452));
#80979=CARTESIAN_POINT('Ctrl Pts',(0.633466112297581,-8.42536771274805,
23.6085853733309));
#80980=CARTESIAN_POINT('Ctrl Pts',(7.44027256985801,-4.01701224108319,23.9261129751941));
#80981=CARTESIAN_POINT('Ctrl Pts',(7.3959224475177,2.70419869817981,24.1907193100799));
#80982=CARTESIAN_POINT('Ctrl Pts',(4.01921558372116,6.25006876197528,24.4024043779886));
#80983=CARTESIAN_POINT('Ctrl Pts',(-0.631876540752792,7.85582834410108,
24.6140894458972));
#80984=CARTESIAN_POINT('Ctrl Pts',(-5.49965773175034,5.64234982831051,24.825774513806));
#80985=CARTESIAN_POINT('Ctrl Pts',(-7.35980694503976,1.07778714178239,25.0374595817147));
#80986=CARTESIAN_POINT('Ctrl Pts',(-6.99724773323839,-2.56980030167315,
25.1962233826462));
#80987=CARTESIAN_POINT('Ctrl Pts',(-4.90712379803821,-5.59004326840594,
25.3549871835777));
#80988=CARTESIAN_POINT('Ctrl Pts',(-0.544833791248015,-7.85605635303897,
25.5666722514863));
#80989=CARTESIAN_POINT('Ctrl Pts',(5.90992624931247,-6.03828387359638,25.8312785863723));
#80990=CARTESIAN_POINT('Ctrl Pts',(8.27913281497273,1.71755730350853,26.1488061882353));
#80991=CARTESIAN_POINT('Ctrl Pts',(3.91727608688812,6.83134741526356,26.4134125231212));
#80992=CARTESIAN_POINT('Ctrl Pts',(-0.949475040141325,7.36993558899901,
26.6250975910298));
#80993=CARTESIAN_POINT('Ctrl Pts',(-5.54197206657227,5.60355713347054,26.8367826589385));
#80994=CARTESIAN_POINT('Ctrl Pts',(-7.84097097908883,0.775577756594261,
27.0484677268472));
#80995=CARTESIAN_POINT('Ctrl Pts',(-6.32494219125582,-3.91452291710228,
27.2601527947559));
#80996=CARTESIAN_POINT('Ctrl Pts',(-3.69879492243045,-6.47180543222624,
27.4189165956874));
#80997=CARTESIAN_POINT('Ctrl Pts',(-0.154860747096868,-7.43669724144609,
27.5776803966189));
#80998=CARTESIAN_POINT('Ctrl Pts',(4.6418266401032,-6.36143935956612,27.7893654645276));
#80999=CARTESIAN_POINT('Ctrl Pts',(8.40981434922058,-0.814323659296858,
28.0539717994135));
#81000=CARTESIAN_POINT('Ctrl Pts',(5.22833222578838,6.64519265300687,28.3714994012766));
#81001=CARTESIAN_POINT('Ctrl Pts',(-1.40176536255414,7.74902660450176,28.6361057361623));
#81002=CARTESIAN_POINT('Ctrl Pts',(-5.47208804219018,5.0272960820271,28.8477908040711));
#81003=CARTESIAN_POINT('Ctrl Pts',(-7.84836595190842,0.718650693773629,
29.0594758719798));
#81004=CARTESIAN_POINT('Ctrl Pts',(-6.49847839774445,-4.45557238359858,
29.2711609398884));
#81005=CARTESIAN_POINT('Ctrl Pts',(-2.3185246830527,-7.06773136765416,29.4828460077972));
#81006=CARTESIAN_POINT('Ctrl Pts',(1.33740724756926,-7.33325925390194,29.6416098087286));
#81007=CARTESIAN_POINT('Ctrl Pts',(4.67015820669236,-5.78947925433603,29.8003736096602));
#81008=CARTESIAN_POINT('Ctrl Pts',(7.64768726003397,-1.87812269432075,30.0120586775688));
#81009=CARTESIAN_POINT('Ctrl Pts',(6.95864546901471,4.79221802999488,30.2766650124548));
#81010=CARTESIAN_POINT('Ctrl Pts',(-0.278817300155773,8.45081677543235,
30.5941926143177));
#81011=CARTESIAN_POINT('Ctrl Pts',(-6.06223640958164,5.02609681196815,30.8587989492036));
#81012=CARTESIAN_POINT('Ctrl Pts',(-7.4238319670998,0.322757435410584,31.0704840171123));
#81013=CARTESIAN_POINT('Ctrl Pts',(-6.46747973936085,-4.50388862603115,
31.282169085021));
#81014=CARTESIAN_POINT('Ctrl Pts',(-2.10290314806414,-7.59342775703431,
31.4938541529297));
#81015=CARTESIAN_POINT('Ctrl Pts',(2.777170513354,-6.90041356231668,31.7055392208384));
#81016=CARTESIAN_POINT('Ctrl Pts',(5.74527542334076,-4.74943783418069,31.8643030217699));
#81017=CARTESIAN_POINT('Ctrl Pts',(7.30106675393053,-1.42227703580339,32.0230668227014));
#81018=CARTESIAN_POINT('Ctrl Pts',(7.06054964293635,3.4875641960886,32.2347518906101));
#81019=CARTESIAN_POINT('Ctrl Pts',(2.23820052505865,8.14730377610127,32.499358225496));
#81020=CARTESIAN_POINT('Ctrl Pts',(-5.6549742745155,6.28612036262135,32.8168858273589));
#81021=CARTESIAN_POINT('Ctrl Pts',(-7.87457782062009,-0.058168685139664,
33.0814921622449));
#81022=CARTESIAN_POINT('Ctrl Pts',(-5.88774823080518,-4.5334174977048,33.2931772301535));
#81023=CARTESIAN_POINT('Ctrl Pts',(-2.04807449335629,-7.61043348334377,
33.5048622980623));
#81024=CARTESIAN_POINT('Ctrl Pts',(3.28064755703563,-7.16377682217656,33.7165473659709));
#81025=CARTESIAN_POINT('Ctrl Pts',(6.56810932797811,-3.4911779168318,33.9282324338796));
#81026=CARTESIAN_POINT('Ctrl Pts',(7.45392699082019,0.0657407507670758,
34.0869962348112));
#81027=CARTESIAN_POINT('Ctrl Pts',(6.50182457934332,3.61313227703756,34.2457600357426));
#81028=CARTESIAN_POINT('Ctrl Pts',(3.15625985199202,7.21474109229927,34.4574451036513));
#81029=CARTESIAN_POINT('Ctrl Pts',(-3.53378461232003,7.67466394861541,34.7220514385372));
#81030=CARTESIAN_POINT('Ctrl Pts',(-8.37433947537304,1.16811027304956,35.0395790404002));
#81031=CARTESIAN_POINT('Ctrl Pts',(-5.98732440451525,-5.11510566108166,
35.3041853752861));
#81032=CARTESIAN_POINT('Ctrl Pts',(-1.5855120233048,-7.25972486130166,35.5158704431948));
#81033=CARTESIAN_POINT('Ctrl Pts',(3.33354688331943,-7.14148248695229,35.7275555111035));
#81034=CARTESIAN_POINT('Ctrl Pts',(7.12290080998369,-3.36847603562356,35.9392405790121));
#81035=CARTESIAN_POINT('Ctrl Pts',(7.27325181835091,1.55826550308438,36.1509256469209));
#81036=CARTESIAN_POINT('Ctrl Pts',(5.66061180334153,4.85003334448958,36.3096894478524));
#81037=CARTESIAN_POINT('Ctrl Pts',(2.64792765009157,6.95103782695821,36.4684532487839));
#81038=CARTESIAN_POINT('Ctrl Pts',(-2.23088818069513,7.55232435793397,36.6801383166926));
#81039=CARTESIAN_POINT('Ctrl Pts',(-7.64554471036468,3.59635183098948,36.9447446515784));
#81040=CARTESIAN_POINT('Ctrl Pts',(-7.15931432419098,-4.49869555162702,
37.2622722534414));
#81041=CARTESIAN_POINT('Ctrl Pts',(-1.28713613654189,-7.76888923945637,
37.5268785883273));
#81042=CARTESIAN_POINT('Ctrl Pts',(3.46162152515911,-6.57530454461241,37.738563656236));
#81043=CARTESIAN_POINT('Ctrl Pts',(7.14901791054088,-3.31735585210594,37.9502487241447));
#81044=CARTESIAN_POINT('Ctrl Pts',(7.61870837515603,2.00938534028792,38.1619337920533));
#81045=CARTESIAN_POINT('Ctrl Pts',(4.56131146102861,5.87561240610175,38.3736188599621));
#81046=CARTESIAN_POINT('Ctrl Pts',(1.20785624672071,7.35570749269215,38.5323826608936));
#81047=CARTESIAN_POINT('Ctrl Pts',(-2.45000542434561,7.02324149752807,38.6911464618251));
#81048=CARTESIAN_POINT('Ctrl Pts',(-6.56993146907149,4.34171230897587,38.9028315297338));
#81049=CARTESIAN_POINT('Ctrl Pts',(-8.16531317336679,-2.17158034419366,
39.1674378646196));
#81050=CARTESIAN_POINT('Ctrl Pts',(-2.58073586983221,-8.05194669809458,
39.4849654664827));
#81051=CARTESIAN_POINT('Ctrl Pts',(4.01776800332386,-6.77273207209629,39.7495718013686));
#81052=CARTESIAN_POINT('Ctrl Pts',(6.88243333552675,-2.80170748292457,39.9612568692772));
#81053=CARTESIAN_POINT('Ctrl Pts',(7.60577304422771,2.06531434276588,40.172941937186));
#81054=CARTESIAN_POINT('Ctrl Pts',(4.53513241827669,6.44320733021469,40.3846270050946));
#81055=CARTESIAN_POINT('Ctrl Pts',(-0.293601468362634,7.43250843047103,
40.5963120730034));
#81056=CARTESIAN_POINT('Ctrl Pts',(-3.81236829986945,6.4055598800527,40.7550758739348));
#81057=CARTESIAN_POINT('Ctrl Pts',(-6.39688918530141,3.79582092081505,40.9138396748664));
#81058=CARTESIAN_POINT('Ctrl Pts',(-7.82232236396769,-0.908701335081412,
41.125524742775));
#81059=CARTESIAN_POINT('Ctrl Pts',(-4.8488949776899,-6.91927148663638,41.3901310776609));
#81060=CARTESIAN_POINT('Ctrl Pts',(3.21031102305723,-7.82227245715925,41.7076586795239));
#81061=CARTESIAN_POINT('Ctrl Pts',(7.43506444403943,-2.59464374470073,41.9722650144098));
#81062=CARTESIAN_POINT('Ctrl Pts',(7.06977468610669,2.28817379705533,42.1839500823185));
#81063=CARTESIAN_POINT('Ctrl Pts',(4.48922186844248,6.47766886701024,42.3956351502272));
#81064=CARTESIAN_POINT('Ctrl Pts',(-0.679116803540349,7.84991382873632,
42.6073202181359));
#81065=CARTESIAN_POINT('Ctrl Pts',(-5.01057602209241,5.49750046094407,42.8190052860445));
#81066=CARTESIAN_POINT('Ctrl Pts',(-7.04148501024886,2.44598411303715,42.9777690869761));
#81067=CARTESIAN_POINT('Ctrl Pts',(-7.33841841438875,-1.21493328511627,
43.1365328879076));
#81068=CARTESIAN_POINT('Ctrl Pts',(-5.3996688294086,-5.73219345581792,43.3482179558163));
#81069=CARTESIAN_POINT('Ctrl Pts',(0.745606841701872,-8.41618505310172,
43.6128242907021));
#81070=CARTESIAN_POINT('Ctrl Pts',(7.49310562293818,-3.91757723373606,43.9303518925652));
#81071=CARTESIAN_POINT('Ctrl Pts',(7.35925603732857,2.80244714954233,44.1949582274511));
#81072=CARTESIAN_POINT('Ctrl Pts',(3.93562979912596,6.30303669052284,44.4066432953597));
#81073=CARTESIAN_POINT('Ctrl Pts',(-0.736433107028406,7.84671735272832,
44.6183283632685));
#81074=CARTESIAN_POINT('Ctrl Pts',(-5.57430676013242,5.56861301361288,44.8300134311771));
#81075=CARTESIAN_POINT('Ctrl Pts',(-7.37350677123859,0.979684278604959,
45.0416984990858));
#81076=CARTESIAN_POINT('Ctrl Pts',(-6.96240639730474,-2.66275169506281,
45.2004623000174));
#81077=CARTESIAN_POINT('Ctrl Pts',(-4.83224855106344,-5.65489360224126,
45.3592261009488));
#81078=CARTESIAN_POINT('Ctrl Pts',(-0.440169850607679,-7.86261507291464,
45.5709111688576));
#81079=CARTESIAN_POINT('Ctrl Pts',(5.98981137818155,-5.95904858716997,45.8355175037433));
#81080=CARTESIAN_POINT('Ctrl Pts',(8.2555267585719,1.82765456180822,46.1530451056065));
#81081=CARTESIAN_POINT('Ctrl Pts',(3.82595871025544,6.88290631901628,46.4176514404922));
#81082=CARTESIAN_POINT('Ctrl Pts',(-1.04753302609511,7.35663836253256,46.629336508401));
#81083=CARTESIAN_POINT('Ctrl Pts',(-5.61610075779896,5.52926027719673,46.8410215763096));
#81084=CARTESIAN_POINT('Ctrl Pts',(-7.85060375198737,0.671094241308602,
47.0527066442183));
#81085=CARTESIAN_POINT('Ctrl Pts',(-6.27225339138328,-3.998402279102,47.264391712127));
#81086=CARTESIAN_POINT('Ctrl Pts',(-3.61228478006291,-6.52048679919805,
47.4231555130585));
#81087=CARTESIAN_POINT('Ctrl Pts',(-0.0558158050509224,-7.43810004690919,
47.5819193139901));
#81088=CARTESIAN_POINT('Ctrl Pts',(4.72612752925907,-6.29906214125468,47.7936043818987));
#81089=CARTESIAN_POINT('Ctrl Pts',(8.41991264524431,-0.702261672669268,
48.0582107167846));
#81090=CARTESIAN_POINT('Ctrl Pts',(5.1393775394395,6.71422681817487,48.3757383186477));
#81091=CARTESIAN_POINT('Ctrl Pts',(-1.50483143176698,7.72967281396177,48.6403446535335));
#81092=CARTESIAN_POINT('Ctrl Pts',(-5.53854911622968,4.95398093708056,48.8520297214422));
#81093=CARTESIAN_POINT('Ctrl Pts',(-7.85723999656229,0.61407375058509,49.0637147893509));
#81094=CARTESIAN_POINT('Ctrl Pts',(-6.43856929390096,-4.54171467609673,
49.2753998572596));
#81095=CARTESIAN_POINT('Ctrl Pts',(-2.22420124594441,-7.09797944550326,
49.4870849251683));
#81096=CARTESIAN_POINT('Ctrl Pts',(1.43494243330327,-7.31479935773328,49.6458487260998));
#81097=CARTESIAN_POINT('Ctrl Pts',(4.74684004375429,-5.72677547236965,49.8046125270314));
#81098=CARTESIAN_POINT('Ctrl Pts',(7.67201927494928,-1.77611529102583,50.01629759494));
#81099=CARTESIAN_POINT('Ctrl Pts',(6.89421260118454,4.88445831388825,50.2809039298258));
#81100=CARTESIAN_POINT('Ctrl Pts',(-0.391328369939513,8.4463545607366,50.598431531689));
#81101=CARTESIAN_POINT('Ctrl Pts',(-6.12862918543473,4.94492302835666,50.8630378665747));
#81102=CARTESIAN_POINT('Ctrl Pts',(-7.42747171931677,0.223868927257572,
51.0747229344835));
#81103=CARTESIAN_POINT('Ctrl Pts',(-6.40692997809917,-4.58961383892871,
51.2864080023921));
#81104=CARTESIAN_POINT('Ctrl Pts',(-2.00159836346711,-7.62075788506456,
51.4980930703008));
#81105=CARTESIAN_POINT('Ctrl Pts',(2.86881402151197,-6.86281935513654,51.7097781382095));
#81106=CARTESIAN_POINT('Ctrl Pts',(5.80801215856054,-4.6725094110997,51.868541939141));
#81107=CARTESIAN_POINT('Ctrl Pts',(7.31935920825085,-1.32492584412404,52.0273057400726));
#81108=CARTESIAN_POINT('Ctrl Pts',(7.01348123788996,3.58127717557574,52.2389908079812));
#81109=CARTESIAN_POINT('Ctrl Pts',(2.12950802153738,8.17638648768663,52.5035971428671));
#81110=CARTESIAN_POINT('Ctrl Pts',(-5.73818233873579,6.21025818353877,52.8211247447302));
#81111=CARTESIAN_POINT('Ctrl Pts',(-7.873104980814,-0.163025800264569,53.0857310796159));
#81112=CARTESIAN_POINT('Ctrl Pts',(-5.82685665086243,-4.61142006388278,
53.2974161475247));
#81113=CARTESIAN_POINT('Ctrl Pts',(-1.94654811296497,-7.63703197482712,
53.5091012154332));
#81114=CARTESIAN_POINT('Ctrl Pts',(3.37575351505398,-7.11945468085971,53.7207862833422));
#81115=CARTESIAN_POINT('Ctrl Pts',(6.6140174110158,-3.40340374805446,53.9324713512506));
#81116=CARTESIAN_POINT('Ctrl Pts',(7.45239061759393,0.164995574769106,54.0912351521824));
#81117=CARTESIAN_POINT('Ctrl Pts',(6.45313357826351,3.6993938248483,54.2499989531137));
#81118=CARTESIAN_POINT('Ctrl Pts',(3.05990447673085,7.25613189013641,54.4616840210225));
#81119=CARTESIAN_POINT('Ctrl Pts',(-3.63567139626818,7.62692558076465,54.7262903559084));
#81120=CARTESIAN_POINT('Ctrl Pts',(-8.38915211246843,1.05648934208145,55.0438179577714));
#81121=CARTESIAN_POINT('Ctrl Pts',(-5.91867795214696,-5.19438269905205,
55.3084242926573));
#81122=CARTESIAN_POINT('Ctrl Pts',(-1.48869683481292,-7.280194659444,55.5201093605659));
#81123=CARTESIAN_POINT('Ctrl Pts',(3.42835112574471,-7.09645801521317,55.7317944284747));
#81124=CARTESIAN_POINT('Ctrl Pts',(7.16712601997843,-3.27332457050499,55.9434794963832));
#81125=CARTESIAN_POINT('Ctrl Pts',(7.25185581801874,1.65498168861816,56.155164564292));
#81126=CARTESIAN_POINT('Ctrl Pts',(5.59552486519911,4.92498383619882,56.3139283652234));
#81127=CARTESIAN_POINT('Ctrl Pts',(2.55512762082478,6.98568153459991,56.4726921661551));
#81128=CARTESIAN_POINT('Ctrl Pts',(-2.33125843887759,7.52194960659085,56.6843772340637));
#81129=CARTESIAN_POINT('Ctrl Pts',(-7.69276380499366,3.49421510251371,56.9489835689495));
#81130=CARTESIAN_POINT('Ctrl Pts',(-7.09876190604784,-4.59362446876616,
57.2665111708127));
#81131=CARTESIAN_POINT('Ctrl Pts',(-1.18358469634226,-7.78535672122115,
57.5311175056984));
#81132=CARTESIAN_POINT('Ctrl Pts',(3.54889838194794,-6.52860316985953,57.7428025736072));
#81133=CARTESIAN_POINT('Ctrl Pts',(7.19249959080346,-3.22191666131488,57.9544876415158));
#81134=CARTESIAN_POINT('Ctrl Pts',(7.59139710526208,2.11077452177849,58.1661727094246));
#81135=CARTESIAN_POINT('Ctrl Pts',(4.48251286310495,5.93569352038678,58.3778577773332));
#81136=CARTESIAN_POINT('Ctrl Pts',(1.11011110261031,7.37142872296306,58.5366215782647));
#81137=CARTESIAN_POINT('Ctrl Pts',(-2.54388752560662,6.98946603881242,58.6953853791963));
#81138=CARTESIAN_POINT('Ctrl Pts',(-6.62592548180662,4.2549773013165,58.9070704471049));
#81139=CARTESIAN_POINT('Ctrl Pts',(-8.13823691959708,-2.28247792862617,
59.1716767819908));
#81140=CARTESIAN_POINT('Ctrl Pts',(-2.46879882883055,-8.08148114908733,
59.4892043838539));
#81141=CARTESIAN_POINT('Ctrl Pts',(4.10006641658602,-6.72554991167464,59.7538107187397));
#81142=CARTESIAN_POINT('Ctrl Pts',(6.92927008283139,-2.70048724128809,59.9654957866484));
#81143=CARTESIAN_POINT('Ctrl Pts',(7.39449643883256,0.930216882217807,60.1242595875799));
#81144=CARTESIAN_POINT('Ctrl Pts',(6.03812441791351,4.36307444356796,60.2830880368553));
#81145=CARTESIAN_POINT('Ctrl Pts',(4.15875444436768,5.93146837941342,60.3889952191537));
#81146=CARTESIAN_POINT('Ctrl Pts',(3.08588518346614,6.44513774759855,60.4419811344748));
#81147=CARTESIAN_POINT('Ctrl Pts',(3.92310195780859,-5.50507296558183,-59.9960106818844));
#81148=CARTESIAN_POINT('Ctrl Pts',(4.83892195707862,-4.85243511881996,-59.94305719595));
#81149=CARTESIAN_POINT('Ctrl Pts',(6.33530927587413,-3.08625648992924,-59.8371824430386));
#81150=CARTESIAN_POINT('Ctrl Pts',(7.04247861132623,0.332438649457811,-59.6783864231499));
#81151=CARTESIAN_POINT('Ctrl Pts',(6.0199900274931,3.64075869155507,-59.5196226222184));
#81152=CARTESIAN_POINT('Ctrl Pts',(2.73033299632717,6.93317850862972,-59.3079375543098));
#81153=CARTESIAN_POINT('Ctrl Pts',(-3.61171668904582,7.1314192372823,-59.0433312194238));
#81154=CARTESIAN_POINT('Ctrl Pts',(-7.95497482546268,0.807220027998837,
-58.7258036175609));
#81155=CARTESIAN_POINT('Ctrl Pts',(-5.48513671916016,-5.04032525277668,
-58.461197282675));
#81156=CARTESIAN_POINT('Ctrl Pts',(-1.23718245068589,-6.92673261012629,
-58.2495122147664));
#81157=CARTESIAN_POINT('Ctrl Pts',(2.23026237868773,-6.69003737759096,-58.0907484138348));
#81158=CARTESIAN_POINT('Ctrl Pts',(5.14043011189061,-4.80494102070203,-57.9319846129032));
#81159=CARTESIAN_POINT('Ctrl Pts',(7.41747518458126,-0.735891892932647,
-57.7202995449947));
#81160=CARTESIAN_POINT('Ctrl Pts',(6.18074115598698,4.16942168380601,-57.5086144770858));
#81161=CARTESIAN_POINT('Ctrl Pts',(2.24859475984408,6.66022634333414,-57.2969294091773));
#81162=CARTESIAN_POINT('Ctrl Pts',(-2.36587839035156,7.06389668382096,-57.0852443412685));
#81163=CARTESIAN_POINT('Ctrl Pts',(-7.36106375900914,3.12978898030585,-56.8206380063827));
#81164=CARTESIAN_POINT('Ctrl Pts',(-6.60281545143133,-4.50434425269732,
-56.5031104045197));
#81165=CARTESIAN_POINT('Ctrl Pts',(-0.95264512747938,-7.38851342469737,
-56.2385040696336));
#81166=CARTESIAN_POINT('Ctrl Pts',(3.51443494488682,-6.09614235035376,-56.0268190017251));
#81167=CARTESIAN_POINT('Ctrl Pts',(6.01380851126865,-3.68243850274338,-55.8680552007936));
#81168=CARTESIAN_POINT('Ctrl Pts',(7.02709623719541,-0.366171308569067,
-55.709291399862));
#81169=CARTESIAN_POINT('Ctrl Pts',(6.14875484919133,4.21321773474829,-55.4976063319533));
#81170=CARTESIAN_POINT('Ctrl Pts',(2.04413954277891,7.16990856068301,-55.2859212640447));
#81171=CARTESIAN_POINT('Ctrl Pts',(-2.56830228731816,6.54360132081494,-55.0742361961359));
#81172=CARTESIAN_POINT('Ctrl Pts',(-6.35868061211583,3.88109994176148,-54.8625511282274));
#81173=CARTESIAN_POINT('Ctrl Pts',(-7.64724290279666,-2.34536274202442,
-54.5979447933414));
#81174=CARTESIAN_POINT('Ctrl Pts',(-2.15131782745559,-7.69792650446685,
-54.2804171914784));
#81175=CARTESIAN_POINT('Ctrl Pts',(4.02874913907503,-6.26632429205159,-54.0158108565925));
#81176=CARTESIAN_POINT('Ctrl Pts',(6.61429988284118,-2.40109622158015,-53.8041257886839));
#81177=CARTESIAN_POINT('Ctrl Pts',(6.97231607962482,1.05500774201836,-53.6453619877523));
#81178=CARTESIAN_POINT('Ctrl Pts',(5.61216422778529,4.244735701355,-53.4865981868208));
#81179=CARTESIAN_POINT('Ctrl Pts',(1.99138902220475,7.18280986143957,-53.2749131189121));
#81180=CARTESIAN_POINT('Ctrl Pts',(-3.05289432493803,6.80190640246115,-53.0632280510034));
#81181=CARTESIAN_POINT('Ctrl Pts',(-6.17854720639058,3.35267804890413,-52.8515429830947));
#81182=CARTESIAN_POINT('Ctrl Pts',(-7.36409817019778,-1.12508365977983,
-52.639857915186));
#81183=CARTESIAN_POINT('Ctrl Pts',(-4.34062130214816,-6.71863508772395,
-52.3752515803003));
#81184=CARTESIAN_POINT('Ctrl Pts',(3.31089474128444,-7.27490322676852,-52.057723978437));
#81185=CARTESIAN_POINT('Ctrl Pts',(7.11737972380877,-2.20012397569399,-51.7931176435514));
#81186=CARTESIAN_POINT('Ctrl Pts',(6.6066660368453,2.42202186987603,-51.5814325756425));
#81187=CARTESIAN_POINT('Ctrl Pts',(4.65512571783568,5.29679500997594,-51.422668774711));
#81188=CARTESIAN_POINT('Ctrl Pts',(1.56055286681731,6.86140242581805,-51.2639049737795));
#81189=CARTESIAN_POINT('Ctrl Pts',(-3.10156094261667,6.77780993141143,-51.052219905871));
#81190=CARTESIAN_POINT('Ctrl Pts',(-6.71563277804662,3.2382666431682,-50.8405348379621));
#81191=CARTESIAN_POINT('Ctrl Pts',(-6.88601787296009,-1.4133837188701,-50.6288497700535));
#81192=CARTESIAN_POINT('Ctrl Pts',(-4.90975194539534,-5.60268604645359,
-50.4171647021448));
#81193=CARTESIAN_POINT('Ctrl Pts',(1.0052893485505,-7.93539186533052,-50.152558367259));
#81194=CARTESIAN_POINT('Ctrl Pts',(7.2175992617459,-3.43402123524581,-49.8350307653958));
#81195=CARTESIAN_POINT('Ctrl Pts',(6.86215851718836,2.89972759513651,-49.5704244305101));
#81196=CARTESIAN_POINT('Ctrl Pts',(3.49512134281254,6.10723774382978,-49.3587393626013));
#81197=CARTESIAN_POINT('Ctrl Pts',(0.150887440188818,7.0500684966136,-49.1999755616699));
#81198=CARTESIAN_POINT('Ctrl Pts',(-3.22422964974452,6.25447932803763,-49.0412117607383));
#81199=CARTESIAN_POINT('Ctrl Pts',(-6.73735103342042,3.18849318638109,-48.8295266928297));
#81200=CARTESIAN_POINT('Ctrl Pts',(-7.2232661766579,-1.8467593787403,-48.6178416249209));
#81201=CARTESIAN_POINT('Ctrl Pts',(-4.35833401012841,-5.51541660617352,
-48.4061565570123));
#81202=CARTESIAN_POINT('Ctrl Pts',(-0.148730580325022,-7.44806245374694,
-48.1944714891035));
#81203=CARTESIAN_POINT('Ctrl Pts',(5.87889997784911,-5.4239824650442,-47.9298651542178));
#81204=CARTESIAN_POINT('Ctrl Pts',(7.73336734070007,2.02021546402088,-47.6123375523546));
#81205=CARTESIAN_POINT('Ctrl Pts',(3.38299226469952,6.63724362804317,-47.3477312174689));
#81206=CARTESIAN_POINT('Ctrl Pts',(-1.25848380636106,6.9231816796737,-47.1360461495601));
#81207=CARTESIAN_POINT('Ctrl Pts',(-4.42424002109247,5.49111400922566,-46.9772823486285));
#81208=CARTESIAN_POINT('Ctrl Pts',(-6.49422069361746,2.70910798635499,-46.8185185476971));
#81209=CARTESIAN_POINT('Ctrl Pts',(-7.20783250708978,-1.89882550458687,
-46.6068334797883));
#81210=CARTESIAN_POINT('Ctrl Pts',(-4.33730073213373,-6.06415013178661,
-46.3951484118797));
#81211=CARTESIAN_POINT('Ctrl Pts',(0.216960572431575,-7.02622400678393,
-46.183463343971));
#81212=CARTESIAN_POINT('Ctrl Pts',(4.68216664325364,-5.79422735360303,-45.9717782760624));
#81213=CARTESIAN_POINT('Ctrl Pts',(7.99051517795909,-0.364304709640845,
-45.7071719411764));
#81214=CARTESIAN_POINT('Ctrl Pts',(4.61588339500148,6.52532462265482,-45.3896443393135));
#81215=CARTESIAN_POINT('Ctrl Pts',(-1.68555451940014,7.25648300508906,-45.1250380044276));
#81216=CARTESIAN_POINT('Ctrl Pts',(-5.4208343783223,4.48651097217447,-44.9133529365189));
#81217=CARTESIAN_POINT('Ctrl Pts',(-6.92079312970003,1.35235175987873,-44.7545891355874));
#81218=CARTESIAN_POINT('Ctrl Pts',(-6.71312940244499,-2.1090429405705,-44.5958253346557));
#81219=CARTESIAN_POINT('Ctrl Pts',(-4.29196610718577,-6.09404747945881,
-44.3841402667472));
#81220=CARTESIAN_POINT('Ctrl Pts',(0.586393682488183,-7.43251215343463,
-44.1724551988384));
#81221=CARTESIAN_POINT('Ctrl Pts',(4.6903238223225,-5.23600593250722,-43.9607701309298));
#81222=CARTESIAN_POINT('Ctrl Pts',(7.3133117165843,-1.41817729375046,-43.7490850630211));
#81223=CARTESIAN_POINT('Ctrl Pts',(6.34806644067571,4.86652886515926,-43.4844787281352));
#81224=CARTESIAN_POINT('Ctrl Pts',(-0.67021183626058,7.9647383536317,-43.1669511262723));
#81225=CARTESIAN_POINT('Ctrl Pts',(-5.96220249661876,4.46651777454531,-42.9023447913863));
#81226=CARTESIAN_POINT('Ctrl Pts',(-7.03639561354893,-0.0579899152633749,
-42.6906597234777));
#81227=CARTESIAN_POINT('Ctrl Pts',(-6.16585377158498,-3.42176563983885,
-42.5318959225461));
#81228=CARTESIAN_POINT('Ctrl Pts',(-3.77810917984525,-5.93633384542265,
-42.3731321216146));
#81229=CARTESIAN_POINT('Ctrl Pts',(0.6403303757177,-7.42619450035234,-42.1614470537058));
#81230=CARTESIAN_POINT('Ctrl Pts',(5.23459154557155,-5.30896843208227,-41.9497619857972));
#81231=CARTESIAN_POINT('Ctrl Pts',(6.96010255683114,-0.985833698901345,
-41.7380769178885));
#81232=CARTESIAN_POINT('Ctrl Pts',(6.50855320088531,3.62415374007287,-41.5263918499799));
#81233=CARTESIAN_POINT('Ctrl Pts',(1.72320082959013,7.81099415129477,-41.2617855150938));
#81234=CARTESIAN_POINT('Ctrl Pts',(-5.64143148955485,5.66219848609485,-40.9442579132311));
#81235=CARTESIAN_POINT('Ctrl Pts',(-7.43771827128143,-0.421884531670146,
-40.679651578345));
#81236=CARTESIAN_POINT('Ctrl Pts',(-5.34615260039369,-4.57524627030576,
-40.4679665104363));
#81237=CARTESIAN_POINT('Ctrl Pts',(-2.51410378591528,-6.58828619446641,
-40.3092027095049));
#81238=CARTESIAN_POINT('Ctrl Pts',(0.931923430280503,-6.97464602823941,
-40.1504389085732));
#81239=CARTESIAN_POINT('Ctrl Pts',(5.2717900392219,-5.26940390646711,-39.9387538406647));
#81240=CARTESIAN_POINT('Ctrl Pts',(7.42349974953265,-0.691191674214921,
-39.7270687727558));
#81241=CARTESIAN_POINT('Ctrl Pts',(5.95992066586817,3.72749800000675,-39.5153837048473));
#81242=CARTESIAN_POINT('Ctrl Pts',(2.64597872315084,6.96380296225215,-39.3036986369385));
#81243=CARTESIAN_POINT('Ctrl Pts',(-3.71125038982958,7.08573717228143,-39.0390923020528));
#81244=CARTESIAN_POINT('Ctrl Pts',(-7.96222197294639,0.699472802048286,
-38.7215647001897));
#81245=CARTESIAN_POINT('Ctrl Pts',(-5.41888239065558,-5.11207915404871,
-38.4569583653038));
#81246=CARTESIAN_POINT('Ctrl Pts',(-1.14420687045995,-6.94298327077308,
-38.2452732973951));
#81247=CARTESIAN_POINT('Ctrl Pts',(2.31880988537035,-6.65953103018969,-38.0865094964637));
#81248=CARTESIAN_POINT('Ctrl Pts',(5.20412442828714,-4.73616484447559,-37.9277456955321));
#81249=CARTESIAN_POINT('Ctrl Pts',(7.42648363308103,-0.636968283911715,
-37.7160606276233));
#81250=CARTESIAN_POINT('Ctrl Pts',(6.12473637308791,4.2513173043175,-37.5043755597148));
#81251=CARTESIAN_POINT('Ctrl Pts',(2.15967861067737,6.68959520315537,-37.2926904918059));
#81252=CARTESIAN_POINT('Ctrl Pts',(-2.45971626464659,7.03175305296422,-37.0810054238974));
#81253=CARTESIAN_POINT('Ctrl Pts',(-7.40210048456495,3.03149454016741,-36.8163990890115));
#81254=CARTESIAN_POINT('Ctrl Pts',(-6.54224109123133,-4.59187570078724,
-36.4988714871485));
#81255=CARTESIAN_POINT('Ctrl Pts',(-0.854174246392727,-7.40054227728048,
-36.2342651522626));
#81256=CARTESIAN_POINT('Ctrl Pts',(3.59530441734421,-6.04880254325333,-36.022580084354));
#81257=CARTESIAN_POINT('Ctrl Pts',(6.06231187612364,-3.60202825407587,-35.8638162834224));
#81258=CARTESIAN_POINT('Ctrl Pts',(7.03134967606554,-0.272562345225122,
-35.7050524824909));
#81259=CARTESIAN_POINT('Ctrl Pts',(6.09210377326671,4.29472459686056,-35.4933674145823));
#81260=CARTESIAN_POINT('Ctrl Pts',(1.94847993991589,7.19649361741958,-35.2816823466735));
#81261=CARTESIAN_POINT('Ctrl Pts',(-2.65521286424894,6.50882019486048,-35.0699972787649));
#81262=CARTESIAN_POINT('Ctrl Pts',(-6.40979964046684,3.79608003992402,-34.8583122108561));
#81263=CARTESIAN_POINT('Ctrl Pts',(-7.6153326946967,-2.4469897179483,-34.5937058759703));
#81264=CARTESIAN_POINT('Ctrl Pts',(-2.04861717107107,-7.72589209306399,
-34.2761782741073));
#81265=CARTESIAN_POINT('Ctrl Pts',(4.11183777668357,-6.21211958507354,-34.0115719392213));
#81266=CARTESIAN_POINT('Ctrl Pts',(6.64568773823915,-2.31280361173633,-33.7998868713127));
#81267=CARTESIAN_POINT('Ctrl Pts',(6.9576487755742,1.14776144834246,-33.6411230703812));
#81268=CARTESIAN_POINT('Ctrl Pts',(5.55514133261181,4.31909403392073,-33.4823592694497));
#81269=CARTESIAN_POINT('Ctrl Pts',(1.89556214181054,7.20869141478983,-33.2706742015409));
#81270=CARTESIAN_POINT('Ctrl Pts',(-3.14320160819109,6.76064923746827,-33.0589891336322));
#81271=CARTESIAN_POINT('Ctrl Pts',(-6.22264549105552,3.27010378675402,-32.8473040657235));
#81272=CARTESIAN_POINT('Ctrl Pts',(-7.34846295884596,-1.22304834038044,
-32.6356189978149));
#81273=CARTESIAN_POINT('Ctrl Pts',(-4.25076732811253,-6.77584148670202,
-32.3710126629291));
#81274=CARTESIAN_POINT('Ctrl Pts',(3.40747783789418,-7.2301684442021,-32.053485061066));
#81275=CARTESIAN_POINT('Ctrl Pts',(7.14604670946127,-2.1051498918638,-31.7888787261801));
#81276=CARTESIAN_POINT('Ctrl Pts',(6.57382723358979,2.5097851628289,-31.5771936582715));
#81277=CARTESIAN_POINT('Ctrl Pts',(4.5841778728095,5.35831559886071,-31.4184298573399));
#81278=CARTESIAN_POINT('Ctrl Pts',(1.46904422986937,6.88157522300156,-31.2596660564085));
#81279=CARTESIAN_POINT('Ctrl Pts',(-3.19154302893877,6.73590683141938,-31.0479809884997));
#81280=CARTESIAN_POINT('Ctrl Pts',(-6.75815987344691,3.14855039450655,-30.8362959205911));
#81281=CARTESIAN_POINT('Ctrl Pts',(-6.86658588827577,-1.50495645200409,
-30.6246108526823));
#81282=CARTESIAN_POINT('Ctrl Pts',(-4.83470810709648,-5.6675702571397,-30.4129257847737));
#81283=CARTESIAN_POINT('Ctrl Pts',(1.11087231682787,-7.92130124577817,-30.1483194498878));
#81284=CARTESIAN_POINT('Ctrl Pts',(7.26268862552777,-3.33760316333525,-29.8307918480246));
#81285=CARTESIAN_POINT('Ctrl Pts',(6.82293566355775,2.99085081071726,-29.5661855131389));
#81286=CARTESIAN_POINT('Ctrl Pts',(3.41348404682912,6.15323920570995,-29.3545004452302));
#81287=CARTESIAN_POINT('Ctrl Pts',(0.0569914145846386,7.05145267340099,
-29.1957366442987));
#81288=CARTESIAN_POINT('Ctrl Pts',(-3.30723189674889,6.21098910643613,-29.036972843367));
#81289=CARTESIAN_POINT('Ctrl Pts',(-6.77921339195171,3.09849213868819,-28.8252877754586));
#81290=CARTESIAN_POINT('Ctrl Pts',(-7.19803321626531,-1.94278467138195,
-28.6136027075498));
#81291=CARTESIAN_POINT('Ctrl Pts',(-4.28450119423596,-5.57296556602382,
-28.4019176396412));
#81292=CARTESIAN_POINT('Ctrl Pts',(-0.049534836327076,-7.44938261874288,
-28.1902325717324));
#81293=CARTESIAN_POINT('Ctrl Pts',(5.95060747741717,-5.3452148114335,-27.9256262368466));
#81294=CARTESIAN_POINT('Ctrl Pts',(7.70577931196721,2.12301816820624,-27.6080986349835));
#81295=CARTESIAN_POINT('Ctrl Pts',(3.29430705698815,6.68170492129775,-27.3434923000977));
#81296=CARTESIAN_POINT('Ctrl Pts',(-1.35056516835081,6.90580913338042,-27.131807232189));
#81297=CARTESIAN_POINT('Ctrl Pts',(-4.4969704654332,5.43171146689254,-26.9730434312574));
#81298=CARTESIAN_POINT('Ctrl Pts',(-6.52972084949016,2.62238710469586,-26.814279630326));
#81299=CARTESIAN_POINT('Ctrl Pts',(-7.18190757360148,-1.99464065720506,
-26.6025945624171));
#81300=CARTESIAN_POINT('Ctrl Pts',(-4.25616253938917,-6.12137034495673,
-26.3909094945086));
#81301=CARTESIAN_POINT('Ctrl Pts',(0.310506454680001,-7.02271182842488,
-26.1792244265999));
#81302=CARTESIAN_POINT('Ctrl Pts',(4.75891064387549,-5.73136323958333,-25.9675393586912));
#81303=CARTESIAN_POINT('Ctrl Pts',(7.99465794946795,-0.257866247636377,
-25.7029330238053));
#81304=CARTESIAN_POINT('Ctrl Pts',(4.5285792436425,6.58621370601699,-25.3854054219423));
#81305=CARTESIAN_POINT('Ctrl Pts',(-1.78203643978692,7.23339379325415,-25.1207990870564));
#81306=CARTESIAN_POINT('Ctrl Pts',(-5.48009860066973,4.41392630065121,-24.9091140191477));
#81307=CARTESIAN_POINT('Ctrl Pts',(-6.93818813862285,1.26007070421613,-24.7503502182163));
#81308=CARTESIAN_POINT('Ctrl Pts',(-6.68444896123671,-2.19825171073812,
-24.5915864172847));
#81309=CARTESIAN_POINT('Ctrl Pts',(-4.21043380446389,-6.15066134048668,
-24.379901349376));
#81310=CARTESIAN_POINT('Ctrl Pts',(0.685317167062233,-7.42404437233138,
-24.1682162814673));
#81311=CARTESIAN_POINT('Ctrl Pts',(4.75963351168402,-5.17308269003613,-23.9565312135587));
#81312=CARTESIAN_POINT('Ctrl Pts',(7.33154849070669,-1.32066340482921,-23.74484614565));
#81313=CARTESIAN_POINT('Ctrl Pts',(6.28269814790344,4.9506317488773,-23.4802398107641));
#81314=CARTESIAN_POINT('Ctrl Pts',(-0.776215309838923,7.955107211097,-23.162712208901));
#81315=CARTESIAN_POINT('Ctrl Pts',(-6.02115247566208,4.38672571582093,-22.8981058740152));
#81316=CARTESIAN_POINT('Ctrl Pts',(-7.03499947526807,-0.151685344119284,
-22.6864208061065));
#81317=CARTESIAN_POINT('Ctrl Pts',(-6.11974090886601,-3.50357018409825,
-22.527657005175));
#81318=CARTESIAN_POINT('Ctrl Pts',(-3.69872264321837,-5.98611888519477,
-22.3688932042435));
#81319=CARTESIAN_POINT('Ctrl Pts',(0.739164948369388,-7.41700902832348,
-22.1572081363348));
#81320=CARTESIAN_POINT('Ctrl Pts',(5.30482458446264,-5.23879094733663,-21.9455230684261));
#81321=CARTESIAN_POINT('Ctrl Pts',(6.97261332117276,-0.893061675866078,
-21.7338380005174));
#81322=CARTESIAN_POINT('Ctrl Pts',(6.45971483836194,3.71050391557333,-21.5221529326087));
#81323=CARTESIAN_POINT('Ctrl Pts',(1.61903247740699,7.83324865989599,-21.2575465977228));
#81324=CARTESIAN_POINT('Ctrl Pts',(-5.71633226276247,5.58657197295241,-20.9400189958598));
#81325=CARTESIAN_POINT('Ctrl Pts',(-7.4314407242151,-0.520891930724535,
-20.6754126609739));
#81326=CARTESIAN_POINT('Ctrl Pts',(-5.28475202819951,-4.64603293801106,
-20.4637275930653));
#81327=CARTESIAN_POINT('Ctrl Pts',(-2.42614756643601,-6.62118122485914,
-20.3049637921337));
#81328=CARTESIAN_POINT('Ctrl Pts',(1.02471907613325,-6.96161757884978,-20.1461999912023));
#81329=CARTESIAN_POINT('Ctrl Pts',(5.34149291644613,-5.19873457397912,-19.9345149232935));
#81330=CARTESIAN_POINT('Ctrl Pts',(7.43204580714285,-0.592274921253531,
-19.7228298553849));
#81331=CARTESIAN_POINT('Ctrl Pts',(5.90975476036394,3.80653311503425,-19.5111447874762));
#81332=CARTESIAN_POINT('Ctrl Pts',(2.55301021957051,6.99842081609893,-19.2994597195675));
#81333=CARTESIAN_POINT('Ctrl Pts',(-3.80527894640322,7.03568780367081,-19.0348533846816));
#81334=CARTESIAN_POINT('Ctrl Pts',(-7.97083053855895,0.593381389034304,
-18.7173257828186));
#81335=CARTESIAN_POINT('Ctrl Pts',(-5.35032660329299,-5.1837867316385,-18.4527194479327));
#81336=CARTESIAN_POINT('Ctrl Pts',(-1.05164877455481,-6.95760453860522,
-18.241034380024));
#81337=CARTESIAN_POINT('Ctrl Pts',(2.40728630981526,-6.62806196780977,-18.0822705790925));
#81338=CARTESIAN_POINT('Ctrl Pts',(5.26673239643959,-4.66644386695429,-17.923506778161));
#81339=CARTESIAN_POINT('Ctrl Pts',(7.43430735718676,-0.538016603841439,
-17.7118217102523));
#81340=CARTESIAN_POINT('Ctrl Pts',(6.06758038330864,4.33250075059474,-17.5001366423436));
#81341=CARTESIAN_POINT('Ctrl Pts',(2.07040473052971,6.71776152712322,-17.2884515744349));
#81342=CARTESIAN_POINT('Ctrl Pts',(-2.55313691120353,6.99837459793973,-17.0767665065262));
#81343=CARTESIAN_POINT('Ctrl Pts',(-7.44181321864497,2.932655238766,-16.8121601716404));
#81344=CARTESIAN_POINT('Ctrl Pts',(-6.48051301594269,-4.678588675816,-16.4946325697774));
#81345=CARTESIAN_POINT('Ctrl Pts',(-0.755548756394746,-7.41126073740003,
-16.2300262348915));
#81346=CARTESIAN_POINT('Ctrl Pts',(3.67553485456433,-6.00038912017591,-16.0183411669828));
#81347=CARTESIAN_POINT('Ctrl Pts',(6.10974095364035,-3.52097973665857,-15.8595773660513));
#81348=CARTESIAN_POINT('Ctrl Pts',(7.03435580357583,-0.17890480105438,-15.7008135651198));
#81349=CARTESIAN_POINT('Ctrl Pts',(6.03437264126526,4.37546964033347,-15.4891284972111));
#81350=CARTESIAN_POINT('Ctrl Pts',(1.85247464443622,7.22180255570149,-15.2774434293024));
#81351=CARTESIAN_POINT('Ctrl Pts',(-2.74165251049031,6.47288476610073,-15.0657583613937));
#81352=CARTESIAN_POINT('Ctrl Pts',(-6.4597820083646,3.71038697508052,-14.854073293485));
#81353=CARTESIAN_POINT('Ctrl Pts',(-7.58207196787757,-2.54818276514574,
-14.589466958599));
#81354=CARTESIAN_POINT('Ctrl Pts',(-1.94555323095193,-7.75248757321215,
-14.2719393567361));
#81355=CARTESIAN_POINT('Ctrl Pts',(4.19419723412819,-6.15681323431598,-14.0073330218502));
#81356=CARTESIAN_POINT('Ctrl Pts',(6.67589705341909,-2.22410085040965,-13.7956479539416));
#81357=CARTESIAN_POINT('Ctrl Pts',(6.94174761381799,1.24031161108916,-13.63688415301));
#81358=CARTESIAN_POINT('Ctrl Pts',(5.49713329566522,4.39268642505134,-13.4781203520784));
#81359=CARTESIAN_POINT('Ctrl Pts',(1.79939910583755,7.23329458857038,-13.2664352841698));
#81360=CARTESIAN_POINT('Ctrl Pts',(-3.23295148088592,6.71819314876056,-13.054750216261));
#81361=CARTESIAN_POINT('Ctrl Pts',(-6.265640260461,3.18694960895007,-12.8430651483524));
#81362=CARTESIAN_POINT('Ctrl Pts',(-7.33152458160375,-1.32079612725738,
-12.6313800804438));
#81363=CARTESIAN_POINT('Ctrl Pts',(-4.16015952896897,-6.83184626760507,
-12.3667737455578));
#81364=CARTESIAN_POINT('Ctrl Pts',(3.50345665718391,-7.18415147380051,-12.0492461436949));
#81365=CARTESIAN_POINT('Ctrl Pts',(7.17344642534743,-2.00980248374984,-11.784639808809));
#81366=CARTESIAN_POINT('Ctrl Pts',(6.53982263713274,2.59710337404747,-11.5729547409003));
#81367=CARTESIAN_POINT('Ctrl Pts',(4.51241707618843,5.41888595165771,-11.4141909399688));
#81368=CARTESIAN_POINT('Ctrl Pts',(1.37727507470006,6.90052765140112,-11.2554271390373));
#81369=CARTESIAN_POINT('Ctrl Pts',(-3.28095913154713,6.69280919526674,-11.0437420711286));
#81370=CARTESIAN_POINT('Ctrl Pts',(-6.79948848636568,3.05827578638617,-10.8320570032198));
#81371=CARTESIAN_POINT('Ctrl Pts',(-6.84593619299317,-1.59626229829667,
-10.6203719353112));
#81372=CARTESIAN_POINT('Ctrl Pts',(-4.75880688852233,-5.73144938895834,
-10.4086868674024));
#81373=CARTESIAN_POINT('Ctrl Pts',(1.21625828458495,-7.90580587390299,-10.1440805325167));
#81374=CARTESIAN_POINT('Ctrl Pts',(7.30649003441419,-3.24059320561566,-9.82655293065358));
#81375=CARTESIAN_POINT('Ctrl Pts',(6.78250284019818,3.08144363305912,-9.56194659576771));
#81376=CARTESIAN_POINT('Ctrl Pts',(3.33124140842834,6.19814946088065,-9.35026152785902));
#81377=CARTESIAN_POINT('Ctrl Pts',(-0.0369147177961642,7.05158635557704,
-9.19149772692751));
#81378=CARTESIAN_POINT('Ctrl Pts',(-3.38964764394158,6.16639743683966,-9.03273392599598));
#81379=CARTESIAN_POINT('Ctrl Pts',(-6.8198735343995,3.00794160879609,-8.82104885808732));
#81380=CARTESIAN_POINT('Ctrl Pts',(-7.17152376687591,-2.03846543334665,
-8.60936379017862));
#81381=CARTESIAN_POINT('Ctrl Pts',(-4.2099085709813,-5.62952622406857,-8.39767872226993));
#81382=CARTESIAN_POINT('Ctrl Pts',(0.0496696921086477,-7.44938172079558,
-8.18599365436123));
#81383=CARTESIAN_POINT('Ctrl Pts',(6.02125970469887,-5.26549924501289,-7.92138731947539));
#81384=CARTESIAN_POINT('Ctrl Pts',(7.6768247512655,2.22544437936245,-7.60385971761233));
#81385=CARTESIAN_POINT('Ctrl Pts',(3.20503764153763,6.72498129048212,-7.33925338272649));
#81386=CARTESIAN_POINT('Ctrl Pts',(-1.44240702302965,6.88721192069529,-7.12756831481779));
#81387=CARTESIAN_POINT('Ctrl Pts',(-4.56890342341336,5.37134567255369,-6.96880451388627));
#81388=CARTESIAN_POINT('Ctrl Pts',(-6.56406303393157,2.53520117263162,-6.81004071295475));
#81389=CARTESIAN_POINT('Ctrl Pts',(-7.15470901081791,-2.09010208308626,
-6.59835564504608));
#81390=CARTESIAN_POINT('Ctrl Pts',(-4.17426956481358,-6.17750500298273,
-6.38667057713737));
#81391=CARTESIAN_POINT('Ctrl Pts',(0.403997272147747,-7.01795425233056,
-6.17498550922869));
#81392=CARTESIAN_POINT('Ctrl Pts',(4.83481070605209,-5.66748273370333,-5.96330044131999));
#81393=CARTESIAN_POINT('Ctrl Pts',(7.99738295964715,-0.151382056073881,
-5.69869410643413));
#81394=CARTESIAN_POINT('Ctrl Pts',(4.44047200052455,6.64593479972095,-5.38116650457111));
#81395=CARTESIAN_POINT('Ctrl Pts',(-1.87820233645865,7.20902182139955,-5.11656016968524));
#81396=CARTESIAN_POINT('Ctrl Pts',(-5.53839098997102,4.34055887001719,-4.90487510177656));
#81397=CARTESIAN_POINT('Ctrl Pts',(-6.95435273940389,1.16756618871284,-4.74611130084502));
#81398=CARTESIAN_POINT('Ctrl Pts',(-6.65458310877973,-2.28707064478078,
-4.58734749991352));
#81399=CARTESIAN_POINT('Ctrl Pts',(-4.1281548306516,-6.2061844548941,-4.37566243200482));
#81400=CARTESIAN_POINT('Ctrl Pts',(0.784119120890008,-7.41426001610747,
-4.16397736409614));
#81401=CARTESIAN_POINT('Ctrl Pts',(4.82809913155386,-5.10924206699896,-3.95229229618746));
#81402=CARTESIAN_POINT('Ctrl Pts',(7.34848510506071,-1.22291529595122,-3.74060722827875));
#81403=CARTESIAN_POINT('Ctrl Pts',(6.21621567622543,5.0338566618374,-3.47600089339291));
#81404=CARTESIAN_POINT('Ctrl Pts',(-0.88208110558023,7.94406537887752,-3.15847329152986));
#81405=CARTESIAN_POINT('Ctrl Pts',(-6.07903471426388,4.30615562359862,-2.893866956644));
#81406=CARTESIAN_POINT('Ctrl Pts',(-7.03235570173644,-0.245353737911625,
-2.68218188873531));
#81407=CARTESIAN_POINT('Ctrl Pts',(-6.07254290742731,-3.58475370555032,
-2.5234180878038));
#81408=CARTESIAN_POINT('Ctrl Pts',(-3.61867994279838,-6.03484180458674,
-2.36465428687228));
#81409=CARTESIAN_POINT('Ctrl Pts',(0.83786789650287,-7.40650949062282,-2.15296921896358));
#81410=CARTESIAN_POINT('Ctrl Pts',(5.37411791268271,-5.16768201409678,-1.94128415105492));
#81411=CARTESIAN_POINT('Ctrl Pts',(6.98388635697521,-0.800134094673566,
-1.7295990831462));
#81412=CARTESIAN_POINT('Ctrl Pts',(6.40973376103728,3.79620266144416,-1.51791401523753));
#81413=CARTESIAN_POINT('Ctrl Pts',(1.51457095822232,7.85410001054634,-1.25330768035165));
#81414=CARTESIAN_POINT('Ctrl Pts',(-5.79020864255492,5.50997946566744,-0.935780078488634));
#81415=CARTESIAN_POINT('Ctrl Pts',(-7.42386336108424,-0.61984882046184,
-0.671173743602752));
#81416=CARTESIAN_POINT('Ctrl Pts',(-5.2223892511724,-4.7159377152133,-0.45948867569408));
#81417=CARTESIAN_POINT('Ctrl Pts',(-2.33781566303131,-6.65302851753602,
-0.300724874762546));
#81418=CARTESIAN_POINT('Ctrl Pts',(1.11743471057894,-6.94711885568928,-0.14196107383103));
#81419=CARTESIAN_POINT('Ctrl Pts',(5.41001647346126,-5.12768111829485,0.0697239940776447));
#81420=CARTESIAN_POINT('Ctrl Pts',(7.43971882199819,-0.492221914184057,
0.281409061986343));
#81421=CARTESIAN_POINT('Ctrl Pts',(5.85802083447291,3.88368773050881,0.493094129895022));
#81422=CARTESIAN_POINT('Ctrl Pts',(2.46080141762815,7.03461357653157,0.704779197803715));
#81423=CARTESIAN_POINT('Ctrl Pts',(-3.9011713930233,6.97843216915639,0.969385532689581));
#81424=CARTESIAN_POINT('Ctrl Pts',(-7.9737779581346,0.497495361200036,1.28691313455261));
#81425=CARTESIAN_POINT('Ctrl Pts',(-4.74911250865948,-6.42452853835538,
1.60444073641564));
#81426=CARTESIAN_POINT('Ctrl Pts',(2.83261554749834,-7.47622517968333,1.92196833827868));
#81427=CARTESIAN_POINT('Ctrl Pts',(6.96864010952473,-2.64185291264415,2.18657467316454));
#81428=CARTESIAN_POINT('Ctrl Pts',(6.74201681238604,1.986113739625,2.39825974107324));
#81429=CARTESIAN_POINT('Ctrl Pts',(4.40955949058423,6.01227774326799,2.60994480898192));
#81430=CARTESIAN_POINT('Ctrl Pts',(-0.445016813261593,7.44065534277421,
2.82162987689062));
#81431=CARTESIAN_POINT('Ctrl Pts',(-4.59957704198864,5.32494241868321,3.0333149447993));
#81432=CARTESIAN_POINT('Ctrl Pts',(-6.59738751825183,2.49051168707897,3.19207874573082));
#81433=CARTESIAN_POINT('Ctrl Pts',(-6.97022255151235,-0.964062034788524,
3.35084254666235));
#81434=CARTESIAN_POINT('Ctrl Pts',(-5.25072352308984,-5.28468184930254,
3.56252761457101));
#81435=CARTESIAN_POINT('Ctrl Pts',(0.493092895115608,-7.97767191812129,
3.82713394945689));
#81436=CARTESIAN_POINT('Ctrl Pts',(6.9872488172523,-3.8934773826184,4.14466155131991));
#81437=CARTESIAN_POINT('Ctrl Pts',(7.02998899293067,2.46477104279695,4.40926788620579));
#81438=CARTESIAN_POINT('Ctrl Pts',(3.88056947259661,5.8614045914742,4.62095295411446));
#81439=CARTESIAN_POINT('Ctrl Pts',(-0.49873573962075,7.43890740635084,4.83263802202317));
#81440=CARTESIAN_POINT('Ctrl Pts',(-5.13113239802791,5.40646703130468,5.04432308993184));
#81441=CARTESIAN_POINT('Ctrl Pts',(-6.9481759541162,1.11220998262044,5.25600815784053));
#81442=CARTESIAN_POINT('Ctrl Pts',(-6.65117684641269,-2.34266579984132,
5.41477195877206));
#81443=CARTESIAN_POINT('Ctrl Pts',(-4.71214358271871,-5.22589016611478,
5.57353575970356));
#81444=CARTESIAN_POINT('Ctrl Pts',(-0.614333013769389,-7.4243002539006,
5.78522082761227));
#81445=CARTESIAN_POINT('Ctrl Pts',(5.51422265003698,-5.7861550607049,6.04982716249811));
#81446=CARTESIAN_POINT('Ctrl Pts',(7.85299510856503,1.52036773516451,6.36735476436117));
#81447=CARTESIAN_POINT('Ctrl Pts',(3.79146892837499,6.41252824754307,6.63196109924701));
#81448=CARTESIAN_POINT('Ctrl Pts',(-0.805280546119295,6.98329570943009,
6.84364616715573));
#81449=CARTESIAN_POINT('Ctrl Pts',(-5.17164554705694,5.37030508610091,7.05533123506437));
#81450=CARTESIAN_POINT('Ctrl Pts',(-7.40712401550797,0.83240711967557,7.26701630297311));
#81451=CARTESIAN_POINT('Ctrl Pts',(-6.03217252679437,-3.62312890922495,
7.47870137088176));
#81452=CARTESIAN_POINT('Ctrl Pts',(-3.58027492641036,-6.07518430011776,
7.6374651718133));
#81453=CARTESIAN_POINT('Ctrl Pts',(-0.240168590682506,-7.03253475710761,
7.7962289727448));
#81454=CARTESIAN_POINT('Ctrl Pts',(4.31063684734961,-6.07585793187805,8.00791404065352));
#81455=CARTESIAN_POINT('Ctrl Pts',(7.94471355281213,-0.876223438026825,
8.27252037553935));
#81456=CARTESIAN_POINT('Ctrl Pts',(5.0292718807473,6.21992564904773,8.59004797740241));
#81457=CARTESIAN_POINT('Ctrl Pts',(-1.22833328830734,7.34758140023083,8.85465431228825));
#81458=CARTESIAN_POINT('Ctrl Pts',(-5.11280060736866,4.82433058910742,9.06633938019695));
#81459=CARTESIAN_POINT('Ctrl Pts',(-7.41483616626323,0.778652097589249,
9.27802444810563));
#81460=CARTESIAN_POINT('Ctrl Pts',(-6.20313892391525,-4.13272975620328,
9.48970951601433));
#81461=CARTESIAN_POINT('Ctrl Pts',(-2.28216335448501,-6.65626764204876,
9.70139458392301));
#81462=CARTESIAN_POINT('Ctrl Pts',(1.172693573114,-6.95348995901458,9.86015838485453));
#81463=CARTESIAN_POINT('Ctrl Pts',(4.34464135000243,-5.5351890302411,10.0189221857861));
#81464=CARTESIAN_POINT('Ctrl Pts',(7.21040472992183,-1.87288634778747,10.2306072536948));
#81465=CARTESIAN_POINT('Ctrl Pts',(6.64265886901188,4.44537108655917,10.4952135885806));
#81466=CARTESIAN_POINT('Ctrl Pts',(-0.157278780643135,7.99726916614796,
10.8127411904437));
#81467=CARTESIAN_POINT('Ctrl Pts',(-5.67104607761196,4.83063054745853,11.0773475253295));
#81468=CARTESIAN_POINT('Ctrl Pts',(-7.0182502267125,0.398822565494279,11.2890325932382));
#81469=CARTESIAN_POINT('Ctrl Pts',(-6.1744254806425,-4.1788233326868,11.5007176611469));
#81470=CARTESIAN_POINT('Ctrl Pts',(-2.08482608374679,-7.15624817538203,
11.7124027290556));
#81471=CARTESIAN_POINT('Ctrl Pts',(2.54004040956054,-6.56219195215601,11.9240877969643));
#81472=CARTESIAN_POINT('Ctrl Pts',(5.37471303366855,-4.56494168990841,12.0828515978958));
#81473=CARTESIAN_POINT('Ctrl Pts',(6.88827358848924,-1.43732843524527,12.2416153988273));
#81474=CARTESIAN_POINT('Ctrl Pts',(6.72261626979761,3.20999534735937,12.453300466736));
#81475=CARTESIAN_POINT('Ctrl Pts',(2.21978336802205,7.67846356677739,12.7179068016219));
#81476=CARTESIAN_POINT('Ctrl Pts',(-5.2699375108196,6.01737562087635,13.0354344034849));
#81477=CARTESIAN_POINT('Ctrl Pts',(-7.4494163191068,0.0441769743614518,
13.3000407383708));
#81478=CARTESIAN_POINT('Ctrl Pts',(-5.62642057271849,-4.21405828417065,
13.5117258062795));
#81479=CARTESIAN_POINT('Ctrl Pts',(-2.03317704990997,-7.17302485326342,
13.7234108741881));
#81480=CARTESIAN_POINT('Ctrl Pts',(3.01296933575057,-6.81765381410323,13.9350959420969));
#81481=CARTESIAN_POINT('Ctrl Pts',(6.16889507299606,-3.38510000997113,14.1467810100055));
#81482=CARTESIAN_POINT('Ctrl Pts',(7.05161165730847,-0.0317153127294182,
14.305544810937));
#81483=CARTESIAN_POINT('Ctrl Pts',(6.19569152870785,3.33581062737987,14.4643086118686));
#81484=CARTESIAN_POINT('Ctrl Pts',(3.07644180560223,6.78477305867776,14.6759936797772));
#81485=CARTESIAN_POINT('Ctrl Pts',(-3.24597966964378,7.30409863922549,14.9406000146631));
#81486=CARTESIAN_POINT('Ctrl Pts',(-7.90670051699391,1.21042871133698,15.2581276165262));
#81487=CARTESIAN_POINT('Ctrl Pts',(-5.72793898690211,-4.76303160421653,
15.5227339514119));
#81488=CARTESIAN_POINT('Ctrl Pts',(-1.59121410280738,-6.84711131518423,
15.7344190193207));
#81489=CARTESIAN_POINT('Ctrl Pts',(3.06328846900944,-6.79723165836278,15.9461040872294));
#81490=CARTESIAN_POINT('Ctrl Pts',(6.69522654827307,-3.27602338429213,16.1577891551381));
#81491=CARTESIAN_POINT('Ctrl Pts',(6.89951025983584,1.38236271418235,16.3694742230468));
#81492=CARTESIAN_POINT('Ctrl Pts',(5.41555730687422,4.51641139429432,16.5282380239783));
#81493=CARTESIAN_POINT('Ctrl Pts',(2.59228061532602,6.54173579962135,16.6870018249098));
#81494=CARTESIAN_POINT('Ctrl Pts',(-2.01509118438118,7.17196257377617,16.8986868928185));
#81495=CARTESIAN_POINT('Ctrl Pts',(-7.18673274888623,3.49815856463975,17.1632932277044));
#81496=CARTESIAN_POINT('Ctrl Pts',(-6.82877697123075,-4.16519577065104,
17.4808208295674));
#81497=CARTESIAN_POINT('Ctrl Pts',(-1.3153899643973,-7.33249646041519,17.7454271644533));
#81498=CARTESIAN_POINT('Ctrl Pts',(3.19156863058387,-6.26328870161434,17.9571122323619));
#81499=CARTESIAN_POINT('Ctrl Pts',(6.72057509705298,-3.22799703015457,18.1687973002706));
#81500=CARTESIAN_POINT('Ctrl Pts',(7.23196585891104,1.80473199192428,18.3804823681793));
#81501=CARTESIAN_POINT('Ctrl Pts',(4.38863199158892,5.5003706912847,18.592167436088));
#81502=CARTESIAN_POINT('Ctrl Pts',(1.23519286706014,6.94266025437761,18.7509312370195));
#81503=CARTESIAN_POINT('Ctrl Pts',(-2.22902263126149,6.6742553269984,18.909695037951));
#81504=CARTESIAN_POINT('Ctrl Pts',(-6.15990409720221,4.18965644824107,19.1213801058598));
#81505=CARTESIAN_POINT('Ctrl Pts',(-7.75105093758523,-1.95126889747041,
19.3859864407454));
#81506=CARTESIAN_POINT('Ctrl Pts',(-2.54259153080113,-7.58394877607694,
19.7035140426087));
#81507=CARTESIAN_POINT('Ctrl Pts',(3.71514900230698,-6.45704444704349,19.9681203774944));
#81508=CARTESIAN_POINT('Ctrl Pts',(6.47490452820166,-2.73687906824002,20.1798054454032));
#81509=CARTESIAN_POINT('Ctrl Pts',(7.22043469461147,1.85779904259507,20.3914905133118));
#81510=CARTESIAN_POINT('Ctrl Pts',(4.37101908514151,6.03759719627431,20.6031755812206));
#81511=CARTESIAN_POINT('Ctrl Pts',(-0.184091442732042,7.03422197828974,
20.8148606491293));
#81512=CARTESIAN_POINT('Ctrl Pts',(-3.52548371717569,6.10714314442349,20.9736244500608));
#81513=CARTESIAN_POINT('Ctrl Pts',(-6.00309759665687,3.67110954694288,21.1323882509922));
#81514=CARTESIAN_POINT('Ctrl Pts',(-7.41070162877531,-0.761013147248125,
21.344073318901));
#81515=CARTESIAN_POINT('Ctrl Pts',(-4.67380908245231,-6.48396095053497,
21.6086796537869));
#81516=CARTESIAN_POINT('Ctrl Pts',(2.93814156528294,-7.43964884070595,21.9262072556498));
#81517=CARTESIAN_POINT('Ctrl Pts',(7.00025521768217,-2.54797605713872,22.1908135905358));
#81518=CARTESIAN_POINT('Ctrl Pts',(6.71623311514751,2.07535742138385,22.4024986584444));
#81519=CARTESIAN_POINT('Ctrl Pts',(4.32802572178841,6.07077324674158,22.614183726353));
#81520=CARTESIAN_POINT('Ctrl Pts',(-0.543498046951198,7.43390863678652,
22.8258687942618));
#81521=CARTESIAN_POINT('Ctrl Pts',(-4.67032595475534,5.26329022337551,23.0375538621705));
#81522=CARTESIAN_POINT('Ctrl Pts',(-6.62983514718073,2.40239854057519,23.196317663102));
#81523=CARTESIAN_POINT('Ctrl Pts',(-6.95682722782088,-1.05677858744988,
23.3550814640335));
#81524=CARTESIAN_POINT('Ctrl Pts',(-5.17984032912462,-5.35414734629062,
23.5667665319422));
#81525=CARTESIAN_POINT('Ctrl Pts',(0.599258415449432,-7.9703908498134,23.831372866828));
#81526=CARTESIAN_POINT('Ctrl Pts',(7.03849166383386,-3.80009023956034,24.1489004686911));
#81527=CARTESIAN_POINT('Ctrl Pts',(6.99653648498133,2.55816971969485,24.413506803577));
#81528=CARTESIAN_POINT('Ctrl Pts',(3.80217459986353,5.91255985133764,24.6251918714857));
#81529=CARTESIAN_POINT('Ctrl Pts',(-0.597754682089963,7.43160708069626,
24.8368769393942));
#81530=CARTESIAN_POINT('Ctrl Pts',(-5.20267164077861,5.33765824546381,25.0485620073031));
#81531=CARTESIAN_POINT('Ctrl Pts',(-6.96237124967031,1.01958573985015,25.2602470752116));
#81532=CARTESIAN_POINT('Ctrl Pts',(-6.61939053680676,-2.43102894836384,
25.4190108761433));
#81533=CARTESIAN_POINT('Ctrl Pts',(-4.64213503223238,-5.2881762832912,25.5777746770747));
#81534=CARTESIAN_POINT('Ctrl Pts',(-0.515412313442996,-7.43182277696184,
25.7894597449835));
#81535=CARTESIAN_POINT('Ctrl Pts',(5.59078531721744,-5.71221152304974,26.0540660798693));
#81536=CARTESIAN_POINT('Ctrl Pts',(7.83205275812538,1.62480778081629,26.3715936817324));
#81537=CARTESIAN_POINT('Ctrl Pts',(3.70573992063129,6.46244897396321,26.6362000166182));
#81538=CARTESIAN_POINT('Ctrl Pts',(-0.898202598399992,6.97195293843298,
26.8478850845269));
#81539=CARTESIAN_POINT('Ctrl Pts',(-5.24270096633202,5.3009603884048,27.0595701524356));
#81540=CARTESIAN_POINT('Ctrl Pts',(-7.41755202574982,0.733695912776324,
27.2712552203442));
#81541=CARTESIAN_POINT('Ctrl Pts',(-5.98339005317347,-3.70313542430281,
27.482940288253));
#81542=CARTESIAN_POINT('Ctrl Pts',(-3.49905692074093,-6.1223225570012,27.6417040891845));
#81543=CARTESIAN_POINT('Ctrl Pts',(-0.146498137973434,-7.03510940612958,
27.800467890116));
#81544=CARTESIAN_POINT('Ctrl Pts',(4.39116414144362,-6.01791634404437,28.0121529580247));
#81545=CARTESIAN_POINT('Ctrl Pts',(7.95567738085036,-0.770349504512316,
28.2767592929106));
#81546=CARTESIAN_POINT('Ctrl Pts',(4.94599793777059,6.28634672367265,28.5942868947736));
#81547=CARTESIAN_POINT('Ctrl Pts',(-1.32606886728268,7.33057272385053,28.8588932296594));
#81548=CARTESIAN_POINT('Ctrl Pts',(-5.17659073738139,4.75581791295187,29.0705782975681));
#81549=CARTESIAN_POINT('Ctrl Pts',(-7.42454766388758,0.679842958687934,
29.2822633654768));
#81550=CARTESIAN_POINT('Ctrl Pts',(-6.14755516020086,-4.21496776967729,
29.4939484333855));
#81551=CARTESIAN_POINT('Ctrl Pts',(-2.19332242210769,-6.68606799635041,
29.7056335012942));
#81552=CARTESIAN_POINT('Ctrl Pts',(1.26518614402654,-6.93725715593081,29.8643973022256));
#81553=CARTESIAN_POINT('Ctrl Pts',(4.41796577987675,-5.47684256013266,30.0231611031572));
#81554=CARTESIAN_POINT('Ctrl Pts',(7.23470578825659,-1.7767025070009,30.234846171066));
#81555=CARTESIAN_POINT('Ctrl Pts',(6.58287282695247,4.53343427121724,30.4994525059518));
#81556=CARTESIAN_POINT('Ctrl Pts',(-0.263760934085454,7.99446564194957,
30.8169801078149));
#81557=CARTESIAN_POINT('Ctrl Pts',(-5.73487060217261,4.75468340447343,31.0815864427006));
#81558=CARTESIAN_POINT('Ctrl Pts',(-7.02293886729659,0.305328265497105,
31.2932715106094));
#81559=CARTESIAN_POINT('Ctrl Pts',(-6.11823045514813,-4.26067489483924,
31.504956578518));
#81560=CARTESIAN_POINT('Ctrl Pts',(-1.98934462931711,-7.18337634354049,
31.7166416464268));
#81561=CARTESIAN_POINT('Ctrl Pts',(2.62720099616708,-6.52778549164112,31.9283267143354));
#81562=CARTESIAN_POINT('Ctrl Pts',(5.43502577277014,-4.49296424155314,32.087090515267));
#81563=CARTESIAN_POINT('Ctrl Pts',(6.90680307772866,-1.34547289311988,32.2458543161984));
#81564=CARTESIAN_POINT('Ctrl Pts',(6.67927409073989,3.29923282927815,32.4575393841072));
#81565=CARTESIAN_POINT('Ctrl Pts',(2.11733583544207,7.70734259698044,32.722145718993));
#81566=CARTESIAN_POINT('Ctrl Pts',(-5.34960096107483,5.94666463556916,33.039673320856));
#81567=CARTESIAN_POINT('Ctrl Pts',(-7.44934406989137,-0.0550275277693012,
33.3042796557419));
#81568=CARTESIAN_POINT('Ctrl Pts',(-5.56980493015303,-4.28860918288662,
33.5159647236506));
#81569=CARTESIAN_POINT('Ctrl Pts',(-1.93747676755842,-7.1994637464875,33.7276497915593));
#81570=CARTESIAN_POINT('Ctrl Pts',(3.10348986080373,-6.77692691645844,33.939334859468));
#81571=CARTESIAN_POINT('Ctrl Pts',(6.21342596229719,-3.30265140609674,34.1510199273767));
#81572=CARTESIAN_POINT('Ctrl Pts',(7.05140873470941,0.0621906955560119,
34.3097837283081));
#81573=CARTESIAN_POINT('Ctrl Pts',(6.1507206452107,3.4180201294348,34.4685475292397));
#81574=CARTESIAN_POINT('Ctrl Pts',(2.98581919527262,6.82513907361293,34.6802325971484));
#81575=CARTESIAN_POINT('Ctrl Pts',(-3.34295730459666,7.26022571322132,34.9448389320343));
#81576=CARTESIAN_POINT('Ctrl Pts',(-7.9221181796911,1.10503134691718,35.2623665338973));
#81577=CARTESIAN_POINT('Ctrl Pts',(-5.6640039076763,-4.83888570171544,35.5269728687832));
#81578=CARTESIAN_POINT('Ctrl Pts',(-1.49989305555173,-6.86769368168124,
35.7386579366918));
#81579=CARTESIAN_POINT('Ctrl Pts',(3.15353257947768,-6.75583649387605,35.9503430046006));
#81580=CARTESIAN_POINT('Ctrl Pts',(6.73825824291578,-3.18657552851134,36.1620280725092));
#81581=CARTESIAN_POINT('Ctrl Pts',(6.88049017180109,1.47411787008045,36.3737131404179));
#81582=CARTESIAN_POINT('Ctrl Pts',(5.35493405865668,4.58812751065068,36.5324769413494));
#81583=CARTESIAN_POINT('Ctrl Pts',(2.50493735499844,6.57567600389313,36.691240742281));
#81584=CARTESIAN_POINT('Ctrl Pts',(-2.11041836375434,7.14449256217294,36.9029258101897));
#81585=CARTESIAN_POINT('Ctrl Pts',(-7.23267893805106,3.40214584142843,37.1675321450755));
#81586=CARTESIAN_POINT('Ctrl Pts',(-6.77270539707515,-4.25576225077142,
37.4850597469385));
#81587=CARTESIAN_POINT('Ctrl Pts',(-1.21762971480025,-7.3493627599999,37.7496660818244));
#81588=CARTESIAN_POINT('Ctrl Pts',(3.27469108415253,-6.2202326312501,37.9613511497331));
#81589=CARTESIAN_POINT('Ctrl Pts',(6.76296499832418,-3.13821587741466,38.1730362176418));
#81590=CARTESIAN_POINT('Ctrl Pts',(7.20729178726076,1.90087686092851,38.3847212855504));
#81591=CARTESIAN_POINT('Ctrl Pts',(4.31499684899518,5.55832445007519,38.5964063534592));
#81592=CARTESIAN_POINT('Ctrl Pts',(1.14263100495772,6.95849317115852,38.7551701543905));
#81593=CARTESIAN_POINT('Ctrl Pts',(-2.31770309403215,6.64398061620866,38.9139339553223));
#81594=CARTESIAN_POINT('Ctrl Pts',(-6.21514970625623,4.10725623376965,39.1256190232308));
#81595=CARTESIAN_POINT('Ctrl Pts',(-7.72437947181739,-2.05431319974369,
39.3902253581168));
#81596=CARTESIAN_POINT('Ctrl Pts',(-2.4413739867491,-7.61713488048403,39.7077529599797));
#81597=CARTESIAN_POINT('Ctrl Pts',(3.80080519001087,-6.40699890807125,39.9723592948657));
#81598=CARTESIAN_POINT('Ctrl Pts',(6.51077621204975,-2.65041294897678,40.1840443627743));
#81599=CARTESIAN_POINT('Ctrl Pts',(7.19505497495942,1.9537856507627,40.3957294306831));
#81600=CARTESIAN_POINT('Ctrl Pts',(4.29023149632212,6.09526877628013,40.6074144985916));
#81601=CARTESIAN_POINT('Ctrl Pts',(-0.277746744914853,7.03114679443056,
40.8190995665004));
#81602=CARTESIAN_POINT('Ctrl Pts',(-3.60649724135123,6.05965431973448,40.9778633674319));
#81603=CARTESIAN_POINT('Ctrl Pts',(-6.05145184970988,3.59084343452698,41.1366271683635));
#81604=CARTESIAN_POINT('Ctrl Pts',(-7.39991045135328,-0.859630707320278,
41.3483122362721));
#81605=CARTESIAN_POINT('Ctrl Pts',(-4.58705061660543,-6.54562507236513,
41.612918571158));
#81606=CARTESIAN_POINT('Ctrl Pts',(3.03695155815124,-7.39986323955413,41.930446173021));
#81607=CARTESIAN_POINT('Ctrl Pts',(7.03356478114057,-2.45453082480906,42.1950525079069));
#81608=CARTESIAN_POINT('Ctrl Pts',(6.68800097390752,2.16461050919299,42.4067375758155));
#81609=CARTESIAN_POINT('Ctrl Pts',(4.24680015435768,6.12786936143086,42.6184226437243));
#81610=CARTESIAN_POINT('Ctrl Pts',(-0.642443931402486,7.42601195407965,
42.8301077116328));
#81611=CARTESIAN_POINT('Ctrl Pts',(-4.74000075015738,5.20063086439034,43.0417927795416));
#81612=CARTESIAN_POINT('Ctrl Pts',(-6.66123896407119,2.31389893687908,43.200556580473));
#81613=CARTESIAN_POINT('Ctrl Pts',(-6.94213771746103,-1.14932587739404,
43.3593203814047));
#81614=CARTESIAN_POINT('Ctrl Pts',(-5.10808222231357,-5.42265024237231,
43.5710054493132));
#81615=CARTESIAN_POINT('Ctrl Pts',(0.705343452210856,-7.96170406142419,
43.8356117841993));
#81616=CARTESIAN_POINT('Ctrl Pts',(7.08847168811231,-3.70602480529903,44.1531393860622));
#81617=CARTESIAN_POINT('Ctrl Pts',(6.96185009143382,2.65111267298142,44.4177457209481));
#81618=CARTESIAN_POINT('Ctrl Pts',(3.72310251714552,5.96266746769607,44.6294307888568));
#81619=CARTESIAN_POINT('Ctrl Pts',(-0.696665106838566,7.42298809043423,
44.8411158567655));
#81620=CARTESIAN_POINT('Ctrl Pts',(-5.27328955955073,5.26790328007862,45.0528009246742));
#81621=CARTESIAN_POINT('Ctrl Pts',(-6.97533127386178,0.926780512865594,
45.2644859925829));
#81622=CARTESIAN_POINT('Ctrl Pts',(-6.5864306619872,-2.51896088921308,45.4232497935144));
#81623=CARTESIAN_POINT('Ctrl Pts',(-4.57130311085973,-5.34952464517057,
45.582013594446));
#81624=CARTESIAN_POINT('Ctrl Pts',(-0.41640031263465,-7.43802732051007,
45.7936986623545));
#81625=CARTESIAN_POINT('Ctrl Pts',(5.66635658269597,-5.63725500798157,46.0583049972405));
#81626=CARTESIAN_POINT('Ctrl Pts',(7.80972144840075,1.72895969561206,46.3758325991034));
#81627=CARTESIAN_POINT('Ctrl Pts',(3.61935375827535,6.51122365403746,46.6404389339895));
#81628=CARTESIAN_POINT('Ctrl Pts',(-0.990965371568293,6.95937377325353,
46.8521240018979));
#81629=CARTESIAN_POINT('Ctrl Pts',(-5.31282664658784,5.23067562415428,47.0638090698067));
#81630=CARTESIAN_POINT('Ctrl Pts',(-7.42666462090135,0.634854594203452,
47.2754941377155));
#81631=CARTESIAN_POINT('Ctrl Pts',(-5.9335464923095,-3.78248523100134,47.4871792056241));
#81632=CARTESIAN_POINT('Ctrl Pts',(-3.41721839800217,-6.16837508967364,
47.6459430065556));
#81633=CARTESIAN_POINT('Ctrl Pts',(-0.0528017051626853,-7.03643645893111,
47.8047068074872));
#81634=CARTESIAN_POINT('Ctrl Pts',(4.47091271248134,-5.958907547394,48.0163918753957));
#81635=CARTESIAN_POINT('Ctrl Pts',(7.96523036049119,-0.66433895835216,48.2809982102817));
#81636=CARTESIAN_POINT('Ctrl Pts',(4.86184687845832,6.35165298651348,48.5985258121447));
#81637=CARTESIAN_POINT('Ctrl Pts',(-1.42356928304938,7.31226405409412,48.8631321470306));
#81638=CARTESIAN_POINT('Ctrl Pts',(-5.23946285815445,4.68646184680054,49.0748172149392));
#81639=CARTESIAN_POINT('Ctrl Pts',(-7.43294250275057,0.580913257396659,
49.2865022828479));
#81640=CARTESIAN_POINT('Ctrl Pts',(-6.09088119778471,-4.29645830674553,
49.4981873507567));
#81641=CARTESIAN_POINT('Ctrl Pts',(-2.10409252904161,-6.71468265284166,
49.7098724186654));
#81642=CARTESIAN_POINT('Ctrl Pts',(1.35745434862167,-6.91979410950631,49.8686362195968));
#81643=CARTESIAN_POINT('Ctrl Pts',(4.49050673396954,-5.41752483453627,50.0274000205284));
#81644=CARTESIAN_POINT('Ctrl Pts',(7.25772385413221,-1.68020358831217,50.2390850884371));
#81645=CARTESIAN_POINT('Ctrl Pts',(6.52191938756684,4.62069350307433,50.5036914233229));
#81646=CARTESIAN_POINT('Ctrl Pts',(-0.370196312537869,7.99024439055812,
50.821219025186));
#81647=CARTESIAN_POINT('Ctrl Pts',(-5.7976781129181,4.67789307268023,51.0858253600718));
#81648=CARTESIAN_POINT('Ctrl Pts',(-7.02638206986709,0.211779819018986,
51.2975104279806));
#81649=CARTESIAN_POINT('Ctrl Pts',(-6.06095043134714,-4.34177087495216,
51.5091954958891));
#81650=CARTESIAN_POINT('Ctrl Pts',(-1.8935103873323,-7.20923062192969,51.720880563798));
#81651=CARTESIAN_POINT('Ctrl Pts',(2.71389567867474,-6.49222140291163,51.9325656317066));
#81652=CARTESIAN_POINT('Ctrl Pts',(5.49437467211685,-4.4201900172914,52.091329432638));
#81653=CARTESIAN_POINT('Ctrl Pts',(6.92410772430388,-1.25337874674743,52.2500932335697));
#81654=CARTESIAN_POINT('Ctrl Pts',(6.63474741870759,3.38788522994228,52.4617783014783));
#81655=CARTESIAN_POINT('Ctrl Pts',(2.01451281749849,7.73485481795531,52.7263846363642));
#81656=CARTESIAN_POINT('Ctrl Pts',(-5.4283157206323,5.87489907724322,53.0439122382272));
#81657=CARTESIAN_POINT('Ctrl Pts',(-7.44795076465959,-0.154222271479397,
53.3085185731131));
#81658=CARTESIAN_POINT('Ctrl Pts',(-5.51220154616398,-4.36239954562491,
53.5202036410217));
#81659=CARTESIAN_POINT('Ctrl Pts',(-1.8414328961365,-7.22462589731171,53.7318887089303));
#81660=CARTESIAN_POINT('Ctrl Pts',(3.19346001799998,-6.73499820763055,53.9435737768392));
#81661=CARTESIAN_POINT('Ctrl Pts',(6.25685497067417,-3.21961711542544,54.1552588447478));
#81662=CARTESIAN_POINT('Ctrl Pts',(7.04995532691501,0.156085676522665,54.3140226456793));
#81663=CARTESIAN_POINT('Ctrl Pts',(6.10465899868012,3.4996234819296,54.4727864466108));
#81664=CARTESIAN_POINT('Ctrl Pts',(2.89466709040366,6.8642947339467,54.6844715145196));
#81665=CARTESIAN_POINT('Ctrl Pts',(-3.43934211748364,7.21506525693325,54.9490778494054));
#81666=CARTESIAN_POINT('Ctrl Pts',(-7.93613092206531,0.999438039044138,
55.2666054512683));
#81667=CARTESIAN_POINT('Ctrl Pts',(-5.59906442082156,-4.9138817137095,55.5312117861543));
#81668=CARTESIAN_POINT('Ctrl Pts',(-1.40830596774888,-6.88705809370141,
55.742896854063));
#81669=CARTESIAN_POINT('Ctrl Pts',(3.24321731397379,-6.71324338105273,55.9545819219718));
#81670=CARTESIAN_POINT('Ctrl Pts',(6.78009525479357,-3.09656232163611,56.1662669898803));
#81671=CARTESIAN_POINT('Ctrl Pts',(6.86024957327956,1.56561130116725,56.3779520577891));
#81672=CARTESIAN_POINT('Ctrl Pts',(5.29336186929955,4.65903061347959,56.5367158587205));
#81673=CARTESIAN_POINT('Ctrl Pts',(2.41714860448358,6.60844892251285,56.6954796596521));
#81674=CARTESIAN_POINT('Ctrl Pts',(-2.2053685445281,7.11575807266166,56.9071647275608));
#81675=CARTESIAN_POINT('Ctrl Pts',(-7.27734816230319,3.30552458122617,57.1717710624466));
#81676=CARTESIAN_POINT('Ctrl Pts',(-6.71542285986649,-4.34556492744316,
57.4892986643097));
#81677=CARTESIAN_POINT('Ctrl Pts',(-1.11967013848367,-7.36494098405521,
57.7539049991955));
#81678=CARTESIAN_POINT('Ctrl Pts',(3.35725491809626,-6.17605316957025,57.9655900671042));
#81679=CARTESIAN_POINT('Ctrl Pts',(6.80409863169368,-3.04793048229254,58.177275135013));
#81680=CARTESIAN_POINT('Ctrl Pts',(7.18145534865284,1.99679094230443,58.3889602029215));
#81681=CARTESIAN_POINT('Ctrl Pts',(4.24045344088747,5.61516113422602,58.6006452708304));
#81682=CARTESIAN_POINT('Ctrl Pts',(1.05016417991309,6.97336544192119,58.7594090717617));
#81683=CARTESIAN_POINT('Ctrl Pts',(-2.4065154837537,6.61202906035096,58.9181728726935));
#81684=CARTESIAN_POINT('Ctrl Pts',(-6.26811999573962,4.0252049886518,59.1298579406019));
#81685=CARTESIAN_POINT('Ctrl Pts',(-7.69876535826759,-2.15922222239559,
59.3944642754879));
#81686=CARTESIAN_POINT('Ctrl Pts',(-2.3354816390472,-7.64507444656264,59.7119918773507));
#81687=CARTESIAN_POINT('Ctrl Pts',(3.87865942051839,-6.36236462354854,59.9765982122369));
#81688=CARTESIAN_POINT('Ctrl Pts',(6.55508373605099,-2.55465868456236,60.1882832801454));
#81689=CARTESIAN_POINT('Ctrl Pts',(6.99518748195096,0.879984397019229,60.347047081077));
#81690=CARTESIAN_POINT('Ctrl Pts',(5.71206067810625,4.12746479532865,60.5058755303524));
#81691=CARTESIAN_POINT('Ctrl Pts',(3.93417824599609,5.61116415437882,60.6117827126507));
#81692=CARTESIAN_POINT('Ctrl Pts',(2.91924481736993,6.09709494952001,60.6647686279718));
#81693=CARTESIAN_POINT('Ctrl Pts',(3.93301173192297,-5.51252654933401,60.));
#81694=CARTESIAN_POINT('Ctrl Pts',(4.08943068438299,-5.42065063936855,60.0000000000001));
#81695=CARTESIAN_POINT('Ctrl Pts',(4.24173339265253,-5.32238226638426,60.));
#81696=CARTESIAN_POINT('Ctrl Pts',(4.38947572522442,-5.21781239717694,60.));
#81697=CARTESIAN_POINT('Ctrl Pts',(4.53944789002314,-5.11166428522596,60.));
#81698=CARTESIAN_POINT('Ctrl Pts',(4.6847220474222,-4.99902354735396,60.));
#81699=CARTESIAN_POINT('Ctrl Pts',(4.82511408164218,-4.88038463662292,60.));
#81700=CARTESIAN_POINT('Ctrl Pts',(4.96550611586215,-4.76174572589187,60.));
#81701=CARTESIAN_POINT('Ctrl Pts',(5.10101645190341,-4.63710808992744,60.));
#81702=CARTESIAN_POINT('Ctrl Pts',(5.23143491853015,-4.50691912389382,59.9999999999999));
#81703=CARTESIAN_POINT('Ctrl Pts',(5.25943563992776,-4.47896767605638,59.9999999999999));
#81704=CARTESIAN_POINT('Ctrl Pts',(5.28720153910478,-4.45076018096386,59.9999999999999));
#81705=CARTESIAN_POINT('Ctrl Pts',(5.31473034986051,-4.42230082168352,59.9999999999999));
#81706=CARTESIAN_POINT('Ctrl Pts',(5.33559713591147,-4.40072868162566,59.9999999999999));
#81707=CARTESIAN_POINT('Ctrl Pts',(5.3563286782172,-4.37901069779888,59.9999999999999));
#81708=CARTESIAN_POINT('Ctrl Pts',(5.37691127712948,-4.35716240021337,59.9999999999999));
#81709=CARTESIAN_POINT('Ctrl Pts',(5.50477144804138,-4.22143964356225,59.9999999999999));
#81710=CARTESIAN_POINT('Ctrl Pts',(5.62699841484352,-4.08057724269767,59.9999999999999));
#81711=CARTESIAN_POINT('Ctrl Pts',(5.74340953646046,-3.93507696910473,59.9999999999999));
#81712=CARTESIAN_POINT('Ctrl Pts',(5.86128096626322,-3.78775148124004,60.));
#81713=CARTESIAN_POINT('Ctrl Pts',(5.97319021681194,-3.63567053260053,60.));
#81714=CARTESIAN_POINT('Ctrl Pts',(6.07891840170064,-3.47931011242737,59.9999999999999));
#81715=CARTESIAN_POINT('Ctrl Pts',(6.18542930740369,-3.32179213378919,59.9999999999999));
#81716=CARTESIAN_POINT('Ctrl Pts',(6.28566780084611,-3.15993050846068,59.9999999999999));
#81717=CARTESIAN_POINT('Ctrl Pts',(6.37937298743066,-2.99417480689384,60.));
#81718=CARTESIAN_POINT('Ctrl Pts',(6.39382678116988,-2.96860739906009,60.));
#81719=CARTESIAN_POINT('Ctrl Pts',(6.4081250523425,-2.94294728093287,60.));
#81720=CARTESIAN_POINT('Ctrl Pts',(6.42226675335339,-2.91719603854252,60.));
#81721=CARTESIAN_POINT('Ctrl Pts',(6.43451668575209,-2.89488960042585,60.));
#81722=CARTESIAN_POINT('Ctrl Pts',(6.44664514426399,-2.8725220233613,59.9999999999999));
#81723=CARTESIAN_POINT('Ctrl Pts',(6.45864972514055,-2.85009817405855,59.9999999999999));
#81724=CARTESIAN_POINT('Ctrl Pts',(6.50694144611864,-2.75989208648933,59.9999999999999));
#81725=CARTESIAN_POINT('Ctrl Pts',(6.55323905636916,-2.66875676359713,60.));
#81726=CARTESIAN_POINT('Ctrl Pts',(6.59751447498518,-2.57677045843172,60.));
#81727=CARTESIAN_POINT('Ctrl Pts',(6.68196077380915,-2.40132540886417,60.));
#81728=CARTESIAN_POINT('Ctrl Pts',(6.75905350802381,-2.22278690146021,60.));
#81729=CARTESIAN_POINT('Ctrl Pts',(6.82877465833766,-2.04163087927507,60.));
#81730=CARTESIAN_POINT('Ctrl Pts',(6.89802150956567,-1.86170722539323,60.));
#81731=CARTESIAN_POINT('Ctrl Pts',(6.95999692380297,-1.67920088449624,60.));
#81732=CARTESIAN_POINT('Ctrl Pts',(7.01464054137877,-1.49454522797912,60.));
#81733=CARTESIAN_POINT('Ctrl Pts',(7.06984557259439,-1.30799240196921,60.));
#81734=CARTESIAN_POINT('Ctrl Pts',(7.1175677183855,-1.11924526300582,60.));
#81735=CARTESIAN_POINT('Ctrl Pts',(7.15769680819296,-0.928726386214075,
60.0000000000001));
#81736=CARTESIAN_POINT('Ctrl Pts',(7.19782589800042,-0.738207509422325,
60.0000000000001));
#81737=CARTESIAN_POINT('Ctrl Pts',(7.23036220953441,-0.545916226512543,
60.));
#81738=CARTESIAN_POINT('Ctrl Pts',(7.25514335619632,-0.352260600144331,
60.));
#81739=CARTESIAN_POINT('Ctrl Pts',(7.25810700464038,-0.32910076805098,60.));
#81740=CARTESIAN_POINT('Ctrl Pts',(7.26095967090388,-0.305921412473712,
60.));
#81741=CARTESIAN_POINT('Ctrl Pts',(7.2637010242391,-0.282723224613104,60.));
#81742=CARTESIAN_POINT('Ctrl Pts',(7.26647943597639,-0.259211436983195,
60.));
#81743=CARTESIAN_POINT('Ctrl Pts',(7.26914233841631,-0.235690110937071,
60.0000000000001));
#81744=CARTESIAN_POINT('Ctrl Pts',(7.27168943529372,-0.212162315957714,
60.));
#81745=CARTESIAN_POINT('Ctrl Pts',(7.29297172671287,-0.0155756083033903,
60.0000000000001));
#81746=CARTESIAN_POINT('Ctrl Pts',(7.30617899232667,0.181512276274655,60.0000000000001));
#81747=CARTESIAN_POINT('Ctrl Pts',(7.31126922514826,0.378646193900632,60.0000000000001));
#81748=CARTESIAN_POINT('Ctrl Pts',(7.31596526012799,0.5605136654503,60.));
#81749=CARTESIAN_POINT('Ctrl Pts',(7.3137524527044,0.74242103248043,60.));
#81750=CARTESIAN_POINT('Ctrl Pts',(7.30456172141971,0.924026543563235,60.));
#81751=CARTESIAN_POINT('Ctrl Pts',(7.29474439159223,1.11801341420085,60.));
#81752=CARTESIAN_POINT('Ctrl Pts',(7.27696618509513,1.31165628281886,60.));
#81753=CARTESIAN_POINT('Ctrl Pts',(7.25145299411574,1.50450172189991,60.));
#81754=CARTESIAN_POINT('Ctrl Pts',(7.22565302124297,1.69951484671629,60.));
#81755=CARTESIAN_POINT('Ctrl Pts',(7.19194313577524,1.89371321377546,60.));
#81756=CARTESIAN_POINT('Ctrl Pts',(7.15050363732496,2.08662930880182,60.));
#81757=CARTESIAN_POINT('Ctrl Pts',(7.1179488313502,2.2381838950748,60.));
#81758=CARTESIAN_POINT('Ctrl Pts',(7.08062249907401,2.38894725733733,60.));
#81759=CARTESIAN_POINT('Ctrl Pts',(7.03858982148013,2.53868895506453,59.9999999999999));
#81760=CARTESIAN_POINT('Ctrl Pts',(7.03300180162727,2.55859631351987,59.9999999999999));
#81761=CARTESIAN_POINT('Ctrl Pts',(7.02733083309508,2.57848457739548,59.9999999999999));
#81762=CARTESIAN_POINT('Ctrl Pts',(7.02157995933159,2.5983435215292,59.9999999999999));
#81763=CARTESIAN_POINT('Ctrl Pts',(6.9659804061741,2.79034015811396,59.9999999999999));
#81764=CARTESIAN_POINT('Ctrl Pts',(6.9028482219688,2.9798404774229,59.9999999999999));
#81765=CARTESIAN_POINT('Ctrl Pts',(6.8324580727966,3.16637611832398,59.9999999999999));
#81766=CARTESIAN_POINT('Ctrl Pts',(6.76136569194129,3.35477269059982,59.9999999999999));
#81767=CARTESIAN_POINT('Ctrl Pts',(6.68286970430263,3.54014584826076,59.9999999999999));
#81768=CARTESIAN_POINT('Ctrl Pts',(6.59719965578521,3.72201525869361,59.9999999999999));
#81769=CARTESIAN_POINT('Ctrl Pts',(6.51129089759076,3.90439142719392,60.));
#81770=CARTESIAN_POINT('Ctrl Pts',(6.41816787659654,4.08324503974194,59.9999999999999));
#81771=CARTESIAN_POINT('Ctrl Pts',(6.3180107511728,4.2580829378152,59.9999999999999));
#81772=CARTESIAN_POINT('Ctrl Pts',(6.27742617235638,4.32892884542708,59.9999999999999));
#81773=CARTESIAN_POINT('Ctrl Pts',(6.23568606124396,4.39911523202738,60.));
#81774=CARTESIAN_POINT('Ctrl Pts',(6.19280011122803,4.46860844401259,60.));
#81775=CARTESIAN_POINT('Ctrl Pts',(6.08722571743203,4.63968320685557,60.));
#81776=CARTESIAN_POINT('Ctrl Pts',(5.97471037226409,4.80655917740463,59.9999999999999));
#81777=CARTESIAN_POINT('Ctrl Pts',(5.85558066445649,4.96895350572671,60.));
#81778=CARTESIAN_POINT('Ctrl Pts',(5.81668657376114,5.02197285623473,60.0000000000001));
#81779=CARTESIAN_POINT('Ctrl Pts',(5.7770870938084,5.07451426995668,60.));
#81780=CARTESIAN_POINT('Ctrl Pts',(5.73679261859994,5.12656719766218,60.));
#81781=CARTESIAN_POINT('Ctrl Pts',(5.71566740085255,5.15385702899708,60.));
#81782=CARTESIAN_POINT('Ctrl Pts',(5.69434724576312,5.18101737942238,60.));
#81783=CARTESIAN_POINT('Ctrl Pts',(5.67285512479792,5.20801998658619,60.));
#81784=CARTESIAN_POINT('Ctrl Pts',(5.54699632712769,5.36614843175431,60.));
#81785=CARTESIAN_POINT('Ctrl Pts',(5.41513767804764,5.51901110932468,60.));
#81786=CARTESIAN_POINT('Ctrl Pts',(5.27770276549599,5.66637944969325,60.));
#81787=CARTESIAN_POINT('Ctrl Pts',(5.13773272163551,5.81646615387973,60.));
#81788=CARTESIAN_POINT('Ctrl Pts',(4.99197850428412,5.96085449177701,60.));
#81789=CARTESIAN_POINT('Ctrl Pts',(4.84083762292807,6.0992821473738,60.));
#81790=CARTESIAN_POINT('Ctrl Pts',(4.68918631562009,6.23817729440803,60.));
#81791=CARTESIAN_POINT('Ctrl Pts',(4.5321114673821,6.37107194887579,60.0000000000001));
#81792=CARTESIAN_POINT('Ctrl Pts',(4.36997047171315,6.49767239337633,60.0000000000001));
#81793=CARTESIAN_POINT('Ctrl Pts',(4.20894762566035,6.62339978144942,60.));
#81794=CARTESIAN_POINT('Ctrl Pts',(4.04292777468119,6.74291993626482,60.));
#81795=CARTESIAN_POINT('Ctrl Pts',(3.87222449617968,6.8559096253412,60.));
#81796=CARTESIAN_POINT('Ctrl Pts',(3.7251270308196,6.95327446227263,60.));
#81797=CARTESIAN_POINT('Ctrl Pts',(3.57455113397834,7.04578972027165,60.));
#81798=CARTESIAN_POINT('Ctrl Pts',(3.4206796250975,7.13322310757506,60.));
#81799=CARTESIAN_POINT('Ctrl Pts',(3.4248577137498,7.13737126555389,-60.));
#81800=CARTESIAN_POINT('Ctrl Pts',(3.60861991098295,7.03458684113382,-60.));
#81801=CARTESIAN_POINT('Ctrl Pts',(3.78767901468881,6.92437773889514,-60.));
#81802=CARTESIAN_POINT('Ctrl Pts',(3.96154458364234,6.80675795931553,-60.));
#81803=CARTESIAN_POINT('Ctrl Pts',(4.13076522420728,6.69228046636872,-60.));
#81804=CARTESIAN_POINT('Ctrl Pts',(4.29506657128387,6.57078249333906,-60.));
#81805=CARTESIAN_POINT('Ctrl Pts',(4.45418747522949,6.44274262314797,-60.));
#81806=CARTESIAN_POINT('Ctrl Pts',(4.61440833160287,6.31381765387451,-60.));
#81807=CARTESIAN_POINT('Ctrl Pts',(4.76937730965001,6.17825938241126,-60.));
#81808=CARTESIAN_POINT('Ctrl Pts',(4.91878898868684,6.03651990623725,-60.));
#81809=CARTESIAN_POINT('Ctrl Pts',(5.0675274265728,5.89541910067236,-60.));
#81810=CARTESIAN_POINT('Ctrl Pts',(5.21075889024205,5.74819197850466,-60.));
#81811=CARTESIAN_POINT('Ctrl Pts',(5.34813792788795,5.595258661849,-60.));
#81812=CARTESIAN_POINT('Ctrl Pts',(5.46090011722494,5.46972935327202,-60.));
#81813=CARTESIAN_POINT('Ctrl Pts',(5.56971864085314,5.34035497301831,-60.));
#81814=CARTESIAN_POINT('Ctrl Pts',(5.67437750866333,5.20735958609987,-60.));
#81815=CARTESIAN_POINT('Ctrl Pts',(5.69455286498308,5.18172172687107,-60.));
#81816=CARTESIAN_POINT('Ctrl Pts',(5.71457658133583,5.15594526087748,-60.));
#81817=CARTESIAN_POINT('Ctrl Pts',(5.73442860333554,5.13005609206325,-60.));
#81818=CARTESIAN_POINT('Ctrl Pts',(5.85765046658865,4.96936154823243,-60.));
#81819=CARTESIAN_POINT('Ctrl Pts',(5.97438553496247,4.80417296037974,-60.));
#81820=CARTESIAN_POINT('Ctrl Pts',(6.08437659315306,4.63494157400739,-60.));
#81821=CARTESIAN_POINT('Ctrl Pts',(6.19442667221929,4.46561937857496,-60.));
#81822=CARTESIAN_POINT('Ctrl Pts',(6.29772586482784,4.29224936825753,-60.));
#81823=CARTESIAN_POINT('Ctrl Pts',(6.39397171685177,4.11525752541809,-60.));
#81824=CARTESIAN_POINT('Ctrl Pts',(6.42699095565242,4.05453661327915,-60.));
#81825=CARTESIAN_POINT('Ctrl Pts',(6.45917961583643,3.99338923911971,-60.));
#81826=CARTESIAN_POINT('Ctrl Pts',(6.49052415144755,3.93183211822112,-60.));
#81827=CARTESIAN_POINT('Ctrl Pts',(6.58200931504942,3.75216560964246,-60.));
#81828=CARTESIAN_POINT('Ctrl Pts',(6.66630731358913,3.56900914058539,-60.));
#81829=CARTESIAN_POINT('Ctrl Pts',(6.7432492526404,3.38277223025193,-60.));
#81830=CARTESIAN_POINT('Ctrl Pts',(6.81951943947852,3.19816128695583,-60.));
#81831=CARTESIAN_POINT('Ctrl Pts',(6.88856152296434,3.01052281825039,-60.));
#81832=CARTESIAN_POINT('Ctrl Pts',(6.95016018173248,2.82025301605453,-60.));
#81833=CARTESIAN_POINT('Ctrl Pts',(6.96705468955314,2.76806820025631,-60.));
#81834=CARTESIAN_POINT('Ctrl Pts',(6.98338898298803,2.71568546353412,-60.));
#81835=CARTESIAN_POINT('Ctrl Pts',(6.99915793217927,2.66311304111913,-60.));
#81836=CARTESIAN_POINT('Ctrl Pts',(7.00922467652644,2.62955131612756,-60.));
#81837=CARTESIAN_POINT('Ctrl Pts',(7.01906101322371,2.59591228702048,-60.));
#81838=CARTESIAN_POINT('Ctrl Pts',(7.02866554329771,2.56219810720566,-60.));
#81839=CARTESIAN_POINT('Ctrl Pts',(7.03567914496781,2.53757870094282,-60.));
#81840=CARTESIAN_POINT('Ctrl Pts',(7.04256711476104,2.51292621131787,-60.));
#81841=CARTESIAN_POINT('Ctrl Pts',(7.0493270299122,2.48824942657131,-60.));
#81842=CARTESIAN_POINT('Ctrl Pts',(7.06363748749976,2.43600970556635,-60.));
#81843=CARTESIAN_POINT('Ctrl Pts',(7.07737720041661,2.38365021216742,-60.));
#81844=CARTESIAN_POINT('Ctrl Pts',(7.09054441676118,2.3311792008664,-60.));
#81845=CARTESIAN_POINT('Ctrl Pts',(7.13858283449617,2.139747367904,-60.));
#81846=CARTESIAN_POINT('Ctrl Pts',(7.17900498375673,1.94683219772224,-60.));
#81847=CARTESIAN_POINT('Ctrl Pts',(7.21169252079291,1.75283065323041,-60.));
#81848=CARTESIAN_POINT('Ctrl Pts',(7.24420959030436,1.55984083877647,-60.));
#81849=CARTESIAN_POINT('Ctrl Pts',(7.2690725791835,1.36577531784115,-60.));
#81850=CARTESIAN_POINT('Ctrl Pts',(7.28611380189689,1.17102122652283,-60.));
#81851=CARTESIAN_POINT('Ctrl Pts',(7.30289509392125,0.979237729861928,-60.));
#81852=CARTESIAN_POINT('Ctrl Pts',(7.31209139548342,0.78678594030478,-60.));
#81853=CARTESIAN_POINT('Ctrl Pts',(7.31349255663583,0.594040875125159,-60.));
#81854=CARTESIAN_POINT('Ctrl Pts',(7.31410769614461,0.50942169730248,-60.));
#81855=CARTESIAN_POINT('Ctrl Pts',(7.31321974938026,0.424746113772566,-60.));
#81856=CARTESIAN_POINT('Ctrl Pts',(7.31080782602045,0.340046611414358,-60.));
#81857=CARTESIAN_POINT('Ctrl Pts',(7.30678229620877,0.198682098155049,-60.));
#81858=CARTESIAN_POINT('Ctrl Pts',(7.29851215479959,0.057250540439187,-60.));
#81859=CARTESIAN_POINT('Ctrl Pts',(7.2860244774147,-0.0840501440206062,
-60.));
#81860=CARTESIAN_POINT('Ctrl Pts',(7.28245939678781,-0.124389777821812,
-60.));
#81861=CARTESIAN_POINT('Ctrl Pts',(7.27855049671512,-0.164718701457005,
-60.));
#81862=CARTESIAN_POINT('Ctrl Pts',(7.27429822708433,-0.20503219790969,-60.));
#81863=CARTESIAN_POINT('Ctrl Pts',(7.27144834789734,-0.232050379838477,
-60.));
#81864=CARTESIAN_POINT('Ctrl Pts',(7.26844391232975,-0.259064365716766,
-60.));
#81865=CARTESIAN_POINT('Ctrl Pts',(7.26528611071862,-0.28606362287843,-60.));
#81866=CARTESIAN_POINT('Ctrl Pts',(7.26002333336482,-0.331060458227003,
-60.));
#81867=CARTESIAN_POINT('Ctrl Pts',(7.25433702839529,-0.375996037536274,
-60.));
#81868=CARTESIAN_POINT('Ctrl Pts',(7.24823054744924,-0.420859007874808,
-60.));
#81869=CARTESIAN_POINT('Ctrl Pts',(7.22223958985405,-0.611808847883335,
-60.));
#81870=CARTESIAN_POINT('Ctrl Pts',(7.18863664734709,-0.801478953923177,
-60.));
#81871=CARTESIAN_POINT('Ctrl Pts',(7.14759919930349,-0.98939764097146,-60.));
#81872=CARTESIAN_POINT('Ctrl Pts',(7.10643012046813,-1.17791909175732,-60.));
#81873=CARTESIAN_POINT('Ctrl Pts',(7.05777850127931,-1.36467859587107,-60.));
#81874=CARTESIAN_POINT('Ctrl Pts',(7.00177368720448,-1.54918517106434,-60.));
#81875=CARTESIAN_POINT('Ctrl Pts',(6.94620176777722,-1.73226558477193,-60.));
#81876=CARTESIAN_POINT('Ctrl Pts',(6.88338955967928,-1.91312842201592,-60.));
#81877=CARTESIAN_POINT('Ctrl Pts',(6.81341899657811,-2.09126921993615,-60.));
#81878=CARTESIAN_POINT('Ctrl Pts',(6.74495504259696,-2.26557428267148,-60.));
#81879=CARTESIAN_POINT('Ctrl Pts',(6.66963730643464,-2.4372737762835,-60.));
#81880=CARTESIAN_POINT('Ctrl Pts',(6.58750516330558,-2.60586284078176,-60.));
#81881=CARTESIAN_POINT('Ctrl Pts',(6.53702924311811,-2.70947255848659,-60.));
#81882=CARTESIAN_POINT('Ctrl Pts',(6.48397884068404,-2.81190681635542,-60.));
#81883=CARTESIAN_POINT('Ctrl Pts',(6.42835674087745,-2.91304091849508,-60.));
#81884=CARTESIAN_POINT('Ctrl Pts',(6.40310580363065,-2.95895308066658,-60.));
#81885=CARTESIAN_POINT('Ctrl Pts',(6.37734514144749,-3.00456010758804,-60.));
#81886=CARTESIAN_POINT('Ctrl Pts',(6.35108059795691,-3.04984579985723,-60.));
#81887=CARTESIAN_POINT('Ctrl Pts',(6.34509772234999,-3.06016155743805,-60.));
#81888=CARTESIAN_POINT('Ctrl Pts',(6.33908864170211,-3.07046074555373,-60.));
#81889=CARTESIAN_POINT('Ctrl Pts',(6.33305338320512,-3.08074324429301,-60.));
#81890=CARTESIAN_POINT('Ctrl Pts',(6.23708789041981,-3.24424329306003,-60.));
#81891=CARTESIAN_POINT('Ctrl Pts',(6.13450706082851,-3.40352647237428,-60.));
#81892=CARTESIAN_POINT('Ctrl Pts',(6.02564607812735,-3.55828730005497,-60.));
#81893=CARTESIAN_POINT('Ctrl Pts',(5.91677903996887,-3.71305673639935,-60.));
#81894=CARTESIAN_POINT('Ctrl Pts',(5.80163059279153,-3.8633037709451,-60.));
#81895=CARTESIAN_POINT('Ctrl Pts',(5.68050054265185,-4.00868504968493,-60.));
#81896=CARTESIAN_POINT('Ctrl Pts',(5.57662125738459,-4.1333618190689,-60.));
#81897=CARTESIAN_POINT('Ctrl Pts',(5.46834202505428,-4.2544596084174,-60.));
#81898=CARTESIAN_POINT('Ctrl Pts',(5.35583581478516,-4.37173590025246,-60.));
#81899=CARTESIAN_POINT('Ctrl Pts',(5.33669698721178,-4.39168618319691,-60.));
#81900=CARTESIAN_POINT('Ctrl Pts',(5.31743557941832,-4.41152596850129,-60.));
#81901=CARTESIAN_POINT('Ctrl Pts',(5.29806298900613,-4.43124345790525,-60.));
#81902=CARTESIAN_POINT('Ctrl Pts',(5.16723317262104,-4.56440249670221,-60.));
#81903=CARTESIAN_POINT('Ctrl Pts',(5.03121965193352,-4.69210870498326,-60.));
#81904=CARTESIAN_POINT('Ctrl Pts',(4.89032787541421,-4.8140473373547,-60.));
#81905=CARTESIAN_POINT('Ctrl Pts',(4.75110811375755,-4.93453887884054,-60.));
#81906=CARTESIAN_POINT('Ctrl Pts',(4.60712461558511,-5.04939924921015,-60.));
#81907=CARTESIAN_POINT('Ctrl Pts',(4.45864629338521,-5.15828165385862,-60.));
#81908=CARTESIAN_POINT('Ctrl Pts',(4.31072242009514,-5.26675746898168,-60.));
#81909=CARTESIAN_POINT('Ctrl Pts',(4.15833671963038,-5.3693002495206,-60.));
#81910=CARTESIAN_POINT('Ctrl Pts',(4.00173737932556,-5.46551877007183,-60.));
#81911=CARTESIAN_POINT('Ctrl Pts',(3.97755260405217,-5.48037849612265,-60.));
#81912=CARTESIAN_POINT('Ctrl Pts',(3.9532673039551,-5.49508728270992,-60.));
#81913=CARTESIAN_POINT('Ctrl Pts',(3.92888236737297,-5.50964357679758,-60.));
#81914=CARTESIAN_POINT('Origin',(-15.3358035470651,3.40523243981596E-15,
65.));
#81915=CARTESIAN_POINT('',(-13.3358035470651,3.65016179964543E-15,65.));
#81916=CARTESIAN_POINT('Origin',(-15.3358035470651,3.40523243981596E-15,
65.));
#81917=CARTESIAN_POINT('',(-13.3358035470651,3.65016179964543E-15,60.));
#81918=CARTESIAN_POINT('',(-13.3358035470651,3.16030307998649E-15,65.));
#81919=CARTESIAN_POINT('Origin',(-15.3358035470651,3.40523243981596E-15,
60.));
#81920=CARTESIAN_POINT('Origin',(0.,-15.3358035470651,65.));
#81921=CARTESIAN_POINT('',(2.,-15.3358035470651,65.));
#81922=CARTESIAN_POINT('Origin',(0.,-15.3358035470651,65.));
#81923=CARTESIAN_POINT('',(2.,-15.3358035470651,60.));
#81924=CARTESIAN_POINT('',(2.,-15.3358035470651,65.));
#81925=CARTESIAN_POINT('Origin',(0.,-15.3358035470651,60.));
#81926=CARTESIAN_POINT('Origin',(1.87809427262659E-15,15.3358035470651,
65.));
#81927=CARTESIAN_POINT('',(2.,15.3358035470651,65.));
#81928=CARTESIAN_POINT('Origin',(1.87809427262659E-15,15.3358035470651,
65.));
#81929=CARTESIAN_POINT('',(2.,15.3358035470651,60.));
#81930=CARTESIAN_POINT('',(2.,15.3358035470651,65.));
#81931=CARTESIAN_POINT('Origin',(1.87809427262659E-15,15.3358035470651,
60.));
#81932=CARTESIAN_POINT('Origin',(15.3358035470651,3.40523243981596E-15,
65.));
#81933=CARTESIAN_POINT('',(17.3358035470651,3.65016179964543E-15,65.));
#81934=CARTESIAN_POINT('Origin',(15.3358035470651,3.40523243981596E-15,
65.));
#81935=CARTESIAN_POINT('',(17.3358035470651,3.65016179964543E-15,60.));
#81936=CARTESIAN_POINT('',(17.3358035470651,3.16030307998649E-15,65.));
#81937=CARTESIAN_POINT('Origin',(15.3358035470651,3.40523243981596E-15,
60.));
#81938=CARTESIAN_POINT('Origin',(0.,0.,61.));
#81939=CARTESIAN_POINT('',(20.,-2.44929359829471E-15,61.));
#81940=CARTESIAN_POINT('',(-20.,-2.44929359829471E-15,61.));
#81941=CARTESIAN_POINT('Origin',(0.,0.,61.));
#81942=CARTESIAN_POINT('',(-19.,-2.32682891837997E-15,60.));
#81943=CARTESIAN_POINT('Origin',(-19.,-2.32682891837997E-15,61.));
#81944=CARTESIAN_POINT('Origin',(0.,0.,60.));
#81945=CARTESIAN_POINT('Origin',(0.,0.,61.));
#81946=CARTESIAN_POINT('Origin',(0.,0.,60.));
#81947=CARTESIAN_POINT('',(-20.,-2.44929359829471E-15,64.));
#81948=CARTESIAN_POINT('',(20.,2.44929359829471E-15,64.));
#81949=CARTESIAN_POINT('Origin',(0.,0.,64.));
#81950=CARTESIAN_POINT('Origin',(0.,0.,64.));
#81951=CARTESIAN_POINT('',(20.,2.44929359829471E-15,60.));
#81952=CARTESIAN_POINT('Origin',(0.,0.,60.));
#81953=CARTESIAN_POINT('Origin',(0.,0.,64.));
#81954=CARTESIAN_POINT('',(-19.,-2.32682891837997E-15,65.));
#81955=CARTESIAN_POINT('Origin',(0.,0.,65.));
#81956=CARTESIAN_POINT('Origin',(-19.,-2.32682891837997E-15,64.));
#81957=CARTESIAN_POINT('Origin',(0.,0.,65.));
#81958=CARTESIAN_POINT('Origin',(0.,0.,-60.));
#88465=UNCERTAINTY_MEASURE_WITH_UNIT(LENGTH_MEASURE(0.01),#88484,
'DISTANCE_ACCURACY_VALUE',
'Maximum model space distance between geometric entities at asserted c
onnectivities');
#88472=UNCERTAINTY_MEASURE_WITH_UNIT(LENGTH_MEASURE(0.01),#88484,
'DISTANCE_ACCURACY_VALUE',
'Maximum model space distance between geometric entities at asserted c
onnectivities');
#88476=(
GEOMETRIC_REPRESENTATION_CONTEXT(3)
GLOBAL_UNCERTAINTY_ASSIGNED_CONTEXT((#88465))
GLOBAL_UNIT_ASSIGNED_CONTEXT((#88484,#88486,#88487))
REPRESENTATION_CONTEXT('','3D')
);
#88483=(
GEOMETRIC_REPRESENTATION_CONTEXT(3)
GLOBAL_UNCERTAINTY_ASSIGNED_CONTEXT((#88472))
GLOBAL_UNIT_ASSIGNED_CONTEXT((#88484,#88486,#88487))
REPRESENTATION_CONTEXT('','3D')
);
#88484=(
LENGTH_UNIT()
NAMED_UNIT(*)
SI_UNIT(.MILLI.,.METRE.)
);
#88486=(
NAMED_UNIT(*)
PLANE_ANGLE_UNIT()
SI_UNIT($,.RADIAN.)
);
#88487=(
NAMED_UNIT(*)
SI_UNIT($,.STERADIAN.)
SOLID_ANGLE_UNIT()
);
#88491=SHAPE_DEFINITION_REPRESENTATION(#88501,#88522);
#88501=PRODUCT_DEFINITION_SHAPE('',$,#88533);
#88522=SHAPE_REPRESENTATION('',(#13735),#88476);
#88529=PRODUCT_DEFINITION_CONTEXT('part definition',#88561,'design');
#88533=PRODUCT_DEFINITION('Lifting_Screw','Lifting_Screw',#88543,#88529);
#88543=PRODUCT_DEFINITION_FORMATION('',$,#88566);
#88561=APPLICATION_CONTEXT(
'Core Data for Automotive Mechanical Design Process');
#88562=PRODUCT_CONTEXT('part definition',#88561,'mechanical');
#88566=PRODUCT('Lifting_Screw','Lifting_Screw',$,(#88562));
#88574=PRESENTATION_STYLE_ASSIGNMENT((#88576));
#88576=SURFACE_STYLE_USAGE(.BOTH.,#88578);
#88578=SURFACE_SIDE_STYLE('',(#88580));
#88580=SURFACE_STYLE_FILL_AREA(#88582);
#88582=FILL_AREA_STYLE('Opaque(160,160,160)',(#88584));
#88584=FILL_AREA_STYLE_COLOUR('Opaque(160,160,160)',#88586);
#88586=COLOUR_RGB('Opaque(160,160,160)', 0.66274510, 0.83137255, 0.94901961);
ENDSEC;
END-ISO-10303-21;
